ISO-10303-21;
HEADER;
/* Generated by software containing ST-Developer
 * from STEP Tools, Inc. (www.steptools.com) 
 */

FILE_DESCRIPTION(
/* description */ (''),
/* implementation_level */ '2;1');

FILE_NAME(
/* name */ 'Screw_01.step',
/* time_stamp */ '2026-10-04T16:49:01-07:00',
/* author */ (''),
/* organization */ (''),
/* preprocessor_version */ 'ST-DEVELOPER v20.2',
/* originating_system */ 'Autodesk Translation Framework v15.15.0.0',
/* authorisation */ '');

FILE_SCHEMA (('AUTOMOTIVE_DESIGN { 1 0 10303 214 3 1 1 }'));
ENDSEC;

DATA;
#10=MECHANICAL_DESIGN_GEOMETRIC_PRESENTATION_REPRESENTATION('',(#81),#51553);
#48=B_SPLINE_SURFACE_WITH_KNOTS('',3,3,((#17982,#17983,#17984,#17985,#17986,
#17987,#17988,#17989,#17990,#17991,#17992,#17993,#17994,#17995,#17996,#17997,
#17998,#17999,#18000,#18001,#18002,#18003,#18004,#18005,#18006,#18007,#18008,
#18009,#18010,#18011,#18012,#18013,#18014,#18015,#18016,#18017,#18018,#18019,
#18020,#18021,#18022,#18023,#18024,#18025,#18026,#18027,#18028,#18029,#18030,
#18031,#18032,#18033,#18034,#18035,#18036,#18037,#18038,#18039,#18040,#18041,
#18042,#18043,#18044,#18045,#18046,#18047,#18048,#18049,#18050,#18051,#18052,
#18053,#18054,#18055,#18056,#18057,#18058,#18059,#18060,#18061,#18062,#18063,
#18064,#18065,#18066,#18067,#18068,#18069,#18070,#18071,#18072,#18073,#18074,
#18075,#18076,#18077,#18078,#18079,#18080,#18081,#18082,#18083,#18084,#18085,
#18086,#18087,#18088,#18089,#18090,#18091,#18092,#18093,#18094,#18095,#18096,
#18097,#18098,#18099,#18100,#18101,#18102,#18103,#18104,#18105,#18106,#18107,
#18108,#18109,#18110,#18111,#18112),(#18113,#18114,#18115,#18116,#18117,
#18118,#18119,#18120,#18121,#18122,#18123,#18124,#18125,#18126,#18127,#18128,
#18129,#18130,#18131,#18132,#18133,#18134,#18135,#18136,#18137,#18138,#18139,
#18140,#18141,#18142,#18143,#18144,#18145,#18146,#18147,#18148,#18149,#18150,
#18151,#18152,#18153,#18154,#18155,#18156,#18157,#18158,#18159,#18160,#18161,
#18162,#18163,#18164,#18165,#18166,#18167,#18168,#18169,#18170,#18171,#18172,
#18173,#18174,#18175,#18176,#18177,#18178,#18179,#18180,#18181,#18182,#18183,
#18184,#18185,#18186,#18187,#18188,#18189,#18190,#18191,#18192,#18193,#18194,
#18195,#18196,#18197,#18198,#18199,#18200,#18201,#18202,#18203,#18204,#18205,
#18206,#18207,#18208,#18209,#18210,#18211,#18212,#18213,#18214,#18215,#18216,
#18217,#18218,#18219,#18220,#18221,#18222,#18223,#18224,#18225,#18226,#18227,
#18228,#18229,#18230,#18231,#18232,#18233,#18234,#18235,#18236,#18237,#18238,
#18239,#18240,#18241,#18242,#18243),(#18244,#18245,#18246,#18247,#18248,
#18249,#18250,#18251,#18252,#18253,#18254,#18255,#18256,#18257,#18258,#18259,
#18260,#18261,#18262,#18263,#18264,#18265,#18266,#18267,#18268,#18269,#18270,
#18271,#18272,#18273,#18274,#18275,#18276,#18277,#18278,#18279,#18280,#18281,
#18282,#18283,#18284,#18285,#18286,#18287,#18288,#18289,#18290,#18291,#18292,
#18293,#18294,#18295,#18296,#18297,#18298,#18299,#18300,#18301,#18302,#18303,
#18304,#18305,#18306,#18307,#18308,#18309,#18310,#18311,#18312,#18313,#18314,
#18315,#18316,#18317,#18318,#18319,#18320,#18321,#18322,#18323,#18324,#18325,
#18326,#18327,#18328,#18329,#18330,#18331,#18332,#18333,#18334,#18335,#18336,
#18337,#18338,#18339,#18340,#18341,#18342,#18343,#18344,#18345,#18346,#18347,
#18348,#18349,#18350,#18351,#18352,#18353,#18354,#18355,#18356,#18357,#18358,
#18359,#18360,#18361,#18362,#18363,#18364,#18365,#18366,#18367,#18368,#18369,
#18370,#18371,#18372,#18373,#18374),(#18375,#18376,#18377,#18378,#18379,
#18380,#18381,#18382,#18383,#18384,#18385,#18386,#18387,#18388,#18389,#18390,
#18391,#18392,#18393,#18394,#18395,#18396,#18397,#18398,#18399,#18400,#18401,
#18402,#18403,#18404,#18405,#18406,#18407,#18408,#18409,#18410,#18411,#18412,
#18413,#18414,#18415,#18416,#18417,#18418,#18419,#18420,#18421,#18422,#18423,
#18424,#18425,#18426,#18427,#18428,#18429,#18430,#18431,#18432,#18433,#18434,
#18435,#18436,#18437,#18438,#18439,#18440,#18441,#18442,#18443,#18444,#18445,
#18446,#18447,#18448,#18449,#18450,#18451,#18452,#18453,#18454,#18455,#18456,
#18457,#18458,#18459,#18460,#18461,#18462,#18463,#18464,#18465,#18466,#18467,
#18468,#18469,#18470,#18471,#18472,#18473,#18474,#18475,#18476,#18477,#18478,
#18479,#18480,#18481,#18482,#18483,#18484,#18485,#18486,#18487,#18488,#18489,
#18490,#18491,#18492,#18493,#18494,#18495,#18496,#18497,#18498,#18499,#18500,
#18501,#18502,#18503,#18504,#18505)),.UNSPECIFIED.,.F.,.F.,.F.,(4,4),(4,
1,1,1,1,1,1,1,1,1,1,1,1,1,1,1,1,1,1,1,1,1,1,1,1,1,1,1,1,1,1,1,1,1,1,1,1,
1,1,1,1,1,1,1,1,1,1,1,1,1,1,1,1,1,1,1,1,1,1,1,1,1,1,1,1,1,1,1,1,1,1,1,1,
1,1,1,1,1,1,1,1,1,1,1,1,1,1,1,1,1,1,1,1,1,1,1,1,1,1,1,1,1,1,1,1,1,1,1,1,
1,1,1,1,1,1,1,1,1,1,1,1,1,1,1,1,1,1,1,4),(-0.000314077148181808,0.0826777824702824),
(11.6145490510227,12.613065069482,13.6109159112094,14.6087667529368,15.6066175946642,
16.6044684363917,17.6023192781191,18.6001701198465,19.5980209615739,20.5958718033013,
21.5937226450287,22.5915734867561,23.5894243284835,24.5872751702109,25.5851260119383,
26.5829768536657,27.5808276953931,28.5786785371205,29.5765293788479,30.5743802205753,
31.5722310623027,32.5700819040301,33.5679327457575,34.5657835874849,35.5636344292123,
36.5614852709397,37.5593361126671,38.5571869543945,39.5550377961219,40.5528886378493,
41.5507394795767,42.5485903213041,43.5464411630315,44.5442920047589,45.5421428464863,
46.5399936882137,47.5378445299411,48.5356953716685,49.5335462133959,50.5313970551233,
51.5292478968507,52.5270987385781,53.5249495803055,54.522800422033,55.5206512637604,
56.5185021054878,57.5163529472152,58.5142037889426,59.51205463067,60.5099054723974,
61.5077563141248,62.5056071558522,63.5034579975796,64.501308839307,65.4991596810344,
66.4970105227618,67.4948613644892,68.4927122062166,69.490563047944,70.4884138896714,
71.4862647313988,72.4841155731262,73.4819664148536,74.479817256581,75.4776680983084,
76.4755189400358,77.4733697817632,78.4712206234906,79.469071465218,80.4669223069454,
81.4647731486728,82.4626239904002,83.4604748321276,84.458325673855,85.4561765155824,
86.4540273573098,87.4518781990372,88.4497290407646,89.4475798824921,90.4454307242194,
91.4432815659468,92.4411324076742,93.4389832494017,94.4368340911291,95.4346849328565,
96.4325357745839,97.4303866163113,98.4282374580387,99.4260882997661,100.423939141493,
101.421789983221,102.419640824948,103.417491666676,104.415342508403,105.41319335013,
106.411044191858,107.408895033585,108.406745875313,109.40459671704,110.402447558768,
111.400298400495,112.398149242222,113.39600008395,114.393850925677,115.391701767405,
116.389552609132,117.387403450859,118.385254292587,119.383105134314,120.380955976042,
121.378806817769,122.376657659496,123.374508501224,124.372359342951,125.370210184679,
126.368061026406,127.365911868133,128.363762709861,129.361613551588,130.359464393316,
131.357315235043,132.35516607677,133.353016918498,134.350867760225,135.348718601953,
136.34656944368,137.344420285407,138.342271127135,139.340121968862),
 .UNSPECIFIED.);
#49=B_SPLINE_SURFACE_WITH_KNOTS('',3,3,((#18820,#18821,#18822,#18823,#18824,
#18825,#18826,#18827,#18828,#18829,#18830,#18831,#18832,#18833,#18834,#18835,
#18836,#18837,#18838,#18839,#18840,#18841,#18842,#18843,#18844,#18845,#18846,
#18847,#18848,#18849,#18850,#18851,#18852,#18853,#18854,#18855,#18856,#18857,
#18858,#18859,#18860,#18861,#18862,#18863,#18864,#18865,#18866,#18867,#18868,
#18869,#18870,#18871,#18872,#18873,#18874,#18875,#18876,#18877,#18878,#18879,
#18880,#18881,#18882,#18883,#18884,#18885,#18886,#18887,#18888,#18889,#18890,
#18891,#18892,#18893,#18894,#18895,#18896,#18897,#18898,#18899,#18900,#18901,
#18902,#18903,#18904,#18905,#18906,#18907,#18908,#18909,#18910,#18911,#18912,
#18913,#18914,#18915,#18916,#18917,#18918,#18919,#18920,#18921,#18922,#18923,
#18924,#18925,#18926,#18927,#18928,#18929,#18930,#18931,#18932,#18933,#18934,
#18935,#18936,#18937,#18938,#18939,#18940,#18941,#18942,#18943,#18944,#18945,
#18946,#18947,#18948,#18949,#18950),(#18951,#18952,#18953,#18954,#18955,
#18956,#18957,#18958,#18959,#18960,#18961,#18962,#18963,#18964,#18965,#18966,
#18967,#18968,#18969,#18970,#18971,#18972,#18973,#18974,#18975,#18976,#18977,
#18978,#18979,#18980,#18981,#18982,#18983,#18984,#18985,#18986,#18987,#18988,
#18989,#18990,#18991,#18992,#18993,#18994,#18995,#18996,#18997,#18998,#18999,
#19000,#19001,#19002,#19003,#19004,#19005,#19006,#19007,#19008,#19009,#19010,
#19011,#19012,#19013,#19014,#19015,#19016,#19017,#19018,#19019,#19020,#19021,
#19022,#19023,#19024,#19025,#19026,#19027,#19028,#19029,#19030,#19031,#19032,
#19033,#19034,#19035,#19036,#19037,#19038,#19039,#19040,#19041,#19042,#19043,
#19044,#19045,#19046,#19047,#19048,#19049,#19050,#19051,#19052,#19053,#19054,
#19055,#19056,#19057,#19058,#19059,#19060,#19061,#19062,#19063,#19064,#19065,
#19066,#19067,#19068,#19069,#19070,#19071,#19072,#19073,#19074,#19075,#19076,
#19077,#19078,#19079,#19080,#19081),(#19082,#19083,#19084,#19085,#19086,
#19087,#19088,#19089,#19090,#19091,#19092,#19093,#19094,#19095,#19096,#19097,
#19098,#19099,#19100,#19101,#19102,#19103,#19104,#19105,#19106,#19107,#19108,
#19109,#19110,#19111,#19112,#19113,#19114,#19115,#19116,#19117,#19118,#19119,
#19120,#19121,#19122,#19123,#19124,#19125,#19126,#19127,#19128,#19129,#19130,
#19131,#19132,#19133,#19134,#19135,#19136,#19137,#19138,#19139,#19140,#19141,
#19142,#19143,#19144,#19145,#19146,#19147,#19148,#19149,#19150,#19151,#19152,
#19153,#19154,#19155,#19156,#19157,#19158,#19159,#19160,#19161,#19162,#19163,
#19164,#19165,#19166,#19167,#19168,#19169,#19170,#19171,#19172,#19173,#19174,
#19175,#19176,#19177,#19178,#19179,#19180,#19181,#19182,#19183,#19184,#19185,
#19186,#19187,#19188,#19189,#19190,#19191,#19192,#19193,#19194,#19195,#19196,
#19197,#19198,#19199,#19200,#19201,#19202,#19203,#19204,#19205,#19206,#19207,
#19208,#19209,#19210,#19211,#19212),(#19213,#19214,#19215,#19216,#19217,
#19218,#19219,#19220,#19221,#19222,#19223,#19224,#19225,#19226,#19227,#19228,
#19229,#19230,#19231,#19232,#19233,#19234,#19235,#19236,#19237,#19238,#19239,
#19240,#19241,#19242,#19243,#19244,#19245,#19246,#19247,#19248,#19249,#19250,
#19251,#19252,#19253,#19254,#19255,#19256,#19257,#19258,#19259,#19260,#19261,
#19262,#19263,#19264,#19265,#19266,#19267,#19268,#19269,#19270,#19271,#19272,
#19273,#19274,#19275,#19276,#19277,#19278,#19279,#19280,#19281,#19282,#19283,
#19284,#19285,#19286,#19287,#19288,#19289,#19290,#19291,#19292,#19293,#19294,
#19295,#19296,#19297,#19298,#19299,#19300,#19301,#19302,#19303,#19304,#19305,
#19306,#19307,#19308,#19309,#19310,#19311,#19312,#19313,#19314,#19315,#19316,
#19317,#19318,#19319,#19320,#19321,#19322,#19323,#19324,#19325,#19326,#19327,
#19328,#19329,#19330,#19331,#19332,#19333,#19334,#19335,#19336,#19337,#19338,
#19339,#19340,#19341,#19342,#19343)),.UNSPECIFIED.,.F.,.F.,.F.,(4,4),(4,
1,1,1,1,1,1,1,1,1,1,1,1,1,1,1,1,1,1,1,1,1,1,1,1,1,1,1,1,1,1,1,1,1,1,1,1,
1,1,1,1,1,1,1,1,1,1,1,1,1,1,1,1,1,1,1,1,1,1,1,1,1,1,1,1,1,1,1,1,1,1,1,1,
1,1,1,1,1,1,1,1,1,1,1,1,1,1,1,1,1,1,1,1,1,1,1,1,1,1,1,1,1,1,1,1,1,1,1,1,
1,1,1,1,1,1,1,1,1,1,1,1,1,1,1,1,1,1,1,4),(-0.000314077148181808,0.0826777824702824),
(11.6145490510227,12.613065069482,13.6109159112094,14.6087667529368,15.6066175946642,
16.6044684363917,17.6023192781191,18.6001701198465,19.5980209615739,20.5958718033013,
21.5937226450287,22.5915734867561,23.5894243284835,24.5872751702109,25.5851260119383,
26.5829768536657,27.5808276953931,28.5786785371205,29.5765293788479,30.5743802205753,
31.5722310623027,32.5700819040301,33.5679327457575,34.5657835874849,35.5636344292123,
36.5614852709397,37.5593361126671,38.5571869543945,39.5550377961219,40.5528886378493,
41.5507394795767,42.5485903213041,43.5464411630315,44.5442920047589,45.5421428464863,
46.5399936882137,47.5378445299411,48.5356953716685,49.5335462133959,50.5313970551233,
51.5292478968507,52.5270987385781,53.5249495803055,54.522800422033,55.5206512637604,
56.5185021054878,57.5163529472152,58.5142037889426,59.51205463067,60.5099054723974,
61.5077563141248,62.5056071558522,63.5034579975796,64.501308839307,65.4991596810344,
66.4970105227618,67.4948613644892,68.4927122062166,69.490563047944,70.4884138896714,
71.4862647313988,72.4841155731262,73.4819664148536,74.479817256581,75.4776680983084,
76.4755189400358,77.4733697817632,78.4712206234906,79.469071465218,80.4669223069454,
81.4647731486728,82.4626239904002,83.4604748321276,84.458325673855,85.4561765155824,
86.4540273573098,87.4518781990372,88.4497290407646,89.4475798824921,90.4454307242194,
91.4432815659468,92.4411324076742,93.4389832494017,94.4368340911291,95.4346849328565,
96.4325357745839,97.4303866163113,98.4282374580387,99.4260882997661,100.423939141493,
101.421789983221,102.419640824948,103.417491666676,104.415342508403,105.41319335013,
106.411044191858,107.408895033585,108.406745875313,109.40459671704,110.402447558768,
111.400298400495,112.398149242222,113.39600008395,114.393850925677,115.391701767405,
116.389552609132,117.387403450859,118.385254292587,119.383105134314,120.380955976042,
121.378806817769,122.376657659496,123.374508501224,124.372359342951,125.370210184679,
126.368061026406,127.365911868133,128.363762709861,129.361613551588,130.359464393316,
131.357315235043,132.35516607677,133.353016918498,134.350867760225,135.348718601953,
136.34656944368,137.344420285407,138.342271127135,139.340121968862),
 .UNSPECIFIED.);
#50=B_SPLINE_SURFACE_WITH_KNOTS('',3,3,((#19498,#19499,#19500,#19501,#19502,
#19503,#19504,#19505,#19506,#19507,#19508,#19509,#19510,#19511,#19512,#19513,
#19514,#19515,#19516,#19517,#19518,#19519,#19520,#19521,#19522,#19523,#19524,
#19525,#19526,#19527,#19528,#19529,#19530,#19531,#19532,#19533,#19534,#19535,
#19536,#19537,#19538,#19539,#19540,#19541,#19542,#19543,#19544,#19545,#19546,
#19547,#19548,#19549,#19550,#19551,#19552,#19553,#19554,#19555,#19556,#19557,
#19558,#19559,#19560,#19561,#19562,#19563,#19564,#19565,#19566,#19567,#19568,
#19569,#19570,#19571,#19572,#19573,#19574,#19575,#19576,#19577,#19578,#19579,
#19580,#19581,#19582,#19583,#19584,#19585,#19586,#19587,#19588,#19589,#19590,
#19591,#19592,#19593,#19594,#19595,#19596,#19597,#19598,#19599,#19600,#19601,
#19602,#19603,#19604,#19605,#19606,#19607,#19608,#19609,#19610,#19611,#19612,
#19613,#19614,#19615,#19616,#19617,#19618,#19619,#19620,#19621,#19622,#19623,
#19624,#19625,#19626,#19627,#19628),(#19629,#19630,#19631,#19632,#19633,
#19634,#19635,#19636,#19637,#19638,#19639,#19640,#19641,#19642,#19643,#19644,
#19645,#19646,#19647,#19648,#19649,#19650,#19651,#19652,#19653,#19654,#19655,
#19656,#19657,#19658,#19659,#19660,#19661,#19662,#19663,#19664,#19665,#19666,
#19667,#19668,#19669,#19670,#19671,#19672,#19673,#19674,#19675,#19676,#19677,
#19678,#19679,#19680,#19681,#19682,#19683,#19684,#19685,#19686,#19687,#19688,
#19689,#19690,#19691,#19692,#19693,#19694,#19695,#19696,#19697,#19698,#19699,
#19700,#19701,#19702,#19703,#19704,#19705,#19706,#19707,#19708,#19709,#19710,
#19711,#19712,#19713,#19714,#19715,#19716,#19717,#19718,#19719,#19720,#19721,
#19722,#19723,#19724,#19725,#19726,#19727,#19728,#19729,#19730,#19731,#19732,
#19733,#19734,#19735,#19736,#19737,#19738,#19739,#19740,#19741,#19742,#19743,
#19744,#19745,#19746,#19747,#19748,#19749,#19750,#19751,#19752,#19753,#19754,
#19755,#19756,#19757,#19758,#19759),(#19760,#19761,#19762,#19763,#19764,
#19765,#19766,#19767,#19768,#19769,#19770,#19771,#19772,#19773,#19774,#19775,
#19776,#19777,#19778,#19779,#19780,#19781,#19782,#19783,#19784,#19785,#19786,
#19787,#19788,#19789,#19790,#19791,#19792,#19793,#19794,#19795,#19796,#19797,
#19798,#19799,#19800,#19801,#19802,#19803,#19804,#19805,#19806,#19807,#19808,
#19809,#19810,#19811,#19812,#19813,#19814,#19815,#19816,#19817,#19818,#19819,
#19820,#19821,#19822,#19823,#19824,#19825,#19826,#19827,#19828,#19829,#19830,
#19831,#19832,#19833,#19834,#19835,#19836,#19837,#19838,#19839,#19840,#19841,
#19842,#19843,#19844,#19845,#19846,#19847,#19848,#19849,#19850,#19851,#19852,
#19853,#19854,#19855,#19856,#19857,#19858,#19859,#19860,#19861,#19862,#19863,
#19864,#19865,#19866,#19867,#19868,#19869,#19870,#19871,#19872,#19873,#19874,
#19875,#19876,#19877,#19878,#19879,#19880,#19881,#19882,#19883,#19884,#19885,
#19886,#19887,#19888,#19889,#19890),(#19891,#19892,#19893,#19894,#19895,
#19896,#19897,#19898,#19899,#19900,#19901,#19902,#19903,#19904,#19905,#19906,
#19907,#19908,#19909,#19910,#19911,#19912,#19913,#19914,#19915,#19916,#19917,
#19918,#19919,#19920,#19921,#19922,#19923,#19924,#19925,#19926,#19927,#19928,
#19929,#19930,#19931,#19932,#19933,#19934,#19935,#19936,#19937,#19938,#19939,
#19940,#19941,#19942,#19943,#19944,#19945,#19946,#19947,#19948,#19949,#19950,
#19951,#19952,#19953,#19954,#19955,#19956,#19957,#19958,#19959,#19960,#19961,
#19962,#19963,#19964,#19965,#19966,#19967,#19968,#19969,#19970,#19971,#19972,
#19973,#19974,#19975,#19976,#19977,#19978,#19979,#19980,#19981,#19982,#19983,
#19984,#19985,#19986,#19987,#19988,#19989,#19990,#19991,#19992,#19993,#19994,
#19995,#19996,#19997,#19998,#19999,#20000,#20001,#20002,#20003,#20004,#20005,
#20006,#20007,#20008,#20009,#20010,#20011,#20012,#20013,#20014,#20015,#20016,
#20017,#20018,#20019,#20020,#20021)),.UNSPECIFIED.,.F.,.F.,.F.,(4,4),(4,
1,1,1,1,1,1,1,1,1,1,1,1,1,1,1,1,1,1,1,1,1,1,1,1,1,1,1,1,1,1,1,1,1,1,1,1,
1,1,1,1,1,1,1,1,1,1,1,1,1,1,1,1,1,1,1,1,1,1,1,1,1,1,1,1,1,1,1,1,1,1,1,1,
1,1,1,1,1,1,1,1,1,1,1,1,1,1,1,1,1,1,1,1,1,1,1,1,1,1,1,1,1,1,1,1,1,1,1,1,
1,1,1,1,1,1,1,1,1,1,1,1,1,1,1,1,1,1,1,4),(-0.000314077148181808,0.0826777824702824),
(11.6145490510227,12.613065069482,13.6109159112094,14.6087667529368,15.6066175946642,
16.6044684363917,17.6023192781191,18.6001701198465,19.5980209615739,20.5958718033013,
21.5937226450287,22.5915734867561,23.5894243284835,24.5872751702109,25.5851260119383,
26.5829768536657,27.5808276953931,28.5786785371205,29.5765293788479,30.5743802205753,
31.5722310623027,32.5700819040301,33.5679327457575,34.5657835874849,35.5636344292123,
36.5614852709397,37.5593361126671,38.5571869543945,39.5550377961219,40.5528886378493,
41.5507394795767,42.5485903213041,43.5464411630315,44.5442920047589,45.5421428464863,
46.5399936882137,47.5378445299411,48.5356953716685,49.5335462133959,50.5313970551233,
51.5292478968507,52.5270987385781,53.5249495803055,54.522800422033,55.5206512637604,
56.5185021054878,57.5163529472152,58.5142037889426,59.51205463067,60.5099054723974,
61.5077563141248,62.5056071558522,63.5034579975796,64.501308839307,65.4991596810344,
66.4970105227618,67.4948613644892,68.4927122062166,69.490563047944,70.4884138896714,
71.4862647313988,72.4841155731262,73.4819664148536,74.479817256581,75.4776680983084,
76.4755189400358,77.4733697817632,78.4712206234906,79.469071465218,80.4669223069454,
81.4647731486728,82.4626239904002,83.4604748321276,84.458325673855,85.4561765155824,
86.4540273573098,87.4518781990372,88.4497290407646,89.4475798824921,90.4454307242194,
91.4432815659468,92.4411324076742,93.4389832494017,94.4368340911291,95.4346849328565,
96.4325357745839,97.4303866163113,98.4282374580387,99.4260882997661,100.423939141493,
101.421789983221,102.419640824948,103.417491666676,104.415342508403,105.41319335013,
106.411044191858,107.408895033585,108.406745875313,109.40459671704,110.402447558768,
111.400298400495,112.398149242222,113.39600008395,114.393850925677,115.391701767405,
116.389552609132,117.387403450859,118.385254292587,119.383105134314,120.380955976042,
121.378806817769,122.376657659496,123.374508501224,124.372359342951,125.370210184679,
126.368061026406,127.365911868133,128.363762709861,129.361613551588,130.359464393316,
131.357315235043,132.35516607677,133.353016918498,134.350867760225,135.348718601953,
136.34656944368,137.344420285407,138.342271127135,139.340121968862),
 .UNSPECIFIED.);
#51=B_SPLINE_SURFACE_WITH_KNOTS('',3,3,((#20214,#20215,#20216,#20217,#20218,
#20219,#20220,#20221,#20222,#20223,#20224,#20225,#20226,#20227,#20228,#20229,
#20230,#20231,#20232,#20233,#20234,#20235,#20236,#20237,#20238,#20239,#20240,
#20241,#20242,#20243,#20244,#20245,#20246,#20247,#20248,#20249,#20250,#20251,
#20252,#20253,#20254,#20255,#20256,#20257,#20258,#20259,#20260,#20261,#20262,
#20263,#20264,#20265,#20266,#20267,#20268,#20269,#20270,#20271,#20272,#20273,
#20274,#20275,#20276,#20277,#20278,#20279,#20280,#20281,#20282,#20283,#20284,
#20285,#20286,#20287,#20288,#20289,#20290,#20291,#20292,#20293,#20294,#20295,
#20296,#20297,#20298,#20299,#20300,#20301,#20302,#20303,#20304,#20305,#20306,
#20307,#20308,#20309,#20310,#20311,#20312,#20313,#20314,#20315,#20316,#20317,
#20318,#20319,#20320,#20321,#20322,#20323,#20324,#20325,#20326,#20327,#20328,
#20329,#20330,#20331,#20332,#20333,#20334,#20335,#20336,#20337,#20338,#20339,
#20340,#20341,#20342,#20343,#20344),(#20345,#20346,#20347,#20348,#20349,
#20350,#20351,#20352,#20353,#20354,#20355,#20356,#20357,#20358,#20359,#20360,
#20361,#20362,#20363,#20364,#20365,#20366,#20367,#20368,#20369,#20370,#20371,
#20372,#20373,#20374,#20375,#20376,#20377,#20378,#20379,#20380,#20381,#20382,
#20383,#20384,#20385,#20386,#20387,#20388,#20389,#20390,#20391,#20392,#20393,
#20394,#20395,#20396,#20397,#20398,#20399,#20400,#20401,#20402,#20403,#20404,
#20405,#20406,#20407,#20408,#20409,#20410,#20411,#20412,#20413,#20414,#20415,
#20416,#20417,#20418,#20419,#20420,#20421,#20422,#20423,#20424,#20425,#20426,
#20427,#20428,#20429,#20430,#20431,#20432,#20433,#20434,#20435,#20436,#20437,
#20438,#20439,#20440,#20441,#20442,#20443,#20444,#20445,#20446,#20447,#20448,
#20449,#20450,#20451,#20452,#20453,#20454,#20455,#20456,#20457,#20458,#20459,
#20460,#20461,#20462,#20463,#20464,#20465,#20466,#20467,#20468,#20469,#20470,
#20471,#20472,#20473,#20474,#20475),(#20476,#20477,#20478,#20479,#20480,
#20481,#20482,#20483,#20484,#20485,#20486,#20487,#20488,#20489,#20490,#20491,
#20492,#20493,#20494,#20495,#20496,#20497,#20498,#20499,#20500,#20501,#20502,
#20503,#20504,#20505,#20506,#20507,#20508,#20509,#20510,#20511,#20512,#20513,
#20514,#20515,#20516,#20517,#20518,#20519,#20520,#20521,#20522,#20523,#20524,
#20525,#20526,#20527,#20528,#20529,#20530,#20531,#20532,#20533,#20534,#20535,
#20536,#20537,#20538,#20539,#20540,#20541,#20542,#20543,#20544,#20545,#20546,
#20547,#20548,#20549,#20550,#20551,#20552,#20553,#20554,#20555,#20556,#20557,
#20558,#20559,#20560,#20561,#20562,#20563,#20564,#20565,#20566,#20567,#20568,
#20569,#20570,#20571,#20572,#20573,#20574,#20575,#20576,#20577,#20578,#20579,
#20580,#20581,#20582,#20583,#20584,#20585,#20586,#20587,#20588,#20589,#20590,
#20591,#20592,#20593,#20594,#20595,#20596,#20597,#20598,#20599,#20600,#20601,
#20602,#20603,#20604,#20605,#20606),(#20607,#20608,#20609,#20610,#20611,
#20612,#20613,#20614,#20615,#20616,#20617,#20618,#20619,#20620,#20621,#20622,
#20623,#20624,#20625,#20626,#20627,#20628,#20629,#20630,#20631,#20632,#20633,
#20634,#20635,#20636,#20637,#20638,#20639,#20640,#20641,#20642,#20643,#20644,
#20645,#20646,#20647,#20648,#20649,#20650,#20651,#20652,#20653,#20654,#20655,
#20656,#20657,#20658,#20659,#20660,#20661,#20662,#20663,#20664,#20665,#20666,
#20667,#20668,#20669,#20670,#20671,#20672,#20673,#20674,#20675,#20676,#20677,
#20678,#20679,#20680,#20681,#20682,#20683,#20684,#20685,#20686,#20687,#20688,
#20689,#20690,#20691,#20692,#20693,#20694,#20695,#20696,#20697,#20698,#20699,
#20700,#20701,#20702,#20703,#20704,#20705,#20706,#20707,#20708,#20709,#20710,
#20711,#20712,#20713,#20714,#20715,#20716,#20717,#20718,#20719,#20720,#20721,
#20722,#20723,#20724,#20725,#20726,#20727,#20728,#20729,#20730,#20731,#20732,
#20733,#20734,#20735,#20736,#20737)),.UNSPECIFIED.,.F.,.F.,.F.,(4,4),(4,
1,1,1,1,1,1,1,1,1,1,1,1,1,1,1,1,1,1,1,1,1,1,1,1,1,1,1,1,1,1,1,1,1,1,1,1,
1,1,1,1,1,1,1,1,1,1,1,1,1,1,1,1,1,1,1,1,1,1,1,1,1,1,1,1,1,1,1,1,1,1,1,1,
1,1,1,1,1,1,1,1,1,1,1,1,1,1,1,1,1,1,1,1,1,1,1,1,1,1,1,1,1,1,1,1,1,1,1,1,
1,1,1,1,1,1,1,1,1,1,1,1,1,1,1,1,1,1,1,4),(-0.000314077148181808,0.0826777824702824),
(11.6145490510227,12.613065069482,13.6109159112094,14.6087667529368,15.6066175946642,
16.6044684363917,17.6023192781191,18.6001701198465,19.5980209615739,20.5958718033013,
21.5937226450287,22.5915734867561,23.5894243284835,24.5872751702109,25.5851260119383,
26.5829768536657,27.5808276953931,28.5786785371205,29.5765293788479,30.5743802205753,
31.5722310623027,32.5700819040301,33.5679327457575,34.5657835874849,35.5636344292123,
36.5614852709397,37.5593361126671,38.5571869543945,39.5550377961219,40.5528886378493,
41.5507394795767,42.5485903213041,43.5464411630315,44.5442920047589,45.5421428464863,
46.5399936882137,47.5378445299411,48.5356953716685,49.5335462133959,50.5313970551233,
51.5292478968507,52.5270987385781,53.5249495803055,54.522800422033,55.5206512637604,
56.5185021054878,57.5163529472152,58.5142037889426,59.51205463067,60.5099054723974,
61.5077563141248,62.5056071558522,63.5034579975796,64.501308839307,65.4991596810344,
66.4970105227618,67.4948613644892,68.4927122062166,69.490563047944,70.4884138896714,
71.4862647313988,72.4841155731262,73.4819664148536,74.479817256581,75.4776680983084,
76.4755189400358,77.4733697817632,78.4712206234906,79.469071465218,80.4669223069454,
81.4647731486728,82.4626239904002,83.4604748321276,84.458325673855,85.4561765155824,
86.4540273573098,87.4518781990372,88.4497290407646,89.4475798824921,90.4454307242194,
91.4432815659468,92.4411324076742,93.4389832494017,94.4368340911291,95.4346849328565,
96.4325357745839,97.4303866163113,98.4282374580387,99.4260882997661,100.423939141493,
101.421789983221,102.419640824948,103.417491666676,104.415342508403,105.41319335013,
106.411044191858,107.408895033585,108.406745875313,109.40459671704,110.402447558768,
111.400298400495,112.398149242222,113.39600008395,114.393850925677,115.391701767405,
116.389552609132,117.387403450859,118.385254292587,119.383105134314,120.380955976042,
121.378806817769,122.376657659496,123.374508501224,124.372359342951,125.370210184679,
126.368061026406,127.365911868133,128.363762709861,129.361613551588,130.359464393316,
131.357315235043,132.35516607677,133.353016918498,134.350867760225,135.348718601953,
136.34656944368,137.344420285407,138.342271127135,139.340121968862),
 .UNSPECIFIED.);
#52=B_SPLINE_SURFACE_WITH_KNOTS('',3,3,((#21566,#21567,#21568,#21569,#21570,
#21571,#21572,#21573,#21574,#21575,#21576,#21577,#21578,#21579,#21580,#21581,
#21582,#21583,#21584,#21585,#21586,#21587,#21588,#21589,#21590,#21591,#21592,
#21593,#21594,#21595,#21596,#21597,#21598,#21599,#21600,#21601,#21602,#21603,
#21604,#21605,#21606,#21607,#21608,#21609,#21610,#21611,#21612,#21613,#21614,
#21615,#21616,#21617,#21618,#21619,#21620,#21621,#21622,#21623,#21624,#21625,
#21626,#21627,#21628,#21629,#21630,#21631,#21632,#21633,#21634,#21635,#21636,
#21637,#21638,#21639,#21640,#21641,#21642,#21643,#21644,#21645,#21646,#21647,
#21648,#21649,#21650,#21651,#21652,#21653,#21654,#21655,#21656,#21657,#21658,
#21659,#21660,#21661,#21662,#21663,#21664,#21665,#21666,#21667,#21668,#21669,
#21670,#21671,#21672,#21673,#21674,#21675,#21676,#21677,#21678,#21679,#21680,
#21681,#21682,#21683,#21684,#21685,#21686,#21687,#21688,#21689,#21690,#21691,
#21692,#21693,#21694,#21695,#21696),(#21697,#21698,#21699,#21700,#21701,
#21702,#21703,#21704,#21705,#21706,#21707,#21708,#21709,#21710,#21711,#21712,
#21713,#21714,#21715,#21716,#21717,#21718,#21719,#21720,#21721,#21722,#21723,
#21724,#21725,#21726,#21727,#21728,#21729,#21730,#21731,#21732,#21733,#21734,
#21735,#21736,#21737,#21738,#21739,#21740,#21741,#21742,#21743,#21744,#21745,
#21746,#21747,#21748,#21749,#21750,#21751,#21752,#21753,#21754,#21755,#21756,
#21757,#21758,#21759,#21760,#21761,#21762,#21763,#21764,#21765,#21766,#21767,
#21768,#21769,#21770,#21771,#21772,#21773,#21774,#21775,#21776,#21777,#21778,
#21779,#21780,#21781,#21782,#21783,#21784,#21785,#21786,#21787,#21788,#21789,
#21790,#21791,#21792,#21793,#21794,#21795,#21796,#21797,#21798,#21799,#21800,
#21801,#21802,#21803,#21804,#21805,#21806,#21807,#21808,#21809,#21810,#21811,
#21812,#21813,#21814,#21815,#21816,#21817,#21818,#21819,#21820,#21821,#21822,
#21823,#21824,#21825,#21826,#21827),(#21828,#21829,#21830,#21831,#21832,
#21833,#21834,#21835,#21836,#21837,#21838,#21839,#21840,#21841,#21842,#21843,
#21844,#21845,#21846,#21847,#21848,#21849,#21850,#21851,#21852,#21853,#21854,
#21855,#21856,#21857,#21858,#21859,#21860,#21861,#21862,#21863,#21864,#21865,
#21866,#21867,#21868,#21869,#21870,#21871,#21872,#21873,#21874,#21875,#21876,
#21877,#21878,#21879,#21880,#21881,#21882,#21883,#21884,#21885,#21886,#21887,
#21888,#21889,#21890,#21891,#21892,#21893,#21894,#21895,#21896,#21897,#21898,
#21899,#21900,#21901,#21902,#21903,#21904,#21905,#21906,#21907,#21908,#21909,
#21910,#21911,#21912,#21913,#21914,#21915,#21916,#21917,#21918,#21919,#21920,
#21921,#21922,#21923,#21924,#21925,#21926,#21927,#21928,#21929,#21930,#21931,
#21932,#21933,#21934,#21935,#21936,#21937,#21938,#21939,#21940,#21941,#21942,
#21943,#21944,#21945,#21946,#21947,#21948,#21949,#21950,#21951,#21952,#21953,
#21954,#21955,#21956,#21957,#21958),(#21959,#21960,#21961,#21962,#21963,
#21964,#21965,#21966,#21967,#21968,#21969,#21970,#21971,#21972,#21973,#21974,
#21975,#21976,#21977,#21978,#21979,#21980,#21981,#21982,#21983,#21984,#21985,
#21986,#21987,#21988,#21989,#21990,#21991,#21992,#21993,#21994,#21995,#21996,
#21997,#21998,#21999,#22000,#22001,#22002,#22003,#22004,#22005,#22006,#22007,
#22008,#22009,#22010,#22011,#22012,#22013,#22014,#22015,#22016,#22017,#22018,
#22019,#22020,#22021,#22022,#22023,#22024,#22025,#22026,#22027,#22028,#22029,
#22030,#22031,#22032,#22033,#22034,#22035,#22036,#22037,#22038,#22039,#22040,
#22041,#22042,#22043,#22044,#22045,#22046,#22047,#22048,#22049,#22050,#22051,
#22052,#22053,#22054,#22055,#22056,#22057,#22058,#22059,#22060,#22061,#22062,
#22063,#22064,#22065,#22066,#22067,#22068,#22069,#22070,#22071,#22072,#22073,
#22074,#22075,#22076,#22077,#22078,#22079,#22080,#22081,#22082,#22083,#22084,
#22085,#22086,#22087,#22088,#22089)),.UNSPECIFIED.,.F.,.F.,.F.,(4,4),(4,
1,1,1,1,1,1,1,1,1,1,1,1,1,1,1,1,1,1,1,1,1,1,1,1,1,1,1,1,1,1,1,1,1,1,1,1,
1,1,1,1,1,1,1,1,1,1,1,1,1,1,1,1,1,1,1,1,1,1,1,1,1,1,1,1,1,1,1,1,1,1,1,1,
1,1,1,1,1,1,1,1,1,1,1,1,1,1,1,1,1,1,1,1,1,1,1,1,1,1,1,1,1,1,1,1,1,1,1,1,
1,1,1,1,1,1,1,1,1,1,1,1,1,1,1,1,1,1,1,4),(-0.000646252380093648,0.082354798859151),
(8.31473274985794,9.31258359158534,10.3104344333127,11.3082852750401,12.3061361167675,
13.3039869584949,14.3018378002224,15.2996886419498,16.2975394836772,17.2953903254046,
18.293241167132,19.2910920088594,20.2889428505868,21.2867936923142,22.2846445340416,
23.282495375769,24.2803462174964,25.2781970592238,26.2760479009512,27.2738987426786,
28.271749584406,29.2696004261334,30.2674512678608,31.2653021095882,32.2631529513156,
33.261003793043,34.2588546347704,35.2567054764978,36.2545563182252,37.2524071599526,
38.25025800168,39.2481088434074,40.2459596851348,41.2438105268622,42.2416613685896,
43.239512210317,44.2373630520444,45.2352138937718,46.2330647354992,47.2309155772266,
48.228766418954,49.2266172606814,50.2244681024088,51.2223189441362,52.2201697858636,
53.218020627591,54.2158714693185,55.2137223110459,56.2115731527733,57.2094239945007,
58.2072748362281,59.2051256779555,60.2029765196829,61.2008273614103,62.1986782031377,
63.1965290448651,64.1943798865925,65.1922307283199,66.1900815700473,67.1879324117747,
68.1857832535021,69.1836340952295,70.1814849369569,71.1793357786843,72.1771866204117,
73.1750374621391,74.1728883038665,75.1707391455939,76.1685899873213,77.1664408290487,
78.1642916707761,79.1621425125035,80.1599933542309,81.1578441959583,82.1556950376857,
83.1535458794131,84.1513967211405,85.1492475628679,86.1470984045953,87.1449492463227,
88.1428000880501,89.1406509297776,90.1385017715049,91.1363526132323,92.1342034549598,
93.1320542966872,94.1299051384146,95.127755980142,96.1256068218694,97.1234576635968,
98.1213085053242,99.1191593470516,100.117010188779,101.114861030506,102.112711872234,
103.110562713961,104.108413555689,105.106264397416,106.104115239143,107.101966080871,
108.099816922598,109.097667764326,110.095518606053,111.09336944778,112.091220289508,
113.089071131235,114.086921972963,115.08477281469,116.082623656417,117.080474498145,
118.078325339872,119.0761761816,120.074027023327,121.071877865054,122.069728706782,
123.067579548509,124.065430390237,125.063281231964,126.061132073691,127.058982915419,
128.056833757146,129.054684598874,130.052535440601,131.050386282328,132.048237124056,
133.046087965783,134.043938807511,135.041789649238,136.040286743345),
 .UNSPECIFIED.);
#53=B_SPLINE_SURFACE_WITH_KNOTS('',3,3,((#22184,#22185,#22186,#22187,#22188,
#22189,#22190,#22191,#22192,#22193,#22194,#22195,#22196,#22197,#22198,#22199,
#22200,#22201,#22202,#22203,#22204,#22205,#22206,#22207,#22208,#22209,#22210,
#22211,#22212,#22213,#22214,#22215,#22216,#22217,#22218,#22219,#22220,#22221,
#22222,#22223,#22224,#22225,#22226,#22227,#22228,#22229,#22230,#22231,#22232,
#22233,#22234,#22235,#22236,#22237,#22238,#22239,#22240,#22241,#22242,#22243,
#22244,#22245,#22246,#22247,#22248,#22249,#22250,#22251,#22252,#22253,#22254,
#22255,#22256,#22257,#22258,#22259,#22260,#22261,#22262,#22263,#22264,#22265,
#22266,#22267,#22268,#22269,#22270,#22271,#22272,#22273,#22274,#22275,#22276,
#22277,#22278,#22279,#22280,#22281,#22282,#22283,#22284,#22285,#22286,#22287,
#22288,#22289,#22290,#22291,#22292,#22293,#22294,#22295,#22296,#22297,#22298,
#22299,#22300,#22301,#22302,#22303,#22304,#22305,#22306,#22307,#22308,#22309,
#22310,#22311,#22312,#22313,#22314),(#22315,#22316,#22317,#22318,#22319,
#22320,#22321,#22322,#22323,#22324,#22325,#22326,#22327,#22328,#22329,#22330,
#22331,#22332,#22333,#22334,#22335,#22336,#22337,#22338,#22339,#22340,#22341,
#22342,#22343,#22344,#22345,#22346,#22347,#22348,#22349,#22350,#22351,#22352,
#22353,#22354,#22355,#22356,#22357,#22358,#22359,#22360,#22361,#22362,#22363,
#22364,#22365,#22366,#22367,#22368,#22369,#22370,#22371,#22372,#22373,#22374,
#22375,#22376,#22377,#22378,#22379,#22380,#22381,#22382,#22383,#22384,#22385,
#22386,#22387,#22388,#22389,#22390,#22391,#22392,#22393,#22394,#22395,#22396,
#22397,#22398,#22399,#22400,#22401,#22402,#22403,#22404,#22405,#22406,#22407,
#22408,#22409,#22410,#22411,#22412,#22413,#22414,#22415,#22416,#22417,#22418,
#22419,#22420,#22421,#22422,#22423,#22424,#22425,#22426,#22427,#22428,#22429,
#22430,#22431,#22432,#22433,#22434,#22435,#22436,#22437,#22438,#22439,#22440,
#22441,#22442,#22443,#22444,#22445),(#22446,#22447,#22448,#22449,#22450,
#22451,#22452,#22453,#22454,#22455,#22456,#22457,#22458,#22459,#22460,#22461,
#22462,#22463,#22464,#22465,#22466,#22467,#22468,#22469,#22470,#22471,#22472,
#22473,#22474,#22475,#22476,#22477,#22478,#22479,#22480,#22481,#22482,#22483,
#22484,#22485,#22486,#22487,#22488,#22489,#22490,#22491,#22492,#22493,#22494,
#22495,#22496,#22497,#22498,#22499,#22500,#22501,#22502,#22503,#22504,#22505,
#22506,#22507,#22508,#22509,#22510,#22511,#22512,#22513,#22514,#22515,#22516,
#22517,#22518,#22519,#22520,#22521,#22522,#22523,#22524,#22525,#22526,#22527,
#22528,#22529,#22530,#22531,#22532,#22533,#22534,#22535,#22536,#22537,#22538,
#22539,#22540,#22541,#22542,#22543,#22544,#22545,#22546,#22547,#22548,#22549,
#22550,#22551,#22552,#22553,#22554,#22555,#22556,#22557,#22558,#22559,#22560,
#22561,#22562,#22563,#22564,#22565,#22566,#22567,#22568,#22569,#22570,#22571,
#22572,#22573,#22574,#22575,#22576),(#22577,#22578,#22579,#22580,#22581,
#22582,#22583,#22584,#22585,#22586,#22587,#22588,#22589,#22590,#22591,#22592,
#22593,#22594,#22595,#22596,#22597,#22598,#22599,#22600,#22601,#22602,#22603,
#22604,#22605,#22606,#22607,#22608,#22609,#22610,#22611,#22612,#22613,#22614,
#22615,#22616,#22617,#22618,#22619,#22620,#22621,#22622,#22623,#22624,#22625,
#22626,#22627,#22628,#22629,#22630,#22631,#22632,#22633,#22634,#22635,#22636,
#22637,#22638,#22639,#22640,#22641,#22642,#22643,#22644,#22645,#22646,#22647,
#22648,#22649,#22650,#22651,#22652,#22653,#22654,#22655,#22656,#22657,#22658,
#22659,#22660,#22661,#22662,#22663,#22664,#22665,#22666,#22667,#22668,#22669,
#22670,#22671,#22672,#22673,#22674,#22675,#22676,#22677,#22678,#22679,#22680,
#22681,#22682,#22683,#22684,#22685,#22686,#22687,#22688,#22689,#22690,#22691,
#22692,#22693,#22694,#22695,#22696,#22697,#22698,#22699,#22700,#22701,#22702,
#22703,#22704,#22705,#22706,#22707)),.UNSPECIFIED.,.F.,.F.,.F.,(4,4),(4,
1,1,1,1,1,1,1,1,1,1,1,1,1,1,1,1,1,1,1,1,1,1,1,1,1,1,1,1,1,1,1,1,1,1,1,1,
1,1,1,1,1,1,1,1,1,1,1,1,1,1,1,1,1,1,1,1,1,1,1,1,1,1,1,1,1,1,1,1,1,1,1,1,
1,1,1,1,1,1,1,1,1,1,1,1,1,1,1,1,1,1,1,1,1,1,1,1,1,1,1,1,1,1,1,1,1,1,1,1,
1,1,1,1,1,1,1,1,1,1,1,1,1,1,1,1,1,1,1,4),(-0.000646252380093648,0.082354798859151),
(8.31473274985794,9.31258359158534,10.3104344333127,11.3082852750401,12.3061361167675,
13.3039869584949,14.3018378002224,15.2996886419498,16.2975394836772,17.2953903254046,
18.293241167132,19.2910920088594,20.2889428505868,21.2867936923142,22.2846445340416,
23.282495375769,24.2803462174964,25.2781970592238,26.2760479009512,27.2738987426786,
28.271749584406,29.2696004261334,30.2674512678608,31.2653021095882,32.2631529513156,
33.261003793043,34.2588546347704,35.2567054764978,36.2545563182252,37.2524071599526,
38.25025800168,39.2481088434074,40.2459596851348,41.2438105268622,42.2416613685896,
43.239512210317,44.2373630520444,45.2352138937718,46.2330647354992,47.2309155772266,
48.228766418954,49.2266172606814,50.2244681024088,51.2223189441362,52.2201697858636,
53.218020627591,54.2158714693185,55.2137223110459,56.2115731527733,57.2094239945007,
58.2072748362281,59.2051256779555,60.2029765196829,61.2008273614103,62.1986782031377,
63.1965290448651,64.1943798865925,65.1922307283199,66.1900815700473,67.1879324117747,
68.1857832535021,69.1836340952295,70.1814849369569,71.1793357786843,72.1771866204117,
73.1750374621391,74.1728883038665,75.1707391455939,76.1685899873213,77.1664408290487,
78.1642916707761,79.1621425125035,80.1599933542309,81.1578441959583,82.1556950376857,
83.1535458794131,84.1513967211405,85.1492475628679,86.1470984045953,87.1449492463227,
88.1428000880501,89.1406509297776,90.1385017715049,91.1363526132323,92.1342034549598,
93.1320542966872,94.1299051384146,95.127755980142,96.1256068218694,97.1234576635968,
98.1213085053242,99.1191593470516,100.117010188779,101.114861030506,102.112711872234,
103.110562713961,104.108413555689,105.106264397416,106.104115239143,107.101966080871,
108.099816922598,109.097667764326,110.095518606053,111.09336944778,112.091220289508,
113.089071131235,114.086921972963,115.08477281469,116.082623656417,117.080474498145,
118.078325339872,119.0761761816,120.074027023327,121.071877865054,122.069728706782,
123.067579548509,124.065430390237,125.063281231964,126.061132073691,127.058982915419,
128.056833757146,129.054684598874,130.052535440601,131.050386282328,132.048237124056,
133.046087965783,134.043938807511,135.041789649238,136.040286743345),
 .UNSPECIFIED.);
#54=B_SPLINE_SURFACE_WITH_KNOTS('',3,3,((#22708,#22709,#22710,#22711,#22712,
#22713,#22714,#22715,#22716,#22717,#22718,#22719,#22720,#22721,#22722,#22723,
#22724,#22725,#22726,#22727,#22728,#22729,#22730,#22731,#22732,#22733,#22734,
#22735,#22736,#22737,#22738,#22739,#22740,#22741,#22742,#22743,#22744,#22745,
#22746,#22747,#22748,#22749,#22750,#22751,#22752,#22753,#22754,#22755,#22756,
#22757,#22758,#22759,#22760,#22761,#22762,#22763,#22764,#22765,#22766,#22767,
#22768,#22769,#22770,#22771,#22772,#22773,#22774,#22775,#22776,#22777,#22778,
#22779,#22780,#22781,#22782,#22783,#22784,#22785,#22786,#22787,#22788,#22789,
#22790,#22791,#22792,#22793,#22794,#22795,#22796,#22797,#22798,#22799,#22800,
#22801,#22802,#22803,#22804,#22805,#22806,#22807,#22808,#22809,#22810,#22811,
#22812,#22813,#22814,#22815,#22816,#22817,#22818,#22819,#22820,#22821,#22822,
#22823,#22824,#22825,#22826,#22827,#22828,#22829,#22830,#22831,#22832,#22833,
#22834,#22835,#22836,#22837,#22838),(#22839,#22840,#22841,#22842,#22843,
#22844,#22845,#22846,#22847,#22848,#22849,#22850,#22851,#22852,#22853,#22854,
#22855,#22856,#22857,#22858,#22859,#22860,#22861,#22862,#22863,#22864,#22865,
#22866,#22867,#22868,#22869,#22870,#22871,#22872,#22873,#22874,#22875,#22876,
#22877,#22878,#22879,#22880,#22881,#22882,#22883,#22884,#22885,#22886,#22887,
#22888,#22889,#22890,#22891,#22892,#22893,#22894,#22895,#22896,#22897,#22898,
#22899,#22900,#22901,#22902,#22903,#22904,#22905,#22906,#22907,#22908,#22909,
#22910,#22911,#22912,#22913,#22914,#22915,#22916,#22917,#22918,#22919,#22920,
#22921,#22922,#22923,#22924,#22925,#22926,#22927,#22928,#22929,#22930,#22931,
#22932,#22933,#22934,#22935,#22936,#22937,#22938,#22939,#22940,#22941,#22942,
#22943,#22944,#22945,#22946,#22947,#22948,#22949,#22950,#22951,#22952,#22953,
#22954,#22955,#22956,#22957,#22958,#22959,#22960,#22961,#22962,#22963,#22964,
#22965,#22966,#22967,#22968,#22969),(#22970,#22971,#22972,#22973,#22974,
#22975,#22976,#22977,#22978,#22979,#22980,#22981,#22982,#22983,#22984,#22985,
#22986,#22987,#22988,#22989,#22990,#22991,#22992,#22993,#22994,#22995,#22996,
#22997,#22998,#22999,#23000,#23001,#23002,#23003,#23004,#23005,#23006,#23007,
#23008,#23009,#23010,#23011,#23012,#23013,#23014,#23015,#23016,#23017,#23018,
#23019,#23020,#23021,#23022,#23023,#23024,#23025,#23026,#23027,#23028,#23029,
#23030,#23031,#23032,#23033,#23034,#23035,#23036,#23037,#23038,#23039,#23040,
#23041,#23042,#23043,#23044,#23045,#23046,#23047,#23048,#23049,#23050,#23051,
#23052,#23053,#23054,#23055,#23056,#23057,#23058,#23059,#23060,#23061,#23062,
#23063,#23064,#23065,#23066,#23067,#23068,#23069,#23070,#23071,#23072,#23073,
#23074,#23075,#23076,#23077,#23078,#23079,#23080,#23081,#23082,#23083,#23084,
#23085,#23086,#23087,#23088,#23089,#23090,#23091,#23092,#23093,#23094,#23095,
#23096,#23097,#23098,#23099,#23100),(#23101,#23102,#23103,#23104,#23105,
#23106,#23107,#23108,#23109,#23110,#23111,#23112,#23113,#23114,#23115,#23116,
#23117,#23118,#23119,#23120,#23121,#23122,#23123,#23124,#23125,#23126,#23127,
#23128,#23129,#23130,#23131,#23132,#23133,#23134,#23135,#23136,#23137,#23138,
#23139,#23140,#23141,#23142,#23143,#23144,#23145,#23146,#23147,#23148,#23149,
#23150,#23151,#23152,#23153,#23154,#23155,#23156,#23157,#23158,#23159,#23160,
#23161,#23162,#23163,#23164,#23165,#23166,#23167,#23168,#23169,#23170,#23171,
#23172,#23173,#23174,#23175,#23176,#23177,#23178,#23179,#23180,#23181,#23182,
#23183,#23184,#23185,#23186,#23187,#23188,#23189,#23190,#23191,#23192,#23193,
#23194,#23195,#23196,#23197,#23198,#23199,#23200,#23201,#23202,#23203,#23204,
#23205,#23206,#23207,#23208,#23209,#23210,#23211,#23212,#23213,#23214,#23215,
#23216,#23217,#23218,#23219,#23220,#23221,#23222,#23223,#23224,#23225,#23226,
#23227,#23228,#23229,#23230,#23231)),.UNSPECIFIED.,.F.,.F.,.F.,(4,4),(4,
1,1,1,1,1,1,1,1,1,1,1,1,1,1,1,1,1,1,1,1,1,1,1,1,1,1,1,1,1,1,1,1,1,1,1,1,
1,1,1,1,1,1,1,1,1,1,1,1,1,1,1,1,1,1,1,1,1,1,1,1,1,1,1,1,1,1,1,1,1,1,1,1,
1,1,1,1,1,1,1,1,1,1,1,1,1,1,1,1,1,1,1,1,1,1,1,1,1,1,1,1,1,1,1,1,1,1,1,1,
1,1,1,1,1,1,1,1,1,1,1,1,1,1,1,1,1,1,1,4),(-0.000646252380093648,0.082354798859151),
(8.31473274985794,9.31258359158534,10.3104344333127,11.3082852750401,12.3061361167675,
13.3039869584949,14.3018378002224,15.2996886419498,16.2975394836772,17.2953903254046,
18.293241167132,19.2910920088594,20.2889428505868,21.2867936923142,22.2846445340416,
23.282495375769,24.2803462174964,25.2781970592238,26.2760479009512,27.2738987426786,
28.271749584406,29.2696004261334,30.2674512678608,31.2653021095882,32.2631529513156,
33.261003793043,34.2588546347704,35.2567054764978,36.2545563182252,37.2524071599526,
38.25025800168,39.2481088434074,40.2459596851348,41.2438105268622,42.2416613685896,
43.239512210317,44.2373630520444,45.2352138937718,46.2330647354992,47.2309155772266,
48.228766418954,49.2266172606814,50.2244681024088,51.2223189441362,52.2201697858636,
53.218020627591,54.2158714693185,55.2137223110459,56.2115731527733,57.2094239945007,
58.2072748362281,59.2051256779555,60.2029765196829,61.2008273614103,62.1986782031377,
63.1965290448651,64.1943798865925,65.1922307283199,66.1900815700473,67.1879324117747,
68.1857832535021,69.1836340952295,70.1814849369569,71.1793357786843,72.1771866204117,
73.1750374621391,74.1728883038665,75.1707391455939,76.1685899873213,77.1664408290487,
78.1642916707761,79.1621425125035,80.1599933542309,81.1578441959583,82.1556950376857,
83.1535458794131,84.1513967211405,85.1492475628679,86.1470984045953,87.1449492463227,
88.1428000880501,89.1406509297776,90.1385017715049,91.1363526132323,92.1342034549598,
93.1320542966872,94.1299051384146,95.127755980142,96.1256068218694,97.1234576635968,
98.1213085053242,99.1191593470516,100.117010188779,101.114861030506,102.112711872234,
103.110562713961,104.108413555689,105.106264397416,106.104115239143,107.101966080871,
108.099816922598,109.097667764326,110.095518606053,111.09336944778,112.091220289508,
113.089071131235,114.086921972963,115.08477281469,116.082623656417,117.080474498145,
118.078325339872,119.0761761816,120.074027023327,121.071877865054,122.069728706782,
123.067579548509,124.065430390237,125.063281231964,126.061132073691,127.058982915419,
128.056833757146,129.054684598874,130.052535440601,131.050386282328,132.048237124056,
133.046087965783,134.043938807511,135.041789649238,136.040286743345),
 .UNSPECIFIED.);
#55=B_SPLINE_SURFACE_WITH_KNOTS('',3,3,((#23232,#23233,#23234,#23235,#23236,
#23237,#23238,#23239,#23240,#23241,#23242,#23243,#23244,#23245,#23246,#23247,
#23248,#23249,#23250,#23251,#23252,#23253,#23254,#23255,#23256,#23257,#23258,
#23259,#23260,#23261,#23262,#23263,#23264,#23265,#23266,#23267,#23268,#23269,
#23270,#23271,#23272,#23273,#23274,#23275,#23276,#23277,#23278,#23279,#23280,
#23281,#23282,#23283,#23284,#23285,#23286,#23287,#23288,#23289,#23290,#23291,
#23292,#23293,#23294,#23295,#23296,#23297,#23298,#23299,#23300,#23301,#23302,
#23303,#23304,#23305,#23306,#23307,#23308,#23309,#23310,#23311,#23312,#23313,
#23314,#23315,#23316,#23317,#23318,#23319,#23320,#23321,#23322,#23323,#23324,
#23325,#23326,#23327,#23328,#23329,#23330,#23331,#23332,#23333,#23334,#23335,
#23336,#23337,#23338,#23339,#23340,#23341,#23342,#23343,#23344,#23345,#23346,
#23347,#23348,#23349,#23350,#23351,#23352,#23353,#23354,#23355,#23356,#23357,
#23358,#23359,#23360,#23361,#23362),(#23363,#23364,#23365,#23366,#23367,
#23368,#23369,#23370,#23371,#23372,#23373,#23374,#23375,#23376,#23377,#23378,
#23379,#23380,#23381,#23382,#23383,#23384,#23385,#23386,#23387,#23388,#23389,
#23390,#23391,#23392,#23393,#23394,#23395,#23396,#23397,#23398,#23399,#23400,
#23401,#23402,#23403,#23404,#23405,#23406,#23407,#23408,#23409,#23410,#23411,
#23412,#23413,#23414,#23415,#23416,#23417,#23418,#23419,#23420,#23421,#23422,
#23423,#23424,#23425,#23426,#23427,#23428,#23429,#23430,#23431,#23432,#23433,
#23434,#23435,#23436,#23437,#23438,#23439,#23440,#23441,#23442,#23443,#23444,
#23445,#23446,#23447,#23448,#23449,#23450,#23451,#23452,#23453,#23454,#23455,
#23456,#23457,#23458,#23459,#23460,#23461,#23462,#23463,#23464,#23465,#23466,
#23467,#23468,#23469,#23470,#23471,#23472,#23473,#23474,#23475,#23476,#23477,
#23478,#23479,#23480,#23481,#23482,#23483,#23484,#23485,#23486,#23487,#23488,
#23489,#23490,#23491,#23492,#23493),(#23494,#23495,#23496,#23497,#23498,
#23499,#23500,#23501,#23502,#23503,#23504,#23505,#23506,#23507,#23508,#23509,
#23510,#23511,#23512,#23513,#23514,#23515,#23516,#23517,#23518,#23519,#23520,
#23521,#23522,#23523,#23524,#23525,#23526,#23527,#23528,#23529,#23530,#23531,
#23532,#23533,#23534,#23535,#23536,#23537,#23538,#23539,#23540,#23541,#23542,
#23543,#23544,#23545,#23546,#23547,#23548,#23549,#23550,#23551,#23552,#23553,
#23554,#23555,#23556,#23557,#23558,#23559,#23560,#23561,#23562,#23563,#23564,
#23565,#23566,#23567,#23568,#23569,#23570,#23571,#23572,#23573,#23574,#23575,
#23576,#23577,#23578,#23579,#23580,#23581,#23582,#23583,#23584,#23585,#23586,
#23587,#23588,#23589,#23590,#23591,#23592,#23593,#23594,#23595,#23596,#23597,
#23598,#23599,#23600,#23601,#23602,#23603,#23604,#23605,#23606,#23607,#23608,
#23609,#23610,#23611,#23612,#23613,#23614,#23615,#23616,#23617,#23618,#23619,
#23620,#23621,#23622,#23623,#23624),(#23625,#23626,#23627,#23628,#23629,
#23630,#23631,#23632,#23633,#23634,#23635,#23636,#23637,#23638,#23639,#23640,
#23641,#23642,#23643,#23644,#23645,#23646,#23647,#23648,#23649,#23650,#23651,
#23652,#23653,#23654,#23655,#23656,#23657,#23658,#23659,#23660,#23661,#23662,
#23663,#23664,#23665,#23666,#23667,#23668,#23669,#23670,#23671,#23672,#23673,
#23674,#23675,#23676,#23677,#23678,#23679,#23680,#23681,#23682,#23683,#23684,
#23685,#23686,#23687,#23688,#23689,#23690,#23691,#23692,#23693,#23694,#23695,
#23696,#23697,#23698,#23699,#23700,#23701,#23702,#23703,#23704,#23705,#23706,
#23707,#23708,#23709,#23710,#23711,#23712,#23713,#23714,#23715,#23716,#23717,
#23718,#23719,#23720,#23721,#23722,#23723,#23724,#23725,#23726,#23727,#23728,
#23729,#23730,#23731,#23732,#23733,#23734,#23735,#23736,#23737,#23738,#23739,
#23740,#23741,#23742,#23743,#23744,#23745,#23746,#23747,#23748,#23749,#23750,
#23751,#23752,#23753,#23754,#23755)),.UNSPECIFIED.,.F.,.F.,.F.,(4,4),(4,
1,1,1,1,1,1,1,1,1,1,1,1,1,1,1,1,1,1,1,1,1,1,1,1,1,1,1,1,1,1,1,1,1,1,1,1,
1,1,1,1,1,1,1,1,1,1,1,1,1,1,1,1,1,1,1,1,1,1,1,1,1,1,1,1,1,1,1,1,1,1,1,1,
1,1,1,1,1,1,1,1,1,1,1,1,1,1,1,1,1,1,1,1,1,1,1,1,1,1,1,1,1,1,1,1,1,1,1,1,
1,1,1,1,1,1,1,1,1,1,1,1,1,1,1,1,1,1,1,4),(-0.000646252380093648,0.082354798859151),
(8.31473274985794,9.31258359158534,10.3104344333127,11.3082852750401,12.3061361167675,
13.3039869584949,14.3018378002224,15.2996886419498,16.2975394836772,17.2953903254046,
18.293241167132,19.2910920088594,20.2889428505868,21.2867936923142,22.2846445340416,
23.282495375769,24.2803462174964,25.2781970592238,26.2760479009512,27.2738987426786,
28.271749584406,29.2696004261334,30.2674512678608,31.2653021095882,32.2631529513156,
33.261003793043,34.2588546347704,35.2567054764978,36.2545563182252,37.2524071599526,
38.25025800168,39.2481088434074,40.2459596851348,41.2438105268622,42.2416613685896,
43.239512210317,44.2373630520444,45.2352138937718,46.2330647354992,47.2309155772266,
48.228766418954,49.2266172606814,50.2244681024088,51.2223189441362,52.2201697858636,
53.218020627591,54.2158714693185,55.2137223110459,56.2115731527733,57.2094239945007,
58.2072748362281,59.2051256779555,60.2029765196829,61.2008273614103,62.1986782031377,
63.1965290448651,64.1943798865925,65.1922307283199,66.1900815700473,67.1879324117747,
68.1857832535021,69.1836340952295,70.1814849369569,71.1793357786843,72.1771866204117,
73.1750374621391,74.1728883038665,75.1707391455939,76.1685899873213,77.1664408290487,
78.1642916707761,79.1621425125035,80.1599933542309,81.1578441959583,82.1556950376857,
83.1535458794131,84.1513967211405,85.1492475628679,86.1470984045953,87.1449492463227,
88.1428000880501,89.1406509297776,90.1385017715049,91.1363526132323,92.1342034549598,
93.1320542966872,94.1299051384146,95.127755980142,96.1256068218694,97.1234576635968,
98.1213085053242,99.1191593470516,100.117010188779,101.114861030506,102.112711872234,
103.110562713961,104.108413555689,105.106264397416,106.104115239143,107.101966080871,
108.099816922598,109.097667764326,110.095518606053,111.09336944778,112.091220289508,
113.089071131235,114.086921972963,115.08477281469,116.082623656417,117.080474498145,
118.078325339872,119.0761761816,120.074027023327,121.071877865054,122.069728706782,
123.067579548509,124.065430390237,125.063281231964,126.061132073691,127.058982915419,
128.056833757146,129.054684598874,130.052535440601,131.050386282328,132.048237124056,
133.046087965783,134.043938807511,135.041789649238,136.040286743345),
 .UNSPECIFIED.);
#56=B_SPLINE_SURFACE_WITH_KNOTS('',3,3,((#24051,#24052,#24053,#24054,#24055,
#24056,#24057,#24058,#24059,#24060,#24061,#24062,#24063,#24064,#24065,#24066,
#24067,#24068,#24069,#24070,#24071,#24072,#24073,#24074,#24075,#24076,#24077,
#24078,#24079,#24080,#24081,#24082,#24083,#24084,#24085,#24086,#24087,#24088,
#24089,#24090,#24091,#24092,#24093,#24094,#24095,#24096,#24097,#24098,#24099,
#24100,#24101,#24102,#24103,#24104,#24105,#24106,#24107,#24108,#24109,#24110,
#24111,#24112,#24113,#24114,#24115,#24116,#24117,#24118,#24119,#24120,#24121,
#24122,#24123,#24124,#24125,#24126,#24127,#24128,#24129,#24130,#24131,#24132,
#24133,#24134,#24135,#24136,#24137,#24138,#24139,#24140,#24141,#24142,#24143,
#24144,#24145,#24146,#24147,#24148,#24149,#24150,#24151,#24152,#24153,#24154,
#24155,#24156,#24157,#24158,#24159,#24160,#24161,#24162,#24163,#24164,#24165,
#24166,#24167,#24168,#24169,#24170,#24171,#24172,#24173,#24174,#24175,#24176,
#24177,#24178,#24179,#24180,#24181),(#24182,#24183,#24184,#24185,#24186,
#24187,#24188,#24189,#24190,#24191,#24192,#24193,#24194,#24195,#24196,#24197,
#24198,#24199,#24200,#24201,#24202,#24203,#24204,#24205,#24206,#24207,#24208,
#24209,#24210,#24211,#24212,#24213,#24214,#24215,#24216,#24217,#24218,#24219,
#24220,#24221,#24222,#24223,#24224,#24225,#24226,#24227,#24228,#24229,#24230,
#24231,#24232,#24233,#24234,#24235,#24236,#24237,#24238,#24239,#24240,#24241,
#24242,#24243,#24244,#24245,#24246,#24247,#24248,#24249,#24250,#24251,#24252,
#24253,#24254,#24255,#24256,#24257,#24258,#24259,#24260,#24261,#24262,#24263,
#24264,#24265,#24266,#24267,#24268,#24269,#24270,#24271,#24272,#24273,#24274,
#24275,#24276,#24277,#24278,#24279,#24280,#24281,#24282,#24283,#24284,#24285,
#24286,#24287,#24288,#24289,#24290,#24291,#24292,#24293,#24294,#24295,#24296,
#24297,#24298,#24299,#24300,#24301,#24302,#24303,#24304,#24305,#24306,#24307,
#24308,#24309,#24310,#24311,#24312),(#24313,#24314,#24315,#24316,#24317,
#24318,#24319,#24320,#24321,#24322,#24323,#24324,#24325,#24326,#24327,#24328,
#24329,#24330,#24331,#24332,#24333,#24334,#24335,#24336,#24337,#24338,#24339,
#24340,#24341,#24342,#24343,#24344,#24345,#24346,#24347,#24348,#24349,#24350,
#24351,#24352,#24353,#24354,#24355,#24356,#24357,#24358,#24359,#24360,#24361,
#24362,#24363,#24364,#24365,#24366,#24367,#24368,#24369,#24370,#24371,#24372,
#24373,#24374,#24375,#24376,#24377,#24378,#24379,#24380,#24381,#24382,#24383,
#24384,#24385,#24386,#24387,#24388,#24389,#24390,#24391,#24392,#24393,#24394,
#24395,#24396,#24397,#24398,#24399,#24400,#24401,#24402,#24403,#24404,#24405,
#24406,#24407,#24408,#24409,#24410,#24411,#24412,#24413,#24414,#24415,#24416,
#24417,#24418,#24419,#24420,#24421,#24422,#24423,#24424,#24425,#24426,#24427,
#24428,#24429,#24430,#24431,#24432,#24433,#24434,#24435,#24436,#24437,#24438,
#24439,#24440,#24441,#24442,#24443),(#24444,#24445,#24446,#24447,#24448,
#24449,#24450,#24451,#24452,#24453,#24454,#24455,#24456,#24457,#24458,#24459,
#24460,#24461,#24462,#24463,#24464,#24465,#24466,#24467,#24468,#24469,#24470,
#24471,#24472,#24473,#24474,#24475,#24476,#24477,#24478,#24479,#24480,#24481,
#24482,#24483,#24484,#24485,#24486,#24487,#24488,#24489,#24490,#24491,#24492,
#24493,#24494,#24495,#24496,#24497,#24498,#24499,#24500,#24501,#24502,#24503,
#24504,#24505,#24506,#24507,#24508,#24509,#24510,#24511,#24512,#24513,#24514,
#24515,#24516,#24517,#24518,#24519,#24520,#24521,#24522,#24523,#24524,#24525,
#24526,#24527,#24528,#24529,#24530,#24531,#24532,#24533,#24534,#24535,#24536,
#24537,#24538,#24539,#24540,#24541,#24542,#24543,#24544,#24545,#24546,#24547,
#24548,#24549,#24550,#24551,#24552,#24553,#24554,#24555,#24556,#24557,#24558,
#24559,#24560,#24561,#24562,#24563,#24564,#24565,#24566,#24567,#24568,#24569,
#24570,#24571,#24572,#24573,#24574)),.UNSPECIFIED.,.F.,.F.,.F.,(4,4),(4,
1,1,1,1,1,1,1,1,1,1,1,1,1,1,1,1,1,1,1,1,1,1,1,1,1,1,1,1,1,1,1,1,1,1,1,1,
1,1,1,1,1,1,1,1,1,1,1,1,1,1,1,1,1,1,1,1,1,1,1,1,1,1,1,1,1,1,1,1,1,1,1,1,
1,1,1,1,1,1,1,1,1,1,1,1,1,1,1,1,1,1,1,1,1,1,1,1,1,1,1,1,1,1,1,1,1,1,1,1,
1,1,1,1,1,1,1,1,1,1,1,1,1,1,1,1,1,1,1,4),(-0.000646252380093648,0.082354798859151),
(8.31473274985794,9.31258359158534,10.3104344333127,11.3082852750401,12.3061361167675,
13.3039869584949,14.3018378002224,15.2996886419498,16.2975394836772,17.2953903254046,
18.293241167132,19.2910920088594,20.2889428505868,21.2867936923142,22.2846445340416,
23.282495375769,24.2803462174964,25.2781970592238,26.2760479009512,27.2738987426786,
28.271749584406,29.2696004261334,30.2674512678608,31.2653021095882,32.2631529513156,
33.261003793043,34.2588546347704,35.2567054764978,36.2545563182252,37.2524071599526,
38.25025800168,39.2481088434074,40.2459596851348,41.2438105268622,42.2416613685896,
43.239512210317,44.2373630520444,45.2352138937718,46.2330647354992,47.2309155772266,
48.228766418954,49.2266172606814,50.2244681024088,51.2223189441362,52.2201697858636,
53.218020627591,54.2158714693185,55.2137223110459,56.2115731527733,57.2094239945007,
58.2072748362281,59.2051256779555,60.2029765196829,61.2008273614103,62.1986782031377,
63.1965290448651,64.1943798865925,65.1922307283199,66.1900815700473,67.1879324117747,
68.1857832535021,69.1836340952295,70.1814849369569,71.1793357786843,72.1771866204117,
73.1750374621391,74.1728883038665,75.1707391455939,76.1685899873213,77.1664408290487,
78.1642916707761,79.1621425125035,80.1599933542309,81.1578441959583,82.1556950376857,
83.1535458794131,84.1513967211405,85.1492475628679,86.1470984045953,87.1449492463227,
88.1428000880501,89.1406509297776,90.1385017715049,91.1363526132323,92.1342034549598,
93.1320542966872,94.1299051384146,95.127755980142,96.1256068218694,97.1234576635968,
98.1213085053242,99.1191593470516,100.117010188779,101.114861030506,102.112711872234,
103.110562713961,104.108413555689,105.106264397416,106.104115239143,107.101966080871,
108.099816922598,109.097667764326,110.095518606053,111.09336944778,112.091220289508,
113.089071131235,114.086921972963,115.08477281469,116.082623656417,117.080474498145,
118.078325339872,119.0761761816,120.074027023327,121.071877865054,122.069728706782,
123.067579548509,124.065430390237,125.063281231964,126.061132073691,127.058982915419,
128.056833757146,129.054684598874,130.052535440601,131.050386282328,132.048237124056,
133.046087965783,134.043938807511,135.041789649238,136.040286743345),
 .UNSPECIFIED.);
#57=B_SPLINE_SURFACE_WITH_KNOTS('',3,3,((#24575,#24576,#24577,#24578,#24579,
#24580,#24581,#24582,#24583,#24584,#24585,#24586,#24587,#24588,#24589,#24590,
#24591,#24592,#24593,#24594,#24595,#24596,#24597,#24598,#24599,#24600,#24601,
#24602,#24603,#24604,#24605,#24606,#24607,#24608,#24609,#24610,#24611,#24612,
#24613,#24614,#24615,#24616,#24617,#24618,#24619,#24620,#24621,#24622,#24623,
#24624,#24625,#24626,#24627,#24628,#24629,#24630,#24631,#24632,#24633,#24634,
#24635,#24636,#24637,#24638,#24639,#24640,#24641,#24642,#24643,#24644,#24645,
#24646,#24647,#24648,#24649,#24650,#24651,#24652,#24653,#24654,#24655,#24656,
#24657,#24658,#24659,#24660,#24661,#24662,#24663,#24664,#24665,#24666,#24667,
#24668,#24669,#24670,#24671,#24672,#24673,#24674,#24675,#24676,#24677,#24678,
#24679,#24680,#24681,#24682,#24683,#24684,#24685,#24686,#24687,#24688,#24689,
#24690,#24691,#24692,#24693,#24694,#24695,#24696,#24697,#24698,#24699,#24700,
#24701,#24702,#24703,#24704,#24705),(#24706,#24707,#24708,#24709,#24710,
#24711,#24712,#24713,#24714,#24715,#24716,#24717,#24718,#24719,#24720,#24721,
#24722,#24723,#24724,#24725,#24726,#24727,#24728,#24729,#24730,#24731,#24732,
#24733,#24734,#24735,#24736,#24737,#24738,#24739,#24740,#24741,#24742,#24743,
#24744,#24745,#24746,#24747,#24748,#24749,#24750,#24751,#24752,#24753,#24754,
#24755,#24756,#24757,#24758,#24759,#24760,#24761,#24762,#24763,#24764,#24765,
#24766,#24767,#24768,#24769,#24770,#24771,#24772,#24773,#24774,#24775,#24776,
#24777,#24778,#24779,#24780,#24781,#24782,#24783,#24784,#24785,#24786,#24787,
#24788,#24789,#24790,#24791,#24792,#24793,#24794,#24795,#24796,#24797,#24798,
#24799,#24800,#24801,#24802,#24803,#24804,#24805,#24806,#24807,#24808,#24809,
#24810,#24811,#24812,#24813,#24814,#24815,#24816,#24817,#24818,#24819,#24820,
#24821,#24822,#24823,#24824,#24825,#24826,#24827,#24828,#24829,#24830,#24831,
#24832,#24833,#24834,#24835,#24836),(#24837,#24838,#24839,#24840,#24841,
#24842,#24843,#24844,#24845,#24846,#24847,#24848,#24849,#24850,#24851,#24852,
#24853,#24854,#24855,#24856,#24857,#24858,#24859,#24860,#24861,#24862,#24863,
#24864,#24865,#24866,#24867,#24868,#24869,#24870,#24871,#24872,#24873,#24874,
#24875,#24876,#24877,#24878,#24879,#24880,#24881,#24882,#24883,#24884,#24885,
#24886,#24887,#24888,#24889,#24890,#24891,#24892,#24893,#24894,#24895,#24896,
#24897,#24898,#24899,#24900,#24901,#24902,#24903,#24904,#24905,#24906,#24907,
#24908,#24909,#24910,#24911,#24912,#24913,#24914,#24915,#24916,#24917,#24918,
#24919,#24920,#24921,#24922,#24923,#24924,#24925,#24926,#24927,#24928,#24929,
#24930,#24931,#24932,#24933,#24934,#24935,#24936,#24937,#24938,#24939,#24940,
#24941,#24942,#24943,#24944,#24945,#24946,#24947,#24948,#24949,#24950,#24951,
#24952,#24953,#24954,#24955,#24956,#24957,#24958,#24959,#24960,#24961,#24962,
#24963,#24964,#24965,#24966,#24967),(#24968,#24969,#24970,#24971,#24972,
#24973,#24974,#24975,#24976,#24977,#24978,#24979,#24980,#24981,#24982,#24983,
#24984,#24985,#24986,#24987,#24988,#24989,#24990,#24991,#24992,#24993,#24994,
#24995,#24996,#24997,#24998,#24999,#25000,#25001,#25002,#25003,#25004,#25005,
#25006,#25007,#25008,#25009,#25010,#25011,#25012,#25013,#25014,#25015,#25016,
#25017,#25018,#25019,#25020,#25021,#25022,#25023,#25024,#25025,#25026,#25027,
#25028,#25029,#25030,#25031,#25032,#25033,#25034,#25035,#25036,#25037,#25038,
#25039,#25040,#25041,#25042,#25043,#25044,#25045,#25046,#25047,#25048,#25049,
#25050,#25051,#25052,#25053,#25054,#25055,#25056,#25057,#25058,#25059,#25060,
#25061,#25062,#25063,#25064,#25065,#25066,#25067,#25068,#25069,#25070,#25071,
#25072,#25073,#25074,#25075,#25076,#25077,#25078,#25079,#25080,#25081,#25082,
#25083,#25084,#25085,#25086,#25087,#25088,#25089,#25090,#25091,#25092,#25093,
#25094,#25095,#25096,#25097,#25098)),.UNSPECIFIED.,.F.,.F.,.F.,(4,4),(4,
1,1,1,1,1,1,1,1,1,1,1,1,1,1,1,1,1,1,1,1,1,1,1,1,1,1,1,1,1,1,1,1,1,1,1,1,
1,1,1,1,1,1,1,1,1,1,1,1,1,1,1,1,1,1,1,1,1,1,1,1,1,1,1,1,1,1,1,1,1,1,1,1,
1,1,1,1,1,1,1,1,1,1,1,1,1,1,1,1,1,1,1,1,1,1,1,1,1,1,1,1,1,1,1,1,1,1,1,1,
1,1,1,1,1,1,1,1,1,1,1,1,1,1,1,1,1,1,1,4),(-0.000314077148181808,0.0826777824702824),
(11.6145490510227,12.613065069482,13.6109159112094,14.6087667529368,15.6066175946642,
16.6044684363917,17.6023192781191,18.6001701198465,19.5980209615739,20.5958718033013,
21.5937226450287,22.5915734867561,23.5894243284835,24.5872751702109,25.5851260119383,
26.5829768536657,27.5808276953931,28.5786785371205,29.5765293788479,30.5743802205753,
31.5722310623027,32.5700819040301,33.5679327457575,34.5657835874849,35.5636344292123,
36.5614852709397,37.5593361126671,38.5571869543945,39.5550377961219,40.5528886378493,
41.5507394795767,42.5485903213041,43.5464411630315,44.5442920047589,45.5421428464863,
46.5399936882137,47.5378445299411,48.5356953716685,49.5335462133959,50.5313970551233,
51.5292478968507,52.5270987385781,53.5249495803055,54.522800422033,55.5206512637604,
56.5185021054878,57.5163529472152,58.5142037889426,59.51205463067,60.5099054723974,
61.5077563141248,62.5056071558522,63.5034579975796,64.501308839307,65.4991596810344,
66.4970105227618,67.4948613644892,68.4927122062166,69.490563047944,70.4884138896714,
71.4862647313988,72.4841155731262,73.4819664148536,74.479817256581,75.4776680983084,
76.4755189400358,77.4733697817632,78.4712206234906,79.469071465218,80.4669223069454,
81.4647731486728,82.4626239904002,83.4604748321276,84.458325673855,85.4561765155824,
86.4540273573098,87.4518781990372,88.4497290407646,89.4475798824921,90.4454307242194,
91.4432815659468,92.4411324076742,93.4389832494017,94.4368340911291,95.4346849328565,
96.4325357745839,97.4303866163113,98.4282374580387,99.4260882997661,100.423939141493,
101.421789983221,102.419640824948,103.417491666676,104.415342508403,105.41319335013,
106.411044191858,107.408895033585,108.406745875313,109.40459671704,110.402447558768,
111.400298400495,112.398149242222,113.39600008395,114.393850925677,115.391701767405,
116.389552609132,117.387403450859,118.385254292587,119.383105134314,120.380955976042,
121.378806817769,122.376657659496,123.374508501224,124.372359342951,125.370210184679,
126.368061026406,127.365911868133,128.363762709861,129.361613551588,130.359464393316,
131.357315235043,132.35516607677,133.353016918498,134.350867760225,135.348718601953,
136.34656944368,137.344420285407,138.342271127135,139.340121968862),
 .UNSPECIFIED.);
#65=SHAPE_REPRESENTATION_RELATIONSHIP('SRR','None',#51586,#73);
#73=ADVANCED_BREP_SHAPE_REPRESENTATION('',(#90),#51546);
#81=STYLED_ITEM('',(#51634),#90);
#90=MANIFOLD_SOLID_BREP('Body1',#4260);
#136=PLANE('',#4448);
#137=PLANE('',#4451);
#138=PLANE('',#4465);
#215=FACE_OUTER_BOUND('',#416,.T.);
#216=FACE_OUTER_BOUND('',#417,.T.);
#217=FACE_OUTER_BOUND('',#418,.T.);
#218=FACE_OUTER_BOUND('',#419,.T.);
#219=FACE_OUTER_BOUND('',#420,.T.);
#220=FACE_OUTER_BOUND('',#421,.T.);
#221=FACE_OUTER_BOUND('',#422,.T.);
#222=FACE_OUTER_BOUND('',#423,.T.);
#223=FACE_OUTER_BOUND('',#424,.T.);
#224=FACE_OUTER_BOUND('',#425,.T.);
#225=FACE_OUTER_BOUND('',#426,.T.);
#226=FACE_OUTER_BOUND('',#427,.T.);
#227=FACE_OUTER_BOUND('',#428,.T.);
#228=FACE_OUTER_BOUND('',#429,.T.);
#229=FACE_OUTER_BOUND('',#430,.T.);
#230=FACE_OUTER_BOUND('',#431,.T.);
#231=FACE_OUTER_BOUND('',#432,.T.);
#232=FACE_OUTER_BOUND('',#433,.T.);
#233=FACE_OUTER_BOUND('',#434,.T.);
#234=FACE_OUTER_BOUND('',#435,.T.);
#235=FACE_OUTER_BOUND('',#436,.T.);
#236=FACE_OUTER_BOUND('',#437,.T.);
#237=FACE_OUTER_BOUND('',#438,.T.);
#238=FACE_OUTER_BOUND('',#439,.T.);
#239=FACE_OUTER_BOUND('',#440,.T.);
#240=FACE_OUTER_BOUND('',#441,.T.);
#241=FACE_OUTER_BOUND('',#442,.T.);
#242=FACE_OUTER_BOUND('',#443,.T.);
#243=FACE_OUTER_BOUND('',#444,.T.);
#244=FACE_OUTER_BOUND('',#445,.T.);
#245=FACE_OUTER_BOUND('',#446,.T.);
#246=FACE_OUTER_BOUND('',#447,.T.);
#247=FACE_OUTER_BOUND('',#448,.T.);
#248=FACE_OUTER_BOUND('',#449,.T.);
#249=FACE_OUTER_BOUND('',#450,.T.);
#250=FACE_OUTER_BOUND('',#451,.T.);
#251=FACE_OUTER_BOUND('',#452,.T.);
#252=FACE_OUTER_BOUND('',#453,.T.);
#253=FACE_OUTER_BOUND('',#454,.T.);
#254=FACE_OUTER_BOUND('',#455,.T.);
#416=EDGE_LOOP('',(#2821,#2822,#2823,#2824));
#417=EDGE_LOOP('',(#2825,#2826,#2827,#2828));
#418=EDGE_LOOP('',(#2829,#2830,#2831,#2832));
#419=EDGE_LOOP('',(#2833,#2834,#2835,#2836,#2837));
#420=EDGE_LOOP('',(#2838,#2839,#2840,#2841,#2842));
#421=EDGE_LOOP('',(#2843,#2844,#2845,#2846));
#422=EDGE_LOOP('',(#2847,#2848,#2849,#2850,#2851));
#423=EDGE_LOOP('',(#2852,#2853,#2854,#2855,#2856,#2857));
#424=EDGE_LOOP('',(#2858,#2859,#2860,#2861,#2862));
#425=EDGE_LOOP('',(#2863,#2864,#2865,#2866));
#426=EDGE_LOOP('',(#2867,#2868,#2869,#2870,#2871));
#427=EDGE_LOOP('',(#2872,#2873,#2874,#2875,#2876));
#428=EDGE_LOOP('',(#2877,#2878,#2879,#2880));
#429=EDGE_LOOP('',(#2881,#2882,#2883,#2884,#2885));
#430=EDGE_LOOP('',(#2886,#2887,#2888,#2889,#2890));
#431=EDGE_LOOP('',(#2891,#2892,#2893,#2894,#2895));
#432=EDGE_LOOP('',(#2896,#2897,#2898,#2899,#2900,#2901,#2902,#2903,#2904,
#2905,#2906,#2907,#2908,#2909,#2910,#2911,#2912,#2913,#2914,#2915,#2916,
#2917,#2918,#2919,#2920,#2921,#2922,#2923));
#433=EDGE_LOOP('',(#2924,#2925,#2926,#2927,#2928,#2929,#2930,#2931,#2932,
#2933));
#434=EDGE_LOOP('',(#2934,#2935,#2936,#2937,#2938,#2939,#2940));
#435=EDGE_LOOP('',(#2941,#2942,#2943,#2944,#2945,#2946,#2947,#2948,#2949,
#2950,#2951,#2952,#2953,#2954,#2955,#2956,#2957,#2958,#2959,#2960,#2961,
#2962,#2963,#2964,#2965,#2966,#2967,#2968,#2969,#2970,#2971,#2972,#2973,
#2974,#2975,#2976));
#436=EDGE_LOOP('',(#2977,#2978,#2979,#2980));
#437=EDGE_LOOP('',(#2981,#2982,#2983,#2984));
#438=EDGE_LOOP('',(#2985,#2986,#2987,#2988));
#439=EDGE_LOOP('',(#2989,#2990,#2991,#2992,#2993,#2994,#2995,#2996,#2997,
#2998,#2999,#3000,#3001,#3002,#3003,#3004,#3005,#3006,#3007,#3008,#3009,
#3010,#3011,#3012,#3013,#3014,#3015,#3016,#3017,#3018,#3019,#3020,#3021,
#3022,#3023,#3024,#3025,#3026,#3027,#3028,#3029,#3030,#3031));
#440=EDGE_LOOP('',(#3032,#3033,#3034,#3035));
#441=EDGE_LOOP('',(#3036,#3037,#3038,#3039));
#442=EDGE_LOOP('',(#3040,#3041,#3042,#3043));
#443=EDGE_LOOP('',(#3044,#3045,#3046,#3047));
#444=EDGE_LOOP('',(#3048,#3049,#3050,#3051));
#445=EDGE_LOOP('',(#3052,#3053,#3054,#3055));
#446=EDGE_LOOP('',(#3056,#3057,#3058,#3059));
#447=EDGE_LOOP('',(#3060,#3061,#3062,#3063,#3064,#3065,#3066,#3067,#3068,
#3069,#3070,#3071,#3072,#3073,#3074,#3075,#3076,#3077,#3078,#3079,#3080,
#3081,#3082,#3083,#3084,#3085,#3086,#3087,#3088,#3089,#3090,#3091,#3092,
#3093,#3094,#3095,#3096,#3097,#3098,#3099,#3100,#3101,#3102,#3103));
#448=EDGE_LOOP('',(#3104,#3105,#3106,#3107,#3108));
#449=EDGE_LOOP('',(#3109,#3110,#3111,#3112));
#450=EDGE_LOOP('',(#3113,#3114,#3115,#3116,#3117,#3118));
#451=EDGE_LOOP('',(#3119,#3120,#3121,#3122));
#452=EDGE_LOOP('',(#3123,#3124,#3125,#3126));
#453=EDGE_LOOP('',(#3127,#3128,#3129));
#454=EDGE_LOOP('',(#3130,#3131,#3132,#3133));
#455=EDGE_LOOP('',(#3134,#3135,#3136,#3137,#3138));
#630=CIRCLE('',#4432,3.22274999999998);
#631=CIRCLE('',#4449,5.);
#632=CIRCLE('',#4452,3.22274999999998);
#633=CIRCLE('',#4453,3.933);
#634=CIRCLE('',#4455,3.933);
#769=LINE('',#5730,#997);
#770=LINE('',#5862,#998);
#771=LINE('',#6296,#999);
#772=LINE('',#6706,#1000);
#773=LINE('',#7183,#1001);
#774=LINE('',#7718,#1002);
#775=LINE('',#8150,#1003);
#776=LINE('',#8599,#1004);
#777=LINE('',#9059,#1005);
#778=LINE('',#9518,#1006);
#779=LINE('',#9946,#1007);
#780=LINE('',#10389,#1008);
#781=LINE('',#10840,#1009);
#782=LINE('',#11296,#1010);
#783=LINE('',#11753,#1011);
#784=LINE('',#12292,#1012);
#785=LINE('',#12767,#1013);
#786=LINE('',#12776,#1014);
#787=LINE('',#12785,#1015);
#788=LINE('',#12794,#1016);
#789=LINE('',#12803,#1017);
#790=LINE('',#12812,#1018);
#791=LINE('',#12821,#1019);
#792=LINE('',#12828,#1020);
#793=LINE('',#12839,#1021);
#794=LINE('',#12848,#1022);
#795=LINE('',#12859,#1023);
#796=LINE('',#12870,#1024);
#797=LINE('',#12880,#1025);
#997=VECTOR('',#4879,3.22274999999998);
#998=VECTOR('',#4884,3.22274999999998);
#999=VECTOR('',#4887,3.22274999999998);
#1000=VECTOR('',#4890,3.22274999999998);
#1001=VECTOR('',#4893,3.22274999999998);
#1002=VECTOR('',#4896,3.22274999999998);
#1003=VECTOR('',#4899,3.22274999999998);
#1004=VECTOR('',#4902,3.22274999999998);
#1005=VECTOR('',#4905,3.22274999999998);
#1006=VECTOR('',#4908,3.22274999999998);
#1007=VECTOR('',#4911,3.22274999999998);
#1008=VECTOR('',#4914,3.22274999999998);
#1009=VECTOR('',#4917,3.22274999999998);
#1010=VECTOR('',#4920,3.22274999999998);
#1011=VECTOR('',#4923,3.22274999999998);
#1012=VECTOR('',#4926,3.22274999999998);
#1013=VECTOR('',#4931,10.);
#1014=VECTOR('',#4932,10.);
#1015=VECTOR('',#4933,10.);
#1016=VECTOR('',#4934,10.);
#1017=VECTOR('',#4935,10.);
#1018=VECTOR('',#4936,10.);
#1019=VECTOR('',#4937,10.);
#1020=VECTOR('',#4938,10.);
#1021=VECTOR('',#4939,10.);
#1022=VECTOR('',#4940,10.);
#1023=VECTOR('',#4941,10.);
#1024=VECTOR('',#4942,10.);
#1025=VECTOR('',#4943,10.);
#1168=B_SPLINE_CURVE_WITH_KNOTS('',3,(#5732,#5733,#5734,#5735,#5736,#5737,
#5738,#5739,#5740,#5741,#5742,#5743,#5744,#5745,#5746,#5747,#5748,#5749,
#5750,#5751,#5752,#5753,#5754,#5755,#5756,#5757,#5758,#5759,#5760,#5761,
#5762),.UNSPECIFIED.,.F.,.F.,(4,3,3,3,3,3,3,3,3,3,4),(135.088484104522,
135.183357452592,135.278085083771,135.37327950967,135.467774090023,135.562205452058,
135.656595638088,135.752356851307,135.846756258313,135.943198374639,136.039640490965),
 .UNSPECIFIED.);
#1169=B_SPLINE_CURVE_WITH_KNOTS('',3,(#5765,#5766,#5767,#5768,#5769,#5770,
#5771,#5772,#5773,#5774,#5775,#5776,#5777,#5778,#5779,#5780,#5781,#5782,
#5783,#5784,#5785,#5786,#5787,#5788,#5789,#5790,#5791,#5792,#5793,#5794,
#5795,#5796,#5797,#5798,#5799,#5800,#5801,#5802,#5803,#5804,#5805,#5806,
#5807,#5808,#5809,#5810,#5811,#5812,#5813,#5814,#5815,#5816,#5817,#5818,
#5819,#5820,#5821,#5822,#5823,#5824,#5825,#5826,#5827,#5828,#5829,#5830,
#5831,#5832,#5833,#5834,#5835,#5836,#5837,#5838,#5839,#5840,#5841,#5842,
#5843,#5844,#5845,#5846,#5847,#5848,#5849,#5850,#5851,#5852,#5853,#5854,
#5855,#5856,#5857,#5858),.UNSPECIFIED.,.F.,.F.,(4,2,2,2,2,2,2,2,2,2,2,2,
2,2,2,2,2,2,2,2,2,2,2,2,2,2,2,2,2,2,2,2,2,2,2,2,2,2,2,2,2,2,2,2,2,2,4),
(0.0057209449088494,0.103861911368512,0.131206262754794,0.138793528122716,
0.143482252567016,0.147782848695881,0.15330943057905,0.165272569137304,
0.237793745170985,0.29160869938094,0.297545267653851,0.300502332474027,
0.300522608840903,0.300543258027676,0.300564293317863,0.300585728630467,
0.300607578554829,0.300629858367842,0.300652584102735,0.300675772583853,
0.300699441476995,0.300723609353366,0.300748295753824,0.303095417880315,
0.30597791581334,0.311474715542388,0.34887979776667,0.401918797533959,0.431924592452901,
0.444711052939809,0.45474683107368,0.459923226535699,0.464135470813334,
0.468998551959832,0.477319251816791,0.512144776417391,0.51915990933343,
0.584122643035605,0.605243372488193,0.61769635853554,0.621638370754149,
0.624159844368455,0.626558058277041,0.629516330011378,0.636789063423376,
0.705917753616687,0.708678555662593),.UNSPECIFIED.);
#1170=B_SPLINE_CURVE_WITH_KNOTS('',3,(#5863,#5864,#5865,#5866,#5867,#5868,
#5869,#5870,#5871,#5872,#5873,#5874,#5875,#5876,#5877,#5878,#5879,#5880,
#5881,#5882,#5883,#5884,#5885,#5886,#5887,#5888,#5889,#5890,#5891,#5892,
#5893,#5894,#5895,#5896,#5897,#5898,#5899,#5900,#5901,#5902,#5903,#5904,
#5905,#5906,#5907,#5908,#5909,#5910,#5911,#5912,#5913,#5914,#5915,#5916,
#5917,#5918,#5919,#5920,#5921,#5922,#5923,#5924,#5925,#5926,#5927,#5928,
#5929,#5930,#5931,#5932,#5933,#5934,#5935,#5936,#5937,#5938,#5939,#5940,
#5941,#5942,#5943,#5944,#5945,#5946,#5947,#5948,#5949,#5950,#5951,#5952,
#5953,#5954,#5955,#5956,#5957,#5958,#5959,#5960,#5961,#5962,#5963,#5964,
#5965,#5966,#5967,#5968,#5969,#5970,#5971,#5972,#5973,#5974,#5975,#5976,
#5977,#5978,#5979,#5980,#5981,#5982,#5983,#5984,#5985,#5986,#5987,#5988,
#5989,#5990,#5991,#5992,#5993,#5994,#5995,#5996,#5997,#5998,#5999,#6000,
#6001,#6002,#6003,#6004,#6005,#6006,#6007,#6008,#6009,#6010,#6011,#6012,
#6013,#6014,#6015,#6016,#6017,#6018,#6019,#6020,#6021,#6022,#6023,#6024,
#6025,#6026,#6027,#6028,#6029,#6030,#6031,#6032,#6033,#6034,#6035,#6036,
#6037,#6038,#6039,#6040,#6041,#6042,#6043,#6044,#6045,#6046,#6047,#6048,
#6049,#6050,#6051,#6052,#6053,#6054,#6055,#6056,#6057,#6058,#6059,#6060,
#6061,#6062,#6063,#6064,#6065,#6066,#6067,#6068,#6069,#6070),
 .UNSPECIFIED.,.F.,.F.,(4,3,3,3,3,3,3,3,3,3,3,3,3,3,3,3,3,3,3,3,3,3,3,3,
3,3,3,3,3,3,3,3,3,3,3,3,3,3,3,3,3,3,3,3,3,3,3,3,3,3,3,3,3,3,3,3,3,3,3,3,
3,3,3,3,3,3,3,3,3,4),(128.80529879735,128.929991698112,129.054684598874,
129.147800779154,129.240791211017,129.333683471756,129.426508042657,129.519297567574,
129.612076820608,129.704870560763,129.797762815361,129.890706836103,129.983804530045,
130.052535440601,130.145654979342,130.238649150331,130.331545520457,130.424374733419,
130.517169225087,130.609953761454,130.702753093673,130.79565137859,130.888601682427,
130.981706002525,131.050386282328,131.143352725217,131.236193216463,131.328935523828,
131.421610721533,131.5142512722,131.606882118562,131.699528188761,131.792274812806,
131.885074106871,131.978030044583,132.048237124056,132.14151054607,132.23465782876,
132.327706349228,132.420685659563,132.513628936106,132.606560773306,132.699505749532,
132.792546233298,132.885637032366,132.978877645127,133.046087965783,133.139304490498,
133.232397384719,133.325394057745,133.418325495527,133.511223352139,133.60411225829,
133.697016830648,133.790021022654,133.883077764359,133.976288264225,134.043938807511,
134.136039163594,134.228013262994,134.319889832992,134.411703498339,134.503485161219,
134.595260602326,134.687055591602,134.778962943864,134.870927981932,134.963066833032,
135.041789649238,135.088484104361),.UNSPECIFIED.);
#1171=B_SPLINE_CURVE_WITH_KNOTS('',3,(#6071,#6072,#6073,#6074,#6075,#6076,
#6077,#6078,#6079,#6080,#6081,#6082,#6083,#6084,#6085,#6086,#6087,#6088,
#6089,#6090,#6091,#6092,#6093,#6094,#6095,#6096,#6097,#6098,#6099,#6100,
#6101,#6102,#6103,#6104,#6105,#6106,#6107,#6108,#6109,#6110,#6111,#6112,
#6113,#6114,#6115,#6116,#6117,#6118,#6119,#6120,#6121,#6122,#6123,#6124,
#6125,#6126,#6127,#6128,#6129,#6130,#6131,#6132,#6133,#6134,#6135,#6136,
#6137,#6138,#6139,#6140,#6141,#6142,#6143,#6144,#6145,#6146,#6147,#6148,
#6149,#6150,#6151,#6152,#6153,#6154,#6155,#6156,#6157,#6158,#6159,#6160,
#6161,#6162,#6163,#6164,#6165,#6166,#6167,#6168,#6169,#6170,#6171,#6172,
#6173,#6174,#6175,#6176,#6177,#6178,#6179,#6180,#6181,#6182,#6183,#6184,
#6185,#6186,#6187,#6188,#6189,#6190,#6191,#6192,#6193,#6194,#6195,#6196,
#6197,#6198,#6199,#6200,#6201,#6202,#6203,#6204,#6205,#6206,#6207,#6208,
#6209,#6210,#6211,#6212,#6213,#6214,#6215,#6216,#6217,#6218,#6219,#6220,
#6221,#6222,#6223,#6224,#6225,#6226,#6227,#6228,#6229,#6230,#6231,#6232,
#6233,#6234,#6235,#6236,#6237,#6238,#6239,#6240,#6241,#6242,#6243,#6244,
#6245,#6246,#6247,#6248,#6249,#6250,#6251,#6252,#6253,#6254,#6255,#6256,
#6257,#6258,#6259,#6260,#6261,#6262,#6263,#6264,#6265,#6266,#6267,#6268,
#6269,#6270,#6271,#6272,#6273,#6274,#6275,#6276,#6277,#6278,#6279,#6280,
#6281,#6282,#6283,#6284,#6285,#6286,#6287,#6288,#6289,#6290,#6291,#6292),
 .UNSPECIFIED.,.F.,.F.,(4,2,2,2,2,2,2,2,2,2,2,2,2,2,2,2,2,2,2,2,2,2,2,2,
2,2,2,2,2,2,2,2,2,2,2,2,2,2,2,2,2,2,2,2,2,2,2,2,2,2,2,2,2,2,2,2,2,2,2,2,
2,2,2,2,2,2,2,2,2,2,2,2,2,2,2,2,2,2,2,2,2,2,2,2,2,2,2,2,2,2,2,2,2,2,2,2,
2,2,2,2,2,2,2,2,2,2,2,2,2,2,4),(0.708678555662593,0.748782942643991,0.772922702532529,
0.780095352477205,0.784622173095557,0.788837082782898,0.794340571426341,
0.806601129882489,0.879417765593598,0.920425270664686,0.933095479641559,
0.941685625067459,0.94508716036817,0.947483975195023,0.949730252618617,
0.953555287368893,0.964101507653615,1.03042803317628,1.09240834791634,1.10151067405403,
1.10648471987993,1.11026484485518,1.1151165806436,1.12342447751245,1.15833689535541,
1.22663825629169,1.25999084264512,1.26525775098546,1.2680737677987,1.27043189604108,
1.27340843871699,1.2781448522497,1.30506424409905,1.33021297985093,1.36941582660573,
1.4143362359503,1.42235477472665,1.4275520376078,1.43174678235489,1.4365514636124,
1.4448924915533,1.48422852283635,1.52766876700422,1.57769265420215,1.5857982001687,
1.58890037360076,1.59112443660229,1.59355292734,1.59707265337207,1.60633841131265,
1.62034442202954,1.71955623966095,1.74030455069573,1.74736738309538,1.75188820093921,
1.75614231277469,1.76186267717969,1.77489705735033,1.7928118823639,1.8445755689971,
1.9001802182269,1.90821351613968,1.91130419222833,1.91352378887723,1.91595594649535,
1.91948892928184,1.92883239688369,1.94299463293385,2.04629108962734,2.06368208733208,
2.07028352174064,2.07426716567051,2.07852483246027,2.08424224073038,2.09723661782448,
2.11507613799312,2.16645374092106,2.22240976487947,2.2304379643149,2.23353035380687,
2.23575250962831,2.23818555558296,2.24172256417779,2.2510954368527,2.26531900898129,
2.31594572969656,2.37542367057146,2.3877449062705,2.39291475139969,2.39720189867906,
2.40150899436374,2.40776452549063,2.41492935379913,2.42792507971324,2.45870700168226,
2.52522355114272,2.54931724224462,2.55434447079601,2.55713212681062,2.55948361544353,
2.56247162777653,2.5686227413984,2.62051316394283,2.68786101994759,2.70728249431015,
2.71416416296146,2.718647805993,2.72264393838857,2.72680812058983,2.73206999633021,
2.73781577962203),.UNSPECIFIED.);
#1172=B_SPLINE_CURVE_WITH_KNOTS('',3,(#6297,#6298,#6299,#6300,#6301,#6302,
#6303,#6304,#6305,#6306,#6307,#6308,#6309,#6310,#6311,#6312,#6313,#6314,
#6315,#6316,#6317,#6318,#6319,#6320,#6321,#6322,#6323,#6324,#6325,#6326,
#6327,#6328,#6329,#6330,#6331,#6332,#6333,#6334,#6335,#6336,#6337,#6338,
#6339,#6340,#6341,#6342,#6343,#6344,#6345,#6346,#6347,#6348,#6349,#6350,
#6351,#6352,#6353,#6354,#6355,#6356,#6357,#6358,#6359,#6360,#6361,#6362,
#6363,#6364,#6365,#6366,#6367,#6368,#6369,#6370,#6371,#6372,#6373,#6374,
#6375,#6376,#6377,#6378,#6379,#6380,#6381,#6382,#6383,#6384,#6385,#6386,
#6387,#6388,#6389,#6390,#6391,#6392,#6393,#6394,#6395,#6396,#6397,#6398,
#6399,#6400,#6401,#6402,#6403,#6404,#6405,#6406,#6407,#6408,#6409,#6410,
#6411,#6412,#6413,#6414,#6415,#6416,#6417,#6418,#6419,#6420,#6421,#6422,
#6423,#6424,#6425,#6426,#6427,#6428,#6429,#6430,#6431,#6432,#6433,#6434,
#6435,#6436,#6437,#6438,#6439,#6440,#6441,#6442,#6443,#6444,#6445,#6446,
#6447,#6448,#6449,#6450,#6451,#6452,#6453,#6454,#6455,#6456,#6457,#6458,
#6459,#6460,#6461,#6462,#6463,#6464,#6465,#6466,#6467,#6468,#6469,#6470,
#6471,#6472,#6473,#6474,#6475,#6476,#6477,#6478,#6479,#6480,#6481,#6482,
#6483,#6484,#6485,#6486,#6487,#6488,#6489,#6490,#6491,#6492,#6493,#6494,
#6495,#6496,#6497,#6498,#6499,#6500,#6501,#6502,#6503,#6504),
 .UNSPECIFIED.,.F.,.F.,(4,3,3,3,3,3,3,3,3,3,3,3,3,3,3,3,3,3,3,3,3,3,3,3,
3,3,3,3,3,3,3,3,3,3,3,3,3,3,3,3,3,3,3,3,3,3,3,3,3,3,3,3,3,3,3,3,3,3,3,3,
3,3,3,3,3,3,3,3,3,4),(122.522113490002,122.617599580213,122.713164379506,
122.808908483514,122.904747907257,123.000792413016,123.067579548509,123.160674799028,
123.253644383959,123.346515905981,123.439319982668,123.532089169703,123.62484826403,
123.717622047648,123.810494779077,123.903419487396,123.99649841021,124.065430390237,
124.158526248507,124.251496449195,124.344368594077,124.43717330165,124.529943124285,
124.62270285815,124.715477284468,124.808350659465,124.901276012828,124.994355576363,
125.063281231964,125.156373615804,125.249340333502,125.342208991388,125.435010220104,
125.527776569966,125.62053284117,125.713303818973,125.806173788477,125.899095754988,
125.992171997024,126.061132073691,126.154229448072,126.247201144654,126.340074763607,
126.432880906914,126.525652141348,126.618413261588,126.711189047344,126.80406373209,
126.896990369618,126.990071162611,127.058982915419,127.152082698318,127.2450568592,
127.337932994276,127.430741720436,127.523515577764,127.616279357587,127.709057836291,
127.801935248434,127.894864636703,127.98794818957,128.056833757146,128.150391887151,
128.242254602021,128.334030345778,128.425745111084,128.520633532608,128.612328933846,
128.708813865514,128.805298797182),.UNSPECIFIED.);
#1173=B_SPLINE_CURVE_WITH_KNOTS('',3,(#6505,#6506,#6507,#6508,#6509,#6510,
#6511,#6512,#6513,#6514,#6515,#6516,#6517,#6518,#6519,#6520,#6521,#6522,
#6523,#6524,#6525,#6526,#6527,#6528,#6529,#6530,#6531,#6532,#6533,#6534,
#6535,#6536,#6537,#6538,#6539,#6540,#6541,#6542,#6543,#6544,#6545,#6546,
#6547,#6548,#6549,#6550,#6551,#6552,#6553,#6554,#6555,#6556,#6557,#6558,
#6559,#6560,#6561,#6562,#6563,#6564,#6565,#6566,#6567,#6568,#6569,#6570,
#6571,#6572,#6573,#6574,#6575,#6576,#6577,#6578,#6579,#6580,#6581,#6582,
#6583,#6584,#6585,#6586,#6587,#6588,#6589,#6590,#6591,#6592,#6593,#6594,
#6595,#6596,#6597,#6598,#6599,#6600,#6601,#6602,#6603,#6604,#6605,#6606,
#6607,#6608,#6609,#6610,#6611,#6612,#6613,#6614,#6615,#6616,#6617,#6618,
#6619,#6620,#6621,#6622,#6623,#6624,#6625,#6626,#6627,#6628,#6629,#6630,
#6631,#6632,#6633,#6634,#6635,#6636,#6637,#6638,#6639,#6640,#6641,#6642,
#6643,#6644,#6645,#6646,#6647,#6648,#6649,#6650,#6651,#6652,#6653,#6654,
#6655,#6656,#6657,#6658,#6659,#6660,#6661,#6662,#6663,#6664,#6665,#6666,
#6667,#6668,#6669,#6670,#6671,#6672,#6673,#6674,#6675,#6676,#6677,#6678,
#6679,#6680,#6681,#6682,#6683,#6684,#6685,#6686,#6687,#6688,#6689,#6690,
#6691,#6692,#6693,#6694,#6695,#6696,#6697,#6698,#6699,#6700,#6701,#6702),
 .UNSPECIFIED.,.F.,.F.,(4,2,2,2,2,2,2,2,2,2,2,2,2,2,2,2,2,2,2,2,2,2,2,2,
2,2,2,2,2,2,2,2,2,2,2,2,2,2,2,2,2,2,2,2,2,2,2,2,2,2,2,2,2,2,2,2,2,2,2,2,
2,2,2,2,2,2,2,2,2,2,2,2,2,2,2,2,2,2,2,2,2,2,2,2,2,2,2,2,2,2,2,2,2,2,2,2,
2,2,4),(0.00123641856443392,0.0677816156057305,0.128275151421882,0.137946939738651,
0.141528241670278,0.143970738293946,0.14618430044594,0.149243239419923,
0.157056842957665,0.218570542838502,0.279998979667933,0.290193460988853,
0.296257860872615,0.301545558887788,0.305639497662884,0.310133741016137,
0.317052529516095,0.336668786541449,0.437223046630292,0.451284103375782,
0.460580309110921,0.464107503933,0.466539726717936,0.468764759148168,0.4718672993043,
0.47996441925814,0.530841491770515,0.575776038492868,0.612972332189931,
0.62119311238409,0.625971368883615,0.630168539259352,0.635402123184994,
0.643540808168967,0.691935516511364,0.75647883328083,0.780328918877284,
0.785180678060024,0.787901045940586,0.790263163023318,0.793301829823471,
0.798361056364487,0.837991832148,0.893690639457914,0.921031188758042,0.933036913526042,
0.942580054022896,0.947640018094949,0.951419275461906,0.956181594110284,
0.9643290701301,0.995623213593347,1.07657046313531,1.10255582368811,1.10751815313142,
1.11026257949089,1.11262127136096,1.11567523096426,1.12067523167856,1.15504229037769,
1.20711992232119,1.25238046297746,1.26385821622653,1.2693020636188,1.2735217222203,
1.27817542647944,1.28582475963549,1.31167030776758,1.38073826029963,1.42406510506264,
1.42955817615089,1.43241513397301,1.4347656444174,1.43767859840649,1.44326654188307,
1.49039135801682,1.57456582415384,1.58624280399073,1.59172382345238,1.59594798814397,
1.60058232592772,1.60814419958438,1.6331784212617,1.7029498735112,1.74654194398789,
1.75203912186308,1.7548967987899,1.75724712215969,1.76015887297431,1.76574176004426,
1.80897166316429,1.89351458394855,1.90760243040227,1.9135061885,1.91779649706356,
1.92173660333723,1.9270749532319,1.94036234462692,2.03158365045162),
 .UNSPECIFIED.);
#1174=B_SPLINE_CURVE_WITH_KNOTS('',3,(#6707,#6708,#6709,#6710,#6711,#6712,
#6713,#6714,#6715,#6716,#6717,#6718,#6719,#6720,#6721,#6722,#6723,#6724,
#6725,#6726,#6727,#6728,#6729,#6730,#6731,#6732,#6733,#6734,#6735,#6736,
#6737,#6738,#6739,#6740,#6741,#6742,#6743,#6744,#6745,#6746,#6747,#6748,
#6749,#6750,#6751,#6752,#6753,#6754,#6755,#6756,#6757,#6758,#6759,#6760,
#6761,#6762,#6763,#6764,#6765,#6766,#6767,#6768,#6769,#6770,#6771,#6772,
#6773,#6774,#6775,#6776,#6777,#6778,#6779,#6780,#6781,#6782,#6783,#6784,
#6785,#6786,#6787,#6788,#6789,#6790,#6791,#6792,#6793,#6794,#6795,#6796,
#6797,#6798,#6799,#6800,#6801,#6802,#6803,#6804,#6805,#6806,#6807,#6808,
#6809,#6810,#6811,#6812,#6813,#6814,#6815,#6816,#6817,#6818,#6819,#6820,
#6821,#6822,#6823,#6824,#6825,#6826,#6827,#6828,#6829,#6830,#6831,#6832,
#6833,#6834,#6835,#6836,#6837,#6838,#6839,#6840,#6841,#6842,#6843,#6844,
#6845,#6846,#6847,#6848,#6849,#6850,#6851,#6852,#6853,#6854,#6855,#6856,
#6857,#6858,#6859,#6860,#6861,#6862,#6863,#6864,#6865,#6866,#6867,#6868,
#6869,#6870,#6871,#6872,#6873,#6874,#6875,#6876,#6877,#6878,#6879,#6880,
#6881,#6882,#6883,#6884,#6885,#6886,#6887,#6888,#6889,#6890,#6891,#6892,
#6893,#6894,#6895,#6896,#6897,#6898,#6899,#6900,#6901,#6902,#6903,#6904,
#6905,#6906,#6907,#6908,#6909,#6910,#6911,#6912,#6913,#6914,#6915,#6916,
#6917,#6918,#6919,#6920,#6921,#6922,#6923,#6924,#6925,#6926,#6927,#6928,
#6929,#6930,#6931,#6932,#6933,#6934,#6935,#6936,#6937,#6938,#6939,#6940,
#6941,#6942),.UNSPECIFIED.,.F.,.F.,(4,2,2,2,2,2,2,2,2,2,2,2,2,2,2,2,2,2,
2,2,2,2,2,2,2,2,2,2,2,2,2,2,2,2,2,2,2,2,2,2,2,2,2,2,2,2,2,2,2,2,2,2,2,2,
2,2,2,2,2,2,2,2,2,2,2,2,2,2,2,2,2,2,2,2,2,2,2,2,2,2,2,2,2,2,2,2,2,2,2,2,
2,2,2,2,2,2,2,2,2,2,2,2,2,2,2,2,2,2,2,2,2,2,2,2,2,2,2,4),(2.03108651980245,
2.05799265149469,2.12022779959758,2.13280091659172,2.13838566411232,2.14264032252365,
2.14718848448666,2.15435057938612,2.17804302546848,2.21953691392989,2.2851851115457,
2.29643757141376,2.3003626107332,2.30262921761593,2.30503146641448,2.30839460671581,
2.31663008999095,2.32858413587513,2.3655895006738,2.44383965386118,2.45567389466241,
2.46112605643676,2.46536013406124,2.46996631871562,2.47739489346602,2.5038223780982,
2.58643101373637,2.5939915804093,2.61693084811006,2.62189421505243,2.62466958514322,
2.62702560706743,2.63003853925066,2.63630514543607,2.6446735412035,2.66578274271971,
2.7305193536904,2.77138561500042,2.78002044516204,2.78494119648462,2.78871099010059,
2.79359435595854,2.80229571390002,2.8495413206444,2.89369677964559,2.93833062799393,
2.94391661959199,2.94682964123487,2.94918079590174,2.95203926479678,2.95753739424577,
3.00106613708808,3.07064583680315,3.09594198397455,3.10355172644917,3.1081975190175,
3.11242049617677,3.11788347674092,3.12945850297983,3.17547889411409,3.25358170137673,
3.26417671435543,3.26800972103492,3.27025823001799,3.27267261447915,3.27610347803792,
3.28476335177624,3.29754519120734,3.33908300070259,3.41064487986249,3.42296360826239,
3.42850329251727,3.43275070222199,3.43731755540097,3.44456568238514,3.46910560663978,
3.51299631491247,3.58034611516104,3.58781290348878,3.59081401570421,3.59301361805139,
3.59547465500316,3.59914113953224,3.60941127504253,3.62552207277897,3.69127031919621,
3.73844657849807,3.7472498644596,3.75224604997061,3.75633439896778,3.75647026840979,
3.7565914756702,3.7567004332773,3.75679903302306,3.75688878269824,3.75697090112621,
3.75704638582414,3.75711606218003,3.75718061986786,3.75724064024039,3.75729661724579,
3.75734897358605,3.75739807338706,3.75744423221015,3.7574877250313,3.76272154697002,
3.76857235197011,3.80273549208015,3.88986596894535,3.90764897091345,3.91229014690864,
3.91496522864601,3.91733787376142,3.92050902815266,3.92762182229513,3.95877841656303,
4.05167384684634,4.06186733040656),.UNSPECIFIED.);
#1175=B_SPLINE_CURVE_WITH_KNOTS('',3,(#6944,#6945,#6946,#6947,#6948,#6949,
#6950,#6951,#6952,#6953,#6954,#6955,#6956,#6957,#6958,#6959,#6960,#6961,
#6962,#6963,#6964,#6965,#6966,#6967,#6968,#6969,#6970,#6971,#6972,#6973,
#6974,#6975,#6976,#6977,#6978,#6979,#6980,#6981,#6982,#6983,#6984,#6985,
#6986,#6987,#6988,#6989,#6990,#6991,#6992,#6993,#6994,#6995,#6996,#6997,
#6998,#6999,#7000,#7001,#7002,#7003,#7004,#7005,#7006,#7007,#7008,#7009,
#7010,#7011,#7012,#7013,#7014,#7015,#7016,#7017,#7018,#7019,#7020,#7021,
#7022,#7023,#7024,#7025,#7026,#7027,#7028,#7029,#7030,#7031,#7032,#7033,
#7034,#7035,#7036,#7037,#7038,#7039,#7040,#7041,#7042,#7043,#7044,#7045,
#7046,#7047,#7048,#7049,#7050,#7051,#7052,#7053,#7054,#7055,#7056,#7057,
#7058,#7059,#7060,#7061,#7062,#7063,#7064,#7065,#7066,#7067,#7068,#7069,
#7070,#7071,#7072,#7073,#7074,#7075,#7076,#7077,#7078,#7079,#7080,#7081,
#7082,#7083,#7084,#7085,#7086,#7087,#7088,#7089,#7090,#7091,#7092,#7093,
#7094,#7095,#7096,#7097,#7098,#7099,#7100,#7101,#7102,#7103,#7104,#7105,
#7106,#7107,#7108,#7109,#7110,#7111,#7112,#7113,#7114,#7115,#7116,#7117,
#7118,#7119,#7120,#7121,#7122,#7123,#7124,#7125,#7126,#7127,#7128,#7129,
#7130,#7131,#7132,#7133,#7134,#7135,#7136,#7137,#7138,#7139,#7140,#7141,
#7142,#7143,#7144,#7145,#7146,#7147,#7148,#7149,#7150,#7151,#7152,#7153,
#7154,#7155,#7156,#7157,#7158,#7159,#7160,#7161,#7162,#7163,#7164,#7165,
#7166,#7167,#7168,#7169,#7170,#7171,#7172,#7173,#7174,#7175),
 .UNSPECIFIED.,.F.,.F.,(4,2,2,2,2,2,2,2,2,2,2,2,2,2,2,2,2,2,2,2,2,2,2,2,
2,2,2,2,2,2,2,2,2,2,2,2,2,2,2,2,2,2,2,2,2,2,2,2,2,2,2,2,2,2,2,2,2,2,2,2,
2,2,2,2,2,2,2,2,2,2,2,2,2,2,2,2,2,2,2,2,2,2,2,2,2,2,2,2,2,2,2,2,2,2,2,2,
2,2,2,2,2,2,2,2,2,2,2,2,2,2,2,2,2,2,2,4),(2.03158365045162,2.03183675089734,
2.06897030236158,2.07399098085856,2.07701850502147,2.07937954312591,2.082107541352,
2.08699405146832,2.11148236435685,2.16020461862623,2.22359754250598,2.23183653410937,
2.23710059476907,2.2413005264641,2.24605865805253,2.25418651919738,2.28984290371337,
2.33646636594381,2.3872900328422,2.39539640596704,2.39850011741762,2.40072545712093,
2.40315719251953,2.40668257234865,2.4159675873056,2.4300075298418,2.529914816234,
2.55011836158748,2.55711357394152,2.56162399496799,2.56589181759944,2.57166710887943,
2.58499216572997,2.60342550996571,2.65793042469855,2.70975742918681,2.71786190655743,
2.72096500311263,2.72318992883676,2.72562124732132,2.72914607433902,2.73842992547275,
2.75246836338354,2.85238251094338,2.87256207215379,2.87955341047536,2.88406246614374,
2.88832980652235,2.89410570493662,2.90743791101066,2.92588523826528,2.98047520506316,
2.98687273272193,2.99481874662263,3.03610760752572,3.04118537409018,3.04422889829452,
3.04659085343359,3.04930640850465,3.05413875698219,3.07765901654107,3.14017539615574,
3.19085513967979,3.19905005646943,3.20429960775176,3.2084966863313,3.21326095229262,
3.22142274467525,3.25767145160014,3.30594907640004,3.3276664585342,3.3382294314538,
3.35954925307577,3.36440701164568,3.36715706696493,3.36951370721529,3.3725560864371,
3.378983245884,3.38763078850444,3.40981333119848,3.47861236186263,3.49681523815673,
3.5170195076196,3.52401359453024,3.52852293837773,3.53278949060702,3.53856267218446,
3.55188108078516,3.57030396294056,3.62476447447846,3.67663637613913,3.68472341817868,
3.68782359383213,3.69004736014268,3.6924784999807,3.69565918182362,3.70382309162939,
3.71574036153947,3.7525734065989,3.8309973652987,3.8428000361503,3.84824369450076,
3.85247367225165,3.857077907669,3.86450890964671,3.89100794484308,3.93192639663793,
3.97074509242552,4.00307608630314,4.00800307102287,4.01103443792538,4.01338994254457,
4.0156162905569,4.01834914861004,4.02245881606929,4.06089890765304),
 .UNSPECIFIED.);
#1176=B_SPLINE_CURVE_WITH_KNOTS('',3,(#7176,#7177,#7178,#7179),
 .UNSPECIFIED.,.F.,.F.,(4,4),(0.00110109624755596,0.0013400475596189),
 .UNSPECIFIED.);
#1177=B_SPLINE_CURVE_WITH_KNOTS('',3,(#7185,#7186,#7187,#7188),
 .UNSPECIFIED.,.F.,.F.,(4,4),(4.06225937330911,4.06250570235455),
 .UNSPECIFIED.);
#1178=B_SPLINE_CURVE_WITH_KNOTS('',3,(#7189,#7190,#7191,#7192,#7193,#7194,
#7195,#7196,#7197,#7198,#7199,#7200,#7201,#7202,#7203,#7204,#7205,#7206,
#7207,#7208,#7209,#7210,#7211,#7212,#7213,#7214,#7215,#7216,#7217,#7218,
#7219,#7220,#7221,#7222,#7223,#7224,#7225,#7226,#7227,#7228,#7229,#7230,
#7231,#7232,#7233,#7234,#7235,#7236,#7237,#7238,#7239,#7240,#7241,#7242,
#7243,#7244,#7245,#7246,#7247,#7248,#7249,#7250,#7251,#7252,#7253,#7254,
#7255,#7256,#7257,#7258,#7259,#7260,#7261,#7262,#7263,#7264,#7265,#7266,
#7267,#7268,#7269,#7270,#7271,#7272,#7273,#7274,#7275,#7276,#7277,#7278,
#7279,#7280,#7281,#7282,#7283,#7284,#7285,#7286,#7287,#7288,#7289,#7290,
#7291,#7292,#7293,#7294,#7295,#7296,#7297,#7298,#7299,#7300,#7301,#7302,
#7303,#7304,#7305,#7306,#7307,#7308,#7309,#7310,#7311,#7312,#7313,#7314,
#7315,#7316,#7317,#7318,#7319,#7320,#7321,#7322,#7323,#7324,#7325,#7326,
#7327,#7328,#7329,#7330,#7331,#7332,#7333,#7334,#7335,#7336,#7337,#7338,
#7339,#7340,#7341,#7342,#7343,#7344,#7345,#7346,#7347,#7348,#7349,#7350,
#7351,#7352,#7353,#7354,#7355,#7356,#7357,#7358,#7359,#7360,#7361,#7362,
#7363,#7364,#7365,#7366,#7367,#7368,#7369,#7370,#7371,#7372,#7373,#7374,
#7375,#7376,#7377,#7378,#7379,#7380,#7381,#7382,#7383,#7384,#7385,#7386,
#7387,#7388,#7389,#7390,#7391,#7392,#7393,#7394,#7395,#7396,#7397,#7398,
#7399,#7400,#7401,#7402,#7403,#7404,#7405,#7406,#7407,#7408,#7409,#7410,
#7411,#7412,#7413,#7414,#7415,#7416,#7417,#7418,#7419,#7420,#7421,#7422,
#7423,#7424,#7425,#7426,#7427,#7428,#7429,#7430,#7431,#7432,#7433,#7434,
#7435,#7436,#7437,#7438,#7439,#7440,#7441,#7442,#7443,#7444,#7445,#7446,
#7447,#7448,#7449,#7450,#7451,#7452,#7453,#7454,#7455,#7456,#7457,#7458,
#7459,#7460,#7461,#7462,#7463,#7464,#7465,#7466,#7467,#7468,#7469,#7470,
#7471,#7472,#7473,#7474,#7475,#7476,#7477,#7478,#7479,#7480,#7481,#7482,
#7483,#7484,#7485,#7486,#7487,#7488,#7489,#7490,#7491,#7492,#7493,#7494,
#7495,#7496,#7497,#7498,#7499,#7500,#7501,#7502,#7503,#7504,#7505,#7506,
#7507,#7508),.UNSPECIFIED.,.F.,.F.,(4,2,2,2,2,2,2,2,2,2,2,2,2,2,2,2,2,2,
2,2,2,2,2,2,2,2,2,2,2,2,2,2,2,2,2,2,2,2,2,2,2,2,2,2,2,2,2,2,2,2,2,2,2,2,
2,2,2,2,2,2,2,2,2,2,2,2,2,2,2,2,2,2,2,2,2,2,2,2,2,2,2,2,2,2,2,2,2,2,2,2,
2,2,2,2,2,2,2,2,2,2,2,2,2,2,2,2,2,2,2,2,2,2,2,2,2,2,2,2,2,2,2,2,2,2,2,2,
2,2,2,2,2,2,2,2,2,2,2,2,2,2,2,2,2,2,2,2,2,2,2,2,2,2,2,2,2,2,2,2,2,4),(0.00111869507802623,
0.0346707320864722,0.0393382984862259,0.0423002843642449,0.0445921219449508,
0.0469465709571225,0.0497252332677127,0.0547067207279609,0.0779540567567848,
0.0848654127461771,0.123089164967028,0.155224727930418,0.192594780075219,
0.200825434674942,0.205605754085145,0.209802549278348,0.215032804565348,
0.223160794066955,0.271225141539507,0.350686734167333,0.358329923100332,
0.364112921647033,0.367019792324655,0.367028818940242,0.367037942371699,
0.367047163914033,0.367056484873357,0.367065906561771,0.367075430339832,
0.36708505756838,0.36709478960344,0.367104627870344,0.367114573800352,0.367124628862736,
0.367134794526613,0.367145072300748,0.367155463701468,0.367165970298893,
0.367176593658883,0.367187335374079,0.367198197055757,0.367209180388204,
0.367220287056655,0.367231518758393,0.367242877215067,0.367254364191546,
0.367265981493172,0.367277730952031,0.367289614413733,0.367301633790629,
0.367313790977865,0.367326087919605,0.367338526589154,0.367351108976622,
0.36736383714054,0.36737671318693,0.36738973918717,0.367402917310764,0.367416249730712,
0.367429738664116,0.36744338637168,0.367457195127561,0.367471167262364,
0.367485305143567,0.367499611167711,0.367514087747956,0.367528737394157,
0.367543562627308,0.367557153159669,0.36991900206317,0.372954787638147,
0.378004013932083,0.417071762226864,0.473206377051136,0.50062650535798,
0.512655777652281,0.522213721523594,0.527276812784424,0.531424624902641,
0.536320032952254,0.544847722221461,0.583626850929751,0.650048585915722,
0.681730061433135,0.686928400272485,0.689723324232265,0.692076617464239,
0.695061451147228,0.699830213431351,0.727586562803716,0.752413019782802,
0.792282613439576,0.821740748275609,0.834364180248572,0.84429308731521,
0.849432655190175,0.853623545945797,0.858471351220697,0.866788545467634,
0.901978768934724,0.970993838751653,1.00399173699691,1.00923479691719,1.01203929572447,
1.01439203743749,1.01736525159813,1.02209517036967,1.04891824059525,1.07430793646373,
1.10278572509421,1.15330356948103,1.16541989244579,1.1709823748974,1.1752180556021,
1.17925044980252,1.18610111681302,1.20521652883861,1.30640863378967,1.32049618328232,
1.32980574176163,1.33333525671414,1.33576822722659,1.33799340598454,1.34109524928743,
1.34918400312664,1.40218169951785,1.45590326279395,1.47419623269013,1.48744380736369,
1.49320718663859,1.49747434195323,1.5019915630707,1.50901280076575,1.52940562857986,
1.62906833330264,1.64309737918719,1.6523786206395,1.65590417520522,1.65833656065081,
1.66056291784519,1.66366864719864,1.67178442150596,1.72165332070677,1.7682260403789,
1.8048663784259,1.81305642912942,1.81782909927807,1.82202872607258,1.82727507081422,
1.83545247381546,1.88515648076462,1.94854753605004,1.97221739956403,1.9770605184349,
1.97977964637341,1.9821430659936,1.9851864548552,1.9902598483679,2.03084076488749,
2.03108651980245),.UNSPECIFIED.);
#1179=B_SPLINE_CURVE_WITH_KNOTS('',3,(#7509,#7510,#7511,#7512,#7513,#7514,
#7515,#7516,#7517,#7518,#7519,#7520,#7521,#7522,#7523,#7524,#7525,#7526,
#7527,#7528,#7529,#7530,#7531,#7532,#7533,#7534,#7535,#7536,#7537,#7538,
#7539,#7540,#7541,#7542,#7543,#7544,#7545,#7546,#7547,#7548,#7549,#7550,
#7551,#7552,#7553,#7554,#7555,#7556,#7557,#7558,#7559,#7560,#7561,#7562,
#7563,#7564,#7565,#7566,#7567,#7568,#7569,#7570,#7571,#7572,#7573,#7574,
#7575,#7576,#7577,#7578,#7579,#7580,#7581,#7582,#7583,#7584,#7585,#7586,
#7587,#7588,#7589,#7590,#7591,#7592,#7593,#7594,#7595,#7596,#7597,#7598,
#7599,#7600,#7601,#7602,#7603,#7604,#7605,#7606,#7607,#7608,#7609,#7610,
#7611,#7612,#7613,#7614,#7615,#7616,#7617,#7618,#7619,#7620,#7621,#7622,
#7623,#7624,#7625,#7626,#7627,#7628,#7629,#7630,#7631,#7632,#7633,#7634,
#7635,#7636,#7637,#7638,#7639,#7640,#7641,#7642,#7643,#7644,#7645,#7646,
#7647,#7648,#7649,#7650,#7651,#7652,#7653,#7654,#7655,#7656,#7657,#7658,
#7659,#7660,#7661,#7662,#7663,#7664,#7665,#7666,#7667,#7668,#7669,#7670,
#7671,#7672,#7673,#7674,#7675,#7676,#7677,#7678,#7679,#7680,#7681,#7682,
#7683,#7684,#7685,#7686,#7687,#7688,#7689,#7690,#7691,#7692,#7693,#7694,
#7695,#7696,#7697,#7698,#7699,#7700,#7701,#7702,#7703,#7704,#7705,#7706,
#7707,#7708,#7709,#7710,#7711,#7712,#7713,#7714),.UNSPECIFIED.,.F.,.F.,
(4,2,2,2,2,2,2,2,2,2,2,2,2,2,2,2,2,2,2,2,2,2,2,2,2,2,2,2,2,2,2,2,2,2,2,
2,2,2,2,2,2,2,2,2,2,2,2,2,2,2,2,2,2,2,2,2,2,2,2,2,2,2,2,2,2,2,2,2,2,2,2,
2,2,2,2,2,2,2,2,2,2,2,2,2,2,2,2,2,2,2,2,2,2,2,2,2,2,2,2,2,2,2,4),(0.0013400475596189,
0.062460897083141,0.0993597373398082,0.107562023802153,0.112335756122383,
0.116532677378207,0.121770846481562,0.129926168815735,0.178927808864556,
0.20875603014885,0.248554397764219,0.261024162353363,0.269427984894191,
0.272756873678616,0.275189824293852,0.277412762539173,0.280508564309726,
0.288560427938979,0.343586429761991,0.395796527808926,0.422985429972921,
0.430479913709594,0.435098769460633,0.439325828027745,0.444743085260552,
0.456397785439991,0.536240839669448,0.572159194354239,0.583900659867113,
0.592024996633251,0.595368797526696,0.597766652030345,0.600036913335066,
0.603984844683962,0.615414134880948,0.680888801237364,0.722347400740166,
0.746020502164547,0.753177811686764,0.757723098392572,0.761975171508534,
0.767556666693733,0.780123123268052,0.840208382040955,0.903866122695068,
0.913742610437099,0.917353044025897,0.919801444322793,0.922009171465023,
0.925046129469945,0.932730560407458,0.996397258520831,1.04268066625386,
1.06802203388068,1.07534570522573,1.07992716083896,1.08416572511621,1.08966202083245,
1.1017504281087,1.17690339063022,1.21585110749391,1.22816588786884,1.23658699804471,
1.23997879742136,1.24238498237208,1.24464169453353,1.2485212385943,1.2594583820186,
1.33706012708394,1.38311732862221,1.39469266572583,1.40015354195006,1.40437391343766,
1.40901584996815,1.41661700523665,1.4420338676837,1.51144022631826,1.55488841124938,
1.56038158430457,1.56323785579834,1.56558740120547,1.56849865824267,1.57408190781462,
1.61978096423188,1.6297108806708,1.67573076799502,1.71115724135569,1.71926906328463,
1.72402275606319,1.72822176151621,1.73348863542531,1.7417397581883,1.80268619993668,
1.87052589749619,1.8806562375186,1.88430201684389,1.88675762987702,1.88895891486739,
1.89197057409146,1.89958130078598,1.96534875952032,2.03091503449202,2.03102410849652),
 .UNSPECIFIED.);
#1180=B_SPLINE_CURVE_WITH_KNOTS('',3,(#7719,#7720,#7721,#7722,#7723,#7724,
#7725,#7726,#7727,#7728,#7729,#7730,#7731,#7732,#7733,#7734,#7735,#7736,
#7737,#7738,#7739,#7740,#7741,#7742,#7743,#7744,#7745,#7746,#7747,#7748,
#7749,#7750,#7751,#7752,#7753,#7754,#7755,#7756,#7757,#7758,#7759,#7760,
#7761,#7762,#7763,#7764,#7765,#7766,#7767,#7768,#7769,#7770,#7771,#7772,
#7773,#7774,#7775,#7776,#7777,#7778,#7779,#7780,#7781,#7782,#7783,#7784,
#7785,#7786,#7787,#7788,#7789,#7790,#7791,#7792,#7793,#7794,#7795,#7796,
#7797,#7798,#7799,#7800,#7801,#7802,#7803,#7804,#7805,#7806,#7807,#7808,
#7809,#7810,#7811,#7812,#7813,#7814,#7815,#7816,#7817,#7818,#7819,#7820,
#7821,#7822,#7823,#7824,#7825,#7826,#7827,#7828,#7829,#7830,#7831,#7832,
#7833,#7834,#7835,#7836,#7837,#7838,#7839,#7840,#7841,#7842,#7843,#7844,
#7845,#7846,#7847,#7848,#7849,#7850,#7851,#7852,#7853,#7854,#7855,#7856,
#7857,#7858,#7859,#7860,#7861,#7862,#7863,#7864,#7865,#7866,#7867,#7868,
#7869,#7870,#7871,#7872,#7873,#7874,#7875,#7876,#7877,#7878,#7879,#7880,
#7881,#7882,#7883,#7884,#7885,#7886,#7887,#7888,#7889,#7890,#7891,#7892,
#7893,#7894,#7895,#7896,#7897,#7898,#7899,#7900,#7901,#7902,#7903,#7904,
#7905,#7906,#7907,#7908,#7909,#7910,#7911,#7912,#7913,#7914,#7915,#7916,
#7917,#7918,#7919,#7920,#7921,#7922,#7923,#7924,#7925,#7926,#7927,#7928),
 .UNSPECIFIED.,.F.,.F.,(4,2,2,2,2,2,2,2,2,2,2,2,2,2,2,2,2,2,2,2,2,2,2,2,
2,2,2,2,2,2,2,2,2,2,2,2,2,2,2,2,2,2,2,2,2,2,2,2,2,2,2,2,2,2,2,2,2,2,2,2,
2,2,2,2,2,2,2,2,2,2,2,2,2,2,2,2,2,2,2,2,2,2,2,2,2,2,2,2,2,2,2,2,2,2,2,2,
2,2,2,2,2,2,2,2,4),(2.03190008286785,2.07977363910376,2.13446066374539,
2.144561461824,2.16431389066328,2.1690642552616,2.17179087983579,2.17391586994911,
2.17686909045172,2.18283405403035,2.19068941942356,2.27050931605199,2.31793496203556,
2.32604351323317,2.33126834329475,2.33546538521858,2.34025097474141,2.3485033876091,
2.3862363833622,2.43076221789267,2.48139102331639,2.48948748698368,2.49259008776981,
2.49481529832414,2.49724768520681,2.50077534327836,2.5100740521279,2.52414157736048,
2.62474370308302,2.64436841281063,2.65128847165212,2.65578306260333,2.66005946684776,
2.66588336640092,2.67949208349358,2.69844192487076,2.80384044773164,2.81209681550401,
2.81522004392104,2.81745068143635,2.81987815567379,2.8233807710882,2.83251193913524,
2.84623812506606,2.89351731596356,2.95736011873939,2.96866060178893,2.97479726756399,
2.9790879741144,2.98348658707277,2.98994844119316,3.00775850881061,3.03501376653203,
3.07685825613384,3.12637204719132,3.1344991864415,3.1376058197589,3.13983203173373,
3.14226331411159,3.14578571886053,3.15504964765729,3.16904624023057,3.26788304988401,
3.28897780356245,3.29608917532169,3.30062496082718,3.30488191909982,3.31058902757393,
3.32351849998876,3.34123900157135,3.4263046039849,3.43347946749547,3.45417033147242,
3.45898695644855,3.46172832064346,3.4640647828861,3.46711018335079,3.47354925991919,
3.48221649964425,3.50447087075489,3.58016178176387,3.60965873108932,3.61765844334337,
3.62238838501746,3.62617171075306,3.63127569604962,3.64103268665636,3.70524630603049,
3.77230139931496,3.77972756596522,3.78272101073167,3.78491813155336,3.78712378737464,
3.79039302266121,3.79843676072109,3.81020757208602,3.84627301351861,3.9259545786378,
3.93763389499367,3.94305624549346,3.94728460289099,3.95190217627877,3.9593885339276,
3.98647823277419,4.06225937330911),.UNSPECIFIED.);
#1181=B_SPLINE_CURVE_WITH_KNOTS('',3,(#7929,#7930,#7931,#7932,#7933,#7934,
#7935,#7936,#7937,#7938,#7939,#7940,#7941,#7942,#7943,#7944,#7945,#7946,
#7947,#7948,#7949,#7950,#7951,#7952,#7953,#7954,#7955,#7956,#7957,#7958,
#7959,#7960,#7961,#7962,#7963,#7964,#7965,#7966,#7967,#7968,#7969,#7970,
#7971,#7972,#7973,#7974,#7975,#7976,#7977,#7978,#7979,#7980,#7981,#7982,
#7983,#7984,#7985,#7986,#7987,#7988,#7989,#7990,#7991,#7992,#7993,#7994,
#7995,#7996,#7997,#7998,#7999,#8000,#8001,#8002,#8003,#8004,#8005,#8006,
#8007,#8008,#8009,#8010,#8011,#8012,#8013,#8014,#8015,#8016,#8017,#8018,
#8019,#8020,#8021,#8022,#8023,#8024,#8025,#8026,#8027,#8028,#8029,#8030,
#8031,#8032,#8033,#8034,#8035,#8036,#8037,#8038,#8039,#8040,#8041,#8042,
#8043,#8044,#8045,#8046,#8047,#8048,#8049,#8050,#8051,#8052,#8053,#8054,
#8055,#8056,#8057,#8058,#8059,#8060,#8061,#8062,#8063,#8064,#8065,#8066,
#8067,#8068,#8069,#8070,#8071,#8072,#8073,#8074,#8075,#8076,#8077,#8078,
#8079,#8080,#8081,#8082,#8083,#8084,#8085,#8086,#8087,#8088,#8089,#8090,
#8091,#8092,#8093,#8094,#8095,#8096,#8097,#8098,#8099,#8100,#8101,#8102,
#8103,#8104,#8105,#8106,#8107,#8108,#8109,#8110,#8111,#8112,#8113,#8114,
#8115,#8116,#8117,#8118,#8119,#8120,#8121,#8122,#8123,#8124,#8125,#8126,
#8127,#8128,#8129,#8130,#8131,#8132,#8133,#8134,#8135,#8136,#8137,#8138,
#8139,#8140,#8141,#8142,#8143,#8144,#8145,#8146),.UNSPECIFIED.,.F.,.F.,
(4,2,2,2,2,2,2,2,2,2,2,2,2,2,2,2,2,2,2,2,2,2,2,2,2,2,2,2,2,2,2,2,2,2,2,
2,2,2,2,2,2,2,2,2,2,2,2,2,2,2,2,2,2,2,2,2,2,2,2,2,2,2,2,2,2,2,2,2,2,2,2,
2,2,2,2,2,2,2,2,2,2,2,2,2,2,2,2,2,2,2,2,2,2,2,2,2,2,2,2,2,2,2,2,2,2,2,2,
2,4),(2.03102410849652,2.03956001958603,2.04494502964436,2.04915612514696,
2.05383829019968,2.06162328646331,2.0923457163036,2.15849044276081,2.19930894983273,
2.20438168325408,2.2074238021063,2.20978567501983,2.21250231315925,2.21733935844911,
2.24094137470707,2.30395272082228,2.35407602431123,2.36225920440289,2.36750529867725,
2.37170221323921,2.37646909037772,2.38464238161448,2.42107760980727,2.46988313640751,
2.49521368967327,2.52217724186554,2.52691123800625,2.52988497017717,2.53223670976782,
2.53503829881938,2.54027140563818,2.57301583289198,2.6418034164573,2.67744879076333,
2.68579250804491,2.69064489391482,2.69483323608056,2.69996144464477,2.70984222298223,
2.72238862327668,2.75158321810497,2.79167779618078,2.81589587792283,2.84427688193517,
2.84906914118907,2.85206028642371,2.85441290132757,2.85720030294585,2.86236722664191,
2.89322246417659,2.93703971901881,2.99842501694261,3.00664819113256,3.01190607744833,
3.01610358928176,3.02086166448348,3.02899613349939,3.0648067240458,3.11187343865224,
3.16202177648116,3.17011789054082,3.17321920968406,3.17544321365416,3.17787393490828,
3.18139857862447,3.19068586740167,3.20473294144917,3.30494861826134,3.32484325360536,
3.33179613451347,3.33629593100398,3.34056567539944,3.34636228058863,3.35982255192645,
3.37850464596329,3.47793378420726,3.49103774008786,3.49519952982131,3.49776699663231,
3.50017547725813,3.50358296369839,3.51210636104867,3.52462352413051,3.56469247098305,
3.5943776452994,3.64320785512963,3.65135655874794,3.65659181986569,3.66078730369643,
3.66556036427294,3.67333669735231,3.7025768799795,3.76442289533049,3.81059529882349,
3.81617716488816,3.81908779863048,3.8214368914524,3.82429266854063,3.82952495521428,
3.86264196085627,3.91453396581379,3.96533475118296,3.9735313397,3.9787811118797,
3.98297782358756,3.98774108898918,3.99269916895108,4.00019602089878,4.06019991115425),
 .UNSPECIFIED.);
#1182=B_SPLINE_CURVE_WITH_KNOTS('',3,(#8151,#8152,#8153,#8154,#8155,#8156,
#8157,#8158,#8159,#8160,#8161,#8162,#8163,#8164,#8165,#8166,#8167,#8168,
#8169,#8170,#8171,#8172,#8173,#8174,#8175,#8176,#8177,#8178,#8179,#8180,
#8181,#8182,#8183,#8184,#8185,#8186,#8187,#8188,#8189,#8190,#8191,#8192,
#8193,#8194,#8195,#8196,#8197,#8198,#8199,#8200,#8201,#8202,#8203,#8204,
#8205,#8206,#8207,#8208,#8209,#8210,#8211,#8212,#8213,#8214,#8215,#8216,
#8217,#8218,#8219,#8220,#8221,#8222,#8223,#8224,#8225,#8226,#8227,#8228,
#8229,#8230,#8231,#8232,#8233,#8234,#8235,#8236,#8237,#8238,#8239,#8240,
#8241,#8242,#8243,#8244,#8245,#8246,#8247,#8248,#8249,#8250,#8251,#8252,
#8253,#8254,#8255,#8256,#8257,#8258,#8259,#8260,#8261,#8262,#8263,#8264,
#8265,#8266,#8267,#8268,#8269,#8270,#8271,#8272,#8273,#8274,#8275,#8276,
#8277,#8278,#8279,#8280,#8281,#8282,#8283,#8284,#8285,#8286,#8287,#8288,
#8289,#8290,#8291,#8292,#8293,#8294,#8295,#8296,#8297,#8298,#8299,#8300,
#8301,#8302,#8303,#8304,#8305,#8306,#8307,#8308,#8309,#8310,#8311,#8312,
#8313,#8314,#8315,#8316,#8317,#8318,#8319,#8320,#8321,#8322,#8323,#8324,
#8325,#8326,#8327,#8328,#8329,#8330,#8331,#8332,#8333,#8334,#8335,#8336,
#8337,#8338,#8339,#8340,#8341,#8342,#8343,#8344,#8345,#8346,#8347,#8348,
#8349,#8350,#8351,#8352,#8353,#8354,#8355,#8356,#8357,#8358,#8359,#8360,
#8361,#8362,#8363,#8364,#8365,#8366,#8367,#8368,#8369,#8370),
 .UNSPECIFIED.,.F.,.F.,(4,2,2,2,2,2,2,2,2,2,2,2,2,2,2,2,2,2,2,2,2,2,2,2,
2,2,2,2,2,2,2,2,2,2,2,2,2,2,2,2,2,2,2,2,2,2,2,2,2,2,2,2,2,2,2,2,2,2,2,2,
2,2,2,2,2,2,2,2,2,2,2,2,2,2,2,2,2,2,2,2,2,2,2,2,2,2,2,2,2,2,2,2,2,2,2,2,
2,2,2,2,2,2,2,2,2,2,2,2,2,4),(0.00130988952596835,0.0573674019543287,0.0650598693452133,
0.070099528425691,0.0749205816804568,0.0791131909454157,0.0842866522297215,
0.0922281214241368,0.135080471076808,0.169959837947393,0.222962547915876,
0.231969975323028,0.235498218217464,0.237930400164034,0.240154928260367,
0.243255956739319,0.251343268609958,0.304289159884606,0.311753615946756,
0.359968175821831,0.377181560599029,0.389738872619975,0.395230142819384,
0.399504920928421,0.404002469072135,0.410936548051482,0.430668585815097,
0.531087240987262,0.545143147082112,0.554436804479322,0.557963568358079,
0.560395678679199,0.562620897863997,0.565723880097549,0.573823682389663,
0.62625816110239,0.680372592547324,0.698736546604477,0.712022760612445,
0.717792138967529,0.722059680352674,0.726573572468589,0.733581938031989,
0.753880900196495,0.853633052030626,0.867663827799383,0.876945472320145,
0.880470693852264,0.88290269550838,0.885128577912581,0.8882334838035,0.896345874885187,
0.946250153616599,0.993570979887993,1.02948690398614,1.03763186603329,1.04239416831188,
1.04659425747777,1.05185385447603,1.06007667833684,1.12140113878597,1.17501470565662,
1.18966304777984,1.19924408653291,1.20281317138764,1.2052538702163,1.20747067408061,
1.21054081957405,1.21841899930135,1.27877304694429,1.32727236713757,1.34454583447853,
1.35722390976516,1.36288755631765,1.36713843368776,1.37113991173009,1.37782836943332,
1.39579746872806,1.49841056385381,1.51255130733836,1.521886918665,1.52542037745119,
1.52785419710441,1.5300786626776,1.53317756424001,1.54124444626687,1.59598467826236,
1.6484309151698,1.67569421819001,1.68319782892231,1.6878201898786,1.69204906363819,
1.69746673126553,1.70911472469393,1.78909679388562,1.83987945120788,1.84586310434081,
1.84882021507066,1.85094578598968,1.85367005151241,1.85840946591991,1.87800963932858,
1.88828271382747,1.97181547965497,1.99837075662635,2.0058105219466,2.01041879466552,
2.01465155583869,2.02009751099426,2.03190008286785),.UNSPECIFIED.);
#1183=B_SPLINE_CURVE_WITH_KNOTS('',3,(#8372,#8373,#8374,#8375),
 .UNSPECIFIED.,.F.,.F.,(4,4),(4.06019991115425,4.06049199751014),
 .UNSPECIFIED.);
#1184=B_SPLINE_CURVE_WITH_KNOTS('',3,(#8376,#8377,#8378,#8379,#8380,#8381,
#8382,#8383,#8384,#8385,#8386,#8387,#8388,#8389,#8390,#8391,#8392,#8393,
#8394,#8395,#8396,#8397,#8398,#8399,#8400,#8401,#8402,#8403,#8404,#8405,
#8406,#8407,#8408,#8409,#8410,#8411,#8412,#8413,#8414,#8415,#8416,#8417,
#8418,#8419,#8420,#8421,#8422,#8423,#8424,#8425,#8426,#8427,#8428,#8429,
#8430,#8431,#8432,#8433,#8434,#8435,#8436,#8437,#8438,#8439,#8440,#8441,
#8442,#8443,#8444,#8445,#8446,#8447,#8448,#8449,#8450,#8451,#8452,#8453,
#8454,#8455,#8456,#8457,#8458,#8459,#8460,#8461,#8462,#8463,#8464,#8465,
#8466,#8467,#8468,#8469,#8470,#8471,#8472,#8473,#8474,#8475,#8476,#8477,
#8478,#8479,#8480,#8481,#8482,#8483,#8484,#8485,#8486,#8487,#8488,#8489,
#8490,#8491,#8492,#8493,#8494,#8495,#8496,#8497,#8498,#8499,#8500,#8501,
#8502,#8503,#8504,#8505,#8506,#8507,#8508,#8509,#8510,#8511,#8512,#8513,
#8514,#8515,#8516,#8517,#8518,#8519,#8520,#8521,#8522,#8523,#8524,#8525,
#8526,#8527,#8528,#8529,#8530,#8531,#8532,#8533,#8534,#8535,#8536,#8537,
#8538,#8539,#8540,#8541,#8542,#8543,#8544,#8545,#8546,#8547,#8548,#8549,
#8550,#8551,#8552,#8553,#8554,#8555,#8556,#8557,#8558,#8559,#8560,#8561,
#8562,#8563,#8564,#8565,#8566,#8567,#8568,#8569,#8570,#8571,#8572,#8573,
#8574,#8575,#8576,#8577,#8578,#8579,#8580,#8581,#8582,#8583,#8584,#8585,
#8586,#8587,#8588,#8589,#8590,#8591,#8592,#8593,#8594,#8595),
 .UNSPECIFIED.,.F.,.F.,(4,2,2,2,2,2,2,2,2,2,2,2,2,2,2,2,2,2,2,2,2,2,2,2,
2,2,2,2,2,2,2,2,2,2,2,2,2,2,2,2,2,2,2,2,2,2,2,2,2,2,2,2,2,2,2,2,2,2,2,2,
2,2,2,2,2,2,2,2,2,2,2,2,2,2,2,2,2,2,2,2,2,2,2,2,2,2,2,2,2,2,2,2,2,2,2,2,
2,2,2,2,2,2,2,2,2,2,2,2,2,4),(0.000994439833694746,0.0659502631595153,0.0733296487053945,
0.0773660603147175,0.080891760506465,0.0833233080423989,0.0855481362709591,
0.0886507210913307,0.0967505802559279,0.14792612363284,0.18619872495472,
0.228442905746919,0.237113053470544,0.241218972857156,0.245439703015733,
0.250084169382157,0.257694363837813,0.28318741069681,0.366143308611974,
0.396385679007049,0.401659909442459,0.404470730843828,0.406822660667148,
0.40978709472243,0.414488742025188,0.440878130615305,0.526769176470696,
0.553630067711241,0.561095538639456,0.565708227825213,0.569937403213718,
0.575368125474658,0.587094867669498,0.666242590443618,0.702604141897903,
0.714431981881784,0.72260148295881,0.725952799465748,0.728352049571391,
0.730620321913657,0.73455775775061,0.745909229444491,0.811475512277769,
0.852945551138045,0.876623294234471,0.883781357468483,0.888326981503506,
0.892579271878954,0.898160909614941,0.910727063761941,0.970583230225985,
1.0209508256157,1.03513934063388,1.04449712275035,1.04803282886827,1.0504662620616,
1.05268882218408,1.05578302789872,1.06382323123028,1.11975718681435,1.17130842716486,
1.18918744312778,1.20220397536833,1.20792586619817,1.21218478301565,1.21671418513933,
1.22379782664218,1.24467792128572,1.34371676738214,1.35771710571413,1.36698330342056,
1.37050568046181,1.37293667390736,1.37516238360264,1.37826801694417,1.38638972937924,
1.43606074743629,1.44709540424683,1.49506885089472,1.52096100607504,1.52833787513419,
1.53293147103154,1.53716703446471,1.54263940599612,1.55459241529065,1.63144074207897,
1.66927999831409,1.68138986810137,1.68970583154832,1.69308111037679,1.69548468895388,
1.69774647544496,1.70165041605265,1.71275824843856,1.77854845336969,1.82008939109822,
1.84379349825791,1.85095468750353,1.85550124382183,1.8597536741489,1.8653344336001,
1.87789397151222,1.94029182340544,2.00184670814057,2.01158899706795,2.01518070129991,
2.0176255280612,2.01983717678426,2.02288870598913,2.03065902089388),
 .UNSPECIFIED.);
#1185=B_SPLINE_CURVE_WITH_KNOTS('',3,(#8601,#8602,#8603,#8604,#8605,#8606,
#8607,#8608,#8609,#8610,#8611,#8612,#8613,#8614,#8615,#8616,#8617,#8618,
#8619,#8620,#8621,#8622,#8623,#8624,#8625,#8626,#8627,#8628,#8629,#8630,
#8631,#8632,#8633,#8634,#8635,#8636,#8637,#8638,#8639,#8640,#8641,#8642,
#8643,#8644,#8645,#8646,#8647,#8648,#8649,#8650,#8651,#8652,#8653,#8654,
#8655,#8656,#8657,#8658,#8659,#8660,#8661,#8662,#8663,#8664,#8665,#8666,
#8667,#8668,#8669,#8670,#8671,#8672,#8673,#8674,#8675,#8676,#8677,#8678,
#8679,#8680,#8681,#8682,#8683,#8684,#8685,#8686,#8687,#8688,#8689,#8690,
#8691,#8692,#8693,#8694,#8695,#8696,#8697,#8698,#8699,#8700,#8701,#8702,
#8703,#8704,#8705,#8706,#8707,#8708,#8709,#8710,#8711,#8712,#8713,#8714,
#8715,#8716,#8717,#8718,#8719,#8720,#8721,#8722,#8723,#8724,#8725,#8726,
#8727,#8728,#8729,#8730,#8731,#8732,#8733,#8734,#8735,#8736,#8737,#8738,
#8739,#8740,#8741,#8742,#8743,#8744,#8745,#8746,#8747,#8748,#8749,#8750,
#8751,#8752,#8753,#8754,#8755,#8756,#8757,#8758,#8759,#8760,#8761,#8762,
#8763,#8764,#8765,#8766,#8767,#8768,#8769,#8770,#8771,#8772,#8773,#8774,
#8775,#8776,#8777,#8778,#8779,#8780,#8781,#8782,#8783,#8784,#8785,#8786,
#8787,#8788,#8789,#8790,#8791,#8792,#8793,#8794,#8795,#8796,#8797,#8798,
#8799,#8800,#8801,#8802,#8803,#8804,#8805,#8806,#8807,#8808,#8809,#8810,
#8811,#8812,#8813,#8814,#8815,#8816,#8817,#8818,#8819,#8820,#8821,#8822,
#8823,#8824),.UNSPECIFIED.,.F.,.F.,(4,2,2,2,2,2,2,2,2,2,2,2,2,2,2,2,2,2,
2,2,2,2,2,2,2,2,2,2,2,2,2,2,2,2,2,2,2,2,2,2,2,2,2,2,2,2,2,2,2,2,2,2,2,2,
2,2,2,2,2,2,2,2,2,2,2,2,2,2,2,2,2,2,2,2,2,2,2,2,2,2,2,2,2,2,2,2,2,2,2,2,
2,2,2,2,2,2,2,2,2,2,2,2,2,2,2,2,2,2,2,2,2,4),(2.03118787455235,2.03624725675821,
2.03928615281083,2.04164853071416,2.04436928762826,2.04922203066296,2.07308122157576,
2.1376664293898,2.1860662189869,2.19420566582604,2.1994396559146,2.20363713626479,
2.20841573420626,2.21663710656503,2.25384133694866,2.29873065790328,2.34957053914338,
2.35766596939636,2.36076826798253,2.36299328522015,2.36542548806491,2.36895292457676,
2.37825131015617,2.3923185751308,2.4929351512513,2.51253956156871,2.51945658846259,
2.52395028502474,2.52822661672449,2.53405164456053,2.54766874288209,2.56663442277931,
2.6654652165202,2.67869098458684,2.68286875689106,2.68544063857928,2.68784886625183,
2.69124968209712,2.69972422074796,2.71214367071196,2.75165759357714,2.78169765236756,
2.83093151813495,2.83909495281487,2.84433614742495,2.84853412694834,2.85330759423796,
2.86150575398539,2.89831852066463,2.94536845441438,2.94793593314125,2.96969841540064,
2.97745146849416,2.99952343365957,3.00443316892829,3.00719573006907,3.00955203211667,
3.01257972026627,3.01892636700058,3.02743356966184,3.04907330692725,3.11639516208406,
3.15411539810479,3.16258719939068,3.1674698811342,3.17165829725855,3.1767539905184,
3.18647004198533,3.24946051795983,3.31791938087541,3.3252741972512,3.32825539195769,
3.33066760118873,3.33318565277603,3.33711947277431,3.34952430452682,3.37054977835078,
3.43481817839165,3.47616765338134,3.48406044143621,3.48921905771577,3.49341079467507,
3.49824322712112,3.50671384163061,3.54862803699206,3.60750270921351,3.60961678988223,
3.6433254055801,3.64830047924921,3.651346915815,3.65370476216334,3.65645397276523,
3.66143906965294,3.68758516587915,3.77031735367454,3.79991793479009,3.80792562488444,
3.81265713522846,3.81643997556057,3.82044939222957,3.82809058534521,3.86040976074722,
3.90639870016087,3.96162577993268,3.96966331704312,3.97275722226204,3.97497979798098,
3.97741350831253,3.98095009110326,3.98500250769485,3.99242424884924,4.06083257184693),
 .UNSPECIFIED.);
#1186=B_SPLINE_CURVE_WITH_KNOTS('',3,(#8825,#8826,#8827,#8828),
 .UNSPECIFIED.,.F.,.F.,(4,4),(0.00101359709204687,0.00130988952596835),
 .UNSPECIFIED.);
#1187=B_SPLINE_CURVE_WITH_KNOTS('',3,(#8830,#8831,#8832,#8833,#8834,#8835,
#8836,#8837,#8838,#8839,#8840,#8841,#8842,#8843,#8844,#8845,#8846,#8847,
#8848,#8849,#8850,#8851,#8852,#8853,#8854,#8855,#8856,#8857,#8858,#8859,
#8860,#8861,#8862,#8863,#8864,#8865,#8866,#8867,#8868,#8869,#8870,#8871,
#8872,#8873,#8874,#8875,#8876,#8877,#8878,#8879,#8880,#8881,#8882,#8883,
#8884,#8885,#8886,#8887,#8888,#8889,#8890,#8891,#8892,#8893,#8894,#8895,
#8896,#8897,#8898,#8899,#8900,#8901,#8902,#8903,#8904,#8905,#8906,#8907,
#8908,#8909,#8910,#8911,#8912,#8913,#8914,#8915,#8916,#8917,#8918,#8919,
#8920,#8921,#8922,#8923,#8924,#8925,#8926,#8927,#8928,#8929,#8930,#8931,
#8932,#8933,#8934,#8935,#8936,#8937,#8938,#8939,#8940,#8941,#8942,#8943,
#8944,#8945,#8946,#8947,#8948,#8949,#8950,#8951,#8952,#8953,#8954,#8955,
#8956,#8957,#8958,#8959,#8960,#8961,#8962,#8963,#8964,#8965,#8966,#8967,
#8968,#8969,#8970,#8971,#8972,#8973,#8974,#8975,#8976,#8977,#8978,#8979,
#8980,#8981,#8982,#8983,#8984,#8985,#8986,#8987,#8988,#8989,#8990,#8991,
#8992,#8993,#8994,#8995,#8996,#8997,#8998,#8999,#9000,#9001,#9002,#9003,
#9004,#9005,#9006,#9007,#9008,#9009,#9010,#9011,#9012,#9013,#9014,#9015,
#9016,#9017,#9018,#9019,#9020,#9021,#9022,#9023,#9024,#9025,#9026,#9027,
#9028,#9029,#9030,#9031,#9032,#9033,#9034,#9035,#9036,#9037,#9038,#9039,
#9040,#9041,#9042,#9043,#9044,#9045,#9046,#9047,#9048,#9049,#9050,#9051),
 .UNSPECIFIED.,.F.,.F.,(4,2,2,2,2,2,2,2,2,2,2,2,2,2,2,2,2,2,2,2,2,2,2,2,
2,2,2,2,2,2,2,2,2,2,2,2,2,2,2,2,2,2,2,2,2,2,2,2,2,2,2,2,2,2,2,2,2,2,2,2,
2,2,2,2,2,2,2,2,2,2,2,2,2,2,2,2,2,2,2,2,2,2,2,2,2,2,2,2,2,2,2,2,2,2,2,2,
2,2,2,2,2,2,2,2,2,2,2,2,2,2,4),(2.03065902089388,2.04206362365894,2.07628240140505,
2.15899822527557,2.17032810560539,2.17574318636432,2.17995849926214,2.18462565439367,
2.19233952964678,2.22213609654879,2.28127762630686,2.33021015762429,2.33526795804928,
2.33830600785598,2.34066778836801,2.34338790739053,2.34823960975793,2.37209527496487,
2.4366731149445,2.4850667005546,2.49320447884936,2.49843728182706,2.50263372953709,
2.50741105888515,2.51562999543571,2.55281679747204,2.59770897459972,2.64854814924202,
2.65664218822806,2.65974380451698,2.6619682934422,2.66439986128824,2.66792625884059,
2.67722119348805,2.69128248530843,2.7917870906739,2.81147141139176,2.81839794470002,
2.82289293970401,2.82716697410541,2.83298330238232,2.84655397545899,2.86543597981326,
2.9691715943992,2.97870275544258,2.98237447516457,2.98459091913283,2.98703010138349,
2.99059507906017,3.00015361392844,3.01475878370679,3.06806380130599,3.12973866491161,
3.13799011728958,3.14325723122961,3.14745647678121,3.15221049273746,3.16032300839317,
3.19575837993672,3.24180305128279,3.2560282901354,3.29735870700056,3.30292438171499,
3.30583191437005,3.30818149028723,3.31104148642996,3.31655228514208,3.3610509220796,
3.4332378307528,3.45555781694311,3.46281282118754,3.46737914811334,3.47162272960065,
3.47724880029418,3.48972470070686,3.50664127262168,3.55344089936151,3.61625648081801,
3.623977499376,3.62702041337682,3.62922953798543,3.63167597545541,3.63527755095458,
3.64509264791623,3.70779093407981,3.76895962647601,3.78153107957739,3.78711309638645,
3.79136488400043,3.79299891134299,3.79305305852087,3.79310035613465,3.79319654675188,
3.79329026326948,3.79338166958506,3.79347091807018,3.79355815061592,3.79847576906934,
3.80864753015346,3.82183990298838,3.85332254606539,3.88265825429793,3.93807574898,
3.9461143581825,3.94920793378023,3.95143007220191,3.9538630573551,3.95739815317952,
3.96675441255142,3.9809423358345,4.06033164206889),.UNSPECIFIED.);
#1188=B_SPLINE_CURVE_WITH_KNOTS('',3,(#9052,#9053,#9054,#9055),
 .UNSPECIFIED.,.F.,.F.,(4,4),(0.00112887916970517,0.00138569478241305),
 .UNSPECIFIED.);
#1189=B_SPLINE_CURVE_WITH_KNOTS('',3,(#9061,#9062,#9063,#9064),
 .UNSPECIFIED.,.F.,.F.,(4,4),(4.05989386051375,4.06014004056529),
 .UNSPECIFIED.);
#1190=B_SPLINE_CURVE_WITH_KNOTS('',3,(#9065,#9066,#9067,#9068,#9069,#9070,
#9071,#9072,#9073,#9074,#9075,#9076,#9077,#9078,#9079,#9080,#9081,#9082,
#9083,#9084,#9085,#9086,#9087,#9088,#9089,#9090,#9091,#9092,#9093,#9094,
#9095,#9096,#9097,#9098,#9099,#9100,#9101,#9102,#9103,#9104,#9105,#9106,
#9107,#9108,#9109,#9110,#9111,#9112,#9113,#9114,#9115,#9116,#9117,#9118,
#9119,#9120,#9121,#9122,#9123,#9124,#9125,#9126,#9127,#9128,#9129,#9130,
#9131,#9132,#9133,#9134,#9135,#9136,#9137,#9138,#9139,#9140,#9141,#9142,
#9143,#9144,#9145,#9146,#9147,#9148,#9149,#9150,#9151,#9152,#9153,#9154,
#9155,#9156,#9157,#9158,#9159,#9160,#9161,#9162,#9163,#9164,#9165,#9166,
#9167,#9168,#9169,#9170,#9171,#9172,#9173,#9174,#9175,#9176,#9177,#9178,
#9179,#9180,#9181,#9182,#9183,#9184,#9185,#9186,#9187,#9188,#9189,#9190,
#9191,#9192,#9193,#9194,#9195,#9196,#9197,#9198,#9199,#9200,#9201,#9202,
#9203,#9204,#9205,#9206,#9207,#9208,#9209,#9210,#9211,#9212,#9213,#9214,
#9215,#9216,#9217,#9218,#9219,#9220,#9221,#9222,#9223,#9224,#9225,#9226,
#9227,#9228,#9229,#9230,#9231,#9232,#9233,#9234,#9235,#9236,#9237,#9238,
#9239,#9240,#9241,#9242,#9243,#9244,#9245,#9246,#9247,#9248,#9249,#9250,
#9251,#9252,#9253,#9254,#9255,#9256,#9257,#9258,#9259,#9260,#9261,#9262,
#9263,#9264,#9265,#9266,#9267,#9268),.UNSPECIFIED.,.F.,.F.,(4,2,2,2,2,2,
2,2,2,2,2,2,2,2,2,2,2,2,2,2,2,2,2,2,2,2,2,2,2,2,2,2,2,2,2,2,2,2,2,2,2,2,
2,2,2,2,2,2,2,2,2,2,2,2,2,2,2,2,2,2,2,2,2,2,2,2,2,2,2,2,2,2,2,2,2,2,2,2,
2,2,2,2,2,2,2,2,2,2,2,2,2,2,2,2,2,2,2,2,2,2,2,4),(0.00111348523567152,0.0224816007626239,
0.0901262012177608,0.100246350923435,0.103891281144555,0.10634714547644,
0.108549302474072,0.111562989800143,0.11910739814605,0.185509403693803,
0.229997598019453,0.246416065213366,0.25850663970398,0.263970423952956,
0.268226907461397,0.272764194180999,0.279882144044013,0.301033111249466,
0.399755124484115,0.4137431033698,0.423003543322421,0.426525378231244,0.428956524058265,
0.431182806531379,0.434289821560384,0.442419689913735,0.491956264196637,
0.53382936746426,0.561093271252557,0.578905500369908,0.585367538732415,
0.589766078637995,0.594056557024971,0.600192630588166,0.611491173796425,
0.670690552486911,0.735223835276311,0.745156642648614,0.748775685157619,
0.751226377402732,0.753433425081234,0.756465955988553,0.764120796493412,
0.828642753807549,0.895388726786414,0.904992749063346,0.910065418588115,
0.91421365812635,0.919100911398923,0.927592444692042,0.965684890353983,
1.0326688752449,1.06453190964363,1.06973662846895,1.07253292432333,1.07488613900785,
1.077869303875,1.08263246935774,1.11025244246143,1.19497168802161,1.21266583818951,
1.22557956722103,1.23128403640875,1.23554067053093,1.24007764965408,1.24719413334218,
1.26833238620149,1.36706965935031,1.38105830085798,1.39031907372458,1.39384096572875,
1.39627212890743,1.39849840963472,1.40160539910848,1.40973502039596,1.45927656418336,
1.50115852666669,1.52841438255367,1.54622286092332,1.5526844026193,1.55708285156407,
1.56137343093722,1.56750998060345,1.57881026456769,1.64235146004286,1.70288101210086,
1.7125563503411,1.71613883844027,1.71858208944097,1.72079601302236,1.72385546363711,
1.73167025832051,1.79317603254048,1.8408980902137,1.86671052084986,1.87408054325659,
1.87867305987981,1.88290977622055,1.88838666419224,1.90036204480245,1.97696467006013,
2.03118787455235),.UNSPECIFIED.);
#1191=B_SPLINE_CURVE_WITH_KNOTS('',3,(#9269,#9270,#9271,#9272,#9273,#9274,
#9275,#9276,#9277,#9278,#9279,#9280,#9281,#9282,#9283,#9284,#9285,#9286,
#9287,#9288,#9289,#9290,#9291,#9292,#9293,#9294,#9295,#9296,#9297,#9298,
#9299,#9300,#9301,#9302,#9303,#9304,#9305,#9306,#9307,#9308,#9309,#9310,
#9311,#9312,#9313,#9314,#9315,#9316,#9317,#9318,#9319,#9320,#9321,#9322,
#9323,#9324,#9325,#9326,#9327,#9328,#9329,#9330,#9331,#9332,#9333,#9334,
#9335,#9336,#9337,#9338,#9339,#9340,#9341,#9342,#9343,#9344,#9345,#9346,
#9347,#9348,#9349,#9350,#9351,#9352,#9353,#9354,#9355,#9356,#9357,#9358,
#9359,#9360,#9361,#9362,#9363,#9364,#9365,#9366,#9367,#9368,#9369,#9370,
#9371,#9372,#9373,#9374,#9375,#9376,#9377,#9378,#9379,#9380,#9381,#9382,
#9383,#9384,#9385,#9386,#9387,#9388,#9389,#9390,#9391,#9392,#9393,#9394,
#9395,#9396,#9397,#9398,#9399,#9400,#9401,#9402,#9403,#9404,#9405,#9406,
#9407,#9408,#9409,#9410,#9411,#9412,#9413,#9414,#9415,#9416,#9417,#9418,
#9419,#9420,#9421,#9422,#9423,#9424,#9425,#9426,#9427,#9428,#9429,#9430,
#9431,#9432,#9433,#9434,#9435,#9436,#9437,#9438,#9439,#9440,#9441,#9442,
#9443,#9444,#9445,#9446,#9447,#9448,#9449,#9450,#9451,#9452,#9453,#9454,
#9455,#9456,#9457,#9458,#9459,#9460,#9461,#9462,#9463,#9464,#9465,#9466,
#9467,#9468,#9469,#9470,#9471,#9472,#9473,#9474,#9475,#9476,#9477,#9478,
#9479,#9480,#9481,#9482,#9483,#9484,#9485,#9486,#9487,#9488,#9489,#9490,
#9491,#9492,#9493,#9494,#9495,#9496,#9497,#9498,#9499,#9500,#9501,#9502,
#9503,#9504,#9505,#9506,#9507,#9508,#9509,#9510,#9511,#9512,#9513,#9514),
 .UNSPECIFIED.,.F.,.F.,(4,2,2,2,2,2,2,2,2,2,2,2,2,2,2,2,2,2,2,2,2,2,2,2,
2,2,2,2,2,2,2,2,2,2,2,2,2,2,2,2,2,2,2,2,2,2,2,2,2,2,2,2,2,2,2,2,2,2,2,2,
2,2,2,2,2,2,2,2,2,2,2,2,2,2,2,2,2,2,2,2,2,2,2,2,2,2,2,2,2,2,2,2,2,2,2,2,
2,2,2,2,2,2,2,2,2,2,2,2,2,2,2,2,2,2,2,2,2,2,2,2,2,2,4),(0.00138569478241305,
0.0267213414297853,0.0408251368465114,0.0462378673492938,0.0503775404732197,
0.0543978425872758,0.0589295209120385,0.0660224417239157,0.08696289358787,
0.115688684107862,0.155137456901873,0.204341363940377,0.210423711120401,
0.213399555807341,0.21552628154065,0.218235077329387,0.222910379132293,
0.241786800393865,0.259796115646,0.318478283315475,0.346593894146785,0.358827616224174,
0.368432488138858,0.373476715932667,0.37351491088737,0.373555770386838,
0.373599488837467,0.373646275847383,0.373696357497504,0.373749977729205,
0.373807399865922,0.373868908246732,0.373934809986602,0.374005436893115,
0.374081147488881,0.374162329195859,0.374249400619812,0.378441099864665,
0.383607964054376,0.391528942332894,0.432499708934886,0.497034964896065,
0.528138629967786,0.533315707151181,0.536105822897071,0.53845904938096,
0.541448851836776,0.546235015476269,0.574430401252419,0.658606133568633,
0.676252530802476,0.689139071104937,0.694838170496325,0.699093347876914,
0.703631160320024,0.710753956023984,0.731953135923117,0.830612365047775,
0.844596881256467,0.853855268463663,0.857376425466993,0.859807131914509,
0.86203302249243,0.865139489799158,0.873267899031018,0.922812835964177,
0.964702884909765,0.991947171916137,1.00974951825666,1.0162095182313,1.02060709900641,
1.02489696537361,1.03103272023084,1.04233208688768,1.1058367902302,1.16639282644824,
1.17606915969118,1.17965140193449,1.18209429452891,1.18430773159755,1.18796243260164,
1.19738494437535,1.30131284910325,1.32020849299303,1.33378560522356,1.33960322662293,
1.34387765679379,1.34837256205309,1.35529793890983,1.37497210811089,1.47544378061878,
1.4895000366673,1.49879330955964,1.50231946935156,1.50475101417417,1.50697558476106,
1.51007747627904,1.51817301458386,1.56909105305033,1.6140955276345,1.65117090383273,
1.65938349986985,1.66415942851689,1.66835600617083,1.67359075817074,1.68173496178498,
1.73035500514378,1.79467135058144,1.81062226787019,1.82081769722814,1.82447262464397,
1.8269302756948,1.8291302134018,1.83213601309703,1.83963587039484,1.9065834288418,
1.97084737961853,1.98060519909095,1.98570875135073,1.98949137605346,1.99421996306415,
2.00221618307605,2.03141751110446),.UNSPECIFIED.);
#1192=B_SPLINE_CURVE_WITH_KNOTS('',3,(#9519,#9520,#9521,#9522,#9523,#9524,
#9525,#9526,#9527,#9528,#9529,#9530,#9531,#9532,#9533,#9534,#9535,#9536,
#9537,#9538,#9539,#9540,#9541,#9542,#9543,#9544,#9545,#9546,#9547,#9548,
#9549,#9550,#9551,#9552,#9553,#9554,#9555,#9556,#9557,#9558,#9559,#9560,
#9561,#9562,#9563,#9564,#9565,#9566,#9567,#9568,#9569,#9570,#9571,#9572,
#9573,#9574,#9575,#9576,#9577,#9578,#9579,#9580,#9581,#9582,#9583,#9584,
#9585,#9586,#9587,#9588,#9589,#9590,#9591,#9592,#9593,#9594,#9595,#9596,
#9597,#9598,#9599,#9600,#9601,#9602,#9603,#9604,#9605,#9606,#9607,#9608,
#9609,#9610,#9611,#9612,#9613,#9614,#9615,#9616,#9617,#9618,#9619,#9620,
#9621,#9622,#9623,#9624,#9625,#9626,#9627,#9628,#9629,#9630,#9631,#9632,
#9633,#9634,#9635,#9636,#9637,#9638,#9639,#9640,#9641,#9642,#9643,#9644,
#9645,#9646,#9647,#9648,#9649,#9650,#9651,#9652,#9653,#9654,#9655,#9656,
#9657,#9658,#9659,#9660,#9661,#9662,#9663,#9664,#9665,#9666,#9667,#9668,
#9669,#9670,#9671,#9672,#9673,#9674,#9675,#9676,#9677,#9678,#9679,#9680,
#9681,#9682,#9683,#9684,#9685,#9686,#9687,#9688,#9689,#9690,#9691,#9692,
#9693,#9694,#9695,#9696,#9697,#9698,#9699,#9700,#9701,#9702,#9703,#9704,
#9705,#9706,#9707,#9708,#9709,#9710,#9711,#9712,#9713,#9714,#9715,#9716,
#9717,#9718,#9719,#9720,#9721,#9722,#9723,#9724,#9725,#9726,#9727,#9728,
#9729,#9730,#9731,#9732,#9733,#9734,#9735,#9736),.UNSPECIFIED.,.F.,.F.,
(4,2,2,2,2,2,2,2,2,2,2,2,2,2,2,2,2,2,2,2,2,2,2,2,2,2,2,2,2,2,2,2,2,2,2,
2,2,2,2,2,2,2,2,2,2,2,2,2,2,2,2,2,2,2,2,2,2,2,2,2,2,2,2,2,2,2,2,2,2,2,2,
2,2,2,2,2,2,2,2,2,2,2,2,2,2,2,2,2,2,2,2,2,2,2,2,2,2,2,2,2,2,2,2,2,2,2,2,
2,4),(2.03078233277413,2.05701474884909,2.06473078008979,2.06939792509912,
2.07361238998611,2.07902521861311,2.09034612622446,2.13438924023311,2.18871322588318,
2.22220599552371,2.22717223774696,2.23021557887311,2.2325725205178,2.23532240679641,
2.24031298585521,2.26691708277014,2.35435241548298,2.37955708470908,2.38714104364052,
2.39177888272704,2.39599969979284,2.40146708392961,2.41307917357678,2.45943370353251,
2.53655785716989,2.54751133360523,2.55139279923023,2.55364965670384,2.55605514036883,
2.5594446101676,2.56785311667929,2.58014540046924,2.6189750865854,2.6943339615967,
2.70640696476809,2.71189995836232,2.71613747650923,2.72071929588646,2.72804683584302,
2.75343799314438,2.7998749849234,2.86320462922567,2.87089746669002,2.87393548423825,
2.87614320917402,2.87859067704753,2.88219819085504,2.89205693805071,2.95545406107523,
3.0158398079194,3.02840593896334,3.0339866498923,3.03823786678702,3.0427819956265,
3.04993698955352,3.07359870563441,3.11502762492672,3.18052306976554,3.19187636999115,
3.1958133020623,3.19808101783125,3.20047945327617,3.20382930585367,3.21199360710417,
3.22381397324974,3.26014505159502,3.33934521446711,3.34990240154371,3.35524315227204,
3.35918272682049,3.36347023621106,3.36936612660064,3.38341581095883,3.45295128470277,
3.50717823148167,3.51524274842077,3.51833980134792,3.52056273438184,3.52299461512872,
3.52652484035116,3.53584934819174,3.5499726453274,3.65221007564477,3.67044300038479,
3.6771662715017,3.68117223256025,3.68541577713138,3.69073923512959,3.70239876617017,
3.71803415508925,3.75909665197433,3.82346919710859,3.83610422941879,3.84020825199906,
3.84276275113584,3.84517776000279,3.84862175762956,3.85737947082623,3.87035951401955,
3.9381573549767,3.96722909062668,3.99112001235569,3.99855299014072,4.0031571303506,
4.00738614355311,4.01151265483841,4.01689034996646,4.03172592743479,4.05989386051375),
 .UNSPECIFIED.);
#1193=B_SPLINE_CURVE_WITH_KNOTS('',3,(#9737,#9738,#9739,#9740,#9741,#9742,
#9743,#9744,#9745,#9746,#9747,#9748,#9749,#9750,#9751,#9752,#9753,#9754,
#9755,#9756,#9757,#9758,#9759,#9760,#9761,#9762,#9763,#9764,#9765,#9766,
#9767,#9768,#9769,#9770,#9771,#9772,#9773,#9774,#9775,#9776,#9777,#9778,
#9779,#9780,#9781,#9782,#9783,#9784,#9785,#9786,#9787,#9788,#9789,#9790,
#9791,#9792,#9793,#9794,#9795,#9796,#9797,#9798,#9799,#9800,#9801,#9802,
#9803,#9804,#9805,#9806,#9807,#9808,#9809,#9810,#9811,#9812,#9813,#9814,
#9815,#9816,#9817,#9818,#9819,#9820,#9821,#9822,#9823,#9824,#9825,#9826,
#9827,#9828,#9829,#9830,#9831,#9832,#9833,#9834,#9835,#9836,#9837,#9838,
#9839,#9840,#9841,#9842,#9843,#9844,#9845,#9846,#9847,#9848,#9849,#9850,
#9851,#9852,#9853,#9854,#9855,#9856,#9857,#9858,#9859,#9860,#9861,#9862,
#9863,#9864,#9865,#9866,#9867,#9868,#9869,#9870,#9871,#9872,#9873,#9874,
#9875,#9876,#9877,#9878,#9879,#9880,#9881,#9882,#9883,#9884,#9885,#9886,
#9887,#9888,#9889,#9890,#9891,#9892,#9893,#9894,#9895,#9896,#9897,#9898,
#9899,#9900,#9901,#9902,#9903,#9904,#9905,#9906,#9907,#9908,#9909,#9910,
#9911,#9912,#9913,#9914,#9915,#9916,#9917,#9918,#9919,#9920,#9921,#9922,
#9923,#9924,#9925,#9926,#9927,#9928,#9929,#9930,#9931,#9932,#9933,#9934,
#9935,#9936,#9937,#9938,#9939,#9940,#9941,#9942),.UNSPECIFIED.,.F.,.F.,
(4,2,2,2,2,2,2,2,2,2,2,2,2,2,2,2,2,2,2,2,2,2,2,2,2,2,2,2,2,2,2,2,2,2,2,
2,2,2,2,2,2,2,2,2,2,2,2,2,2,2,2,2,2,2,2,2,2,2,2,2,2,2,2,2,2,2,2,2,2,2,2,
2,2,2,2,2,2,2,2,2,2,2,2,2,2,2,2,2,2,2,2,2,2,2,2,2,2,2,2,2,2,2,4),(2.03141751110446,
2.03161830192352,2.09123891434952,2.13952401981648,2.14458719413026,2.14762663706429,
2.14998834914161,2.15270704310881,2.15755302771701,2.18131190211232,2.24528898181316,
2.29433678003636,2.30249303325431,2.30773114366241,2.31192762581724,2.31670043479166,
2.32490008025686,2.36176996849567,2.4068735926888,2.45783800300492,2.46593108065273,
2.46903234995985,2.47125659537007,2.473687903252,2.47721393412981,2.48650796173833,
2.50056793355411,2.60106680936354,2.62074474348472,2.62766996689504,2.63216435541657,
2.63643798923999,2.64225404948089,2.65582538994824,2.67470925824242,2.77853019570927,
2.78798409861485,2.79164334825657,2.79385727399629,2.79629851129585,2.79987463715443,
2.80951198480618,2.8695049850929,2.93366203436167,2.94495486772932,2.95108801564918,
2.95537656629576,2.95977321855179,2.96623264768075,2.98403888376495,3.01129067961153,
3.05311352647787,3.10260650690707,3.11073056980414,3.11383583214611,3.11606101290349,
3.11849110028305,3.12201163711483,3.13126983827728,3.14525693852776,3.24395678793102,
3.26513162701057,3.27225016583536,3.27678608273155,3.28104005029894,3.28673839608964,
3.29962711084333,3.31727719145908,3.40156538659544,3.42954704371025,3.4343229838228,
3.43730918281886,3.43966142643616,3.44245254966432,3.44763718099059,3.47898369327795,
3.54420209592779,3.55667822944215,3.5857464284422,3.59371174068327,3.59843277690088,
3.60221532014369,3.60732652410096,3.61712569014735,3.68273673647865,3.74808621824093,
3.75563632499945,3.75865015644376,3.76085167085968,3.76325665991628,3.76665422237609,
3.77067044364147,3.77799813593805,3.79535607494124,3.87515547019287,3.90757173847285,
3.91569716153532,3.92049941471741,3.92469135940706,3.92988425143375,3.94008589735922,
4.00006936679343,4.06108277158193),.UNSPECIFIED.);
#1194=B_SPLINE_CURVE_WITH_KNOTS('',3,(#9947,#9948,#9949,#9950,#9951,#9952,
#9953,#9954,#9955,#9956,#9957,#9958,#9959,#9960,#9961,#9962,#9963,#9964,
#9965,#9966,#9967,#9968,#9969,#9970,#9971,#9972,#9973,#9974,#9975,#9976,
#9977,#9978,#9979,#9980,#9981,#9982,#9983,#9984,#9985,#9986,#9987,#9988,
#9989,#9990,#9991,#9992,#9993,#9994,#9995,#9996,#9997,#9998,#9999,#10000,
#10001,#10002,#10003,#10004,#10005,#10006,#10007,#10008,#10009,#10010,#10011,
#10012,#10013,#10014,#10015,#10016,#10017,#10018,#10019,#10020,#10021,#10022,
#10023,#10024,#10025,#10026,#10027,#10028,#10029,#10030,#10031,#10032,#10033,
#10034,#10035,#10036,#10037,#10038,#10039,#10040,#10041,#10042,#10043,#10044,
#10045,#10046,#10047,#10048,#10049,#10050,#10051,#10052,#10053,#10054,#10055,
#10056,#10057,#10058,#10059,#10060,#10061,#10062,#10063,#10064,#10065,#10066,
#10067,#10068,#10069,#10070,#10071,#10072,#10073,#10074,#10075,#10076,#10077,
#10078,#10079,#10080,#10081,#10082,#10083,#10084,#10085,#10086,#10087,#10088,
#10089,#10090,#10091,#10092,#10093,#10094,#10095,#10096,#10097,#10098,#10099,
#10100,#10101,#10102,#10103,#10104,#10105,#10106,#10107,#10108,#10109,#10110,
#10111,#10112,#10113,#10114,#10115,#10116,#10117,#10118,#10119,#10120,#10121,
#10122,#10123,#10124,#10125,#10126,#10127,#10128,#10129,#10130,#10131,#10132,
#10133,#10134,#10135,#10136,#10137,#10138,#10139,#10140,#10141,#10142,#10143,
#10144,#10145,#10146,#10147,#10148,#10149,#10150,#10151,#10152,#10153,#10154,
#10155,#10156,#10157,#10158,#10159,#10160),.UNSPECIFIED.,.F.,.F.,(4,2,2,
2,2,2,2,2,2,2,2,2,2,2,2,2,2,2,2,2,2,2,2,2,2,2,2,2,2,2,2,2,2,2,2,2,2,2,2,
2,2,2,2,2,2,2,2,2,2,2,2,2,2,2,2,2,2,2,2,2,2,2,2,2,2,2,2,2,2,2,2,2,2,2,2,
2,2,2,2,2,2,2,2,2,2,2,2,2,2,2,2,2,2,2,2,2,2,2,2,2,2,2,2,2,2,2,4),(0.00133785408364666,
0.0856446905644938,0.122424369273886,0.130619548823976,0.135391751336176,
0.139588895196584,0.144829411282487,0.152992426471294,0.202280327718648,
0.232371091602562,0.271726767326629,0.284116017797875,0.289917394424944,
0.294484431904405,0.297168247421122,0.299441867234976,0.302455039434137,
0.307319419132626,0.337606206181498,0.400229279607729,0.429283530695928,
0.441789773401134,0.451645353802899,0.456769108232272,0.460958096126468,
0.465816054162684,0.47418138133987,0.510146124647116,0.578701652886667,
0.600755850148186,0.609370945059377,0.615780121469759,0.618819460377261,
0.621176317749108,0.623929610123252,0.628800016880675,0.650298526928026,
0.658625984900809,0.741936234768132,0.759505277556927,0.772348261240176,
0.778039530209684,0.782293290394936,0.786833758300268,0.79396951646743,
0.81528193128391,0.832037407607788,0.90082236936071,0.933577603067133,0.938811250509593,
0.941613160343803,0.943965183938087,0.946939334546403,0.951674161147222,
0.978643077751603,1.06393850810934,1.09071853919903,1.09817571901747,1.10278602781095,
1.10701484654733,1.11244765221054,1.12418915702739,1.20316690973005,1.25446502501371,
1.26060306725689,1.26358957727483,1.26571721569795,1.26841800222674,1.27305964407883,
1.29152930041788,1.30297675943305,1.35687929893693,1.40552039177682,1.41741174239851,
1.42293145473048,1.42715963511997,1.43177285553398,1.43924283045255,1.46345611036264,
1.53390562619572,1.57774569770444,1.58324526712038,1.58610286705057,1.58845239375949,
1.59136227229474,1.59693913841422,1.63945863497612,1.65236283912661,1.69852166868732,
1.73399920493521,1.74211419439026,1.746868593284,1.75106753235136,1.75633341305377,
1.764581211114,1.8294960181138,1.88010504815956,1.89432755814597,1.90370156891809,
1.90723944827798,1.90967314008361,1.91189496461671,1.91498689290402,1.92301254776039,
1.97924609245589,2.03056810395715,2.03078233277413),.UNSPECIFIED.);
#1195=B_SPLINE_CURVE_WITH_KNOTS('',3,(#10162,#10163,#10164,#10165),
 .UNSPECIFIED.,.F.,.F.,(4,4),(4.06108277158193,4.06123005647539),
 .UNSPECIFIED.);
#1196=B_SPLINE_CURVE_WITH_KNOTS('',3,(#10166,#10167,#10168,#10169,#10170,
#10171,#10172,#10173,#10174,#10175,#10176,#10177,#10178,#10179,#10180,#10181,
#10182,#10183,#10184,#10185,#10186,#10187,#10188,#10189,#10190,#10191,#10192,
#10193,#10194,#10195,#10196,#10197,#10198,#10199,#10200,#10201,#10202,#10203,
#10204,#10205,#10206,#10207,#10208,#10209,#10210,#10211,#10212,#10213,#10214,
#10215,#10216,#10217,#10218,#10219,#10220,#10221,#10222,#10223,#10224,#10225,
#10226,#10227,#10228,#10229,#10230,#10231,#10232,#10233,#10234,#10235,#10236,
#10237,#10238,#10239,#10240,#10241,#10242,#10243,#10244,#10245,#10246,#10247,
#10248,#10249,#10250,#10251,#10252,#10253,#10254,#10255,#10256,#10257,#10258,
#10259,#10260,#10261,#10262,#10263,#10264,#10265,#10266,#10267,#10268,#10269,
#10270,#10271,#10272,#10273,#10274,#10275,#10276,#10277,#10278,#10279,#10280,
#10281,#10282,#10283,#10284,#10285,#10286,#10287,#10288,#10289,#10290,#10291,
#10292,#10293,#10294,#10295,#10296,#10297,#10298,#10299,#10300,#10301,#10302,
#10303,#10304,#10305,#10306,#10307,#10308,#10309,#10310,#10311,#10312,#10313,
#10314,#10315,#10316,#10317,#10318,#10319,#10320,#10321,#10322,#10323,#10324,
#10325,#10326,#10327,#10328,#10329,#10330,#10331,#10332,#10333,#10334,#10335,
#10336,#10337,#10338,#10339,#10340,#10341,#10342,#10343,#10344,#10345,#10346,
#10347,#10348,#10349,#10350,#10351,#10352,#10353,#10354,#10355,#10356,#10357,
#10358,#10359,#10360,#10361,#10362,#10363,#10364,#10365,#10366,#10367,#10368,
#10369,#10370,#10371,#10372,#10373,#10374,#10375,#10376,#10377,#10378,#10379,
#10380,#10381,#10382,#10383,#10384,#10385),.UNSPECIFIED.,.F.,.F.,(4,2,2,
2,2,2,2,2,2,2,2,2,2,2,2,2,2,2,2,2,2,2,2,2,2,2,2,2,2,2,2,2,2,2,2,2,2,2,2,
2,2,2,2,2,2,2,2,2,2,2,2,2,2,2,2,2,2,2,2,2,2,2,2,2,2,2,2,2,2,2,2,2,2,2,2,
2,2,2,2,2,2,2,2,2,2,2,2,2,2,2,2,2,2,2,2,2,2,2,2,2,2,2,2,2,2,2,2,2,2,4),
(0.00121494437820566,0.0110361665019738,0.0175286064381429,0.0202186781558045,
0.0224361585553646,0.024688223990178,0.0277264892490866,0.0341297955183033,
0.0525492195787883,0.101534616884938,0.16712361780516,0.176925211388578,
0.182037979192517,0.186226504471999,0.191093539198829,0.199498524411382,
0.236051393496236,0.311691777226034,0.328721898705432,0.335955557793333,
0.3399364298102,0.343377037528105,0.345766590671855,0.34798396783837,0.351660042345005,
0.361218153486806,0.464967376756704,0.483854905481767,0.497427387690942,
0.503244014607295,0.507518077682627,0.512012927590382,0.518938889311041,
0.538619475515404,0.639075929909461,0.653130982850428,0.662423521828384,
0.665949443411343,0.668380836701181,0.670605278814104,0.673707004490731,
0.681802209719301,0.732653298747103,0.779291827000504,0.814950317454205,
0.823076865996563,0.827833875829596,0.832032598530283,0.837294854313059,
0.845530379778327,0.909080647558641,0.96032546087957,0.975017586554573,
0.984618643950791,0.988189693159059,0.990630049122151,0.992845200938749,
0.996510324930135,1.00599994239505,1.10982373079634,1.12871278344703,1.14228576587521,
1.14810211707737,1.15237579747298,1.15687008115234,1.16379483847946,1.18346964695222,
1.28392037135659,1.29797416392352,1.30726583912665,1.31079141301791,1.31322256024172,
1.3154467721997,1.31854817036355,1.32664247140017,1.37751960319005,1.42413134557623,
1.45977802037419,1.46790322919262,1.47265964171562,1.47685795019831,1.48211983672294,
1.49035507813956,1.55373945001163,1.60273633120165,1.62687127579128,1.63173735238195,
1.63446027282125,1.63682102982063,1.63985342979978,1.64489294222184,1.68329757418375,
1.74675996326157,1.78209350692148,1.79019907981403,1.79495120894009,1.7991501047521,
1.80441853144757,1.81267540833835,1.87404164475143,1.92751968150728,1.94214609837832,
1.95171531626248,1.9552815328654,1.95772073749243,1.95993654073915,1.96300574714687,
1.97088400219229,2.03074823704563,2.03104238026227),.UNSPECIFIED.);
#1197=B_SPLINE_CURVE_WITH_KNOTS('',3,(#10391,#10392,#10393,#10394,#10395,
#10396,#10397,#10398,#10399,#10400,#10401,#10402,#10403,#10404,#10405,#10406,
#10407,#10408,#10409,#10410,#10411,#10412,#10413,#10414,#10415,#10416,#10417,
#10418,#10419,#10420,#10421,#10422,#10423,#10424,#10425,#10426,#10427,#10428,
#10429,#10430,#10431,#10432,#10433,#10434,#10435,#10436,#10437,#10438,#10439,
#10440,#10441,#10442,#10443,#10444,#10445,#10446,#10447,#10448,#10449,#10450,
#10451,#10452,#10453,#10454,#10455,#10456,#10457,#10458,#10459,#10460,#10461,
#10462,#10463,#10464,#10465,#10466,#10467,#10468,#10469,#10470,#10471,#10472,
#10473,#10474,#10475,#10476,#10477,#10478,#10479,#10480,#10481,#10482,#10483,
#10484,#10485,#10486,#10487,#10488,#10489,#10490,#10491,#10492,#10493,#10494,
#10495,#10496,#10497,#10498,#10499,#10500,#10501,#10502,#10503,#10504,#10505,
#10506,#10507,#10508,#10509,#10510,#10511,#10512,#10513,#10514,#10515,#10516,
#10517,#10518,#10519,#10520,#10521,#10522,#10523,#10524,#10525,#10526,#10527,
#10528,#10529,#10530,#10531,#10532,#10533,#10534,#10535,#10536,#10537,#10538,
#10539,#10540,#10541,#10542,#10543,#10544,#10545,#10546,#10547,#10548,#10549,
#10550,#10551,#10552,#10553,#10554,#10555,#10556,#10557,#10558,#10559,#10560,
#10561,#10562,#10563,#10564,#10565,#10566,#10567,#10568,#10569,#10570,#10571,
#10572,#10573,#10574,#10575,#10576,#10577,#10578,#10579,#10580,#10581,#10582,
#10583,#10584,#10585,#10586,#10587,#10588,#10589,#10590,#10591,#10592,#10593,
#10594,#10595,#10596,#10597,#10598,#10599,#10600,#10601,#10602,#10603,#10604,
#10605,#10606,#10607,#10608,#10609,#10610,#10611,#10612,#10613,#10614),
 .UNSPECIFIED.,.F.,.F.,(4,2,2,2,2,2,2,2,2,2,2,2,2,2,2,2,2,2,2,2,2,2,2,2,
2,2,2,2,2,2,2,2,2,2,2,2,2,2,2,2,2,2,2,2,2,2,2,2,2,2,2,2,2,2,2,2,2,2,2,2,
2,2,2,2,2,2,2,2,2,2,2,2,2,2,2,2,2,2,2,2,2,2,2,2,2,2,2,2,2,2,2,2,2,2,2,2,
2,2,2,2,2,2,2,2,2,2,2,2,2,2,2,4),(2.03130412200221,2.03159818914461,2.08772320577085,
2.0957527707976,2.09884565652699,2.10106805355868,2.10350221507385,2.10704053262685,
2.11641413762186,2.13063628820749,2.18122394352423,2.24087321478513,2.25344102976112,
2.25902336299018,2.2632761588798,2.26782230738462,2.27498118413346,2.29866252645453,
2.34013626646325,2.4057494348067,2.41700386422519,2.42092813416422,2.42319393413138,
2.4255950129249,2.42895601204101,2.43718379074069,2.44912471045109,2.48607261896767,
2.56435277197644,2.57617548651034,2.58162409555845,2.58585614438439,2.59046085540838,
2.59788868383068,2.62433201270105,2.70710180167611,2.71421797542152,2.73733688044322,
2.74231078912408,2.74508781395693,2.74744251782633,2.75045027257915,2.75669431730239,
2.76502503589402,2.78599701818555,2.84994284859199,2.89167719950095,2.89957689543349,
2.90473754649871,2.90892929991236,2.91375993323543,2.92222262214858,2.96397581402302,
3.02099412247387,3.05874272827858,3.0637727282486,3.06680282896265,3.06916395463783,
3.07188981872865,3.07676721488255,3.10109110451491,3.1499163565872,3.2133563160021,
3.22159426090094,3.22685773909182,3.23105726818484,3.23581501581692,3.2439424182159,
3.27960156205471,3.32624072037417,3.37703053618904,3.38512501366353,3.3882269225244,
3.3904516541001,3.39288353752763,3.39641049889102,3.40570756356702,3.41977277016236,
3.52037034318773,3.53997711545056,3.54689389225322,3.55138714413535,3.55566284828734,
3.56148669911958,3.57509953733178,3.59405818932627,3.6950714440059,3.70656512687793,
3.71052198386052,3.7127941338675,3.71514342943226,3.71836722028747,3.7220390594721,
3.72847385963401,3.74284904014334,3.79450484163212,3.858238837025,3.8664742612871,
3.87173682841542,3.87593607615401,3.88069398203353,3.88882284477652,3.92451054746185,
4.00299342900153,4.02155406800738,4.02995181813464,4.03343836083613,4.03583835866016,
4.03803438413862,4.04055012496013,4.04412071707633,4.06112080728385),
 .UNSPECIFIED.);
#1198=B_SPLINE_CURVE_WITH_KNOTS('',3,(#10615,#10616,#10617,#10618),
 .UNSPECIFIED.,.F.,.F.,(4,4),(0.00120377071706689,0.00133785408364666),
 .UNSPECIFIED.);
#1199=B_SPLINE_CURVE_WITH_KNOTS('',3,(#10619,#10620,#10621,#10622,#10623,
#10624,#10625,#10626,#10627,#10628,#10629,#10630,#10631,#10632,#10633,#10634,
#10635,#10636,#10637,#10638,#10639,#10640,#10641,#10642,#10643,#10644,#10645,
#10646,#10647,#10648,#10649,#10650,#10651,#10652,#10653,#10654,#10655,#10656,
#10657,#10658,#10659,#10660,#10661,#10662,#10663,#10664,#10665,#10666,#10667,
#10668,#10669,#10670,#10671,#10672,#10673,#10674,#10675,#10676,#10677,#10678,
#10679,#10680,#10681,#10682,#10683,#10684,#10685,#10686,#10687,#10688,#10689,
#10690,#10691,#10692,#10693,#10694,#10695,#10696,#10697,#10698,#10699,#10700,
#10701,#10702,#10703,#10704,#10705,#10706,#10707,#10708,#10709,#10710,#10711,
#10712,#10713,#10714,#10715,#10716,#10717,#10718,#10719,#10720,#10721,#10722,
#10723,#10724,#10725,#10726,#10727,#10728,#10729,#10730,#10731,#10732,#10733,
#10734,#10735,#10736,#10737,#10738,#10739,#10740,#10741,#10742,#10743,#10744,
#10745,#10746,#10747,#10748,#10749,#10750,#10751,#10752,#10753,#10754,#10755,
#10756,#10757,#10758,#10759,#10760,#10761,#10762,#10763,#10764,#10765,#10766,
#10767,#10768,#10769,#10770,#10771,#10772,#10773,#10774,#10775,#10776,#10777,
#10778,#10779,#10780,#10781,#10782,#10783,#10784,#10785,#10786,#10787,#10788,
#10789,#10790,#10791,#10792,#10793,#10794,#10795,#10796,#10797,#10798,#10799,
#10800,#10801,#10802,#10803,#10804,#10805,#10806,#10807,#10808,#10809,#10810,
#10811,#10812,#10813,#10814,#10815,#10816,#10817,#10818,#10819,#10820,#10821,
#10822,#10823,#10824,#10825,#10826,#10827,#10828,#10829,#10830,#10831,#10832,
#10833,#10834,#10835,#10836),.UNSPECIFIED.,.F.,.F.,(4,2,2,2,2,2,2,2,2,2,
2,2,2,2,2,2,2,2,2,2,2,2,2,2,2,2,2,2,2,2,2,2,2,2,2,2,2,2,2,2,2,2,2,2,2,2,
2,2,2,2,2,2,2,2,2,2,2,2,2,2,2,2,2,2,2,2,2,2,2,2,2,2,2,2,2,2,2,2,2,2,2,2,
2,2,2,2,2,2,2,2,2,2,2,2,2,2,2,2,2,2,2,2,2,2,2,2,2,2,4),(2.03104238026227,
2.09724542452292,2.10958014687469,2.11470220533646,2.11897823506359,2.12339070044557,
2.12992747070857,2.14831097586602,2.17680989517851,2.23818411945571,2.25279894878368,
2.27166408981011,2.2763375696431,2.27904552430693,2.28117169927647,2.28414695405555,
2.2902286742074,2.33944382197764,2.39958941507056,2.42716490016722,2.43498533056113,
2.43967496086213,2.44388403670093,2.44925442402646,2.46035559345829,2.50271421110341,
2.57034551267571,2.59339390432458,2.5983622924609,2.60113743175028,2.60349129734894,
2.6064989339772,2.61274592863724,2.62108258912497,2.64208060718408,2.70620503857858,
2.74769742203716,2.75558830570707,2.76074520127322,2.76493521875067,2.76976530601767,
2.77823083738869,2.82009296209893,2.8773436686462,2.91471534053356,2.91973776613717,
2.92276505414384,2.92512508999524,2.92785096815099,2.93273139858635,2.95713760355033,
3.00588638951751,3.06927598660031,3.07751105570501,3.0827725961731,3.08697050810402,
3.09172634172455,3.09985025279019,3.13548882473561,3.18208799443039,3.23290457360636,
3.24099645609327,3.24409724081228,3.24632113203405,3.24875204502355,3.25227749035114,
3.26156990065317,3.27562736098389,3.37610367943317,3.39578374012999,3.40270854645824,
3.40720236150998,3.4114752311517,3.41728990700404,3.43085641042182,3.44973238587553,
3.55341670789118,3.5629638718,3.56663749073389,3.56885388471243,3.57129186371868,
3.57485315179539,3.58439029039193,3.5989524292132,3.65195911205504,3.71396163534035,
3.72294157396361,3.7279756972016,3.73207673277969,3.7368718033689,3.7419813495068,
3.76258159138641,3.79614747560425,3.87553996959618,3.88520074504443,3.88889174257148,
3.89111147880631,3.89354631154953,3.89709157713696,3.90651843912977,3.92085221103114,
3.97223147174009,4.0190802381283,4.04007701665561,4.04702611149955,4.05158544928812,
4.0556183792297,4.05837181477896,4.0604205322052),.UNSPECIFIED.);
#1200=B_SPLINE_CURVE_WITH_KNOTS('',3,(#10841,#10842,#10843,#10844,#10845,
#10846,#10847,#10848,#10849,#10850,#10851,#10852,#10853,#10854,#10855,#10856,
#10857,#10858,#10859,#10860,#10861,#10862,#10863,#10864,#10865,#10866,#10867,
#10868,#10869,#10870,#10871,#10872,#10873,#10874,#10875,#10876,#10877,#10878,
#10879,#10880,#10881,#10882,#10883,#10884,#10885,#10886,#10887,#10888,#10889,
#10890,#10891,#10892,#10893,#10894,#10895,#10896,#10897,#10898,#10899,#10900,
#10901,#10902,#10903,#10904,#10905,#10906,#10907,#10908,#10909,#10910,#10911,
#10912,#10913,#10914,#10915,#10916,#10917,#10918,#10919,#10920,#10921,#10922,
#10923,#10924,#10925,#10926,#10927,#10928,#10929,#10930,#10931,#10932,#10933,
#10934,#10935,#10936,#10937,#10938,#10939,#10940,#10941,#10942,#10943,#10944,
#10945,#10946,#10947,#10948,#10949,#10950,#10951,#10952,#10953,#10954,#10955,
#10956,#10957,#10958,#10959,#10960,#10961,#10962,#10963,#10964,#10965,#10966,
#10967,#10968,#10969,#10970,#10971,#10972,#10973,#10974,#10975,#10976,#10977,
#10978,#10979,#10980,#10981,#10982,#10983,#10984,#10985,#10986,#10987,#10988,
#10989,#10990,#10991,#10992,#10993,#10994,#10995,#10996,#10997,#10998,#10999,
#11000,#11001,#11002,#11003,#11004,#11005,#11006,#11007,#11008,#11009,#11010,
#11011,#11012,#11013,#11014,#11015,#11016,#11017,#11018,#11019,#11020,#11021,
#11022,#11023,#11024,#11025,#11026,#11027,#11028,#11029,#11030,#11031,#11032,
#11033,#11034,#11035,#11036,#11037,#11038,#11039,#11040,#11041,#11042,#11043,
#11044,#11045,#11046,#11047,#11048,#11049,#11050,#11051,#11052),
 .UNSPECIFIED.,.F.,.F.,(4,2,2,2,2,2,2,2,2,2,2,2,2,2,2,2,2,2,2,2,2,2,2,2,
2,2,2,2,2,2,2,2,2,2,2,2,2,2,2,2,2,2,2,2,2,2,2,2,2,2,2,2,2,2,2,2,2,2,2,2,
2,2,2,2,2,2,2,2,2,2,2,2,2,2,2,2,2,2,2,2,2,2,2,2,2,2,2,2,2,2,2,2,2,2,2,2,
2,2,2,2,2,2,2,2,2,4),(0.00125155003270578,0.0033132412163655,0.00662460547463569,
0.0106349599505179,0.0171288983854706,0.0347121459144986,0.0495379607755764,
0.131385330900832,0.158297684923628,0.163303816321884,0.166057685301177,
0.168415134003331,0.171455391128603,0.176409326417822,0.209498440746812,
0.28220805351899,0.314242264093352,0.322126805827004,0.326106965746669,
0.330209623558016,0.335034045232269,0.343522013722197,0.382132439440515,
0.4486397705076,0.470079459925927,0.482653924452503,0.486607217852261,0.489129572222461,
0.491538883006436,0.494509113523836,0.501800706094395,0.570913410083924,
0.613759433789263,0.637929535964344,0.645138775441384,0.649696029864435,
0.653944780123184,0.659500971845563,0.671919822664633,0.740922541111079,
0.784229319441231,0.797311548801108,0.806122767466081,0.809576359706321,
0.811994288352569,0.814547929292512,0.818643395444061,0.831197085470782,
0.930913367662087,0.949882764852105,0.963500452931096,0.96932533312387,
0.973601394208901,0.978094657373839,0.98501072290671,1.00461068785063,1.10517155477238,
1.11923159298535,1.12852693568994,1.13205365404792,1.13448551638714,1.13671033581554,
1.13981253432267,1.14790859197987,1.198751894151,1.24539996395251,1.28106393319932,
1.28919181023295,1.29394964434165,1.2981491289487,1.30341239195831,1.31164961417293,
1.37505710353216,1.42408445425791,1.44819072459155,1.453056224355,1.45577948855589,
1.45814098678398,1.46117492215529,1.46621819634657,1.50479408533015,1.56126770394926,
1.60279868470962,1.61125074238818,1.61607900129604,1.62027083121103,1.62543430950392,
1.63334342010044,1.67536297205957,1.73901509700709,1.75993072288712,1.77229137240521,
1.77621987335247,1.77873664981951,1.78114945965377,1.78413336161747,1.7915044553703,
1.85984085796907,1.90314070661222,1.92746935502212,1.93469420114988,1.93925460590421,
1.94350166857908,1.94904900641244,1.96141952355341,2.03130412200221),
 .UNSPECIFIED.);
#1201=B_SPLINE_CURVE_WITH_KNOTS('',3,(#11053,#11054,#11055,#11056,#11057,
#11058,#11059,#11060,#11061,#11062,#11063,#11064,#11065,#11066,#11067,#11068,
#11069,#11070,#11071,#11072,#11073,#11074,#11075,#11076,#11077,#11078,#11079,
#11080,#11081,#11082,#11083,#11084,#11085,#11086,#11087,#11088,#11089,#11090,
#11091,#11092,#11093,#11094,#11095,#11096,#11097,#11098,#11099,#11100,#11101,
#11102,#11103,#11104,#11105,#11106,#11107,#11108,#11109,#11110,#11111,#11112,
#11113,#11114,#11115,#11116,#11117,#11118,#11119,#11120,#11121,#11122,#11123,
#11124,#11125,#11126,#11127,#11128,#11129,#11130,#11131,#11132,#11133,#11134,
#11135,#11136,#11137,#11138,#11139,#11140,#11141,#11142,#11143,#11144,#11145,
#11146,#11147,#11148,#11149,#11150,#11151,#11152,#11153,#11154,#11155,#11156,
#11157,#11158,#11159,#11160,#11161,#11162,#11163,#11164,#11165,#11166,#11167,
#11168,#11169,#11170,#11171,#11172,#11173,#11174,#11175,#11176,#11177,#11178,
#11179,#11180,#11181,#11182,#11183,#11184,#11185,#11186,#11187,#11188,#11189,
#11190,#11191,#11192,#11193,#11194,#11195,#11196,#11197,#11198,#11199,#11200,
#11201,#11202,#11203,#11204,#11205,#11206,#11207,#11208,#11209,#11210,#11211,
#11212,#11213,#11214,#11215,#11216,#11217,#11218,#11219,#11220,#11221,#11222,
#11223,#11224,#11225,#11226,#11227,#11228,#11229,#11230,#11231,#11232,#11233,
#11234,#11235,#11236,#11237,#11238,#11239,#11240,#11241,#11242,#11243,#11244,
#11245,#11246,#11247,#11248,#11249,#11250,#11251,#11252,#11253,#11254,#11255,
#11256,#11257,#11258,#11259,#11260,#11261,#11262,#11263,#11264,#11265,#11266,
#11267,#11268,#11269,#11270,#11271,#11272,#11273,#11274,#11275,#11276,#11277,
#11278,#11279,#11280,#11281,#11282,#11283,#11284,#11285,#11286,#11287,#11288,
#11289,#11290,#11291,#11292),.UNSPECIFIED.,.F.,.F.,(4,2,2,2,2,2,2,2,2,2,
2,2,2,2,2,2,2,2,2,2,2,2,2,2,2,2,2,2,2,2,2,2,2,2,2,2,2,2,2,2,2,2,2,2,2,2,
2,2,2,2,2,2,2,2,2,2,2,2,2,2,2,2,2,2,2,2,2,2,2,2,2,2,2,2,2,2,2,2,2,2,2,2,
2,2,2,2,2,2,2,2,2,2,2,2,2,2,2,2,2,2,2,2,2,2,2,2,2,2,2,2,2,2,2,2,2,2,2,2,
2,4),(0.00124959457603072,0.00492543247451525,0.0116818150862804,0.0377034604979688,
0.114471961733272,0.135439625127425,0.14376941206842,0.150013273990401,
0.153020890359151,0.155375465320991,0.158152271004239,0.163125656412322,
0.186235736995255,0.193494712808228,0.221420716211356,0.274843012937881,
0.293078382164194,0.306293226992382,0.311840961930181,0.311988334968319,
0.312135099985741,0.312281944293211,0.31242960352371,0.312578881378219,
0.312730674935975,0.312886007992206,0.313046076134992,0.313212309449408,
0.313386462370007,0.313570746834712,0.313661175647747,0.313791566679259,
0.313990742769881,0.317857527833423,0.322759921545408,0.331593068575246,
0.379990737876284,0.44455792119756,0.468410828991787,0.473262591831226,
0.475982894394741,0.478344913456056,0.481383408228347,0.486442256031224,
0.535421646772217,0.566639068530259,0.617071005605761,0.629176502670673,
0.634736499732904,0.638971294402423,0.643568014306446,0.650958642964771,
0.67444457057856,0.770475177984643,0.784348615058876,0.793552960890251,
0.797066440625881,0.799495953831366,0.801724041088134,0.805454421680962,
0.815373917829648,0.918700270757783,0.937573655740761,0.951139134054692,
0.956955364302162,0.961230093736521,0.965726515877643,0.972656666995343,
0.992361705031603,1.09281642674985,1.10687367921614,1.11616783475831,1.11969447597409,
1.12212639910168,1.12435135276931,1.12745382685068,1.13555124869866,1.18618535191786,
1.23070715505844,1.26849478271473,1.27674958652149,1.28153518284876,1.28573139859682,
1.29095410627343,1.29905716419411,1.34635659010491,1.41188863489402,1.43589232881538,
1.4407524741973,1.44347466216422,1.4458364755782,1.44887237338436,1.45392209825609,
1.49290057670856,1.50954595970559,1.55565038421919,1.5911142191012,1.59923018326806,
1.60398568942568,1.60818592485367,1.61345384759458,1.62170564350074,1.68305717564142,
1.72689190888643,1.75771603732155,1.76288353189489,1.76567187486503,1.76802565509607,
1.77101877603656,1.77581516977206,1.80424916536834,1.85887737188161,1.90342876299138,
1.91796652879128,1.92394369465665,1.92824742385816,1.93217256159791,1.93744941525408,
1.95037299426595,2.03151358947421),.UNSPECIFIED.);
#1202=B_SPLINE_CURVE_WITH_KNOTS('',3,(#11297,#11298,#11299,#11300,#11301,
#11302,#11303,#11304,#11305,#11306,#11307,#11308,#11309,#11310,#11311,#11312,
#11313,#11314,#11315,#11316,#11317,#11318,#11319,#11320,#11321,#11322,#11323,
#11324,#11325,#11326,#11327,#11328,#11329,#11330,#11331,#11332,#11333,#11334,
#11335,#11336,#11337,#11338,#11339,#11340,#11341,#11342,#11343,#11344,#11345,
#11346,#11347,#11348,#11349,#11350,#11351,#11352,#11353,#11354,#11355,#11356,
#11357,#11358,#11359,#11360,#11361,#11362,#11363,#11364,#11365,#11366,#11367,
#11368,#11369,#11370,#11371,#11372,#11373,#11374,#11375,#11376,#11377,#11378,
#11379,#11380,#11381,#11382,#11383,#11384,#11385,#11386,#11387,#11388,#11389,
#11390,#11391,#11392,#11393,#11394,#11395,#11396,#11397,#11398,#11399,#11400,
#11401,#11402,#11403,#11404,#11405,#11406,#11407,#11408,#11409,#11410,#11411,
#11412,#11413,#11414,#11415,#11416,#11417,#11418,#11419,#11420,#11421,#11422,
#11423,#11424,#11425,#11426,#11427,#11428,#11429,#11430,#11431,#11432,#11433,
#11434,#11435,#11436,#11437,#11438,#11439,#11440,#11441,#11442,#11443,#11444,
#11445,#11446,#11447,#11448,#11449,#11450,#11451,#11452,#11453,#11454,#11455,
#11456,#11457,#11458,#11459,#11460,#11461,#11462,#11463,#11464,#11465,#11466,
#11467,#11468,#11469,#11470,#11471,#11472,#11473,#11474,#11475,#11476,#11477,
#11478,#11479,#11480,#11481,#11482,#11483,#11484,#11485,#11486,#11487,#11488,
#11489,#11490,#11491,#11492,#11493,#11494,#11495,#11496,#11497,#11498,#11499,
#11500,#11501,#11502,#11503,#11504,#11505,#11506,#11507,#11508,#11509,#11510,
#11511,#11512,#11513,#11514,#11515,#11516),.UNSPECIFIED.,.F.,.F.,(4,2,2,
2,2,2,2,2,2,2,2,2,2,2,2,2,2,2,2,2,2,2,2,2,2,2,2,2,2,2,2,2,2,2,2,2,2,2,2,
2,2,2,2,2,2,2,2,2,2,2,2,2,2,2,2,2,2,2,2,2,2,2,2,2,2,2,2,2,2,2,2,2,2,2,2,
2,2,2,2,2,2,2,2,2,2,2,2,2,2,2,2,2,2,2,2,2,2,2,2,2,2,2,2,2,2,2,2,2,2,4),
(2.03073768813154,2.11072975512029,2.12234333454239,2.12775320390847,2.13197944191807,
2.136602429535,2.14411497645868,2.17150650529066,2.22440946936597,2.27841097866719,
2.28647353178428,2.28957086092473,2.29179425912932,2.29422696006808,2.29775889429554,
2.30709091128042,2.32122821912819,2.42377002578307,2.44178602378642,2.44847921611095,
2.45248021059465,2.45672809294067,2.46238351711885,2.47502514037414,2.49223477848027,
2.54044248844621,2.54664704473423,2.60074121370944,2.60883564648511,2.61193696324897,
2.61416112680092,2.61659222238102,2.62011776362682,2.6294094896026,2.64346521996227,
2.74389551145599,2.7636108902075,2.77054072289667,2.77503590122977,2.77930870117297,
2.78512114230213,2.79867252370822,2.81752042894719,2.92052646222894,2.93061782703941,
2.93437258328928,2.93660467497578,2.93902868209343,2.94251798554393,2.95156812592516,
2.96513276971133,3.01140327684648,3.07648032594718,3.08776076166595,3.0938904673702,
3.09817824927165,3.10257549351041,3.10903838043567,3.12687129045731,3.15418090070068,
3.20979388129932,3.24941162964769,3.25446822808309,3.25750549108827,3.25986662399677,
3.26258597571072,3.26743628011954,3.29128495022569,3.35584900595195,3.40420923089798,
3.41234396785359,3.41757507662633,3.42177034105811,3.42654651884582,3.43476398690763,
3.47195577295523,3.5168166377711,3.56762680974727,3.57571799429181,3.57881866410196,
3.58104251271806,3.58347343761378,3.58699901986224,3.5962925126977,3.61035237130263,
3.71091566817458,3.73051012943634,3.73728664320116,3.74171521995412,3.74573931209866,
3.74602017566641,3.74631065043745,3.74661625993346,3.74694250778996,3.7533028847529,
3.77040267249736,3.7961692600928,3.83979136985615,3.88987827349401,3.89797329345074,
3.90107409025273,3.90329769576141,3.90572796582772,3.90925195165624,3.91853751959072,
3.9325821291337,4.03280542314696,4.05202382614655,4.05720470954994,4.06024052944633),
 .UNSPECIFIED.);
#1203=B_SPLINE_CURVE_WITH_KNOTS('',3,(#11518,#11519,#11520,#11521,#11522,
#11523,#11524,#11525,#11526,#11527,#11528,#11529,#11530,#11531,#11532,#11533,
#11534,#11535,#11536,#11537,#11538,#11539,#11540,#11541,#11542,#11543,#11544,
#11545,#11546,#11547,#11548,#11549,#11550,#11551,#11552,#11553,#11554,#11555,
#11556,#11557,#11558,#11559,#11560,#11561,#11562,#11563,#11564,#11565,#11566,
#11567,#11568,#11569,#11570,#11571,#11572,#11573,#11574,#11575,#11576,#11577,
#11578,#11579,#11580,#11581,#11582,#11583,#11584,#11585,#11586,#11587,#11588,
#11589,#11590,#11591,#11592,#11593,#11594,#11595,#11596,#11597,#11598,#11599,
#11600,#11601,#11602,#11603,#11604,#11605,#11606,#11607,#11608,#11609,#11610,
#11611,#11612,#11613,#11614,#11615,#11616,#11617,#11618,#11619,#11620,#11621,
#11622,#11623,#11624,#11625,#11626,#11627,#11628,#11629,#11630,#11631,#11632,
#11633,#11634,#11635,#11636,#11637,#11638,#11639,#11640,#11641,#11642,#11643,
#11644,#11645,#11646,#11647,#11648,#11649,#11650,#11651,#11652,#11653,#11654,
#11655,#11656,#11657,#11658,#11659,#11660,#11661,#11662,#11663,#11664,#11665,
#11666,#11667,#11668,#11669,#11670,#11671,#11672,#11673,#11674,#11675,#11676,
#11677,#11678,#11679,#11680,#11681,#11682,#11683,#11684,#11685,#11686,#11687,
#11688,#11689,#11690,#11691,#11692,#11693,#11694,#11695,#11696,#11697,#11698,
#11699,#11700,#11701,#11702,#11703,#11704,#11705,#11706,#11707,#11708,#11709,
#11710,#11711,#11712,#11713,#11714,#11715,#11716,#11717,#11718,#11719,#11720,
#11721,#11722,#11723,#11724,#11725,#11726,#11727,#11728,#11729,#11730,#11731,
#11732,#11733,#11734,#11735,#11736,#11737,#11738,#11739,#11740,#11741,#11742,
#11743,#11744,#11745),.UNSPECIFIED.,.F.,.F.,(4,2,2,2,2,2,2,2,2,2,2,2,2,
2,2,2,2,2,2,2,2,2,2,2,2,2,2,2,2,2,2,2,2,2,2,2,2,2,2,2,2,2,2,2,2,2,2,2,2,
2,2,2,2,2,2,2,2,2,2,2,2,2,2,2,2,2,2,2,2,2,2,2,2,2,2,2,2,2,2,2,2,2,2,2,2,
2,2,2,2,2,2,2,2,2,2,2,2,2,2,2,2,2,2,2,2,2,2,2,2,2,2,2,2,4),(2.03151358947421,
2.03179279629966,2.07934242230676,2.08493183850827,2.08784507076267,2.09019551517515,
2.09305203002042,2.0985432905786,2.14174761963465,2.21047983714227,2.2367551795405,
2.24445258535579,2.24911666327236,2.25333360557995,2.25875694838213,2.27012733002251,
2.31454045187498,2.3733550174524,2.3835803675052,2.40320846220856,2.40794896053077,
2.41067301154721,2.41279787424561,2.41575331764715,2.42173113411769,2.45341399541341,
2.5223699682621,2.52421233111449,2.55797513019204,2.56619990527858,2.57102649160007,
2.57521878205303,2.58038526940911,2.59044747216621,2.6032853402125,2.63349537403812,
2.67269619515577,2.69798114073147,2.72477341442969,2.72950142514258,2.7324738966228,
2.73482633783964,2.73763078196616,2.74287455373235,2.77589984591938,2.84495539878062,
2.8801411781844,2.88845761097629,2.89330483261521,2.89749512882616,2.90263384752023,
2.91256073392481,2.92518022432155,2.95462430648263,2.99446680045347,3.01917949875696,
3.04701462729239,3.05178593330778,3.05477132472137,3.05712433871354,3.05991804051801,
3.06511179797319,3.09667169775675,3.16265954969188,3.20200902523218,3.21056557897601,
3.21546702999504,3.21961386608028,3.22466827030457,3.23418681047777,3.30184721346629,
3.36547964700241,3.37316439571593,3.37620158875579,3.37840953731662,3.38085822139737,
3.38446915809363,3.39434737263569,3.45802040604519,3.51816343832614,3.53073345281895,
3.53631587068988,3.54056837177271,3.5451138522323,3.55227091686359,3.57593861676319,
3.61737549323501,3.68243986239268,3.69416704299009,3.69815523259854,3.70043354833431,
3.70277939126246,3.70596798518041,3.70960262062157,3.71594266015058,3.73001422510341,
3.83076929402906,3.85025218777052,3.85715208789866,3.86164152914446,3.86591879301661,
3.87175295172683,3.88542826978344,3.90450174863351,3.97648544401523,3.99690977804572,
4.015266653672,4.01989911977734,4.02259783855968,4.02490759915752,4.02722459528333,
4.0302635598406,4.03511993261798,4.06121199284332),.UNSPECIFIED.);
#1204=B_SPLINE_CURVE_WITH_KNOTS('',3,(#11746,#11747,#11748,#11749),
 .UNSPECIFIED.,.F.,.F.,(4,4),(0.00115314525638064,0.00134934797194002),
 .UNSPECIFIED.);
#1205=B_SPLINE_CURVE_WITH_KNOTS('',3,(#11755,#11756,#11757,#11758),
 .UNSPECIFIED.,.F.,.F.,(4,4),(4.06070745563291,4.06091392182859),
 .UNSPECIFIED.);
#1206=B_SPLINE_CURVE_WITH_KNOTS('',3,(#11759,#11760,#11761,#11762,#11763,
#11764,#11765,#11766,#11767,#11768,#11769,#11770,#11771,#11772,#11773,#11774,
#11775,#11776,#11777,#11778,#11779,#11780,#11781,#11782,#11783,#11784,#11785,
#11786,#11787,#11788,#11789,#11790,#11791,#11792,#11793,#11794,#11795,#11796,
#11797,#11798,#11799,#11800,#11801,#11802,#11803,#11804,#11805,#11806,#11807,
#11808,#11809,#11810,#11811,#11812,#11813,#11814,#11815,#11816,#11817,#11818,
#11819,#11820,#11821,#11822,#11823,#11824,#11825,#11826,#11827,#11828,#11829,
#11830,#11831,#11832,#11833,#11834,#11835,#11836,#11837,#11838,#11839,#11840,
#11841,#11842,#11843,#11844,#11845,#11846,#11847,#11848,#11849,#11850,#11851,
#11852,#11853,#11854,#11855,#11856,#11857,#11858,#11859,#11860,#11861,#11862,
#11863,#11864,#11865,#11866,#11867,#11868,#11869,#11870,#11871,#11872,#11873,
#11874,#11875,#11876,#11877,#11878,#11879,#11880,#11881,#11882,#11883,#11884,
#11885,#11886,#11887,#11888,#11889,#11890,#11891,#11892,#11893,#11894,#11895,
#11896,#11897,#11898,#11899,#11900,#11901,#11902,#11903,#11904,#11905,#11906,
#11907,#11908,#11909,#11910,#11911,#11912,#11913,#11914,#11915,#11916,#11917,
#11918,#11919,#11920,#11921,#11922,#11923,#11924,#11925,#11926,#11927,#11928,
#11929,#11930,#11931,#11932,#11933,#11934,#11935,#11936,#11937,#11938,#11939,
#11940,#11941,#11942,#11943,#11944,#11945,#11946,#11947,#11948,#11949,#11950,
#11951,#11952,#11953,#11954,#11955,#11956,#11957,#11958,#11959,#11960,#11961,
#11962,#11963,#11964,#11965,#11966,#11967,#11968,#11969,#11970,#11971,#11972,
#11973,#11974,#11975,#11976,#11977,#11978,#11979,#11980,#11981,#11982,#11983,
#11984,#11985,#11986,#11987,#11988,#11989,#11990,#11991,#11992,#11993,#11994,
#11995,#11996,#11997,#11998,#11999,#12000,#12001,#12002,#12003,#12004,#12005,
#12006,#12007,#12008,#12009,#12010,#12011,#12012,#12013,#12014,#12015,#12016,
#12017,#12018,#12019,#12020,#12021,#12022,#12023,#12024,#12025,#12026,#12027,
#12028,#12029,#12030,#12031,#12032,#12033,#12034,#12035,#12036,#12037,#12038,
#12039,#12040,#12041,#12042,#12043,#12044,#12045,#12046,#12047,#12048,#12049,
#12050,#12051,#12052,#12053,#12054,#12055,#12056,#12057,#12058,#12059,#12060,
#12061,#12062,#12063,#12064,#12065,#12066,#12067,#12068,#12069,#12070,#12071,
#12072,#12073,#12074,#12075,#12076),.UNSPECIFIED.,.F.,.F.,(4,2,2,2,2,2,
2,2,2,2,2,2,2,2,2,2,2,2,2,2,2,2,2,2,2,2,2,2,2,2,2,2,2,2,2,2,2,2,2,2,2,2,
2,2,2,2,2,2,2,2,2,2,2,2,2,2,2,2,2,2,2,2,2,2,2,2,2,2,2,2,2,2,2,2,2,2,2,2,
2,2,2,2,2,2,2,2,2,2,2,2,2,2,2,2,2,2,2,2,2,2,2,2,2,2,2,2,2,2,2,2,2,2,2,2,
2,2,2,2,2,2,2,2,2,2,2,2,2,2,2,2,2,2,2,2,2,2,2,2,2,2,2,2,2,2,2,2,2,2,2,2,
2,2,2,2,2,2,2,2,4),(0.0011683366425719,0.0190896020491265,0.0283003389842762,
0.0314305038094561,0.0337794422462348,0.0360500179959316,0.03867520572741,
0.0430940587683594,0.0584996142433649,0.0781669975701139,0.144699861170873,
0.182131045967224,0.190364861544194,0.195145680566725,0.199342117590731,
0.204570882354306,0.212694534858354,0.26063603369651,0.340144243133286,
0.347825600067614,0.353637852873017,0.356547027409714,0.356556090594668,
0.356565251946185,0.356574512743948,0.356583874305357,0.356593337926219,
0.35660290494184,0.356612576718678,0.3566223546711,0.356632240186353,0.356642234676561,
0.356652339593405,0.356662556402393,0.356672886621523,0.356683331769095,
0.356693893376627,0.356704573011764,0.356715372269769,0.356726292743829,
0.356737336103744,0.356748504013963,0.356759798167156,0.356771220283469,
0.356782772095619,0.356794455395882,0.356806271966298,0.356818223651303,
0.356830312311093,0.356842539837938,0.356854908156969,0.356867419181249,
0.356880074908092,0.356892877369787,0.356905828591294,0.356918930631532,
0.356932185603303,0.356945595658919,0.356959162951516,0.356972889719226,
0.356986778198209,0.35700083064486,0.357015049370485,0.357029436715151,
0.357043995074483,0.357058726855779,0.357073634520072,0.357087567614488,
0.359449163843749,0.362483776215833,0.367529307757795,0.406352867542073,
0.462663543957239,0.490124566921263,0.502165718298953,0.511730999589201,
0.516795422044643,0.520943042183884,0.525836723338703,0.534357590478075,
0.573013838138699,0.63953096591555,0.671241181096845,0.676440275088906,
0.679235254969947,0.68158838521942,0.684572744869096,0.689340250253382,
0.717071548480294,0.74191579905805,0.781769880483295,0.811238141615489,
0.82386421530927,0.833794630911215,0.838934314057546,0.843124970321952,
0.84797213668555,0.856287325214198,0.891281214684261,0.960360345705921,
0.993478224151555,0.998724916628295,1.00153007969029,1.00388262013799,1.00685461880762,
1.01158082515537,1.03826646163187,1.12385642139954,1.15067895566725,1.15814142597914,
1.1627537517932,1.1669835887318,1.1724165478094,1.18415374005488,1.26322890060629,
1.29963058690042,1.3114664199087,1.3196402330663,1.32299244914599,1.32539203415961,
1.32766038047844,1.33159744983048,1.34294460252838,1.40851258456327,1.44998298901275,
1.47366122691284,1.48081977160036,1.48536579390186,1.48961852692549,1.49520085480276,
1.50776909209673,1.56807797856574,1.63153210129232,1.64139638053063,1.64500543149153,
1.64745381621774,1.64966225972668,1.6527011527735,1.66039551518431,1.72382918450427,
1.79172218512908,1.80124302074416,1.80629796889047,1.81044490924899,1.81534609060657,
1.82390118518987,1.86322967892115,1.92917909746166,1.95050083483856,1.95892428125475,
1.96522257041947,1.96824067357641,1.97059594373311,1.97336479316313,1.9783032936595,
2.0008347999481,2.00595072121192,2.03046255456567,2.03073768813154),
 .UNSPECIFIED.);
#1207=B_SPLINE_CURVE_WITH_KNOTS('',3,(#12077,#12078,#12079,#12080,#12081,
#12082,#12083,#12084,#12085,#12086,#12087,#12088,#12089,#12090,#12091,#12092,
#12093,#12094,#12095,#12096,#12097,#12098,#12099,#12100,#12101,#12102,#12103,
#12104,#12105,#12106,#12107,#12108,#12109,#12110,#12111,#12112,#12113,#12114,
#12115,#12116,#12117,#12118,#12119,#12120,#12121,#12122,#12123,#12124,#12125,
#12126,#12127,#12128,#12129,#12130,#12131,#12132,#12133,#12134,#12135,#12136,
#12137,#12138,#12139,#12140,#12141,#12142,#12143,#12144,#12145,#12146,#12147,
#12148,#12149,#12150,#12151,#12152,#12153,#12154,#12155,#12156,#12157,#12158,
#12159,#12160,#12161,#12162,#12163,#12164,#12165,#12166,#12167,#12168,#12169,
#12170,#12171,#12172,#12173,#12174,#12175,#12176,#12177,#12178,#12179,#12180,
#12181,#12182,#12183,#12184,#12185,#12186,#12187,#12188,#12189,#12190,#12191,
#12192,#12193,#12194,#12195,#12196,#12197,#12198,#12199,#12200,#12201,#12202,
#12203,#12204,#12205,#12206,#12207,#12208,#12209,#12210,#12211,#12212,#12213,
#12214,#12215,#12216,#12217,#12218,#12219,#12220,#12221,#12222,#12223,#12224,
#12225,#12226,#12227,#12228,#12229,#12230,#12231,#12232,#12233,#12234,#12235,
#12236,#12237,#12238,#12239,#12240,#12241,#12242,#12243,#12244,#12245,#12246,
#12247,#12248,#12249,#12250,#12251,#12252,#12253,#12254,#12255,#12256,#12257,
#12258,#12259,#12260,#12261,#12262,#12263,#12264,#12265,#12266,#12267,#12268,
#12269,#12270,#12271,#12272,#12273,#12274,#12275,#12276,#12277,#12278,#12279,
#12280,#12281,#12282,#12283,#12284,#12285,#12286,#12287,#12288),
 .UNSPECIFIED.,.F.,.F.,(4,2,2,2,2,2,2,2,2,2,2,2,2,2,2,2,2,2,2,2,2,2,2,2,
2,2,2,2,2,2,2,2,2,2,2,2,2,2,2,2,2,2,2,2,2,2,2,2,2,2,2,2,2,2,2,2,2,2,2,2,
2,2,2,2,2,2,2,2,2,2,2,2,2,2,2,2,2,2,2,2,2,2,2,2,2,2,2,2,2,2,2,2,2,2,2,2,
2,2,2,2,2,2,2,2,2,4),(0.00134934797194002,0.0473229576046848,0.0884279385639762,
0.111973379278365,0.119117812896877,0.123660543946948,0.12791414356444,
0.133503334842215,0.146112060610572,0.207310082891032,0.253587591268638,
0.269425402852969,0.276306795270276,0.280152369345684,0.283419464021521,
0.285802081023537,0.288027161629884,0.291130856559744,0.299239359548236,
0.348635487090537,0.396302272346622,0.432338649785541,0.440489056114836,
0.445251522061218,0.449449929275014,0.454704996760686,0.462915983169359,
0.527049013724587,0.578372956499178,0.592699642405142,0.602124597077341,
0.605670215129057,0.608105640788178,0.610326186133742,0.614019057283122,
0.623687729027518,0.727297067802172,0.746178682778632,0.759747888110035,
0.7655639122917,0.769837827112304,0.774332789110485,0.78125946676895,0.800945943482425,
0.901393568363701,0.915448136692731,0.924740405160243,0.928266256754718,
0.930697612106519,0.932922027750942,0.936023727307062,0.944118945279267,
0.994911647752351,1.03970809255952,1.07707492367711,1.08530408200541,1.09008339212788,
1.0942792113274,1.09950812576685,1.10763377327201,1.15566687551174,1.2205057997157,
1.23651230161904,1.24673330847152,1.25039158276503,1.25284980801153,1.25504897094317,
1.25805208327741,1.26553695239642,1.3326489107978,1.37668430654995,1.4012668318682,
1.40851608814383,1.41308118086029,1.41732524892068,1.42285812571963,1.43515133050792,
1.50696829250819,1.54822468315412,1.560953429463,1.56958567336523,1.57301080261353,
1.57542293533072,1.57767078127043,1.58150556451832,1.59212474990427,1.69454598316592,
1.71337563602228,1.72691605468796,1.73272680255419,1.73699943990992,1.74149542539934,
1.74842848287844,1.76816724739095,1.86853746743152,1.88258784581406,1.89187778603315,
1.89540304348089,1.8978340805981,1.90005827810948,1.90315976908588,1.91125516024819,
1.9616825875539,2.0058667471811,2.0311634453307,2.03132451219564),
 .UNSPECIFIED.);
#1208=B_SPLINE_CURVE_WITH_KNOTS('',3,(#12294,#12295,#12296,#12297),
 .UNSPECIFIED.,.F.,.F.,(4,4),(4.06083740610103,4.06111488809983),
 .UNSPECIFIED.);
#1209=B_SPLINE_CURVE_WITH_KNOTS('',3,(#12299,#12300,#12301,#12302,#12303,
#12304,#12305,#12306,#12307,#12308,#12309,#12310,#12311,#12312,#12313,#12314,
#12315,#12316,#12317,#12318,#12319,#12320,#12321,#12322,#12323,#12324,#12325,
#12326,#12327,#12328,#12329,#12330,#12331,#12332,#12333,#12334,#12335,#12336,
#12337,#12338,#12339,#12340,#12341,#12342,#12343,#12344,#12345,#12346,#12347,
#12348,#12349,#12350,#12351,#12352,#12353,#12354,#12355,#12356,#12357,#12358,
#12359,#12360,#12361,#12362,#12363,#12364,#12365,#12366,#12367,#12368,#12369,
#12370,#12371,#12372,#12373,#12374,#12375,#12376,#12377,#12378,#12379,#12380,
#12381,#12382,#12383,#12384,#12385,#12386,#12387,#12388,#12389,#12390,#12391,
#12392,#12393,#12394,#12395,#12396,#12397,#12398,#12399,#12400,#12401,#12402,
#12403,#12404,#12405,#12406,#12407,#12408,#12409,#12410,#12411,#12412,#12413,
#12414,#12415,#12416,#12417,#12418,#12419,#12420,#12421,#12422,#12423,#12424,
#12425,#12426,#12427,#12428,#12429,#12430,#12431,#12432,#12433,#12434,#12435,
#12436,#12437,#12438,#12439,#12440,#12441,#12442,#12443,#12444,#12445,#12446,
#12447,#12448,#12449,#12450,#12451,#12452,#12453,#12454,#12455,#12456,#12457,
#12458,#12459,#12460,#12461,#12462,#12463,#12464,#12465,#12466,#12467,#12468,
#12469,#12470,#12471,#12472,#12473,#12474,#12475,#12476,#12477,#12478,#12479,
#12480,#12481,#12482,#12483,#12484,#12485,#12486,#12487,#12488,#12489,#12490,
#12491,#12492,#12493,#12494),.UNSPECIFIED.,.F.,.F.,(4,2,2,2,2,2,2,2,2,2,
2,2,2,2,2,2,2,2,2,2,2,2,2,2,2,2,2,2,2,2,2,2,2,2,2,2,2,2,2,2,2,2,2,2,2,2,
2,2,2,2,2,2,2,2,2,2,2,2,2,2,2,2,2,2,2,2,2,2,2,2,2,2,2,2,2,2,2,2,2,2,2,2,
2,2,2,2,2,2,2,2,2,2,2,2,2,2,2,4),(0.00105193336829144,0.074271434275133,
0.0828669383037076,0.0892649539556792,0.0923023120117424,0.0946591793586463,
0.0974142605159078,0.102291905373549,0.123895849262207,0.134072461991593,
0.185084519971552,0.221242007588178,0.242839577362775,0.249508341103851,
0.253449005727344,0.257648024539186,0.262907018089082,0.271130323091447,
0.333385818722025,0.386221732369265,0.400761692043544,0.410289940472626,
0.413850784359742,0.416289363818054,0.418507008444209,0.422184054678848,
0.43174767616498,0.53549632692033,0.554384637010092,0.567957724552597,0.573774647016554,
0.578048940536365,0.582544044867368,0.589470423091558,0.609152366496295,
0.709613996600506,0.723669807503864,0.732962849858252,0.736488963911017,
0.738920490389783,0.741145054737096,0.744246951342368,0.752342606342695,
0.803194090118001,0.848093780819342,0.885322932162282,0.893544496917441,
0.898322360808603,0.902518679749868,0.907750537846343,0.915885255553501,
0.964193141839613,1.02879071133128,1.05264659624483,1.05749805548636,1.06021807237497,
1.06257976767387,1.06561775005651,1.07067554718112,1.11026134068559,1.16597776442856,
1.1933190804272,1.20532433836122,1.21486683467606,1.21992613151303,1.22407303455375,
1.22896993998142,1.23750676257852,1.27648312124341,1.34273525537125,1.37436349056789,
1.37955922301171,1.38235326889992,1.38470613002344,1.38769078361802,1.39245993338831,
1.42024115869083,1.4450439541917,1.48492594308059,1.51436799222037,1.52698614878675,
1.53691140947995,1.54204963767549,1.54623969913531,1.55108683376348,1.55940357334363,
1.59460323965626,1.66361222672057,1.69659629369557,1.70183815578237,1.70464207579407,
1.70699436215234,1.70996701612311,1.71469605882798,1.74151342011804,1.76673937606761,
1.82401017269133,1.84306999215748),.UNSPECIFIED.);
#1210=B_SPLINE_CURVE_WITH_KNOTS('',3,(#12496,#12497,#12498,#12499,#12500,
#12501),.UNSPECIFIED.,.F.,.F.,(4,2,4),(0.320887946935547,0.378623714396801,
0.396029912319007),.UNSPECIFIED.);
#1211=B_SPLINE_CURVE_WITH_KNOTS('',3,(#12502,#12503,#12504,#12505,#12506,
#12507,#12508,#12509,#12510,#12511,#12512,#12513,#12514,#12515,#12516,#12517,
#12518,#12519,#12520,#12521,#12522,#12523,#12524,#12525,#12526,#12527,#12528,
#12529,#12530,#12531,#12532,#12533,#12534,#12535,#12536,#12537,#12538,#12539,
#12540,#12541,#12542,#12543,#12544,#12545,#12546,#12547,#12548,#12549,#12550,
#12551,#12552,#12553,#12554,#12555,#12556,#12557,#12558,#12559,#12560,#12561,
#12562,#12563,#12564,#12565,#12566,#12567,#12568,#12569,#12570,#12571,#12572,
#12573,#12574,#12575,#12576,#12577,#12578,#12579,#12580,#12581,#12582,#12583,
#12584,#12585,#12586,#12587,#12588,#12589,#12590,#12591,#12592,#12593,#12594,
#12595,#12596,#12597,#12598,#12599,#12600,#12601,#12602,#12603,#12604,#12605,
#12606,#12607,#12608,#12609,#12610,#12611,#12612,#12613,#12614,#12615,#12616,
#12617,#12618,#12619,#12620,#12621,#12622,#12623,#12624,#12625,#12626,#12627,
#12628,#12629,#12630,#12631,#12632,#12633,#12634,#12635,#12636,#12637,#12638,
#12639,#12640,#12641,#12642,#12643,#12644,#12645,#12646,#12647,#12648,#12649,
#12650,#12651,#12652,#12653,#12654,#12655,#12656,#12657,#12658,#12659,#12660,
#12661,#12662,#12663,#12664,#12665,#12666,#12667,#12668,#12669,#12670,#12671,
#12672,#12673,#12674,#12675,#12676,#12677,#12678,#12679,#12680,#12681,#12682,
#12683,#12684,#12685,#12686,#12687,#12688,#12689,#12690,#12691,#12692,#12693,
#12694,#12695,#12696,#12697,#12698,#12699,#12700,#12701,#12702,#12703,#12704,
#12705,#12706,#12707,#12708,#12709,#12710,#12711,#12712,#12713,#12714,#12715,
#12716,#12717,#12718,#12719,#12720,#12721,#12722,#12723,#12724,#12725,#12726,
#12727,#12728,#12729,#12730,#12731,#12732,#12733,#12734,#12735,#12736,#12737,
#12738,#12739,#12740,#12741,#12742,#12743,#12744,#12745),.UNSPECIFIED.,
 .F.,.F.,(4,2,2,2,2,2,2,2,2,2,2,2,2,2,2,2,2,2,2,2,2,2,2,2,2,2,2,2,2,2,2,
2,2,2,2,2,2,2,2,2,2,2,2,2,2,2,2,2,2,2,2,2,2,2,2,2,2,2,2,2,2,2,2,2,2,2,2,
2,2,2,2,2,2,2,2,2,2,2,2,2,2,2,2,2,2,2,2,2,2,2,2,2,2,2,2,2,2,2,2,2,2,2,2,
2,2,2,2,2,2,2,2,2,2,2,2,2,2,2,2,2,2,4),(0.112200587611434,0.117175410522727,
0.152928885655975,0.182368339026361,0.21521303229137,0.222288891030475,
0.225452486921332,0.227823212755877,0.230500246255892,0.235154078995901,
0.253105054356244,0.271276271681732,0.330837168835884,0.358965543661657,
0.371203219709213,0.380802311059297,0.385849987467527,0.385885864854495,
0.385924240245527,0.385965296738259,0.386009231980911,0.38605625943733,
0.386106609776702,0.386160532405191,0.386218297123432,0.386280195938184,
0.38634654503799,0.386417686918759,0.386493992700438,0.386575864618516,
0.386663738676338,0.38675808745914,0.38682414110453,0.391023904951597,0.396289955575155,
0.404536323115612,0.467610196584102,0.519735038112093,0.534175511413127,
0.543655736077999,0.547209648218229,0.549646896227527,0.551866046008907,
0.555550783543033,0.565164220475125,0.668704244943297,0.687664391154196,
0.701276728938032,0.707100380253507,0.711375927596264,0.71586900356524,
0.722785494212219,0.742391705638046,0.84293352866078,0.856991887461833,
0.866286185003037,0.86981254943419,0.872244181194704,0.874468800429131,
0.87757073386914,0.885666205273227,0.936422404891006,0.981159832924879,
1.01861025676021,1.0268447872605,1.03162556575424,1.0358216955753,1.04104972168781,
1.04917153804975,1.09706939478725,1.16202809251959,1.18593997382092,1.19079458878314,
1.19351534527639,1.19587701578634,1.19891414433071,1.20396883989234,1.24333621222392,
1.29921079114077,1.32658528985591,1.33860040646458,1.34814913730591,1.3532098253402,
1.35735691343316,1.3622529244792,1.37078537360544,1.40967598947049,1.47598956667862,
1.50763639647932,1.51283286572484,1.51562712244927,1.51798005664305,1.52096469302807,
1.52573362273362,1.5535080962,1.57831182100707,1.61818755394369,1.64762955939873,
1.66024770207484,1.67017299312081,1.67531132566215,1.67950152330356,1.68434887857098,
1.69266617114479,1.72787307314038,1.79686729467227,1.82984558844559,1.83508734395831,
1.83789129580703,1.84024366822052,1.84321652918665,1.84794609616524,1.87477440902351,
1.89996443843373,1.95724441004869,1.97662465914178,1.99046610892694,1.99632899760937,
2.00061207621772,2.00509388709481,2.01195454307251,2.03100183139203),
 .UNSPECIFIED.);
#1212=B_SPLINE_CURVE_WITH_KNOTS('',3,(#12749,#12750,#12751,#12752,#12753,
#12754,#12755,#12756),.UNSPECIFIED.,.F.,.F.,(4,2,2,4),(-0.0831448232791332,
-0.0490560578977458,-0.00142471500823912,-0.000102382691227175),
 .UNSPECIFIED.);
#1213=B_SPLINE_CURVE_WITH_KNOTS('',3,(#12760,#12761,#12762,#12763,#12764,
#12765),.UNSPECIFIED.,.F.,.F.,(4,2,4),(-0.0960086291905594,-0.0470065127227869,
-0.0454387767918283),.UNSPECIFIED.);
#1214=B_SPLINE_CURVE_WITH_KNOTS('',3,(#12769,#12770,#12771,#12772,#12773,
#12774),.UNSPECIFIED.,.F.,.F.,(4,2,4),(-0.0932727713439407,-0.047751044771726,
-0.00126085793865929),.UNSPECIFIED.);
#1215=B_SPLINE_CURVE_WITH_KNOTS('',3,(#12778,#12779,#12780,#12781,#12782,
#12783),.UNSPECIFIED.,.F.,.F.,(4,2,4),(-0.0950156675258279,-0.0473137239138524,
-0.000590793973779404),.UNSPECIFIED.);
#1216=B_SPLINE_CURVE_WITH_KNOTS('',3,(#12787,#12788,#12789,#12790,#12791,
#12792),.UNSPECIFIED.,.F.,.F.,(4,2,4),(-0.0929898096602351,-0.0473375247997017,
-0.00112505768103942),.UNSPECIFIED.);
#1217=B_SPLINE_CURVE_WITH_KNOTS('',3,(#12796,#12797,#12798,#12799,#12800,
#12801),.UNSPECIFIED.,.F.,.F.,(4,2,4),(-0.0942916337962443,-0.0469654289747836,
-0.000383531894571019),.UNSPECIFIED.);
#1218=B_SPLINE_CURVE_WITH_KNOTS('',3,(#12805,#12806,#12807,#12808,#12809,
#12810),.UNSPECIFIED.,.F.,.F.,(4,2,4),(-0.0930000698261243,-0.0474064095804956,
-2.37639472703122E-5),.UNSPECIFIED.);
#1219=B_SPLINE_CURVE_WITH_KNOTS('',3,(#12814,#12815,#12816,#12817,#12818,
#12819),.UNSPECIFIED.,.F.,.F.,(4,2,4),(-0.0938672630693478,-0.0468733216732729,
-0.00100573708691378),.UNSPECIFIED.);
#1220=B_SPLINE_CURVE_WITH_KNOTS('',3,(#12823,#12824,#12825,#12826),
 .UNSPECIFIED.,.F.,.F.,(4,4),(-0.0936312282255871,-0.0913169723171845),
 .UNSPECIFIED.);
#1221=B_SPLINE_CURVE_WITH_KNOTS('',3,(#12830,#12831,#12832,#12833,#12834,
#12835,#12836,#12837),.UNSPECIFIED.,.F.,.F.,(4,2,2,4),(-0.0958223528200869,
-0.0488517447323541,-0.00155186802867582,-0.000922707505804365),
 .UNSPECIFIED.);
#1222=B_SPLINE_CURVE_WITH_KNOTS('',3,(#12841,#12842,#12843,#12844,#12845,
#12846),.UNSPECIFIED.,.F.,.F.,(4,2,4),(-0.0931685739517461,-0.0489870992666756,
-0.00144168232493454),.UNSPECIFIED.);
#1223=B_SPLINE_CURVE_WITH_KNOTS('',3,(#12850,#12851,#12852,#12853,#12854,
#12855,#12856,#12857),.UNSPECIFIED.,.F.,.F.,(4,2,2,4),(-0.0945405801644211,
-0.0487921724313465,-0.00154988310282899,-0.00035365744226039),
 .UNSPECIFIED.);
#1224=B_SPLINE_CURVE_WITH_KNOTS('',3,(#12861,#12862,#12863,#12864,#12865,
#12866,#12867,#12868),.UNSPECIFIED.,.F.,.F.,(4,2,2,4),(-0.092843423921612,
-0.0486414832741236,-0.00140880394837164,-0.00070368441099022),
 .UNSPECIFIED.);
#1225=B_SPLINE_CURVE_WITH_KNOTS('',3,(#12872,#12873,#12874,#12875,#12876,
#12877,#12878,#12879),.UNSPECIFIED.,.F.,.F.,(4,2,2,4),(-0.0945127436503505,
-0.0484329844501563,-0.00154044317359045,-0.000351343130144288),
 .UNSPECIFIED.);
#1226=B_SPLINE_CURVE_WITH_KNOTS('',3,(#12883,#12884,#12885,#12886),
 .UNSPECIFIED.,.F.,.F.,(4,4),(-0.026106848360131,0.),.UNSPECIFIED.);
#1227=B_SPLINE_CURVE_WITH_KNOTS('',3,(#12888,#12889,#12890,#12891),
 .UNSPECIFIED.,.F.,.F.,(4,4),(0.984691230773821,1.02983398123988),
 .UNSPECIFIED.);
#1228=B_SPLINE_CURVE_WITH_KNOTS('',3,(#12893,#12894,#12895,#12896,#12897,
#12898,#12899,#12900),.UNSPECIFIED.,.F.,.F.,(4,2,2,4),(-0.0860848159738799,
-0.0428840848156451,-0.00102967768936712,-0.000703274869736634),
 .UNSPECIFIED.);
#1229=B_SPLINE_CURVE_WITH_KNOTS('',3,(#12902,#12903,#12904,#12905,#12906,
#12907),.UNSPECIFIED.,.F.,.F.,(4,2,4),(0.679792780811918,0.754908335318789,
0.769264950774119),.UNSPECIFIED.);
#1230=B_SPLINE_CURVE_WITH_KNOTS('',3,(#12908,#12909,#12910,#12911,#12912,
#12913,#12914,#12915,#12916,#12917,#12918,#12919,#12920,#12921,#12922,#12923,
#12924,#12925,#12926,#12927,#12928,#12929,#12930,#12931,#12932,#12933,#12934,
#12935,#12936,#12937,#12938,#12939,#12940,#12941,#12942,#12943,#12944,#12945,
#12946,#12947,#12948,#12949,#12950,#12951,#12952,#12953,#12954,#12955,#12956,
#12957,#12958,#12959,#12960,#12961,#12962,#12963),.UNSPECIFIED.,.F.,.F.,
(4,2,2,2,2,2,2,2,2,2,2,2,2,2,2,2,2,2,2,2,2,2,2,2,2,2,2,4),(-0.325036416517763,
-0.287179950509608,-0.236779639746712,-0.200445653912114,-0.181391465406389,
-0.177124007539468,-0.174887587830202,-0.174466868660744,-0.174240191480089,
-0.174070434879753,-0.173884176187582,-0.17361100981857,-0.172814926867466,
-0.172526825059135,-0.123766680032299,-0.117959327419192,-0.111861646552513,
-0.105409658342378,-0.0985371190589346,-0.0911704642285506,-0.0832352014871189,
-0.0746399665009568,-0.065281858464088,-0.0550395262469432,-0.0437673431195303,
-0.0312871771278163,-0.0173761699319152,-0.00212616365527593),
 .UNSPECIFIED.);
#1231=B_SPLINE_CURVE_WITH_KNOTS('',3,(#12965,#12966,#12967,#12968,#12969,
#12970),.UNSPECIFIED.,.F.,.F.,(4,2,4),(-0.0942580482856856,-0.0500230495864651,
-0.00152799126305741),.UNSPECIFIED.);
#1232=B_SPLINE_CURVE_WITH_KNOTS('',3,(#12972,#12973,#12974,#12975,#12976,
#12977),.UNSPECIFIED.,.F.,.F.,(4,2,4),(0.31497790761872,0.320913430649623,
0.353605235463099),.UNSPECIFIED.);
#1233=B_SPLINE_CURVE_WITH_KNOTS('',3,(#12978,#12979,#12980,#12981),
 .UNSPECIFIED.,.F.,.F.,(4,4),(-0.0867509478555809,-0.0011253459254421),
 .UNSPECIFIED.);
#1234=B_SPLINE_CURVE_WITH_KNOTS('',3,(#12984,#12985,#12986,#12987),
 .UNSPECIFIED.,.F.,.F.,(4,4),(0.,0.00543966212988572),.UNSPECIFIED.);
#1235=B_SPLINE_CURVE_WITH_KNOTS('',3,(#12989,#12990,#12991,#12992),
 .UNSPECIFIED.,.F.,.F.,(4,4),(0.,0.0146364967117825),.UNSPECIFIED.);
#1236=B_SPLINE_CURVE_WITH_KNOTS('',3,(#12996,#12997,#12998,#12999,#13000,
#13001,#13002,#13003,#13004,#13005,#13006,#13007,#13008,#13009,#13010,#13011,
#13012,#13013,#13014,#13015,#13016,#13017,#13018,#13019,#13020,#13021,#13022,
#13023,#13024,#13025,#13026,#13027,#13028,#13029,#13030,#13031,#13032,#13033,
#13034,#13035,#13036,#13037,#13038,#13039,#13040,#13041,#13042,#13043,#13044,
#13045,#13046,#13047,#13048,#13049,#13050,#13051,#13052,#13053,#13054,#13055,
#13056,#13057,#13058,#13059,#13060,#13061,#13062,#13063,#13064,#13065,#13066,
#13067,#13068,#13069,#13070,#13071,#13072,#13073,#13074,#13075,#13076,#13077,
#13078,#13079,#13080,#13081,#13082,#13083),.UNSPECIFIED.,.F.,.F.,(4,3,3,
3,3,3,3,3,3,3,3,3,3,3,3,3,3,3,3,3,3,3,3,3,3,3,3,3,3,4),(0.,0.0258260740408234,
0.0621538547068688,0.0989229457645657,0.135638978855683,0.14769608638293,
0.154010732384414,0.189902252988839,0.225722717925846,0.260776849486767,
0.288525653206241,0.294827662437031,0.300967317524399,0.335458380531023,
0.369020467026818,0.402151952636654,0.436300775758561,0.44111937264328,
0.474534957939434,0.508516755568951,0.542217627328803,0.567490167559029,
0.575924259490715,0.608982407913722,0.642836293227944,0.654907851897474,
0.664022037486317,0.695845847471868,0.726802774478787,0.744397949170613),
 .UNSPECIFIED.);
#1237=B_SPLINE_CURVE_WITH_KNOTS('',3,(#13086,#13087,#13088,#13089),
 .UNSPECIFIED.,.F.,.F.,(4,4),(0.720569046407016,0.741270768406323),
 .UNSPECIFIED.);
#1238=B_SPLINE_CURVE_WITH_KNOTS('',3,(#13092,#13093,#13094,#13095,#13096,
#13097,#13098,#13099,#13100,#13101,#13102,#13103,#13104,#13105,#13106,#13107,
#13108,#13109,#13110,#13111,#13112,#13113,#13114,#13115,#13116,#13117,#13118,
#13119,#13120,#13121,#13122,#13123,#13124,#13125,#13126,#13127,#13128,#13129,
#13130,#13131,#13132,#13133,#13134,#13135,#13136,#13137,#13138,#13139,#13140,
#13141,#13142,#13143,#13144,#13145,#13146,#13147,#13148,#13149,#13150,#13151,
#13152,#13153,#13154,#13155,#13156,#13157,#13158,#13159,#13160,#13161,#13162,
#13163,#13164,#13165,#13166,#13167,#13168,#13169,#13170,#13171,#13172,#13173,
#13174,#13175,#13176,#13177,#13178,#13179,#13180,#13181,#13182,#13183,#13184,
#13185,#13186,#13187,#13188,#13189,#13190,#13191,#13192,#13193,#13194,#13195,
#13196,#13197,#13198,#13199,#13200,#13201,#13202,#13203,#13204,#13205,#13206,
#13207,#13208,#13209,#13210,#13211,#13212,#13213,#13214,#13215,#13216,#13217,
#13218,#13219,#13220,#13221,#13222,#13223,#13224,#13225,#13226,#13227,#13228,
#13229,#13230,#13231,#13232,#13233,#13234,#13235,#13236,#13237,#13238,#13239,
#13240,#13241,#13242,#13243,#13244,#13245,#13246,#13247,#13248,#13249,#13250,
#13251,#13252,#13253,#13254,#13255,#13256,#13257,#13258,#13259,#13260,#13261,
#13262,#13263,#13264,#13265,#13266,#13267,#13268,#13269,#13270,#13271,#13272,
#13273,#13274,#13275,#13276,#13277,#13278,#13279,#13280,#13281,#13282,#13283,
#13284,#13285,#13286,#13287,#13288,#13289,#13290,#13291,#13292,#13293),
 .UNSPECIFIED.,.F.,.F.,(4,3,3,3,3,3,3,3,3,3,3,3,3,3,3,3,3,3,3,3,3,3,3,3,
3,3,3,3,3,3,3,3,3,3,3,3,3,3,3,3,3,3,3,3,3,3,3,3,3,3,3,3,3,3,3,3,3,3,3,3,
3,3,3,3,3,3,3,4),(-29.2254901136586,-29.1178016057759,-29.0085140011152,
-28.9376744100947,-28.8491012607996,-28.7606424677612,-28.6722742554,-28.5807179195209,
-28.4924512759753,-28.404197885369,-28.3159364031115,-28.2276454839452,
-28.1392544983622,-28.0508039100885,-27.9622239853604,-27.9398235683673,
-27.8512504190762,-27.7627916260421,-27.6744234136853,-27.5828670778046,
-27.4946004342638,-27.4063470436626,-27.3180855614104,-27.2297946422494,
-27.1414036566721,-27.052953068404,-26.9643731436818,-26.9419727266399,
-26.853399577259,-26.7649407841347,-26.6765725716875,-26.5850162358407,
-26.4967495922096,-26.4084962015182,-26.3202347191761,-26.2319437999256,
-26.1435528142598,-26.0551022259036,-25.9665223010947,-25.9441218849125,
-25.8555487357036,-25.7670899427513,-25.6787217304758,-25.5871653945645,
-25.4988987511032,-25.4106453605806,-25.3223838784063,-25.2340929593222,
-25.1457019738199,-25.057251385626,-24.9686714609759,-24.9462710431851,
-24.8576978939488,-24.7692391009706,-24.6808708886705,-24.5893145527689,
-24.5010479092867,-24.4127945187446,-24.3245330365521,-24.2362421174512,
-24.1478511319343,-24.0594005437268,-23.9708206190652,-23.9484202014577,
-23.8598575551356,-23.7713953969511,-23.6830309769814,-23.6507319389946),
 .UNSPECIFIED.);
#1239=B_SPLINE_CURVE_WITH_KNOTS('',3,(#13295,#13296,#13297,#13298,#13299,
#13300,#13301,#13302,#13303,#13304),.UNSPECIFIED.,.F.,.F.,(4,1,1,1,1,1,
1,4),(-35.5086755760922,-34.9247794604591,-33.9269286187317,-32.9290777770043,
-31.9312269352769,-30.9333760935495,-29.9355252518221,-29.2254902689126),
 .UNSPECIFIED.);
#1240=B_SPLINE_CURVE_WITH_KNOTS('',3,(#13306,#13307,#13308,#13309,#13310,
#13311,#13312,#13313,#13314,#13315,#13316,#13317,#13318,#13319,#13320,#13321,
#13322,#13323,#13324,#13325,#13326,#13327,#13328,#13329,#13330,#13331,#13332,
#13333,#13334,#13335,#13336,#13337,#13338,#13339,#13340,#13341,#13342,#13343,
#13344,#13345,#13346,#13347,#13348,#13349,#13350,#13351,#13352,#13353,#13354,
#13355,#13356,#13357,#13358,#13359,#13360,#13361,#13362,#13363,#13364,#13365,
#13366,#13367,#13368,#13369,#13370,#13371,#13372,#13373,#13374,#13375,#13376,
#13377,#13378,#13379,#13380,#13381,#13382,#13383,#13384,#13385,#13386,#13387,
#13388,#13389,#13390,#13391,#13392,#13393,#13394,#13395,#13396,#13397,#13398,
#13399,#13400,#13401,#13402,#13403,#13404,#13405,#13406,#13407,#13408,#13409,
#13410,#13411,#13412,#13413,#13414,#13415,#13416,#13417,#13418,#13419,#13420,
#13421,#13422,#13423,#13424,#13425,#13426,#13427,#13428,#13429,#13430,#13431,
#13432,#13433,#13434,#13435,#13436,#13437,#13438,#13439,#13440,#13441,#13442,
#13443,#13444,#13445,#13446,#13447,#13448,#13449,#13450,#13451,#13452,#13453,
#13454,#13455,#13456,#13457,#13458,#13459,#13460,#13461,#13462,#13463,#13464,
#13465,#13466,#13467,#13468,#13469,#13470,#13471,#13472,#13473,#13474,#13475,
#13476,#13477,#13478,#13479,#13480,#13481,#13482,#13483,#13484,#13485,#13486,
#13487,#13488,#13489,#13490,#13491,#13492,#13493,#13494,#13495,#13496,#13497,
#13498,#13499,#13500,#13501,#13502,#13503,#13504,#13505,#13506,#13507,#13508,
#13509,#13510,#13511,#13512,#13513,#13514,#13515,#13516,#13517,#13518,#13519,
#13520,#13521,#13522,#13523,#13524,#13525,#13526,#13527,#13528,#13529,#13530,
#13531),.UNSPECIFIED.,.F.,.F.,(4,3,3,3,3,3,3,3,3,3,3,3,3,3,3,3,3,3,3,3,
3,3,3,3,3,3,3,3,3,3,3,3,3,3,3,3,3,3,3,3,3,3,3,3,3,3,3,3,3,3,3,3,3,3,3,3,
3,3,3,3,3,3,3,3,3,3,3,3,3,3,3,3,3,3,3,4),(-41.7918608832718,-41.7045602143125,
-41.6173582380344,-41.529174022133,-41.4420878044719,-41.3550194181906,
-41.2679464497759,-41.1789309650378,-41.0917343409792,-41.0018094259014,
-40.9118845108235,-40.823311361517,-40.7348525684672,-40.6464843560947,
-40.5549280202198,-40.466661376663,-40.3784079860458,-40.2901465037774,
-40.2018555846002,-40.1134645990067,-40.0250140107227,-39.9364340859845,
-39.9140336690961,-39.8254605197895,-39.7370017267396,-39.6486335143673,
-39.5570771784925,-39.4688105349357,-39.3805571443185,-39.2922956620502,
-39.2040047428731,-39.1156137572796,-39.027163168995,-38.9385832442569,
-38.9161828273687,-38.8276096780622,-38.7391508850123,-38.6507826726396,
-38.5592263367648,-38.470959693208,-38.3827063025907,-38.2944448203224,
-38.2061539011449,-38.1177629155515,-38.0293123272675,-37.9407324025291,
-37.9183319856413,-37.8297588363347,-37.7413000432849,-37.6529318309125,
-37.5613754950377,-37.4731088514809,-37.3848554608634,-37.2965939785949,
-37.2083030594178,-37.1199120738244,-37.0314614855404,-36.942881560802,
-36.9204811439139,-36.8319079946074,-36.7434492015581,-36.6550809891854,
-36.5635246533106,-36.4752580097538,-36.3870046191366,-36.2987431368686,
-36.2104522176913,-36.122061232098,-36.0336106438137,-35.9450307190755,
-35.9226303021865,-35.8250780890747,-35.727916662375,-35.6310133550191,
-35.5344973374085,-35.5086757767519),.UNSPECIFIED.);
#1241=B_SPLINE_CURVE_WITH_KNOTS('',3,(#13533,#13534,#13535,#13536,#13537,
#13538,#13539,#13540,#13541,#13542,#13543),.UNSPECIFIED.,.F.,.F.,(4,1,1,
1,1,1,1,1,4),(-48.0750461904514,-47.8968404029153,-46.8989895611879,-45.9011387194605,
-44.9032878777331,-43.9054370360057,-42.9075861942783,-41.9097353525509,
-41.7918608832718),.UNSPECIFIED.);
#1242=B_SPLINE_CURVE_WITH_KNOTS('',3,(#13545,#13546,#13547,#13548,#13549,
#13550,#13551,#13552,#13553,#13554,#13555,#13556,#13557,#13558,#13559,#13560,
#13561,#13562,#13563,#13564,#13565,#13566,#13567,#13568,#13569,#13570,#13571,
#13572,#13573,#13574,#13575,#13576,#13577,#13578,#13579,#13580,#13581,#13582,
#13583,#13584,#13585,#13586,#13587,#13588,#13589,#13590,#13591,#13592,#13593,
#13594,#13595,#13596,#13597,#13598,#13599,#13600,#13601,#13602,#13603,#13604,
#13605,#13606,#13607,#13608,#13609,#13610,#13611,#13612,#13613,#13614,#13615,
#13616,#13617,#13618,#13619,#13620,#13621,#13622,#13623,#13624,#13625,#13626,
#13627,#13628,#13629,#13630,#13631,#13632,#13633,#13634,#13635,#13636,#13637,
#13638,#13639,#13640,#13641,#13642,#13643,#13644,#13645,#13646,#13647,#13648,
#13649,#13650,#13651,#13652,#13653,#13654,#13655,#13656,#13657,#13658,#13659,
#13660,#13661,#13662,#13663,#13664,#13665,#13666,#13667,#13668,#13669,#13670,
#13671,#13672,#13673,#13674,#13675,#13676,#13677,#13678,#13679,#13680,#13681,
#13682,#13683,#13684,#13685,#13686,#13687,#13688,#13689,#13690,#13691,#13692,
#13693,#13694,#13695,#13696,#13697,#13698,#13699,#13700,#13701,#13702,#13703,
#13704,#13705,#13706,#13707,#13708,#13709,#13710,#13711,#13712,#13713,#13714,
#13715,#13716,#13717,#13718,#13719,#13720,#13721,#13722,#13723,#13724,#13725,
#13726,#13727,#13728,#13729,#13730,#13731,#13732,#13733,#13734,#13735,#13736,
#13737,#13738,#13739,#13740,#13741,#13742,#13743,#13744,#13745,#13746,#13747,
#13748,#13749,#13750,#13751,#13752,#13753,#13754,#13755,#13756,#13757,#13758,
#13759,#13760,#13761,#13762,#13763,#13764,#13765,#13766,#13767,#13768,#13769,
#13770),.UNSPECIFIED.,.F.,.F.,(4,3,3,3,3,3,3,3,3,3,3,3,3,3,3,3,3,3,3,3,
3,3,3,3,3,3,3,3,3,3,3,3,3,3,3,3,3,3,3,3,3,3,3,3,3,3,3,3,3,3,3,3,3,3,3,3,
3,3,3,3,3,3,3,3,3,3,3,3,3,3,3,3,3,3,3,4),(-54.3582314975006,-54.2647917556389,
-54.1695801800491,-54.0757075390233,-53.9798264961515,-53.8839454532797,
-53.7953723039732,-53.7069135109234,-53.6185452985508,-53.526988962676,
-53.4387223191192,-53.3504689285019,-53.2622074462337,-53.1739165270565,
-53.0855255414631,-52.9970749531788,-52.9084950284406,-52.8860946115523,
-52.7975214622457,-52.709062669196,-52.6206944568234,-52.5291381209486,
-52.4408714773918,-52.3526180867744,-52.2643566045061,-52.176065685329,
-52.0876746997355,-51.9992241114512,-51.9106441867131,-51.8882437698249,
-51.7996706205183,-51.7112118274686,-51.622843615096,-51.5312872792212,
-51.4430206356644,-51.354767245047,-51.2665057627787,-51.1782148436015,
-51.089823858008,-51.0013732697238,-50.9127933449856,-50.8903929280975,
-50.8018197787909,-50.7133609857412,-50.6249927733686,-50.5334364374938,
-50.445169793937,-50.3569164033197,-50.2686549210514,-50.1803640018742,
-50.0919730162807,-50.0035224279965,-49.9149425032583,-49.8925420863701,
-49.8039689370635,-49.7155101440138,-49.6271419316412,-49.5355855957664,
-49.4473189522096,-49.3590655615923,-49.270804079324,-49.1825131601468,
-49.0941221745533,-49.0056715862691,-48.9170916615308,-48.8946912446427,
-48.8074317150173,-48.7158835244466,-48.6288408914097,-48.5418520352153,
-48.4548944238513,-48.3679455587705,-48.2809477662494,-48.1939214043438,
-48.1068026622736,-48.0750461904514),.UNSPECIFIED.);
#1243=B_SPLINE_CURVE_WITH_KNOTS('',3,(#13772,#13773,#13774,#13775,#13776,
#13777,#13778,#13779,#13780,#13781,#13782,#13783,#13784,#13785,#13786,#13787,
#13788,#13789,#13790,#13791,#13792,#13793,#13794,#13795,#13796,#13797,#13798,
#13799,#13800,#13801,#13802,#13803,#13804,#13805,#13806,#13807,#13808,#13809,
#13810,#13811,#13812,#13813,#13814,#13815,#13816,#13817,#13818,#13819,#13820,
#13821,#13822,#13823,#13824,#13825,#13826,#13827,#13828,#13829,#13830,#13831,
#13832,#13833,#13834,#13835,#13836,#13837,#13838,#13839,#13840,#13841,#13842,
#13843,#13844,#13845,#13846,#13847,#13848,#13849,#13850,#13851,#13852,#13853,
#13854,#13855,#13856,#13857,#13858,#13859,#13860,#13861,#13862,#13863,#13864,
#13865,#13866,#13867,#13868,#13869,#13870,#13871,#13872,#13873,#13874,#13875,
#13876,#13877,#13878,#13879,#13880,#13881,#13882,#13883,#13884,#13885,#13886,
#13887,#13888,#13889,#13890,#13891,#13892,#13893,#13894,#13895,#13896,#13897,
#13898,#13899,#13900,#13901,#13902,#13903,#13904,#13905,#13906,#13907,#13908,
#13909,#13910,#13911,#13912,#13913,#13914,#13915,#13916,#13917,#13918,#13919,
#13920,#13921,#13922,#13923,#13924,#13925,#13926,#13927,#13928,#13929,#13930,
#13931,#13932,#13933,#13934,#13935,#13936,#13937,#13938,#13939,#13940,#13941,
#13942,#13943,#13944,#13945,#13946,#13947,#13948,#13949,#13950,#13951,#13952,
#13953,#13954,#13955,#13956,#13957,#13958,#13959,#13960,#13961,#13962,#13963,
#13964,#13965,#13966,#13967,#13968,#13969,#13970,#13971,#13972,#13973,#13974,
#13975,#13976,#13977,#13978,#13979,#13980,#13981,#13982,#13983,#13984,#13985,
#13986,#13987,#13988,#13989,#13990,#13991,#13992,#13993,#13994,#13995,#13996,
#13997),.UNSPECIFIED.,.F.,.F.,(4,3,3,3,3,3,3,3,3,3,3,3,3,3,3,3,3,3,3,3,
3,3,3,3,3,3,3,3,3,3,3,3,3,3,3,3,3,3,3,3,3,3,3,3,3,3,3,3,3,3,3,3,3,3,3,3,
3,3,3,3,3,3,3,3,3,3,3,3,3,3,3,3,3,3,3,4),(-60.6414168048105,-60.554197711858,
-60.4670437575023,-60.3799239860027,-60.2928160031432,-60.2056974286979,
-60.1184916829168,-60.0312413217147,-59.9438501869995,-59.8710505036442,
-59.7824773543376,-59.6940185612878,-59.6056503489153,-59.5140940130405,
-59.4258273694837,-59.3375739788664,-59.2493124965982,-59.161021577421,
-59.0726305918274,-58.9841800035434,-58.8956000788052,-58.8731996619168,
-58.7846265126102,-58.6961677195605,-58.607799507188,-58.5162431713132,
-58.4279765277564,-58.3397231371391,-58.2514616548708,-58.1631707356939,
-58.0747797501003,-57.986329161816,-57.8977492370779,-57.8753488201894,
-57.7867756708829,-57.6983168778333,-57.6099486654606,-57.5183923295858,
-57.430125686029,-57.3418722954117,-57.2536108131436,-57.1653198939667,
-57.0769289083732,-56.9884783200889,-56.8998983953508,-56.877497978462,
-56.7889248291554,-56.7004660361058,-56.6120978237337,-56.5205414878588,
-56.432274844302,-56.3440214536848,-56.2557599714167,-56.1674690522392,
-56.0790780666456,-55.9906274783613,-55.9020475536231,-55.8796471367345,
-55.7910739874278,-55.7026151943779,-55.6142469820052,-55.5226906461304,
-55.4344240025736,-55.3461706119563,-55.2579091296881,-55.1696182105107,
-55.0812272249172,-54.9927766366329,-54.9041967118949,-54.8817962950071,
-54.7896385149841,-54.6976344620866,-54.6058196949302,-54.5141167775383,
-54.4225461234989,-54.358231497631),.UNSPECIFIED.);
#1244=B_SPLINE_CURVE_WITH_KNOTS('',3,(#13999,#14000,#14001,#14002,#14003,
#14004,#14005,#14006,#14007,#14008,#14009),.UNSPECIFIED.,.F.,.F.,(4,1,1,
1,1,1,1,1,4),(-66.9246021119902,-66.856006395736,-65.8581555540086,-64.8603047122812,
-63.8624538705538,-62.8646030288264,-61.866752187099,-60.8689013453716,
-60.6414168048105),.UNSPECIFIED.);
#1245=B_SPLINE_CURVE_WITH_KNOTS('',3,(#14011,#14012,#14013,#14014,#14015,
#14016,#14017,#14018,#14019,#14020,#14021,#14022,#14023,#14024,#14025,#14026,
#14027,#14028,#14029,#14030,#14031,#14032,#14033,#14034,#14035,#14036,#14037,
#14038,#14039,#14040,#14041,#14042,#14043,#14044,#14045,#14046,#14047,#14048,
#14049,#14050,#14051,#14052,#14053,#14054,#14055,#14056,#14057,#14058,#14059,
#14060,#14061,#14062,#14063,#14064,#14065,#14066,#14067,#14068,#14069,#14070,
#14071,#14072,#14073,#14074,#14075,#14076,#14077,#14078,#14079,#14080,#14081,
#14082,#14083,#14084,#14085,#14086,#14087,#14088,#14089,#14090,#14091,#14092,
#14093,#14094,#14095,#14096,#14097,#14098,#14099,#14100,#14101,#14102,#14103,
#14104,#14105,#14106,#14107,#14108,#14109,#14110,#14111,#14112,#14113,#14114,
#14115,#14116,#14117,#14118,#14119,#14120,#14121,#14122,#14123,#14124,#14125,
#14126,#14127,#14128,#14129,#14130,#14131,#14132,#14133,#14134,#14135,#14136,
#14137,#14138,#14139,#14140,#14141,#14142,#14143,#14144,#14145,#14146,#14147,
#14148,#14149,#14150,#14151,#14152,#14153,#14154,#14155,#14156,#14157,#14158,
#14159,#14160,#14161,#14162,#14163,#14164,#14165,#14166,#14167,#14168,#14169,
#14170,#14171,#14172,#14173,#14174,#14175,#14176,#14177,#14178,#14179,#14180,
#14181,#14182,#14183,#14184,#14185,#14186,#14187,#14188,#14189,#14190,#14191,
#14192,#14193,#14194,#14195,#14196,#14197,#14198,#14199,#14200,#14201,#14202,
#14203,#14204,#14205,#14206,#14207,#14208,#14209,#14210,#14211,#14212,#14213,
#14214,#14215,#14216,#14217,#14218,#14219,#14220,#14221,#14222,#14223,#14224,
#14225,#14226,#14227,#14228,#14229,#14230,#14231,#14232,#14233,#14234,#14235,
#14236),.UNSPECIFIED.,.F.,.F.,(4,3,3,3,3,3,3,3,3,3,3,3,3,3,3,3,3,3,3,3,
3,3,3,3,3,3,3,3,3,3,3,3,3,3,3,3,3,3,3,3,3,3,3,3,3,3,3,3,3,3,3,3,3,3,3,3,
3,3,3,3,3,3,3,3,3,3,3,3,3,3,3,3,3,3,3,4),(-73.2077874189366,-73.1077360066987,
-73.0072421038388,-72.9061731673704,-72.8431114461004,-72.7545382967938,
-72.6660795037441,-72.5777112913716,-72.4861549554968,-72.3978883119399,
-72.3096349213225,-72.2213734390542,-72.133082519877,-72.0446915342834,
-71.9562409459991,-71.8676610212609,-71.845260604373,-71.7566874550664,
-71.6682286620166,-71.5798604496439,-71.4883041137691,-71.4000374702123,
-71.311784079595,-71.2235225973267,-71.1352316781495,-71.046840692556,-70.9583901042718,
-70.8698101795335,-70.8474097626456,-70.758836613339,-70.6703778202893,
-70.5820096079168,-70.4904532720419,-70.4021866284851,-70.3139332378678,
-70.2256717555995,-70.1373808364224,-70.0489898508289,-69.9605392625447,
-69.8719593378065,-69.8495589209182,-69.7609857716116,-69.6725269785619,
-69.5841587661893,-69.4926024303144,-69.4043357867576,-69.3160823961403,
-69.227820913872,-69.1395299946948,-69.0511390091013,-68.962688420817,-68.8741084960788,
-68.8517080791908,-68.7631349298842,-68.6746761368344,-68.5863079244618,
-68.494751588587,-68.4064849450302,-68.3182315544129,-68.2299700721446,
-68.1416791529674,-68.0532881673739,-67.9648375790896,-67.8762576543515,
-67.8538572374634,-67.7661482579468,-67.6785529256837,-67.5910465431623,
-67.5036029660177,-67.416191807519,-67.3287908976864,-67.24137807933,-67.1538814321558,
-67.066339207297,-66.9786674844112,-66.9246021119902),.UNSPECIFIED.);
#1246=B_SPLINE_CURVE_WITH_KNOTS('',3,(#14238,#14239,#14240,#14241,#14242,
#14243,#14244,#14245,#14246,#14247,#14248,#14249,#14250,#14251,#14252,#14253,
#14254,#14255,#14256,#14257,#14258,#14259,#14260,#14261,#14262,#14263,#14264,
#14265,#14266,#14267,#14268,#14269,#14270,#14271,#14272,#14273,#14274,#14275,
#14276,#14277,#14278,#14279,#14280,#14281,#14282,#14283,#14284,#14285,#14286,
#14287,#14288,#14289,#14290,#14291,#14292,#14293,#14294,#14295,#14296,#14297,
#14298,#14299,#14300,#14301,#14302,#14303,#14304,#14305,#14306,#14307,#14308,
#14309,#14310,#14311,#14312,#14313,#14314,#14315,#14316,#14317,#14318,#14319,
#14320,#14321,#14322,#14323,#14324,#14325,#14326,#14327,#14328,#14329,#14330,
#14331,#14332,#14333,#14334,#14335,#14336,#14337,#14338,#14339,#14340,#14341,
#14342,#14343,#14344,#14345,#14346,#14347,#14348,#14349,#14350,#14351,#14352,
#14353,#14354,#14355,#14356,#14357,#14358,#14359,#14360,#14361,#14362,#14363,
#14364,#14365,#14366,#14367,#14368,#14369,#14370,#14371,#14372,#14373,#14374,
#14375,#14376,#14377,#14378,#14379,#14380,#14381,#14382,#14383,#14384,#14385,
#14386,#14387,#14388,#14389,#14390,#14391,#14392,#14393,#14394,#14395,#14396,
#14397,#14398,#14399,#14400,#14401,#14402,#14403,#14404,#14405,#14406,#14407,
#14408,#14409,#14410,#14411,#14412,#14413,#14414,#14415,#14416,#14417,#14418,
#14419,#14420,#14421,#14422,#14423,#14424,#14425,#14426,#14427,#14428,#14429,
#14430,#14431,#14432,#14433,#14434,#14435,#14436,#14437,#14438,#14439,#14440,
#14441,#14442,#14443,#14444,#14445,#14446,#14447,#14448,#14449,#14450,#14451,
#14452,#14453,#14454,#14455,#14456,#14457,#14458,#14459,#14460,#14461,#14462,
#14463),.UNSPECIFIED.,.F.,.F.,(4,3,3,3,3,3,3,3,3,3,3,3,3,3,3,3,3,3,3,3,
3,3,3,3,3,3,3,3,3,3,3,3,3,3,3,3,3,3,3,3,3,3,3,3,3,3,3,3,3,3,3,3,3,3,3,3,
3,3,3,3,3,3,3,3,3,3,3,3,3,3,3,3,3,3,3,4),(-79.4909727263493,-79.4027030535825,
-79.3144454917003,-79.2261787933953,-79.137881709884,-79.0494784849831,
-78.9610151902704,-78.8724102190023,-78.8302164964648,-78.7416433471582,
-78.6531845541085,-78.564816341736,-78.4732600058611,-78.3849933623043,
-78.296739971687,-78.2084784894188,-78.1201875702418,-78.0317965846482,
-77.9433459963641,-77.8547660716259,-77.8323656547374,-77.7437925054308,
-77.655333712381,-77.5669655000085,-77.4754091641337,-77.3871425205769,
-77.2988891299597,-77.2106276476916,-77.1223367285145,-77.033945742921,
-76.9454951546369,-76.8569152298987,-76.83451481301,-76.7459416637034,-76.6574828706536,
-76.5691146582808,-76.477558322406,-76.3892916788491,-76.3010382882317,
-76.2127768059632,-76.1244858867861,-76.0360949011925,-75.9476443129081,
-75.85906438817,-75.8366639712826,-75.7480908219759,-75.659632028926,-75.5712638165536,
-75.4797074806788,-75.3914408371219,-75.3031874465046,-75.2149259642361,
-75.1266350450588,-75.0382440594654,-74.9497934711811,-74.8612135464427,
-74.8388131295552,-74.7502399802486,-74.6617811871993,-74.5734129748265,
-74.4818566389517,-74.3935899953948,-74.3053366047776,-74.2170751225096,
-74.128784203332,-74.0403932177385,-73.9519426294543,-73.8633627047161,
-73.8409622878278,-73.7518618126712,-73.6628783053694,-73.5739909580721,
-73.4824400733465,-73.3936855521496,-73.3007364856597,-73.2077874191697),
 .UNSPECIFIED.);
#1247=B_SPLINE_CURVE_WITH_KNOTS('',3,(#14465,#14466,#14467,#14468,#14469,
#14470,#14471,#14472,#14473,#14474),.UNSPECIFIED.,.F.,.F.,(4,1,1,1,1,1,
1,4),(-85.7741526916333,-84.8173215468292,-83.8194707051018,-82.8216198633744,
-81.823769021647,-80.8259181799196,-79.8280673381922,-79.4909799947471),
 .UNSPECIFIED.);
#1248=B_SPLINE_CURVE_WITH_KNOTS('',3,(#14476,#14477,#14478,#14479,#14480,
#14481,#14482,#14483,#14484,#14485,#14486,#14487,#14488,#14489,#14490,#14491,
#14492,#14493,#14494,#14495,#14496,#14497,#14498,#14499,#14500,#14501,#14502,
#14503,#14504,#14505,#14506,#14507,#14508,#14509,#14510,#14511,#14512,#14513,
#14514,#14515,#14516,#14517,#14518,#14519,#14520,#14521,#14522,#14523,#14524,
#14525,#14526,#14527,#14528,#14529,#14530,#14531,#14532,#14533,#14534,#14535,
#14536,#14537,#14538,#14539,#14540,#14541,#14542,#14543,#14544,#14545,#14546,
#14547,#14548,#14549,#14550,#14551,#14552,#14553,#14554,#14555,#14556,#14557,
#14558,#14559,#14560,#14561,#14562,#14563,#14564,#14565,#14566,#14567,#14568,
#14569,#14570,#14571,#14572,#14573,#14574,#14575,#14576,#14577,#14578,#14579,
#14580,#14581,#14582,#14583,#14584,#14585,#14586,#14587,#14588,#14589,#14590,
#14591,#14592,#14593,#14594,#14595,#14596,#14597,#14598,#14599,#14600,#14601,
#14602,#14603,#14604,#14605,#14606,#14607,#14608,#14609,#14610,#14611,#14612,
#14613,#14614,#14615,#14616,#14617,#14618,#14619,#14620,#14621,#14622,#14623,
#14624,#14625,#14626,#14627,#14628,#14629,#14630,#14631,#14632,#14633,#14634,
#14635,#14636,#14637,#14638,#14639,#14640,#14641,#14642,#14643,#14644,#14645,
#14646,#14647,#14648,#14649,#14650,#14651,#14652,#14653,#14654,#14655,#14656,
#14657,#14658,#14659,#14660,#14661,#14662,#14663,#14664,#14665,#14666,#14667,
#14668,#14669,#14670,#14671,#14672,#14673,#14674,#14675,#14676,#14677,#14678,
#14679,#14680,#14681,#14682,#14683,#14684,#14685,#14686,#14687,#14688,#14689,
#14690,#14691,#14692,#14693,#14694,#14695,#14696,#14697,#14698,#14699,#14700,
#14701,#14702,#14703,#14704),.UNSPECIFIED.,.F.,.F.,(4,3,3,3,3,3,3,3,3,3,
3,3,3,3,3,3,3,3,3,3,3,3,3,3,3,3,3,3,3,3,3,3,3,3,3,3,3,3,3,3,3,3,3,3,3,3,
3,3,3,3,3,3,3,3,3,3,3,3,3,3,3,3,3,3,3,3,3,3,3,3,3,3,3,3,3,3,4),(-92.0573432033913,
-91.9449585863266,-91.830194852235,-91.8022774389211,-91.7137042896145,
-91.6252454965648,-91.5368772841921,-91.4453209483173,-91.3570543047604,
-91.2688009141431,-91.1805394318749,-91.0922485126977,-91.0038575271042,
-90.91540693882,-90.8268270140818,-90.8044265971936,-90.715853447887,-90.6273946548373,
-90.5390264424647,-90.4474701065899,-90.3592034630331,-90.2709500724158,
-90.1826885901474,-90.0943976709703,-90.0060066853768,-89.9175560970926,
-89.8289761723544,-89.8065757554662,-89.7180026061596,-89.6295438131099,
-89.5411756007373,-89.4496192648625,-89.3613526213056,-89.2730992306883,
-89.18483774842,-89.0965468292428,-89.0081558436493,-88.919705255365,-88.8311253306268,
-88.8087249137388,-88.7201517644322,-88.6316929713825,-88.5433247590099,
-88.4517684231351,-88.3635017795783,-88.275248388961,-88.1869869066927,
-88.0986959875155,-88.010305001922,-87.9218544136378,-87.8332744888996,
-87.8108740720114,-87.7223009227048,-87.6338421296551,-87.5454739172824,
-87.4539175814076,-87.3656509378508,-87.2773975472335,-87.1891360649651,
-87.100845145788,-87.0124541601946,-86.9240035719104,-86.8354236471722,
-86.813023230284,-86.7244500809774,-86.6359912879277,-86.5476230755552,
-86.4560667396804,-86.3678000961236,-86.2795467055063,-86.191285223238,
-86.1029943040609,-86.0146033184674,-85.9261527301832,-85.837572805445,
-85.8151723885566,-85.7741580335289),.UNSPECIFIED.);
#1249=B_SPLINE_CURVE_WITH_KNOTS('',3,(#14706,#14707,#14708,#14709,#14710,
#14711,#14712,#14713,#14714,#14715),.UNSPECIFIED.,.F.,.F.,(4,1,1,1,1,1,
1,4),(-98.3405286478881,-97.7893824892855,-96.791531647558,-95.7936808058307,
-94.7958299641032,-93.7979791223758,-92.8001282806485,-92.0573433407085),
 .UNSPECIFIED.);
#1250=B_SPLINE_CURVE_WITH_KNOTS('',3,(#14717,#14718,#14719,#14720,#14721,
#14722,#14723,#14724,#14725,#14726),.UNSPECIFIED.,.F.,.F.,(4,1,1,1,1,1,
1,4),(-104.623706641862,-103.77648753965,-102.778636697922,-101.780785856195,
-100.782935014468,-99.7850841727403,-98.7872333310129,-98.3405286478881),
 .UNSPECIFIED.);
#1251=B_SPLINE_CURVE_WITH_KNOTS('',3,(#14728,#14729,#14730,#14731,#14732,
#14733,#14734,#14735,#14736,#14737,#14738,#14739,#14740,#14741,#14742,#14743,
#14744,#14745,#14746,#14747,#14748,#14749,#14750,#14751,#14752,#14753,#14754,
#14755,#14756,#14757,#14758,#14759,#14760,#14761,#14762,#14763,#14764,#14765,
#14766,#14767,#14768,#14769,#14770,#14771,#14772,#14773,#14774,#14775,#14776,
#14777,#14778,#14779,#14780,#14781,#14782,#14783,#14784,#14785,#14786,#14787,
#14788,#14789,#14790,#14791,#14792,#14793,#14794,#14795,#14796,#14797,#14798,
#14799,#14800,#14801,#14802,#14803,#14804,#14805,#14806,#14807,#14808,#14809,
#14810,#14811,#14812,#14813,#14814,#14815,#14816,#14817,#14818,#14819,#14820,
#14821,#14822,#14823,#14824,#14825,#14826,#14827,#14828,#14829,#14830,#14831,
#14832,#14833,#14834,#14835,#14836,#14837,#14838,#14839,#14840,#14841,#14842,
#14843,#14844,#14845,#14846,#14847,#14848,#14849,#14850,#14851,#14852,#14853,
#14854,#14855,#14856,#14857,#14858,#14859,#14860,#14861,#14862,#14863,#14864,
#14865,#14866,#14867,#14868,#14869,#14870,#14871,#14872,#14873,#14874,#14875,
#14876,#14877,#14878,#14879,#14880,#14881,#14882,#14883,#14884,#14885,#14886,
#14887,#14888,#14889,#14890,#14891,#14892,#14893,#14894,#14895,#14896,#14897,
#14898,#14899,#14900,#14901,#14902,#14903,#14904,#14905,#14906,#14907,#14908,
#14909,#14910,#14911,#14912,#14913,#14914,#14915,#14916,#14917,#14918,#14919,
#14920,#14921,#14922,#14923,#14924,#14925,#14926,#14927,#14928,#14929,#14930,
#14931,#14932,#14933,#14934,#14935,#14936,#14937,#14938,#14939,#14940,#14941,
#14942,#14943,#14944,#14945,#14946,#14947,#14948,#14949,#14950),
 .UNSPECIFIED.,.F.,.F.,(4,3,3,3,3,3,3,3,3,3,3,3,3,3,3,3,3,3,3,3,3,3,3,3,
3,3,3,3,3,3,3,3,3,3,3,3,3,3,3,3,3,3,3,3,3,3,3,3,3,3,3,3,3,3,3,3,3,3,3,3,
3,3,3,3,3,3,3,3,3,3,3,3,3,3,4),(-110.906899262247,-110.761443431742,-110.672870261492,
-110.584411447275,-110.496043213538,-110.404486885598,-110.316220220321,
-110.22796680789,-110.139705303736,-110.051414362625,-109.963023355137,
-109.874572744955,-109.785992798481,-109.763592590014,-109.675019440711,
-109.586560647612,-109.498192435137,-109.406636099281,-109.318369455489,
-109.230116064587,-109.141854581985,-109.053563662425,-108.965172676378,
-108.876722087598,-108.788142162306,-108.765741748287,-108.677168604673,
-108.588709817407,-108.500341610901,-108.408785272858,-108.320518635341,
-108.232265250816,-108.144003774687,-108.05571286169,-107.967321882306,
-107.878871300257,-107.790291381742,-107.767890906559,-107.679317754033,
-107.590858957727,-107.502490742065,-107.410934407411,-107.322667760504,
-107.234414366519,-107.14615288087,-107.057861958303,-106.969470969322,
-106.881020377648,-106.792440449541,-106.770040064832,-106.681466915798,
-106.593008123017,-106.504639910909,-106.413083574933,-106.324816931629,
-106.236563541259,-106.148302059232,-106.060011140292,-105.971620154925,
-105.883169566862,-105.794589642336,-105.772189223105,-105.68361607452,
-105.595157282203,-105.506789070576,-105.415232734426,-105.326966091637,
-105.238712701796,-105.15045122031,-105.062160301921,-104.97376931712,-104.885318729632,
-104.79673880569,-104.774338381377,-104.623713955068),.UNSPECIFIED.);
#1252=B_SPLINE_CURVE_WITH_KNOTS('',3,(#14952,#14953,#14954,#14955,#14956,
#14957,#14958,#14959,#14960,#14961),.UNSPECIFIED.,.F.,.F.,(4,1,1,1,1,1,
1,4),(-117.19008011828,-116.748548482106,-115.750697640379,-114.752846798651,
-113.754995956924,-112.757145115197,-111.759294273469,-110.906906884946),
 .UNSPECIFIED.);
#1253=B_SPLINE_CURVE_WITH_KNOTS('',3,(#14963,#14964,#14965,#14966,#14967,
#14968,#14969,#14970,#14971,#14972,#14973,#14974,#14975,#14976,#14977,#14978,
#14979,#14980,#14981,#14982,#14983,#14984,#14985,#14986,#14987,#14988,#14989,
#14990,#14991,#14992,#14993,#14994,#14995,#14996,#14997,#14998,#14999,#15000,
#15001,#15002,#15003,#15004,#15005,#15006,#15007,#15008,#15009,#15010,#15011,
#15012,#15013,#15014,#15015,#15016,#15017,#15018,#15019,#15020,#15021,#15022,
#15023,#15024,#15025,#15026,#15027,#15028,#15029,#15030,#15031,#15032,#15033,
#15034,#15035,#15036,#15037,#15038,#15039,#15040,#15041,#15042,#15043,#15044,
#15045,#15046,#15047,#15048,#15049,#15050,#15051,#15052,#15053,#15054,#15055,
#15056,#15057,#15058,#15059,#15060,#15061,#15062,#15063,#15064,#15065,#15066,
#15067,#15068,#15069,#15070,#15071,#15072,#15073,#15074,#15075,#15076,#15077,
#15078,#15079,#15080,#15081,#15082,#15083,#15084,#15085,#15086,#15087,#15088,
#15089,#15090,#15091,#15092,#15093,#15094,#15095,#15096,#15097,#15098,#15099,
#15100,#15101,#15102,#15103,#15104,#15105,#15106,#15107,#15108,#15109,#15110,
#15111,#15112,#15113,#15114,#15115,#15116,#15117,#15118,#15119,#15120,#15121,
#15122,#15123,#15124,#15125,#15126,#15127,#15128,#15129,#15130,#15131,#15132,
#15133,#15134,#15135,#15136,#15137,#15138,#15139,#15140,#15141,#15142,#15143,
#15144,#15145,#15146,#15147,#15148,#15149,#15150,#15151,#15152,#15153,#15154,
#15155,#15156,#15157,#15158,#15159,#15160,#15161,#15162,#15163,#15164,#15165,
#15166,#15167,#15168,#15169,#15170,#15171,#15172,#15173,#15174,#15175,#15176,
#15177,#15178,#15179,#15180,#15181,#15182,#15183,#15184,#15185,#15186,#15187,
#15188),.UNSPECIFIED.,.F.,.F.,(4,3,3,3,3,3,3,3,3,3,3,3,3,3,3,3,3,3,3,3,
3,3,3,3,3,3,3,3,3,3,3,3,3,3,3,3,3,3,3,3,3,3,3,3,3,3,3,3,3,3,3,3,3,3,3,3,
3,3,3,3,3,3,3,3,3,3,3,3,3,3,3,3,3,3,3,4),(-123.473269876606,-123.385963817173,
-123.298706638601,-123.211472892286,-123.124240298723,-123.036986583253,
-122.949638453688,-122.862236484049,-122.774701382474,-122.735653532471,
-122.64705600505,-122.558572741542,-122.470179996843,-122.378632833581,
-122.290341662701,-122.202063789463,-122.113777896155,-122.025462664474,
-121.937047636497,-121.848573134328,-121.759969668638,-121.737802690743,
-121.649211601926,-121.560734519507,-121.472347691821,-121.38079821147,
-121.292512254859,-121.204239325495,-121.115958098892,-121.027647249759,
-120.93923615818,-120.850765336606,-120.762165146963,-120.739951849016,
-120.651395452075,-120.562953632999,-120.474602594572,-120.383039896162,
-120.294790817753,-120.206555107228,-120.118311401479,-120.030038336789,
-119.941665231825,-119.853232561338,-119.764670471248,-119.742101007288,
-119.653523259052,-119.565059836333,-119.476686969352,-119.385132368878,
-119.296861038376,-119.208602956949,-119.120336785073,-119.032041182565,
-118.943645546695,-118.855190321758,-118.766605816084,-118.744250165561,
-118.655675059032,-118.567214265706,-118.478844012632,-118.387288426532,
-118.299019653933,-118.210764105141,-118.122500437758,-118.0342073087,-117.945814087448,
-117.857361245723,-117.768779058712,-117.746399323834,-117.655351667581,
-117.564442627165,-117.47085311273,-117.380199332793,-117.28514195111,-117.190084569427),
 .UNSPECIFIED.);
#1254=B_SPLINE_CURVE_WITH_KNOTS('',3,(#15190,#15191,#15192,#15193,#15194,
#15195,#15196,#15197),.UNSPECIFIED.,.F.,.F.,(4,1,1,1,1,4),(-127.724907741108,
-126.72705689938,-125.729206057653,-124.731355215925,-123.733504374198,
-123.473272729035),.UNSPECIFIED.);
#1255=B_SPLINE_CURVE_WITH_KNOTS('',3,(#15201,#15202,#15203,#15204,#15205,
#15206,#15207,#15208,#15209,#15210,#15211,#15212,#15213,#15214,#15215,#15216,
#15217,#15218,#15219,#15220,#15221,#15222,#15223,#15224,#15225,#15226,#15227,
#15228,#15229,#15230,#15231,#15232,#15233,#15234,#15235,#15236,#15237,#15238,
#15239,#15240,#15241,#15242,#15243,#15244,#15245,#15246,#15247,#15248,#15249,
#15250,#15251,#15252,#15253,#15254,#15255,#15256,#15257,#15258,#15259,#15260,
#15261,#15262,#15263,#15264,#15265,#15266,#15267,#15268,#15269,#15270,#15271,
#15272,#15273,#15274,#15275,#15276,#15277,#15278,#15279,#15280,#15281,#15282,
#15283,#15284,#15285,#15286,#15287,#15288,#15289,#15290,#15291,#15292,#15293,
#15294,#15295,#15296,#15297,#15298,#15299,#15300,#15301,#15302,#15303,#15304,
#15305,#15306,#15307,#15308,#15309,#15310,#15311,#15312,#15313,#15314,#15315,
#15316,#15317,#15318,#15319,#15320,#15321,#15322,#15323,#15324,#15325,#15326,
#15327,#15328,#15329,#15330,#15331,#15332,#15333,#15334,#15335,#15336,#15337,
#15338,#15339,#15340,#15341,#15342,#15343,#15344,#15345,#15346,#15347,#15348,
#15349,#15350,#15351,#15352,#15353,#15354,#15355,#15356,#15357,#15358,#15359,
#15360,#15361,#15362,#15363,#15364,#15365,#15366,#15367,#15368,#15369,#15370,
#15371,#15372,#15373,#15374,#15375,#15376,#15377,#15378,#15379,#15380,#15381,
#15382,#15383,#15384,#15385,#15386,#15387),.UNSPECIFIED.,.F.,.F.,(4,3,3,
3,3,3,3,3,3,3,3,3,3,3,3,3,3,3,3,3,3,3,3,3,3,3,3,3,3,3,3,3,3,3,3,3,3,3,3,
3,3,3,3,3,3,3,3,3,3,3,3,3,3,3,3,3,3,3,3,3,3,3,4),(120.490566152121,120.603837052801,
120.71967464691,120.739951849016,120.828545137016,120.917023992194,121.005412168038,
121.096960983376,121.185247223457,121.273520042512,121.361800765146,121.450110716473,
121.538520332177,121.626989338908,121.715587232755,121.737802690743,121.826399174075,
121.91488156938,122.003273621172,122.094821110084,122.183112028445,122.271389812282,
122.359675779401,122.44799124832,122.536406754079,122.624881874923,122.71348616021,
122.735653532471,122.82410435621,122.912440558979,123.000686058367,123.092288347846,
123.180432724514,123.268564214759,123.356704288735,123.444874417773,123.5331461304,
123.62147818081,123.70994155568,123.733504374198,123.822247266296,123.910875376148,
123.999412284792,124.090905151184,124.179337895411,124.2677561418,124.356181059584,
124.444633817484,124.533183474876,124.62179107482,124.710524399572,124.731355215925,
124.819152681151,124.906838203155,124.994436379332,125.08197397875,125.169480475744,
125.256977959367,125.344488506912,125.432084824851,125.519727567832,125.607501981674,
125.66337244262),.UNSPECIFIED.);
#1256=B_SPLINE_CURVE_WITH_KNOTS('',3,(#15389,#15390,#15391,#15392,#15393,
#15394,#15395,#15396,#15397,#15398),.UNSPECIFIED.,.F.,.F.,(4,1,1,1,1,1,
1,4),(114.207380740144,114.752846798651,115.750697640379,116.748548482106,
117.746399323834,118.744250165561,119.742101007288,120.490566047323),
 .UNSPECIFIED.);
#1257=B_SPLINE_CURVE_WITH_KNOTS('',3,(#15400,#15401,#15402,#15403,#15404,
#15405,#15406,#15407,#15408,#15409,#15410,#15411,#15412,#15413,#15414,#15415,
#15416,#15417,#15418,#15419,#15420,#15421,#15422,#15423,#15424,#15425,#15426,
#15427,#15428,#15429,#15430,#15431,#15432,#15433,#15434,#15435,#15436,#15437,
#15438,#15439,#15440,#15441,#15442,#15443,#15444,#15445,#15446,#15447,#15448,
#15449,#15450,#15451,#15452,#15453,#15454,#15455,#15456,#15457,#15458,#15459,
#15460,#15461,#15462,#15463,#15464,#15465,#15466,#15467,#15468,#15469,#15470,
#15471,#15472,#15473,#15474,#15475,#15476,#15477,#15478,#15479,#15480,#15481,
#15482,#15483,#15484,#15485,#15486,#15487,#15488,#15489,#15490,#15491,#15492,
#15493,#15494,#15495,#15496,#15497,#15498,#15499,#15500,#15501,#15502,#15503,
#15504,#15505,#15506,#15507,#15508,#15509,#15510,#15511,#15512,#15513,#15514,
#15515,#15516,#15517,#15518,#15519,#15520,#15521,#15522,#15523,#15524,#15525,
#15526,#15527,#15528,#15529,#15530,#15531,#15532,#15533,#15534,#15535,#15536,
#15537,#15538,#15539,#15540,#15541,#15542,#15543,#15544,#15545,#15546,#15547,
#15548,#15549,#15550,#15551,#15552,#15553,#15554,#15555,#15556,#15557,#15558,
#15559,#15560,#15561,#15562,#15563,#15564,#15565,#15566,#15567,#15568,#15569,
#15570,#15571,#15572,#15573,#15574,#15575,#15576,#15577,#15578,#15579,#15580,
#15581,#15582,#15583,#15584,#15585,#15586,#15587,#15588,#15589,#15590,#15591,
#15592,#15593,#15594,#15595,#15596,#15597,#15598,#15599,#15600,#15601,#15602,
#15603,#15604,#15605,#15606,#15607,#15608,#15609,#15610,#15611,#15612,#15613,
#15614,#15615,#15616,#15617,#15618,#15619,#15620,#15621,#15622,#15623,#15624,
#15625),.UNSPECIFIED.,.F.,.F.,(4,3,3,3,3,3,3,3,3,3,3,3,3,3,3,3,3,3,3,3,
3,3,3,3,3,3,3,3,3,3,3,3,3,3,3,3,3,3,3,3,3,3,3,3,3,3,3,3,3,3,3,3,3,3,3,3,
3,3,3,3,3,3,3,3,3,3,3,3,3,3,3,3,3,3,3,4),(107.92419543314,108.011346351858,
108.098408182763,108.185408306089,108.272376673895,108.359335784728,108.446308125387,
108.53336836748,108.620475808099,108.70771888384,108.765741748287,108.854314898151,
108.942773691706,109.031141904533,109.122698240218,109.2109648841,109.299218274993,
109.38747975749,109.475770676847,109.564161662549,109.6526122509,109.741192175643,
109.763592590014,109.852165760785,109.940624575388,110.028992809377,110.120549137172,
110.208815802365,110.29706921459,110.385330718413,110.473621659069,110.562012665923,
110.650463275365,110.73904322095,110.761443431742,110.850016534348,110.938475280703,
111.026843446439,111.118399799818,111.206666397174,111.294919741829,111.383181178421,
111.471472052256,111.559862993227,111.648313537255,111.736893418609,111.759294273469,
111.847867440913,111.936326251761,112.024694481579,112.116250810781,112.204517470803,
112.292770877498,112.381032375441,112.469323309875,112.557714310034,112.646164912499,
112.734744850751,112.757145115197,112.845718398669,112.934177326567,113.022545674305,
113.114101959633,113.202368738992,113.290622265342,113.378883883128,113.467174937462,
113.555566056999,113.644016778682,113.732596834996,113.754995956924,113.850301728731,
113.945297041335,114.04010251559,114.134620297776,114.207380494539),
 .UNSPECIFIED.);
#1258=B_SPLINE_CURVE_WITH_KNOTS('',3,(#15627,#15628,#15629,#15630,#15631,
#15632,#15633,#15634,#15635,#15636,#15637,#15638,#15639,#15640,#15641,#15642,
#15643,#15644,#15645,#15646,#15647,#15648,#15649,#15650,#15651,#15652,#15653,
#15654,#15655,#15656,#15657,#15658,#15659,#15660,#15661,#15662,#15663,#15664,
#15665,#15666,#15667,#15668,#15669,#15670,#15671,#15672,#15673,#15674,#15675,
#15676,#15677,#15678,#15679,#15680,#15681,#15682,#15683,#15684,#15685,#15686,
#15687,#15688,#15689,#15690,#15691,#15692,#15693,#15694,#15695,#15696,#15697,
#15698,#15699,#15700,#15701,#15702,#15703,#15704,#15705,#15706,#15707,#15708,
#15709,#15710,#15711,#15712,#15713,#15714,#15715,#15716,#15717,#15718,#15719,
#15720,#15721,#15722,#15723,#15724,#15725,#15726,#15727,#15728,#15729,#15730,
#15731,#15732,#15733,#15734,#15735,#15736,#15737,#15738,#15739,#15740,#15741,
#15742,#15743,#15744,#15745,#15746,#15747,#15748,#15749,#15750,#15751,#15752,
#15753,#15754,#15755,#15756,#15757,#15758,#15759,#15760,#15761,#15762,#15763,
#15764,#15765,#15766,#15767,#15768,#15769,#15770,#15771,#15772,#15773,#15774,
#15775,#15776,#15777,#15778,#15779,#15780,#15781,#15782,#15783,#15784,#15785,
#15786,#15787,#15788,#15789,#15790,#15791,#15792,#15793,#15794,#15795,#15796,
#15797,#15798,#15799,#15800,#15801,#15802,#15803,#15804,#15805,#15806,#15807,
#15808,#15809,#15810,#15811,#15812,#15813,#15814,#15815,#15816,#15817,#15818,
#15819,#15820,#15821,#15822,#15823,#15824,#15825,#15826,#15827,#15828,#15829,
#15830,#15831,#15832,#15833,#15834,#15835,#15836,#15837,#15838,#15839,#15840,
#15841,#15842,#15843,#15844,#15845,#15846,#15847,#15848,#15849,#15850,#15851,
#15852),.UNSPECIFIED.,.F.,.F.,(4,3,3,3,3,3,3,3,3,3,3,3,3,3,3,3,3,3,3,3,
3,3,3,3,3,3,3,3,3,3,3,3,3,3,3,3,3,3,3,3,3,3,3,3,3,3,3,3,3,3,3,3,3,3,3,3,
3,3,3,3,3,3,3,3,3,3,3,3,3,3,3,3,3,3,3,4),(101.641010125785,101.780785856195,
101.869359005405,101.957817798359,102.046186010637,102.137742346547,102.22600899001,
102.314262380534,102.40252386271,102.490814781796,102.5792057673,102.667656355496,
102.756236280147,102.778636697922,102.867209847159,102.955668640139,103.04403685244,
103.135593188341,103.223859831825,103.312113222368,103.400374704562,103.488665623664,
103.577056609182,103.66550719739,103.754087122053,103.77648753965,103.865060689457,
103.953519483008,104.041887695882,104.133444031569,104.221710675627,104.309964066744,
104.39822554951,104.486516469182,104.574907455265,104.663358044036,104.751937969252,
104.774338381377,104.862911529898,104.951370322164,105.039738533755,105.131294869924,
105.219561512709,105.30781490256,105.396076384068,105.484367302492,105.572758287345,
105.661208874896,105.749788798917,105.772189223105,105.860762372204,105.949221165039,
106.037589377189,106.129145713144,106.217412356462,106.305665746834,106.393927228852,
106.482218147774,106.570609133106,106.659059721124,106.747639645593,106.770040064832,
106.858613217461,106.947072013844,107.035440229556,107.126996564182,107.215263211076,
107.303516605024,107.391778090612,107.480069013096,107.568460001958,107.656910593494,
107.745490521433,107.767890906559,107.913755880126,107.924195432964),
 .UNSPECIFIED.);
#1259=B_SPLINE_CURVE_WITH_KNOTS('',3,(#15854,#15855,#15856,#15857,#15858,
#15859,#15860,#15861,#15862,#15863),.UNSPECIFIED.,.F.,.F.,(4,1,1,1,1,1,
1,4),(95.3578296359417,95.7936808058306,96.791531647558,97.7893824892855,
98.7872333310129,99.7850841727403,100.782935014468,101.641002196766),
 .UNSPECIFIED.);
#1260=B_SPLINE_CURVE_WITH_KNOTS('',3,(#15865,#15866,#15867,#15868,#15869,
#15870,#15871,#15872,#15873,#15874,#15875,#15876,#15877,#15878,#15879,#15880,
#15881,#15882,#15883,#15884,#15885,#15886,#15887,#15888,#15889,#15890,#15891,
#15892,#15893,#15894,#15895,#15896,#15897,#15898,#15899,#15900,#15901,#15902,
#15903,#15904,#15905,#15906,#15907,#15908,#15909,#15910,#15911,#15912,#15913,
#15914,#15915,#15916,#15917,#15918,#15919,#15920,#15921,#15922,#15923,#15924,
#15925,#15926,#15927,#15928,#15929,#15930,#15931,#15932,#15933,#15934,#15935,
#15936,#15937,#15938,#15939,#15940,#15941,#15942,#15943,#15944,#15945,#15946,
#15947,#15948,#15949,#15950,#15951,#15952,#15953,#15954,#15955,#15956,#15957,
#15958,#15959,#15960,#15961,#15962,#15963,#15964,#15965,#15966,#15967,#15968,
#15969,#15970,#15971,#15972,#15973,#15974,#15975,#15976,#15977,#15978,#15979,
#15980,#15981,#15982,#15983,#15984,#15985,#15986,#15987,#15988,#15989,#15990,
#15991,#15992,#15993,#15994,#15995,#15996,#15997,#15998,#15999,#16000,#16001,
#16002,#16003,#16004,#16005,#16006,#16007,#16008,#16009,#16010,#16011,#16012,
#16013,#16014,#16015,#16016,#16017,#16018,#16019,#16020,#16021,#16022,#16023,
#16024,#16025,#16026,#16027,#16028,#16029,#16030,#16031,#16032,#16033,#16034,
#16035,#16036,#16037,#16038,#16039,#16040,#16041,#16042,#16043,#16044,#16045,
#16046,#16047,#16048,#16049,#16050,#16051,#16052,#16053,#16054,#16055,#16056,
#16057,#16058,#16059,#16060,#16061,#16062,#16063,#16064,#16065,#16066,#16067,
#16068,#16069,#16070,#16071,#16072,#16073,#16074,#16075,#16076,#16077,#16078,
#16079,#16080,#16081,#16082,#16083,#16084,#16085,#16086,#16087,#16088,#16089,
#16090,#16091,#16092,#16093),.UNSPECIFIED.,.F.,.F.,(4,3,3,3,3,3,3,3,3,3,
3,3,3,3,3,3,3,3,3,3,3,3,3,3,3,3,3,3,3,3,3,3,3,3,3,3,3,3,3,3,3,3,3,3,3,3,
3,3,3,3,3,3,3,3,3,3,3,3,3,3,3,3,3,3,3,3,3,3,3,3,3,3,3,3,3,3,4),(89.0746395114255,
89.1661315419306,89.2535335418103,89.3409155597643,89.4282997621435,89.515708312922,
89.6032130314677,89.690774292348,89.778465706738,89.8065757554662,89.8951489047728,
89.9836076978226,90.0719759101952,90.16353224607,90.2517988896268,90.3400522802442,
90.4283137625124,90.5166046816894,90.6049956672829,90.6934462555673,90.7820261803054,
90.8044265971937,90.8929997465003,90.98145853955,91.0698267519225,91.1613830877973,
91.2496497313541,91.3379031219715,91.4261646042399,91.5144555234169,91.6028465090104,
91.6912970972943,91.7798770220325,91.8022774389211,91.8908505882279,91.979309381278,
92.0676775936506,92.1592339295253,92.2475005730823,92.3357539636997,92.4240154459682,
92.5123063651454,92.6006973507391,92.6891479390237,92.777727863762,92.8001282806484,
92.8887014299548,92.9771602230042,93.0655284353769,93.1570847712517,93.2453514148085,
93.3336048054257,93.4218662876938,93.5101572068713,93.5985481924647,93.6869987807487,
93.7755787054866,93.7979791223758,93.8865522716819,93.9750110647312,94.0633792771031,
94.1549356129782,94.2432022565346,94.3314556471514,94.4197171294191,94.5080080485956,
94.5963990341886,94.6848496224724,94.7734295472099,94.7958299641032,94.8867065999364,
94.977446835222,95.0725413310677,95.1630320672469,95.2534488825782,95.3437980500512,
95.3578248186051),.UNSPECIFIED.);
#1261=B_SPLINE_CURVE_WITH_KNOTS('',3,(#16095,#16096,#16097,#16098,#16099,
#16100,#16101,#16102,#16103,#16104,#16105,#16106,#16107,#16108,#16109,#16110,
#16111,#16112,#16113,#16114,#16115,#16116,#16117,#16118,#16119,#16120,#16121,
#16122,#16123,#16124,#16125,#16126,#16127,#16128,#16129,#16130,#16131,#16132,
#16133,#16134,#16135,#16136,#16137,#16138,#16139,#16140,#16141,#16142,#16143,
#16144,#16145,#16146,#16147,#16148,#16149,#16150,#16151,#16152,#16153,#16154,
#16155,#16156,#16157,#16158,#16159,#16160,#16161,#16162,#16163,#16164,#16165,
#16166,#16167,#16168,#16169,#16170,#16171,#16172,#16173,#16174,#16175,#16176,
#16177,#16178,#16179,#16180,#16181,#16182,#16183,#16184,#16185,#16186,#16187,
#16188,#16189,#16190,#16191,#16192,#16193,#16194,#16195,#16196,#16197,#16198,
#16199,#16200,#16201,#16202,#16203,#16204,#16205,#16206,#16207,#16208,#16209,
#16210,#16211,#16212,#16213,#16214,#16215,#16216,#16217,#16218,#16219,#16220,
#16221,#16222,#16223,#16224,#16225,#16226,#16227,#16228,#16229,#16230,#16231,
#16232,#16233,#16234,#16235,#16236,#16237,#16238,#16239,#16240,#16241,#16242,
#16243,#16244,#16245,#16246,#16247,#16248,#16249,#16250,#16251,#16252,#16253,
#16254,#16255,#16256,#16257,#16258,#16259,#16260,#16261,#16262,#16263,#16264,
#16265,#16266,#16267,#16268,#16269,#16270,#16271,#16272,#16273,#16274,#16275,
#16276,#16277,#16278,#16279,#16280,#16281,#16282,#16283,#16284,#16285,#16286,
#16287,#16288,#16289,#16290,#16291,#16292,#16293,#16294,#16295,#16296,#16297,
#16298,#16299,#16300,#16301,#16302,#16303,#16304,#16305,#16306,#16307,#16308,
#16309,#16310,#16311,#16312,#16313,#16314,#16315,#16316,#16317,#16318,#16319,
#16320,#16321,#16322,#16323),.UNSPECIFIED.,.F.,.F.,(4,3,3,3,3,3,3,3,3,3,
3,3,3,3,3,3,3,3,3,3,3,3,3,3,3,3,3,3,3,3,3,3,3,3,3,3,3,3,3,3,3,3,3,3,3,3,
3,3,3,3,3,3,3,3,3,3,3,3,3,3,3,3,3,3,3,3,3,3,3,3,3,3,3,3,3,3,4),(82.7914542042459,
82.8216198633744,82.910193012681,82.9986518057307,83.0870200181033,83.1785763539781,
83.2668429975349,83.3550963881522,83.4433578704206,83.5316487895978,83.6200397751913,
83.7084903634755,83.7970702882138,83.8194707051018,83.9080438544084,83.9965026474582,
84.0848708598308,84.1764271957056,84.2646938392624,84.3529472298798,84.4412087121482,
84.5294996313254,84.6178906169189,84.7063412052032,84.7949211299414,84.8173215468292,
84.9058946961358,84.9943534891855,85.082721701558,85.1742780374329,85.2625446809897,
85.3507980716069,85.4390595538753,85.5273504730524,85.6157414586459,85.7041920469301,
85.7927719716683,85.8151723885566,85.9037455378632,85.9922043309129,86.0805725432855,
86.1721288791603,86.2603955227172,86.3486489133345,86.4369103956028,86.52520131478,
86.6135923003735,86.7020428886577,86.7906228133959,86.813023230284,86.9015963795906,
86.9900551726403,87.0784233850128,87.1699797208877,87.2582463644445,87.3464997550618,
87.4347612373301,87.5230521565073,87.6114431421008,87.699893730385,87.7884736551232,
87.8108740720114,87.8994472213179,87.9879060143677,88.0762742267402,88.167830562615,
88.2560972061718,88.344350596789,88.4326120790573,88.5209029982345,88.609293983828,
88.697744572112,88.7863244968503,88.8087249137388,88.9216441128932,89.0325337049013,
89.0746395112361),.UNSPECIFIED.);
#1262=B_SPLINE_CURVE_WITH_KNOTS('',3,(#16325,#16326,#16327,#16328,#16329,
#16330,#16331,#16332,#16333,#16334),.UNSPECIFIED.,.F.,.F.,(4,1,1,1,1,1,
1,4),(76.5082758295062,76.83451481301,77.8323656547374,78.8302164964648,
79.8280673381922,80.8259181799196,81.823769021647,82.7914500653136),
 .UNSPECIFIED.);
#1263=B_SPLINE_CURVE_WITH_KNOTS('',3,(#16336,#16337,#16338,#16339,#16340,
#16341,#16342,#16343,#16344,#16345,#16346,#16347,#16348,#16349,#16350,#16351,
#16352,#16353,#16354,#16355,#16356,#16357,#16358,#16359,#16360,#16361,#16362,
#16363,#16364,#16365,#16366,#16367,#16368,#16369,#16370,#16371,#16372,#16373,
#16374,#16375,#16376,#16377,#16378,#16379,#16380,#16381,#16382,#16383,#16384,
#16385,#16386,#16387,#16388,#16389,#16390,#16391,#16392,#16393,#16394,#16395,
#16396,#16397,#16398,#16399,#16400,#16401,#16402,#16403,#16404,#16405,#16406,
#16407,#16408,#16409,#16410,#16411,#16412,#16413,#16414,#16415,#16416,#16417,
#16418,#16419,#16420,#16421,#16422,#16423,#16424,#16425,#16426,#16427,#16428,
#16429,#16430,#16431,#16432,#16433,#16434,#16435,#16436,#16437,#16438,#16439,
#16440,#16441,#16442,#16443,#16444,#16445,#16446,#16447,#16448,#16449,#16450,
#16451,#16452,#16453,#16454,#16455,#16456,#16457,#16458,#16459,#16460,#16461,
#16462,#16463,#16464,#16465,#16466,#16467,#16468,#16469,#16470,#16471,#16472,
#16473,#16474,#16475,#16476,#16477,#16478,#16479,#16480,#16481,#16482,#16483,
#16484,#16485,#16486,#16487,#16488,#16489,#16490,#16491,#16492,#16493,#16494,
#16495,#16496,#16497,#16498,#16499,#16500,#16501,#16502,#16503,#16504,#16505,
#16506,#16507,#16508,#16509,#16510,#16511,#16512,#16513,#16514,#16515,#16516,
#16517,#16518,#16519,#16520,#16521,#16522,#16523,#16524,#16525,#16526,#16527,
#16528,#16529,#16530,#16531,#16532,#16533,#16534,#16535,#16536,#16537,#16538,
#16539,#16540,#16541,#16542,#16543,#16544,#16545,#16546,#16547,#16548,#16549,
#16550,#16551,#16552,#16553,#16554,#16555,#16556,#16557,#16558,#16559,#16560,
#16561),.UNSPECIFIED.,.F.,.F.,(4,3,3,3,3,3,3,3,3,3,3,3,3,3,3,3,3,3,3,3,
3,3,3,3,3,3,3,3,3,3,3,3,3,3,3,3,3,3,3,3,3,3,3,3,3,3,3,3,3,3,3,3,3,3,3,3,
3,3,3,3,3,3,3,3,3,3,3,3,3,3,3,3,3,3,3,4),(70.2250835898867,70.3140257139893,
70.4029773741115,70.4919588141693,70.5810544107303,70.6702073895619,70.7595248544879,
70.8474097626456,70.9359829119522,71.0244417050018,71.1128099173743,71.2043662532491,
71.2926328968059,71.3808862874233,71.4691477696917,71.557438688869,71.6458296744625,
71.7342802627467,71.8228601874848,71.845260604373,71.9338337536796,72.0222925467293,
72.1106607591019,72.2022170949768,72.2904837385335,72.3787371291508,72.466998611419,
72.5552895305961,72.6436805161896,72.7321311044739,72.8207110292122,72.8431114461004,
72.931684595407,73.0201433884567,73.1085116008294,73.2000679367042,73.288334580261,
73.3765879708783,73.4648494531465,73.5531403723238,73.6415313579173,73.7299819462015,
73.8185618709397,73.8409622878278,73.9295354371344,74.0179942301841,74.1063624425564,
74.1979187784313,74.2861854219882,74.3744388126055,74.462700294874,74.5509912140511,
74.6393821996446,74.7278327879289,74.816412712667,74.8388131295552,74.9273862788618,
75.0158450719113,75.1042132842839,75.1957696201587,75.2840362637154,75.3722896543324,
75.4605511366011,75.5488420557785,75.637233041372,75.7256836296562,75.8142635543943,
75.8366639712826,75.9250774885632,76.0133803059621,76.1015940720835,76.1897403602782,
76.2778480053841,76.3659320489739,76.4540370202494,76.5082688970663),
 .UNSPECIFIED.);
#1264=B_SPLINE_CURVE_WITH_KNOTS('',3,(#16563,#16564,#16565,#16566,#16567,
#16568,#16569,#16570,#16571,#16572),.UNSPECIFIED.,.F.,.F.,(4,1,1,1,1,1,
1,4),(63.9418982827071,64.8603047122812,65.8581555540086,66.856006395736,
67.8538572374634,68.8517080791908,69.8495589209182,70.2250761086419),
 .UNSPECIFIED.);
#1265=B_SPLINE_CURVE_WITH_KNOTS('',3,(#16574,#16575,#16576,#16577,#16578,
#16579,#16580,#16581,#16582,#16583,#16584),.UNSPECIFIED.,.F.,.F.,(4,1,1,
1,1,1,1,1,4),(57.6587129755275,57.8753488201894,58.8731996619168,59.8710505036442,
60.8689013453716,61.866752187099,62.8646030288264,63.8624538705538,63.9418982827071),
 .UNSPECIFIED.);
#1266=B_SPLINE_CURVE_WITH_KNOTS('',3,(#16586,#16587,#16588,#16589,#16590,
#16591,#16592,#16593,#16594,#16595,#16596,#16597,#16598,#16599,#16600,#16601,
#16602,#16603,#16604,#16605,#16606,#16607,#16608,#16609,#16610,#16611,#16612,
#16613,#16614,#16615,#16616,#16617,#16618,#16619,#16620,#16621,#16622,#16623,
#16624,#16625,#16626,#16627,#16628,#16629,#16630,#16631,#16632,#16633,#16634,
#16635,#16636,#16637,#16638,#16639,#16640,#16641,#16642,#16643,#16644,#16645,
#16646,#16647,#16648,#16649,#16650,#16651,#16652,#16653,#16654,#16655,#16656,
#16657,#16658,#16659,#16660,#16661,#16662,#16663,#16664,#16665,#16666,#16667,
#16668,#16669,#16670,#16671,#16672,#16673,#16674,#16675,#16676,#16677,#16678,
#16679,#16680,#16681,#16682,#16683,#16684,#16685,#16686,#16687,#16688,#16689,
#16690,#16691,#16692,#16693,#16694,#16695,#16696,#16697,#16698,#16699,#16700,
#16701,#16702,#16703,#16704,#16705,#16706,#16707,#16708,#16709,#16710,#16711,
#16712,#16713,#16714,#16715,#16716,#16717,#16718,#16719,#16720,#16721,#16722,
#16723,#16724,#16725,#16726,#16727,#16728,#16729,#16730,#16731,#16732,#16733,
#16734,#16735,#16736,#16737,#16738,#16739,#16740,#16741,#16742,#16743,#16744,
#16745,#16746,#16747,#16748,#16749,#16750,#16751,#16752,#16753,#16754,#16755,
#16756,#16757,#16758,#16759,#16760,#16761,#16762,#16763,#16764,#16765,#16766,
#16767,#16768,#16769,#16770,#16771,#16772,#16773,#16774,#16775,#16776,#16777,
#16778,#16779,#16780,#16781,#16782,#16783,#16784,#16785,#16786,#16787,#16788,
#16789,#16790,#16791,#16792,#16793,#16794,#16795,#16796,#16797,#16798,#16799,
#16800,#16801,#16802,#16803,#16804,#16805,#16806,#16807,#16808,#16809,#16810,
#16811),.UNSPECIFIED.,.F.,.F.,(4,3,3,3,3,3,3,3,3,3,3,3,3,3,3,3,3,3,3,3,
3,3,3,3,3,3,3,3,3,3,3,3,3,3,3,3,3,3,3,3,3,3,3,3,3,3,3,3,3,3,3,3,3,3,3,3,
3,3,3,3,3,3,3,3,3,3,3,3,3,3,3,3,3,3,3,4),(51.3755276683479,51.4674551182634,
51.5594915131789,51.6517320877936,51.7440828937285,51.8366378040778,51.8882437698249,
51.9768169191315,52.0652757121811,52.1536439245537,52.2452002604286,52.3334669039854,
52.4217202946027,52.509981776871,52.5982726960484,52.6866636816419,52.775114269926,
52.8636941946643,52.8860946115523,52.9746677608589,53.0631265539085,53.1514947662813,
53.2430511021561,53.3313177457129,53.4195711363302,53.5078326185985,53.596123537776,
53.6845145233695,53.7729651116536,53.8615450363917,53.8839454532797,53.9725186025863,
54.0609773956361,54.1493456080086,54.2409019438834,54.3291685874402,54.4174219780575,
54.5056834603262,54.5939743795036,54.6823653650971,54.7708159533812,54.8593958781193,
54.8817962950071,54.9703694443136,55.0588282373635,55.1471964497362,55.238752785611,
55.3270194291679,55.4152728197852,55.5035343020536,55.5918252212311,55.6802162068246,
55.7686667951087,55.857246719847,55.8796471367346,55.9682202860412,56.0566790790908,
56.1450472914633,56.2366036273381,56.3248702708951,56.4131236615125,56.5013851437809,
56.589676062958,56.6780670485515,56.7665176368355,56.8550975615738,56.877497978462,
56.9648624461654,57.0520884991057,57.1392356291962,57.2263263599901,57.3133831580112,
57.4004603167863,57.4875438192577,57.5747123789985,57.6587129755275),
 .UNSPECIFIED.);
#1267=B_SPLINE_CURVE_WITH_KNOTS('',3,(#16813,#16814,#16815,#16816,#16817,
#16818,#16819,#16820,#16821,#16822),.UNSPECIFIED.,.F.,.F.,(4,1,1,1,1,1,
1,4),(45.0923466255027,45.9011387194605,46.8989895611879,47.8968404029153,
48.8946912446427,49.8925420863701,50.8903929280975,51.3755266026442),
 .UNSPECIFIED.);
#1268=B_SPLINE_CURVE_WITH_KNOTS('',3,(#16824,#16825,#16826,#16827,#16828,
#16829,#16830,#16831,#16832,#16833,#16834,#16835,#16836,#16837,#16838,#16839,
#16840,#16841,#16842,#16843,#16844,#16845,#16846,#16847,#16848,#16849,#16850,
#16851,#16852,#16853,#16854,#16855,#16856,#16857,#16858,#16859,#16860,#16861,
#16862,#16863,#16864,#16865,#16866,#16867,#16868,#16869,#16870,#16871,#16872,
#16873,#16874,#16875,#16876,#16877,#16878,#16879,#16880,#16881,#16882,#16883,
#16884,#16885,#16886,#16887,#16888,#16889,#16890,#16891,#16892,#16893,#16894,
#16895,#16896,#16897,#16898,#16899,#16900,#16901,#16902,#16903,#16904,#16905,
#16906,#16907,#16908,#16909,#16910,#16911,#16912,#16913,#16914,#16915,#16916,
#16917,#16918,#16919,#16920,#16921,#16922,#16923,#16924,#16925,#16926,#16927,
#16928,#16929,#16930,#16931,#16932,#16933,#16934,#16935,#16936,#16937,#16938,
#16939,#16940,#16941,#16942,#16943,#16944,#16945,#16946,#16947,#16948,#16949,
#16950,#16951,#16952,#16953,#16954,#16955,#16956,#16957,#16958,#16959,#16960,
#16961,#16962,#16963,#16964,#16965,#16966,#16967,#16968,#16969,#16970,#16971,
#16972,#16973,#16974,#16975,#16976,#16977,#16978,#16979,#16980,#16981,#16982,
#16983,#16984,#16985,#16986,#16987,#16988,#16989,#16990,#16991,#16992,#16993,
#16994,#16995,#16996,#16997,#16998,#16999,#17000,#17001,#17002,#17003,#17004,
#17005,#17006,#17007,#17008,#17009,#17010,#17011,#17012,#17013,#17014,#17015,
#17016,#17017,#17018,#17019,#17020,#17021,#17022,#17023,#17024,#17025,#17026,
#17027,#17028,#17029,#17030,#17031,#17032,#17033,#17034,#17035,#17036,#17037,
#17038,#17039,#17040,#17041,#17042,#17043,#17044,#17045,#17046,#17047,#17048,
#17049),.UNSPECIFIED.,.F.,.F.,(4,3,3,3,3,3,3,3,3,3,3,3,3,3,3,3,3,3,3,3,
3,3,3,3,3,3,3,3,3,3,3,3,3,3,3,3,3,3,3,3,3,3,3,3,3,3,3,3,3,3,3,3,3,3,3,3,
3,3,3,3,3,3,3,3,3,3,3,3,3,3,3,3,3,3,3,4),(38.8091570539888,38.9161828273687,
39.0047559766754,39.0932147697253,39.1815829820979,39.2731393179727,39.3614059615296,
39.4496593521471,39.5379208344156,39.6262117535929,39.7146027391865,39.8030533274707,
39.8916332522091,39.9140336690961,40.0026068184027,40.0910656114524,40.179433823825,
40.2709901596998,40.3592568032566,40.4475101938739,40.5357716761421,40.6240625953193,
40.7124535809127,40.8009041691969,40.8894840939351,40.9118845108235,41.00045766013,
41.0889164531798,41.1772846655523,41.2688410014271,41.3571076449839,41.4453610356012,
41.5336225178695,41.6219134370467,41.7103044226401,41.7987550109243,41.8873349356625,
41.9097353525509,41.9983085018575,42.0867672949073,42.1751355072798,42.2666918431546,
42.3549584867115,42.4432118773288,42.5314733595971,42.6197642787743,42.7081552643678,
42.7966058526521,42.8851857773903,42.9075861942783,42.9961593435849,43.0846181366347,
43.1729863490072,43.264542684882,43.3528093284388,43.4410627190561,43.5293242013244,
43.6176151205017,43.7060061060952,43.7944566943794,43.8830366191176,43.9054370360057,
43.9940101853123,44.082468978362,44.1708371907345,44.2623935266093,44.3506601701662,
44.4389135607834,44.5271750430518,44.6154659622291,44.7038569478225,44.7923075361068,
44.880887460845,44.9032878777331,45.0337718756031,45.0923423611683),
 .UNSPECIFIED.);
#1269=B_SPLINE_CURVE_WITH_KNOTS('',3,(#17051,#17052,#17053,#17054,#17055,
#17056,#17057,#17058,#17059,#17060,#17061,#17062,#17063,#17064,#17065,#17066,
#17067,#17068,#17069,#17070,#17071,#17072,#17073,#17074,#17075,#17076,#17077,
#17078,#17079,#17080,#17081,#17082,#17083,#17084,#17085,#17086,#17087,#17088,
#17089,#17090,#17091,#17092,#17093,#17094,#17095,#17096,#17097,#17098,#17099,
#17100,#17101,#17102,#17103,#17104,#17105,#17106,#17107,#17108,#17109,#17110,
#17111,#17112,#17113,#17114,#17115,#17116,#17117,#17118,#17119,#17120,#17121,
#17122,#17123,#17124,#17125,#17126,#17127,#17128,#17129,#17130,#17131,#17132,
#17133,#17134,#17135,#17136,#17137,#17138,#17139,#17140,#17141,#17142,#17143,
#17144,#17145,#17146,#17147,#17148,#17149,#17150,#17151,#17152,#17153,#17154,
#17155,#17156,#17157,#17158,#17159,#17160,#17161,#17162,#17163,#17164,#17165,
#17166,#17167,#17168,#17169,#17170,#17171,#17172,#17173,#17174,#17175,#17176,
#17177,#17178,#17179,#17180,#17181,#17182,#17183,#17184,#17185,#17186,#17187,
#17188,#17189,#17190,#17191,#17192,#17193,#17194,#17195,#17196,#17197,#17198,
#17199,#17200,#17201,#17202,#17203,#17204,#17205,#17206,#17207,#17208,#17209,
#17210,#17211,#17212,#17213,#17214,#17215,#17216,#17217,#17218,#17219,#17220,
#17221,#17222,#17223,#17224,#17225,#17226,#17227,#17228,#17229,#17230,#17231,
#17232,#17233,#17234,#17235,#17236,#17237,#17238,#17239,#17240,#17241,#17242,
#17243,#17244,#17245,#17246,#17247,#17248,#17249,#17250,#17251,#17252,#17253,
#17254,#17255,#17256,#17257,#17258,#17259,#17260,#17261,#17262,#17263,#17264,
#17265,#17266,#17267,#17268,#17269,#17270,#17271,#17272,#17273,#17274,#17275,
#17276),.UNSPECIFIED.,.F.,.F.,(4,3,3,3,3,3,3,3,3,3,3,3,3,3,3,3,3,3,3,3,
3,3,3,3,3,3,3,3,3,3,3,3,3,3,3,3,3,3,3,3,3,3,3,3,3,3,3,3,3,3,3,3,3,3,3,3,
3,3,3,3,3,3,3,3,3,3,3,3,3,3,3,3,3,3,3,4),(32.525971963069,32.6267484165528,
32.7244048484166,32.8267413127105,32.9290777770043,33.0176509263104,33.1061097193596,
33.1944779317316,33.2860342676066,33.3743009111629,33.4625543017797,33.5508157840475,
33.6391067032241,33.7274976888171,33.8159482771008,33.9045282018386,33.9269286187317,
34.0155017680382,34.1039605610878,34.1923287734603,34.2838851093351,34.3721517528918,
34.460405143509,34.5486666257773,34.6369575449543,34.7253485305477,34.8137991188318,
34.9023790435699,34.9247794604591,35.0133526097659,35.1018114028158,35.1901796151886,
35.2817359510633,35.3700025946204,35.4582559852379,35.5465174675064,35.6348083866838,
35.7231993722774,35.8116499605619,35.9002298853003,35.9226303021865,36.011203451493,
36.0996622445427,36.1880304569152,36.27958679279,36.3678534363467,36.456106826964,
36.5443683092322,36.6326592284093,36.7210502140027,36.8095008022868,36.8980807270249,
36.9204811439139,37.0090542932205,37.0975130862702,37.1858812986428,37.2774376345176,
37.3657042780745,37.4539576686918,37.5422191509601,37.6305100701371,37.7189010557306,
37.8073516440148,37.8959315687529,37.9183319856413,38.0057567402233,38.0930680815749,
38.1825792030983,38.269738045414,38.3568657274586,38.4439846320749,38.5352777374967,
38.6224901904464,38.7097513439574,38.79712291786,38.809157053762),
 .UNSPECIFIED.);
#1270=B_SPLINE_CURVE_WITH_KNOTS('',3,(#17278,#17279,#17280,#17281,#17282,
#17283,#17284,#17285,#17286,#17287),.UNSPECIFIED.,.F.,.F.,(4,1,1,1,1,1,
1,4),(26.2427864396296,26.9419727266399,27.9398235683673,28.9376744100947,
29.9355252518221,30.9333760935495,31.9312269352769,32.5259717468092),
 .UNSPECIFIED.);
#1271=B_SPLINE_CURVE_WITH_KNOTS('',3,(#17288,#17289,#17290,#17291,#17292,
#17293,#17294,#17295,#17296,#17297,#17298,#17299,#17300,#17301,#17302,#17303,
#17304,#17305,#17306,#17307,#17308,#17309,#17310,#17311,#17312,#17313,#17314,
#17315,#17316,#17317,#17318,#17319,#17320,#17321,#17322,#17323,#17324,#17325,
#17326,#17327,#17328,#17329,#17330,#17331,#17332,#17333,#17334,#17335,#17336,
#17337,#17338,#17339,#17340,#17341,#17342,#17343,#17344,#17345,#17346,#17347,
#17348,#17349,#17350,#17351,#17352,#17353,#17354,#17355,#17356,#17357,#17358,
#17359,#17360,#17361,#17362,#17363,#17364,#17365,#17366,#17367,#17368,#17369,
#17370,#17371,#17372,#17373,#17374,#17375,#17376,#17377,#17378,#17379,#17380,
#17381,#17382,#17383,#17384,#17385,#17386,#17387,#17388,#17389,#17390,#17391,
#17392,#17393,#17394,#17395,#17396,#17397,#17398,#17399,#17400,#17401,#17402,
#17403,#17404,#17405,#17406,#17407,#17408,#17409,#17410,#17411,#17412,#17413,
#17414,#17415,#17416,#17417,#17418,#17419,#17420,#17421,#17422,#17423,#17424,
#17425,#17426,#17427,#17428,#17429,#17430,#17431,#17432,#17433,#17434,#17435,
#17436,#17437,#17438,#17439,#17440,#17441,#17442,#17443,#17444,#17445,#17446,
#17447,#17448,#17449,#17450,#17451,#17452,#17453,#17454,#17455,#17456,#17457,
#17458,#17459,#17460,#17461,#17462,#17463,#17464,#17465,#17466,#17467,#17468,
#17469,#17470,#17471,#17472,#17473,#17474,#17475,#17476,#17477,#17478,#17479,
#17480,#17481,#17482,#17483,#17484,#17485,#17486),.UNSPECIFIED.,.F.,.F.,
(4,3,3,3,3,3,3,3,3,3,3,3,3,3,3,3,3,3,3,3,3,3,3,3,3,3,3,3,3,3,3,3,3,3,3,
3,3,3,3,3,3,3,3,3,3,3,3,3,3,3,3,3,3,3,3,3,3,3,3,3,3,3,3,3,3,3,4),(20.7587652524469,
20.8471770515305,20.9357172601531,20.9548676762754,21.0434408253141,21.1318996180998,
21.2202678302125,21.3118241661863,21.4000908094954,21.4883441998699,21.5766056819008,
21.664896600846,21.7532875862169,21.8417381742837,21.930318098814,21.9527185180029,
22.0412916665946,22.1297504589173,22.2181186705516,22.3096750066989,22.3979416494941,
22.4861950393424,22.5744565208353,22.6627474392314,22.751138424039,22.8395890115339,
22.9281689354835,22.9505693597303,23.0391425095139,23.1276013030463,23.2159695159069,
23.3075258516008,23.3957924956554,23.4840458867733,23.5723073695444,23.6605982892259,
23.748989275324,23.8374398641133,23.9260197893538,23.9484202014577,24.0369933506891,
24.1254521436636,24.213820355961,24.305376691864,24.3936433353464,24.4818967258899,
24.5701582080845,24.6584491271886,24.7468401127105,24.8352907009236,24.9238706255922,
24.9462710431851,25.0348441924046,25.1233029853661,25.2116711976484,25.3032275335564,
25.3914941770201,25.4797475675431,25.5680090497163,25.6562999687983,25.7446909542951,
25.8331415424822,25.921721467123,25.9441218849125,26.0521117090049,26.1587324119638,
26.2427862611992),.UNSPECIFIED.);
#1272=B_SPLINE_CURVE_WITH_KNOTS('',3,(#17488,#17489,#17490,#17491,#17492,
#17493,#17494,#17495,#17496,#17497,#17498,#17499,#17500,#17501,#17502,#17503,
#17504,#17505,#17506,#17507,#17508,#17509,#17510,#17511,#17512,#17513,#17514,
#17515,#17516,#17517,#17518,#17519,#17520,#17521,#17522,#17523,#17524,#17525,
#17526,#17527,#17528,#17529,#17530,#17531,#17532,#17533,#17534,#17535,#17536,
#17537,#17538,#17539,#17540,#17541,#17542,#17543,#17544,#17545,#17546,#17547,
#17548,#17549,#17550,#17551,#17552,#17553,#17554,#17555,#17556,#17557,#17558,
#17559,#17560,#17561,#17562,#17563,#17564,#17565,#17566,#17567,#17568,#17569,
#17570,#17571,#17572,#17573,#17574,#17575,#17576,#17577,#17578,#17579,#17580,
#17581,#17582,#17583,#17584,#17585,#17586,#17587,#17588,#17589,#17590,#17591,
#17592,#17593,#17594,#17595,#17596,#17597,#17598,#17599,#17600,#17601,#17602,
#17603,#17604,#17605,#17606,#17607,#17608,#17609,#17610,#17611,#17612,#17613,
#17614,#17615,#17616,#17617,#17618,#17619,#17620,#17621,#17622,#17623,#17624,
#17625,#17626,#17627,#17628,#17629,#17630,#17631,#17632,#17633,#17634,#17635,
#17636,#17637,#17638,#17639,#17640,#17641,#17642,#17643,#17644,#17645,#17646,
#17647),.UNSPECIFIED.,.F.,.F.,(4,3,3,3,3,3,3,3,3,3,3,3,3,3,3,3,3,3,3,3,
3,3,3,3,3,3,3,3,3,3,3,3,3,3,3,3,3,3,3,3,3,3,3,3,3,3,3,3,3,3,3,3,3,4),(-22.0660092005583,
-21.9775604397691,-21.9527185180029,-21.8641453689077,-21.7756865760771,
-21.6873183639311,-21.5957620279741,-21.5074953846606,-21.4192419942923,
-21.3309805122783,-21.2426895933606,-21.1542986080331,-21.0658480200188,
-20.9772680955541,-20.9548676762754,-20.8662945236151,-20.7778357272005,
-20.689467511456,-20.5979111768425,-20.5096445299166,-20.421391135937,-20.3331296503169,
-20.2448387278021,-20.1564477389083,-20.0679971473415,-19.979417219372,
-19.957016834548,-19.8684436914371,-19.7799849045778,-19.6916166983834,
-19.6000603601881,-19.5117937227411,-19.4235403381984,-19.3352788619628,
-19.246987948771,-19.1585969690613,-19.0701463866092,-18.9815664675831,
-18.9591659928206,-18.8705928429654,-18.7821340494192,-18.6937658366019,
-18.6022095009133,-18.5139428570424,-18.4256894661595,-18.3374279836741,
-18.2491370643286,-18.160746078639,-18.0722954903006,-17.9837155655689,
-17.9613151510932,-17.8727403843232,-17.7842934699967,-17.7185431288346),
 .UNSPECIFIED.);
#1273=B_SPLINE_CURVE_WITH_KNOTS('',3,(#17648,#17649,#17650,#17651,#17652,
#17653,#17654,#17655,#17656,#17657,#17658,#17659,#17660,#17661,#17662,#17663,
#17664,#17665,#17666,#17667,#17668,#17669,#17670,#17671,#17672,#17673,#17674,
#17675,#17676,#17677,#17678,#17679,#17680,#17681,#17682,#17683,#17684,#17685,
#17686,#17687,#17688,#17689,#17690,#17691,#17692,#17693,#17694,#17695,#17696,
#17697,#17698,#17699,#17700,#17701,#17702,#17703,#17704,#17705,#17706,#17707,
#17708,#17709,#17710,#17711,#17712,#17713,#17714,#17715,#17716,#17717,#17718,
#17719,#17720,#17721,#17722,#17723,#17724,#17725,#17726,#17727,#17728,#17729,
#17730,#17731,#17732,#17733,#17734,#17735,#17736,#17737,#17738,#17739,#17740,
#17741,#17742,#17743,#17744,#17745,#17746,#17747,#17748,#17749,#17750,#17751,
#17752,#17753,#17754,#17755,#17756,#17757,#17758,#17759,#17760,#17761,#17762,
#17763,#17764,#17765,#17766,#17767,#17768,#17769,#17770,#17771,#17772,#17773,
#17774,#17775,#17776,#17777,#17778,#17779,#17780,#17781,#17782,#17783,#17784,
#17785,#17786,#17787,#17788,#17789,#17790,#17791,#17792,#17793,#17794,#17795,
#17796,#17797,#17798,#17799,#17800,#17801,#17802,#17803,#17804),
 .UNSPECIFIED.,.F.,.F.,(4,3,3,3,3,3,3,3,3,3,3,3,3,3,3,3,3,3,3,3,3,3,3,3,
3,3,3,3,3,3,3,3,3,3,3,3,3,3,3,3,3,3,3,3,3,3,3,3,3,3,3,3,4),(14.7355974371875,
14.8240238515058,14.9125887089936,14.967762625911,15.0563357887042,15.1447945957911,
15.2331628227319,15.3247191533452,15.4129858127104,15.5012392195697,15.5895007184981,
15.6777916547382,15.7661826579098,15.8546332640942,15.9432132070692,15.9656134676384,
16.0541865737118,16.1426453228713,16.231013490753,16.3225698430796,16.4108364409255,
16.4990897854578,16.5873512213152,16.6756420938033,16.7640330325289,16.8524835737835,
16.9410634516159,16.9634643093658,17.0520374794408,17.1404962934807,17.2288645270386,
17.3204208550455,17.4086875201402,17.496940932389,17.5852024363594,17.6734933772864,
17.7618843845908,17.8503349945898,17.9389149408814,17.9613151510932,18.0498883004087,
18.1383470935207,18.2267153060082,18.3182716418598,18.4065382856639,18.4947916765772,
18.5830531591902,18.6713440787606,18.7597350648179,18.8481856536076,18.936765578909,
18.9591659928206,18.9739239990975),.UNSPECIFIED.);
#1274=B_SPLINE_CURVE_WITH_KNOTS('',3,(#17806,#17807,#17808,#17809,#17810,
#17811,#17812,#17813),.UNSPECIFIED.,.F.,.F.,(4,1,1,1,1,4),(-15.5984662374724,
-14.967762625911,-13.9699117841836,-12.9720609424562,-11.9742101007288,
-11.4361522655988),.UNSPECIFIED.);
#1275=B_SPLINE_CURVE_WITH_KNOTS('',3,(#17814,#17815,#17816,#17817,#17818,
#17819,#17820,#17821),.UNSPECIFIED.,.F.,.F.,(4,1,1,1,1,4),(8.45339075667584,
8.98065757554662,9.97850841727402,10.9763592590014,11.9742101007288,12.615721686902),
 .UNSPECIFIED.);
#1276=B_SPLINE_CURVE_WITH_KNOTS('',3,(#17823,#17824,#17825,#17826,#17827,
#17828,#17829,#17830),.UNSPECIFIED.,.F.,.F.,(4,1,1,1,1,4),(-9.31667937974296,
-8.98065757554662,-7.98280673381922,-6.98495589209182,-5.98710505036441,
-5.15395682855483),.UNSPECIFIED.);
#1277=B_SPLINE_CURVE_WITH_KNOTS('',3,(#17831,#17832,#17833,#17834,#17835,
#17836,#17837,#17838,#17839,#17840,#17841,#17842,#17843,#17844,#17845,#17846,
#17847,#17848,#17849,#17850,#17851,#17852,#17853,#17854,#17855,#17856,#17857,
#17858,#17859,#17860,#17861,#17862,#17863,#17864,#17865,#17866,#17867,#17868,
#17869,#17870,#17871,#17872,#17873,#17874,#17875,#17876,#17877,#17878,#17879,
#17880,#17881,#17882,#17883,#17884,#17885,#17886,#17887,#17888,#17889,#17890,
#17891,#17892,#17893,#17894,#17895,#17896,#17897,#17898,#17899,#17900,#17901,
#17902,#17903,#17904,#17905,#17906,#17907,#17908,#17909,#17910,#17911,#17912,
#17913,#17914,#17915,#17916,#17917,#17918,#17919,#17920,#17921,#17922,#17923,
#17924,#17925,#17926,#17927,#17928,#17929,#17930,#17931,#17932,#17933,#17934,
#17935,#17936,#17937,#17938,#17939,#17940,#17941,#17942,#17943,#17944,#17945,
#17946,#17947,#17948,#17949,#17950,#17951,#17952,#17953,#17954,#17955,#17956,
#17957,#17958,#17959,#17960,#17961,#17962,#17963,#17964,#17965,#17966,#17967,
#17968,#17969,#17970,#17971,#17972,#17973,#17974,#17975,#17976,#17977,#17978,
#17979,#17980,#17981),.UNSPECIFIED.,.F.,.F.,(4,3,3,3,3,3,3,3,3,3,3,3,3,
3,3,3,3,3,3,3,3,3,3,3,3,3,3,3,3,3,3,3,3,3,3,3,3,3,3,3,3,3,3,3,3,3,3,3,3,
3,4),(2.17031737188971,2.25881290186963,2.3506553547837,2.43904646041468,
2.52742311294194,2.61580651482276,2.70421786808851,2.79272702145135,2.881294244772,
2.96998899437975,2.99355252518221,3.08227858874621,3.17089309169939,3.2594196018157,
3.35091757245244,3.4393479542858,3.52776681491773,3.61619532292152,3.70465464856639,
3.79321523827935,3.88183633344943,3.9705867777702,3.99140336690961,4.07986039758296,
4.1682016225605,4.25645096449381,4.34805137001171,4.43619662711166,4.52432790356672,
4.61246666977451,4.70063439648283,4.78890209727742,4.87722919356262,4.96568627168405,
4.98925420863701,5.07785161744967,5.16633476132244,5.25472738550838,5.34627459361539,
5.4345656425618,5.52284339355104,5.61112916442565,5.69944427361828,5.78785917964294,
5.87633356002678,5.96493690510802,5.98710505036441,6.0756768503468,6.16414887291111,
6.25252666002196,6.33364065268233),.UNSPECIFIED.);
#1278=B_SPLINE_CURVE_WITH_KNOTS('',3,(#18506,#18507,#18508,#18509,#18510,
#18511,#18512,#18513,#18514,#18515,#18516,#18517,#18518,#18519,#18520,#18521,
#18522,#18523,#18524,#18525,#18526,#18527,#18528,#18529,#18530,#18531,#18532,
#18533,#18534,#18535,#18536,#18537,#18538,#18539,#18540,#18541,#18542,#18543,
#18544,#18545,#18546,#18547,#18548,#18549,#18550,#18551,#18552,#18553,#18554,
#18555,#18556,#18557,#18558,#18559,#18560,#18561,#18562,#18563,#18564,#18565,
#18566,#18567,#18568,#18569,#18570,#18571,#18572,#18573,#18574,#18575,#18576,
#18577,#18578,#18579,#18580,#18581,#18582,#18583,#18584,#18585,#18586,#18587,
#18588,#18589,#18590,#18591,#18592,#18593,#18594,#18595,#18596,#18597,#18598,
#18599,#18600,#18601,#18602,#18603,#18604,#18605,#18606,#18607,#18608,#18609,
#18610,#18611,#18612,#18613,#18614,#18615,#18616,#18617,#18618,#18619,#18620,
#18621,#18622,#18623,#18624,#18625,#18626,#18627,#18628,#18629,#18630,#18631,
#18632,#18633,#18634,#18635,#18636,#18637,#18638,#18639,#18640,#18641,#18642,
#18643,#18644,#18645,#18646,#18647,#18648,#18649,#18650,#18651,#18652,#18653,
#18654,#18655,#18656,#18657,#18658,#18659,#18660,#18661,#18662,#18663,#18664,
#18665,#18666,#18667,#18668,#18669,#18670,#18671,#18672,#18673,#18674,#18675,
#18676,#18677,#18678,#18679,#18680,#18681,#18682,#18683,#18684,#18685,#18686,
#18687,#18688,#18689,#18690,#18691,#18692,#18693,#18694,#18695,#18696,#18697,
#18698,#18699,#18700,#18701,#18702,#18703,#18704,#18705,#18706,#18707,#18708,
#18709,#18710,#18711,#18712,#18713,#18714,#18715,#18716,#18717,#18718,#18719,
#18720,#18721,#18722,#18723),.UNSPECIFIED.,.F.,.F.,(4,2,2,2,2,2,2,2,2,2,
2,2,2,2,2,2,2,2,2,2,2,2,2,2,2,2,2,2,2,2,2,2,2,2,2,2,2,2,2,2,2,2,2,2,2,2,
2,2,2,2,2,2,2,2,2,2,2,2,2,2,2,2,2,2,2,2,2,2,2,2,2,2,2,2,2,2,2,2,2,2,2,2,
2,2,2,2,2,2,2,2,2,2,2,2,2,2,2,2,2,2,2,2,2,2,2,2,2,2,4),(2.03132451219564,
2.04771864970936,2.054188022303,2.05814698897628,2.06242056802813,2.06823430844965,
2.0817897698534,2.10064397805793,2.20370857919037,2.21377989580146,2.2175320623633,
2.21976390896051,2.22218884705627,2.22568143858123,2.23475090456857,2.24835366133737,
2.29485606209288,2.35966392834093,2.37095468450181,2.37708768999893,2.38137662830883,
2.38577408674184,2.39223546346006,2.41005207867283,2.43732461440137,2.47913470812155,
2.52862412889425,2.53674984560304,2.5398555957629,2.54208109135899,2.54451148219816,
2.54803239165717,2.55729118947681,2.57127885605092,2.66996057549393,2.69116499558442,
2.69828760099901,2.70282479670568,2.70707904550392,2.7127763701719,2.72565665508832,
2.74329096533933,2.82738094384854,2.85559067256685,2.86037638324324,2.8633657240369,
2.86571845065722,2.86850779348139,2.87368300521173,2.90475334948206,2.96883722346092,
3.01038229618799,3.01827447807536,3.0234318638587,3.02762204312451,3.03245205411302,
3.04091676178286,3.08275717061232,3.13996540164022,3.17740586865857,3.18242954396431,
3.18545724954237,3.18781739862515,3.1905431584796,3.19542278361477,3.21981157227677,
3.26857495939193,3.33197371593967,3.34020907084036,3.34547079137238,3.34966884535167,
3.35442483817035,3.36254901686561,3.39818868269499,3.44478912959587,3.49560784772432,
3.50370000263359,3.50680089198984,3.50902485831906,3.51145585347853,3.51498141809216,
3.52427414349188,3.53833208109676,3.63881185324464,3.65849253024262,3.66541756413956,
3.66991152965345,3.6741845443711,3.67967676578006,3.69226103363765,3.70951482656912,
3.75794415447515,3.81824270779646,3.82611542164801,3.82918325833868,3.83139835011756,
3.83383707614073,3.83740312448355,3.846974911804,3.90962690510115,3.94173461786071,
3.97769715987629,3.98606014211005,3.99091632105627,3.99510351997158,3.99911650182043,
4.00412635044493,4.01174920751113,4.06083740610103),.UNSPECIFIED.);
#1279=B_SPLINE_CURVE_WITH_KNOTS('',3,(#18725,#18726,#18727,#18728),
 .UNSPECIFIED.,.F.,.F.,(4,4),(0.,0.0148042672212818),.UNSPECIFIED.);
#1280=B_SPLINE_CURVE_WITH_KNOTS('',3,(#18729,#18730,#18731,#18732,#18733,
#18734,#18735,#18736,#18737,#18738,#18739,#18740,#18741,#18742,#18743,#18744,
#18745,#18746,#18747,#18748,#18749,#18750,#18751,#18752,#18753,#18754,#18755,
#18756,#18757,#18758,#18759,#18760,#18761,#18762,#18763,#18764,#18765,#18766,
#18767,#18768,#18769,#18770,#18771,#18772,#18773,#18774,#18775,#18776,#18777,
#18778,#18779,#18780,#18781,#18782,#18783,#18784,#18785,#18786,#18787,#18788,
#18789,#18790,#18791,#18792,#18793,#18794,#18795,#18796,#18797,#18798,#18799,
#18800,#18801,#18802,#18803,#18804,#18805,#18806,#18807,#18808,#18809,#18810,
#18811,#18812,#18813,#18814,#18815,#18816,#18817,#18818,#18819),
 .UNSPECIFIED.,.F.,.F.,(4,3,3,3,3,3,3,3,3,3,3,3,3,3,3,3,3,3,3,3,3,3,3,3,
3,3,3,3,3,3,4),(0.,0.0213307452137482,0.0521561464407917,0.0839669760524937,
0.115759968726801,0.125948380810053,0.130779959365576,0.163494710583772,
0.196733919866297,0.230225396295248,0.259366443292864,0.264034736052148,
0.29841870568857,0.33269054668832,0.364788977591868,0.388319089517784,0.395090312303456,
0.401763820706065,0.435663949756398,0.470194310390573,0.505432883798703,
0.534520684831987,0.540918384207332,0.546655482151201,0.582601778959208,
0.618814597237711,0.635163545672189,0.641284826970611,0.678126477849349,
0.714525403155029,0.741270768406514),.UNSPECIFIED.);
#1281=B_SPLINE_CURVE_WITH_KNOTS('',3,(#19344,#19345,#19346,#19347,#19348,
#19349,#19350,#19351,#19352,#19353,#19354,#19355,#19356,#19357,#19358,#19359,
#19360,#19361,#19362,#19363,#19364,#19365,#19366,#19367,#19368,#19369,#19370,
#19371,#19372,#19373,#19374,#19375,#19376,#19377,#19378,#19379,#19380,#19381,
#19382,#19383,#19384,#19385,#19386,#19387,#19388,#19389,#19390,#19391,#19392,
#19393,#19394,#19395,#19396,#19397,#19398,#19399,#19400,#19401,#19402,#19403,
#19404,#19405,#19406,#19407,#19408,#19409,#19410,#19411,#19412,#19413,#19414,
#19415,#19416,#19417,#19418,#19419,#19420,#19421,#19422,#19423,#19424,#19425,
#19426,#19427,#19428,#19429,#19430,#19431,#19432,#19433,#19434,#19435,#19436,
#19437,#19438,#19439,#19440,#19441,#19442,#19443,#19444,#19445,#19446,#19447,
#19448,#19449,#19450,#19451,#19452,#19453,#19454,#19455,#19456,#19457,#19458,
#19459,#19460,#19461,#19462,#19463,#19464,#19465,#19466,#19467,#19468,#19469,
#19470,#19471,#19472,#19473,#19474,#19475,#19476,#19477,#19478,#19479,#19480,
#19481,#19482,#19483,#19484,#19485,#19486,#19487,#19488,#19489,#19490,#19491,
#19492,#19493,#19494,#19495,#19496,#19497),.UNSPECIFIED.,.F.,.F.,(4,2,2,
2,2,2,2,2,2,2,2,2,2,2,2,2,2,2,2,2,2,2,2,2,2,2,2,2,2,2,2,2,2,2,2,2,2,2,2,
2,2,2,2,2,2,2,2,2,2,2,2,2,2,2,2,2,2,2,2,2,2,2,2,2,2,2,2,2,2,2,2,2,2,2,2,
2,4),(2.29812698965297,2.33178680710208,2.343698682039,2.34771175618191,
2.34999527417306,2.35238664207991,2.35568912049544,2.36356174417911,2.3748249844316,
2.40834603517596,2.49226078206667,2.50344108419059,2.50882799377206,2.51304041355705,
2.51772388540368,2.52551066317873,2.55623450036125,2.62236224341244,2.66323886779315,
2.66831369188992,2.67135690112496,2.67371951851705,2.67643689399347,2.68127497132266,
2.70487603980923,2.7678565060481,2.81805201859086,2.82623901100133,2.83148711299157,
2.83568535443051,2.84045343806509,2.8486280427595,2.88505451296413,2.9338179921185,
2.959078252197,2.98619587606192,2.99093747377553,2.9939139741472,2.99626654178504,
2.99906750127949,3.00429517840024,3.03683769124635,3.10535480575199,3.14147168447426,
3.14984779067923,3.15470844716903,3.15889763575437,3.16401895218815,3.17386136502113,
3.18634501935978,3.21531750118195,3.28203716994859,3.30859430794303,3.31331295715945,
3.31628247771575,3.31863458179563,3.32144100135327,3.32669476223459,3.36004089016106,
3.42920761730249,3.46398461360625,3.47227227587684,3.47711271054028,3.48088407589505,
3.48584648937806,3.49492658587954,3.55653966581214,3.62216199348397,3.63341098950873,
3.63733435388478,3.63959987208859,3.64200085564126,3.6453620190887,3.65359162423786,
3.66553623385595,3.70250391739545,3.75982114661551),.UNSPECIFIED.);
#1282=B_SPLINE_CURVE_WITH_KNOTS('',3,(#20022,#20023,#20024,#20025,#20026,
#20027,#20028,#20029,#20030,#20031,#20032,#20033,#20034,#20035,#20036,#20037,
#20038,#20039,#20040,#20041,#20042,#20043,#20044,#20045,#20046,#20047,#20048,
#20049,#20050,#20051,#20052,#20053,#20054,#20055,#20056,#20057,#20058,#20059,
#20060,#20061,#20062,#20063,#20064,#20065,#20066,#20067,#20068,#20069,#20070,
#20071,#20072,#20073,#20074,#20075,#20076,#20077,#20078,#20079,#20080,#20081,
#20082,#20083,#20084,#20085,#20086,#20087,#20088,#20089,#20090,#20091,#20092,
#20093,#20094,#20095,#20096,#20097,#20098,#20099,#20100,#20101,#20102,#20103,
#20104,#20105,#20106,#20107,#20108,#20109,#20110,#20111,#20112,#20113,#20114,
#20115,#20116,#20117,#20118,#20119,#20120,#20121,#20122,#20123,#20124,#20125,
#20126,#20127,#20128,#20129,#20130,#20131,#20132,#20133,#20134,#20135,#20136,
#20137,#20138,#20139,#20140,#20141,#20142,#20143,#20144,#20145,#20146,#20147,
#20148,#20149,#20150,#20151,#20152,#20153,#20154,#20155,#20156,#20157,#20158,
#20159,#20160,#20161,#20162,#20163,#20164,#20165,#20166,#20167,#20168,#20169,
#20170,#20171,#20172,#20173,#20174,#20175,#20176,#20177,#20178,#20179,#20180,
#20181,#20182,#20183,#20184,#20185,#20186,#20187,#20188,#20189,#20190,#20191,
#20192,#20193,#20194,#20195,#20196,#20197,#20198,#20199,#20200,#20201,#20202,
#20203,#20204,#20205,#20206,#20207,#20208,#20209,#20210,#20211,#20212,#20213),
 .UNSPECIFIED.,.F.,.F.,(4,2,2,2,2,2,2,2,2,2,2,2,2,2,2,2,2,2,2,2,2,2,2,2,
2,2,2,2,2,2,2,2,2,2,2,2,2,2,2,2,2,2,2,2,2,2,2,2,2,2,2,2,2,2,2,2,2,2,2,2,
2,2,2,2,2,2,2,2,2,2,2,2,2,2,2,2,2,2,2,2,2,2,2,2,2,2,2,2,2,2,2,2,2,2,2,4),
(0.302215230993473,0.329128974360592,0.357185769673646,0.369402245040697,
0.378989406177068,0.384033554243151,0.384070159127476,0.384109313688677,
0.384151204849934,0.384196034379097,0.384244020179286,0.384295397705355,
0.384350421504573,0.384409366917275,0.38447253189265,0.384540238998633,
0.384612837573121,0.384690706047362,0.38477425445222,0.38486392706983,0.384960205242976,
0.385037539250905,0.385146049371129,0.385298292617762,0.38570222586489,
0.389955650760635,0.395543788853112,0.408146525352725,0.469715663524433,
0.531966096927452,0.541753248185602,0.545351210882397,0.54779720883181,
0.550007524781269,0.553054116064316,0.560795258722229,0.623382942899022,
0.692052308270695,0.701577049809445,0.706632611330204,0.710779313113456,
0.71567933677062,0.724230157428683,0.763480756018339,0.829501312458737,
0.861061657216598,0.866254908924068,0.869048392518178,0.871401214228517,
0.874386379678638,0.879157445918688,0.906988701133725,0.931748156993207,
0.97165600671502,1.00107308561578,1.01368393066366,1.02360457088653,1.0287417232672,
1.03293155613221,1.0377791516955,1.04609847437421,1.08134226978856,1.08754697792447,
1.15217797306174,1.18337278354229,1.18855307273335,1.19134383270273,1.19369694614796,
1.19668576131112,1.20146875606336,1.22958768252735,1.31383767257273,1.34048421317768,
1.34792998110663,1.35253816827687,1.35676831414208,1.36220736758336,1.37398064730734,
1.45268733617976,1.48931711425151,1.50119642118929,1.50939260987216,1.51274819502265,
1.51514813521365,1.51741522950933,1.52134645457812,1.53265220593135,1.59824802683231,
1.639724373617,1.66340376052312,1.67056196732202,1.67510762657115,1.67935991591873,
1.68494150859781,1.69750740525998,1.73011464129713),.UNSPECIFIED.);
#1283=B_SPLINE_CURVE_WITH_KNOTS('',3,(#20738,#20739,#20740,#20741,#20742,
#20743,#20744,#20745,#20746,#20747,#20748,#20749,#20750,#20751,#20752,#20753,
#20754,#20755,#20756,#20757,#20758,#20759,#20760,#20761,#20762,#20763,#20764,
#20765,#20766,#20767,#20768,#20769,#20770,#20771,#20772,#20773,#20774,#20775,
#20776,#20777,#20778,#20779,#20780,#20781,#20782,#20783,#20784,#20785,#20786,
#20787,#20788,#20789,#20790,#20791,#20792,#20793,#20794,#20795,#20796,#20797,
#20798,#20799,#20800,#20801,#20802,#20803,#20804,#20805,#20806,#20807,#20808,
#20809,#20810,#20811,#20812,#20813,#20814,#20815,#20816,#20817,#20818,#20819,
#20820,#20821,#20822,#20823,#20824,#20825,#20826,#20827,#20828,#20829,#20830,
#20831,#20832,#20833,#20834,#20835,#20836,#20837,#20838,#20839,#20840,#20841,
#20842,#20843,#20844,#20845,#20846,#20847,#20848,#20849,#20850,#20851,#20852,
#20853,#20854,#20855,#20856,#20857,#20858,#20859,#20860,#20861,#20862,#20863,
#20864,#20865,#20866,#20867,#20868,#20869,#20870,#20871,#20872,#20873,#20874,
#20875,#20876,#20877,#20878,#20879),.UNSPECIFIED.,.F.,.F.,(4,2,2,2,2,2,
2,2,2,2,2,2,2,2,2,2,2,2,2,2,2,2,2,2,2,2,2,2,2,2,2,2,2,2,2,2,2,2,2,2,2,2,
2,2,2,2,2,2,2,2,2,2,2,2,2,2,2,2,2,2,2,2,2,2,2,2,2,2,2,2,4),(2.33187697907722,
2.34000409178357,2.38271068663288,2.45303195363635,2.4732949170467,2.47808089597807,
2.48081495411595,2.48315271451519,2.48620928169482,2.4927041936187,2.54881461406063,
2.62166647798696,2.63268654209339,2.63814233847343,2.64211218048268,2.6463809720684,
2.65215891201936,2.66549643523321,2.68395147161456,2.73857417766915,2.74988897894658,
2.79414139013763,2.79972351460422,2.80263449545506,2.80498264728649,2.8078354289298,
2.8133218128894,2.85661449696997,2.92558724271068,2.95159091325247,2.95925084758828,
2.96390227143753,2.96811417032225,2.97353992920464,2.98494856249953,3.0297196538535,
3.08424430961922,3.11673561973802,3.12166499252487,3.1246957183138,3.12704994809193,
3.12980514136111,3.13482312746102,3.16204370662117,3.25733726872406,3.27586210312986,
3.28262899631771,3.28664460702511,3.29088640159593,3.29649699748084,3.30888401877498,
3.3256454764821,3.37173253357554,3.43546188845268,3.44314074139632,3.44617931693045,
3.44838928742662,3.45084813917423,3.45447784087544,3.46443143634096,3.52924641917268,
3.59293790347914,3.60116373260668,3.60642876603047,3.61063580943842,3.61540899080695,
3.62358055265985,3.65978812734178,3.7078645478554,3.75667841923273,3.75929980855926),
 .UNSPECIFIED.);
#1284=B_SPLINE_CURVE_WITH_KNOTS('',3,(#20881,#20882,#20883,#20884,#20885,
#20886,#20887,#20888,#20889,#20890,#20891,#20892,#20893,#20894,#20895,#20896,
#20897,#20898,#20899,#20900,#20901,#20902,#20903,#20904,#20905,#20906,#20907,
#20908,#20909,#20910,#20911,#20912,#20913,#20914,#20915,#20916,#20917,#20918,
#20919,#20920,#20921,#20922,#20923,#20924,#20925,#20926,#20927,#20928,#20929,
#20930,#20931,#20932,#20933,#20934,#20935,#20936,#20937,#20938,#20939,#20940,
#20941,#20942,#20943,#20944,#20945,#20946,#20947,#20948,#20949,#20950,#20951,
#20952,#20953,#20954,#20955,#20956,#20957,#20958,#20959,#20960,#20961,#20962,
#20963,#20964,#20965,#20966,#20967,#20968,#20969,#20970,#20971,#20972,#20973,
#20974,#20975,#20976,#20977,#20978,#20979,#20980,#20981,#20982,#20983,#20984,
#20985,#20986,#20987,#20988,#20989,#20990,#20991,#20992,#20993,#20994,#20995,
#20996,#20997,#20998,#20999,#21000,#21001,#21002,#21003,#21004,#21005,#21006,
#21007,#21008,#21009,#21010,#21011,#21012,#21013,#21014,#21015,#21016,#21017,
#21018,#21019,#21020,#21021,#21022,#21023,#21024,#21025,#21026,#21027,#21028,
#21029,#21030,#21031,#21032,#21033,#21034,#21035,#21036,#21037,#21038,#21039,
#21040,#21041,#21042,#21043,#21044,#21045,#21046,#21047,#21048,#21049,#21050,
#21051,#21052,#21053,#21054,#21055,#21056,#21057,#21058,#21059,#21060,#21061,
#21062,#21063,#21064,#21065,#21066,#21067,#21068,#21069,#21070,#21071,#21072,
#21073,#21074,#21075,#21076,#21077,#21078,#21079,#21080,#21081,#21082,#21083,
#21084,#21085,#21086),.UNSPECIFIED.,.F.,.F.,(4,2,2,2,2,2,2,2,2,2,2,2,2,
2,2,2,2,2,2,2,2,2,2,2,2,2,2,2,2,2,2,2,2,2,2,2,2,2,2,2,2,2,2,2,2,2,2,2,2,
2,2,2,2,2,2,2,2,2,2,2,2,2,2,2,2,2,2,2,2,2,2,2,2,2,2,2,2,2,2,2,2,2,2,2,2,
2,2,2,2,2,2,2,2,2,2,2,2,2,2,2,2,2,4),(2.03100183139203,2.0311472448286,
2.0622708037727,2.1307986436883,2.15265245736636,2.15754705736789,2.16030608582901,
2.16266263124956,2.16569484294027,2.17206554650664,2.18061445438363,2.20241417761017,
2.27029695476723,2.30728161376276,2.31571320665052,2.32058659138894,2.32477522958079,
2.32988143952482,2.33964953485503,2.40420335186027,2.47074499864376,2.47827448833059,
2.48128558801495,2.48348706779254,2.48594361662004,2.48959206774801,2.4997379536851,
2.56782034138872,2.62855310475401,2.63682059551014,2.64209294234794,2.64629318834684,
2.65104495693733,2.65914525368751,2.69437508074936,2.7729750427622,2.7971826404337,
2.80177646559555,2.80470824980164,2.80705889596875,2.80989786529937,2.81530591202188,
2.85434264552798,2.87971731437408,2.94566451311948,2.95801528969989,2.96314115027234,
2.96741918288954,2.97183251333061,2.97836829542996,2.99673365855859,3.02518936748285,
3.08614823250679,3.11885393924503,3.12379461090875,3.12683074091925,3.12918757736804,
3.13194371636431,3.13696141444024,3.16413342245865,3.25880189067027,3.27776297334542,
3.2845907817082,3.28861788340449,3.29285389393087,3.29842669702448,3.31060588700989,
3.36167721604079,3.41666941594778,3.44179447666789,3.44643354893427,3.449378812166,
3.45172954565832,3.4545557543779,3.45990431575374,3.49653725141768,3.58560785748541,
3.60121535936558,3.60753736150401,3.61146953061622,3.61576432738407,3.62169840492567,
3.63597792093371,3.70314519568518,3.75950691993871,3.76752008821574,3.77061012087802,
3.77283141818765,3.77521681384309,3.77850114381141,3.78236976497366,3.78931156482314,
3.80535352678214,3.8519522794886,3.91259087507341,3.92515931254135,3.93074093028329,
3.93499279186394,3.93953756523577,3.94669347964855,3.97035732895371,4.01178858053361,
4.06070745563291),.UNSPECIFIED.);
#1285=B_SPLINE_CURVE_WITH_KNOTS('',3,(#21088,#21089,#21090,#21091,#21092,
#21093,#21094,#21095,#21096,#21097,#21098,#21099,#21100,#21101,#21102,#21103,
#21104,#21105,#21106,#21107,#21108,#21109,#21110,#21111,#21112,#21113,#21114,
#21115,#21116,#21117,#21118,#21119,#21120,#21121,#21122,#21123,#21124,#21125,
#21126,#21127,#21128,#21129,#21130,#21131,#21132,#21133,#21134,#21135,#21136,
#21137,#21138,#21139,#21140,#21141,#21142,#21143,#21144,#21145,#21146,#21147,
#21148,#21149,#21150,#21151,#21152,#21153,#21154,#21155,#21156,#21157,#21158,
#21159,#21160,#21161,#21162,#21163,#21164,#21165,#21166,#21167,#21168,#21169,
#21170,#21171,#21172,#21173,#21174,#21175,#21176,#21177,#21178,#21179,#21180,
#21181,#21182,#21183,#21184,#21185,#21186,#21187,#21188,#21189,#21190,#21191,
#21192,#21193,#21194,#21195,#21196,#21197,#21198,#21199,#21200,#21201,#21202,
#21203,#21204,#21205,#21206,#21207,#21208,#21209,#21210,#21211,#21212,#21213,
#21214,#21215,#21216,#21217,#21218,#21219,#21220,#21221,#21222,#21223,#21224,
#21225,#21226,#21227,#21228,#21229,#21230,#21231,#21232,#21233,#21234,#21235,
#21236,#21237,#21238,#21239,#21240,#21241,#21242,#21243,#21244,#21245,#21246,
#21247,#21248,#21249,#21250,#21251,#21252,#21253,#21254,#21255,#21256,#21257),
 .UNSPECIFIED.,.F.,.F.,(4,2,2,2,2,2,2,2,2,2,2,2,2,2,2,2,2,2,2,2,2,2,2,2,
2,2,2,2,2,2,2,2,2,2,2,2,2,2,2,2,2,2,2,2,2,2,2,2,2,2,2,2,2,2,2,2,2,2,2,2,
2,2,2,2,2,2,2,2,2,2,2,2,2,2,2,2,2,2,2,2,2,2,2,2,4),(2.33214412619499,2.34314390748205,
2.34815976670484,2.35118603662359,2.35354714568822,2.35627647635811,2.36116839331613,
2.38575313385532,2.4344059690819,2.49775933657462,2.5059987165985,2.5112631569145,
2.51546348242276,2.52022216312754,2.52835123624104,2.56401913740978,2.61067247325097,
2.66146448119969,2.66956051740221,2.67266301938936,2.67488817530125,2.67732052144944,
2.68084815180698,2.69014696781106,2.70421481321656,2.80483048721128,2.82444188424143,
2.83136009644012,2.8358542296935,2.8401307355468,2.84595562003803,2.85957060127714,
2.87853203977876,2.97998146077599,2.99115573880753,2.9950692164851,2.99733307911335,
2.99973585156921,3.0031052138381,3.01138290597708,3.02341961134417,3.06086763776495,
3.13838682435815,3.14910298331414,3.15448450492669,3.15843564724393,3.16271800332851,
3.16857468337451,3.18237669982729,3.20168124026125,3.25854126081562,3.28358938223161,
3.31100908242314,3.31576364870506,3.3187442189316,3.3210972553409,3.32389553658596,
3.32910974010845,3.36124235303482,3.42893272730556,3.4661794014146,3.47462562401882,
3.47950250916065,3.48369122997518,3.48879388304669,3.49854374588661,3.56253348743775,
3.62976256051955,3.63723535957617,3.6402368847183,3.64243606917896,3.64489574106813,
3.64855867656192,3.65880894340948,3.67487898764247,3.74027143458282,3.78777384684983,
3.79588402007578,3.80110894017101,3.8053054379871,3.80924984992859,3.81598532022518,
3.83818153678218,3.87584990582865,3.88120708400659),.UNSPECIFIED.);
#1286=B_SPLINE_CURVE_WITH_KNOTS('',3,(#21259,#21260,#21261,#21262,#21263,
#21264,#21265,#21266,#21267,#21268,#21269,#21270,#21271,#21272,#21273,#21274,
#21275,#21276,#21277,#21278,#21279,#21280,#21281,#21282,#21283,#21284,#21285,
#21286,#21287,#21288,#21289,#21290,#21291,#21292,#21293,#21294,#21295,#21296,
#21297,#21298,#21299,#21300,#21301,#21302,#21303,#21304,#21305,#21306,#21307,
#21308,#21309,#21310,#21311,#21312,#21313,#21314,#21315,#21316,#21317,#21318,
#21319,#21320,#21321,#21322,#21323,#21324,#21325,#21326,#21327,#21328,#21329,
#21330,#21331,#21332,#21333,#21334,#21335,#21336,#21337,#21338,#21339,#21340,
#21341,#21342,#21343,#21344,#21345,#21346,#21347,#21348,#21349,#21350,#21351,
#21352,#21353,#21354,#21355,#21356,#21357,#21358,#21359,#21360,#21361,#21362,
#21363,#21364,#21365,#21366,#21367,#21368,#21369,#21370,#21371,#21372,#21373,
#21374,#21375,#21376,#21377,#21378,#21379,#21380,#21381,#21382,#21383,#21384,
#21385,#21386,#21387,#21388,#21389,#21390,#21391,#21392,#21393,#21394,#21395,
#21396,#21397,#21398,#21399,#21400,#21401,#21402,#21403,#21404,#21405,#21406,
#21407,#21408,#21409,#21410),.UNSPECIFIED.,.F.,.F.,(4,2,2,2,2,2,2,2,2,2,
2,2,2,2,2,2,2,2,2,2,2,2,2,2,2,2,2,2,2,2,2,2,2,2,2,2,2,2,2,2,2,2,2,2,2,2,
2,2,2,2,2,2,2,2,2,2,2,2,2,2,2,2,2,2,2,2,2,2,2,2,2,2,2,2,2,4),(0.301764389565749,
0.336997421742996,0.402082561451209,0.412049110741382,0.415672773957841,
0.418124329011747,0.420330373038981,0.423359284103103,0.430993232595732,
0.495970310647265,0.541381653988435,0.558002432545585,0.570309617785616,
0.575906333243603,0.580146535002168,0.584167219828148,0.590958727159664,
0.609654629986511,0.612060019638961,0.711477517129167,0.725494253380263,
0.734768867433389,0.738292895505578,0.74072454168496,0.742950473644679,
0.746055936666919,0.754173521210122,0.806227076830489,0.860614627825897,
0.879029039364973,0.892343234318116,0.898117562918137,0.902386070272692,
0.906898503025551,0.913899501389437,0.93413983033226,1.03396779548654,1.04800204454639,
1.05728549503769,1.06081107926912,1.06324322932423,1.06546917102268,1.06857405240924,
1.076685567579,1.12662310049518,1.1739252833292,1.20983528000517,1.21798015619441,
1.22274258104761,1.22694288265329,1.23220288395753,1.24042661088312,1.30176537997898,
1.36934405933428,1.37946192939676,1.3831071305885,1.38556349497273,1.38776634224661,
1.39078128546721,1.39833043639893,1.46471256066369,1.52993648428243,1.53944564985019,
1.54449911708538,1.54864722191747,1.55355257507023,1.56212209826921,1.60169513190205,
1.66746908985183,1.6989644829291,1.70415692239507,1.70695086905996,1.70930465801907,
1.71229179931322,1.71706738939369,1.7301847824281),.UNSPECIFIED.);
#1287=B_SPLINE_CURVE_WITH_KNOTS('',3,(#21412,#21413,#21414,#21415,#21416,
#21417,#21418,#21419,#21420,#21421,#21422,#21423,#21424,#21425,#21426,#21427,
#21428,#21429,#21430,#21431,#21432,#21433,#21434,#21435,#21436,#21437,#21438,
#21439,#21440,#21441,#21442,#21443,#21444,#21445,#21446,#21447,#21448,#21449,
#21450,#21451,#21452,#21453,#21454,#21455,#21456,#21457,#21458,#21459,#21460,
#21461,#21462,#21463,#21464,#21465,#21466,#21467,#21468,#21469,#21470,#21471,
#21472,#21473,#21474,#21475,#21476,#21477,#21478,#21479,#21480,#21481,#21482,
#21483,#21484,#21485,#21486,#21487,#21488,#21489,#21490,#21491,#21492,#21493,
#21494,#21495,#21496,#21497,#21498,#21499,#21500,#21501,#21502,#21503,#21504,
#21505,#21506,#21507,#21508,#21509,#21510,#21511,#21512,#21513,#21514,#21515,
#21516,#21517,#21518,#21519,#21520,#21521,#21522,#21523,#21524,#21525,#21526,
#21527,#21528,#21529,#21530,#21531,#21532,#21533,#21534,#21535,#21536,#21537,
#21538,#21539,#21540,#21541,#21542,#21543,#21544,#21545,#21546,#21547,#21548,
#21549,#21550,#21551,#21552,#21553,#21554,#21555,#21556,#21557,#21558,#21559,
#21560,#21561,#21562,#21563,#21564,#21565),.UNSPECIFIED.,.F.,.F.,(4,2,2,
2,2,2,2,2,2,2,2,2,2,2,2,2,2,2,2,2,2,2,2,2,2,2,2,2,2,2,2,2,2,2,2,2,2,2,2,
2,2,2,2,2,2,2,2,2,2,2,2,2,2,2,2,2,2,2,2,2,2,2,2,2,2,2,2,2,2,2,2,2,2,2,2,
2,4),(2.02429205743456,2.05982563655793,2.06831357651967,2.0732008319214,
2.07739042046877,2.08248414896639,2.09218608974965,2.15473965184139,2.22371438725919,
2.23113277901731,2.23403844746681,2.23643191535898,2.23898220662163,2.24306189954909,
2.25679125124458,2.28118682621688,2.36250058773232,2.38468531338238,2.39192507882908,
2.39648859072482,2.40073421316354,2.40636995271312,2.41889671966936,2.43590192211972,
2.48311572678428,2.54531869209189,2.55308440903767,2.55613485598263,2.55834598806923,
2.56079041955842,2.5643820272343,2.57412690853977,2.63573887958691,2.69810893458408,
2.71066961404753,2.71624977324714,2.72050129125558,2.72504643215298,2.73220446309448,
2.75588971687803,2.7973788235357,2.86304967048591,2.8742322698189,2.87814595134809,
2.88040924477266,2.88281112641316,2.8861783425374,2.89444589921121,2.90646402436641,
2.94382066934414,3.02144595405536,3.03214895875594,3.03752665854793,3.04147629715229,
3.04575827329045,3.05161669654854,3.06543366834844,3.08476732237958,3.14180416032355,
3.16715890002166,3.19403536748223,3.19876638997552,3.20173958629876,3.20409174214718,
3.20689483258659,3.21213375952348,3.24503719982133,3.31698945877872,3.34967688859921,
3.35782181140696,3.36262927634612,3.36682191085842,3.37190739490323,3.38169003524407,
3.3942227840258,3.42336842327489,3.45200167847295),.UNSPECIFIED.);
#1288=B_SPLINE_CURVE_WITH_KNOTS('',3,(#22090,#22091,#22092,#22093,#22094,
#22095,#22096,#22097,#22098,#22099,#22100,#22101,#22102,#22103,#22104,#22105,
#22106,#22107,#22108,#22109,#22110,#22111,#22112,#22113,#22114,#22115,#22116,
#22117,#22118,#22119,#22120,#22121,#22122,#22123,#22124,#22125,#22126,#22127,
#22128,#22129,#22130,#22131,#22132,#22133,#22134,#22135,#22136,#22137,#22138,
#22139,#22140,#22141,#22142,#22143,#22144,#22145,#22146,#22147,#22148,#22149,
#22150,#22151,#22152,#22153,#22154,#22155,#22156,#22157,#22158,#22159,#22160,
#22161,#22162,#22163,#22164,#22165,#22166,#22167,#22168,#22169,#22170,#22171,
#22172,#22173,#22174,#22175,#22176,#22177,#22178,#22179,#22180,#22181,#22182,
#22183),.UNSPECIFIED.,.F.,.F.,(4,3,3,3,3,3,3,3,3,3,3,3,3,3,3,3,3,3,3,3,
3,3,3,3,3,3,3,3,3,3,3,4),(0.,0.0258260740408245,0.0620914164741229,0.0993864137683754,
0.136681411062628,0.147696100525531,0.154010737947389,0.189902258745158,
0.22572273166162,0.260776893843891,0.288525741895271,0.294828798261742,
0.299623899892133,0.334131254550439,0.368141603593604,0.402151952636769,
0.423542327420144,0.431068176013837,0.436300783095514,0.441119373588802,
0.474798699922684,0.508767094152298,0.542465821270648,0.56749016733248,
0.575255905600941,0.608325399901122,0.640746061995403,0.657708562027131,
0.662778546763718,0.694621529164936,0.72559455743344,0.744397949170769),
 .UNSPECIFIED.);
#1289=B_SPLINE_CURVE_WITH_KNOTS('',3,(#23756,#23757,#23758,#23759,#23760,
#23761,#23762,#23763,#23764,#23765,#23766,#23767,#23768,#23769,#23770,#23771,
#23772,#23773,#23774,#23775,#23776,#23777,#23778,#23779,#23780,#23781,#23782,
#23783,#23784,#23785,#23786,#23787,#23788,#23789,#23790,#23791,#23792,#23793,
#23794,#23795,#23796,#23797,#23798,#23799,#23800,#23801,#23802,#23803,#23804,
#23805,#23806,#23807,#23808,#23809,#23810,#23811,#23812,#23813,#23814,#23815,
#23816,#23817,#23818,#23819,#23820,#23821,#23822,#23823,#23824,#23825,#23826,
#23827,#23828,#23829,#23830,#23831,#23832,#23833,#23834,#23835,#23836,#23837,
#23838,#23839,#23840,#23841,#23842,#23843,#23844,#23845,#23846,#23847,#23848,
#23849,#23850,#23851,#23852,#23853,#23854,#23855,#23856,#23857,#23858,#23859,
#23860,#23861,#23862,#23863,#23864,#23865,#23866,#23867,#23868,#23869,#23870,
#23871,#23872,#23873,#23874,#23875,#23876,#23877,#23878,#23879,#23880,#23881,
#23882,#23883,#23884,#23885,#23886,#23887,#23888,#23889,#23890,#23891,#23892,
#23893,#23894,#23895,#23896,#23897,#23898,#23899,#23900,#23901),
 .UNSPECIFIED.,.F.,.F.,(4,2,2,2,2,2,2,2,2,2,2,2,2,2,2,2,2,2,2,2,2,2,2,2,
2,2,2,2,2,2,2,2,2,2,2,2,2,2,2,2,2,2,2,2,2,2,2,2,2,2,2,2,2,2,2,2,2,2,2,2,
2,2,2,2,2,2,2,2,2,2,2,2,4),(0.00561840038966108,0.0829874935783554,0.113427462423338,
0.126395668356017,0.136577031974214,0.1418189926542,0.146080884437416,0.150998255954348,
0.159408985883126,0.195113324983282,0.259907465387342,0.281920212796875,
0.294766066261603,0.29881970124982,0.301371020753402,0.303763134602496,
0.307169565336292,0.315270901268713,0.364708929927512,0.411921772563163,
0.447764628065761,0.45592937153838,0.460710921840607,0.464932961417181,
0.4702269313106,0.478517238233412,0.540306725514118,0.58453028550462,0.605265236649418,
0.617560623264396,0.621484960969627,0.624002963893898,0.62640450493714,
0.629374199664684,0.636710300272061,0.705249954748309,0.748473115816585,
0.772740034761623,0.779926576082181,0.784457139716752,0.788672088869992,
0.794170698250464,0.806399405848167,0.879829039931145,0.920414664077409,
0.933011134198793,0.941564284506154,0.944960511711001,0.947356833621923,
0.94960519711638,0.953439151550553,0.9640459149341,1.03032509859657,1.07205030445187,
1.09583966565259,1.10302064013644,1.10757890181242,1.11184185903787,1.11743609652098,
1.13002667538366,1.19096936970976,1.25326166676231,1.26305870208845,1.26666723466649,
1.2691224866918,1.2713376802449,1.27439436336967,1.28217677566595,1.34418144738385,
1.39148325654162,1.40850471952644,1.42103960946813,1.42238233932181),
 .UNSPECIFIED.);
#1290=B_SPLINE_CURVE_WITH_KNOTS('',3,(#23903,#23904,#23905,#23906),
 .UNSPECIFIED.,.F.,.F.,(4,4),(0.,0.0501024666884938),.UNSPECIFIED.);
#1291=B_SPLINE_CURVE_WITH_KNOTS('',3,(#23907,#23908,#23909,#23910,#23911,
#23912,#23913,#23914,#23915,#23916,#23917,#23918,#23919,#23920,#23921,#23922,
#23923,#23924,#23925,#23926,#23927,#23928,#23929,#23930,#23931,#23932,#23933,
#23934,#23935,#23936,#23937,#23938,#23939,#23940,#23941,#23942,#23943),
 .UNSPECIFIED.,.F.,.F.,(4,3,3,3,3,3,3,3,3,3,3,3,4),(-3.03270570277863,-2.99355252518221,
-2.90575452476498,-2.81806846465193,-2.73046974794672,-2.64293160597546,
-2.55542456519864,-2.46792653698669,-2.3804154444671,-2.29281858352263,
-2.20517529783961,-2.11740034625084,-2.06153490655644),.UNSPECIFIED.);
#1292=B_SPLINE_CURVE_WITH_KNOTS('',3,(#23945,#23946,#23947,#23948,#23949,
#23950,#23951,#23952,#23953,#23954,#23955,#23956,#23957,#23958,#23959,#23960,
#23961,#23962,#23963,#23964,#23965,#23966,#23967,#23968,#23969,#23970,#23971,
#23972,#23973,#23974,#23975,#23976,#23977,#23978,#23979,#23980,#23981,#23982,
#23983,#23984,#23985,#23986,#23987,#23988,#23989,#23990,#23991,#23992,#23993,
#23994,#23995,#23996,#23997,#23998,#23999,#24000,#24001,#24002,#24003,#24004,
#24005,#24006,#24007,#24008,#24009,#24010,#24011,#24012,#24013,#24014,#24015,
#24016,#24017,#24018,#24019,#24020,#24021,#24022,#24023,#24024,#24025,#24026,
#24027,#24028,#24029,#24030,#24031,#24032,#24033,#24034,#24035,#24036,#24037,
#24038,#24039,#24040,#24041,#24042,#24043,#24044,#24045,#24046,#24047,#24048,
#24049,#24050),.UNSPECIFIED.,.F.,.F.,(4,3,3,3,3,3,3,3,3,3,3,3,3,3,3,3,3,
3,3,3,3,3,3,3,3,3,3,3,3,3,3,3,3,3,3,4),(11.6152142277546,11.710478589548,
11.8056881718592,11.9008650919448,11.9960581933183,12.0912656561396,12.186507565826,
12.2818040356968,12.3772412794828,12.4727567243883,12.5684397131032,12.613065069482,
12.7052250926877,12.7972467196939,12.8891587437926,12.9809895468936,13.0727771628103,
13.1645473844809,13.2563259834302,13.3481995729483,13.4401212358669,13.5322010952523,
13.6109159112094,13.7041429367066,13.79724435493,13.8902475827988,13.9831825993322,
14.0760822056078,14.1689710331669,14.2618736980142,14.3548731676223,14.4479236129884,
14.541125320041,14.6087667529368,14.7020045732548,14.7774109291987),
 .UNSPECIFIED.);
#1546=VERTEX_POINT('',#5728);
#1547=VERTEX_POINT('',#5729);
#1548=VERTEX_POINT('',#5731);
#1549=VERTEX_POINT('',#5763);
#1550=VERTEX_POINT('',#5860);
#1551=VERTEX_POINT('',#5861);
#1552=VERTEX_POINT('',#6294);
#1553=VERTEX_POINT('',#6295);
#1554=VERTEX_POINT('',#6704);
#1555=VERTEX_POINT('',#6705);
#1556=VERTEX_POINT('',#6943);
#1557=VERTEX_POINT('',#7181);
#1558=VERTEX_POINT('',#7182);
#1559=VERTEX_POINT('',#7184);
#1560=VERTEX_POINT('',#7716);
#1561=VERTEX_POINT('',#7717);
#1562=VERTEX_POINT('',#8148);
#1563=VERTEX_POINT('',#8149);
#1564=VERTEX_POINT('',#8371);
#1565=VERTEX_POINT('',#8597);
#1566=VERTEX_POINT('',#8598);
#1567=VERTEX_POINT('',#8600);
#1568=VERTEX_POINT('',#8829);
#1569=VERTEX_POINT('',#9057);
#1570=VERTEX_POINT('',#9058);
#1571=VERTEX_POINT('',#9060);
#1572=VERTEX_POINT('',#9516);
#1573=VERTEX_POINT('',#9517);
#1574=VERTEX_POINT('',#9944);
#1575=VERTEX_POINT('',#9945);
#1576=VERTEX_POINT('',#10161);
#1577=VERTEX_POINT('',#10387);
#1578=VERTEX_POINT('',#10388);
#1579=VERTEX_POINT('',#10390);
#1580=VERTEX_POINT('',#10838);
#1581=VERTEX_POINT('',#10839);
#1582=VERTEX_POINT('',#11294);
#1583=VERTEX_POINT('',#11295);
#1584=VERTEX_POINT('',#11517);
#1585=VERTEX_POINT('',#11751);
#1586=VERTEX_POINT('',#11752);
#1587=VERTEX_POINT('',#11754);
#1588=VERTEX_POINT('',#12290);
#1589=VERTEX_POINT('',#12291);
#1590=VERTEX_POINT('',#12293);
#1591=VERTEX_POINT('',#12298);
#1592=VERTEX_POINT('',#12495);
#1593=VERTEX_POINT('',#12747);
#1594=VERTEX_POINT('',#12748);
#1595=VERTEX_POINT('',#12757);
#1596=VERTEX_POINT('',#12759);
#1597=VERTEX_POINT('',#12766);
#1598=VERTEX_POINT('',#12768);
#1599=VERTEX_POINT('',#12775);
#1600=VERTEX_POINT('',#12777);
#1601=VERTEX_POINT('',#12784);
#1602=VERTEX_POINT('',#12786);
#1603=VERTEX_POINT('',#12793);
#1604=VERTEX_POINT('',#12795);
#1605=VERTEX_POINT('',#12802);
#1606=VERTEX_POINT('',#12804);
#1607=VERTEX_POINT('',#12811);
#1608=VERTEX_POINT('',#12813);
#1609=VERTEX_POINT('',#12820);
#1610=VERTEX_POINT('',#12822);
#1611=VERTEX_POINT('',#12827);
#1612=VERTEX_POINT('',#12829);
#1613=VERTEX_POINT('',#12838);
#1614=VERTEX_POINT('',#12840);
#1615=VERTEX_POINT('',#12847);
#1616=VERTEX_POINT('',#12849);
#1617=VERTEX_POINT('',#12858);
#1618=VERTEX_POINT('',#12860);
#1619=VERTEX_POINT('',#12869);
#1620=VERTEX_POINT('',#12871);
#1621=VERTEX_POINT('',#12882);
#1622=VERTEX_POINT('',#12887);
#1623=VERTEX_POINT('',#12892);
#1624=VERTEX_POINT('',#12901);
#1625=VERTEX_POINT('',#12964);
#1626=VERTEX_POINT('',#12971);
#1627=VERTEX_POINT('',#12983);
#1628=VERTEX_POINT('',#12988);
#1629=VERTEX_POINT('',#12993);
#1630=VERTEX_POINT('',#12995);
#1631=VERTEX_POINT('',#13084);
#1632=VERTEX_POINT('',#13091);
#1633=VERTEX_POINT('',#13294);
#1634=VERTEX_POINT('',#13305);
#1635=VERTEX_POINT('',#13532);
#1636=VERTEX_POINT('',#13544);
#1637=VERTEX_POINT('',#13771);
#1638=VERTEX_POINT('',#13998);
#1639=VERTEX_POINT('',#14010);
#1640=VERTEX_POINT('',#14237);
#1641=VERTEX_POINT('',#14464);
#1642=VERTEX_POINT('',#14475);
#1643=VERTEX_POINT('',#14705);
#1644=VERTEX_POINT('',#14716);
#1645=VERTEX_POINT('',#14727);
#1646=VERTEX_POINT('',#14951);
#1647=VERTEX_POINT('',#14962);
#1648=VERTEX_POINT('',#15189);
#1649=VERTEX_POINT('',#15198);
#1650=VERTEX_POINT('',#15200);
#1651=VERTEX_POINT('',#15388);
#1652=VERTEX_POINT('',#15399);
#1653=VERTEX_POINT('',#15626);
#1654=VERTEX_POINT('',#15853);
#1655=VERTEX_POINT('',#15864);
#1656=VERTEX_POINT('',#16094);
#1657=VERTEX_POINT('',#16324);
#1658=VERTEX_POINT('',#16335);
#1659=VERTEX_POINT('',#16562);
#1660=VERTEX_POINT('',#16573);
#1661=VERTEX_POINT('',#16585);
#1662=VERTEX_POINT('',#16812);
#1663=VERTEX_POINT('',#16823);
#1664=VERTEX_POINT('',#17050);
#1665=VERTEX_POINT('',#17277);
#1666=VERTEX_POINT('',#18724);
#2064=EDGE_CURVE('',#1546,#1547,#769,.T.);
#2065=EDGE_CURVE('',#1547,#1548,#1168,.T.);
#2066=EDGE_CURVE('',#1548,#1549,#630,.T.);
#2067=EDGE_CURVE('',#1546,#1549,#1169,.F.);
#2068=EDGE_CURVE('',#1550,#1551,#770,.T.);
#2069=EDGE_CURVE('',#1551,#1547,#1170,.T.);
#2070=EDGE_CURVE('',#1550,#1546,#1171,.F.);
#2071=EDGE_CURVE('',#1552,#1553,#771,.T.);
#2072=EDGE_CURVE('',#1553,#1551,#1172,.T.);
#2073=EDGE_CURVE('',#1552,#1550,#1173,.F.);
#2074=EDGE_CURVE('',#1554,#1555,#772,.T.);
#2075=EDGE_CURVE('',#1555,#1553,#1174,.T.);
#2076=EDGE_CURVE('',#1556,#1552,#1175,.F.);
#2077=EDGE_CURVE('',#1554,#1556,#1176,.F.);
#2078=EDGE_CURVE('',#1557,#1558,#773,.T.);
#2079=EDGE_CURVE('',#1558,#1559,#1177,.T.);
#2080=EDGE_CURVE('',#1559,#1555,#1178,.T.);
#2081=EDGE_CURVE('',#1557,#1554,#1179,.F.);
#2082=EDGE_CURVE('',#1560,#1561,#774,.T.);
#2083=EDGE_CURVE('',#1561,#1558,#1180,.T.);
#2084=EDGE_CURVE('',#1560,#1557,#1181,.F.);
#2085=EDGE_CURVE('',#1562,#1563,#775,.T.);
#2086=EDGE_CURVE('',#1563,#1561,#1182,.T.);
#2087=EDGE_CURVE('',#1564,#1560,#1183,.F.);
#2088=EDGE_CURVE('',#1562,#1564,#1184,.F.);
#2089=EDGE_CURVE('',#1565,#1566,#776,.T.);
#2090=EDGE_CURVE('',#1566,#1567,#1185,.T.);
#2091=EDGE_CURVE('',#1567,#1563,#1186,.T.);
#2092=EDGE_CURVE('',#1568,#1562,#1187,.F.);
#2093=EDGE_CURVE('',#1565,#1568,#1188,.F.);
#2094=EDGE_CURVE('',#1569,#1570,#777,.T.);
#2095=EDGE_CURVE('',#1570,#1571,#1189,.T.);
#2096=EDGE_CURVE('',#1571,#1566,#1190,.T.);
#2097=EDGE_CURVE('',#1569,#1565,#1191,.F.);
#2098=EDGE_CURVE('',#1572,#1573,#778,.T.);
#2099=EDGE_CURVE('',#1573,#1570,#1192,.T.);
#2100=EDGE_CURVE('',#1572,#1569,#1193,.F.);
#2101=EDGE_CURVE('',#1574,#1575,#779,.T.);
#2102=EDGE_CURVE('',#1575,#1573,#1194,.T.);
#2103=EDGE_CURVE('',#1576,#1572,#1195,.F.);
#2104=EDGE_CURVE('',#1574,#1576,#1196,.F.);
#2105=EDGE_CURVE('',#1577,#1578,#780,.T.);
#2106=EDGE_CURVE('',#1578,#1579,#1197,.T.);
#2107=EDGE_CURVE('',#1579,#1575,#1198,.T.);
#2108=EDGE_CURVE('',#1577,#1574,#1199,.F.);
#2109=EDGE_CURVE('',#1580,#1581,#781,.T.);
#2110=EDGE_CURVE('',#1581,#1578,#1200,.T.);
#2111=EDGE_CURVE('',#1580,#1577,#1201,.F.);
#2112=EDGE_CURVE('',#1582,#1583,#782,.T.);
#2113=EDGE_CURVE('',#1583,#1581,#1202,.T.);
#2114=EDGE_CURVE('',#1584,#1580,#1203,.F.);
#2115=EDGE_CURVE('',#1582,#1584,#1204,.F.);
#2116=EDGE_CURVE('',#1585,#1586,#783,.T.);
#2117=EDGE_CURVE('',#1586,#1587,#1205,.T.);
#2118=EDGE_CURVE('',#1587,#1583,#1206,.T.);
#2119=EDGE_CURVE('',#1585,#1582,#1207,.F.);
#2120=EDGE_CURVE('',#1588,#1589,#784,.T.);
#2121=EDGE_CURVE('',#1590,#1588,#1208,.F.);
#2122=EDGE_CURVE('',#1591,#1590,#1209,.F.);
#2123=EDGE_CURVE('',#1591,#1592,#1210,.T.);
#2124=EDGE_CURVE('',#1592,#1589,#1211,.T.);
#2125=EDGE_CURVE('',#1593,#1594,#1212,.T.);
#2126=EDGE_CURVE('',#1595,#1593,#631,.T.);
#2127=EDGE_CURVE('',#1596,#1595,#1213,.T.);
#2128=EDGE_CURVE('',#1597,#1596,#785,.T.);
#2129=EDGE_CURVE('',#1598,#1597,#1214,.T.);
#2130=EDGE_CURVE('',#1599,#1598,#786,.T.);
#2131=EDGE_CURVE('',#1600,#1599,#1215,.T.);
#2132=EDGE_CURVE('',#1601,#1600,#787,.T.);
#2133=EDGE_CURVE('',#1602,#1601,#1216,.T.);
#2134=EDGE_CURVE('',#1603,#1602,#788,.T.);
#2135=EDGE_CURVE('',#1604,#1603,#1217,.T.);
#2136=EDGE_CURVE('',#1605,#1604,#789,.T.);
#2137=EDGE_CURVE('',#1606,#1605,#1218,.T.);
#2138=EDGE_CURVE('',#1607,#1606,#790,.T.);
#2139=EDGE_CURVE('',#1608,#1607,#1219,.T.);
#2140=EDGE_CURVE('',#1609,#1608,#791,.T.);
#2141=EDGE_CURVE('',#1610,#1609,#1220,.T.);
#2142=EDGE_CURVE('',#1611,#1610,#792,.T.);
#2143=EDGE_CURVE('',#1612,#1611,#1221,.T.);
#2144=EDGE_CURVE('',#1613,#1612,#793,.T.);
#2145=EDGE_CURVE('',#1614,#1613,#1222,.T.);
#2146=EDGE_CURVE('',#1615,#1614,#794,.T.);
#2147=EDGE_CURVE('',#1616,#1615,#1223,.T.);
#2148=EDGE_CURVE('',#1617,#1616,#795,.T.);
#2149=EDGE_CURVE('',#1618,#1617,#1224,.T.);
#2150=EDGE_CURVE('',#1619,#1618,#796,.T.);
#2151=EDGE_CURVE('',#1620,#1619,#1225,.T.);
#2152=EDGE_CURVE('',#1594,#1620,#797,.T.);
#2153=EDGE_CURVE('',#1621,#1593,#1226,.T.);
#2154=EDGE_CURVE('',#1622,#1621,#1227,.T.);
#2155=EDGE_CURVE('',#1623,#1622,#1228,.T.);
#2156=EDGE_CURVE('',#1624,#1623,#1229,.T.);
#2157=EDGE_CURVE('',#1592,#1624,#1230,.T.);
#2158=EDGE_CURVE('',#1625,#1591,#1231,.T.);
#2159=EDGE_CURVE('',#1626,#1625,#1232,.T.);
#2160=EDGE_CURVE('',#1595,#1626,#1233,.T.);
#2161=EDGE_CURVE('',#1627,#1608,#1234,.T.);
#2162=EDGE_CURVE('',#1628,#1627,#1235,.T.);
#2163=EDGE_CURVE('',#1629,#1628,#632,.T.);
#2164=EDGE_CURVE('',#1630,#1629,#1236,.T.);
#2165=EDGE_CURVE('',#1631,#1630,#633,.F.);
#2166=EDGE_CURVE('',#1609,#1631,#1237,.T.);
#2167=EDGE_CURVE('',#1632,#1625,#1238,.T.);
#2168=EDGE_CURVE('',#1633,#1632,#1239,.T.);
#2169=EDGE_CURVE('',#1634,#1633,#1240,.T.);
#2170=EDGE_CURVE('',#1635,#1634,#1241,.T.);
#2171=EDGE_CURVE('',#1636,#1635,#1242,.T.);
#2172=EDGE_CURVE('',#1637,#1636,#1243,.T.);
#2173=EDGE_CURVE('',#1638,#1637,#1244,.T.);
#2174=EDGE_CURVE('',#1639,#1638,#1245,.T.);
#2175=EDGE_CURVE('',#1640,#1639,#1246,.T.);
#2176=EDGE_CURVE('',#1641,#1640,#1247,.T.);
#2177=EDGE_CURVE('',#1642,#1641,#1248,.T.);
#2178=EDGE_CURVE('',#1643,#1642,#1249,.T.);
#2179=EDGE_CURVE('',#1644,#1643,#1250,.T.);
#2180=EDGE_CURVE('',#1645,#1644,#1251,.T.);
#2181=EDGE_CURVE('',#1646,#1645,#1252,.T.);
#2182=EDGE_CURVE('',#1647,#1646,#1253,.T.);
#2183=EDGE_CURVE('',#1648,#1647,#1254,.T.);
#2184=EDGE_CURVE('',#1648,#1649,#634,.T.);
#2185=EDGE_CURVE('',#1650,#1649,#1255,.T.);
#2186=EDGE_CURVE('',#1651,#1650,#1256,.T.);
#2187=EDGE_CURVE('',#1652,#1651,#1257,.T.);
#2188=EDGE_CURVE('',#1653,#1652,#1258,.T.);
#2189=EDGE_CURVE('',#1654,#1653,#1259,.T.);
#2190=EDGE_CURVE('',#1655,#1654,#1260,.T.);
#2191=EDGE_CURVE('',#1656,#1655,#1261,.T.);
#2192=EDGE_CURVE('',#1657,#1656,#1262,.T.);
#2193=EDGE_CURVE('',#1658,#1657,#1263,.T.);
#2194=EDGE_CURVE('',#1659,#1658,#1264,.T.);
#2195=EDGE_CURVE('',#1660,#1659,#1265,.T.);
#2196=EDGE_CURVE('',#1661,#1660,#1266,.T.);
#2197=EDGE_CURVE('',#1662,#1661,#1267,.T.);
#2198=EDGE_CURVE('',#1663,#1662,#1268,.T.);
#2199=EDGE_CURVE('',#1664,#1663,#1269,.T.);
#2200=EDGE_CURVE('',#1665,#1664,#1270,.T.);
#2201=EDGE_CURVE('',#1626,#1665,#1271,.T.);
#2202=EDGE_CURVE('',#1622,#1598,#1272,.T.);
#2203=EDGE_CURVE('',#1599,#1621,#1273,.T.);
#2204=EDGE_CURVE('',#1619,#1602,#1274,.T.);
#2205=EDGE_CURVE('',#1603,#1618,#1275,.T.);
#2206=EDGE_CURVE('',#1615,#1606,#1276,.T.);
#2207=EDGE_CURVE('',#1607,#1614,#1277,.T.);
#2208=EDGE_CURVE('',#1588,#1585,#1278,.F.);
#2209=EDGE_CURVE('',#1549,#1666,#1279,.T.);
#2210=EDGE_CURVE('',#1666,#1648,#1280,.T.);
#2211=EDGE_CURVE('',#1597,#1623,#1281,.F.);
#2212=EDGE_CURVE('',#1601,#1620,#1282,.F.);
#2213=EDGE_CURVE('',#1605,#1616,#1283,.F.);
#2214=EDGE_CURVE('',#1589,#1586,#1284,.T.);
#2215=EDGE_CURVE('',#1596,#1624,#1285,.T.);
#2216=EDGE_CURVE('',#1600,#1594,#1286,.T.);
#2217=EDGE_CURVE('',#1604,#1617,#1287,.T.);
#2218=EDGE_CURVE('',#1649,#1548,#1288,.T.);
#2219=EDGE_CURVE('',#1628,#1613,#1289,.T.);
#2220=EDGE_CURVE('',#1631,#1610,#1290,.T.);
#2221=EDGE_CURVE('',#1611,#1630,#1291,.T.);
#2222=EDGE_CURVE('',#1629,#1612,#1292,.T.);
#2821=ORIENTED_EDGE('',*,*,#2064,.T.);
#2822=ORIENTED_EDGE('',*,*,#2065,.T.);
#2823=ORIENTED_EDGE('',*,*,#2066,.T.);
#2824=ORIENTED_EDGE('',*,*,#2067,.F.);
#2825=ORIENTED_EDGE('',*,*,#2068,.T.);
#2826=ORIENTED_EDGE('',*,*,#2069,.T.);
#2827=ORIENTED_EDGE('',*,*,#2064,.F.);
#2828=ORIENTED_EDGE('',*,*,#2070,.F.);
#2829=ORIENTED_EDGE('',*,*,#2071,.T.);
#2830=ORIENTED_EDGE('',*,*,#2072,.T.);
#2831=ORIENTED_EDGE('',*,*,#2068,.F.);
#2832=ORIENTED_EDGE('',*,*,#2073,.F.);
#2833=ORIENTED_EDGE('',*,*,#2074,.T.);
#2834=ORIENTED_EDGE('',*,*,#2075,.T.);
#2835=ORIENTED_EDGE('',*,*,#2071,.F.);
#2836=ORIENTED_EDGE('',*,*,#2076,.F.);
#2837=ORIENTED_EDGE('',*,*,#2077,.F.);
#2838=ORIENTED_EDGE('',*,*,#2078,.T.);
#2839=ORIENTED_EDGE('',*,*,#2079,.T.);
#2840=ORIENTED_EDGE('',*,*,#2080,.T.);
#2841=ORIENTED_EDGE('',*,*,#2074,.F.);
#2842=ORIENTED_EDGE('',*,*,#2081,.F.);
#2843=ORIENTED_EDGE('',*,*,#2082,.T.);
#2844=ORIENTED_EDGE('',*,*,#2083,.T.);
#2845=ORIENTED_EDGE('',*,*,#2078,.F.);
#2846=ORIENTED_EDGE('',*,*,#2084,.F.);
#2847=ORIENTED_EDGE('',*,*,#2085,.T.);
#2848=ORIENTED_EDGE('',*,*,#2086,.T.);
#2849=ORIENTED_EDGE('',*,*,#2082,.F.);
#2850=ORIENTED_EDGE('',*,*,#2087,.F.);
#2851=ORIENTED_EDGE('',*,*,#2088,.F.);
#2852=ORIENTED_EDGE('',*,*,#2089,.T.);
#2853=ORIENTED_EDGE('',*,*,#2090,.T.);
#2854=ORIENTED_EDGE('',*,*,#2091,.T.);
#2855=ORIENTED_EDGE('',*,*,#2085,.F.);
#2856=ORIENTED_EDGE('',*,*,#2092,.F.);
#2857=ORIENTED_EDGE('',*,*,#2093,.F.);
#2858=ORIENTED_EDGE('',*,*,#2094,.T.);
#2859=ORIENTED_EDGE('',*,*,#2095,.T.);
#2860=ORIENTED_EDGE('',*,*,#2096,.T.);
#2861=ORIENTED_EDGE('',*,*,#2089,.F.);
#2862=ORIENTED_EDGE('',*,*,#2097,.F.);
#2863=ORIENTED_EDGE('',*,*,#2098,.T.);
#2864=ORIENTED_EDGE('',*,*,#2099,.T.);
#2865=ORIENTED_EDGE('',*,*,#2094,.F.);
#2866=ORIENTED_EDGE('',*,*,#2100,.F.);
#2867=ORIENTED_EDGE('',*,*,#2101,.T.);
#2868=ORIENTED_EDGE('',*,*,#2102,.T.);
#2869=ORIENTED_EDGE('',*,*,#2098,.F.);
#2870=ORIENTED_EDGE('',*,*,#2103,.F.);
#2871=ORIENTED_EDGE('',*,*,#2104,.F.);
#2872=ORIENTED_EDGE('',*,*,#2105,.T.);
#2873=ORIENTED_EDGE('',*,*,#2106,.T.);
#2874=ORIENTED_EDGE('',*,*,#2107,.T.);
#2875=ORIENTED_EDGE('',*,*,#2101,.F.);
#2876=ORIENTED_EDGE('',*,*,#2108,.F.);
#2877=ORIENTED_EDGE('',*,*,#2109,.T.);
#2878=ORIENTED_EDGE('',*,*,#2110,.T.);
#2879=ORIENTED_EDGE('',*,*,#2105,.F.);
#2880=ORIENTED_EDGE('',*,*,#2111,.F.);
#2881=ORIENTED_EDGE('',*,*,#2112,.T.);
#2882=ORIENTED_EDGE('',*,*,#2113,.T.);
#2883=ORIENTED_EDGE('',*,*,#2109,.F.);
#2884=ORIENTED_EDGE('',*,*,#2114,.F.);
#2885=ORIENTED_EDGE('',*,*,#2115,.F.);
#2886=ORIENTED_EDGE('',*,*,#2116,.T.);
#2887=ORIENTED_EDGE('',*,*,#2117,.T.);
#2888=ORIENTED_EDGE('',*,*,#2118,.T.);
#2889=ORIENTED_EDGE('',*,*,#2112,.F.);
#2890=ORIENTED_EDGE('',*,*,#2119,.F.);
#2891=ORIENTED_EDGE('',*,*,#2120,.F.);
#2892=ORIENTED_EDGE('',*,*,#2121,.F.);
#2893=ORIENTED_EDGE('',*,*,#2122,.F.);
#2894=ORIENTED_EDGE('',*,*,#2123,.T.);
#2895=ORIENTED_EDGE('',*,*,#2124,.T.);
#2896=ORIENTED_EDGE('',*,*,#2125,.F.);
#2897=ORIENTED_EDGE('',*,*,#2126,.F.);
#2898=ORIENTED_EDGE('',*,*,#2127,.F.);
#2899=ORIENTED_EDGE('',*,*,#2128,.F.);
#2900=ORIENTED_EDGE('',*,*,#2129,.F.);
#2901=ORIENTED_EDGE('',*,*,#2130,.F.);
#2902=ORIENTED_EDGE('',*,*,#2131,.F.);
#2903=ORIENTED_EDGE('',*,*,#2132,.F.);
#2904=ORIENTED_EDGE('',*,*,#2133,.F.);
#2905=ORIENTED_EDGE('',*,*,#2134,.F.);
#2906=ORIENTED_EDGE('',*,*,#2135,.F.);
#2907=ORIENTED_EDGE('',*,*,#2136,.F.);
#2908=ORIENTED_EDGE('',*,*,#2137,.F.);
#2909=ORIENTED_EDGE('',*,*,#2138,.F.);
#2910=ORIENTED_EDGE('',*,*,#2139,.F.);
#2911=ORIENTED_EDGE('',*,*,#2140,.F.);
#2912=ORIENTED_EDGE('',*,*,#2141,.F.);
#2913=ORIENTED_EDGE('',*,*,#2142,.F.);
#2914=ORIENTED_EDGE('',*,*,#2143,.F.);
#2915=ORIENTED_EDGE('',*,*,#2144,.F.);
#2916=ORIENTED_EDGE('',*,*,#2145,.F.);
#2917=ORIENTED_EDGE('',*,*,#2146,.F.);
#2918=ORIENTED_EDGE('',*,*,#2147,.F.);
#2919=ORIENTED_EDGE('',*,*,#2148,.F.);
#2920=ORIENTED_EDGE('',*,*,#2149,.F.);
#2921=ORIENTED_EDGE('',*,*,#2150,.F.);
#2922=ORIENTED_EDGE('',*,*,#2151,.F.);
#2923=ORIENTED_EDGE('',*,*,#2152,.F.);
#2924=ORIENTED_EDGE('',*,*,#2153,.F.);
#2925=ORIENTED_EDGE('',*,*,#2154,.F.);
#2926=ORIENTED_EDGE('',*,*,#2155,.F.);
#2927=ORIENTED_EDGE('',*,*,#2156,.F.);
#2928=ORIENTED_EDGE('',*,*,#2157,.F.);
#2929=ORIENTED_EDGE('',*,*,#2123,.F.);
#2930=ORIENTED_EDGE('',*,*,#2158,.F.);
#2931=ORIENTED_EDGE('',*,*,#2159,.F.);
#2932=ORIENTED_EDGE('',*,*,#2160,.F.);
#2933=ORIENTED_EDGE('',*,*,#2126,.T.);
#2934=ORIENTED_EDGE('',*,*,#2140,.T.);
#2935=ORIENTED_EDGE('',*,*,#2161,.F.);
#2936=ORIENTED_EDGE('',*,*,#2162,.F.);
#2937=ORIENTED_EDGE('',*,*,#2163,.F.);
#2938=ORIENTED_EDGE('',*,*,#2164,.F.);
#2939=ORIENTED_EDGE('',*,*,#2165,.F.);
#2940=ORIENTED_EDGE('',*,*,#2166,.F.);
#2941=ORIENTED_EDGE('',*,*,#2159,.T.);
#2942=ORIENTED_EDGE('',*,*,#2167,.F.);
#2943=ORIENTED_EDGE('',*,*,#2168,.F.);
#2944=ORIENTED_EDGE('',*,*,#2169,.F.);
#2945=ORIENTED_EDGE('',*,*,#2170,.F.);
#2946=ORIENTED_EDGE('',*,*,#2171,.F.);
#2947=ORIENTED_EDGE('',*,*,#2172,.F.);
#2948=ORIENTED_EDGE('',*,*,#2173,.F.);
#2949=ORIENTED_EDGE('',*,*,#2174,.F.);
#2950=ORIENTED_EDGE('',*,*,#2175,.F.);
#2951=ORIENTED_EDGE('',*,*,#2176,.F.);
#2952=ORIENTED_EDGE('',*,*,#2177,.F.);
#2953=ORIENTED_EDGE('',*,*,#2178,.F.);
#2954=ORIENTED_EDGE('',*,*,#2179,.F.);
#2955=ORIENTED_EDGE('',*,*,#2180,.F.);
#2956=ORIENTED_EDGE('',*,*,#2181,.F.);
#2957=ORIENTED_EDGE('',*,*,#2182,.F.);
#2958=ORIENTED_EDGE('',*,*,#2183,.F.);
#2959=ORIENTED_EDGE('',*,*,#2184,.T.);
#2960=ORIENTED_EDGE('',*,*,#2185,.F.);
#2961=ORIENTED_EDGE('',*,*,#2186,.F.);
#2962=ORIENTED_EDGE('',*,*,#2187,.F.);
#2963=ORIENTED_EDGE('',*,*,#2188,.F.);
#2964=ORIENTED_EDGE('',*,*,#2189,.F.);
#2965=ORIENTED_EDGE('',*,*,#2190,.F.);
#2966=ORIENTED_EDGE('',*,*,#2191,.F.);
#2967=ORIENTED_EDGE('',*,*,#2192,.F.);
#2968=ORIENTED_EDGE('',*,*,#2193,.F.);
#2969=ORIENTED_EDGE('',*,*,#2194,.F.);
#2970=ORIENTED_EDGE('',*,*,#2195,.F.);
#2971=ORIENTED_EDGE('',*,*,#2196,.F.);
#2972=ORIENTED_EDGE('',*,*,#2197,.F.);
#2973=ORIENTED_EDGE('',*,*,#2198,.F.);
#2974=ORIENTED_EDGE('',*,*,#2199,.F.);
#2975=ORIENTED_EDGE('',*,*,#2200,.F.);
#2976=ORIENTED_EDGE('',*,*,#2201,.F.);
#2977=ORIENTED_EDGE('',*,*,#2130,.T.);
#2978=ORIENTED_EDGE('',*,*,#2202,.F.);
#2979=ORIENTED_EDGE('',*,*,#2154,.T.);
#2980=ORIENTED_EDGE('',*,*,#2203,.F.);
#2981=ORIENTED_EDGE('',*,*,#2134,.T.);
#2982=ORIENTED_EDGE('',*,*,#2204,.F.);
#2983=ORIENTED_EDGE('',*,*,#2150,.T.);
#2984=ORIENTED_EDGE('',*,*,#2205,.F.);
#2985=ORIENTED_EDGE('',*,*,#2138,.T.);
#2986=ORIENTED_EDGE('',*,*,#2206,.F.);
#2987=ORIENTED_EDGE('',*,*,#2146,.T.);
#2988=ORIENTED_EDGE('',*,*,#2207,.F.);
#2989=ORIENTED_EDGE('',*,*,#2158,.T.);
#2990=ORIENTED_EDGE('',*,*,#2122,.T.);
#2991=ORIENTED_EDGE('',*,*,#2121,.T.);
#2992=ORIENTED_EDGE('',*,*,#2208,.T.);
#2993=ORIENTED_EDGE('',*,*,#2119,.T.);
#2994=ORIENTED_EDGE('',*,*,#2115,.T.);
#2995=ORIENTED_EDGE('',*,*,#2114,.T.);
#2996=ORIENTED_EDGE('',*,*,#2111,.T.);
#2997=ORIENTED_EDGE('',*,*,#2108,.T.);
#2998=ORIENTED_EDGE('',*,*,#2104,.T.);
#2999=ORIENTED_EDGE('',*,*,#2103,.T.);
#3000=ORIENTED_EDGE('',*,*,#2100,.T.);
#3001=ORIENTED_EDGE('',*,*,#2097,.T.);
#3002=ORIENTED_EDGE('',*,*,#2093,.T.);
#3003=ORIENTED_EDGE('',*,*,#2092,.T.);
#3004=ORIENTED_EDGE('',*,*,#2088,.T.);
#3005=ORIENTED_EDGE('',*,*,#2087,.T.);
#3006=ORIENTED_EDGE('',*,*,#2084,.T.);
#3007=ORIENTED_EDGE('',*,*,#2081,.T.);
#3008=ORIENTED_EDGE('',*,*,#2077,.T.);
#3009=ORIENTED_EDGE('',*,*,#2076,.T.);
#3010=ORIENTED_EDGE('',*,*,#2073,.T.);
#3011=ORIENTED_EDGE('',*,*,#2070,.T.);
#3012=ORIENTED_EDGE('',*,*,#2067,.T.);
#3013=ORIENTED_EDGE('',*,*,#2209,.T.);
#3014=ORIENTED_EDGE('',*,*,#2210,.T.);
#3015=ORIENTED_EDGE('',*,*,#2183,.T.);
#3016=ORIENTED_EDGE('',*,*,#2182,.T.);
#3017=ORIENTED_EDGE('',*,*,#2181,.T.);
#3018=ORIENTED_EDGE('',*,*,#2180,.T.);
#3019=ORIENTED_EDGE('',*,*,#2179,.T.);
#3020=ORIENTED_EDGE('',*,*,#2178,.T.);
#3021=ORIENTED_EDGE('',*,*,#2177,.T.);
#3022=ORIENTED_EDGE('',*,*,#2176,.T.);
#3023=ORIENTED_EDGE('',*,*,#2175,.T.);
#3024=ORIENTED_EDGE('',*,*,#2174,.T.);
#3025=ORIENTED_EDGE('',*,*,#2173,.T.);
#3026=ORIENTED_EDGE('',*,*,#2172,.T.);
#3027=ORIENTED_EDGE('',*,*,#2171,.T.);
#3028=ORIENTED_EDGE('',*,*,#2170,.T.);
#3029=ORIENTED_EDGE('',*,*,#2169,.T.);
#3030=ORIENTED_EDGE('',*,*,#2168,.T.);
#3031=ORIENTED_EDGE('',*,*,#2167,.T.);
#3032=ORIENTED_EDGE('',*,*,#2129,.T.);
#3033=ORIENTED_EDGE('',*,*,#2211,.T.);
#3034=ORIENTED_EDGE('',*,*,#2155,.T.);
#3035=ORIENTED_EDGE('',*,*,#2202,.T.);
#3036=ORIENTED_EDGE('',*,*,#2133,.T.);
#3037=ORIENTED_EDGE('',*,*,#2212,.T.);
#3038=ORIENTED_EDGE('',*,*,#2151,.T.);
#3039=ORIENTED_EDGE('',*,*,#2204,.T.);
#3040=ORIENTED_EDGE('',*,*,#2137,.T.);
#3041=ORIENTED_EDGE('',*,*,#2213,.T.);
#3042=ORIENTED_EDGE('',*,*,#2147,.T.);
#3043=ORIENTED_EDGE('',*,*,#2206,.T.);
#3044=ORIENTED_EDGE('',*,*,#2120,.T.);
#3045=ORIENTED_EDGE('',*,*,#2214,.T.);
#3046=ORIENTED_EDGE('',*,*,#2116,.F.);
#3047=ORIENTED_EDGE('',*,*,#2208,.F.);
#3048=ORIENTED_EDGE('',*,*,#2128,.T.);
#3049=ORIENTED_EDGE('',*,*,#2215,.T.);
#3050=ORIENTED_EDGE('',*,*,#2156,.T.);
#3051=ORIENTED_EDGE('',*,*,#2211,.F.);
#3052=ORIENTED_EDGE('',*,*,#2132,.T.);
#3053=ORIENTED_EDGE('',*,*,#2216,.T.);
#3054=ORIENTED_EDGE('',*,*,#2152,.T.);
#3055=ORIENTED_EDGE('',*,*,#2212,.F.);
#3056=ORIENTED_EDGE('',*,*,#2136,.T.);
#3057=ORIENTED_EDGE('',*,*,#2217,.T.);
#3058=ORIENTED_EDGE('',*,*,#2148,.T.);
#3059=ORIENTED_EDGE('',*,*,#2213,.F.);
#3060=ORIENTED_EDGE('',*,*,#2127,.T.);
#3061=ORIENTED_EDGE('',*,*,#2160,.T.);
#3062=ORIENTED_EDGE('',*,*,#2201,.T.);
#3063=ORIENTED_EDGE('',*,*,#2200,.T.);
#3064=ORIENTED_EDGE('',*,*,#2199,.T.);
#3065=ORIENTED_EDGE('',*,*,#2198,.T.);
#3066=ORIENTED_EDGE('',*,*,#2197,.T.);
#3067=ORIENTED_EDGE('',*,*,#2196,.T.);
#3068=ORIENTED_EDGE('',*,*,#2195,.T.);
#3069=ORIENTED_EDGE('',*,*,#2194,.T.);
#3070=ORIENTED_EDGE('',*,*,#2193,.T.);
#3071=ORIENTED_EDGE('',*,*,#2192,.T.);
#3072=ORIENTED_EDGE('',*,*,#2191,.T.);
#3073=ORIENTED_EDGE('',*,*,#2190,.T.);
#3074=ORIENTED_EDGE('',*,*,#2189,.T.);
#3075=ORIENTED_EDGE('',*,*,#2188,.T.);
#3076=ORIENTED_EDGE('',*,*,#2187,.T.);
#3077=ORIENTED_EDGE('',*,*,#2186,.T.);
#3078=ORIENTED_EDGE('',*,*,#2185,.T.);
#3079=ORIENTED_EDGE('',*,*,#2218,.T.);
#3080=ORIENTED_EDGE('',*,*,#2065,.F.);
#3081=ORIENTED_EDGE('',*,*,#2069,.F.);
#3082=ORIENTED_EDGE('',*,*,#2072,.F.);
#3083=ORIENTED_EDGE('',*,*,#2075,.F.);
#3084=ORIENTED_EDGE('',*,*,#2080,.F.);
#3085=ORIENTED_EDGE('',*,*,#2079,.F.);
#3086=ORIENTED_EDGE('',*,*,#2083,.F.);
#3087=ORIENTED_EDGE('',*,*,#2086,.F.);
#3088=ORIENTED_EDGE('',*,*,#2091,.F.);
#3089=ORIENTED_EDGE('',*,*,#2090,.F.);
#3090=ORIENTED_EDGE('',*,*,#2096,.F.);
#3091=ORIENTED_EDGE('',*,*,#2095,.F.);
#3092=ORIENTED_EDGE('',*,*,#2099,.F.);
#3093=ORIENTED_EDGE('',*,*,#2102,.F.);
#3094=ORIENTED_EDGE('',*,*,#2107,.F.);
#3095=ORIENTED_EDGE('',*,*,#2106,.F.);
#3096=ORIENTED_EDGE('',*,*,#2110,.F.);
#3097=ORIENTED_EDGE('',*,*,#2113,.F.);
#3098=ORIENTED_EDGE('',*,*,#2118,.F.);
#3099=ORIENTED_EDGE('',*,*,#2117,.F.);
#3100=ORIENTED_EDGE('',*,*,#2214,.F.);
#3101=ORIENTED_EDGE('',*,*,#2124,.F.);
#3102=ORIENTED_EDGE('',*,*,#2157,.T.);
#3103=ORIENTED_EDGE('',*,*,#2215,.F.);
#3104=ORIENTED_EDGE('',*,*,#2131,.T.);
#3105=ORIENTED_EDGE('',*,*,#2203,.T.);
#3106=ORIENTED_EDGE('',*,*,#2153,.T.);
#3107=ORIENTED_EDGE('',*,*,#2125,.T.);
#3108=ORIENTED_EDGE('',*,*,#2216,.F.);
#3109=ORIENTED_EDGE('',*,*,#2135,.T.);
#3110=ORIENTED_EDGE('',*,*,#2205,.T.);
#3111=ORIENTED_EDGE('',*,*,#2149,.T.);
#3112=ORIENTED_EDGE('',*,*,#2217,.F.);
#3113=ORIENTED_EDGE('',*,*,#2139,.T.);
#3114=ORIENTED_EDGE('',*,*,#2207,.T.);
#3115=ORIENTED_EDGE('',*,*,#2145,.T.);
#3116=ORIENTED_EDGE('',*,*,#2219,.F.);
#3117=ORIENTED_EDGE('',*,*,#2162,.T.);
#3118=ORIENTED_EDGE('',*,*,#2161,.T.);
#3119=ORIENTED_EDGE('',*,*,#2142,.T.);
#3120=ORIENTED_EDGE('',*,*,#2220,.F.);
#3121=ORIENTED_EDGE('',*,*,#2165,.T.);
#3122=ORIENTED_EDGE('',*,*,#2221,.F.);
#3123=ORIENTED_EDGE('',*,*,#2144,.T.);
#3124=ORIENTED_EDGE('',*,*,#2222,.F.);
#3125=ORIENTED_EDGE('',*,*,#2163,.T.);
#3126=ORIENTED_EDGE('',*,*,#2219,.T.);
#3127=ORIENTED_EDGE('',*,*,#2141,.T.);
#3128=ORIENTED_EDGE('',*,*,#2166,.T.);
#3129=ORIENTED_EDGE('',*,*,#2220,.T.);
#3130=ORIENTED_EDGE('',*,*,#2143,.T.);
#3131=ORIENTED_EDGE('',*,*,#2221,.T.);
#3132=ORIENTED_EDGE('',*,*,#2164,.T.);
#3133=ORIENTED_EDGE('',*,*,#2222,.T.);
#3134=ORIENTED_EDGE('',*,*,#2218,.F.);
#3135=ORIENTED_EDGE('',*,*,#2184,.F.);
#3136=ORIENTED_EDGE('',*,*,#2210,.F.);
#3137=ORIENTED_EDGE('',*,*,#2209,.F.);
#3138=ORIENTED_EDGE('',*,*,#2066,.F.);
#3969=CYLINDRICAL_SURFACE('',#4431,3.22274999999998);
#3970=CYLINDRICAL_SURFACE('',#4433,3.22274999999998);
#3971=CYLINDRICAL_SURFACE('',#4434,3.22274999999998);
#3972=CYLINDRICAL_SURFACE('',#4435,3.22274999999998);
#3973=CYLINDRICAL_SURFACE('',#4436,3.22274999999998);
#3974=CYLINDRICAL_SURFACE('',#4437,3.22274999999998);
#3975=CYLINDRICAL_SURFACE('',#4438,3.22274999999998);
#3976=CYLINDRICAL_SURFACE('',#4439,3.22274999999998);
#3977=CYLINDRICAL_SURFACE('',#4440,3.22274999999998);
#3978=CYLINDRICAL_SURFACE('',#4441,3.22274999999998);
#3979=CYLINDRICAL_SURFACE('',#4442,3.22274999999998);
#3980=CYLINDRICAL_SURFACE('',#4443,3.22274999999998);
#3981=CYLINDRICAL_SURFACE('',#4444,3.22274999999998);
#3982=CYLINDRICAL_SURFACE('',#4445,3.22274999999998);
#3983=CYLINDRICAL_SURFACE('',#4446,3.22274999999998);
#3984=CYLINDRICAL_SURFACE('',#4447,3.22274999999998);
#3985=CYLINDRICAL_SURFACE('',#4450,5.);
#3986=CYLINDRICAL_SURFACE('',#4454,3.933);
#3987=CYLINDRICAL_SURFACE('',#4456,3.933);
#3988=CYLINDRICAL_SURFACE('',#4457,3.933);
#3989=CYLINDRICAL_SURFACE('',#4458,3.933);
#3990=CYLINDRICAL_SURFACE('',#4459,3.22274999999998);
#3991=CYLINDRICAL_SURFACE('',#4460,3.22274999999998);
#3992=CYLINDRICAL_SURFACE('',#4461,3.22274999999998);
#3993=CYLINDRICAL_SURFACE('',#4462,3.22274999999998);
#3994=CYLINDRICAL_SURFACE('',#4463,3.933);
#3995=CYLINDRICAL_SURFACE('',#4464,3.22274999999998);
#4098=ADVANCED_FACE('',(#215),#3969,.T.);
#4099=ADVANCED_FACE('',(#216),#3970,.T.);
#4100=ADVANCED_FACE('',(#217),#3971,.T.);
#4101=ADVANCED_FACE('',(#218),#3972,.T.);
#4102=ADVANCED_FACE('',(#219),#3973,.T.);
#4103=ADVANCED_FACE('',(#220),#3974,.T.);
#4104=ADVANCED_FACE('',(#221),#3975,.T.);
#4105=ADVANCED_FACE('',(#222),#3976,.T.);
#4106=ADVANCED_FACE('',(#223),#3977,.T.);
#4107=ADVANCED_FACE('',(#224),#3978,.T.);
#4108=ADVANCED_FACE('',(#225),#3979,.T.);
#4109=ADVANCED_FACE('',(#226),#3980,.T.);
#4110=ADVANCED_FACE('',(#227),#3981,.T.);
#4111=ADVANCED_FACE('',(#228),#3982,.T.);
#4112=ADVANCED_FACE('',(#229),#3983,.T.);
#4113=ADVANCED_FACE('',(#230),#3984,.T.);
#4114=ADVANCED_FACE('',(#231),#136,.T.);
#4115=ADVANCED_FACE('',(#232),#3985,.F.);
#4116=ADVANCED_FACE('',(#233),#137,.F.);
#4117=ADVANCED_FACE('',(#234),#3986,.T.);
#4118=ADVANCED_FACE('',(#235),#3987,.T.);
#4119=ADVANCED_FACE('',(#236),#3988,.T.);
#4120=ADVANCED_FACE('',(#237),#3989,.T.);
#4121=ADVANCED_FACE('',(#238),#48,.T.);
#4122=ADVANCED_FACE('',(#239),#49,.T.);
#4123=ADVANCED_FACE('',(#240),#50,.T.);
#4124=ADVANCED_FACE('',(#241),#51,.T.);
#4125=ADVANCED_FACE('',(#242),#3990,.T.);
#4126=ADVANCED_FACE('',(#243),#3991,.T.);
#4127=ADVANCED_FACE('',(#244),#3992,.T.);
#4128=ADVANCED_FACE('',(#245),#3993,.T.);
#4129=ADVANCED_FACE('',(#246),#52,.T.);
#4130=ADVANCED_FACE('',(#247),#53,.T.);
#4131=ADVANCED_FACE('',(#248),#54,.T.);
#4132=ADVANCED_FACE('',(#249),#55,.T.);
#4133=ADVANCED_FACE('',(#250),#3994,.T.);
#4134=ADVANCED_FACE('',(#251),#3995,.T.);
#4135=ADVANCED_FACE('',(#252),#56,.T.);
#4136=ADVANCED_FACE('',(#253),#57,.T.);
#4137=ADVANCED_FACE('',(#254),#138,.T.);
#4260=CLOSED_SHELL('',(#4098,#4099,#4100,#4101,#4102,#4103,#4104,#4105,
#4106,#4107,#4108,#4109,#4110,#4111,#4112,#4113,#4114,#4115,#4116,#4117,
#4118,#4119,#4120,#4121,#4122,#4123,#4124,#4125,#4126,#4127,#4128,#4129,
#4130,#4131,#4132,#4133,#4134,#4135,#4136,#4137));
#4430=AXIS2_PLACEMENT_3D('',#5726,#4875,#4876);
#4431=AXIS2_PLACEMENT_3D('',#5727,#4877,#4878);
#4432=AXIS2_PLACEMENT_3D('',#5764,#4880,#4881);
#4433=AXIS2_PLACEMENT_3D('',#5859,#4882,#4883);
#4434=AXIS2_PLACEMENT_3D('',#6293,#4885,#4886);
#4435=AXIS2_PLACEMENT_3D('',#6703,#4888,#4889);
#4436=AXIS2_PLACEMENT_3D('',#7180,#4891,#4892);
#4437=AXIS2_PLACEMENT_3D('',#7715,#4894,#4895);
#4438=AXIS2_PLACEMENT_3D('',#8147,#4897,#4898);
#4439=AXIS2_PLACEMENT_3D('',#8596,#4900,#4901);
#4440=AXIS2_PLACEMENT_3D('',#9056,#4903,#4904);
#4441=AXIS2_PLACEMENT_3D('',#9515,#4906,#4907);
#4442=AXIS2_PLACEMENT_3D('',#9943,#4909,#4910);
#4443=AXIS2_PLACEMENT_3D('',#10386,#4912,#4913);
#4444=AXIS2_PLACEMENT_3D('',#10837,#4915,#4916);
#4445=AXIS2_PLACEMENT_3D('',#11293,#4918,#4919);
#4446=AXIS2_PLACEMENT_3D('',#11750,#4921,#4922);
#4447=AXIS2_PLACEMENT_3D('',#12289,#4924,#4925);
#4448=AXIS2_PLACEMENT_3D('',#12746,#4927,#4928);
#4449=AXIS2_PLACEMENT_3D('',#12758,#4929,#4930);
#4450=AXIS2_PLACEMENT_3D('',#12881,#4944,#4945);
#4451=AXIS2_PLACEMENT_3D('',#12982,#4946,#4947);
#4452=AXIS2_PLACEMENT_3D('',#12994,#4948,#4949);
#4453=AXIS2_PLACEMENT_3D('',#13085,#4950,#4951);
#4454=AXIS2_PLACEMENT_3D('',#13090,#4952,#4953);
#4455=AXIS2_PLACEMENT_3D('',#15199,#4954,#4955);
#4456=AXIS2_PLACEMENT_3D('',#17487,#4956,#4957);
#4457=AXIS2_PLACEMENT_3D('',#17805,#4958,#4959);
#4458=AXIS2_PLACEMENT_3D('',#17822,#4960,#4961);
#4459=AXIS2_PLACEMENT_3D('',#20880,#4962,#4963);
#4460=AXIS2_PLACEMENT_3D('',#21087,#4964,#4965);
#4461=AXIS2_PLACEMENT_3D('',#21258,#4966,#4967);
#4462=AXIS2_PLACEMENT_3D('',#21411,#4968,#4969);
#4463=AXIS2_PLACEMENT_3D('',#23902,#4970,#4971);
#4464=AXIS2_PLACEMENT_3D('',#23944,#4972,#4973);
#4465=AXIS2_PLACEMENT_3D('',#25099,#4974,#4975);
#4875=DIRECTION('axis',(0.,0.,1.));
#4876=DIRECTION('refdir',(1.,0.,0.));
#4877=DIRECTION('center_axis',(0.,-2.22044604925031E-16,-1.));
#4878=DIRECTION('ref_axis',(-1.,1.08690987399046E-13,-2.41342473559327E-29));
#4879=DIRECTION('',(0.,2.22044604925031E-16,1.));
#4880=DIRECTION('center_axis',(0.,-2.22044604925031E-16,-1.));
#4881=DIRECTION('ref_axis',(-1.,1.08690987399046E-13,-2.41342473559327E-29));
#4882=DIRECTION('center_axis',(0.,-2.22044604925031E-16,-1.));
#4883=DIRECTION('ref_axis',(-1.,1.08690987399046E-13,-2.41342473559327E-29));
#4884=DIRECTION('',(0.,2.22044604925031E-16,1.));
#4885=DIRECTION('center_axis',(0.,-2.22044604925031E-16,-1.));
#4886=DIRECTION('ref_axis',(-1.,1.08690987399046E-13,-2.41342473559327E-29));
#4887=DIRECTION('',(0.,2.22044604925031E-16,1.));
#4888=DIRECTION('center_axis',(0.,-2.22044604925031E-16,-1.));
#4889=DIRECTION('ref_axis',(-1.,1.08690987399046E-13,-2.41342473559327E-29));
#4890=DIRECTION('',(0.,2.22044604925031E-16,1.));
#4891=DIRECTION('center_axis',(0.,-2.22044604925031E-16,-1.));
#4892=DIRECTION('ref_axis',(-1.,1.08690987399046E-13,-2.41342473559327E-29));
#4893=DIRECTION('',(0.,2.22044604925031E-16,1.));
#4894=DIRECTION('center_axis',(0.,-2.22044604925031E-16,-1.));
#4895=DIRECTION('ref_axis',(-1.,1.08690987399046E-13,-2.41342473559327E-29));
#4896=DIRECTION('',(0.,2.22044604925031E-16,1.));
#4897=DIRECTION('center_axis',(0.,-2.22044604925031E-16,-1.));
#4898=DIRECTION('ref_axis',(-1.,1.08690987399046E-13,-2.41342473559327E-29));
#4899=DIRECTION('',(0.,2.22044604925031E-16,1.));
#4900=DIRECTION('center_axis',(0.,-2.22044604925031E-16,-1.));
#4901=DIRECTION('ref_axis',(-1.,1.08690987399046E-13,-2.41342473559327E-29));
#4902=DIRECTION('',(0.,2.22044604925031E-16,1.));
#4903=DIRECTION('center_axis',(0.,-2.22044604925031E-16,-1.));
#4904=DIRECTION('ref_axis',(-1.,1.08690987399046E-13,-2.41342473559327E-29));
#4905=DIRECTION('',(0.,2.22044604925031E-16,1.));
#4906=DIRECTION('center_axis',(0.,-2.22044604925031E-16,-1.));
#4907=DIRECTION('ref_axis',(-1.,1.08690987399046E-13,-2.41342473559327E-29));
#4908=DIRECTION('',(0.,2.22044604925031E-16,1.));
#4909=DIRECTION('center_axis',(0.,-2.22044604925031E-16,-1.));
#4910=DIRECTION('ref_axis',(-1.,1.08690987399046E-13,-2.41342473559327E-29));
#4911=DIRECTION('',(0.,2.22044604925031E-16,1.));
#4912=DIRECTION('center_axis',(0.,-2.22044604925031E-16,-1.));
#4913=DIRECTION('ref_axis',(-1.,1.08690987399046E-13,-2.41342473559327E-29));
#4914=DIRECTION('',(0.,2.22044604925031E-16,1.));
#4915=DIRECTION('center_axis',(0.,-2.22044604925031E-16,-1.));
#4916=DIRECTION('ref_axis',(-1.,1.08690987399046E-13,-2.41342473559327E-29));
#4917=DIRECTION('',(0.,2.22044604925031E-16,1.));
#4918=DIRECTION('center_axis',(0.,-2.22044604925031E-16,-1.));
#4919=DIRECTION('ref_axis',(-1.,1.08690987399046E-13,-2.41342473559327E-29));
#4920=DIRECTION('',(0.,2.22044604925031E-16,1.));
#4921=DIRECTION('center_axis',(0.,-2.22044604925031E-16,-1.));
#4922=DIRECTION('ref_axis',(-1.,1.08690987399046E-13,-2.41342473559327E-29));
#4923=DIRECTION('',(0.,2.22044604925031E-16,1.));
#4924=DIRECTION('center_axis',(0.,-2.22044604925031E-16,-1.));
#4925=DIRECTION('ref_axis',(-1.,1.08690987399046E-13,-2.41342473559327E-29));
#4926=DIRECTION('',(0.,2.22044604925031E-16,1.));
#4927=DIRECTION('center_axis',(1.,0.,0.));
#4928=DIRECTION('ref_axis',(0.,1.,0.));
#4929=DIRECTION('center_axis',(-1.,0.,0.));
#4930=DIRECTION('ref_axis',(0.,1.,0.));
#4931=DIRECTION('',(0.,2.22044604925031E-16,1.));
#4932=DIRECTION('',(0.,2.22044604925031E-16,1.));
#4933=DIRECTION('',(0.,2.22044604925031E-16,1.));
#4934=DIRECTION('',(0.,2.22044604925031E-16,1.));
#4935=DIRECTION('',(0.,2.22044604925031E-16,1.));
#4936=DIRECTION('',(0.,2.22044604925031E-16,1.));
#4937=DIRECTION('',(0.,-1.,2.22044604925031E-16));
#4938=DIRECTION('',(0.,-2.22044604925031E-16,-1.));
#4939=DIRECTION('',(0.,-2.22044604925031E-16,-1.));
#4940=DIRECTION('',(0.,-2.22044604925031E-16,-1.));
#4941=DIRECTION('',(0.,-2.22044604925031E-16,-1.));
#4942=DIRECTION('',(0.,-2.22044604925031E-16,-1.));
#4943=DIRECTION('',(0.,-2.22044604925031E-16,-1.));
#4944=DIRECTION('center_axis',(-1.,0.,0.));
#4945=DIRECTION('ref_axis',(0.,1.,0.));
#4946=DIRECTION('center_axis',(0.,2.22044604925031E-16,1.));
#4947=DIRECTION('ref_axis',(-1.,0.,0.));
#4948=DIRECTION('center_axis',(0.,2.22044604925031E-16,1.));
#4949=DIRECTION('ref_axis',(-1.,1.08690987399046E-13,-2.41342473559327E-29));
#4950=DIRECTION('center_axis',(0.,-2.22044604925031E-16,-1.));
#4951=DIRECTION('ref_axis',(-1.,0.,0.));
#4952=DIRECTION('center_axis',(0.,-2.22044604925031E-16,-1.));
#4953=DIRECTION('ref_axis',(-1.,0.,0.));
#4954=DIRECTION('center_axis',(0.,-2.22044604925031E-16,-1.));
#4955=DIRECTION('ref_axis',(-1.,0.,0.));
#4956=DIRECTION('center_axis',(0.,-2.22044604925031E-16,-1.));
#4957=DIRECTION('ref_axis',(-1.,0.,0.));
#4958=DIRECTION('center_axis',(0.,-2.22044604925031E-16,-1.));
#4959=DIRECTION('ref_axis',(-1.,0.,0.));
#4960=DIRECTION('center_axis',(0.,-2.22044604925031E-16,-1.));
#4961=DIRECTION('ref_axis',(-1.,0.,0.));
#4962=DIRECTION('center_axis',(0.,-2.22044604925031E-16,-1.));
#4963=DIRECTION('ref_axis',(-1.,1.08690987399046E-13,-2.41342473559327E-29));
#4964=DIRECTION('center_axis',(0.,-2.22044604925031E-16,-1.));
#4965=DIRECTION('ref_axis',(-1.,1.08690987399046E-13,-2.41342473559327E-29));
#4966=DIRECTION('center_axis',(0.,-2.22044604925031E-16,-1.));
#4967=DIRECTION('ref_axis',(-1.,1.08690987399046E-13,-2.41342473559327E-29));
#4968=DIRECTION('center_axis',(0.,-2.22044604925031E-16,-1.));
#4969=DIRECTION('ref_axis',(-1.,1.08690987399046E-13,-2.41342473559327E-29));
#4970=DIRECTION('center_axis',(0.,-2.22044604925031E-16,-1.));
#4971=DIRECTION('ref_axis',(-1.,0.,0.));
#4972=DIRECTION('center_axis',(0.,-2.22044604925031E-16,-1.));
#4973=DIRECTION('ref_axis',(-1.,1.08690987399046E-13,-2.41342473559327E-29));
#4974=DIRECTION('center_axis',(0.,2.22044604925031E-16,1.));
#4975=DIRECTION('ref_axis',(-1.,0.,0.));
#5726=CARTESIAN_POINT('',(0.,0.,0.));
#5727=CARTESIAN_POINT('Origin',(4.45646910621825,-5.13094777615093E-16,
-2.31077344927308));
#5728=CARTESIAN_POINT('',(7.67921910621823,-7.83531977023612E-9,24.5634577632816));
#5729=CARTESIAN_POINT('',(7.67921909177343,0.00030512938119044,24.8107734493052));
#5730=CARTESIAN_POINT('',(7.67921910621823,-3.51191647465084E-13,-2.31077344927308));
#5731=CARTESIAN_POINT('',(6.32805563795728,-2.62360084935053,25.));
#5732=CARTESIAN_POINT('Ctrl Pts',(7.67921909177343,0.00030512938123435,
24.8107734493052));
#5733=CARTESIAN_POINT('Ctrl Pts',(7.67922866593268,-0.100816307841584,24.8170649336023));
#5734=CARTESIAN_POINT('Ctrl Pts',(7.67447455962406,-0.202100590921019,24.8233564178993));
#5735=CARTESIAN_POINT('Ctrl Pts',(7.66493680196462,-0.303071951608608,24.8296479021964));
#5736=CARTESIAN_POINT('Ctrl Pts',(7.65541369343921,-0.40388822940893,24.835929723342));
#5737=CARTESIAN_POINT('Ctrl Pts',(7.64112158799093,-0.504392131358855,24.8422115444877));
#5738=CARTESIAN_POINT('Ctrl Pts',(7.62209250725414,-0.604107643813442,24.8484933656333));
#5739=CARTESIAN_POINT('Ctrl Pts',(7.60296965583703,-0.704314530053787,24.8548061420653));
#5740=CARTESIAN_POINT('Ctrl Pts',(7.57906299733081,-0.803724810365966,24.8611189184972));
#5741=CARTESIAN_POINT('Ctrl Pts',(7.55045802283427,-0.901859271925004,24.8674316949291));
#5742=CARTESIAN_POINT('Ctrl Pts',(7.52206334493677,-0.999272273532457,24.8736980614119));
#5743=CARTESIAN_POINT('Ctrl Pts',(7.48903930758529,-1.09542774532358,24.8799644278946));
#5744=CARTESIAN_POINT('Ctrl Pts',(7.45152072289721,-1.18986695723875,24.8862307943773));
#5745=CARTESIAN_POINT('Ctrl Pts',(7.41402723871525,-1.28424298787894,24.8924929685651));
#5746=CARTESIAN_POINT('Ctrl Pts',(7.37204534178874,-1.3769046584151,24.898755142753));
#5747=CARTESIAN_POINT('Ctrl Pts',(7.32575909003815,-1.46741015099755,24.9050173169408));
#5748=CARTESIAN_POINT('Ctrl Pts',(7.27949302102046,-1.55787617941703,24.91127676056));
#5749=CARTESIAN_POINT('Ctrl Pts',(7.22892652098825,-1.64618753215808,24.9175362041791));
#5750=CARTESIAN_POINT('Ctrl Pts',(7.17429069621859,-1.73192475801575,24.9237956477983));
#5751=CARTESIAN_POINT('Ctrl Pts',(7.11886128045777,-1.81890732592385,24.9301460104818));
#5752=CARTESIAN_POINT('Ctrl Pts',(7.05924358165052,-1.90324000330923,24.9364963731652));
#5753=CARTESIAN_POINT('Ctrl Pts',(6.99572561601069,-1.98451352728485,24.9428467358487));
#5754=CARTESIAN_POINT('Ctrl Pts',(6.93311093007416,-2.06463127235786,24.9491067909529));
#5755=CARTESIAN_POINT('Ctrl Pts',(6.8667064827474,-2.1417760003413,24.955366846057));
#5756=CARTESIAN_POINT('Ctrl Pts',(6.79682929633059,-2.21558835144013,24.9616269011612));
#5757=CARTESIAN_POINT('Ctrl Pts',(6.72544003706848,-2.29099792843581,24.9680224176343));
#5758=CARTESIAN_POINT('Ctrl Pts',(6.65042630261387,-2.3629288987071,24.9744179341074));
#5759=CARTESIAN_POINT('Ctrl Pts',(6.57216557829183,-2.43103805000153,24.9808134505806));
#5760=CARTESIAN_POINT('Ctrl Pts',(6.49390485396981,-2.49914720129594,24.9872089670537));
#5761=CARTESIAN_POINT('Ctrl Pts',(6.41239751072598,-2.56343426068115,24.9936044835268));
#5762=CARTESIAN_POINT('Ctrl Pts',(6.3280556379573,-2.62360084935053,25.));
#5763=CARTESIAN_POINT('',(2.62314711761431,-2.65048072028474,25.));
#5764=CARTESIAN_POINT('Origin',(4.45646910621825,5.55111512312578E-15,25.));
#5765=CARTESIAN_POINT('Ctrl Pts',(2.62314711761429,-2.65048072028473,25.));
#5766=CARTESIAN_POINT('Ctrl Pts',(2.89144904079663,-2.8360635889283,24.9786416469637));
#5767=CARTESIAN_POINT('Ctrl Pts',(3.18648460629579,-2.97991334644022,24.9559344725635));
#5768=CARTESIAN_POINT('Ctrl Pts',(3.58512066923102,-3.10405331522512,24.928741492428));
#5769=CARTESIAN_POINT('Ctrl Pts',(3.67309955673177,-3.12741584059926,24.922921141824));
#5770=CARTESIAN_POINT('Ctrl Pts',(3.78661194416149,-3.15246672202482,24.915635611859));
#5771=CARTESIAN_POINT('Ctrl Pts',(3.81133084498954,-3.15761804725921,24.9140623241602));
#5772=CARTESIAN_POINT('Ctrl Pts',(3.85142009765253,-3.1654820695268,24.9115315157959));
#5773=CARTESIAN_POINT('Ctrl Pts',(3.86675371263984,-3.16837447333492,24.9105684001871));
#5774=CARTESIAN_POINT('Ctrl Pts',(3.89619116696891,-3.17370619888223,24.9087285488888));
#5775=CARTESIAN_POINT('Ctrl Pts',(3.91029139758291,-3.17616314550513,24.9078512832115));
#5776=CARTESIAN_POINT('Ctrl Pts',(3.94254820011921,-3.18156269199861,24.9058532878385));
#5777=CARTESIAN_POINT('Ctrl Pts',(3.96071463471363,-3.18444396812544,24.9047344846621));
#5778=CARTESIAN_POINT('Ctrl Pts',(4.01828094934606,-3.19306967907415,24.9012087320305));
#5779=CARTESIAN_POINT('Ctrl Pts',(4.05776401829735,-3.19823971799934,24.8988194688504));
#5780=CARTESIAN_POINT('Ctrl Pts',(4.33720985013774,-3.22957562514283,24.8820913837109));
#5781=CARTESIAN_POINT('Ctrl Pts',(4.5793490161818,-3.22944192584949,24.8686180366021));
#5782=CARTESIAN_POINT('Ctrl Pts',(4.99722054928059,-3.18210555296314,24.8449564574255));
#5783=CARTESIAN_POINT('Ctrl Pts',(5.17320613386012,-3.14713821540364,24.8348323999712));
#5784=CARTESIAN_POINT('Ctrl Pts',(5.3643396599289,-3.09229347408763,24.8228055157499));
#5785=CARTESIAN_POINT('Ctrl Pts',(5.38327855959523,-3.08667006112428,24.8216021234757));
#5786=CARTESIAN_POINT('Ctrl Pts',(5.41157107911454,-3.07798547988199,24.8197851945844));
#5787=CARTESIAN_POINT('Ctrl Pts',(5.4209647098772,-3.07505489670163,24.8191787521801));
#5788=CARTESIAN_POINT('Ctrl Pts',(5.43040894855634,-3.07206099395158,24.8185656896257));
#5789=CARTESIAN_POINT('Ctrl Pts',(5.43047326528825,-3.07204060278614,24.8185615144177));
#5790=CARTESIAN_POINT('Ctrl Pts',(5.43060308003227,-3.07199944145218,24.8185530870008));
#5791=CARTESIAN_POINT('Ctrl Pts',(5.43066857802779,-3.07197867120643,24.818548834787));
#5792=CARTESIAN_POINT('Ctrl Pts',(5.43080079736073,-3.07193673812383,24.8185402506102));
#5793=CARTESIAN_POINT('Ctrl Pts',(5.4308675186954,-3.07191557520083,24.8185359186411));
#5794=CARTESIAN_POINT('Ctrl Pts',(5.4310022287794,-3.07187284252112,24.8185271720733));
#5795=CARTESIAN_POINT('Ctrl Pts',(5.4310702175018,-3.07185127268109,24.8185227574699));
#5796=CARTESIAN_POINT('Ctrl Pts',(5.43120750855455,-3.07180771123408,24.8185138426144));
#5797=CARTESIAN_POINT('Ctrl Pts',(5.43127681082203,-3.07178571955001,24.8185093423595));
#5798=CARTESIAN_POINT('Ctrl Pts',(5.4314167773327,-3.07174129877255,24.8185002530393));
#5799=CARTESIAN_POINT('Ctrl Pts',(5.43148744156385,-3.07171886958039,24.8184956639675));
#5800=CARTESIAN_POINT('Ctrl Pts',(5.43163018276345,-3.07167355736409,24.8184863936949));
#5801=CARTESIAN_POINT('Ctrl Pts',(5.43170225968432,-3.07165067424653,24.8184817124895));
#5802=CARTESIAN_POINT('Ctrl Pts',(5.43184787952696,-3.07160443694051,24.818472254467));
#5803=CARTESIAN_POINT('Ctrl Pts',(5.43192142242619,-3.07158108264431,24.8184674776432));
#5804=CARTESIAN_POINT('Ctrl Pts',(5.43207003015147,-3.07153388487311,24.8184578247266));
#5805=CARTESIAN_POINT('Ctrl Pts',(5.43214509496395,-3.0715100412807,24.8184529486261));
#5806=CARTESIAN_POINT('Ctrl Pts',(5.43229680530598,-3.07146184587413,24.8184430933109));
#5807=CARTESIAN_POINT('Ctrl Pts',(5.4323734508071,-3.07143749393993,24.818438114089));
#5808=CARTESIAN_POINT('Ctrl Pts',(5.43252838438359,-3.07138826180528,24.8184280484846));
#5809=CARTESIAN_POINT('Ctrl Pts',(5.43260667236773,-3.07136338149683,24.8184229620984));
#5810=CARTESIAN_POINT('Ctrl Pts',(5.44012829660415,-3.06897265549072,24.8179342582337));
#5811=CARTESIAN_POINT('Ctrl Pts',(5.44756277903329,-3.06657983646212,24.8174490996786));
#5812=CARTESIAN_POINT('Ctrl Pts',(5.46410833260847,-3.06118812759831,24.816364558583));
#5813=CARTESIAN_POINT('Ctrl Pts',(5.47321457565503,-3.05817563393195,24.8157644199452));
#5814=CARTESIAN_POINT('Ctrl Pts',(5.49964614648011,-3.04930053683947,24.8140133288337));
#5815=CARTESIAN_POINT('Ctrl Pts',(5.51693485844124,-3.04333114430815,24.8128564985214));
#5816=CARTESIAN_POINT('Ctrl Pts',(5.65146370021255,-2.99559595550017,24.8037702655541));
#5817=CARTESIAN_POINT('Ctrl Pts',(5.76623462366233,-2.94722153919545,24.7955186803279));
#5818=CARTESIAN_POINT('Ctrl Pts',(6.0362565760378,-2.81451939040535,24.7753119021079));
#5819=CARTESIAN_POINT('Ctrl Pts',(6.18795618391751,-2.723821825785,24.7632960451225));
#5820=CARTESIAN_POINT('Ctrl Pts',(6.41266011586314,-2.56308392031462,24.7449139354335));
#5821=CARTESIAN_POINT('Ctrl Pts',(6.49111351955375,-2.50126119380454,24.7383650553318));
#5822=CARTESIAN_POINT('Ctrl Pts',(6.59873347582763,-2.40803467484539,24.7292122340131));
#5823=CARTESIAN_POINT('Ctrl Pts',(6.63033702006829,-2.37954327292256,24.7265016329432));
#5824=CARTESIAN_POINT('Ctrl Pts',(6.68572408421306,-2.32758566401385,24.7217089657711));
#5825=CARTESIAN_POINT('Ctrl Pts',(6.70972391047598,-2.30436015006208,24.7196174031608));
#5826=CARTESIAN_POINT('Ctrl Pts',(6.74555005361194,-2.26859487589108,24.7164713455871));
#5827=CARTESIAN_POINT('Ctrl Pts',(6.75764337791683,-2.25632694533578,24.7154051197527));
#5828=CARTESIAN_POINT('Ctrl Pts',(6.77939841895775,-2.23390095371312,24.7134790340792));
#5829=CARTESIAN_POINT('Ctrl Pts',(6.78909325922473,-2.22377576063541,24.7126177472709));
#5830=CARTESIAN_POINT('Ctrl Pts',(6.80983816047952,-2.20182505765355,24.710768189018));
#5831=CARTESIAN_POINT('Ctrl Pts',(6.82086586360541,-2.18997887628746,24.7097808865825));
#5832=CARTESIAN_POINT('Ctrl Pts',(6.85051913469938,-2.15763965010232,24.7071144303846));
#5833=CARTESIAN_POINT('Ctrl Pts',(6.86897082773634,-2.13698851527668,24.7054425923759));
#5834=CARTESIAN_POINT('Ctrl Pts',(6.96326059272684,-2.0286814509089,24.6968282102518));
#5835=CARTESIAN_POINT('Ctrl Pts',(7.03460001662489,-1.93721377370374,24.6900709408979));
#5836=CARTESIAN_POINT('Ctrl Pts',(7.1142092148304,-1.82293180691672,24.6821034185282));
#5837=CARTESIAN_POINT('Ctrl Pts',(7.12734823766184,-1.80362622181835,24.6807727284219));
#5838=CARTESIAN_POINT('Ctrl Pts',(7.25999626248985,-1.6040937323485,24.6671638089495));
#5839=CARTESIAN_POINT('Ctrl Pts',(7.36128014951148,-1.41242599409194,24.6553304067686));
#5840=CARTESIAN_POINT('Ctrl Pts',(7.46904534215338,-1.14692822079476,24.6389675339684));
#5841=CARTESIAN_POINT('Ctrl Pts',(7.49334556596313,-1.08094406249499,24.6348992717646));
#5842=CARTESIAN_POINT('Ctrl Pts',(7.52851055709442,-0.974882875378807,24.6282812163858));
#5843=CARTESIAN_POINT('Ctrl Pts',(7.54079298548282,-0.935297352539703,24.6257940318784));
#5844=CARTESIAN_POINT('Ctrl Pts',(7.55595310793775,-0.882886501311716,24.6224653033926));
#5845=CARTESIAN_POINT('Ctrl Pts',(7.55952115770807,-0.870262950628422,24.6216608497017));
#5846=CARTESIAN_POINT('Ctrl Pts',(7.56524483441555,-0.849530127301381,24.6203346659984));
#5847=CARTESIAN_POINT('Ctrl Pts',(7.56744607541187,-0.84143345476036,24.6198155245752));
#5848=CARTESIAN_POINT('Ctrl Pts',(7.57167915405762,-0.825619527948426,24.6187989987597));
#5849=CARTESIAN_POINT('Ctrl Pts',(7.57371397129826,-0.817903229437207,24.6183017863248));
#5850=CARTESIAN_POINT('Ctrl Pts',(7.57819466377029,-0.800652234048019,24.6171876034298));
#5851=CARTESIAN_POINT('Ctrl Pts',(7.58062555277428,-0.791113739003178,24.6165697888871));
#5852=CARTESIAN_POINT('Ctrl Pts',(7.58888124715934,-0.758087941053018,24.6144249827482));
#5853=CARTESIAN_POINT('Ctrl Pts',(7.59448502020283,-0.734546927917138,24.6128861970076));
#5854=CARTESIAN_POINT('Ctrl Pts',(7.65056119171044,-0.486613497735651,24.5965914733977));
#5855=CARTESIAN_POINT('Ctrl Pts',(7.67713536569223,-0.257511450764323,24.580829062891));
#5856=CARTESIAN_POINT('Ctrl Pts',(7.6791798551556,-0.0183668891246562,24.5646956232636));
#5857=CARTESIAN_POINT('Ctrl Pts',(7.67921910619591,-0.00918318951676182,
24.5640764582002));
#5858=CARTESIAN_POINT('Ctrl Pts',(7.67921910621823,-7.83531977023612E-9,
24.5634577632816));
#5859=CARTESIAN_POINT('Origin',(4.45646910621825,-5.13094777615093E-16,
-2.31077344927308));
#5860=CARTESIAN_POINT('',(7.67921904725112,0.000460467671602397,23.3113459957337));
#5861=CARTESIAN_POINT('',(7.67921772993528,-0.00297839383558276,23.5607734493065));
#5862=CARTESIAN_POINT('',(7.67921910621823,-3.51191647465084E-13,-2.31077344927308));
#5863=CARTESIAN_POINT('Ctrl Pts',(7.67921772993528,-0.00297839383558212,
23.5607734493065));
#5864=CARTESIAN_POINT('Ctrl Pts',(7.67909389703478,-0.136970851418603,23.5690424041084));
#5865=CARTESIAN_POINT('Ctrl Pts',(7.67060927382305,-0.27059027499549,23.5773113589104));
#5866=CARTESIAN_POINT('Ctrl Pts',(7.65392828640833,-0.402954530335666,23.5855803137124));
#5867=CARTESIAN_POINT('Ctrl Pts',(7.63724729899361,-0.535318785675873,23.5938492685144));
#5868=CARTESIAN_POINT('Ctrl Pts',(7.61237013154434,-0.666428332467331,23.6021182233164));
#5869=CARTESIAN_POINT('Ctrl Pts',(7.57951436673159,-0.79542810063828,23.6103871781184));
#5870=CARTESIAN_POINT('Ctrl Pts',(7.55497886149549,-0.891760494830071,23.6165621366073));
#5871=CARTESIAN_POINT('Ctrl Pts',(7.52593914343194,-0.987124984549361,23.6227370950963));
#5872=CARTESIAN_POINT('Ctrl Pts',(7.49248746935389,-1.08106894377883,23.6289120535852));
#5873=CARTESIAN_POINT('Ctrl Pts',(7.45908096997117,-1.17488603671971,23.6350786731233));
#5874=CARTESIAN_POINT('Ctrl Pts',(7.42127450157948,-1.26728600695842,23.6412452926613));
#5875=CARTESIAN_POINT('Ctrl Pts',(7.3792108548205,-1.3578284992875,23.6474119121993));
#5876=CARTESIAN_POINT('Ctrl Pts',(7.33719161516261,-1.44827540481132,23.6535720215624));
#5877=CARTESIAN_POINT('Ctrl Pts',(7.29092431440421,-1.53686833969911,23.6597321309256));
#5878=CARTESIAN_POINT('Ctrl Pts',(7.24060053819386,-1.623185057837,23.6658922402887));
#5879=CARTESIAN_POINT('Ctrl Pts',(7.19031343251127,-1.70943887768212,23.6720478608301));
#5880=CARTESIAN_POINT('Ctrl Pts',(7.13597594635355,-1.79341940481737,23.6782034813714));
#5881=CARTESIAN_POINT('Ctrl Pts',(7.07782606176562,-1.87472805337289,23.6843591019128));
#5882=CARTESIAN_POINT('Ctrl Pts',(7.01969813170893,-1.95600600378896,23.6905123983952));
#5883=CARTESIAN_POINT('Ctrl Pts',(6.95776091550689,-2.03461372753706,23.6966656948775));
#5884=CARTESIAN_POINT('Ctrl Pts',(6.89229577913865,-2.11018150451315,23.7028189913599));
#5885=CARTESIAN_POINT('Ctrl Pts',(6.82683788981856,-2.1857409160699,23.7089716066669));
#5886=CARTESIAN_POINT('Ctrl Pts',(6.75785314097224,-2.25826072196952,23.7151242219739));
#5887=CARTESIAN_POINT('Ctrl Pts',(6.68566260354822,-2.3274049742066,23.7212768372809));
#5888=CARTESIAN_POINT('Ctrl Pts',(6.61346079385243,-2.39656002304986,23.7274304132949));
#5889=CARTESIAN_POINT('Ctrl Pts',(6.53805251472234,-2.46233817112081,23.7335839893089));
#5890=CARTESIAN_POINT('Ctrl Pts',(6.45979429750234,-2.52444166905603,23.7397375653229));
#5891=CARTESIAN_POINT('Ctrl Pts',(6.3814529974721,-2.58661109914914,23.7458976742788));
#5892=CARTESIAN_POINT('Ctrl Pts',(6.3002560581271,-2.6450978186819,23.7520577832347));
#5893=CARTESIAN_POINT('Ctrl Pts',(6.21659147482746,-2.69964568231117,23.7582178921907));
#5894=CARTESIAN_POINT('Ctrl Pts',(6.13288026769513,-2.75422394387428,23.7643814339957));
#5895=CARTESIAN_POINT('Ctrl Pts',(6.04669905209313,-2.80485875824551,23.7705449758007));
#5896=CARTESIAN_POINT('Ctrl Pts',(5.9584612529553,-2.85133953671605,23.7767085176057));
#5897=CARTESIAN_POINT('Ctrl Pts',(5.87007756186255,-2.89789716628332,23.7828822501812));
#5898=CARTESIAN_POINT('Ctrl Pts',(5.7796308883881,-2.94028685690416,23.7890559827568));
#5899=CARTESIAN_POINT('Ctrl Pts',(5.6875556021465,-2.97834578282021,23.7952297153323));
#5900=CARTESIAN_POINT('Ctrl Pts',(5.6195795009656,-3.00644341362332,23.7997875753982));
#5901=CARTESIAN_POINT('Ctrl Pts',(5.55071616800071,-3.03218162616531,23.8043454354641));
#5902=CARTESIAN_POINT('Ctrl Pts',(5.48114496854143,-3.05551254942147,23.8089032955301));
#5903=CARTESIAN_POINT('Ctrl Pts',(5.38688697092628,-3.08712226904296,23.8150784767338));
#5904=CARTESIAN_POINT('Ctrl Pts',(5.2910007126141,-3.11442140077743,23.8212536579376));
#5905=CARTESIAN_POINT('Ctrl Pts',(5.19391666630963,-3.13724220592148,23.8274288391413));
#5906=CARTESIAN_POINT('Ctrl Pts',(5.09696332521211,-3.16003228719099,23.8335957066379));
#5907=CARTESIAN_POINT('Ctrl Pts',(4.9988158201432,-3.17835592755096,23.8397625741344));
#5908=CARTESIAN_POINT('Ctrl Pts',(4.89992168927485,-3.19209451130136,23.8459294416309));
#5909=CARTESIAN_POINT('Ctrl Pts',(4.8011315641874,-3.20581864634668,23.8520898235063));
#5910=CARTESIAN_POINT('Ctrl Pts',(4.70159680186188,-3.21496725239346,23.8582502053816));
#5911=CARTESIAN_POINT('Ctrl Pts',(4.6017761575287,-3.21947253806261,23.864410587257));
#5912=CARTESIAN_POINT('Ctrl Pts',(4.502027676094,-3.22397456674545,23.8705665156346));
#5913=CARTESIAN_POINT('Ctrl Pts',(4.40199415571737,-3.22383992953218,23.8767224440122));
#5914=CARTESIAN_POINT('Ctrl Pts',(4.30213960679824,-3.21905265072018,23.8828783723899));
#5915=CARTESIAN_POINT('Ctrl Pts',(4.2023224068897,-3.21426716251391,23.8890319982401));
#5916=CARTESIAN_POINT('Ctrl Pts',(4.10268447833616,-3.20483251145545,23.8951856240904));
#5917=CARTESIAN_POINT('Ctrl Pts',(4.00368907718172,-3.19078482630928,23.9013392499406));
#5918=CARTESIAN_POINT('Ctrl Pts',(3.90470429658175,-3.17673864824528,23.9074922156095));
#5919=CARTESIAN_POINT('Ctrl Pts',(3.80636233590325,-3.15808048105445,23.9136451812784));
#5920=CARTESIAN_POINT('Ctrl Pts',(3.70911958060973,-3.1348981241936,23.9197981469472));
#5921=CARTESIAN_POINT('Ctrl Pts',(3.61186131853573,-3.11171207056667,23.9259520937965));
#5922=CARTESIAN_POINT('Ctrl Pts',(3.51570303210624,-3.08400049486412,23.9321060406459));
#5923=CARTESIAN_POINT('Ctrl Pts',(3.4210882167591,-3.05190169832559,23.9382599874952));
#5924=CARTESIAN_POINT('Ctrl Pts',(3.32637251284984,-3.01976867457416,23.944420496349));
#5925=CARTESIAN_POINT('Ctrl Pts',(3.23320397815096,-2.98323922807735,23.9505810052029));
#5926=CARTESIAN_POINT('Ctrl Pts',(3.14200819326913,-2.94250064924866,23.9567415140567));
#5927=CARTESIAN_POINT('Ctrl Pts',(3.05076134279166,-2.9017392586223,23.9629054725224));
#5928=CARTESIAN_POINT('Ctrl Pts',(2.96148982956291,-2.85676423698174,23.969069430988));
#5929=CARTESIAN_POINT('Ctrl Pts',(2.87459472566633,-2.80780893343071,23.9752333894537));
#5930=CARTESIAN_POINT('Ctrl Pts',(2.78755563881885,-2.75877251220157,23.9814075614398));
#5931=CARTESIAN_POINT('Ctrl Pts',(2.70290119425992,-2.7057428660593,23.987581733426));
#5932=CARTESIAN_POINT('Ctrl Pts',(2.62100367301257,-2.64899683012399,23.9937559054122));
#5933=CARTESIAN_POINT('Ctrl Pts',(2.56059031444356,-2.60713697204629,23.998310407922));
#5934=CARTESIAN_POINT('Ctrl Pts',(2.50167653506242,-2.56325571668601,24.0028649104318));
#5935=CARTESIAN_POINT('Ctrl Pts',(2.44439945696367,-2.51747756475572,24.0074194129417));
#5936=CARTESIAN_POINT('Ctrl Pts',(2.36686852340884,-2.45551171430765,24.0135844416614));
#5937=CARTESIAN_POINT('Ctrl Pts',(2.29206481509825,-2.38985060767553,24.0197494703812));
#5938=CARTESIAN_POINT('Ctrl Pts',(2.22036215039852,-2.32076350467566,24.025914499101));
#5939=CARTESIAN_POINT('Ctrl Pts',(2.1487566290135,-2.25177000140764,24.032071175393));
#5940=CARTESIAN_POINT('Ctrl Pts',(2.08024411192564,-2.17936002632762,24.0382278516851));
#5941=CARTESIAN_POINT('Ctrl Pts',(2.01516648640477,-2.10384388227637,24.0443845279771));
#5942=CARTESIAN_POINT('Ctrl Pts',(1.95015768402078,-2.02840760066442,24.0505346932483));
#5943=CARTESIAN_POINT('Ctrl Pts',(1.88857683437181,-1.94987200854449,24.0566848585195));
#5944=CARTESIAN_POINT('Ctrl Pts',(1.83072926894333,-1.86858445606488,24.0628350237907));
#5945=CARTESIAN_POINT('Ctrl Pts',(1.7729235628409,-1.78735572442136,24.0689807387144));
#5946=CARTESIAN_POINT('Ctrl Pts',(1.718846022187,-1.7033793449688,24.075126453638));
#5947=CARTESIAN_POINT('Ctrl Pts',(1.66876133744719,-1.61703523722687,24.0812721685616));
#5948=CARTESIAN_POINT('Ctrl Pts',(1.61869537709102,-1.53072340961621,24.0874155858822));
#5949=CARTESIAN_POINT('Ctrl Pts',(1.57261952503715,-1.44204598873221,24.0935590032028));
#5950=CARTESIAN_POINT('Ctrl Pts',(1.53075430939148,-1.35141055572641,24.0997024205234));
#5951=CARTESIAN_POINT('Ctrl Pts',(1.48889347922091,-1.26078461698518,24.1058451943072));
#5952=CARTESIAN_POINT('Ctrl Pts',(1.45124259119734,-1.16820146922694,24.1119879680911));
#5953=CARTESIAN_POINT('Ctrl Pts',(1.41797504454764,-1.0740909643472,24.118130741875));
#5954=CARTESIAN_POINT('Ctrl Pts',(1.38470203039162,-0.979964992448368,24.1242745252209));
#5955=CARTESIAN_POINT('Ctrl Pts',(1.35581393362782,-0.884311575459887,24.1304183085669));
#5956=CARTESIAN_POINT('Ctrl Pts',(1.33143473289778,-0.78757712515373,24.1365620919129));
#5957=CARTESIAN_POINT('Ctrl Pts',(1.30702907208843,-0.690737683660381,24.1427125434428));
#5958=CARTESIAN_POINT('Ctrl Pts',(1.28714218588264,-0.592815289057748,24.1488629949727));
#5959=CARTESIAN_POINT('Ctrl Pts',(1.27184717551692,-0.494267863608402,24.1550134465026));
#5960=CARTESIAN_POINT('Ctrl Pts',(1.25654347924464,-0.395664473912563,24.1611673908217));
#5961=CARTESIAN_POINT('Ctrl Pts',(1.24583689809394,-0.296435779492924,24.1673213351408));
#5962=CARTESIAN_POINT('Ctrl Pts',(1.23974853920379,-0.197044046461753,24.1734752794599));
#5963=CARTESIAN_POINT('Ctrl Pts',(1.23364990326623,-0.097484541856869,24.1796396115336));
#5964=CARTESIAN_POINT('Ctrl Pts',(1.23218506639979,0.00223811550083505,
24.1858039436072));
#5965=CARTESIAN_POINT('Ctrl Pts',(1.23532298439493,0.101662305514315,24.1919682756808));
#5966=CARTESIAN_POINT('Ctrl Pts',(1.23769296810425,0.176754679186507,24.1966240272384));
#5967=CARTESIAN_POINT('Ctrl Pts',(1.24268744706056,0.251676815485055,24.2012797787959));
#5968=CARTESIAN_POINT('Ctrl Pts',(1.25027362877931,0.326233233975295,24.2059355303534));
#5969=CARTESIAN_POINT('Ctrl Pts',(1.26035222960196,0.425284958358905,24.2121209162587));
#5970=CARTESIAN_POINT('Ctrl Pts',(1.27504260668428,0.524039787490354,24.218306302164));
#5971=CARTESIAN_POINT('Ctrl Pts',(1.29431956327251,0.62203523256157,24.2244916880692));
#5972=CARTESIAN_POINT('Ctrl Pts',(1.31357045045947,0.719898152430063,24.2306687091008));
#5973=CARTESIAN_POINT('Ctrl Pts',(1.33739550453645,0.817003309036331,24.2368457301323));
#5974=CARTESIAN_POINT('Ctrl Pts',(1.36571774450379,0.912892974318512,24.2430227511639));
#5975=CARTESIAN_POINT('Ctrl Pts',(1.39400995495996,1.00868096968411,24.2491932228222));
#5976=CARTESIAN_POINT('Ctrl Pts',(1.42678974872925,1.10325562373446,24.2553636944804));
#5977=CARTESIAN_POINT('Ctrl Pts',(1.46392922433137,1.19616997864699,24.2615341661387));
#5978=CARTESIAN_POINT('Ctrl Pts',(1.50104107533489,1.28901522322026,24.2677000481575));
#5979=CARTESIAN_POINT('Ctrl Pts',(1.54250599988026,1.38020222406898,24.2738659301763));
#5980=CARTESIAN_POINT('Ctrl Pts',(1.58814673392486,1.46930062652308,24.2800318121951));
#5981=CARTESIAN_POINT('Ctrl Pts',(1.63376978006936,1.55836449921611,24.2861953046488));
#5982=CARTESIAN_POINT('Ctrl Pts',(1.68356522275971,1.64534099769534,24.2923587971025));
#5983=CARTESIAN_POINT('Ctrl Pts',(1.73730863917843,1.72982193216171,24.2985222895562));
#5984=CARTESIAN_POINT('Ctrl Pts',(1.79104544092444,1.81429246881996,24.304685023415));
#5985=CARTESIAN_POINT('Ctrl Pts',(1.84872901811546,1.89626768742934,24.3108477572737));
#5986=CARTESIAN_POINT('Ctrl Pts',(1.91009069429663,1.97536693953287,24.3170104911324));
#5987=CARTESIAN_POINT('Ctrl Pts',(1.97146104600473,2.05447737496341,24.3231740962999));
#5988=CARTESIAN_POINT('Ctrl Pts',(2.036510264532,2.130710694613,24.3293377014673));
#5989=CARTESIAN_POINT('Ctrl Pts',(2.10492895072005,2.20371877960402,24.3355013066348));
#5990=CARTESIAN_POINT('Ctrl Pts',(2.17341794194965,2.2768018855686,24.3416712453427));
#5991=CARTESIAN_POINT('Ctrl Pts',(2.24528301873515,2.34665282264687,24.3478411840506));
#5992=CARTESIAN_POINT('Ctrl Pts',(2.32017750797366,2.41295996024995,24.3540111227586));
#5993=CARTESIAN_POINT('Ctrl Pts',(2.39511249935403,2.47930295604664,24.3601843981036));
#5994=CARTESIAN_POINT('Ctrl Pts',(2.47307982966312,2.54209806376006,24.3663576734486));
#5995=CARTESIAN_POINT('Ctrl Pts',(2.55370089840971,2.60107491431004,24.3725309487937));
#5996=CARTESIAN_POINT('Ctrl Pts',(2.6344517129546,2.66014667799717,24.3787141589678));
#5997=CARTESIAN_POINT('Ctrl Pts',(2.71786443605039,2.71538767138475,24.3848973691419));
#5998=CARTESIAN_POINT('Ctrl Pts',(2.80353265476014,2.76657164193175,24.391080579316));
#5999=CARTESIAN_POINT('Ctrl Pts',(2.86528459180756,2.80346641311598,24.3955376021323));
#6000=CARTESIAN_POINT('Ctrl Pts',(2.92820790224037,2.83825413743604,24.3999946249486));
#6001=CARTESIAN_POINT('Ctrl Pts',(2.99214374432667,2.87086551357269,24.404451647765));
#6002=CARTESIAN_POINT('Ctrl Pts',(3.08081877140353,2.91609545921145,24.4106332605509));
#6003=CARTESIAN_POINT('Ctrl Pts',(3.17174214636608,2.9572900072321,24.4168148733368));
#6004=CARTESIAN_POINT('Ctrl Pts',(3.26451146915699,2.99422019129376,24.4229964861227));
#6005=CARTESIAN_POINT('Ctrl Pts',(3.35715775456585,3.03110139587569,24.4291699004069));
#6006=CARTESIAN_POINT('Ctrl Pts',(3.45164472248631,3.06372932025985,24.4353433146911));
#6007=CARTESIAN_POINT('Ctrl Pts',(3.54754596933506,3.0919211331692,24.4415167289753));
#6008=CARTESIAN_POINT('Ctrl Pts',(3.64334809226331,3.12008380690557,24.4476837623933));
#6009=CARTESIAN_POINT('Ctrl Pts',(3.740561174617,3.14381936444606,24.4538507958112));
#6010=CARTESIAN_POINT('Ctrl Pts',(3.83874033576257,3.16299363398841,24.4600178292292));
#6011=CARTESIAN_POINT('Ctrl Pts',(3.9368506262569,3.18215445317719,24.4661805366007));
#6012=CARTESIAN_POINT('Ctrl Pts',(4.03592522462356,3.19676026336572,24.4723432439723));
#6013=CARTESIAN_POINT('Ctrl Pts',(4.135506506055,3.20672739280974,24.4785059513438));
#6014=CARTESIAN_POINT('Ctrl Pts',(4.23505180336641,3.2166909205891,24.4846664317949));
#6015=CARTESIAN_POINT('Ctrl Pts',(4.3351029897508,3.22201905553797,24.4908269122459));
#6016=CARTESIAN_POINT('Ctrl Pts',(4.43519559393369,3.22267978554727,24.4969873926969));
#6017=CARTESIAN_POINT('Ctrl Pts',(4.53527855446147,3.223340451897,24.503147279602));
#6018=CARTESIAN_POINT('Ctrl Pts',(4.63540249211706,3.21933460465401,24.5093071665072));
#6019=CARTESIAN_POINT('Ctrl Pts',(4.73510218792276,3.21068235244157,24.5154670534124));
#6020=CARTESIAN_POINT('Ctrl Pts',(4.83481869861019,3.20202864098098,24.5216279792151));
#6021=CARTESIAN_POINT('Ctrl Pts',(4.9341103941629,3.18872700520829,24.5277889050178));
#6022=CARTESIAN_POINT('Ctrl Pts',(5.03251741807506,3.17084939801732,24.5339498308205));
#6023=CARTESIAN_POINT('Ctrl Pts',(5.13102996180132,3.15295262103835,24.5401173628564));
#6024=CARTESIAN_POINT('Ctrl Pts',(5.22865551306772,3.13047015211669,24.5462848948923));
#6025=CARTESIAN_POINT('Ctrl Pts',(5.32494475491672,3.10352502972309,24.5524524269282));
#6026=CARTESIAN_POINT('Ctrl Pts',(5.42128840259861,3.07656468266058,24.5586234437741));
#6027=CARTESIAN_POINT('Ctrl Pts',(5.51629382624657,3.04513679608577,24.56479446062));
#6028=CARTESIAN_POINT('Ctrl Pts',(5.60952918659088,3.00941356638647,24.570965477466));
#6029=CARTESIAN_POINT('Ctrl Pts',(5.70291860022974,2.97363131099987,24.5771466907167));
#6030=CARTESIAN_POINT('Ctrl Pts',(5.79453171212724,2.93353970981319,24.5833279039674));
#6031=CARTESIAN_POINT('Ctrl Pts',(5.88395876826429,2.88935820334752,24.5895091172182));
#6032=CARTESIAN_POINT('Ctrl Pts',(5.94886335455936,2.85729204213281,24.5939953332044));
#6033=CARTESIAN_POINT('Ctrl Pts',(6.01261690397324,2.82307246632287,24.5984815491906));
#6034=CARTESIAN_POINT('Ctrl Pts',(6.07507241288918,2.786797606238,24.6029677651768));
#6035=CARTESIAN_POINT('Ctrl Pts',(6.16010017957156,2.73741252566994,24.6090753597314));
#6036=CARTESIAN_POINT('Ctrl Pts',(6.24303275959794,2.68403523352434,24.615182954286));
#6037=CARTESIAN_POINT('Ctrl Pts',(6.32346502031454,2.62686958550433,24.6212905488406));
#6038=CARTESIAN_POINT('Ctrl Pts',(6.40378701967242,2.5697823035773,24.6273897707389));
#6039=CARTESIAN_POINT('Ctrl Pts',(6.48161515029577,2.50891723703554,24.6334889926373));
#6040=CARTESIAN_POINT('Ctrl Pts',(6.55656931445129,2.44452381413629,24.6395882145356));
#6041=CARTESIAN_POINT('Ctrl Pts',(6.63144399715611,2.38019867406997,24.6456809688145));
#6042=CARTESIAN_POINT('Ctrl Pts',(6.70345043414893,2.31235289968939,24.6517737230935));
#6043=CARTESIAN_POINT('Ctrl Pts',(6.77223885675924,2.24127821231083,24.6578664773724));
#6044=CARTESIAN_POINT('Ctrl Pts',(6.84098018235994,2.17025218726681,24.6639550601571));
#6045=CARTESIAN_POINT('Ctrl Pts',(6.90650756235692,2.09600195888477,24.6700436429419));
#6046=CARTESIAN_POINT('Ctrl Pts',(6.96850635226542,2.01885770597426,24.6761322257266));
#6047=CARTESIAN_POINT('Ctrl Pts',(7.03048353194658,1.94174034237636,24.6822186862819));
#6048=CARTESIAN_POINT('Ctrl Pts',(7.08893428566251,1.86173130306404,24.6883051468372));
#6049=CARTESIAN_POINT('Ctrl Pts',(7.14358343474165,1.77919480325909,24.6943916073924));
#6050=CARTESIAN_POINT('Ctrl Pts',(7.19822887921723,1.69666389850942,24.7004776553535));
#6051=CARTESIAN_POINT('Ctrl Pts',(7.24907298573405,1.61160624405079,24.7065637033145));
#6052=CARTESIAN_POINT('Ctrl Pts',(7.29588385742796,1.52441511180931,24.7126497512756));
#6053=CARTESIAN_POINT('Ctrl Pts',(7.34270469983793,1.43720540785595,24.7187370955649));
#6054=CARTESIAN_POINT('Ctrl Pts',(7.38549039142958,1.34786171514762,24.7248244398542));
#6055=CARTESIAN_POINT('Ctrl Pts',(7.42405548868829,1.25680094886909,24.7309117841435));
#6056=CARTESIAN_POINT('Ctrl Pts',(7.46266779211284,1.16562871834078,24.7370065797348));
#6057=CARTESIAN_POINT('Ctrl Pts',(7.49704901294095,1.07273562774361,24.7431013753261));
#6058=CARTESIAN_POINT('Ctrl Pts',(7.52706235794148,0.978557430594477,24.7491961709173));
#6059=CARTESIAN_POINT('Ctrl Pts',(7.55709454086888,0.884320122340259,24.7552947919174));
#6060=CARTESIAN_POINT('Ctrl Pts',(7.58275327840586,0.788796531362502,24.7613934129174));
#6061=CARTESIAN_POINT('Ctrl Pts',(7.6039526371208,0.692434101700029,24.7674920339174));
#6062=CARTESIAN_POINT('Ctrl Pts',(7.62519206241875,0.595889547977125,24.7736021812522));
#6063=CARTESIAN_POINT('Ctrl Pts',(7.64195520212604,0.49850342701961,24.779712328587));
#6064=CARTESIAN_POINT('Ctrl Pts',(7.65420784391407,0.40072999381057,24.7858224759218));
#6065=CARTESIAN_POINT('Ctrl Pts',(7.66467641885284,0.31719302845427,24.7910429448106));
#6066=CARTESIAN_POINT('Ctrl Pts',(7.67185326443048,0.233373553073914,24.7962634136995));
#6067=CARTESIAN_POINT('Ctrl Pts',(7.67574717225487,0.149553656041532,24.8014838825884));
#6068=CARTESIAN_POINT('Ctrl Pts',(7.67805684450647,0.0998358663457391,24.8045804048166));
#6069=CARTESIAN_POINT('Ctrl Pts',(7.67921437958694,0.0500747491672077,24.8076769270449));
#6070=CARTESIAN_POINT('Ctrl Pts',(7.67921909177339,0.000305129896709012,
24.8107734492731));
#6071=CARTESIAN_POINT('Ctrl Pts',(7.67921910621823,-7.83532877468573E-9,
24.5634577632816));
#6072=CARTESIAN_POINT('Ctrl Pts',(7.67921910654256,0.133398137250487,24.55447038207));
#6073=CARTESIAN_POINT('Ctrl Pts',(7.67093661792531,0.266687541275268,24.5455903586593));
#6074=CARTESIAN_POINT('Ctrl Pts',(7.64446499824392,0.478801730918038,24.5317288342665));
#6075=CARTESIAN_POINT('Ctrl Pts',(7.63154154501361,0.558109087832411,24.5266057187726));
#6076=CARTESIAN_POINT('Ctrl Pts',(7.6109501571527,0.660254942829582,24.5200814270419));
#6077=CARTESIAN_POINT('Ctrl Pts',(7.60597344436133,0.68360058794858,24.5185952796626));
#6078=CARTESIAN_POINT('Ctrl Pts',(7.59743332482478,0.721587341298214,24.5161847776374));
#6079=CARTESIAN_POINT('Ctrl Pts',(7.59402587349456,0.73626222108192,24.5152554396569));
#6080=CARTESIAN_POINT('Ctrl Pts',(7.58724719352546,0.764554049600949,24.5134672049344));
#6081=CARTESIAN_POINT('Ctrl Pts',(7.58388972074766,0.778173911431171,24.5126078862052));
#6082=CARTESIAN_POINT('Ctrl Pts',(7.57594344365583,0.809526343791456,24.5106331327956));
#6083=CARTESIAN_POINT('Ctrl Pts',(7.57129215056274,0.827242689466017,24.5095197524271));
#6084=CARTESIAN_POINT('Ctrl Pts',(7.55579185650502,0.884296980967118,24.5059415058436));
#6085=CARTESIAN_POINT('Ctrl Pts',(7.54434644538047,0.923469775651678,24.503496061915));
#6086=CARTESIAN_POINT('Ctrl Pts',(7.45978181912304,1.1937215414841,24.4866818717166));
#6087=CARTESIAN_POINT('Ctrl Pts',(7.36154371908736,1.41612668337206,24.4732126560994));
#6088=CARTESIAN_POINT('Ctrl Pts',(7.17043897046691,1.74330707275403,24.4520424700107));
#6089=CARTESIAN_POINT('Ctrl Pts',(7.09417473773427,1.85667861022511,24.4443951695889));
#6090=CARTESIAN_POINT('Ctrl Pts',(6.98524905950513,1.99829124616426,24.4339826033436));
#6091=CARTESIAN_POINT('Ctrl Pts',(6.95888555596945,2.03120839320807,24.4314961089902));
#6092=CARTESIAN_POINT('Ctrl Pts',(6.91357926587741,2.08555616652858,24.4272601994819));
#6093=CARTESIAN_POINT('Ctrl Pts',(6.89498281490939,2.10726970834283,24.4255314657325));
#6094=CARTESIAN_POINT('Ctrl Pts',(6.86862376262849,2.13723082725154,24.4230900734091));
#6095=CARTESIAN_POINT('Ctrl Pts',(6.86110221523411,2.14568993506357,24.4223944134373));
#6096=CARTESIAN_POINT('Ctrl Pts',(6.848205306685,2.16004146334287,24.4212029132762));
#6097=CARTESIAN_POINT('Ctrl Pts',(6.84285237837223,2.16595384375363,24.4207087515198));
#6098=CARTESIAN_POINT('Ctrl Pts',(6.8324400903726,2.17736889792201,24.4197481527618));
#6099=CARTESIAN_POINT('Ctrl Pts',(6.82738360139083,2.1828737684702,24.4192819575488));
#6100=CARTESIAN_POINT('Ctrl Pts',(6.81366528474199,2.19770465287964,24.4180180885247));
#6101=CARTESIAN_POINT('Ctrl Pts',(6.8049673911384,2.20699690946801,24.4172177393123));
#6102=CARTESIAN_POINT('Ctrl Pts',(6.77208273732516,2.24171418989512,24.4141963364709));
#6103=CARTESIAN_POINT('Ctrl Pts',(6.74753723499033,2.26679412232575,24.4119502400114));
#6104=CARTESIAN_POINT('Ctrl Pts',(6.56568147246832,2.44663822679667,24.3954075287975));
#6105=CARTESIAN_POINT('Ctrl Pts',(6.3932617278536,2.58527373241151,24.38029358379));
#6106=CARTESIAN_POINT('Ctrl Pts',(6.03496079596833,2.81726784732446,24.351531859574));
#6107=CARTESIAN_POINT('Ctrl Pts',(5.85149780740907,2.91248285752567,24.3379201401605));
#6108=CARTESIAN_POINT('Ctrl Pts',(5.63206400410108,3.00083517689787,24.3230280181732));
#6109=CARTESIAN_POINT('Ctrl Pts',(5.60380605825753,3.01175250340107,24.3211342891187));
#6110=CARTESIAN_POINT('Ctrl Pts',(5.55987354177247,3.02801754343669,24.3182262270692));
#6111=CARTESIAN_POINT('Ctrl Pts',(5.54430521039196,3.03364536795737,24.3172026307065));
#6112=CARTESIAN_POINT('Ctrl Pts',(5.51682990130281,3.04333876243206,24.3154081157189));
#6113=CARTESIAN_POINT('Ctrl Pts',(5.5049412920116,3.04745499087098,24.3146355361345));
#6114=CARTESIAN_POINT('Ctrl Pts',(5.47773917230597,3.05669523508705,24.3128765762331));
#6115=CARTESIAN_POINT('Ctrl Pts',(5.46241056544166,3.06177401247868,24.3118917004727));
#6116=CARTESIAN_POINT('Ctrl Pts',(5.42073155492803,3.07523658993525,24.3092304530469));
#6117=CARTESIAN_POINT('Ctrl Pts',(5.39431000938255,3.08339693622049,24.3075613902145));
#6118=CARTESIAN_POINT('Ctrl Pts',(5.2563240840812,3.12407636399447,24.2989331680923));
#6119=CARTESIAN_POINT('Ctrl Pts',(5.14315948960798,3.15088585056849,24.2921602930875));
#6120=CARTESIAN_POINT('Ctrl Pts',(4.80502376972901,3.21190383241823,24.2725051494874));
#6121=CARTESIAN_POINT('Ctrl Pts',(4.57763074893569,3.22848741839149,24.260068817103));
#6122=CARTESIAN_POINT('Ctrl Pts',(4.23942743565147,3.21734935897173,24.2407925493243));
#6123=CARTESIAN_POINT('Ctrl Pts',(4.1287377143078,3.20796365079108,24.2343483313036));
#6124=CARTESIAN_POINT('Ctrl Pts',(4.0013995304929,3.19050724816095,24.2265566520593));
#6125=CARTESIAN_POINT('Ctrl Pts',(3.98405336392011,3.18798496772045,24.2254870362918));
#6126=CARTESIAN_POINT('Ctrl Pts',(3.95746644239923,3.18389725471876,24.2238337873915));
#6127=CARTESIAN_POINT('Ctrl Pts',(3.94821019534125,3.18243275835619,24.2232556304219));
#6128=CARTESIAN_POINT('Ctrl Pts',(3.93121500973005,3.17966779377962,24.2221891328721));
#6129=CARTESIAN_POINT('Ctrl Pts',(3.92347431360627,3.17837941287616,24.2217014723261));
#6130=CARTESIAN_POINT('Ctrl Pts',(3.90597365221809,3.17540082966504,24.2205946120525));
#6131=CARTESIAN_POINT('Ctrl Pts',(3.89621681671857,3.17369391087221,24.2199744976119));
#6132=CARTESIAN_POINT('Ctrl Pts',(3.87095563806481,3.16915445350731,24.2183614013051));
#6133=CARTESIAN_POINT('Ctrl Pts',(3.8554641348447,3.16625314414301,24.2173647581553));
#6134=CARTESIAN_POINT('Ctrl Pts',(3.75207556233731,3.14610405004485,24.2106665182324));
#6135=CARTESIAN_POINT('Ctrl Pts',(3.6649167069486,3.12531322144643,24.2047943217843));
#6136=CARTESIAN_POINT('Ctrl Pts',(3.49824257715581,3.0781357105749,24.1932634380833));
#6137=CARTESIAN_POINT('Ctrl Pts',(3.41865995070935,3.05222357901309,24.1876202786106));
#6138=CARTESIAN_POINT('Ctrl Pts',(3.21783871704433,2.97807318543374,24.1731462931991));
#6139=CARTESIAN_POINT('Ctrl Pts',(3.09834806755375,2.92551452563916,24.1643134491597));
#6140=CARTESIAN_POINT('Ctrl Pts',(2.84947139525583,2.79750066554015,24.1456798039763));
#6141=CARTESIAN_POINT('Ctrl Pts',(2.72147695377286,2.71997515267977,24.135951483536));
#6142=CARTESIAN_POINT('Ctrl Pts',(2.57750302450599,2.61845680374688,24.1248663022953));
#6143=CARTESIAN_POINT('Ctrl Pts',(2.55588693723755,2.60280945461253,24.1231975441654));
#6144=CARTESIAN_POINT('Ctrl Pts',(2.52058378264626,2.57658004411053,24.120464163127));
#6145=CARTESIAN_POINT('Ctrl Pts',(2.50678347132565,2.56615327942101,24.1193936036624));
#6146=CARTESIAN_POINT('Ctrl Pts',(2.48199734095253,2.54711085223847,24.1174668350946));
#6147=CARTESIAN_POINT('Ctrl Pts',(2.47098237457753,2.53853400481894,24.1166091328642));
#6148=CARTESIAN_POINT('Ctrl Pts',(2.44747082321841,2.5199799902538,24.1147750609654));
#6149=CARTESIAN_POINT('Ctrl Pts',(2.43499202460595,2.50998081173809,24.1137995971346));
#6150=CARTESIAN_POINT('Ctrl Pts',(2.40105431348308,2.48236947813517,24.1111407177066));
#6151=CARTESIAN_POINT('Ctrl Pts',(2.37974741680168,2.46457203058154,24.1094647950051));
#6152=CARTESIAN_POINT('Ctrl Pts',(2.25928453500097,2.36127895894633,24.0999461889107));
#6153=CARTESIAN_POINT('Ctrl Pts',(2.1651753804256,2.2700742779802,24.0923460839043));
#6154=CARTESIAN_POINT('Ctrl Pts',(1.97934575504301,2.06661287841548,24.0766597395672));
#6155=CARTESIAN_POINT('Ctrl Pts',(1.88911904706794,1.95339294522926,24.0686244308601));
#6156=CARTESIAN_POINT('Ctrl Pts',(1.71200680732183,1.69757953819521,24.0511990055546));
#6157=CARTESIAN_POINT('Ctrl Pts',(1.62797877074432,1.55353743329028,24.0418132318677));
#6158=CARTESIAN_POINT('Ctrl Pts',(1.54371469093157,1.37938646720165,24.0302157365546));
#6159=CARTESIAN_POINT('Ctrl Pts',(1.53227074438938,1.35495724740963,24.0285832605212));
#6160=CARTESIAN_POINT('Ctrl Pts',(1.51687343786853,1.32098503059886,24.0263014524716));
#6161=CARTESIAN_POINT('Ctrl Pts',(1.5126569081527,1.3115616189237,24.025667286771));
#6162=CARTESIAN_POINT('Ctrl Pts',(1.50549537042113,1.2953479658597,24.0245737901254));
#6163=CARTESIAN_POINT('Ctrl Pts',(1.50252831256744,1.2885674708854,24.0241157857353));
#6164=CARTESIAN_POINT('Ctrl Pts',(1.49637046501007,1.27436215665442,24.0231546543602));
#6165=CARTESIAN_POINT('Ctrl Pts',(1.49318422720338,1.26693551241192,24.0226512461872));
#6166=CARTESIAN_POINT('Ctrl Pts',(1.48544866632388,1.24871625556839,24.0214141498326));
#6167=CARTESIAN_POINT('Ctrl Pts',(1.48093020615531,1.23791073403787,24.0206786362247));
#6168=CARTESIAN_POINT('Ctrl Pts',(1.46473141899791,1.19857155675043,24.0179949465732));
#6169=CARTESIAN_POINT('Ctrl Pts',(1.45340223066768,1.16989629621508,24.0160274460453));
#6170=CARTESIAN_POINT('Ctrl Pts',(1.42598684590726,1.09748188724091,24.0110384707653));
#6171=CARTESIAN_POINT('Ctrl Pts',(1.41043507441013,1.05354898319761,24.0079933141749));
#6172=CARTESIAN_POINT('Ctrl Pts',(1.29247241423753,0.695834836972181,23.9831331591239));
#6173=CARTESIAN_POINT('Ctrl Pts',(1.23785653150625,0.368329752488542,23.9602364645673));
#6174=CARTESIAN_POINT('Ctrl Pts',(1.23312726365507,-0.0308683449592165,
23.9344779737535));
#6175=CARTESIAN_POINT('Ctrl Pts',(1.23452847054092,-0.0999259677591112,
23.9300870358221));
#6176=CARTESIAN_POINT('Ctrl Pts',(1.23937946453772,-0.192365335190156,23.924293281993));
#6177=CARTESIAN_POINT('Ctrl Pts',(1.240868255887,-0.215827253189526,23.9228299757338));
#6178=CARTESIAN_POINT('Ctrl Pts',(1.24373087264865,-0.25427748434757,23.9204431962415));
#6179=CARTESIAN_POINT('Ctrl Pts',(1.24495318439968,-0.269275867196935,23.9195150117187));
#6180=CARTESIAN_POINT('Ctrl Pts',(1.24752954412871,-0.298370516814858,23.9177197841499));
#6181=CARTESIAN_POINT('Ctrl Pts',(1.24887153732137,-0.312467477605069,23.9168523844858));
#6182=CARTESIAN_POINT('Ctrl Pts',(1.25223585301616,-0.345498768004624,23.9148254069702));
#6183=CARTESIAN_POINT('Ctrl Pts',(1.25433317167555,-0.364425054633693,23.9136682106925));
#6184=CARTESIAN_POINT('Ctrl Pts',(1.26175909587514,-0.426413100473815,23.9098911097947));
#6185=CARTESIAN_POINT('Ctrl Pts',(1.26778971827805,-0.469387061127087,23.9072932539876));
#6186=CARTESIAN_POINT('Ctrl Pts',(1.28416572602259,-0.571109189977421,23.90118383744));
#6187=CARTESIAN_POINT('Ctrl Pts',(1.29527791424737,-0.62971842405922,23.8976957423725));
#6188=CARTESIAN_POINT('Ctrl Pts',(1.34480149666502,-0.856354511157959,23.8842799581829));
#6189=CARTESIAN_POINT('Ctrl Pts',(1.39503996703573,-1.02150610204247,23.8746768723953));
#6190=CARTESIAN_POINT('Ctrl Pts',(1.5261409338791,-1.35409448013365,23.8546853918375));
#6191=CARTESIAN_POINT('Ctrl Pts',(1.60874442609311,-1.52014528492112,23.8443239016441));
#6192=CARTESIAN_POINT('Ctrl Pts',(1.71905233573639,-1.70099443381679,23.8316230827937));
#6193=CARTESIAN_POINT('Ctrl Pts',(1.73326007906393,-1.72364878329798,23.8300047026801));
#6194=CARTESIAN_POINT('Ctrl Pts',(1.75332135546355,-1.75476939506296,23.8277394906023));
#6195=CARTESIAN_POINT('Ctrl Pts',(1.7589364456938,-1.76338904697531,23.827107554198));
#6196=CARTESIAN_POINT('Ctrl Pts',(1.76865465225191,-1.77815230001433,23.8260171369178));
#6197=CARTESIAN_POINT('Ctrl Pts',(1.77273784267574,-1.78430901009029,23.825559970107));
#6198=CARTESIAN_POINT('Ctrl Pts',(1.78133944053119,-1.79718234012883,23.8245988331067));
#6199=CARTESIAN_POINT('Ctrl Pts',(1.78586202119365,-1.80389602929368,23.8240945717922));
#6200=CARTESIAN_POINT('Ctrl Pts',(1.79701588126895,-1.82031985352653,23.822853725263));
#6201=CARTESIAN_POINT('Ctrl Pts',(1.80367506272029,-1.83001081350776,23.8221152945784));
#6202=CARTESIAN_POINT('Ctrl Pts',(1.82813767841435,-1.86519661730689,23.8194119433302));
#6203=CARTESIAN_POINT('Ctrl Pts',(1.84625619688889,-1.89046896743857,23.8174273643497));
#6204=CARTESIAN_POINT('Ctrl Pts',(1.89274839673714,-1.95337524221768,23.8123865199626));
#6205=CARTESIAN_POINT('Ctrl Pts',(1.92158668453334,-1.99065551233131,23.8093060134129));
#6206=CARTESIAN_POINT('Ctrl Pts',(2.1674461520701,-2.29447846049972,23.7835024547909));
#6207=CARTESIAN_POINT('Ctrl Pts',(2.4250974826434,-2.52544595311274,23.7596454164184));
#6208=CARTESIAN_POINT('Ctrl Pts',(2.76308037760481,-2.74260887281112,23.7338807711373));
#6209=CARTESIAN_POINT('Ctrl Pts',(2.81262017722566,-2.77258547351449,23.7302143476471));
#6210=CARTESIAN_POINT('Ctrl Pts',(2.88204548641158,-2.8120794446459,23.7252226884356));
#6211=CARTESIAN_POINT('Ctrl Pts',(2.90125864001196,-2.82275060566896,23.7238562924268));
#6212=CARTESIAN_POINT('Ctrl Pts',(2.93223923746065,-2.839545167929,23.7216765816477));
#6213=CARTESIAN_POINT('Ctrl Pts',(2.94393767903226,-2.84579376337713,23.7208588301228));
#6214=CARTESIAN_POINT('Ctrl Pts',(2.9682186639187,-2.85857116657437,23.7191723551825));
#6215=CARTESIAN_POINT('Ctrl Pts',(2.98080639658954,-2.86508953977177,23.7183040139281));
#6216=CARTESIAN_POINT('Ctrl Pts',(3.01039774288975,-2.88016623145105,23.7162764050665));
#6217=CARTESIAN_POINT('Ctrl Pts',(3.02743510150431,-2.88865742968223,23.7151195061843));
#6218=CARTESIAN_POINT('Ctrl Pts',(3.0834384156425,-2.91595200733911,23.7113500450175));
#6219=CARTESIAN_POINT('Ctrl Pts',(3.12270889400311,-2.93412224520004,23.7087593442097));
#6220=CARTESIAN_POINT('Ctrl Pts',(3.21673579953138,-2.9753499504563,23.7026705067408));
#6221=CARTESIAN_POINT('Ctrl Pts',(3.27178795144855,-2.99769530742523,23.6991955545032));
#6222=CARTESIAN_POINT('Ctrl Pts',(3.48767360077728,-3.07844502793879,23.6858620576207));
#6223=CARTESIAN_POINT('Ctrl Pts',(3.65244420321299,-3.12552990617507,23.6763226324518));
#6224=CARTESIAN_POINT('Ctrl Pts',(4.00285808221847,-3.19610394970807,23.6563291487158));
#6225=CARTESIAN_POINT('Ctrl Pts',(4.18836302177209,-3.21697758626017,23.6459026342698));
#6226=CARTESIAN_POINT('Ctrl Pts',(4.40132462819749,-3.22238903636769,23.6331292496831));
#6227=CARTESIAN_POINT('Ctrl Pts',(4.4280516836664,-3.22273553989994,23.6315114958831));
#6228=CARTESIAN_POINT('Ctrl Pts',(4.46507406513482,-3.22275495599412,23.629246468284));
#6229=CARTESIAN_POINT('Ctrl Pts',(4.47536897418246,-3.22271102334964,23.6286140434918));
#6230=CARTESIAN_POINT('Ctrl Pts',(4.49306074250226,-3.22255075069525,23.6275225153997));
#6231=CARTESIAN_POINT('Ctrl Pts',(4.50045781112537,-3.22245826658705,23.6270647241671));
#6232=CARTESIAN_POINT('Ctrl Pts',(4.51595296662926,-3.22221117187929,23.6261026714121));
#6233=CARTESIAN_POINT('Ctrl Pts',(4.52405084167679,-3.22205150017221,23.6255981201071));
#6234=CARTESIAN_POINT('Ctrl Pts',(4.54391884716972,-3.22158481766088,23.6243559890034));
#6235=CARTESIAN_POINT('Ctrl Pts',(4.55568799583006,-3.22124382753291,23.6236165566525));
#6236=CARTESIAN_POINT('Ctrl Pts',(4.59863614834341,-3.21976389287901,23.6209055866183));
#6237=CARTESIAN_POINT('Ctrl Pts',(4.62979892885478,-3.2182367218773,23.6189142512396));
#6238=CARTESIAN_POINT('Ctrl Pts',(4.70818035143695,-3.21325385279514,23.6138525388621));
#6239=CARTESIAN_POINT('Ctrl Pts',(4.75535319884567,-3.20920967136437,23.6107576831234));
#6240=CARTESIAN_POINT('Ctrl Pts',(4.96993516516813,-3.18604135726999,23.5965064470594));
#6241=CARTESIAN_POINT('Ctrl Pts',(5.13577049462276,-3.15484598423149,23.5850257969416));
#6242=CARTESIAN_POINT('Ctrl Pts',(5.48946455598691,-3.05912033773592,23.5603031253992));
#6243=CARTESIAN_POINT('Ctrl Pts',(5.67538408925436,-2.98991072380797,23.5471700463777));
#6244=CARTESIAN_POINT('Ctrl Pts',(5.89076082274076,-2.88627911910194,23.5319977510812));
#6245=CARTESIAN_POINT('Ctrl Pts',(5.92737937704093,-2.86779063142463,23.5294180261197));
#6246=CARTESIAN_POINT('Ctrl Pts',(5.97884943753798,-2.84055838041974,23.5257903727994));
#6247=CARTESIAN_POINT('Ctrl Pts',(5.99399796960811,-2.83238747321706,23.524722472469));
#6248=CARTESIAN_POINT('Ctrl Pts',(6.0215879477259,-2.81721924808184,23.5227768774217));
#6249=CARTESIAN_POINT('Ctrl Pts',(6.03404967696782,-2.81025992268162,23.5218978601141));
#6250=CARTESIAN_POINT('Ctrl Pts',(6.05893793797852,-2.7961432069557,23.5201416554475));
#6251=CARTESIAN_POINT('Ctrl Pts',(6.07136375028342,-2.7889852078473,23.5192645158137));
#6252=CARTESIAN_POINT('Ctrl Pts',(6.10171875193144,-2.7712280563091,23.5171206939419));
#6253=CARTESIAN_POINT('Ctrl Pts',(6.11959391940449,-2.76053748822712,23.515857348859));
#6254=CARTESIAN_POINT('Ctrl Pts',(6.15771824562205,-2.73723181605482,23.5131601402178));
#6255=CARTESIAN_POINT('Ctrl Pts',(6.17793357841946,-2.72456359174508,23.5117282719134));
#6256=CARTESIAN_POINT('Ctrl Pts',(6.23441605057961,-2.6882884224586,23.5077210341611));
#6257=CARTESIAN_POINT('Ctrl Pts',(6.27035179322774,-2.66417338513943,23.5051638787774));
#6258=CARTESIAN_POINT('Ctrl Pts',(6.38973711359475,-2.58052294992327,23.4966269297175));
#6259=CARTESIAN_POINT('Ctrl Pts',(6.47083234999511,-2.51773051373397,23.4907599178561));
#6260=CARTESIAN_POINT('Ctrl Pts',(6.71728400119812,-2.30735854710629,23.4724404557752));
#6261=CARTESIAN_POINT('Ctrl Pts',(6.87047701246788,-2.14656494184902,23.4603327240357));
#6262=CARTESIAN_POINT('Ctrl Pts',(7.05503687824137,-1.90787831382013,23.4429224639934));
#6263=CARTESIAN_POINT('Ctrl Pts',(7.10172092246189,-1.84260541163386,23.438206228264));
#6264=CARTESIAN_POINT('Ctrl Pts',(7.15513887606974,-1.76169780647075,23.4323248179688));
#6265=CARTESIAN_POINT('Ctrl Pts',(7.16425139941566,-1.74765920967625,23.431303055027));
#6266=CARTESIAN_POINT('Ctrl Pts',(7.17824594712378,-1.72572724269762,23.4297038027168));
#6267=CARTESIAN_POINT('Ctrl Pts',(7.18320406840346,-1.71788245489541,23.4291311816741));
#6268=CARTESIAN_POINT('Ctrl Pts',(7.1922818181667,-1.70338123943199,23.4280713883739));
#6269=CARTESIAN_POINT('Ctrl Pts',(7.19641114036327,-1.69673111810703,23.4275848616532));
#6270=CARTESIAN_POINT('Ctrl Pts',(7.205732450304,-1.68159673090469,23.4264764708278));
#6271=CARTESIAN_POINT('Ctrl Pts',(7.21090938459066,-1.67310347773368,23.4258536574622));
#6272=CARTESIAN_POINT('Ctrl Pts',(7.2266227802468,-1.64705356325947,23.4239413060423));
#6273=CARTESIAN_POINT('Ctrl Pts',(7.23703107698062,-1.62942072360718,23.4226439583952));
#6274=CARTESIAN_POINT('Ctrl Pts',(7.33364807272611,-1.46211885016639,23.4103160654394));
#6275=CARTESIAN_POINT('Ctrl Pts',(7.40785270425699,-1.30586080326885,23.3986775301669));
#6276=CARTESIAN_POINT('Ctrl Pts',(7.54876386434284,-0.934913234746212,23.3718389061261));
#6277=CARTESIAN_POINT('Ctrl Pts',(7.60629135096761,-0.717633121003952,23.3567147696628));
#6278=CARTESIAN_POINT('Ctrl Pts',(7.65075569699311,-0.432238794097489,23.3381223317963));
#6279=CARTESIAN_POINT('Ctrl Pts',(7.65878419504358,-0.368070962752275,23.3340176750285));
#6280=CARTESIAN_POINT('Ctrl Pts',(7.66703629601794,-0.280892798517734,23.3285399692109));
#6281=CARTESIAN_POINT('Ctrl Pts',(7.66895205378973,-0.258061619725829,23.327114492367));
#6282=CARTESIAN_POINT('Ctrl Pts',(7.67171370172156,-0.220323813622921,23.3247728533729));
#6283=CARTESIAN_POINT('Ctrl Pts',(7.67269974243683,-0.205428572424087,23.323852333077));
#6284=CARTESIAN_POINT('Ctrl Pts',(7.67436883559197,-0.177245339782721,23.3221174958161));
#6285=CARTESIAN_POINT('Ctrl Pts',(7.67507315834198,-0.163958966835426,23.3213025309651));
#6286=CARTESIAN_POINT('Ctrl Pts',(7.67634338032585,-0.136819033873957,23.3196435440727));
#6287=CARTESIAN_POINT('Ctrl Pts',(7.67690219918881,-0.122965410292963,23.3187997592406));
#6288=CARTESIAN_POINT('Ctrl Pts',(7.6779647492397,-0.0915987252782205,23.3168959750869));
#6289=CARTESIAN_POINT('Ctrl Pts',(7.67841511027732,-0.0740842076861186,
23.315837646492));
#6290=CARTESIAN_POINT('Ctrl Pts',(7.67905843342729,-0.0374380329825862,
23.3136326381325));
#6291=CARTESIAN_POINT('Ctrl Pts',(7.67922390057638,-0.0183066048955584,
23.3124868338538));
#6292=CARTESIAN_POINT('Ctrl Pts',(7.6792190005175,0.000825405381727912,
23.3113459957337));
#6293=CARTESIAN_POINT('Origin',(4.45646910621825,-5.13094777615093E-16,
-2.31077344927308));
#6294=CARTESIAN_POINT('',(7.67921910621823,-2.19646041259736E-11,22.0659612921829));
#6295=CARTESIAN_POINT('',(7.67921900305864,0.000815423282546346,22.3107734492731));
#6296=CARTESIAN_POINT('',(7.67921910621823,-3.51191647465084E-13,-2.31077344927308));
#6297=CARTESIAN_POINT('Ctrl Pts',(7.67921900305864,0.000815423282546346,
22.3107734492731));
#6298=CARTESIAN_POINT('Ctrl Pts',(7.67924509448734,-0.102304209114605,22.3171055672954));
#6299=CARTESIAN_POINT('Ctrl Pts',(7.67431750357225,-0.205370600635493,22.3234376853178));
#6300=CARTESIAN_POINT('Ctrl Pts',(7.66447767354317,-0.30789380388341,22.3297698033401));
#6301=CARTESIAN_POINT('Ctrl Pts',(7.65462973255273,-0.410501516898032,22.3361071409206));
#6302=CARTESIAN_POINT('Ctrl Pts',(7.63986152481682,-0.512564754953075,22.342444478501));
#6303=CARTESIAN_POINT('Ctrl Pts',(7.62026604465574,-0.613601250677855,22.3487818160815));
#6304=CARTESIAN_POINT('Ctrl Pts',(7.60063379821649,-0.714827317460683,22.3551310441751));
#6305=CARTESIAN_POINT('Ctrl Pts',(7.57615626072823,-0.815022402810588,22.3614802722688));
#6306=CARTESIAN_POINT('Ctrl Pts',(7.54697718013528,-0.913716262060345,22.3678295003625));
#6307=CARTESIAN_POINT('Ctrl Pts',(7.51776904979301,-1.01250837772573,22.3741850495424));
#6308=CARTESIAN_POINT('Ctrl Pts',(7.48385017622183,-1.10979591354012,22.3805405987224));
#6309=CARTESIAN_POINT('Ctrl Pts',(7.44541291204491,-1.20512758167354,22.3868961479023));
#6310=CARTESIAN_POINT('Ctrl Pts',(7.40689339787825,-1.30066324530179,22.3932652970057));
#6311=CARTESIAN_POINT('Ctrl Pts',(7.36383633604013,-1.39423431600571,22.3996344461092));
#6312=CARTESIAN_POINT('Ctrl Pts',(7.31648092742837,-1.48541238214788,22.4060035952127));
#6313=CARTESIAN_POINT('Ctrl Pts',(7.28355106781503,-1.54881550770199,22.4104325546913));
#6314=CARTESIAN_POINT('Ctrl Pts',(7.24854370443691,-1.61106203584785,22.4148615141699));
#6315=CARTESIAN_POINT('Ctrl Pts',(7.21155137183393,-1.67201652868321,22.4192904736485));
#6316=CARTESIAN_POINT('Ctrl Pts',(7.15998739255039,-1.7569816007573,22.4254640441895));
#6317=CARTESIAN_POINT('Ctrl Pts',(7.10439904072553,-1.83970790273964,22.4316376147305));
#6318=CARTESIAN_POINT('Ctrl Pts',(7.0450064794378,-1.9197895275122,22.4378111852716));
#6319=CARTESIAN_POINT('Ctrl Pts',(6.98569408981377,-1.99976305327453,22.4439764223545));
#6320=CARTESIAN_POINT('Ctrl Pts',(6.92258795393058,-2.07709865192323,22.4501416594374));
#6321=CARTESIAN_POINT('Ctrl Pts',(6.85595299413103,-2.15141688989996,22.4563068965204));
#6322=CARTESIAN_POINT('Ctrl Pts',(6.78938831987777,-2.22565673812496,22.4624656306046));
#6323=CARTESIAN_POINT('Ctrl Pts',(6.71930251005466,-2.29688523173755,22.4686243646889));
#6324=CARTESIAN_POINT('Ctrl Pts',(6.64600187892413,-2.36475449037458,22.4747830987731));
#6325=CARTESIAN_POINT('Ctrl Pts',(6.57275448031797,-2.43257446086895,22.4809373602497));
#6326=CARTESIAN_POINT('Ctrl Pts',(6.49629721980748,-2.49703975260539,22.4870916217263));
#6327=CARTESIAN_POINT('Ctrl Pts',(6.41697388958871,-2.55783864950106,22.4932458832029));
#6328=CARTESIAN_POINT('Ctrl Pts',(6.33768038094169,-2.61861468907769,22.4993978309876));
#6329=CARTESIAN_POINT('Ctrl Pts',(6.2555232878144,-2.67572680888366,22.5055497787722));
#6330=CARTESIAN_POINT('Ctrl Pts',(6.17087947714751,-2.72890356050742,22.5117017265569));
#6331=CARTESIAN_POINT('Ctrl Pts',(6.08624487519753,-2.78207452683337,22.5178530050481));
#6332=CARTESIAN_POINT('Ctrl Pts',(5.99912446122754,-2.83131074527077,22.5240042835394));
#6333=CARTESIAN_POINT('Ctrl Pts',(5.90992322417004,-2.87638465604113,22.5301555620306));
#6334=CARTESIAN_POINT('Ctrl Pts',(5.8207078612431,-2.92146570469656,22.5363078146357));
#6335=CARTESIAN_POINT('Ctrl Pts',(5.72941140823683,-2.96238294062894,22.5424600672407));
#6336=CARTESIAN_POINT('Ctrl Pts',(5.63646162197437,-2.99895568911236,22.5486123198458));
#6337=CARTESIAN_POINT('Ctrl Pts',(5.54341270018547,-3.03556744423388,22.5547711341313));
#6338=CARTESIAN_POINT('Ctrl Pts',(5.44870732873436,-3.06782529997915,22.5609299484169));
#6339=CARTESIAN_POINT('Ctrl Pts',(5.35279121626834,-3.09559755742493,22.5670887627024));
#6340=CARTESIAN_POINT('Ctrl Pts',(5.25682142366214,-3.12338535781376,22.5732510238126));
#6341=CARTESIAN_POINT('Ctrl Pts',(5.15963996278668,-3.14668245924176,22.5794132849227));
#6342=CARTESIAN_POINT('Ctrl Pts',(5.06170356259582,-3.16540815935531,22.5855755460329));
#6343=CARTESIAN_POINT('Ctrl Pts',(4.96360463068712,-3.18416493596547,22.5917480338093));
#6344=CARTESIAN_POINT('Ctrl Pts',(4.86474868687652,-3.19833509620449,22.5979205215858));
#6345=CARTESIAN_POINT('Ctrl Pts',(4.7655985483105,-3.20788973478385,22.6040930093622));
#6346=CARTESIAN_POINT('Ctrl Pts',(4.69217037397495,-3.21496566707668,22.6086642032616));
#6347=CARTESIAN_POINT('Ctrl Pts',(4.61858095894887,-3.21951129524688,22.6132353971609));
#6348=CARTESIAN_POINT('Ctrl Pts',(4.54501750299387,-3.22153329083036,22.6178065910603));
#6349=CARTESIAN_POINT('Ctrl Pts',(4.44566662018497,-3.22426409029657,22.6239802019041));
#6350=CARTESIAN_POINT('Ctrl Pts',(4.3460153608817,-3.22239945011425,22.6301538127479));
#6351=CARTESIAN_POINT('Ctrl Pts',(4.24652417069623,-3.21590433417235,22.6363274235917));
#6352=CARTESIAN_POINT('Ctrl Pts',(4.14716727029211,-3.20941798511421,22.6424927015082));
#6353=CARTESIAN_POINT('Ctrl Pts',(4.04797043900825,-3.19831361120412,22.6486579794248));
#6354=CARTESIAN_POINT('Ctrl Pts',(3.94939614020412,-3.18260813950406,22.6548232573413));
#6355=CARTESIAN_POINT('Ctrl Pts',(3.85092580785642,-3.16691923238786,22.6609820327302));
#6356=CARTESIAN_POINT('Ctrl Pts',(3.7530771290095,-3.1466389433667,22.6671408081192));
#6357=CARTESIAN_POINT('Ctrl Pts',(3.65630849093359,-3.12183608670396,22.6732995835082));
#6358=CARTESIAN_POINT('Ctrl Pts',(3.55961011952949,-3.09705124015508,22.6794538868217));
#6359=CARTESIAN_POINT('Ctrl Pts',(3.46399064894999,-3.06775046261778,22.6856081901352));
#6360=CARTESIAN_POINT('Ctrl Pts',(3.36989839396145,-3.03405366626327,22.6917624934487));
#6361=CARTESIAN_POINT('Ctrl Pts',(3.27584150789532,-3.00036953640693,22.6979144833829));
#6362=CARTESIAN_POINT('Ctrl Pts',(3.18331110499084,-2.96229281742073,22.7040664733171));
#6363=CARTESIAN_POINT('Ctrl Pts',(3.09273959245567,-2.91999304379184,22.7102184632513));
#6364=CARTESIAN_POINT('Ctrl Pts',(3.00217792962281,-2.87769787028683,22.7163697841532));
#6365=CARTESIAN_POINT('Ctrl Pts',(2.91357512696444,-2.83118073896755,22.7225211050551));
#6366=CARTESIAN_POINT('Ctrl Pts',(2.82734195657743,-2.78065860774081,22.728672425957));
#6367=CARTESIAN_POINT('Ctrl Pts',(2.74109512749669,-2.7301284741837,22.7348247211824));
#6368=CARTESIAN_POINT('Ctrl Pts',(2.65721905082264,-2.67559230018017,22.7409770164078));
#6369=CARTESIAN_POINT('Ctrl Pts',(2.57609744321833,-2.61731159235708,22.7471293116333));
#6370=CARTESIAN_POINT('Ctrl Pts',(2.49488931526314,-2.55896872517301,22.7532881685968));
#6371=CARTESIAN_POINT('Ctrl Pts',(2.4164418759712,-2.49687360303757,22.7594470255603));
#6372=CARTESIAN_POINT('Ctrl Pts',(2.34110741893956,-2.43132936775199,22.7656058825238));
#6373=CARTESIAN_POINT('Ctrl Pts',(2.26573079953395,-2.36574844937785,22.7717681864097));
#6374=CARTESIAN_POINT('Ctrl Pts',(2.19347094596956,-2.29671487343409,22.7779304902957));
#6375=CARTESIAN_POINT('Ctrl Pts',(2.12464327316731,-2.22456868781707,22.7840927941816));
#6376=CARTESIAN_POINT('Ctrl Pts',(2.05570138043574,-2.15230277517912,22.7902653244472));
#6377=CARTESIAN_POINT('Ctrl Pts',(1.99020333001169,-2.07691426329369,22.7964378547128));
#6378=CARTESIAN_POINT('Ctrl Pts',(1.92842431175713,-1.99877639562255,22.8026103849785));
#6379=CARTESIAN_POINT('Ctrl Pts',(1.88267679024094,-1.94091510414353,22.8071811594763));
#6380=CARTESIAN_POINT('Ctrl Pts',(1.83896772291095,-1.88154690348,22.811751933974));
#6381=CARTESIAN_POINT('Ctrl Pts',(1.79739295992886,-1.82083266961427,22.8163227084718));
#6382=CARTESIAN_POINT('Ctrl Pts',(1.74124124457877,-1.73883079796932,22.8224960889103));
#6383=CARTESIAN_POINT('Ctrl Pts',(1.68878795284854,-1.65408541782211,22.8286694693488));
#6384=CARTESIAN_POINT('Ctrl Pts',(1.64031213618421,-1.56696441651639,22.8348428497873));
#6385=CARTESIAN_POINT('Ctrl Pts',(1.59190175740682,-1.47996102053691,22.8410078967309));
#6386=CARTESIAN_POINT('Ctrl Pts',(1.54745839088643,-1.39058875358549,22.8471729436745));
#6387=CARTESIAN_POINT('Ctrl Pts',(1.50721851831545,-1.2992453703034,22.8533379906181));
#6388=CARTESIAN_POINT('Ctrl Pts',(1.46702109012038,-1.20799833456543,22.8594965347685));
#6389=CARTESIAN_POINT('Ctrl Pts',(1.43101851506279,-1.11478471117023,22.8656550789189));
#6390=CARTESIAN_POINT('Ctrl Pts',(1.39940146491032,-1.02002695992205,22.8718136230692));
#6391=CARTESIAN_POINT('Ctrl Pts',(1.36780737095772,-0.925338009459091,22.8779676956839));
#6392=CARTESIAN_POINT('Ctrl Pts',(1.34059260812932,-0.829107570824273,22.8841217682985));
#6393=CARTESIAN_POINT('Ctrl Pts',(1.31789945043922,-0.731777342039871,22.8902758409131));
#6394=CARTESIAN_POINT('Ctrl Pts',(1.29521482185299,-0.634483694309692,22.8964276005519));
#6395=CARTESIAN_POINT('Ctrl Pts',(1.27704852007994,-0.536091500147451,22.9025793601908));
#6396=CARTESIAN_POINT('Ctrl Pts',(1.26349249774668,-0.437055992126014,22.9087311198296));
#6397=CARTESIAN_POINT('Ctrl Pts',(1.24993794821603,-0.338031243879885,22.9148822111066));
#6398=CARTESIAN_POINT('Ctrl Pts',(1.24099274112815,-0.238363750908735,22.9210333023836));
#6399=CARTESIAN_POINT('Ctrl Pts',(1.23669725031307,-0.138516274931135,22.9271843936606));
#6400=CARTESIAN_POINT('Ctrl Pts',(1.23240107844362,-0.038652968036155,22.9333364601993));
#6401=CARTESIAN_POINT('Ctrl Pts',(1.23275610582834,0.0613899447312124,22.939488526738));
#6402=CARTESIAN_POINT('Ctrl Pts',(1.23775060464388,0.161148286130284,22.9456405932767));
#6403=CARTESIAN_POINT('Ctrl Pts',(1.24275043286246,0.261013075128447,22.9517992244064));
#6404=CARTESIAN_POINT('Ctrl Pts',(1.25239959633902,0.360592251938886,22.9579578555361));
#6405=CARTESIAN_POINT('Ctrl Pts',(1.2666343461172,0.459425473554663,22.9641164866659));
#6406=CARTESIAN_POINT('Ctrl Pts',(1.28087706579548,0.558314030944969,22.9702785659542));
#6407=CARTESIAN_POINT('Ctrl Pts',(1.29971040295971,0.656455374992856,22.9764406452425));
#6408=CARTESIAN_POINT('Ctrl Pts',(1.32301960403999,0.753400145871158,22.9826027245308));
#6409=CARTESIAN_POINT('Ctrl Pts',(1.34636750468061,0.850505871215389,22.9887750345327));
#6410=CARTESIAN_POINT('Ctrl Pts',(1.37420599120284,0.946410638148802,22.9949473445346));
#6411=CARTESIAN_POINT('Ctrl Pts',(1.40637060934822,1.04068089340155,23.0011196545365));
#6412=CARTESIAN_POINT('Ctrl Pts',(1.43020133655365,1.11052561303604,23.0056927116521));
#6413=CARTESIAN_POINT('Ctrl Pts',(1.45640577378608,1.1794734459682,23.0102657687678));
#6414=CARTESIAN_POINT('Ctrl Pts',(1.48490056087795,1.24735638165042,23.0148388258834));
#6415=CARTESIAN_POINT('Ctrl Pts',(1.52336904858866,1.33899959585093,23.0210125372674));
#6416=CARTESIAN_POINT('Ctrl Pts',(1.56614826883377,1.42902202661247,23.0271862486514));
#6417=CARTESIAN_POINT('Ctrl Pts',(1.61308032646999,1.51698971970861,23.0333599600354));
#6418=CARTESIAN_POINT('Ctrl Pts',(1.65994902767183,1.60483865987432,23.0395253371516));
#6419=CARTESIAN_POINT('Ctrl Pts',(1.71095922063842,1.6906379960412,23.0456907142677));
#6420=CARTESIAN_POINT('Ctrl Pts',(1.76590483597035,1.77397335666725,23.0518560913838));
#6421=CARTESIAN_POINT('Ctrl Pts',(1.82079248811693,1.85722080522016,23.0580149645252));
#6422=CARTESIAN_POINT('Ctrl Pts',(1.87960707114858,1.93800908549988,23.0641738376665));
#6423=CARTESIAN_POINT('Ctrl Pts',(1.94209692262656,2.01594892913493,23.0703327108079));
#6424=CARTESIAN_POINT('Ctrl Pts',(2.00454137323384,2.09383214698707,23.0764871093314));
#6425=CARTESIAN_POINT('Ctrl Pts',(2.07065551264351,2.16887070503612,23.0826415078549));
#6426=CARTESIAN_POINT('Ctrl Pts',(2.14014527643311,2.24070557594464,23.0887959063784));
#6427=CARTESIAN_POINT('Ctrl Pts',(2.20960890176716,2.31251342628959,23.0949479899355));
#6428=CARTESIAN_POINT('Ctrl Pts',(2.28244532695656,2.38111967231176,23.1011000734926));
#6429=CARTESIAN_POINT('Ctrl Pts',(2.35832183509285,2.44620023529738,23.1072521570496));
#6430=CARTESIAN_POINT('Ctrl Pts',(2.43419007094787,2.51127370300758,23.1134035698884));
#6431=CARTESIAN_POINT('Ctrl Pts',(2.51309740124686,2.57282196928315,23.1195549827271));
#6432=CARTESIAN_POINT('Ctrl Pts',(2.59467682086061,2.63056021574924,23.1257063955658));
#6433=CARTESIAN_POINT('Ctrl Pts',(2.67626913816593,2.68830759062171,23.1318587809418));
#6434=CARTESIAN_POINT('Ctrl Pts',(2.7605340295148,2.74224349840427,23.1380111663178));
#6435=CARTESIAN_POINT('Ctrl Pts',(2.84707505486027,2.79212613432012,23.1441635516938));
#6436=CARTESIAN_POINT('Ctrl Pts',(2.93370833294037,2.84206194512679,23.1503224955127));
#6437=CARTESIAN_POINT('Ctrl Pts',(3.02262221327157,2.88793563884925,23.1564814393316));
#6438=CARTESIAN_POINT('Ctrl Pts',(3.11339527590472,2.92955120262931,23.1626403831505));
#6439=CARTESIAN_POINT('Ctrl Pts',(3.20421911570178,2.97119004556558,23.1688027721953));
#6440=CARTESIAN_POINT('Ctrl Pts',(3.29690380634158,3.00856585256235,23.17496516124));
#6441=CARTESIAN_POINT('Ctrl Pts',(3.39100950494955,3.04153142357008,23.1811275502848));
#6442=CARTESIAN_POINT('Ctrl Pts',(3.48527131496083,3.07455168097436,23.1873001620813));
#6443=CARTESIAN_POINT('Ctrl Pts',(3.58095842534341,3.10314696473573,23.1934727738779));
#6444=CARTESIAN_POINT('Ctrl Pts',(3.67761733052942,3.12722040700784,23.1996453856745));
#6445=CARTESIAN_POINT('Ctrl Pts',(3.74917811516308,3.14504302163926,23.2042152382147));
#6446=CARTESIAN_POINT('Ctrl Pts',(3.82127127827554,3.16038823792912,23.2087850907549));
#6447=CARTESIAN_POINT('Ctrl Pts',(3.89371085221291,3.17323505433316,23.2133549432952));
#6448=CARTESIAN_POINT('Ctrl Pts',(3.99157672170618,3.19059110420017,23.219528814399));
#6449=CARTESIAN_POINT('Ctrl Pts',(4.09041747329918,3.20344585013164,23.2257026855029));
#6450=CARTESIAN_POINT('Ctrl Pts',(4.18978282391545,3.21169674616571,23.2318765566067));
#6451=CARTESIAN_POINT('Ctrl Pts',(4.28901409821647,3.21993650904591,23.2380420971418));
#6452=CARTESIAN_POINT('Ctrl Pts',(4.38876813573049,3.22358473387207,23.2442076376768));
#6453=CARTESIAN_POINT('Ctrl Pts',(4.48858499707313,3.22258997268571,23.2503731782119));
#6454=CARTESIAN_POINT('Ctrl Pts',(4.58829661811924,3.22159626030976,23.2565322182088));
#6455=CARTESIAN_POINT('Ctrl Pts',(4.68807049959196,3.21596929863723,23.2626912582057));
#6456=CARTESIAN_POINT('Ctrl Pts',(4.78744308369429,3.20570956088252,23.2688502982026));
#6457=CARTESIAN_POINT('Ctrl Pts',(4.88674354379862,3.19545726958109,23.2750048680069));
#6458=CARTESIAN_POINT('Ctrl Pts',(4.98564285509247,3.18057893184648,23.2811594378113));
#6459=CARTESIAN_POINT('Ctrl Pts',(5.08367988799598,3.16112704548895,23.2873140076156));
#6460=CARTESIAN_POINT('Ctrl Pts',(5.1816800877601,3.14168246732935,23.2934662651087));
#6461=CARTESIAN_POINT('Ctrl Pts',(5.27881822752662,3.11766783929687,23.2996185226019));
#6462=CARTESIAN_POINT('Ctrl Pts',(5.37464159431828,3.0891870847516,23.305770780095));
#6463=CARTESIAN_POINT('Ctrl Pts',(5.47045455235275,3.06070942391165,23.3119223693028));
#6464=CARTESIAN_POINT('Ctrl Pts',(5.56495260525435,3.02776672479357,23.3180739585106));
#6465=CARTESIAN_POINT('Ctrl Pts',(5.65769744527187,2.99051300615035,23.3242255477183));
#6466=CARTESIAN_POINT('Ctrl Pts',(5.75045698116954,2.95325338447053,23.330378111676));
#6467=CARTESIAN_POINT('Ctrl Pts',(5.84146234952923,2.91168154824708,23.3365306756336));
#6468=CARTESIAN_POINT('Ctrl Pts',(5.9302954322741,2.86599956788633,23.3426832395912));
#6469=CARTESIAN_POINT('Ctrl Pts',(6.01922324132289,2.82026887498492,23.3488423642762));
#6470=CARTESIAN_POINT('Ctrl Pts',(6.10597375245543,2.77041948499216,23.3550014889613));
#6471=CARTESIAN_POINT('Ctrl Pts',(6.190153786505,2.71669928255575,23.3611606136463));
#6472=CARTESIAN_POINT('Ctrl Pts',(6.2743809294481,2.66294901717952,23.3673231851053));
#6473=CARTESIAN_POINT('Ctrl Pts',(6.3560343758737,2.60532387568752,23.3734857565644));
#6474=CARTESIAN_POINT('Ctrl Pts',(6.4347519782709,2.54411368469316,23.3796483280234));
#6475=CARTESIAN_POINT('Ctrl Pts',(6.51360016871647,2.48280194945534,23.3858211228397));
#6476=CARTESIAN_POINT('Ctrl Pts',(6.58950245689766,2.41789356754295,23.3919939176561));
#6477=CARTESIAN_POINT('Ctrl Pts',(6.66213158399558,2.34971713119368,23.3981667124725));
#6478=CARTESIAN_POINT('Ctrl Pts',(6.71588005500475,2.29926383016906,23.4027348285505));
#6479=CARTESIAN_POINT('Ctrl Pts',(6.76783669360609,2.2470215505427,23.4073029446286));
#6480=CARTESIAN_POINT('Ctrl Pts',(6.8178831761066,2.19313500565588,23.4118710607067));
#6481=CARTESIAN_POINT('Ctrl Pts',(6.88585467551961,2.11994805881889,23.418075326897));
#6482=CARTESIAN_POINT('Ctrl Pts',(6.95055587273519,2.04345216793193,23.4242795930872));
#6483=CARTESIAN_POINT('Ctrl Pts',(7.0116429694277,1.96397660150807,23.4304838592775));
#6484=CARTESIAN_POINT('Ctrl Pts',(7.07162307533018,1.88594125281966,23.4365756947598));
#6485=CARTESIAN_POINT('Ctrl Pts',(7.12811864870048,1.80503365970823,23.442667530242));
#6486=CARTESIAN_POINT('Ctrl Pts',(7.18084054520929,1.72160327163658,23.4487593657243));
#6487=CARTESIAN_POINT('Ctrl Pts',(7.23351252721221,1.63825187136455,23.4548454337555));
#6488=CARTESIAN_POINT('Ctrl Pts',(7.28241769076799,1.55238279315417,23.4609315017867));
#6489=CARTESIAN_POINT('Ctrl Pts',(7.32730826166912,1.46437703684197,23.4670175698179));
#6490=CARTESIAN_POINT('Ctrl Pts',(7.37216900598024,1.37642975409245,23.4730995940899));
#6491=CARTESIAN_POINT('Ctrl Pts',(7.41302025501747,1.28634900893363,23.479181618362));
#6492=CARTESIAN_POINT('Ctrl Pts',(7.44965914240116,1.19454215906984,23.4852636426341));
#6493=CARTESIAN_POINT('Ctrl Pts',(7.48756586525713,1.09955846653514,23.4915561265206));
#6494=CARTESIAN_POINT('Ctrl Pts',(7.52096314848273,1.00272746696704,23.4978486104072));
#6495=CARTESIAN_POINT('Ctrl Pts',(7.54967999396536,0.904524165748279,23.5041410942938));
#6496=CARTESIAN_POINT('Ctrl Pts',(7.57743051006099,0.809625431388222,23.5102218344462));
#6497=CARTESIAN_POINT('Ctrl Pts',(7.60081044546113,0.713445735394949,23.5163025745986));
#6498=CARTESIAN_POINT('Ctrl Pts',(7.61971633945065,0.616428831210426,23.522383314751));
#6499=CARTESIAN_POINT('Ctrl Pts',(7.63960974593652,0.514344438268555,23.5287816705047));
#6500=CARTESIAN_POINT('Ctrl Pts',(7.65454893198461,0.411333539278742,23.5351800262584));
#6501=CARTESIAN_POINT('Ctrl Pts',(7.66447488326935,0.307922874932377,23.5415783820121));
#6502=CARTESIAN_POINT('Ctrl Pts',(7.6744008345541,0.204512210586012,23.5479767377657));
#6503=CARTESIAN_POINT('Ctrl Pts',(7.67931354939866,0.100702353844344,23.5543750935194));
#6504=CARTESIAN_POINT('Ctrl Pts',(7.67921772993578,-0.0029783932951826,
23.5607734492731));
#6505=CARTESIAN_POINT('Ctrl Pts',(7.67921900114641,0.000822946196721505,
23.3113461423745));
#6506=CARTESIAN_POINT('Ctrl Pts',(7.67916246529529,0.222223699938065,23.2981440527433));
#6507=CARTESIAN_POINT('Ctrl Pts',(7.65629256834702,0.443047830936302,23.2857023480931));
#6508=CARTESIAN_POINT('Ctrl Pts',(7.56973435070216,0.856870180313654,23.2620612092812));
#6509=CARTESIAN_POINT('Ctrl Pts',(7.51014820977475,1.04960502293162,23.2508847166683));
#6510=CARTESIAN_POINT('Ctrl Pts',(7.42065187039683,1.26521681989633,23.2369515898085));
#6511=CARTESIAN_POINT('Ctrl Pts',(7.40787152411228,1.29474964723432,23.2350099785529));
#6512=CARTESIAN_POINT('Ctrl Pts',(7.38975659501365,1.33494719853519,23.2323149582033));
#6513=CARTESIAN_POINT('Ctrl Pts',(7.38480139824918,1.34578211160455,23.2315832728468));
#6514=CARTESIAN_POINT('Ctrl Pts',(7.37636598006021,1.36395961519248,23.2303464529262));
#6515=CARTESIAN_POINT('Ctrl Pts',(7.37291780070969,1.37131710265611,23.2298432649276));
#6516=CARTESIAN_POINT('Ctrl Pts',(7.36629171590265,1.38531735264428,23.2288807082625));
#6517=CARTESIAN_POINT('Ctrl Pts',(7.36311880703881,1.39196239227626,23.2284216648887));
#6518=CARTESIAN_POINT('Ctrl Pts',(7.35550714160626,1.40776403510104,23.2273249854188));
#6519=CARTESIAN_POINT('Ctrl Pts',(7.35104776737681,1.41691053951358,23.226686102204));
#6520=CARTESIAN_POINT('Ctrl Pts',(7.33504414149721,1.44934429928481,23.2244064429076));
#6521=CARTESIAN_POINT('Ctrl Pts',(7.32326191936954,1.47251213873461,23.2227520004627));
#6522=CARTESIAN_POINT('Ctrl Pts',(7.21625161867555,1.67677745649977,23.2079492287376));
#6523=CARTESIAN_POINT('Ctrl Pts',(7.1042656669358,1.84855137085491,23.1940144442717));
#6524=CARTESIAN_POINT('Ctrl Pts',(6.84944412765601,2.16829965786655,23.1663806787226));
#6525=CARTESIAN_POINT('Ctrl Pts',(6.70720139641688,2.31561678349322,23.1527506660772));
#6526=CARTESIAN_POINT('Ctrl Pts',(6.52617955210191,2.47053968967476,23.1375502485921));
#6527=CARTESIAN_POINT('Ctrl Pts',(6.50006651533279,2.49218327119314,23.1354027475394));
#6528=CARTESIAN_POINT('Ctrl Pts',(6.45788118324589,2.52603925273079,23.1320039921066));
#6529=CARTESIAN_POINT('Ctrl Pts',(6.44202796275637,2.53851938447907,23.1307421789972));
#6530=CARTESIAN_POINT('Ctrl Pts',(6.41213395282259,2.56160146204964,23.1283912000536));
#6531=CARTESIAN_POINT('Ctrl Pts',(6.39812159526092,2.57223884468067,23.1273006599017));
#6532=CARTESIAN_POINT('Ctrl Pts',(6.37310663745903,2.59090788421063,23.1253737575749));
#6533=CARTESIAN_POINT('Ctrl Pts',(6.36213899432119,2.59898545152881,23.1245356140653));
#6534=CARTESIAN_POINT('Ctrl Pts',(6.33902427182084,2.6157842429427,23.1227830128144));
#6535=CARTESIAN_POINT('Ctrl Pts',(6.32686701665878,2.62449096504731,23.1218691285983));
#6536=CARTESIAN_POINT('Ctrl Pts',(6.29584075066423,2.64638611351152,23.119556496642));
#6537=CARTESIAN_POINT('Ctrl Pts',(6.27689002144462,2.65945769692104,23.1181622222351));
#6538=CARTESIAN_POINT('Ctrl Pts',(6.20367748751797,2.70880798764787,23.1128433709734));
#6539=CARTESIAN_POINT('Ctrl Pts',(6.14845619360334,2.74363962773884,23.1089727646797));
#6540=CARTESIAN_POINT('Ctrl Pts',(5.80390107549137,2.94661042703668,23.0855775644362));
#6541=CARTESIAN_POINT('Ctrl Pts',(5.49094578375706,3.07048929650484,23.0677513007489));
#6542=CARTESIAN_POINT('Ctrl Pts',(5.11892347952693,3.15427652898885,23.0456058484345));
#6543=CARTESIAN_POINT('Ctrl Pts',(5.07306742663107,3.16356006691765,23.042856109245));
#6544=CARTESIAN_POINT('Ctrl Pts',(4.99658974934862,3.17731706225886,23.0382129738546));
#6545=CARTESIAN_POINT('Ctrl Pts',(4.96607561566509,3.18235369947264,23.0363453939734));
#6546=CARTESIAN_POINT('Ctrl Pts',(4.92389204476934,3.18869425154179,23.0337371159028));
#6547=CARTESIAN_POINT('Ctrl Pts',(4.91227983416712,3.19037486883599,23.0330163559347));
#6548=CARTESIAN_POINT('Ctrl Pts',(4.89264555899072,3.19310712659352,23.0317926244979));
#6549=CARTESIAN_POINT('Ctrl Pts',(4.88462809798105,3.19419205681853,23.0312915051388));
#6550=CARTESIAN_POINT('Ctrl Pts',(4.86926857321914,3.19621165465521,23.0303286219528));
#6551=CARTESIAN_POINT('Ctrl Pts',(4.8619272506051,3.1971512369369,23.0298671563545));
#6552=CARTESIAN_POINT('Ctrl Pts',(4.84434195363117,3.19934035667021,23.0287589053283));
#6553=CARTESIAN_POINT('Ctrl Pts',(4.83409516099281,3.20056598424895,23.0281108136766));
#6554=CARTESIAN_POINT('Ctrl Pts',(4.79708590720555,3.20481249306297,23.0257620902968));
#6555=CARTESIAN_POINT('Ctrl Pts',(4.77029255667467,3.20754698371423,23.0240467068354));
#6556=CARTESIAN_POINT('Ctrl Pts',(4.57492799132225,3.22501445717925,23.0114450221691));
#6557=CARTESIAN_POINT('Ctrl Pts',(4.40547737372048,3.22678474942344,23.0000203398798));
#6558=CARTESIAN_POINT('Ctrl Pts',(4.08761659544302,3.20505725316384,22.9784672388896));
#6559=CARTESIAN_POINT('Ctrl Pts',(3.93942260627164,3.18451140987843,22.9683678690529));
#6560=CARTESIAN_POINT('Ctrl Pts',(3.67212488762544,3.12829420709448,22.9503392742126));
#6561=CARTESIAN_POINT('Ctrl Pts',(3.55262357440905,3.09588277850723,22.9423481048125));
#6562=CARTESIAN_POINT('Ctrl Pts',(3.40933195748334,3.04801068754464,22.9328596047883));
#6563=CARTESIAN_POINT('Ctrl Pts',(3.38350598342889,3.03901555949292,22.9311529781266));
#6564=CARTESIAN_POINT('Ctrl Pts',(3.34285383660536,3.02427367406246,22.9284715366918));
#6565=CARTESIAN_POINT('Ctrl Pts',(3.32795078624666,3.01874421577839,22.927489575792));
#6566=CARTESIAN_POINT('Ctrl Pts',(3.30003463698504,3.00815090011362,22.9256519602629));
#6567=CARTESIAN_POINT('Ctrl Pts',(3.28701240673154,3.00311231178834,22.924795487485));
#6568=CARTESIAN_POINT('Ctrl Pts',(3.2578264801945,2.99160100267817,22.9228773790739));
#6569=CARTESIAN_POINT('Ctrl Pts',(3.24168158459234,2.98508157341726,22.9218173392206));
#6570=CARTESIAN_POINT('Ctrl Pts',(3.20056633126299,2.9680901122468,22.9191198806092));
#6571=CARTESIAN_POINT('Ctrl Pts',(3.17567336787464,2.95743352224281,22.9174887073598));
#6572=CARTESIAN_POINT('Ctrl Pts',(3.00370981661835,2.88123800589189,22.906228150005));
#6573=CARTESIAN_POINT('Ctrl Pts',(2.86158830545213,2.80506803040446,22.8969775356826));
#6574=CARTESIAN_POINT('Ctrl Pts',(2.544564371737,2.6032416029654,22.8757741645235));
#6575=CARTESIAN_POINT('Ctrl Pts',(2.3753852105147,2.47008592096548,22.8640149364311));
#6576=CARTESIAN_POINT('Ctrl Pts',(2.16356480032044,2.26605482825328,22.8470253923365));
#6577=CARTESIAN_POINT('Ctrl Pts',(2.10846963840207,2.20891623524886,22.8423548082257));
#6578=CARTESIAN_POINT('Ctrl Pts',(2.04477740581955,2.13778418073868,22.8365564588816));
#6579=CARTESIAN_POINT('Ctrl Pts',(2.03410160835207,2.12567959524877,22.8355702764694));
#6580=CARTESIAN_POINT('Ctrl Pts',(2.01758292311321,2.10666410148685,22.8340209218618));
#6581=CARTESIAN_POINT('Ctrl Pts',(2.011677292993,2.09980771403798,22.8334622478071));
#6582=CARTESIAN_POINT('Ctrl Pts',(2.00069801171966,2.0869517557105,22.8324144681612));
#6583=CARTESIAN_POINT('Ctrl Pts',(1.99561735569461,2.08095842255152,22.8319258851611));
#6584=CARTESIAN_POINT('Ctrl Pts',(1.98405115664124,2.06721290710908,22.8308051150995));
#6585=CARTESIAN_POINT('Ctrl Pts',(1.97758013611835,2.05944875831949,22.8301719046903));
#6586=CARTESIAN_POINT('Ctrl Pts',(1.96043308584278,2.03867724710293,22.8284777872264));
#6587=CARTESIAN_POINT('Ctrl Pts',(1.94982239095783,2.02561668380669,22.8274124868013));
#6588=CARTESIAN_POINT('Ctrl Pts',(1.85700436846548,1.90952211707044,22.8179468613321));
#6589=CARTESIAN_POINT('Ctrl Pts',(1.78109635054655,1.80162830313741,22.8091804324976));
#6590=CARTESIAN_POINT('Ctrl Pts',(1.61492480762344,1.53168104685169,22.7878403079336));
#6591=CARTESIAN_POINT('Ctrl Pts',(1.53160504612944,1.36586921518023,22.7752183498749));
#6592=CARTESIAN_POINT('Ctrl Pts',(1.42930764846595,1.10935936764252,22.756907600032));
#6593=CARTESIAN_POINT('Ctrl Pts',(1.39921343571928,1.02351102889561,22.7509635488619));
#6594=CARTESIAN_POINT('Ctrl Pts',(1.36118430691327,0.898289561284954,22.7425688502952));
#6595=CARTESIAN_POINT('Ctrl Pts',(1.35029124254801,0.859867100264678,22.7400291929413));
#6596=CARTESIAN_POINT('Ctrl Pts',(1.33202552699521,0.790555204235873,22.7355114739159));
#6597=CARTESIAN_POINT('Ctrl Pts',(1.3243900999343,0.759741024881772,22.7335253060678));
#6598=CARTESIAN_POINT('Ctrl Pts',(1.31340444736956,0.712422226474213,22.7305083674589));
#6599=CARTESIAN_POINT('Ctrl Pts',(1.30972638013775,0.695996488163972,22.7294671460978));
#6600=CARTESIAN_POINT('Ctrl Pts',(1.30352618638333,0.667252998798782,22.7276554295386));
#6601=CARTESIAN_POINT('Ctrl Pts',(1.30094716564796,0.654948020704576,22.7268831307363));
#6602=CARTESIAN_POINT('Ctrl Pts',(1.29528109268812,0.627103577644397,22.7251428135002));
#6603=CARTESIAN_POINT('Ctrl Pts',(1.29223647376713,0.611555733953299,22.7241761651552));
#6604=CARTESIAN_POINT('Ctrl Pts',(1.28429407231168,0.5693485638147,22.7215654979395));
#6605=CARTESIAN_POINT('Ctrl Pts',(1.27961769371987,0.542648508570418,22.719928521869));
#6606=CARTESIAN_POINT('Ctrl Pts',(1.25861232981692,0.413121273881187,22.7120532666378));
#6607=CARTESIAN_POINT('Ctrl Pts',(1.24693488088784,0.309597115909877,22.7059625753096));
#6608=CARTESIAN_POINT('Ctrl Pts',(1.22309922846906,-0.0631150060972825,
22.6845068547967));
#6609=CARTESIAN_POINT('Ctrl Pts',(1.23967379372005,-0.332980062856612,22.6699329128804));
#6610=CARTESIAN_POINT('Ctrl Pts',(1.30564715605125,-0.682578152014254,22.6494563207962));
#6611=CARTESIAN_POINT('Ctrl Pts',(1.32508972884309,-0.76684569151032,22.6443844389545));
#6612=CARTESIAN_POINT('Ctrl Pts',(1.35224852690691,-0.866143539675064,22.6381358663738));
#6613=CARTESIAN_POINT('Ctrl Pts',(1.35672548134662,-0.882031444980441,22.6371276487459));
#6614=CARTESIAN_POINT('Ctrl Pts',(1.36386749809754,-0.906651084201533,22.6355512076021));
#6615=CARTESIAN_POINT('Ctrl Pts',(1.36644801963986,-0.915407327220928,22.6349877413193));
#6616=CARTESIAN_POINT('Ctrl Pts',(1.37131540556405,-0.931668264966201,22.633935952838));
#6617=CARTESIAN_POINT('Ctrl Pts',(1.37359250223412,-0.939175677202566,22.6334481959179));
#6618=CARTESIAN_POINT('Ctrl Pts',(1.37888074389968,-0.956384133657861,22.6323252297143));
#6619=CARTESIAN_POINT('Ctrl Pts',(1.38191034813374,-0.966079280127706,22.6316889670965));
#6620=CARTESIAN_POINT('Ctrl Pts',(1.39002068726323,-0.991608895626863,22.6300043572313));
#6621=CARTESIAN_POINT('Ctrl Pts',(1.39517816511764,-1.00741841101432,22.6289517986947));
#6622=CARTESIAN_POINT('Ctrl Pts',(1.43674560697618,-1.13157029147617,22.6206162147378));
#6623=CARTESIAN_POINT('Ctrl Pts',(1.47877010224343,-1.23793555430004,22.6130570289752));
#6624=CARTESIAN_POINT('Ctrl Pts',(1.59844683068817,-1.49927018963793,22.5937779688046));
#6625=CARTESIAN_POINT('Ctrl Pts',(1.68311679716082,-1.6506430934314,22.5819647930069));
#6626=CARTESIAN_POINT('Ctrl Pts',(1.86334364871756,-1.91949702857235,22.5603320580885));
#6627=CARTESIAN_POINT('Ctrl Pts',(1.95580873112871,-2.03849871830021,22.550477276464));
#6628=CARTESIAN_POINT('Ctrl Pts',(2.08174172089787,-2.17904675773991,22.538527634413));
#6629=CARTESIAN_POINT('Ctrl Pts',(2.10772107653243,-2.20702465349966,22.5361311741812));
#6630=CARTESIAN_POINT('Ctrl Pts',(2.14674754234381,-2.24758353535667,22.5326291537913));
#6631=CARTESIAN_POINT('Ctrl Pts',(2.15941269267318,-2.26052589135035,22.5315073136945));
#6632=CARTESIAN_POINT('Ctrl Pts',(2.18208772346199,-2.28330985685264,22.5295243610722));
#6633=CARTESIAN_POINT('Ctrl Pts',(2.19205399567784,-2.29319401570863,22.5286613687559));
#6634=CARTESIAN_POINT('Ctrl Pts',(2.21314708876907,-2.31384172537308,22.526852612463));
#6635=CARTESIAN_POINT('Ctrl Pts',(2.22428755373985,-2.32459087452439,22.5259074899587));
#6636=CARTESIAN_POINT('Ctrl Pts',(2.25394372076184,-2.35279556750469,22.5234179454305));
#6637=CARTESIAN_POINT('Ctrl Pts',(2.27258967899555,-2.37011302683431,22.5218794679856));
#6638=CARTESIAN_POINT('Ctrl Pts',(2.35512792653043,-2.44496941042161,22.5151822613708));
#6639=CARTESIAN_POINT('Ctrl Pts',(2.42110612888967,-2.50016191562204,22.5101214905855));
#6640=CARTESIAN_POINT('Ctrl Pts',(2.67123371974969,-2.69292758761975,22.4918365526643));
#6641=CARTESIAN_POINT('Ctrl Pts',(2.86772546851955,-2.81332900681846,22.4792188084483));
#6642=CARTESIAN_POINT('Ctrl Pts',(3.20560327854733,-2.97358929848789,22.4581436942687));
#6643=CARTESIAN_POINT('Ctrl Pts',(3.33983383040673,-3.02655147521524,22.4498958437639));
#6644=CARTESIAN_POINT('Ctrl Pts',(3.49454632389235,-3.07589921555084,22.4400613858485));
#6645=CARTESIAN_POINT('Ctrl Pts',(3.51200055550013,-3.08130338405846,22.4389472594558));
#6646=CARTESIAN_POINT('Ctrl Pts',(3.53860047828569,-3.08929199756158,22.4372409995548));
#6647=CARTESIAN_POINT('Ctrl Pts',(3.54771353621437,-3.09198498911904,22.4366549572409));
#6648=CARTESIAN_POINT('Ctrl Pts',(3.56434541547401,-3.09681998241459,22.4355824712363));
#6649=CARTESIAN_POINT('Ctrl Pts',(3.57186025092031,-3.09897496808296,22.4350967863488));
#6650=CARTESIAN_POINT('Ctrl Pts',(3.58870562528697,-3.10373935265144,22.4340055983626));
#6651=CARTESIAN_POINT('Ctrl Pts',(3.59804004512471,-3.10633400801682,22.433399275725));
#6652=CARTESIAN_POINT('Ctrl Pts',(3.6253140676919,-3.11378294999352,22.4316230988031));
#6653=CARTESIAN_POINT('Ctrl Pts',(3.64328378947108,-3.1185240997136,22.4304470859493));
#6654=CARTESIAN_POINT('Ctrl Pts',(3.81317022196487,-3.16177894966179,22.4192812796471));
#6655=CARTESIAN_POINT('Ctrl Pts',(3.96764951185471,-3.18931401920795,22.4087785785176));
#6656=CARTESIAN_POINT('Ctrl Pts',(4.40187603116108,-3.234419180028,22.3792887450694));
#6657=CARTESIAN_POINT('Ctrl Pts',(4.68289869584216,-3.2269549758532,22.3603596064908));
#6658=CARTESIAN_POINT('Ctrl Pts',(4.99781640975944,-3.17719518399707,22.340161950366));
#6659=CARTESIAN_POINT('Ctrl Pts',(5.0360694071743,-3.17044000781401,22.3377229769926));
#6660=CARTESIAN_POINT('Ctrl Pts',(5.09208672285232,-3.15949999688685,22.334171231863));
#6661=CARTESIAN_POINT('Ctrl Pts',(5.10995142454861,-3.15585342917296,22.3330415090427));
#6662=CARTESIAN_POINT('Ctrl Pts',(5.1415282961356,-3.14912828068964,22.3310496692376));
#6663=CARTESIAN_POINT('Ctrl Pts',(5.1552529529293,-3.14611127702715,22.3301856131744));
#6664=CARTESIAN_POINT('Ctrl Pts',(5.18399301652166,-3.13959618468013,22.3283795956119));
#6665=CARTESIAN_POINT('Ctrl Pts',(5.19900396946497,-3.13607991491364,22.3274382405512));
#6666=CARTESIAN_POINT('Ctrl Pts',(5.23844099492223,-3.12654287950546,22.3249698421697));
#6667=CARTESIAN_POINT('Ctrl Pts',(5.26282310449792,-3.12034352215674,22.3234485597827));
#6668=CARTESIAN_POINT('Ctrl Pts',(5.36760289800328,-3.09239217888041,22.3169289563497));
#6669=CARTESIAN_POINT('Ctrl Pts',(5.44721705513011,-3.06781264097421,22.3120221268178));
#6670=CARTESIAN_POINT('Ctrl Pts',(5.74479433618588,-2.96314527865529,22.2937338165805));
#6671=CARTESIAN_POINT('Ctrl Pts',(5.95482415443133,-2.86268168304686,22.2809869827984));
#6672=CARTESIAN_POINT('Ctrl Pts',(6.27558666625827,-2.66420113742317,22.2597335331932));
#6673=CARTESIAN_POINT('Ctrl Pts',(6.39362236700104,-2.57964784707828,22.2514378014791));
#6674=CARTESIAN_POINT('Ctrl Pts',(6.51966205056492,-2.47582043721844,22.2415486800561));
#6675=CARTESIAN_POINT('Ctrl Pts',(6.53367680368052,-2.46407388464559,22.2404336692325));
#6676=CARTESIAN_POINT('Ctrl Pts',(6.55482339236202,-2.44604113016822,22.2387263342749));
#6677=CARTESIAN_POINT('Ctrl Pts',(6.56202889477642,-2.43984136616794,22.2381401132628));
#6678=CARTESIAN_POINT('Ctrl Pts',(6.57511025561722,-2.42848478701234,22.2370674593006));
#6679=CARTESIAN_POINT('Ctrl Pts',(6.58099488163586,-2.42333838059769,22.2365817866953));
#6680=CARTESIAN_POINT('Ctrl Pts',(6.59412784798021,-2.41176832750362,22.23549082747));
#6681=CARTESIAN_POINT('Ctrl Pts',(6.60136592252056,-2.40533344953659,22.2348847229809));
#6682=CARTESIAN_POINT('Ctrl Pts',(6.62239675839439,-2.38646596035163,22.2331097613032));
#6683=CARTESIAN_POINT('Ctrl Pts',(6.63611094039606,-2.37394688468426,22.2319347578213));
#6684=CARTESIAN_POINT('Ctrl Pts',(6.75506206696603,-2.26346197338259,22.221594619939));
#6685=CARTESIAN_POINT('Ctrl Pts',(6.85373091292243,-2.15868391139478,22.2119966297143));
#6686=CARTESIAN_POINT('Ctrl Pts',(7.1236822730977,-1.83060606387584,22.1833402296544));
#6687=CARTESIAN_POINT('Ctrl Pts',(7.27316871492922,-1.59103939593297,22.164247297868));
#6688=CARTESIAN_POINT('Ctrl Pts',(7.40908317398408,-1.29243325749105,22.1433548892878));
#6689=CARTESIAN_POINT('Ctrl Pts',(7.42756459086342,-1.24936205723947,22.1404017610917));
#6690=CARTESIAN_POINT('Ctrl Pts',(7.45244975772723,-1.18768818246058,22.1362560437119));
#6691=CARTESIAN_POINT('Ctrl Pts',(7.45963212804002,-1.16940804457714,22.1350373995376));
#6692=CARTESIAN_POINT('Ctrl Pts',(7.471744889861,-1.13773161435172,22.1329428293128));
#6693=CARTESIAN_POINT('Ctrl Pts',(7.47675415114854,-1.12436628173937,22.1320642826363));
#6694=CARTESIAN_POINT('Ctrl Pts',(7.4861932591141,-1.09866325329039,22.1303845649077));
#6695=CARTESIAN_POINT('Ctrl Pts',(7.49063693466362,-1.08633097331331,22.1295829475777));
#6696=CARTESIAN_POINT('Ctrl Pts',(7.50092387874953,-1.05722662207765,22.1277010633123));
#6697=CARTESIAN_POINT('Ctrl Pts',(7.50670402697339,-1.04043257355392,22.1266228975944));
#6698=CARTESIAN_POINT('Ctrl Pts',(7.52638612418755,-0.981672747244577,22.1228767092465));
#6699=CARTESIAN_POINT('Ctrl Pts',(7.53956357991476,-0.939468269751344,22.1202323800905));
#6700=CARTESIAN_POINT('Ctrl Pts',(7.63634895762852,-0.605479453082931,22.0996355702265));
#6701=CARTESIAN_POINT('Ctrl Pts',(7.67921910621616,-0.303509123726089,22.0831558719124));
#6702=CARTESIAN_POINT('Ctrl Pts',(7.67921910621823,-2.19652074306964E-11,
22.0659612921829));
#6703=CARTESIAN_POINT('Origin',(4.45646910621825,-5.13094777615093E-16,
-2.31077344927308));
#6704=CARTESIAN_POINT('',(7.67921910621823,-1.24761686023381E-10,20.8155686056964));
#6705=CARTESIAN_POINT('',(7.67921910621823,2.36916961325777E-11,21.0595336661193));
#6706=CARTESIAN_POINT('',(7.67921910621823,-3.51191647465084E-13,-2.31077344927308));
#6707=CARTESIAN_POINT('Ctrl Pts',(7.67921910621823,2.36916961325777E-11,
21.0595336661193));
#6708=CARTESIAN_POINT('Ctrl Pts',(7.67921910621822,-0.0894454910351407,
21.0655592747916));
#6709=CARTESIAN_POINT('Ctrl Pts',(7.67549535737132,-0.178852116290269,21.0716247501547));
#6710=CARTESIAN_POINT('Ctrl Pts',(7.65085338500985,-0.47416340077961,21.0916381005274));
#6711=CARTESIAN_POINT('Ctrl Pts',(7.61383322363013,-0.678232801453661,21.1053943607614));
#6712=CARTESIAN_POINT('Ctrl Pts',(7.54610867038377,-0.917601779018526,21.1211849998897));
#6713=CARTESIAN_POINT('Ctrl Pts',(7.53394389311208,-0.957608929184082,21.1238140557288));
#6714=CARTESIAN_POINT('Ctrl Pts',(7.51525570954617,-1.01503055376256,21.127574415035));
#6715=CARTESIAN_POINT('Ctrl Pts',(7.50935519689536,-1.03264178216326,21.1287259328489));
#6716=CARTESIAN_POINT('Ctrl Pts',(7.49869163720208,-1.06357879489786,21.1307458908836));
#6717=CARTESIAN_POINT('Ctrl Pts',(7.49399249617127,-1.07692592438826,21.1316164115736));
#6718=CARTESIAN_POINT('Ctrl Pts',(7.48408836325053,-1.10447634813449,21.1334115044832));
#6719=CARTESIAN_POINT('Ctrl Pts',(7.47887096463145,-1.11867483552624,21.1343356396432));
#6720=CARTESIAN_POINT('Ctrl Pts',(7.46518053903198,-1.15513656798424,21.1367065737599));
#6721=CARTESIAN_POINT('Ctrl Pts',(7.45656020364345,-1.1773438029629,21.1381484314018));
#6722=CARTESIAN_POINT('Ctrl Pts',(7.41836543690256,-1.27259477372468,21.1443258095959));
#6723=CARTESIAN_POINT('Ctrl Pts',(7.38636233326804,-1.34463916919134,21.1489793599));
#6724=CARTESIAN_POINT('Ctrl Pts',(7.29112616054644,-1.53944418116927,21.1615863163779));
#6725=CARTESIAN_POINT('Ctrl Pts',(7.222597558429,-1.65942956209022,21.1693730409075));
#6726=CARTESIAN_POINT('Ctrl Pts',(7.02631843218325,-1.95695932259459,21.1893377020436));
#6727=CARTESIAN_POINT('Ctrl Pts',(6.88784907837612,-2.12654272502494,21.2013650111882));
#6728=CARTESIAN_POINT('Ctrl Pts',(6.70683449527531,-2.30724378010995,21.2165516493302));
#6729=CARTESIAN_POINT('Ctrl Pts',(6.6798903114792,-2.33322011720834,21.2188009880095));
#6730=CARTESIAN_POINT('Ctrl Pts',(6.6429474989928,-2.36761487407249,21.2218803009897));
#6731=CARTESIAN_POINT('Ctrl Pts',(6.63333998719551,-2.37645136876482,21.2226807020673));
#6732=CARTESIAN_POINT('Ctrl Pts',(6.61810042741656,-2.39029797529074,21.2239501566707));
#6733=CARTESIAN_POINT('Ctrl Pts',(6.61250390650538,-2.39534722257058,21.2244163146513));
#6734=CARTESIAN_POINT('Ctrl Pts',(6.60093970677717,-2.40570721898283,21.2253796072465));
#6735=CARTESIAN_POINT('Ctrl Pts',(6.59496997749778,-2.41101542884926,21.2258769315176));
#6736=CARTESIAN_POINT('Ctrl Pts',(6.58059567866102,-2.42370149521078,21.2270744274556));
#6737=CARTESIAN_POINT('Ctrl Pts',(6.57217236120537,-2.43105786886688,21.2277761573094));
#6738=CARTESIAN_POINT('Ctrl Pts',(6.54299151151208,-2.45627598917897,21.2302066292236));
#6739=CARTESIAN_POINT('Ctrl Pts',(6.5220453528253,-2.47391635597328,21.231950317318));
#6740=CARTESIAN_POINT('Ctrl Pts',(6.47015241808022,-2.51650091854812,21.2362626328236));
#6741=CARTESIAN_POINT('Ctrl Pts',(6.43896460881141,-2.54114317711107,21.2388478855091));
#6742=CARTESIAN_POINT('Ctrl Pts',(6.30940305325885,-2.63967605003347,21.2495354859299));
#6743=CARTESIAN_POINT('Ctrl Pts',(6.20729682729648,-2.70847791366628,21.2578340162899));
#6744=CARTESIAN_POINT('Ctrl Pts',(5.8778325078872,-2.90405024984104,21.2837479604227));
#6745=CARTESIAN_POINT('Ctrl Pts',(5.63885164786643,-3.00928612023419,21.3012537384686));
#6746=CARTESIAN_POINT('Ctrl Pts',(5.35211587014347,-3.09604315387601,21.3202384389464));
#6747=CARTESIAN_POINT('Ctrl Pts',(5.31424098962029,-3.10674974091398,21.3227102895318));
#6748=CARTESIAN_POINT('Ctrl Pts',(5.25864212906571,-3.12137225987302,21.3262882427625));
#6749=CARTESIAN_POINT('Ctrl Pts',(5.24106726070012,-3.12583622424566,21.3274119285351));
#6750=CARTESIAN_POINT('Ctrl Pts',(5.20977818947903,-3.1335030371891,21.3293997703925));
#6751=CARTESIAN_POINT('Ctrl Pts',(5.1960790307242,-3.13676473911685,21.3302658005443));
#6752=CARTESIAN_POINT('Ctrl Pts',(5.16743269590826,-3.14338719069717,21.3320679753663));
#6753=CARTESIAN_POINT('Ctrl Pts',(5.15248202146617,-3.14673136619804,21.3330035692662));
#6754=CARTESIAN_POINT('Ctrl Pts',(5.11335845295876,-3.15519007412421,21.3354392348696));
#6755=CARTESIAN_POINT('Ctrl Pts',(5.0891493032062,-3.16013351583897,21.3369338268248));
#6756=CARTESIAN_POINT('Ctrl Pts',(4.97856444449615,-3.18139288246952,21.3437066779751));
#6757=CARTESIAN_POINT('Ctrl Pts',(4.89159611255751,-3.19444998641969,21.3488813123645));
#6758=CARTESIAN_POINT('Ctrl Pts',(4.53099757776638,-3.23358622794944,21.3698795915762));
#6759=CARTESIAN_POINT('Ctrl Pts',(4.25515117475932,-3.22817197185011,21.3847631102892));
#6760=CARTESIAN_POINT('Ctrl Pts',(3.95846915963551,-3.18413977105302,21.4019122577136));
#6761=CARTESIAN_POINT('Ctrl Pts',(3.93363729602362,-3.18015673820093,21.4033573875573));
#6762=CARTESIAN_POINT('Ctrl Pts',(3.83366412538272,-3.16291847664373,21.4092237497656));
#6763=CARTESIAN_POINT('Ctrl Pts',(3.75896354248865,-3.14728825433992,21.4137173148762));
#6764=CARTESIAN_POINT('Ctrl Pts',(3.6688682437167,-3.12507198372703,21.4193482724277));
#6765=CARTESIAN_POINT('Ctrl Pts',(3.65287292847748,-3.12099714494885,21.4203561909509));
#6766=CARTESIAN_POINT('Ctrl Pts',(3.62798401336539,-3.11445263178789,21.4219383589673));
#6767=CARTESIAN_POINT('Ctrl Pts',(3.61906826906285,-3.11206725147489,21.4225079054173));
#6768=CARTESIAN_POINT('Ctrl Pts',(3.60260332888467,-3.10758623029718,21.4235650561599));
#6769=CARTESIAN_POINT('Ctrl Pts',(3.59505141809514,-3.1055013293777,21.4240520423586));
#6770=CARTESIAN_POINT('Ctrl Pts',(3.57785946651129,-3.10068751080452,21.4251654496892));
#6771=CARTESIAN_POINT('Ctrl Pts',(3.56822454399584,-3.09794117600695,21.4257928551082));
#6772=CARTESIAN_POINT('Ctrl Pts',(3.53859031269174,-3.08934463637538,21.4277327700116));
#6773=CARTESIAN_POINT('Ctrl Pts',(3.5186352652549,-3.0833454875905,21.4290534079612));
#6774=CARTESIAN_POINT('Ctrl Pts',(3.47217292080582,-3.06888461610578,21.4321596364767));
#6775=CARTESIAN_POINT('Ctrl Pts',(3.44571455669976,-3.06027235690635,21.4339524883671));
#6776=CARTESIAN_POINT('Ctrl Pts',(3.35292308249869,-3.02873393904662,21.4403170890623));
#6777=CARTESIAN_POINT('Ctrl Pts',(3.28723359685712,-3.00398572042259,21.4449620019285));
#6778=CARTESIAN_POINT('Ctrl Pts',(3.02360682805531,-2.89470831696087,21.4640416878018));
#6779=CARTESIAN_POINT('Ctrl Pts',(2.83354117659888,-2.79258758091511,21.4787801662447));
#6780=CARTESIAN_POINT('Ctrl Pts',(2.54241612605463,-2.5963394411612,21.5020622783845));
#6781=CARTESIAN_POINT('Ctrl Pts',(2.4346605484506,-2.51333957911612,21.5108752289492));
#6782=CARTESIAN_POINT('Ctrl Pts',(2.31085882361731,-2.4048489757991,21.5212284748952));
#6783=CARTESIAN_POINT('Ctrl Pts',(2.28951655508618,-2.38563593368456,21.5230225235111));
#6784=CARTESIAN_POINT('Ctrl Pts',(2.25641861588488,-2.35502934090511,21.5258201889696));
#6785=CARTESIAN_POINT('Ctrl Pts',(2.24448850554569,-2.34382746689756,21.5268318381654));
#6786=CARTESIAN_POINT('Ctrl Pts',(2.22357001165559,-2.32388389911429,21.5286116461956));
#6787=CARTESIAN_POINT('Ctrl Pts',(2.2145464253113,-2.31517978630887,21.5293813960359));
#6788=CARTESIAN_POINT('Ctrl Pts',(2.19395062645879,-2.29507983716735,21.5311430550137));
#6789=CARTESIAN_POINT('Ctrl Pts',(2.18241324388054,-2.28364867706766,21.532133395554));
#6790=CARTESIAN_POINT('Ctrl Pts',(2.15055942767161,-2.25160733954792,21.5348778668066));
#6791=CARTESIAN_POINT('Ctrl Pts',(2.13043314104628,-2.23080968000344,21.5366236516257));
#6792=CARTESIAN_POINT('Ctrl Pts',(2.00284300402277,-2.09535903842841,21.547774270745));
#6793=CARTESIAN_POINT('Ctrl Pts',(1.90359990188212,-1.97324057836944,21.5568202207237));
#6794=CARTESIAN_POINT('Ctrl Pts',(1.72959015113515,-1.7238982203473,21.573998039871));
#6795=CARTESIAN_POINT('Ctrl Pts',(1.65386141776108,-1.59783721366861,21.5821335627164));
#6796=CARTESIAN_POINT('Ctrl Pts',(1.51940519627895,-1.33484802773763,21.5987599413172));
#6797=CARTESIAN_POINT('Ctrl Pts',(1.46104025906988,-1.19814793962146,21.6072366142313));
#6798=CARTESIAN_POINT('Ctrl Pts',(1.40621283385749,-1.040384239427,21.6173446317372));
#6799=CARTESIAN_POINT('Ctrl Pts',(1.40026635069164,-1.02278412810262,21.6184767573136));
#6800=CARTESIAN_POINT('Ctrl Pts',(1.39145111896337,-0.995929790645079,21.6202123511876));
#6801=CARTESIAN_POINT('Ctrl Pts',(1.38847127691293,-0.986712077442884,21.6208095512638));
#6802=CARTESIAN_POINT('Ctrl Pts',(1.38316161464555,-0.97003080218331,21.621893173514));
#6803=CARTESIAN_POINT('Ctrl Pts',(1.38081734729296,-0.962572049203439,21.6223787447266));
#6804=CARTESIAN_POINT('Ctrl Pts',(1.37568311791045,-0.946026221909996,21.6234582388265));
#6805=CARTESIAN_POINT('Ctrl Pts',(1.37290623901174,-0.936935406975188,21.6240528880964));
#6806=CARTESIAN_POINT('Ctrl Pts',(1.36490598090118,-0.910323717797833,21.6257978371717));
#6807=CARTESIAN_POINT('Ctrl Pts',(1.35979153204007,-0.892770852123789,21.6269541281712));
#6808=CARTESIAN_POINT('Ctrl Pts',(1.31552139319692,-0.73587652615707,21.6373311068377));
#6809=CARTESIAN_POINT('Ctrl Pts',(1.28564910399624,-0.594102511906308,21.646992972663));
#6810=CARTESIAN_POINT('Ctrl Pts',(1.23304972865414,-0.221785400111993,21.6723549792319));
#6811=CARTESIAN_POINT('Ctrl Pts',(1.22544067477768,0.0101004426984798,21.6880895363299));
#6812=CARTESIAN_POINT('Ctrl Pts',(1.24901447328468,0.324695961601183,21.7085949282752));
#6813=CARTESIAN_POINT('Ctrl Pts',(1.25858162227676,0.40830187080147,21.7139706268327));
#6814=CARTESIAN_POINT('Ctrl Pts',(1.27526938171719,0.516455552410367,21.720831495374));
#6815=CARTESIAN_POINT('Ctrl Pts',(1.27942311766867,0.541421157809245,21.7224088106833));
#6816=CARTESIAN_POINT('Ctrl Pts',(1.28658581201005,0.581546384167389,21.7249341213125));
#6817=CARTESIAN_POINT('Ctrl Pts',(1.28941041419239,0.596737421631965,21.7258879144106));
#6818=CARTESIAN_POINT('Ctrl Pts',(1.29501097510969,0.625697462857361,21.7277020814093));
#6819=CARTESIAN_POINT('Ctrl Pts',(1.29776790337114,0.639469741876472,21.7285630375081));
#6820=CARTESIAN_POINT('Ctrl Pts',(1.30429766848937,0.671016341099972,21.7305312245234));
#6821=CARTESIAN_POINT('Ctrl Pts',(1.30813098596696,0.688777761266104,21.7316365005493));
#6822=CARTESIAN_POINT('Ctrl Pts',(1.32055441664901,0.744069107095733,21.7350690100018));
#6823=CARTESIAN_POINT('Ctrl Pts',(1.32966713815272,0.781478994718531,21.7373795361948));
#6824=CARTESIAN_POINT('Ctrl Pts',(1.37833664070143,0.966773416103719,21.7487775609975));
#6825=CARTESIAN_POINT('Ctrl Pts',(1.42772616266441,1.11187869866018,21.7575435006204));
#6826=CARTESIAN_POINT('Ctrl Pts',(1.58826818280931,1.49233236978607,21.7808127820048));
#6827=CARTESIAN_POINT('Ctrl Pts',(1.71785298017699,1.71859785588417,21.7949288367245));
#6828=CARTESIAN_POINT('Ctrl Pts',(1.8942320225445,1.95507044815074,21.8124780230518));
#6829=CARTESIAN_POINT('Ctrl Pts',(1.91576151570319,1.98296849161809,21.8145987811537));
#6830=CARTESIAN_POINT('Ctrl Pts',(1.94569545738399,2.02046918814093,21.8175274985888));
#6831=CARTESIAN_POINT('Ctrl Pts',(1.9537067162284,2.03038431401583,21.8183094403864));
#6832=CARTESIAN_POINT('Ctrl Pts',(1.96651026687984,2.04603969996539,21.8195566563613));
#6833=CARTESIAN_POINT('Ctrl Pts',(1.97126417698393,2.0518113783838,21.8200192091416));
#6834=CARTESIAN_POINT('Ctrl Pts',(1.98116414620967,2.06374595847814,21.8209814930568));
#6835=CARTESIAN_POINT('Ctrl Pts',(1.98631317191332,2.06990620101082,21.8214814540787));
#6836=CARTESIAN_POINT('Ctrl Pts',(1.99883438458165,2.08477320014454,21.822695848065));
#6837=CARTESIAN_POINT('Ctrl Pts',(2.00622985554705,2.09346013248053,21.8234119510475));
#6838=CARTESIAN_POINT('Ctrl Pts',(2.03245383391905,2.12393425508118,21.8259465838964));
#6839=CARTESIAN_POINT('Ctrl Pts',(2.05152745412194,2.14550746360978,21.8277817803363));
#6840=CARTESIAN_POINT('Ctrl Pts',(2.09946087266566,2.19828021194679,21.8323671820227));
#6841=CARTESIAN_POINT('Ctrl Pts',(2.12865310768617,2.22916935986334,21.8351366945353));
#6842=CARTESIAN_POINT('Ctrl Pts',(2.25526601364536,2.35794260166899,21.847019801996));
#6843=CARTESIAN_POINT('Ctrl Pts',(2.35831015677296,2.45008438041535,21.8563705800867));
#6844=CARTESIAN_POINT('Ctrl Pts',(2.65408776794743,2.68218776490518,21.8818052850557));
#6845=CARTESIAN_POINT('Ctrl Pts',(2.85695405217752,2.80789952646256,21.8977370870686));
#6846=CARTESIAN_POINT('Ctrl Pts',(3.10883363862467,2.92774218726787,21.9154330318392));
#6847=CARTESIAN_POINT('Ctrl Pts',(3.14615824177829,2.94463603105719,21.9180079327265));
#6848=CARTESIAN_POINT('Ctrl Pts',(3.20072188468266,2.96808960208253,21.9217056011462));
#6849=CARTESIAN_POINT('Ctrl Pts',(3.21770988823403,2.97521975538536,21.9228476573256));
#6850=CARTESIAN_POINT('Ctrl Pts',(3.24782988275535,2.98755892487783,21.9248566463485));
#6851=CARTESIAN_POINT('Ctrl Pts',(3.26093660661545,2.99282795272288,21.9257255892417));
#6852=CARTESIAN_POINT('Ctrl Pts',(3.2882071600684,3.00358324039593,21.9275228297402));
#6853=CARTESIAN_POINT('Ctrl Pts',(3.30237600513869,3.00905589566496,21.9284506529152));
#6854=CARTESIAN_POINT('Ctrl Pts',(3.33913167830573,3.02295480789258,21.9308424726539));
#6855=CARTESIAN_POINT('Ctrl Pts',(3.36177556497799,3.03122826547182,21.9323013563788));
#6856=CARTESIAN_POINT('Ctrl Pts',(3.46148456705871,3.06639615675739,21.938663949643));
#6857=CARTESIAN_POINT('Ctrl Pts',(3.53946620878464,3.09061271400874,21.9434792585718));
#6858=CARTESIAN_POINT('Ctrl Pts',(3.75926544729736,3.14981603179832,21.9566958957305));
#6859=CARTESIAN_POINT('Ctrl Pts',(3.90266692027411,3.17816637382334,21.9649080721699));
#6860=CARTESIAN_POINT('Ctrl Pts',(4.26975206053431,3.22512905950818,21.9856162192215));
#6861=CARTESIAN_POINT('Ctrl Pts',(4.49432918449552,3.23030322141188,21.9979845982489));
#6862=CARTESIAN_POINT('Ctrl Pts',(4.74234183679792,3.21014190544409,22.0129333669061));
#6863=CARTESIAN_POINT('Ctrl Pts',(4.76706886993191,3.20784381987485,22.0144384806114));
#6864=CARTESIAN_POINT('Ctrl Pts',(4.80169248772744,3.20422190126414,22.0165697153987));
#6865=CARTESIAN_POINT('Ctrl Pts',(4.81161393414145,3.20313741834048,22.0171831609168));
#6866=CARTESIAN_POINT('Ctrl Pts',(4.82879782551084,3.20117828224483,22.0182506384496));
#6867=CARTESIAN_POINT('Ctrl Pts',(4.83606269285441,3.20032494856243,22.0187034866824));
#6868=CARTESIAN_POINT('Ctrl Pts',(4.85144942568593,3.19846448927855,22.0196660050579));
#6869=CARTESIAN_POINT('Ctrl Pts',(4.85957044359388,3.19745114888469,22.0201760306036));
#6870=CARTESIAN_POINT('Ctrl Pts',(4.87978011043599,3.19485117188573,22.0214501310605));
#6871=CARTESIAN_POINT('Ctrl Pts',(4.89186368327318,3.1932268581928,22.0222162719655));
#6872=CARTESIAN_POINT('Ctrl Pts',(4.9377573612177,3.18679234397094,22.0251418639114));
#6873=CARTESIAN_POINT('Ctrl Pts',(4.97149814749713,3.18151358584001,22.0273253121985));
#6874=CARTESIAN_POINT('Ctrl Pts',(5.05793222290102,3.16658003655403,22.0329917053537));
#6875=CARTESIAN_POINT('Ctrl Pts',(5.11047900795235,3.15614597707446,22.0365066121112));
#6876=CARTESIAN_POINT('Ctrl Pts',(5.37600886758146,3.09650499856864,22.0545486725428));
#6877=CARTESIAN_POINT('Ctrl Pts',(5.58385238359823,3.02702960087466,22.0695478175534));
#6878=CARTESIAN_POINT('Ctrl Pts',(5.9260116787953,2.872483857061,22.0945969601111));
#6879=CARTESIAN_POINT('Ctrl Pts',(6.06406677136233,2.79756344843145,22.1048268122199));
#6880=CARTESIAN_POINT('Ctrl Pts',(6.22077774984749,2.69707056955922,22.1165432524591));
#6881=CARTESIAN_POINT('Ctrl Pts',(6.24520609819517,2.68093168722429,22.1183733665403));
#6882=CARTESIAN_POINT('Ctrl Pts',(6.28314942412115,2.65511443686881,22.1212226677672));
#6883=CARTESIAN_POINT('Ctrl Pts',(6.29681474923133,2.64566089804919,22.1222502352182));
#6884=CARTESIAN_POINT('Ctrl Pts',(6.32152865269249,2.62827991960129,22.1241113656387));
#6885=CARTESIAN_POINT('Ctrl Pts',(6.33260126592329,2.62038748584474,22.1249462343892));
#6886=CARTESIAN_POINT('Ctrl Pts',(6.34399004651055,2.61216049787625,22.1258060860518));
#6887=CARTESIAN_POINT('Ctrl Pts',(6.34435630426618,2.61189580461282,22.1258337397009));
#6888=CARTESIAN_POINT('Ctrl Pts',(6.34504919044514,2.61139483618877,22.1258860571886));
#6889=CARTESIAN_POINT('Ctrl Pts',(6.34537583019483,2.61115857678696,22.1259107216306));
#6890=CARTESIAN_POINT('Ctrl Pts',(6.3459960143008,2.61070981869984,22.1259575533618));
#6891=CARTESIAN_POINT('Ctrl Pts',(6.34628956714124,2.61049733179346,22.125979721103));
#6892=CARTESIAN_POINT('Ctrl Pts',(6.3468486986376,2.61009246322941,22.1260219456231));
#6893=CARTESIAN_POINT('Ctrl Pts',(6.34711428377475,2.60990009054467,22.1260420027471));
#6894=CARTESIAN_POINT('Ctrl Pts',(6.34762155982898,2.60953253453672,22.1260803137403));
#6895=CARTESIAN_POINT('Ctrl Pts',(6.3478632557635,2.60935735817646,22.1260985678763));
#6896=CARTESIAN_POINT('Ctrl Pts',(6.34832605018759,2.60902183598569,22.1261335215613));
#6897=CARTESIAN_POINT('Ctrl Pts',(6.34854715262481,2.60886149563399,22.12615022132));
#6898=CARTESIAN_POINT('Ctrl Pts',(6.34897145727519,2.60855371360722,22.1261822697158));
#6899=CARTESIAN_POINT('Ctrl Pts',(6.34917466262908,2.60840627630392,22.1261976185194));
#6900=CARTESIAN_POINT('Ctrl Pts',(6.34956540418965,2.60812270087323,22.1262271333225));
#6901=CARTESIAN_POINT('Ctrl Pts',(6.34975294294202,2.60798656626216,22.1262412994573));
#6902=CARTESIAN_POINT('Ctrl Pts',(6.35011421497847,2.60772425894134,22.1262685895347));
#6903=CARTESIAN_POINT('Ctrl Pts',(6.35028795033722,2.60759808909706,22.1262817135877));
#6904=CARTESIAN_POINT('Ctrl Pts',(6.35062318612198,2.60735458346847,22.1263070380061));
#6905=CARTESIAN_POINT('Ctrl Pts',(6.35078468826022,2.60723725003747,22.1263192384625));
#6906=CARTESIAN_POINT('Ctrl Pts',(6.35109679167411,2.60701045848802,22.1263428163573));
#6907=CARTESIAN_POINT('Ctrl Pts',(6.35124739435295,2.60690100233497,22.1263541938698));
#6908=CARTESIAN_POINT('Ctrl Pts',(6.35153884022466,2.60668914450413,22.1263762120114));
#6909=CARTESIAN_POINT('Ctrl Pts',(6.35167968461711,2.60658674445104,22.1263868527045));
#6910=CARTESIAN_POINT('Ctrl Pts',(6.35195259690634,2.60638829142875,22.1264074713941));
#6911=CARTESIAN_POINT('Ctrl Pts',(6.35208466580213,2.60629223983641,22.1264174494436));
#6912=CARTESIAN_POINT('Ctrl Pts',(6.35234087880805,2.60610587044467,22.1264368071289));
#6913=CARTESIAN_POINT('Ctrl Pts',(6.35246502374482,2.60601555382763,22.1264461868081));
#6914=CARTESIAN_POINT('Ctrl Pts',(6.35270613085828,2.60584011977123,22.1264644037604));
#6915=CARTESIAN_POINT('Ctrl Pts',(6.35282309375787,2.60575500332775,22.1264732410718));
#6916=CARTESIAN_POINT('Ctrl Pts',(6.36701439829685,2.59542622110449,22.1275455025337));
#6917=CARTESIAN_POINT('Ctrl Pts',(6.38100572782112,2.58506854703074,22.1286045210584));
#6918=CARTESIAN_POINT('Ctrl Pts',(6.4104590061279,2.56289284395919,22.1308382690139));
#6919=CARTESIAN_POINT('Ctrl Pts',(6.42589925953707,2.55104707029468,22.1320118739534));
#6920=CARTESIAN_POINT('Ctrl Pts',(6.53075741584978,2.46908037118173,22.1400022485682));
#6921=CARTESIAN_POINT('Ctrl Pts',(6.61652507837474,2.3944085061937,22.1466350720116));
#6922=CARTESIAN_POINT('Ctrl Pts',(6.90642010198939,2.11373462169066,22.1697460066299));
#6923=CARTESIAN_POINT('Ctrl Pts',(7.08648568047272,1.88497055543233,22.1853274524097));
#6924=CARTESIAN_POINT('Ctrl Pts',(7.26354373765657,1.58428152051933,22.2057145623015));
#6925=CARTESIAN_POINT('Ctrl Pts',(7.29214449780761,1.53250122818785,22.2092271134562));
#6926=CARTESIAN_POINT('Ctrl Pts',(7.32639037032406,1.46625636434933,22.2137602395819));
#6927=CARTESIAN_POINT('Ctrl Pts',(7.33337955504677,1.45249510696921,22.2147040193848));
#6928=CARTESIAN_POINT('Ctrl Pts',(7.34424066702408,1.43072433046129,22.2162012410957));
#6929=CARTESIAN_POINT('Ctrl Pts',(7.34817884068541,1.42274787095117,22.2167506661345));
#6930=CARTESIAN_POINT('Ctrl Pts',(7.35554743527964,1.40766638578361,22.2177913152666));
#6931=CARTESIAN_POINT('Ctrl Pts',(7.35898483508735,1.4005649753479,22.2182821021845));
#6932=CARTESIAN_POINT('Ctrl Pts',(7.36695539085149,1.38394304063307,22.2194326076356));
#6933=CARTESIAN_POINT('Ctrl Pts',(7.3714679269336,1.37441282759032,22.2200935697106));
#6934=CARTESIAN_POINT('Ctrl Pts',(7.38594975152599,1.34343591638403,22.2222458049025));
#6935=CARTESIAN_POINT('Ctrl Pts',(7.39572948222556,1.32190214411775,22.2237479003812));
#6936=CARTESIAN_POINT('Ctrl Pts',(7.44706623151683,1.2054781188722,22.2318933834356));
#6937=CARTESIAN_POINT('Ctrl Pts',(7.48426325738744,1.10874125717241,22.2387460001017));
#6938=CARTESIAN_POINT('Ctrl Pts',(7.61355085875772,0.717156085212655,22.2663877879574));
#6939=CARTESIAN_POINT('Ctrl Pts',(7.6677405817972,0.41144478362888,22.2875509873347));
#6940=CARTESIAN_POINT('Ctrl Pts',(7.67866302492731,0.0687969074833208,22.3094304860775));
#6941=CARTESIAN_POINT('Ctrl Pts',(7.67920843263985,0.0349000051372115,22.3115779087787));
#6942=CARTESIAN_POINT('Ctrl Pts',(7.67921895108708,0.000999948906710003,
22.3137088975806));
#6943=CARTESIAN_POINT('',(7.67921822734991,-0.00238007247472413,20.815728761447));
#6944=CARTESIAN_POINT('Ctrl Pts',(7.67921910621823,-2.19646041259736E-11,
22.0659612921829));
#6945=CARTESIAN_POINT('Ctrl Pts',(7.67921910621824,0.000842109108049127,
22.0659135845146));
#6946=CARTESIAN_POINT('Ctrl Pts',(7.67921877615567,0.00168423000929225,
22.0658658700222));
#6947=CARTESIAN_POINT('Ctrl Pts',(7.67912126048857,0.126079561885152,22.0588167216195));
#6948=CARTESIAN_POINT('Ctrl Pts',(7.67191931405605,0.24951134855579,22.051690097904));
#6949=CARTESIAN_POINT('Ctrl Pts',(7.65572397793286,0.388799127737251,22.0432006959801));
#6950=CARTESIAN_POINT('Ctrl Pts',(7.65366618859104,0.405373020163533,22.0421832630709));
#6951=CARTESIAN_POINT('Ctrl Pts',(7.65016125844979,0.431913667158585,22.0405412467));
#6952=CARTESIAN_POINT('Ctrl Pts',(7.6487960258009,0.441891175805831,22.0399210637177));
#6953=CARTESIAN_POINT('Ctrl Pts',(7.64628295121627,0.459637761990175,22.0388125532577));
#6954=CARTESIAN_POINT('Ctrl Pts',(7.64515344738692,0.467409251919766,22.0383252587355));
#6955=CARTESIAN_POINT('Ctrl Pts',(7.64265763604375,0.48415137067857,22.0372713886317));
#6956=CARTESIAN_POINT('Ctrl Pts',(7.64128186846532,0.493120230770056,22.0367043123262));
#6957=CARTESIAN_POINT('Ctrl Pts',(7.63733615137166,0.5181375918353,22.0351157470899));
#6958=CARTESIAN_POINT('Ctrl Pts',(7.63468268707784,0.534172380154636,22.0340897559942));
#6959=CARTESIAN_POINT('Ctrl Pts',(7.61800360356846,0.630436935911772,22.0278860413881));
#6960=CARTESIAN_POINT('Ctrl Pts',(7.60106307384245,0.710124985476,22.0225662729259));
#6961=CARTESIAN_POINT('Ctrl Pts',(7.54145529904885,0.946164657647747,22.0064167459452));
#6962=CARTESIAN_POINT('Ctrl Pts',(7.4899976845368,1.10003164587155,21.995377230245));
#6963=CARTESIAN_POINT('Ctrl Pts',(7.34547094238736,1.44368286573009,21.9702396457718));
#6964=CARTESIAN_POINT('Ctrl Pts',(7.24487274784753,1.62953552915293,21.9563053998555));
#6965=CARTESIAN_POINT('Ctrl Pts',(7.11147812723515,1.82696352195835,21.941303067941));
#6966=CARTESIAN_POINT('Ctrl Pts',(7.0958458931962,1.84947529400642,21.9395883740116));
#6967=CARTESIAN_POINT('Ctrl Pts',(7.0697577452087,1.88603994531729,21.9367959574913));
#6968=CARTESIAN_POINT('Ctrl Pts',(7.05947131823346,1.90021148550149,21.9357118405982));
#6969=CARTESIAN_POINT('Ctrl Pts',(7.04077082619802,1.92553820546547,21.9337707666036));
#6970=CARTESIAN_POINT('Ctrl Pts',(7.03239881726623,1.93672375265293,21.9329122116886));
#6971=CARTESIAN_POINT('Ctrl Pts',(7.01438729306753,1.96046490835058,21.9310870189626));
#6972=CARTESIAN_POINT('Ctrl Pts',(7.00472745497092,1.97300469068947,21.930121207837));
#6973=CARTESIAN_POINT('Ctrl Pts',(6.97831712824019,2.00677134669496,21.9275153111671));
#6974=CARTESIAN_POINT('Ctrl Pts',(6.96139101780366,2.02785970140345,21.9258822233686));
#6975=CARTESIAN_POINT('Ctrl Pts',(6.86879011112797,2.14030296978391,21.9171394742127));
#6976=CARTESIAN_POINT('Ctrl Pts',(6.78837611166571,2.22764531667753,21.9102263459081));
#6977=CARTESIAN_POINT('Ctrl Pts',(6.59210561128341,2.41852051185743,21.8945744984749));
#6978=CARTESIAN_POINT('Ctrl Pts',(6.47322207354766,2.51851034840963,21.8859535260676));
#6979=CARTESIAN_POINT('Ctrl Pts',(6.2106578648704,2.70878953694886,21.8677970235736));
#6980=CARTESIAN_POINT('Ctrl Pts',(6.06613393139463,2.7970849342464,21.8582745128319));
#6981=CARTESIAN_POINT('Ctrl Pts',(5.89132580071345,2.88583282597355,21.8465224427134));
#6982=CARTESIAN_POINT('Ctrl Pts',(5.86712792267801,2.89773815739771,21.8448905250422));
#6983=CARTESIAN_POINT('Ctrl Pts',(5.83346392538425,2.91377923435332,21.8426092607368));
#6984=CARTESIAN_POINT('Ctrl Pts',(5.82412230723014,2.9181756070509,21.8419750658686));
#6985=CARTESIAN_POINT('Ctrl Pts',(5.80804707284597,2.92564682727969,21.8408814833456));
#6986=CARTESIAN_POINT('Ctrl Pts',(5.80132362287688,2.92874353337133,21.8404234220518));
#6987=CARTESIAN_POINT('Ctrl Pts',(5.78723110209174,2.93517554853987,21.8394617888629));
#6988=CARTESIAN_POINT('Ctrl Pts',(5.77986009468512,2.93850630031104,21.8389579335414));
#6989=CARTESIAN_POINT('Ctrl Pts',(5.76177285848519,2.94659755966904,21.8377195405781));
#6990=CARTESIAN_POINT('Ctrl Pts',(5.75104309548055,2.95132736928182,21.836983173722));
#6991=CARTESIAN_POINT('Ctrl Pts',(5.71196146689861,2.96830090043147,21.8342954498185));
#6992=CARTESIAN_POINT('Ctrl Pts',(5.6834607985182,2.98019504844327,21.8323247193045));
#6993=CARTESIAN_POINT('Ctrl Pts',(5.61144889062973,3.00903964505913,21.8273265000807));
#6994=CARTESIAN_POINT('Ctrl Pts',(5.56773282375193,3.0254570557488,21.824275253203));
#6995=CARTESIAN_POINT('Ctrl Pts',(5.21018577466158,3.15093802191481,21.799265532027));
#6996=CARTESIAN_POINT('Ctrl Pts',(4.88154189409492,3.2118355338613,21.7762187141575));
#6997=CARTESIAN_POINT('Ctrl Pts',(4.48214848204969,3.22334844004773,21.7504640284719));
#6998=CARTESIAN_POINT('Ctrl Pts',(4.41491971886507,3.22318310433417,21.746192976532));
#6999=CARTESIAN_POINT('Ctrl Pts',(4.32448134831466,3.22013018766958,21.7405304896149));
#7000=CARTESIAN_POINT('Ctrl Pts',(4.30123033828528,3.21909306549873,21.7390820533646));
#7001=CARTESIAN_POINT('Ctrl Pts',(4.26300839351863,3.21697306755446,21.736712615184));
#7002=CARTESIAN_POINT('Ctrl Pts',(4.24803047448806,3.21603733089037,21.7357870478897));
#7003=CARTESIAN_POINT('Ctrl Pts',(4.21889362710179,3.21401261560774,21.7339920546336));
#7004=CARTESIAN_POINT('Ctrl Pts',(4.20473430682369,3.21293460912538,21.7331223067461));
#7005=CARTESIAN_POINT('Ctrl Pts',(4.17143177881153,3.21017764990761,21.7310824416129));
#7006=CARTESIAN_POINT('Ctrl Pts',(4.15229541567964,3.20842098433393,21.7299147843668));
#7007=CARTESIAN_POINT('Ctrl Pts',(4.08906129528561,3.20204542696027,21.7260703552774));
#7008=CARTESIAN_POINT('Ctrl Pts',(4.04504199275132,3.19668757202262,21.7234167158049));
#7009=CARTESIAN_POINT('Ctrl Pts',(3.94042109426429,3.18175652466718,21.7171537219483));
#7010=CARTESIAN_POINT('Ctrl Pts',(3.8799540333302,3.17135793517871,21.7135694708794));
#7011=CARTESIAN_POINT('Ctrl Pts',(3.6420033517624,3.1234060132616,21.699547077474));
#7012=CARTESIAN_POINT('Ctrl Pts',(3.46752971828005,3.07262476574035,21.6894690763852));
#7013=CARTESIAN_POINT('Ctrl Pts',(3.13728345856494,2.94544041364587,21.6696597843506));
#7014=CARTESIAN_POINT('Ctrl Pts',(2.98157454690569,2.87063431478247,21.6599599185457));
#7015=CARTESIAN_POINT('Ctrl Pts',(2.80932594678627,2.77015598152087,21.6480060112895));
#7016=CARTESIAN_POINT('Ctrl Pts',(2.78620525234023,2.75627707245762,21.6463741857773));
#7017=CARTESIAN_POINT('Ctrl Pts',(2.75447775967312,2.73668588080824,21.6440930290269));
#7018=CARTESIAN_POINT('Ctrl Pts',(2.74571946668359,2.7312194745257,21.6434588477069));
#7019=CARTESIAN_POINT('Ctrl Pts',(2.73072705892367,2.72176169842072,21.6423652831093));
#7020=CARTESIAN_POINT('Ctrl Pts',(2.72448008833745,2.71779071970731,21.6419072261066));
#7021=CARTESIAN_POINT('Ctrl Pts',(2.71143555587516,2.70943553147768,21.6409455946213));
#7022=CARTESIAN_POINT('Ctrl Pts',(2.70464077409589,2.70504722338562,21.6404417366692));
#7023=CARTESIAN_POINT('Ctrl Pts',(2.68803614146954,2.69423457013526,21.6392033264973));
#7024=CARTESIAN_POINT('Ctrl Pts',(2.6782447505816,2.6877822085799,21.6384669449442));
#7025=CARTESIAN_POINT('Ctrl Pts',(2.64279374941111,2.66414209470341,21.6357791058896));
#7026=CARTESIAN_POINT('Ctrl Pts',(2.61734724537921,2.64663975979544,21.6338082727896));
#7027=CARTESIAN_POINT('Ctrl Pts',(2.55406673726221,2.60176159871099,21.6288097369357));
#7028=CARTESIAN_POINT('Ctrl Pts',(2.5165696675721,2.57392461349346,21.625758272399));
#7029=CARTESIAN_POINT('Ctrl Pts',(2.21723170070704,2.34144596281452,21.6007429055165));
#7030=CARTESIAN_POINT('Ctrl Pts',(1.98785158780413,2.09822690457166,21.5776903687778));
#7031=CARTESIAN_POINT('Ctrl Pts',(1.76168105448884,1.76882526761004,21.5519357139471));
#7032=CARTESIAN_POINT('Ctrl Pts',(1.72541411513742,1.71229821669841,21.5476690793576));
#7033=CARTESIAN_POINT('Ctrl Pts',(1.67899274227599,1.63471215597493,21.5420114411486));
#7034=CARTESIAN_POINT('Ctrl Pts',(1.66726434443109,1.61461934447604,21.5405635608198));
#7035=CARTESIAN_POINT('Ctrl Pts',(1.64833090244838,1.58136097600671,21.5381947940013));
#7036=CARTESIAN_POINT('Ctrl Pts',(1.64099857096971,1.56826923237064,21.5372693472328));
#7037=CARTESIAN_POINT('Ctrl Pts',(1.62690526103363,1.54268845630915,21.535474421338));
#7038=CARTESIAN_POINT('Ctrl Pts',(1.62013488366135,1.5302050239555,21.5346046214852));
#7039=CARTESIAN_POINT('Ctrl Pts',(1.60439522989349,1.50072037171207,21.5325643789903));
#7040=CARTESIAN_POINT('Ctrl Pts',(1.59549504204625,1.48368273528748,21.5313963989991));
#7041=CARTESIAN_POINT('Ctrl Pts',(1.56655655349929,1.42705699209951,21.5275497547784));
#7042=CARTESIAN_POINT('Ctrl Pts',(1.54718282513905,1.38713367897605,21.5248942604633));
#7043=CARTESIAN_POINT('Ctrl Pts',(1.50298042613934,1.29104290849796,21.5186261199715));
#7044=CARTESIAN_POINT('Ctrl Pts',(1.47892009986949,1.23454029530846,21.5150386345858));
#7045=CARTESIAN_POINT('Ctrl Pts',(1.39010477320703,1.00823796581482,21.5009952647507));
#7046=CARTESIAN_POINT('Ctrl Pts',(1.33814465599626,0.833781208828499,21.4909008008378));
#7047=CARTESIAN_POINT('Ctrl Pts',(1.29682924988139,0.635017363350291,21.4795366082732));
#7048=CARTESIAN_POINT('Ctrl Pts',(1.29270209432549,0.614124873587356,21.4783434322785));
#7049=CARTESIAN_POINT('Ctrl Pts',(1.28391381252941,0.567194921616959,21.4756635988978));
#7050=CARTESIAN_POINT('Ctrl Pts',(1.27936558250794,0.541138009763068,21.4741759175493));
#7051=CARTESIAN_POINT('Ctrl Pts',(1.25317484229494,0.379357777084059,21.4649262768301));
#7052=CARTESIAN_POINT('Ctrl Pts',(1.23991480680202,0.24243698799337,21.4570445553621));
#7053=CARTESIAN_POINT('Ctrl Pts',(1.23488242236496,0.0882176054906887,21.4477055315022));
#7054=CARTESIAN_POINT('Ctrl Pts',(1.23446416447521,0.0713248557818932,21.4466763225296));
#7055=CARTESIAN_POINT('Ctrl Pts',(1.23400772808643,0.0443035399910697,21.4450189352054));
#7056=CARTESIAN_POINT('Ctrl Pts',(1.23388441389743,0.0341764767837041,21.4443952891196));
#7057=CARTESIAN_POINT('Ctrl Pts',(1.23375018772044,0.0161897629948173,21.4432829426017));
#7058=CARTESIAN_POINT('Ctrl Pts',(1.23372028906768,0.00833043366257391,
21.4427953024419));
#7059=CARTESIAN_POINT('Ctrl Pts',(1.23371782024977,-0.00856522920951279,
21.441743476549));
#7060=CARTESIAN_POINT('Ctrl Pts',(1.23375450402847,-0.0176012072661911,
21.441178810483));
#7061=CARTESIAN_POINT('Ctrl Pts',(1.23396208780022,-0.0427156442270686,
21.4396036675532));
#7062=CARTESIAN_POINT('Ctrl Pts',(1.23421531739218,-0.0587929031799864,
21.4385888073402));
#7063=CARTESIAN_POINT('Ctrl Pts',(1.23640685526231,-0.153104865227369,21.4325998571954));
#7064=CARTESIAN_POINT('Ctrl Pts',(1.24107392493832,-0.231243755721218,21.4274946066202));
#7065=CARTESIAN_POINT('Ctrl Pts',(1.26852818691636,-0.516142733974112,21.4085329069887));
#7066=CARTESIAN_POINT('Ctrl Pts',(1.30846833788901,-0.720738339356372,21.3942788224359));
#7067=CARTESIAN_POINT('Ctrl Pts',(1.4159776506892,-1.08164476805225,21.3690791194112));
#7068=CARTESIAN_POINT('Ctrl Pts',(1.47672252803411,-1.23922133088451,21.3580489650839));
#7069=CARTESIAN_POINT('Ctrl Pts',(1.56130457477777,-1.41593910835468,21.3457147415664));
#7070=CARTESIAN_POINT('Ctrl Pts',(1.57338978496306,-1.4403870741801,21.3440086551491));
#7071=CARTESIAN_POINT('Ctrl Pts',(1.59372382682094,-1.48024059512673,21.3412273471052));
#7072=CARTESIAN_POINT('Ctrl Pts',(1.60179001493065,-1.4957372961789,21.3401458168145));
#7073=CARTESIAN_POINT('Ctrl Pts',(1.61653148676677,-1.5235048332093,21.3382075659164));
#7074=CARTESIAN_POINT('Ctrl Pts',(1.62316124558087,-1.53579921727494,21.3373492667883));
#7075=CARTESIAN_POINT('Ctrl Pts',(1.63748709261377,-1.56195690460794,21.3355227071192));
#7076=CARTESIAN_POINT('Ctrl Pts',(1.64520600613941,-1.57580733627731,21.3345552872252));
#7077=CARTESIAN_POINT('Ctrl Pts',(1.666425171527,-1.61322976135414,21.3319403215778));
#7078=CARTESIAN_POINT('Ctrl Pts',(1.68012191952706,-1.63668927653366,21.3302998586874));
#7079=CARTESIAN_POINT('Ctrl Pts',(1.75625636033325,-1.763384299147,21.3214292851569));
#7080=CARTESIAN_POINT('Ctrl Pts',(1.82416046896246,-1.86323079765025,21.3144029243599));
#7081=CARTESIAN_POINT('Ctrl Pts',(1.99520160425979,-2.08664967404673,21.2983286802267));
#7082=CARTESIAN_POINT('Ctrl Pts',(2.10230341826476,-2.20677375784047,21.2894119699326));
#7083=CARTESIAN_POINT('Ctrl Pts',(2.26992793408395,-2.36862449357437,21.2763535845023));
#7084=CARTESIAN_POINT('Ctrl Pts',(2.32361041720719,-2.41707622317187,21.2722852571039));
#7085=CARTESIAN_POINT('Ctrl Pts',(2.40575465883652,-2.4863475517751,21.2661513034181));
#7086=CARTESIAN_POINT('Ctrl Pts',(2.43300286609687,-2.50857292856336,21.2641306474073));
#7087=CARTESIAN_POINT('Ctrl Pts',(2.51632649544916,-2.57429605687005,21.2579754354103));
#7088=CARTESIAN_POINT('Ctrl Pts',(2.57347651286352,-2.61638888851312,21.2537855601515));
#7089=CARTESIAN_POINT('Ctrl Pts',(2.64529077923625,-2.66571041118799,21.2484964762904));
#7090=CARTESIAN_POINT('Ctrl Pts',(2.65868567611587,-2.6747623524345,21.2475089463438));
#7091=CARTESIAN_POINT('Ctrl Pts',(2.67976890916512,-2.68877997032381,21.2459520850319));
#7092=CARTESIAN_POINT('Ctrl Pts',(2.68741146762053,-2.69381446753511,21.2453872193123));
#7093=CARTESIAN_POINT('Ctrl Pts',(2.7016426836614,-2.70310253085828,21.2443342297044));
#7094=CARTESIAN_POINT('Ctrl Pts',(2.70822551498868,-2.70736466085925,21.2438466834194));
#7095=CARTESIAN_POINT('Ctrl Pts',(2.72334210443495,-2.71707395075883,21.2427260529807));
#7096=CARTESIAN_POINT('Ctrl Pts',(2.73188599051141,-2.72250493639574,21.2420919321062));
#7097=CARTESIAN_POINT('Ctrl Pts',(2.75855799134515,-2.73928326418616,21.2401104069708));
#7098=CARTESIAN_POINT('Ctrl Pts',(2.77677314677391,-2.750490207647,21.2387543758944));
#7099=CARTESIAN_POINT('Ctrl Pts',(2.81975331529215,-2.77634776125233,21.2355506734605));
#7100=CARTESIAN_POINT('Ctrl Pts',(2.84460538034556,-2.79084945500261,21.2336951322606));
#7101=CARTESIAN_POINT('Ctrl Pts',(2.93388462219644,-2.84135549409408,21.2270271092326));
#7102=CARTESIAN_POINT('Ctrl Pts',(2.99934740231663,-2.87547553107803,21.2221343988962));
#7103=CARTESIAN_POINT('Ctrl Pts',(3.27239084094545,-3.00607038640625,21.201869056379));
#7104=CARTESIAN_POINT('Ctrl Pts',(3.48882004948076,-3.08255927008653,21.1861920592357));
#7105=CARTESIAN_POINT('Ctrl Pts',(3.77045289720855,-3.1494709691046,21.1671093530028));
#7106=CARTESIAN_POINT('Ctrl Pts',(3.82976275105909,-3.16180731092247,21.1631572100751));
#7107=CARTESIAN_POINT('Ctrl Pts',(3.95556899830644,-3.18429529347676,21.1549194014639));
#7108=CARTESIAN_POINT('Ctrl Pts',(4.02210756245774,-3.19405206028661,21.1506469766707));
#7109=CARTESIAN_POINT('Ctrl Pts',(4.11203066566997,-3.20437536527155,21.14498298276));
#7110=CARTESIAN_POINT('Ctrl Pts',(4.13518304041096,-3.20677947954871,21.1435343736363));
#7111=CARTESIAN_POINT('Ctrl Pts',(4.1733029143296,-3.21032080799395,21.1411647265495));
#7112=CARTESIAN_POINT('Ctrl Pts',(4.18825561295168,-3.21160463267941,21.1402391216426));
#7113=CARTESIAN_POINT('Ctrl Pts',(4.21737271767371,-3.21389982897593,21.1384441070594));
#7114=CARTESIAN_POINT('Ctrl Pts',(4.23153589202662,-3.21492212239086,21.1375743750853));
#7115=CARTESIAN_POINT('Ctrl Pts',(4.26487885882177,-3.2171073862618,21.1355346264945));
#7116=CARTESIAN_POINT('Ctrl Pts',(4.28406334268476,-3.21819251056869,21.1343670690558));
#7117=CARTESIAN_POINT('Ctrl Pts',(4.34753474400673,-3.2212134130724,21.1305233256148));
#7118=CARTESIAN_POINT('Ctrl Pts',(4.39185304959156,-3.22240711267805,21.1278702603562));
#7119=CARTESIAN_POINT('Ctrl Pts',(4.49750438496747,-3.22307214638956,21.1216088593854));
#7120=CARTESIAN_POINT('Ctrl Pts',(4.55882611790766,-3.22170787719385,21.1180256092012));
#7121=CARTESIAN_POINT('Ctrl Pts',(4.80113242525486,-3.20939113864234,21.1040096963537));
#7122=CARTESIAN_POINT('Ctrl Pts',(4.98109278024956,-3.18492680668508,21.0939367799592));
#7123=CARTESIAN_POINT('Ctrl Pts',(5.32659350340669,-3.10786449233529,21.0741221008113));
#7124=CARTESIAN_POINT('Ctrl Pts',(5.49182414907099,-3.05678971827337,21.0644115984847));
#7125=CARTESIAN_POINT('Ctrl Pts',(5.67714092167695,-2.98275080184001,21.0524483080475));
#7126=CARTESIAN_POINT('Ctrl Pts',(5.70200876037321,-2.97245233595862,21.0508194848186));
#7127=CARTESIAN_POINT('Ctrl Pts',(5.73622594850445,-2.95777727984837,21.0485418053271));
#7128=CARTESIAN_POINT('Ctrl Pts',(5.74568840241036,-2.95366511510209,21.047908037168));
#7129=CARTESIAN_POINT('Ctrl Pts',(5.761903858874,-2.94652548550338,21.046814996002));
#7130=CARTESIAN_POINT('Ctrl Pts',(5.76866654762435,-2.94352003599903,21.0463570464011));
#7131=CARTESIAN_POINT('Ctrl Pts',(5.78280060528964,-2.93718024173226,21.0453954162027));
#7132=CARTESIAN_POINT('Ctrl Pts',(5.79016981939347,-2.93384141024268,21.0448914507697));
#7133=CARTESIAN_POINT('Ctrl Pts',(5.80715073355459,-2.92607052777174,21.0437242977306));
#7134=CARTESIAN_POINT('Ctrl Pts',(5.81675330346425,-2.92161881279534,21.0430599285895));
#7135=CARTESIAN_POINT('Ctrl Pts',(5.8509235474757,-2.90557264219218,21.0406807027316));
#7136=CARTESIAN_POINT('Ctrl Pts',(5.87536556466588,-2.89371530992005,21.0389508831883));
#7137=CARTESIAN_POINT('Ctrl Pts',(5.93510858138337,-2.86379385046773,21.0346588040189));
#7138=CARTESIAN_POINT('Ctrl Pts',(5.97023102850904,-2.84538476673711,21.0320798171875));
#7139=CARTESIAN_POINT('Ctrl Pts',(6.11247463059183,-2.76745019535287,21.0214309892446));
#7140=CARTESIAN_POINT('Ctrl Pts',(6.21649385710969,-2.70248852536109,21.0131662447088));
#7141=CARTESIAN_POINT('Ctrl Pts',(6.52960296733948,-2.48118858601443,20.9872339417916));
#7142=CARTESIAN_POINT('Ctrl Pts',(6.72362101636808,-2.30526638462494,20.9696738125613));
#7143=CARTESIAN_POINT('Ctrl Pts',(6.92000852821356,-2.07813229303284,20.9506463919663));
#7144=CARTESIAN_POINT('Ctrl Pts',(6.94515379110272,-2.04795240893094,20.9481794437155));
#7145=CARTESIAN_POINT('Ctrl Pts',(6.98108259752001,-2.00319058298671,20.9446072734778));
#7146=CARTESIAN_POINT('Ctrl Pts',(6.99230406181366,-1.98896628721787,20.9434845470196));
#7147=CARTESIAN_POINT('Ctrl Pts',(7.01203124601801,-1.96352181317441,20.9414978810501));
#7148=CARTESIAN_POINT('Ctrl Pts',(7.02058443405943,-1.95233920124294,20.9406320740342));
#7149=CARTESIAN_POINT('Ctrl Pts',(7.03829419050025,-1.92886796618653,20.93882984984));
#7150=CARTESIAN_POINT('Ctrl Pts',(7.04743695544084,-1.91656933446637,20.9378939868921));
#7151=CARTESIAN_POINT('Ctrl Pts',(7.07110579319574,-1.88425165374463,20.9354564951519));
#7152=CARTESIAN_POINT('Ctrl Pts',(7.08548991676087,-1.86412953661981,20.9339603626393));
#7153=CARTESIAN_POINT('Ctrl Pts',(7.15010519603996,-1.77150273888731,20.9271679739803));
#7154=CARTESIAN_POINT('Ctrl Pts',(7.19758087514342,-1.69711686108284,20.9219761069846));
#7155=CARTESIAN_POINT('Ctrl Pts',(7.31045767863544,-1.50313728456852,20.9089851687597));
#7156=CARTESIAN_POINT('Ctrl Pts',(7.37143708304061,-1.38117257964705,20.9013225220935));
#7157=CARTESIAN_POINT('Ctrl Pts',(7.47487383296203,-1.13668513682375,20.886465823715));
#7158=CARTESIAN_POINT('Ctrl Pts',(7.51802321582908,-1.01474347804668,20.8792798363644));
#7159=CARTESIAN_POINT('Ctrl Pts',(7.58347539939457,-0.787104701564741,20.8657822333784));
#7160=CARTESIAN_POINT('Ctrl Pts',(7.60801366630656,-0.682249332651416,20.8595321725366));
#7161=CARTESIAN_POINT('Ctrl Pts',(7.63019193682435,-0.560240909038873,20.8520215108499));
#7162=CARTESIAN_POINT('Ctrl Pts',(7.63300152491294,-0.544084781188677,20.8510221893566));
#7163=CARTESIAN_POINT('Ctrl Pts',(7.63734026912222,-0.517955591880709,20.8493972704103));
#7164=CARTESIAN_POINT('Ctrl Pts',(7.638946142258,-0.507995333476345,20.8487758211932));
#7165=CARTESIAN_POINT('Ctrl Pts',(7.64171664784164,-0.490282690182273,20.8476667904289));
#7166=CARTESIAN_POINT('Ctrl Pts',(7.64289979624358,-0.482533391075683,20.847180257461));
#7167=CARTESIAN_POINT('Ctrl Pts',(7.64514623937996,-0.467451175904277,20.8462306880971));
#7168=CARTESIAN_POINT('Ctrl Pts',(7.64621250925745,-0.460118986323355,20.845767858341));
#7169=CARTESIAN_POINT('Ctrl Pts',(7.64853126191395,-0.443778630614379,20.8447338369327));
#7170=CARTESIAN_POINT('Ctrl Pts',(7.64977091030739,-0.434768745650329,20.8441619522962));
#7171=CARTESIAN_POINT('Ctrl Pts',(7.65277916626227,-0.41219729204756,20.8427251313785));
#7172=CARTESIAN_POINT('Ctrl Pts',(7.65449959599747,-0.398629626472879,20.8418577213568));
#7173=CARTESIAN_POINT('Ctrl Pts',(7.67141719267095,-0.258049455211929,20.8328342839026));
#7174=CARTESIAN_POINT('Ctrl Pts',(7.67912378100643,-0.130265619523243,20.8243335871624));
#7175=CARTESIAN_POINT('Ctrl Pts',(7.67921822734991,-0.00238007247472413,
20.815728761447));
#7176=CARTESIAN_POINT('Ctrl Pts',(7.67921822450325,-0.00238392389238244,
20.815729020591));
#7177=CARTESIAN_POINT('Ctrl Pts',(7.67921881231805,-0.00158927619454485,
20.8156755524433));
#7178=CARTESIAN_POINT('Ctrl Pts',(7.6792191062182,-0.000794634884726798,
20.8156220807944));
#7179=CARTESIAN_POINT('Ctrl Pts',(7.67921910621823,-1.24761686023381E-10,
20.8155686056964));
#7180=CARTESIAN_POINT('Origin',(4.45646910621825,-5.13094777615093E-16,
-2.31077344927308));
#7181=CARTESIAN_POINT('',(7.67921910621823,-8.48293998545729E-13,19.5612501365773));
#7182=CARTESIAN_POINT('',(7.67921910621823,5.28351711817002E-12,19.808946496524));
#7183=CARTESIAN_POINT('',(7.67921910621823,-3.51191647465084E-13,-2.31077344927308));
#7184=CARTESIAN_POINT('',(7.67921816809758,-0.00245899486517952,19.8090860941722));
#7185=CARTESIAN_POINT('Ctrl Pts',(7.67921910621823,5.28351711817003E-12,
19.808946496524));
#7186=CARTESIAN_POINT('Ctrl Pts',(7.67921910621823,-0.000819655941728086,
19.8089930222664));
#7187=CARTESIAN_POINT('Ctrl Pts',(7.67921879351827,-0.00163932095804614,
19.8090395547947));
#7188=CARTESIAN_POINT('Ctrl Pts',(7.67921816809758,-0.00245899486630962,
19.8090860941722));
#7189=CARTESIAN_POINT('Ctrl Pts',(7.67921816490598,-0.00246317421660369,
19.8090863314671));
#7190=CARTESIAN_POINT('Ctrl Pts',(7.67913282611117,-0.114118094441251,19.8154258682507));
#7191=CARTESIAN_POINT('Ctrl Pts',(7.67324495034378,-0.225684694903017,19.821876714552));
#7192=CARTESIAN_POINT('Ctrl Pts',(7.65995857656981,-0.352156167876153,19.8295423684475));
#7193=CARTESIAN_POINT('Ctrl Pts',(7.65822438964366,-0.367589223768464,19.8304838408652));
#7194=CARTESIAN_POINT('Ctrl Pts',(7.65520755005175,-0.392793903076085,19.8320321904543));
#7195=CARTESIAN_POINT('Ctrl Pts',(7.65399147657129,-0.402573431456799,19.8326356133735));
#7196=CARTESIAN_POINT('Ctrl Pts',(7.6517549709269,-0.419909450366868,19.8337102500715));
#7197=CARTESIAN_POINT('Ctrl Pts',(7.65075253204503,-0.427468240245285,19.8341804839197));
#7198=CARTESIAN_POINT('Ctrl Pts',(7.64866592955735,-0.442784780665778,19.8351368545086));
#7199=CARTESIAN_POINT('Ctrl Pts',(7.6475803123914,-0.450542105353103,19.8356230726358));
#7200=CARTESIAN_POINT('Ctrl Pts',(7.64515180075102,-0.467445926340511,19.8366866681174));
#7201=CARTESIAN_POINT('Ctrl Pts',(7.64379784965398,-0.476590491634979,19.8372646364939));
#7202=CARTESIAN_POINT('Ctrl Pts',(7.63990681365725,-0.502112110544535,19.8388846843901));
#7203=CARTESIAN_POINT('Ctrl Pts',(7.63728276071966,-0.518475338727434,19.8399314330506));
#7204=CARTESIAN_POINT('Ctrl Pts',(7.62169880203334,-0.611080461423574,19.8458982464262));
#7205=CARTESIAN_POINT('Ctrl Pts',(7.60612501604948,-0.686850740133894,19.8509449895099));
#7206=CARTESIAN_POINT('Ctrl Pts',(7.58240794903486,-0.784316482790087,19.8575911537956));
#7207=CARTESIAN_POINT('Ctrl Pts',(7.57673406295805,-0.806593179864548,19.8591208440121));
#7208=CARTESIAN_POINT('Ctrl Pts',(7.53812782042504,-0.951661329855261,19.8691447924729));
#7209=CARTESIAN_POINT('Ctrl Pts',(7.4981930612836,-1.0724709552804,19.8777804320858));
#7210=CARTESIAN_POINT('Ctrl Pts',(7.41174345647061,-1.28992011533772,19.8935855024148));
#7211=CARTESIAN_POINT('Ctrl Pts',(7.36734079704524,-1.38721622984992,19.9007608661631));
#7212=CARTESIAN_POINT('Ctrl Pts',(7.26101764104557,-1.59250607854635,19.9160234404596));
#7213=CARTESIAN_POINT('Ctrl Pts',(7.19750955614411,-1.69949164751796,19.9240543836823));
#7214=CARTESIAN_POINT('Ctrl Pts',(7.11265555434568,-1.82525091957933,19.9335828705979));
#7215=CARTESIAN_POINT('Ctrl Pts',(7.09705087750684,-1.84775413682039,19.9352918242933));
#7216=CARTESIAN_POINT('Ctrl Pts',(7.07193207395194,-1.88300928772761,19.9379761409524));
#7217=CARTESIAN_POINT('Ctrl Pts',(7.06260736855221,-1.89589395413968,19.9389586748279));
#7218=CARTESIAN_POINT('Ctrl Pts',(7.04491754736462,-1.91996020965646,19.9407969108687));
#7219=CARTESIAN_POINT('Ctrl Pts',(7.03657443257313,-1.93115743888423,19.9416534350849));
#7220=CARTESIAN_POINT('Ctrl Pts',(7.01767059842093,-1.95618693372098,19.9435710764523));
#7221=CARTESIAN_POINT('Ctrl Pts',(7.00707003257307,-1.96998866399782,19.9446306024861));
#7222=CARTESIAN_POINT('Ctrl Pts',(6.97971122053792,-2.0050182557509,19.9473256454622));
#7223=CARTESIAN_POINT('Ctrl Pts',(6.96279641038478,-2.02612252463055,19.948954937408));
#7224=CARTESIAN_POINT('Ctrl Pts',(6.84403145326458,-2.17053966883919,19.9601494409179));
#7225=CARTESIAN_POINT('Ctrl Pts',(6.7333849345405,-2.28634205844877,19.9693413166352));
#7226=CARTESIAN_POINT('Ctrl Pts',(6.41817885596634,-2.57055430412483,19.9932929457057));
#7227=CARTESIAN_POINT('Ctrl Pts',(6.20075118951711,-2.72277401004116,20.0076333202954));
#7228=CARTESIAN_POINT('Ctrl Pts',(5.94474967140447,-2.85863345708013,20.0248481903556));
#7229=CARTESIAN_POINT('Ctrl Pts',(5.9221466880512,-2.87028803880192,20.0263713570415));
#7230=CARTESIAN_POINT('Ctrl Pts',(5.8822049854042,-2.89028803914877,20.0290727052385));
#7231=CARTESIAN_POINT('Ctrl Pts',(5.86492476126281,-2.8987480699643,20.0302445693536));
#7232=CARTESIAN_POINT('Ctrl Pts',(5.83884695124865,-2.91122698844464,20.0320193148926));
#7233=CARTESIAN_POINT('Ctrl Pts',(5.83010498220628,-2.91536199454235,20.0326153061962));
#7234=CARTESIAN_POINT('Ctrl Pts',(5.82131746409663,-2.91947024704796,20.0332155841384));
#7235=CARTESIAN_POINT('Ctrl Pts',(5.82129026071566,-2.91948296443702,20.0332174424207));
#7236=CARTESIAN_POINT('Ctrl Pts',(5.82123556182638,-2.91950853485101,20.0332211789634));
#7237=CARTESIAN_POINT('Ctrl Pts',(5.82120806627845,-2.91952138788447,20.0332230572269));
#7238=CARTESIAN_POINT('Ctrl Pts',(5.82115277914063,-2.9195472313871,20.0332268340001));
#7239=CARTESIAN_POINT('Ctrl Pts',(5.82112498756047,-2.91956022184148,20.0332287325095));
#7240=CARTESIAN_POINT('Ctrl Pts',(5.82106910441031,-2.91958634200046,20.0332325500452));
#7241=CARTESIAN_POINT('Ctrl Pts',(5.82104101284883,-2.91959947169059,20.0332344690711));
#7242=CARTESIAN_POINT('Ctrl Pts',(5.82098452576975,-2.91962587214329,20.0332383279115));
#7243=CARTESIAN_POINT('Ctrl Pts',(5.82095613021751,-2.91963914291132,20.0332402677286));
#7244=CARTESIAN_POINT('Ctrl Pts',(5.82089903104375,-2.91966582740976,20.0332441684331));
#7245=CARTESIAN_POINT('Ctrl Pts',(5.82087032748953,-2.91967924109775,20.0332461293162));
#7246=CARTESIAN_POINT('Ctrl Pts',(5.82081260819859,-2.91970621332517,20.0332500724346));
#7247=CARTESIAN_POINT('Ctrl Pts',(5.82078359246063,-2.91971977185393,20.0332520546703));
#7248=CARTESIAN_POINT('Ctrl Pts',(5.82072524470242,-2.91974703564475,20.0332560407746));
#7249=CARTESIAN_POINT('Ctrl Pts',(5.82069591257783,-2.91976074094403,20.0332580446508));
#7250=CARTESIAN_POINT('Ctrl Pts',(5.82063692773613,-2.91978830025504,20.0332620743315));
#7251=CARTESIAN_POINT('Ctrl Pts',(5.820607275043,-2.91980215424376,20.0332641001347));
#7252=CARTESIAN_POINT('Ctrl Pts',(5.82054764473718,-2.91983001291971,20.033268173966));
#7253=CARTESIAN_POINT('Ctrl Pts',(5.82051766708296,-2.91984401761422,20.0332702219972));
#7254=CARTESIAN_POINT('Ctrl Pts',(5.82045738241223,-2.91987217974078,20.033274340589));
#7255=CARTESIAN_POINT('Ctrl Pts',(5.8204270754542,-2.9198863371331,20.0332764111459));
#7256=CARTESIAN_POINT('Ctrl Pts',(5.82036612773428,-2.9199148066927,20.0332805750934));
#7257=CARTESIAN_POINT('Ctrl Pts',(5.8203354869391,-2.91992911886281,20.0332826684865));
#7258=CARTESIAN_POINT('Ctrl Pts',(5.82027386698238,-2.91995790007082,20.0332868784192));
#7259=CARTESIAN_POINT('Ctrl Pts',(5.82024288786449,-2.9199723690753,20.0332889949561));
#7260=CARTESIAN_POINT('Ctrl Pts',(5.82018058667748,-2.92000146605419,20.0332932514904));
#7261=CARTESIAN_POINT('Ctrl Pts',(5.82014926456717,-2.92001609403448,20.0332953914911));
#7262=CARTESIAN_POINT('Ctrl Pts',(5.82008627264695,-2.92004551114234,20.0332996952783));
#7263=CARTESIAN_POINT('Ctrl Pts',(5.82005460292467,-2.92006030021529,20.0333018590593));
#7264=CARTESIAN_POINT('Ctrl Pts',(5.81999091104595,-2.92009004167821,20.0333062107317));
#7265=CARTESIAN_POINT('Ctrl Pts',(5.81995888886353,-2.92010499406627,20.0333083986253));
#7266=CARTESIAN_POINT('Ctrl Pts',(5.8198944872475,-2.92013506436638,20.0333127988532));
#7267=CARTESIAN_POINT('Ctrl Pts',(5.81986210780262,-2.92015018226933,20.0333150111886));
#7268=CARTESIAN_POINT('Ctrl Pts',(5.81979698678821,-2.92018058583132,20.0333194606342));
#7269=CARTESIAN_POINT('Ctrl Pts',(5.81976424512392,-2.92019587151987,20.0333216977512));
#7270=CARTESIAN_POINT('Ctrl Pts',(5.8196983945757,-2.92022661298732,20.0333261971092));
#7271=CARTESIAN_POINT('Ctrl Pts',(5.81966528577417,-2.92024206871264,20.0333284593449));
#7272=CARTESIAN_POINT('Ctrl Pts',(5.8195986958551,-2.92027315258719,20.0333330092897));
#7273=CARTESIAN_POINT('Ctrl Pts',(5.81956521474586,-2.92028878071707,20.0333352969986));
#7274=CARTESIAN_POINT('Ctrl Pts',(5.81949787507735,-2.92032021175049,20.0333398982416));
#7275=CARTESIAN_POINT('Ctrl Pts',(5.81946401650961,-2.92033601464212,20.0333422117767));
#7276=CARTESIAN_POINT('Ctrl Pts',(5.81939591671594,-2.92036779758206,20.0333468650294));
#7277=CARTESIAN_POINT('Ctrl Pts',(5.81936167542007,-2.92038377764672,20.0333492047521));
#7278=CARTESIAN_POINT('Ctrl Pts',(5.81929280483042,-2.92041591737568,20.0333539107459));
#7279=CARTESIAN_POINT('Ctrl Pts',(5.81925817549578,-2.92043207704234,20.0333562770202));
#7280=CARTESIAN_POINT('Ctrl Pts',(5.81918852336661,-2.92046457847383,20.0333610364918));
#7281=CARTESIAN_POINT('Ctrl Pts',(5.81915350056692,-2.92048092022395,20.0333634296898));
#7282=CARTESIAN_POINT('Ctrl Pts',(5.81908305596489,-2.92051378835703,20.0333682433888));
#7283=CARTESIAN_POINT('Ctrl Pts',(5.81904763417721,-2.92053031471561,20.0333706638893));
#7284=CARTESIAN_POINT('Ctrl Pts',(5.81897638601533,-2.92056355461796,20.033375532576));
#7285=CARTESIAN_POINT('Ctrl Pts',(5.8189405596092,-2.92058026815862,20.0333779807649));
#7286=CARTESIAN_POINT('Ctrl Pts',(5.81886849642417,-2.92061388507026,20.0333829052254));
#7287=CARTESIAN_POINT('Ctrl Pts',(5.81883225976557,-2.92063078836666,20.0333853814892));
#7288=CARTESIAN_POINT('Ctrl Pts',(5.81875937034235,-2.92066478740855,20.0333903624926));
#7289=CARTESIAN_POINT('Ctrl Pts',(5.81872271753058,-2.92068188315709,20.0333928672358));
#7290=CARTESIAN_POINT('Ctrl Pts',(5.81864898991746,-2.92071626979044,20.0333979056017));
#7291=CARTESIAN_POINT('Ctrl Pts',(5.81861191514423,-2.9207335606427,20.0334004392228));
#7292=CARTESIAN_POINT('Ctrl Pts',(5.81853733763696,-2.92076834020982,20.0334055357539));
#7293=CARTESIAN_POINT('Ctrl Pts',(5.8184998348711,-2.9207858289196,20.0334080986665));
#7294=CARTESIAN_POINT('Ctrl Pts',(5.81842439535529,-2.92082100695055,20.0334132541937));
#7295=CARTESIAN_POINT('Ctrl Pts',(5.81838645851186,-2.92083869629487,20.0334158468151));
#7296=CARTESIAN_POINT('Ctrl Pts',(5.81831014460997,-2.92087427843873,20.0334210621874));
#7297=CARTESIAN_POINT('Ctrl Pts',(5.81827176755886,-2.92089217121386,20.0334236849382));
#7298=CARTESIAN_POINT('Ctrl Pts',(5.81819456686792,-2.9209281631278,20.0334289610063));
#7299=CARTESIAN_POINT('Ctrl Pts',(5.81815574331681,-2.92094626220372,20.0334316143181));
#7300=CARTESIAN_POINT('Ctrl Pts',(5.81807764335683,-2.92098266957697,20.0334369519383));
#7301=CARTESIAN_POINT('Ctrl Pts',(5.81803836681591,-2.92100097791378,20.0334396362562));
#7302=CARTESIAN_POINT('Ctrl Pts',(5.81795935430806,-2.92103780680397,20.0334450363392));
#7303=CARTESIAN_POINT('Ctrl Pts',(5.81791961843136,-2.92105632729265,20.0334477520987));
#7304=CARTESIAN_POINT('Ctrl Pts',(5.81783968067501,-2.92109358348382,20.033453215516));
#7305=CARTESIAN_POINT('Ctrl Pts',(5.81779947873957,-2.92111231918905,20.0334559631782));
#7306=CARTESIAN_POINT('Ctrl Pts',(5.81771860215329,-2.92115000887153,20.0334614908616));
#7307=CARTESIAN_POINT('Ctrl Pts',(5.81767792752605,-2.92116896281392,20.0334642708817));
#7308=CARTESIAN_POINT('Ctrl Pts',(5.81759609871236,-2.92120709208799,20.0334698637504));
#7309=CARTESIAN_POINT('Ctrl Pts',(5.81755494454887,-2.92122626738448,20.0334726765981));
#7310=CARTESIAN_POINT('Ctrl Pts',(5.81747214977746,-2.92126484250105,20.0334783355943));
#7311=CARTESIAN_POINT('Ctrl Pts',(5.81743050912676,-2.92128424231595,20.0334811817464));
#7312=CARTESIAN_POINT('Ctrl Pts',(5.81734673432384,-2.92132326968141,20.0334869078358));
#7313=CARTESIAN_POINT('Ctrl Pts',(5.81730460018414,-2.92134289720036,20.0334897877729));
#7314=CARTESIAN_POINT('Ctrl Pts',(5.81721983123472,-2.92138238323556,20.0334955819242));
#7315=CARTESIAN_POINT('Ctrl Pts',(5.81717719642748,-2.92140224172418,20.033498496139));
#7316=CARTESIAN_POINT('Ctrl Pts',(5.81709141888581,-2.92144219299921,20.0335043593436));
#7317=CARTESIAN_POINT('Ctrl Pts',(5.81704827613498,-2.92146228576608,20.0335073083353));
#7318=CARTESIAN_POINT('Ctrl Pts',(5.81696147539766,-2.92150270891947,20.0335132415956));
#7319=CARTESIAN_POINT('Ctrl Pts',(5.81691781728047,-2.92152303933896,20.0335162258738));
#7320=CARTESIAN_POINT('Ctrl Pts',(5.81682997820801,-2.92156394125377,20.0335222302288));
#7321=CARTESIAN_POINT('Ctrl Pts',(5.81678579731698,-2.92158451269054,20.0335252503019));
#7322=CARTESIAN_POINT('Ctrl Pts',(5.81669690506214,-2.92162590010846,20.0335313267709));
#7323=CARTESIAN_POINT('Ctrl Pts',(5.81665219366934,-2.92164671607371,20.0335343831695));
#7324=CARTESIAN_POINT('Ctrl Pts',(5.81656649370655,-2.92168661240241,20.0335402415401));
#7325=CARTESIAN_POINT('Ctrl Pts',(5.8165255052001,-2.92170569293563,20.0335430435029));
#7326=CARTESIAN_POINT('Ctrl Pts',(5.80936120444545,-2.92504055853287,20.03403279767));
#7327=CARTESIAN_POINT('Ctrl Pts',(5.80222602422412,-2.92833017458233,20.0345213703911));
#7328=CARTESIAN_POINT('Ctrl Pts',(5.78589245937321,-2.93578832635036,20.0356415912259));
#7329=CARTESIAN_POINT('Ctrl Pts',(5.77668646957328,-2.93993973681065,20.0362742581863));
#7330=CARTESIAN_POINT('Ctrl Pts',(5.75211758274164,-2.95088032637994,20.0379658284221));
#7331=CARTESIAN_POINT('Ctrl Pts',(5.73672109396272,-2.95759268584033,20.0390291041189));
#7332=CARTESIAN_POINT('Ctrl Pts',(5.60174730892285,-3.01518539488075,20.0483739874767));
#7333=CARTESIAN_POINT('Ctrl Pts',(5.4792585254509,-3.05890494407524,20.0570116580039));
#7334=CARTESIAN_POINT('Ctrl Pts',(5.17519390166147,-3.14712598535538,20.0783182687046));
#7335=CARTESIAN_POINT('Ctrl Pts',(4.99171247775257,-3.18347130357153,20.0910440507683));
#7336=CARTESIAN_POINT('Ctrl Pts',(4.7154531055782,-3.21362131739292,20.1094728223012));
#7337=CARTESIAN_POINT('Ctrl Pts',(4.62440820435326,-3.21966357332375,20.1154355373931));
#7338=CARTESIAN_POINT('Ctrl Pts',(4.49321950416103,-3.22278887606631,20.1238537528369));
#7339=CARTESIAN_POINT('Ctrl Pts',(4.45320062382921,-3.22299678498016,20.1263988125576));
#7340=CARTESIAN_POINT('Ctrl Pts',(4.38139349742741,-3.22203231062258,20.1309252434993));
#7341=CARTESIAN_POINT('Ctrl Pts',(4.34960740189976,-3.22113477679159,20.1329147651224));
#7342=CARTESIAN_POINT('Ctrl Pts',(4.30101022805123,-3.21904237737638,20.1359357866314));
#7343=CARTESIAN_POINT('Ctrl Pts',(4.28418729247799,-3.21818586847259,20.1369777792007));
#7344=CARTESIAN_POINT('Ctrl Pts',(4.25359573460019,-3.21638778558901,20.1388659031364));
#7345=CARTESIAN_POINT('Ctrl Pts',(4.23982505984386,-3.21548959860791,20.1397133698728));
#7346=CARTESIAN_POINT('Ctrl Pts',(4.20981483239099,-3.21333852968221,20.1415550446753));
#7347=CARTESIAN_POINT('Ctrl Pts',(4.19357809131214,-3.21205092839857,20.1425481425902));
#7348=CARTESIAN_POINT('Ctrl Pts',(4.14908534781253,-3.20818294452152,20.1452607933752));
#7349=CARTESIAN_POINT('Ctrl Pts',(4.12085215251896,-3.20535238603411,20.1469724951313));
#7350=CARTESIAN_POINT('Ctrl Pts',(3.96445418755285,-3.18758334860892,20.1564064548065));
#7351=CARTESIAN_POINT('Ctrl Pts',(3.8372312947948,-3.16533037149005,20.1638947482334));
#7352=CARTESIAN_POINT('Ctrl Pts',(3.49661533133824,-3.08442180691213,20.1838253745984));
#7353=CARTESIAN_POINT('Ctrl Pts',(3.28739537265973,-3.01135137486931,20.1959120165873));
#7354=CARTESIAN_POINT('Ctrl Pts',(2.99186978768175,-2.87266090425585,20.2145409796746));
#7355=CARTESIAN_POINT('Ctrl Pts',(2.89869762689419,-2.82322070746324,20.2206735830858));
#7356=CARTESIAN_POINT('Ctrl Pts',(2.79326446088465,-2.76046499163195,20.2281133225626));
#7357=CARTESIAN_POINT('Ctrl Pts',(2.7784751074608,-2.75150009488225,20.2291688314202));
#7358=CARTESIAN_POINT('Ctrl Pts',(2.75584678180456,-2.73753314606053,20.230803361959));
#7359=CARTESIAN_POINT('Ctrl Pts',(2.74795585036782,-2.73261531606496,20.2313770493173));
#7360=CARTESIAN_POINT('Ctrl Pts',(2.73346046416206,-2.72349409198464,20.2324379317567));
#7361=CARTESIAN_POINT('Ctrl Pts',(2.72684994291019,-2.71930071811731,20.2329244729903));
#7362=CARTESIAN_POINT('Ctrl Pts',(2.71188965746375,-2.709734064192,20.2340317633046));
#7363=CARTESIAN_POINT('Ctrl Pts',(2.7035494538933,-2.70434628662569,20.2346534521706));
#7364=CARTESIAN_POINT('Ctrl Pts',(2.6819497674388,-2.6902509762051,20.2362746687025));
#7365=CARTESIAN_POINT('Ctrl Pts',(2.6687296200076,-2.68148404889672,20.2372779275445));
#7366=CARTESIAN_POINT('Ctrl Pts',(2.57900949322299,-2.62102785316734,20.2441590443347));
#7367=CARTESIAN_POINT('Ctrl Pts',(2.50470335423577,-2.56617395770382,20.2502183024655));
#7368=CARTESIAN_POINT('Ctrl Pts',(2.36860322579397,-2.45636936876508,20.2618715565205));
#7369=CARTESIAN_POINT('Ctrl Pts',(2.30636282134923,-2.40207754498297,20.2674431279201));
#7370=CARTESIAN_POINT('Ctrl Pts',(2.14978544891488,-2.25453025251069,20.2819928625193));
#7371=CARTESIAN_POINT('Ctrl Pts',(2.05899155860516,-2.1577304560453,20.2909715906244));
#7372=CARTESIAN_POINT('Ctrl Pts',(1.91192627110592,-1.98015592933211,20.3063083074358));
#7373=CARTESIAN_POINT('Ctrl Pts',(1.85290544149997,-1.90188718867303,20.3127323961146));
#7374=CARTESIAN_POINT('Ctrl Pts',(1.77381199807104,-1.78640181666568,20.3217269699739));
#7375=CARTESIAN_POINT('Ctrl Pts',(1.75076438177461,-1.75129746664236,20.3244011813034));
#7376=CARTESIAN_POINT('Ctrl Pts',(1.71082455016542,-1.68779276381244,20.329134128871));
#7377=CARTESIAN_POINT('Ctrl Pts',(1.69367095468105,-1.65956468570267,20.3312021313625));
#7378=CARTESIAN_POINT('Ctrl Pts',(1.66830039732782,-1.61633076657862,20.3343166353418));
#7379=CARTESIAN_POINT('Ctrl Pts',(1.65976434434846,-1.60151565374527,20.3353746560474));
#7380=CARTESIAN_POINT('Ctrl Pts',(1.64448238195334,-1.57449757419441,20.3372876979737));
#7381=CARTESIAN_POINT('Ctrl Pts',(1.63769703908918,-1.56231750673292,20.3381441215073));
#7382=CARTESIAN_POINT('Ctrl Pts',(1.62323351363649,-1.53595369522348,20.3399851467335));
#7383=CARTESIAN_POINT('Ctrl Pts',(1.61558230622519,-1.52175552614142,20.3409687705793));
#7384=CARTESIAN_POINT('Ctrl Pts',(1.59509423658253,-1.48304319123189,20.3436298541507));
#7385=CARTESIAN_POINT('Ctrl Pts',(1.58246581166175,-1.45841982528852,20.3452999569794));
#7386=CARTESIAN_POINT('Ctrl Pts',(1.51807178700059,-1.32877652926377,20.353980939165));
#7387=CARTESIAN_POINT('Ctrl Pts',(1.47173742439461,-1.22114985921871,20.3608017814509));
#7388=CARTESIAN_POINT('Ctrl Pts',(1.35217200510447,-0.895656203089265,20.3806244011082));
#7389=CARTESIAN_POINT('Ctrl Pts',(1.296257402794,-0.672247373377331,20.393168308898));
#7390=CARTESIAN_POINT('Ctrl Pts',(1.24940767471226,-0.336051254309889,20.4125051524799));
#7391=CARTESIAN_POINT('Ctrl Pts',(1.23982242172045,-0.226610598667985,20.418880058432));
#7392=CARTESIAN_POINT('Ctrl Pts',(1.23520751265689,-0.0994763455260606,
20.426592485967));
#7393=CARTESIAN_POINT('Ctrl Pts',(1.23471631830738,-0.0820410874345721,
20.4276568651638));
#7394=CARTESIAN_POINT('Ctrl Pts',(1.23417967116551,-0.0552756420812884,
20.4293022691181));
#7395=CARTESIAN_POINT('Ctrl Pts',(1.23403316091057,-0.0459475041239562,
20.4298778479594));
#7396=CARTESIAN_POINT('Ctrl Pts',(1.23383822938874,-0.0287931573369041,
20.4309404664841));
#7397=CARTESIAN_POINT('Ctrl Pts',(1.23377781117846,-0.0209672873408642,
20.431426836118));
#7398=CARTESIAN_POINT('Ctrl Pts',(1.23370557101281,-0.00325132210821304,
20.432531473411));
#7399=CARTESIAN_POINT('Ctrl Pts',(1.23371076933772,0.00663859296840534,
20.433150661333));
#7400=CARTESIAN_POINT('Ctrl Pts',(1.23384217768,0.0322609461688485,20.4347610960076));
#7401=CARTESIAN_POINT('Ctrl Pts',(1.23403807036731,0.0479925546045979,20.4357559949973));
#7402=CARTESIAN_POINT('Ctrl Pts',(1.23611316789384,0.152920866169307,20.442429938369));
#7403=CARTESIAN_POINT('Ctrl Pts',(1.24158030059646,0.24200026682429,20.4482784897219));
#7404=CARTESIAN_POINT('Ctrl Pts',(1.25939907103643,0.414716411022131,20.4598365065786));
#7405=CARTESIAN_POINT('Ctrl Pts',(1.27136083570037,0.49832808061199,20.4655324263059));
#7406=CARTESIAN_POINT('Ctrl Pts',(1.30367401373184,0.674513195164816,20.4776453424081));
#7407=CARTESIAN_POINT('Ctrl Pts',(1.32485419765819,0.76685964024731,20.484059683078));
#7408=CARTESIAN_POINT('Ctrl Pts',(1.39480270069939,1.02006747699278,20.501695061679));
#7409=CARTESIAN_POINT('Ctrl Pts',(1.45213240989311,1.17826759719335,20.5127533074032));
#7410=CARTESIAN_POINT('Ctrl Pts',(1.53819524297594,1.36799834712336,20.5259645828656));
#7411=CARTESIAN_POINT('Ctrl Pts',(1.5555313261051,1.40438671703225,20.5284970646515));
#7412=CARTESIAN_POINT('Ctrl Pts',(1.58181644870487,1.45699418154849,20.5321579301705));
#7413=CARTESIAN_POINT('Ctrl Pts',(1.59022937067149,1.47347539771574,20.5333047840139));
#7414=CARTESIAN_POINT('Ctrl Pts',(1.60529797065546,1.50237786852277,20.5353161771918));
#7415=CARTESIAN_POINT('Ctrl Pts',(1.61189397798415,1.51482951316069,20.536182784287));
#7416=CARTESIAN_POINT('Ctrl Pts',(1.62492858380067,1.53905028600817,20.5378687941861));
#7417=CARTESIAN_POINT('Ctrl Pts',(1.63135941257534,1.55082324601425,20.5386884494922));
#7418=CARTESIAN_POINT('Ctrl Pts',(1.64891372406711,1.5824884682818,20.5408936432014));
#7419=CARTESIAN_POINT('Ctrl Pts',(1.66017514654665,1.60230368785051,20.5422742340315));
#7420=CARTESIAN_POINT('Ctrl Pts',(1.70365329247344,1.67695170225576,20.5474794678214));
#7421=CARTESIAN_POINT('Ctrl Pts',(1.73728156691112,1.73094825153254,20.5512531149485));
#7422=CARTESIAN_POINT('Ctrl Pts',(1.95885876212814,2.06432086333692,20.5746927623689));
#7423=CARTESIAN_POINT('Ctrl Pts',(2.18798573699663,2.3137461611115,20.5926221221632));
#7424=CARTESIAN_POINT('Ctrl Pts',(2.48823381582663,2.55232515107536,20.6148909545366));
#7425=CARTESIAN_POINT('Ctrl Pts',(2.52555490973856,2.5806750602596,20.6176452888697));
#7426=CARTESIAN_POINT('Ctrl Pts',(2.588540489327,2.62638899941919,20.6222954793586));
#7427=CARTESIAN_POINT('Ctrl Pts',(2.61386186205316,2.64421536130786,20.6241654159564));
#7428=CARTESIAN_POINT('Ctrl Pts',(2.6491306161265,2.66829214229066,20.6267764707066));
#7429=CARTESIAN_POINT('Ctrl Pts',(2.6588620624634,2.67485780570083,20.6274975930849));
#7430=CARTESIAN_POINT('Ctrl Pts',(2.67536153894342,2.68585905714554,20.6287217683737));
#7431=CARTESIAN_POINT('Ctrl Pts',(2.68211091863217,2.69032266864342,20.6292229659869));
#7432=CARTESIAN_POINT('Ctrl Pts',(2.69506521365907,2.69881986428452,20.6301858891662));
#7433=CARTESIAN_POINT('Ctrl Pts',(2.70126731702476,2.70285756361273,20.6306473156675));
#7434=CARTESIAN_POINT('Ctrl Pts',(2.71614798101354,2.71247237146189,20.6317552853609));
#7435=CARTESIAN_POINT('Ctrl Pts',(2.72483945769178,2.71802920115407,20.6324031330788));
#7436=CARTESIAN_POINT('Ctrl Pts',(2.75629112064216,2.73792549743324,20.6347495969276));
#7437=CARTESIAN_POINT('Ctrl Pts',(2.77920324245831,2.75202113450313,20.6364629271834));
#7438=CARTESIAN_POINT('Ctrl Pts',(2.95354164134404,2.85628910374484,20.6495137254482));
#7439=CARTESIAN_POINT('Ctrl Pts',(3.11194687143989,2.93418249981422,20.6614345117631));
#7440=CARTESIAN_POINT('Ctrl Pts',(3.44210615082447,3.06416199695857,20.6854396598147));
#7441=CARTESIAN_POINT('Ctrl Pts',(3.6134741487632,3.11566895043166,20.697478531601));
#7442=CARTESIAN_POINT('Ctrl Pts',(3.8477529416144,3.16532507819361,20.7130876531449));
#7443=CARTESIAN_POINT('Ctrl Pts',(3.90761196640856,3.1762516946349,20.7170064603597));
#7444=CARTESIAN_POINT('Ctrl Pts',(4.01129732122736,3.19215927825279,20.723674691094));
#7445=CARTESIAN_POINT('Ctrl Pts',(4.05498102339162,3.19794721715642,20.7264479140934));
#7446=CARTESIAN_POINT('Ctrl Pts',(4.11782259031509,3.20496545558575,20.7303874057335));
#7447=CARTESIAN_POINT('Ctrl Pts',(4.13689262585017,3.20692312550297,20.731576335498));
#7448=CARTESIAN_POINT('Ctrl Pts',(4.1701109575492,3.21003396048734,20.7336362502505));
#7449=CARTESIAN_POINT('Ctrl Pts',(4.18425134964875,3.21126400659393,20.73450962429));
#7450=CARTESIAN_POINT('Ctrl Pts',(4.21337694933047,3.21360382356192,20.7363015460987));
#7451=CARTESIAN_POINT('Ctrl Pts',(4.22836273611425,3.21470229219921,20.7372197190299));
#7452=CARTESIAN_POINT('Ctrl Pts',(4.26666007168502,3.21724036473999,20.7395567500802));
#7453=CARTESIAN_POINT('Ctrl Pts',(4.28998083752481,3.21853145618465,20.7409709409398));
#7454=CARTESIAN_POINT('Ctrl Pts',(4.38108421032933,3.22258228036187,20.7464627472769));
#7455=CARTESIAN_POINT('Ctrl Pts',(4.4489357965181,3.22345523548394,20.7504816530738));
#7456=CARTESIAN_POINT('Ctrl Pts',(4.84827485961254,3.21598211746203,20.7738165118144));
#7457=CARTESIAN_POINT('Ctrl Pts',(5.17678795814548,3.15866346104973,20.7914900717375));
#7458=CARTESIAN_POINT('Ctrl Pts',(5.53495440649006,3.03729560693319,20.8134535400521));
#7459=CARTESIAN_POINT('Ctrl Pts',(5.57881788371412,3.02136193445235,20.8161965455119));
#7460=CARTESIAN_POINT('Ctrl Pts',(5.65109606151289,2.99331536852946,20.8208293857182));
#7461=CARTESIAN_POINT('Ctrl Pts',(5.67971126637191,2.98173588971379,20.8226935477415));
#7462=CARTESIAN_POINT('Ctrl Pts',(5.71895891253584,2.96519384252772,20.8252978185569));
#7463=CARTESIAN_POINT('Ctrl Pts',(5.7297381847252,2.96058117245109,20.8260180673548));
#7464=CARTESIAN_POINT('Ctrl Pts',(5.74791112929617,2.95268699595843,20.8272411930127));
#7465=CARTESIAN_POINT('Ctrl Pts',(5.75531818572171,2.94943622782203,20.8277422220125));
#7466=CARTESIAN_POINT('Ctrl Pts',(5.76948123786019,2.9431567271634,20.8287051744138));
#7467=CARTESIAN_POINT('Ctrl Pts',(5.7762391487376,2.94013254985871,20.8291668009553));
#7468=CARTESIAN_POINT('Ctrl Pts',(5.79239893157632,2.93283407811172,20.8302757185385));
#7469=CARTESIAN_POINT('Ctrl Pts',(5.8017907263311,2.92853785354625,20.8309243189601));
#7470=CARTESIAN_POINT('Ctrl Pts',(5.83564905679423,2.9128523062008,20.8332770583424));
#7471=CARTESIAN_POINT('Ctrl Pts',(5.85999217588149,2.90120126431552,20.8349960144749));
#7472=CARTESIAN_POINT('Ctrl Pts',(6.03284349692361,2.81578708472014,20.8473836888667));
#7473=CARTESIAN_POINT('Ctrl Pts',(6.1755968630441,2.73097097064393,20.8585693983261));
#7474=CARTESIAN_POINT('Ctrl Pts',(6.4377951656247,2.54645566370535,20.8802568993132));
#7475=CARTESIAN_POINT('Ctrl Pts',(6.55783681924014,2.44833609508093,20.890726944524));
#7476=CARTESIAN_POINT('Ctrl Pts',(6.75889532256174,2.25827201167407,20.9089762780794));
#7477=CARTESIAN_POINT('Ctrl Pts',(6.84261675183808,2.16962312873576,20.9168419363039));
#7478=CARTESIAN_POINT('Ctrl Pts',(6.93867446349931,2.05560598473064,20.9262046031921));
#7479=CARTESIAN_POINT('Ctrl Pts',(6.95595886930006,2.03455410289331,20.9279042989028));
#7480=CARTESIAN_POINT('Ctrl Pts',(6.98289058999791,2.00089079943567,20.9305774483291));
#7481=CARTESIAN_POINT('Ctrl Pts',(6.9927148628753,1.98842323995954,20.9315579725511));
#7482=CARTESIAN_POINT('Ctrl Pts',(7.01101018345009,1.96484923916137,20.9333944162909));
#7483=CARTESIAN_POINT('Ctrl Pts',(7.01950188144625,1.95375936356498,20.9342511416336));
#7484=CARTESIAN_POINT('Ctrl Pts',(7.03843922835544,1.92869186672666,20.9361717855173));
#7485=CARTESIAN_POINT('Ctrl Pts',(7.04884404664413,1.91468384211724,20.9372340908805));
#7486=CARTESIAN_POINT('Ctrl Pts',(7.07517470949746,1.87862669825667,20.939941097252));
#7487=CARTESIAN_POINT('Ctrl Pts',(7.0909363261925,1.85645895271271,20.9415794765655));
#7488=CARTESIAN_POINT('Ctrl Pts',(7.20050333873654,1.69815366806227,20.9531043423383));
#7489=CARTESIAN_POINT('Ctrl Pts',(7.28399717572356,1.55516711557353,20.9625898658224));
#7490=CARTESIAN_POINT('Ctrl Pts',(7.44818744653167,1.21664002217988,20.9837964926371));
#7491=CARTESIAN_POINT('Ctrl Pts',(7.52136408678864,1.01833134794205,20.99535411982));
#7492=CARTESIAN_POINT('Ctrl Pts',(7.5945379959547,0.738132985891712,21.0120888477955));
#7493=CARTESIAN_POINT('Ctrl Pts',(7.61163223008169,0.661256504066419,21.0167242860153));
#7494=CARTESIAN_POINT('Ctrl Pts',(7.62881137678469,0.567997817193637,21.0224832725238));
#7495=CARTESIAN_POINT('Ctrl Pts',(7.63161050260384,0.552135934576607,21.023467481253));
#7496=CARTESIAN_POINT('Ctrl Pts',(7.63579522938433,0.527337403274637,21.0250144523421));
#7497=CARTESIAN_POINT('Ctrl Pts',(7.63726235790212,0.518414524973121,21.0255727398601));
#7498=CARTESIAN_POINT('Ctrl Pts',(7.63993442073019,0.501724951712649,21.0266202822847));
#7499=CARTESIAN_POINT('Ctrl Pts',(7.64114851379147,0.493959919459706,21.0271090186155));
#7500=CARTESIAN_POINT('Ctrl Pts',(7.64386097654276,0.476185941869878,21.028230772511));
#7501=CARTESIAN_POINT('Ctrl Pts',(7.64534061062872,0.466174332302416,21.0288648193733));
#7502=CARTESIAN_POINT('Ctrl Pts',(7.64916093146459,0.439455441262774,21.0305625005589));
#7503=CARTESIAN_POINT('Ctrl Pts',(7.65141758979928,0.422736720527652,21.031630555888));
#7504=CARTESIAN_POINT('Ctrl Pts',(7.67054209998754,0.272140053014318,21.041298477021));
#7505=CARTESIAN_POINT('Ctrl Pts',(7.67911557658673,0.137357291392169,21.0502816467442));
#7506=CARTESIAN_POINT('Ctrl Pts',(7.67921879563721,0.00163395566385627,
21.0594235963388));
#7507=CARTESIAN_POINT('Ctrl Pts',(7.67921910621823,0.000816976217060092,
21.0594786294844));
#7508=CARTESIAN_POINT('Ctrl Pts',(7.67921910621823,2.36916961325777E-11,
21.0595336661193));
#7509=CARTESIAN_POINT('Ctrl Pts',(7.67921910621823,-1.24760202169227E-10,
20.8155686056964));
#7510=CARTESIAN_POINT('Ctrl Pts',(7.6792191062261,0.203257940460228,20.80189032375));
#7511=CARTESIAN_POINT('Ctrl Pts',(7.65998935550836,0.406090050604238,20.7880266178191));
#7512=CARTESIAN_POINT('Ctrl Pts',(7.59870376082183,0.726321729020061,20.7665139614357));
#7513=CARTESIAN_POINT('Ctrl Pts',(7.56876354080615,0.845465263401139,20.7585874627029));
#7514=CARTESIAN_POINT('Ctrl Pts',(7.523943767758,0.988666502017597,20.7491638285754));
#7515=CARTESIAN_POINT('Ctrl Pts',(7.51546199988171,1.01460573698085,20.7474608135917));
#7516=CARTESIAN_POINT('Ctrl Pts',(7.50152389680916,1.05546726803852,20.7447837277565));
#7517=CARTESIAN_POINT('Ctrl Pts',(7.4962850938062,1.07046186650283,20.7438025499587));
#7518=CARTESIAN_POINT('Ctrl Pts',(7.48623244264119,1.09856574117376,20.741965631895));
#7519=CARTESIAN_POINT('Ctrl Pts',(7.48144384267872,1.11168359522666,20.7411090798109));
#7520=CARTESIAN_POINT('Ctrl Pts',(7.47048712685998,1.14110328617626,20.7391897985364));
#7521=CARTESIAN_POINT('Ctrl Pts',(7.46427169298736,1.15738712454581,20.7381286737232));
#7522=CARTESIAN_POINT('Ctrl Pts',(7.44804219250174,1.19889299521616,20.7354265473123));
#7523=CARTESIAN_POINT('Ctrl Pts',(7.4378409880456,1.22404073238074,20.7337918288744));
#7524=CARTESIAN_POINT('Ctrl Pts',(7.36412608603623,1.39936994107175,20.7224057437365));
#7525=CARTESIAN_POINT('Ctrl Pts',(7.28960895896023,1.54467912888601,20.7130435841599));
#7526=CARTESIAN_POINT('Ctrl Pts',(7.15253708840796,1.76838638007053,20.6982482621205));
#7527=CARTESIAN_POINT('Ctrl Pts',(7.09678668209508,1.85059352979628,20.6927150567814));
#7528=CARTESIAN_POINT('Ctrl Pts',(6.95800088501966,2.03617332615649,20.6797461891262));
#7529=CARTESIAN_POINT('Ctrl Pts',(6.87221246868468,2.13725102567721,20.6723066282859));
#7530=CARTESIAN_POINT('Ctrl Pts',(6.75170724713302,2.26268013789008,20.6621570477182));
#7531=CARTESIAN_POINT('Ctrl Pts',(6.72238397565363,2.29204472459433,20.6597079433507));
#7532=CARTESIAN_POINT('Ctrl Pts',(6.67236566993344,2.34023544503516,20.6555473006361));
#7533=CARTESIAN_POINT('Ctrl Pts',(6.65197712163546,2.35937363585616,20.6538558339527));
#7534=CARTESIAN_POINT('Ctrl Pts',(6.62316937748986,2.38571795762875,20.6514677209536));
#7535=CARTESIAN_POINT('Ctrl Pts',(6.61495749831553,2.39315024428694,20.6507871724835));
#7536=CARTESIAN_POINT('Ctrl Pts',(6.600678099961,2.40594074688318,20.6496037966797));
#7537=CARTESIAN_POINT('Ctrl Pts',(6.5946283121756,2.41131878741107,20.6491024351465));
#7538=CARTESIAN_POINT('Ctrl Pts',(6.58301236934597,2.42156685042413,20.6481396556417));
#7539=CARTESIAN_POINT('Ctrl Pts',(6.5774496164347,2.4264405893615,20.6476785395253));
#7540=CARTESIAN_POINT('Ctrl Pts',(6.56409996640319,2.43805574235876,20.6465719239631));
#7541=CARTESIAN_POINT('Ctrl Pts',(6.55629748751088,2.44477901005511,20.6459251265765));
#7542=CARTESIAN_POINT('Ctrl Pts',(6.52808644334703,2.46885332545938,20.6435869123943));
#7543=CARTESIAN_POINT('Ctrl Pts',(6.5074945945319,2.48598661945031,20.6418809145935));
#7544=CARTESIAN_POINT('Ctrl Pts',(6.34453104947261,2.61817631557478,20.628401220226));
#7545=CARTESIAN_POINT('Ctrl Pts',(6.19281620159547,2.72116002521634,20.615998648016));
#7546=CARTESIAN_POINT('Ctrl Pts',(5.88174862151484,2.89566070739654,20.5918700573903));
#7547=CARTESIAN_POINT('Ctrl Pts',(5.72366501311888,2.96824847082924,20.5801823209653));
#7548=CARTESIAN_POINT('Ctrl Pts',(5.47551235773078,3.05873329744433,20.5629773745373));
#7549=CARTESIAN_POINT('Ctrl Pts',(5.38926380573703,3.08612948045021,20.5571903115747));
#7550=CARTESIAN_POINT('Ctrl Pts',(5.27790731466135,3.11640475872218,20.5499578868994));
#7551=CARTESIAN_POINT('Ctrl Pts',(5.25376945080736,3.12266738016391,20.5484041296313));
#7552=CARTESIAN_POINT('Ctrl Pts',(5.21464094984338,3.13233606290279,20.5459073727343));
#7553=CARTESIAN_POINT('Ctrl Pts',(5.19969474289645,3.13591604184041,20.5449588083495));
#7554=CARTESIAN_POINT('Ctrl Pts',(5.17102179811783,3.14256739720128,20.5431487066705));
#7555=CARTESIAN_POINT('Ctrl Pts',(5.15729947838207,3.14565608336492,20.5422866323182));
#7556=CARTESIAN_POINT('Ctrl Pts',(5.12594556248534,3.1524980216798,20.5403262652642));
#7557=CARTESIAN_POINT('Ctrl Pts',(5.10830171704411,3.15619339872267,20.5392298431364));
#7558=CARTESIAN_POINT('Ctrl Pts',(5.05260318548244,3.16737206698251,20.5357891321195));
#7559=CARTESIAN_POINT('Ctrl Pts',(5.01444304553417,3.17431676563756,20.5334619398997));
#7560=CARTESIAN_POINT('Ctrl Pts',(4.71393741233468,3.22341854804529,20.5153498105479));
#7561=CARTESIAN_POINT('Ctrl Pts',(4.44742107592595,3.23367423882385,20.5006737179238));
#7562=CARTESIAN_POINT('Ctrl Pts',(4.06353980416161,3.20093963814636,20.4790725630545));
#7563=CARTESIAN_POINT('Ctrl Pts',(3.94509511252665,3.184164019046,20.4723235635139));
#7564=CARTESIAN_POINT('Ctrl Pts',(3.78954398774724,3.15322930830187,20.4630472432282));
#7565=CARTESIAN_POINT('Ctrl Pts',(3.7513658642522,3.1449122936069,20.4607366398938));
#7566=CARTESIAN_POINT('Ctrl Pts',(3.68704564691588,3.12967025138595,20.4567720802185));
#7567=CARTESIAN_POINT('Ctrl Pts',(3.66082164240132,3.1231063616649,20.4551352820614));
#7568=CARTESIAN_POINT('Ctrl Pts',(3.62392674084557,3.11337671115039,20.4527995567347));
#7569=CARTESIAN_POINT('Ctrl Pts',(3.61318412502423,3.11048416933536,20.4521155077195));
#7570=CARTESIAN_POINT('Ctrl Pts',(3.59476433537833,3.105422047809,20.4509354558885));
#7571=CARTESIAN_POINT('Ctrl Pts',(3.58707973035685,3.10327944587264,20.4504409990242));
#7572=CARTESIAN_POINT('Ctrl Pts',(3.57213506253294,3.09905274435522,20.4494750962023));
#7573=CARTESIAN_POINT('Ctrl Pts',(3.56487430613983,3.09697163739382,20.4490038487882));
#7574=CARTESIAN_POINT('Ctrl Pts',(3.54500772836103,3.09120174594519,20.4477091675299));
#7575=CARTESIAN_POINT('Ctrl Pts',(3.53241720034677,3.08746143924772,20.4468828292859));
#7576=CARTESIAN_POINT('Ctrl Pts',(3.48346842136487,3.07259385096927,20.4436484500621));
#7577=CARTESIAN_POINT('Ctrl Pts',(3.44728692398579,3.06090090251647,20.4412107480804));
#7578=CARTESIAN_POINT('Ctrl Pts',(3.20529514745477,2.97793848262771,20.4246280459604));
#7579=CARTESIAN_POINT('Ctrl Pts',(3.00697034113911,2.88660677169174,20.4097130586563));
#7580=CARTESIAN_POINT('Ctrl Pts',(2.70060084843092,2.70593053389447,20.3857514398787));
#7581=CARTESIAN_POINT('Ctrl Pts',(2.58642818491596,2.62832404664212,20.3765728759691));
#7582=CARTESIAN_POINT('Ctrl Pts',(2.41540983311767,2.49527492241208,20.3625349108826));
#7583=CARTESIAN_POINT('Ctrl Pts',(2.35504024960806,2.44465097302806,20.3575144372955));
#7584=CARTESIAN_POINT('Ctrl Pts',(2.27890749228751,2.37590195233017,20.3510920914764));
#7585=CARTESIAN_POINT('Ctrl Pts',(2.26141027714564,2.35974605738787,20.3496093961948));
#7586=CARTESIAN_POINT('Ctrl Pts',(2.23309616264653,2.333015012279,20.3471985648858));
#7587=CARTESIAN_POINT('Ctrl Pts',(2.22217203866494,2.32255525662752,20.3462655463012));
#7588=CARTESIAN_POINT('Ctrl Pts',(2.20117150344368,2.30216212912379,20.3444661209253));
#7589=CARTESIAN_POINT('Ctrl Pts',(2.19108610178463,2.29223855633506,20.3435993197227));
#7590=CARTESIAN_POINT('Ctrl Pts',(2.1679136661994,2.26913562952003,20.3416013858849));
#7591=CARTESIAN_POINT('Ctrl Pts',(2.15487447642931,2.25590883895909,20.3404723804837));
#7592=CARTESIAN_POINT('Ctrl Pts',(2.11285165171629,2.21253778197229,20.3368173930513));
#7593=CARTESIAN_POINT('Ctrl Pts',(2.08433949533688,2.18194123681857,20.3343117528587));
#7594=CARTESIAN_POINT('Ctrl Pts',(1.92298277105438,2.00188593293669,20.3199596174104));
#7595=CARTESIAN_POINT('Ctrl Pts',(1.80367825308385,1.84087302224888,20.3086884487533));
#7596=CARTESIAN_POINT('Ctrl Pts',(1.59027512033337,1.48860411157131,20.2856448669569));
#7597=CARTESIAN_POINT('Ctrl Pts',(1.49864568288021,1.29702278404258,20.2739297414775));
#7598=CARTESIAN_POINT('Ctrl Pts',(1.41528918661982,1.06696876460386,20.2593346217264));
#7599=CARTESIAN_POINT('Ctrl Pts',(1.40456724890996,1.03590178631152,20.2573525153534));
#7600=CARTESIAN_POINT('Ctrl Pts',(1.39057778088595,0.993263436025819,20.2546100502707));
#7601=CARTESIAN_POINT('Ctrl Pts',(1.38689673438307,0.981828557120877,20.2538724164229));
#7602=CARTESIAN_POINT('Ctrl Pts',(1.38082694378758,0.962605428850905,20.2526283610638));
#7603=CARTESIAN_POINT('Ctrl Pts',(1.37840360118651,0.95482808261079,20.2521239370618));
#7604=CARTESIAN_POINT('Ctrl Pts',(1.37385129024226,0.940020700127089,20.2511613218751));
#7605=CARTESIAN_POINT('Ctrl Pts',(1.37171682348752,0.932992426373027,20.2507034701408));
#7606=CARTESIAN_POINT('Ctrl Pts',(1.3667033594522,0.916279042268058,20.2496125382579));
#7607=CARTESIAN_POINT('Ctrl Pts',(1.36384586601288,0.906587635549567,20.2489782401659));
#7608=CARTESIAN_POINT('Ctrl Pts',(1.35391925631181,0.872327679480057,20.2467303040314));
#7609=CARTESIAN_POINT('Ctrl Pts',(1.34709717001337,0.847689341173257,20.2451034746778));
#7610=CARTESIAN_POINT('Ctrl Pts',(1.28648369248787,0.618197672365597,20.2298725880862));
#7611=CARTESIAN_POINT('Ctrl Pts',(1.25272076689596,0.408605982979522,20.2154244926738));
#7612=CARTESIAN_POINT('Ctrl Pts',(1.23033864421164,0.0435797743187418,20.1907206631199));
#7613=CARTESIAN_POINT('Ctrl Pts',(1.23193806497929,-0.110569175730084,20.1804204087835));
#7614=CARTESIAN_POINT('Ctrl Pts',(1.25145946029103,-0.348049065600556,20.1649425440327));
#7615=CARTESIAN_POINT('Ctrl Pts',(1.26166099667973,-0.431773357404261,20.1595587545492));
#7616=CARTESIAN_POINT('Ctrl Pts',(1.27902942970534,-0.539062577063086,20.1527505866144));
#7617=CARTESIAN_POINT('Ctrl Pts',(1.28319630573297,-0.563072949058847,20.1512328028228));
#7618=CARTESIAN_POINT('Ctrl Pts',(1.29041203669186,-0.602023744971367,20.1487795490925));
#7619=CARTESIAN_POINT('Ctrl Pts',(1.29329522837953,-0.616993507509841,20.1478388638717));
#7620=CARTESIAN_POINT('Ctrl Pts',(1.29905018209044,-0.645772576752312,20.146034389472));
#7621=CARTESIAN_POINT('Ctrl Pts',(1.30190658538588,-0.659584562787673,20.1451701342649));
#7622=CARTESIAN_POINT('Ctrl Pts',(1.30867510920621,-0.691263351746486,20.1431917593684));
#7623=CARTESIAN_POINT('Ctrl Pts',(1.31264886001595,-0.709116598340052,20.1420796335322));
#7624=CARTESIAN_POINT('Ctrl Pts',(1.32584814273356,-0.76612540676154,20.1385367285437));
#7625=CARTESIAN_POINT('Ctrl Pts',(1.33565509216899,-0.805143379692991,20.1361245567497));
#7626=CARTESIAN_POINT('Ctrl Pts',(1.41168727026304,-1.08534479382796,20.1188715974321));
#7627=CARTESIAN_POINT('Ctrl Pts',(1.50505740756165,-1.31827664298623,20.1049915521263));
#7628=CARTESIAN_POINT('Ctrl Pts',(1.68630305642329,-1.65199931205563,20.0837317363204));
#7629=CARTESIAN_POINT('Ctrl Pts',(1.75498278903876,-1.76206936643015,20.0764430315668));
#7630=CARTESIAN_POINT('Ctrl Pts',(1.85384761567692,-1.90109400940692,20.0664836399689));
#7631=CARTESIAN_POINT('Ctrl Pts',(1.87823172031496,-1.93403431536836,20.0640639190838));
#7632=CARTESIAN_POINT('Ctrl Pts',(1.92033470756023,-1.9886993444595,20.0599295794272));
#7633=CARTESIAN_POINT('Ctrl Pts',(1.93772142845937,-2.01067470902559,20.0582341012643));
#7634=CARTESIAN_POINT('Ctrl Pts',(1.96250895929181,-2.04117802014961,20.0558288074632));
#7635=CARTESIAN_POINT('Ctrl Pts',(1.96967194866709,-2.04989873231762,20.0551350880543));
#7636=CARTESIAN_POINT('Ctrl Pts',(1.98199428400089,-2.06474114823008,20.0539436394842));
#7637=CARTESIAN_POINT('Ctrl Pts',(1.98713099088256,-2.07088167840589,20.0534475359148));
#7638=CARTESIAN_POINT('Ctrl Pts',(1.99712953798906,-2.08274406169786,20.0524828396211));
#7639=CARTESIAN_POINT('Ctrl Pts',(2.00198854631444,-2.08846812681644,20.0520144732105));
#7640=CARTESIAN_POINT('Ctrl Pts',(2.01525484993465,-2.1039860075396,20.0507370561269));
#7641=CARTESIAN_POINT('Ctrl Pts',(2.0237009456924,-2.1137462546264,20.0499252291492));
#7642=CARTESIAN_POINT('Ctrl Pts',(2.0561805337055,-2.15082689871259,20.0468097258168));
#7643=CARTESIAN_POINT('Ctrl Pts',(2.08061648811493,-2.17778916729506,20.0444790059511));
#7644=CARTESIAN_POINT('Ctrl Pts',(2.28207448279141,-2.39264851399055,20.0254098062097));
#7645=CARTESIAN_POINT('Ctrl Pts',(2.48062649945428,-2.55906294482358,20.0075953142518));
#7646=CARTESIAN_POINT('Ctrl Pts',(2.82526077354712,-2.78365780893886,19.9800813837387));
#7647=CARTESIAN_POINT('Ctrl Pts',(2.95943637791279,-2.85805805322755,19.9700408879759));
#7648=CARTESIAN_POINT('Ctrl Pts',(3.13334299989975,-2.938866839654,19.9578952435934));
#7649=CARTESIAN_POINT('Ctrl Pts',(3.1685609613684,-2.95447014054449,19.9554770547485));
#7650=CARTESIAN_POINT('Ctrl Pts',(3.22079471556389,-2.97650072554189,19.9519496106603));
#7651=CARTESIAN_POINT('Ctrl Pts',(3.23759768930003,-2.98342089882741,19.9508237339326));
#7652=CARTESIAN_POINT('Ctrl Pts',(3.26748930596217,-2.99543683543929,19.9488362390606));
#7653=CARTESIAN_POINT('Ctrl Pts',(3.28055429751014,-3.00058980420504,19.9479727107522));
#7654=CARTESIAN_POINT('Ctrl Pts',(3.30805952469041,-3.01123091393206,19.9461653946557));
#7655=CARTESIAN_POINT('Ctrl Pts',(3.3225064062497,-3.01670097823114,19.945222230232));
#7656=CARTESIAN_POINT('Ctrl Pts',(3.36071279427442,-3.03085392928518,19.9427436623629));
#7657=CARTESIAN_POINT('Ctrl Pts',(3.38453645659788,-3.03936142735575,19.9412141079569));
#7658=CARTESIAN_POINT('Ctrl Pts',(3.48844873359562,-3.07509499564038,19.9346087210251));
#7659=CARTESIAN_POINT('Ctrl Pts',(3.56949541547581,-3.0994438445374,19.9296274781268));
#7660=CARTESIAN_POINT('Ctrl Pts',(3.87510280463767,-3.17828549753513,19.9113407801115));
#7661=CARTESIAN_POINT('Ctrl Pts',(4.10434396128122,-3.21177452756352,19.8986562972658));
#7662=CARTESIAN_POINT('Ctrl Pts',(4.47971555154625,-3.22590940141942,19.8774889338543));
#7663=CARTESIAN_POINT('Ctrl Pts',(4.62441592132182,-3.22161685842743,19.8692162974869));
#7664=CARTESIAN_POINT('Ctrl Pts',(4.78651243498082,-3.20585762362093,19.8593535461784));
#7665=CARTESIAN_POINT('Ctrl Pts',(4.80469026986745,-3.20393409536691,19.8582389634646));
#7666=CARTESIAN_POINT('Ctrl Pts',(4.83229288190581,-3.20077559077427,19.8565321505794));
#7667=CARTESIAN_POINT('Ctrl Pts',(4.84173052562481,-3.19965334469102,19.8559460178015));
#7668=CARTESIAN_POINT('Ctrl Pts',(4.85892194073672,-3.19753192283268,19.8548734480458));
#7669=CARTESIAN_POINT('Ctrl Pts',(4.86667717562877,-3.1965462640085,19.8543877706623));
#7670=CARTESIAN_POINT('Ctrl Pts',(4.88403362947328,-3.19427612642629,19.853296703348));
#7671=CARTESIAN_POINT('Ctrl Pts',(4.89363259764473,-3.19297658454093,19.8526904947386));
#7672=CARTESIAN_POINT('Ctrl Pts',(4.92162264998712,-3.18905861237541,19.8509149535667));
#7673=CARTESIAN_POINT('Ctrl Pts',(4.93999677737464,-3.18632446650533,19.8497394688616));
#7674=CARTESIAN_POINT('Ctrl Pts',(5.1085324262356,-3.15975436535562,19.8388724412056));
#7675=CARTESIAN_POINT('Ctrl Pts',(5.25683910587114,-3.12548102727469,19.8286976206247));
#7676=CARTESIAN_POINT('Ctrl Pts',(5.43373017371002,-3.07118370025185,19.8162044147342));
#7677=CARTESIAN_POINT('Ctrl Pts',(5.46515468487823,-3.06100668064633,19.8139704444758));
#7678=CARTESIAN_POINT('Ctrl Pts',(5.64130152808877,-3.00095336228902,19.8013802254744));
#7679=CARTESIAN_POINT('Ctrl Pts',(5.78249319775757,-2.94129489771561,19.7910411925474));
#7680=CARTESIAN_POINT('Ctrl Pts',(6.02393773082323,-2.81834155729616,19.7731953955648));
#7681=CARTESIAN_POINT('Ctrl Pts',(6.12595464539173,-2.75913585088555,19.7655945915664));
#7682=CARTESIAN_POINT('Ctrl Pts',(6.24707572910493,-2.6796593074015,19.756498768043));
#7683=CARTESIAN_POINT('Ctrl Pts',(6.26945597515771,-2.6645684014369,19.7548146595061));
#7684=CARTESIAN_POINT('Ctrl Pts',(6.30464751193567,-2.64019021200097,19.7521603860266));
#7685=CARTESIAN_POINT('Ctrl Pts',(6.31758415818323,-2.63108695266961,19.7511833177971));
#7686=CARTESIAN_POINT('Ctrl Pts',(6.34182106850008,-2.61376371900126,19.7493500314472));
#7687=CARTESIAN_POINT('Ctrl Pts',(6.35313587150298,-2.60556481240337,19.7484930348424));
#7688=CARTESIAN_POINT('Ctrl Pts',(6.37852230530873,-2.58691635862701,19.7465674512095));
#7689=CARTESIAN_POINT('Ctrl Pts',(6.39256280608908,-2.57642503303667,19.7455005146797));
#7690=CARTESIAN_POINT('Ctrl Pts',(6.42837835861238,-2.54920486003063,19.7427733380155));
#7691=CARTESIAN_POINT('Ctrl Pts',(6.45002673253861,-2.53231111412581,19.7411195851715));
#7692=CARTESIAN_POINT('Ctrl Pts',(6.6297510256859,-2.38832630670371,19.7273372753132));
#7693=CARTESIAN_POINT('Ctrl Pts',(6.77572779417187,-2.24684466245014,19.7158352373193));
#7694=CARTESIAN_POINT('Ctrl Pts',(7.05407028301371,-1.92082684355086,19.6918202814469));
#7695=CARTESIAN_POINT('Ctrl Pts',(7.18221625672768,-1.73418107325598,19.679400318638));
#7696=CARTESIAN_POINT('Ctrl Pts',(7.30585583971991,-1.50607079426406,19.6639357204327));
#7697=CARTESIAN_POINT('Ctrl Pts',(7.32145310892779,-1.47618442407018,19.6619036633946));
#7698=CARTESIAN_POINT('Ctrl Pts',(7.34202125897629,-1.43521897247623,19.6591028451176));
#7699=CARTESIAN_POINT('Ctrl Pts',(7.34740315719715,-1.42434722846931,19.6583580796775));
#7700=CARTESIAN_POINT('Ctrl Pts',(7.35630692692184,-1.40610274672691,19.6571053784026));
#7701=CARTESIAN_POINT('Ctrl Pts',(7.35986243244629,-1.3987464070686,19.6565995022249));
#7702=CARTESIAN_POINT('Ctrl Pts',(7.36655200965819,-1.38477027029404,19.6556367839711));
#7703=CARTESIAN_POINT('Ctrl Pts',(7.36969156103243,-1.37815316007054,19.6551802979656));
#7704=CARTESIAN_POINT('Ctrl Pts',(7.37707287882182,-1.36245791558826,19.6540960455252));
#7705=CARTESIAN_POINT('Ctrl Pts',(7.38129488731788,-1.35337064851568,19.6534670950788));
#7706=CARTESIAN_POINT('Ctrl Pts',(7.39603633287587,-1.32125063906304,19.6512402017276));
#7707=CARTESIAN_POINT('Ctrl Pts',(7.40632631602469,-1.29811443285608,19.6496293072818));
#7708=CARTESIAN_POINT('Ctrl Pts',(7.50289398300163,-1.07391099812518,19.6339697595508));
#7709=CARTESIAN_POINT('Ctrl Pts',(7.56875016578579,-0.864686239394832,19.619020285394));
#7710=CARTESIAN_POINT('Ctrl Pts',(7.65691843364384,-0.436815108652667,19.5895292030837));
#7711=CARTESIAN_POINT('Ctrl Pts',(7.67914521343245,-0.219257380582916,19.5750715637153));
#7712=CARTESIAN_POINT('Ctrl Pts',(7.6792190449084,-0.000725876579082373,
19.5612958883318));
#7713=CARTESIAN_POINT('Ctrl Pts',(7.67921910621823,-0.000362938246920867,
19.561273011506));
#7714=CARTESIAN_POINT('Ctrl Pts',(7.67921910621823,-6.1812332959659E-13,
19.5612501365773));
#7715=CARTESIAN_POINT('Origin',(4.45646910621825,-5.13094777615093E-16,
-2.31077344927308));
#7716=CARTESIAN_POINT('',(7.67921910621823,-1.45987529487438E-10,18.3139723139554));
#7717=CARTESIAN_POINT('',(7.67921897520325,-0.000918943817116763,18.5636187829496));
#7718=CARTESIAN_POINT('',(7.67921910621823,-3.51191647465084E-13,-2.31077344927308));
#7719=CARTESIAN_POINT('Ctrl Pts',(7.67921897520336,-0.000918943050560485,
18.563618782904));
#7720=CARTESIAN_POINT('Ctrl Pts',(7.67917356350457,-0.160178590564636,18.5730889559059));
#7721=CARTESIAN_POINT('Ctrl Pts',(7.66732338519769,-0.319224689801024,18.582188712083));
#7722=CARTESIAN_POINT('Ctrl Pts',(7.61684168702354,-0.656712027958172,18.601389853412));
#7723=CARTESIAN_POINT('Ctrl Pts',(7.57473373595707,-0.834053580990784,18.6114133596575));
#7724=CARTESIAN_POINT('Ctrl Pts',(7.5073910412776,-1.03880805762323,18.6237545995969));
#7725=CARTESIAN_POINT('Ctrl Pts',(7.49639354296673,-1.07056346511797,18.6256919062879));
#7726=CARTESIAN_POINT('Ctrl Pts',(7.46242930077096,-1.16388954087417,18.6314701367851));
#7727=CARTESIAN_POINT('Ctrl Pts',(7.438075150811,-1.22493250391884,18.6353596962907));
#7728=CARTESIAN_POINT('Ctrl Pts',(7.40557325509175,-1.2996737858473,18.6403102253246));
#7729=CARTESIAN_POINT('Ctrl Pts',(7.39916576821595,-1.31411702777398,18.6412757729855));
#7730=CARTESIAN_POINT('Ctrl Pts',(7.38891397262255,-1.33677481829658,18.642805404894));
#7731=CARTESIAN_POINT('Ctrl Pts',(7.38514065592759,-1.34502147140448,18.6433652739932));
#7732=CARTESIAN_POINT('Ctrl Pts',(7.37836486266749,-1.35966639418101,18.6443653057261));
#7733=CARTESIAN_POINT('Ctrl Pts',(7.37537608714793,-1.36607084314315,18.6448046251953));
#7734=CARTESIAN_POINT('Ctrl Pts',(7.36818336454741,-1.38135227718971,18.64585761081));
#7735=CARTESIAN_POINT('Ctrl Pts',(7.36395991403987,-1.3902198503516,18.6464724634038));
#7736=CARTESIAN_POINT('Ctrl Pts',(7.35108385516542,-1.41693915595175,18.6483363587531));
#7737=CARTESIAN_POINT('Ctrl Pts',(7.34230706769252,-1.43473005502303,18.6495926589333));
#7738=CARTESIAN_POINT('Ctrl Pts',(7.32159332733969,-1.47575852029142,18.6525233890286));
#7739=CARTESIAN_POINT('Ctrl Pts',(7.30953707559525,-1.49893398206685,18.6542040508736));
#7740=CARTESIAN_POINT('Ctrl Pts',(7.17184995981142,-1.75592646754528,18.6731031286075));
#7741=CARTESIAN_POINT('Ctrl Pts',(7.01807954662349,-1.97350568006721,18.6914450774901));
#7742=CARTESIAN_POINT('Ctrl Pts',(6.73319137800491,-2.28637827532187,18.7196838462234));
#7743=CARTESIAN_POINT('Ctrl Pts',(6.61858264811044,-2.39505068158381,18.7299725698775));
#7744=CARTESIAN_POINT('Ctrl Pts',(6.47557964101822,-2.51197883283734,18.7415989456958));
#7745=CARTESIAN_POINT('Ctrl Pts',(6.45448577515163,-2.52878913120045,18.7432859974226));
#7746=CARTESIAN_POINT('Ctrl Pts',(6.41945606182192,-2.55599331767073,18.7460427883805));
#7747=CARTESIAN_POINT('Ctrl Pts',(6.40564306879896,-2.56654252066682,18.7471186480954));
#7748=CARTESIAN_POINT('Ctrl Pts',(6.38058119887818,-2.5853636385761,18.7490508222521));
#7749=CARTESIAN_POINT('Ctrl Pts',(6.36936270492503,-2.59367511044622,18.7499086723365));
#7750=CARTESIAN_POINT('Ctrl Pts',(6.34523741372527,-2.61130719827547,18.7517386315419));
#7751=CARTESIAN_POINT('Ctrl Pts',(6.33231481186469,-2.62060563725948,18.752709867849));
#7752=CARTESIAN_POINT('Ctrl Pts',(6.29692131942659,-2.645677021416,18.755346047474));
#7753=CARTESIAN_POINT('Ctrl Pts',(6.27431662203581,-2.66125942566688,18.757003708272));
#7754=CARTESIAN_POINT('Ctrl Pts',(6.14725794539208,-2.7464721192601,18.7661826513142));
#7755=CARTESIAN_POINT('Ctrl Pts',(6.03899798318785,-2.81024617558669,18.7734821598319));
#7756=CARTESIAN_POINT('Ctrl Pts',(5.79545616018205,-2.93516293020397,18.7890917753257));
#7757=CARTESIAN_POINT('Ctrl Pts',(5.65912042505228,-2.9936097426788,18.7973262161945));
#7758=CARTESIAN_POINT('Ctrl Pts',(5.36020121707528,-3.09802645040613,18.8150566582545));
#7759=CARTESIAN_POINT('Ctrl Pts',(5.19706273181819,-3.14102003279783,18.8245450803554));
#7760=CARTESIAN_POINT('Ctrl Pts',(5.00483253038499,-3.1758684797173,18.8362565915394));
#7761=CARTESIAN_POINT('Ctrl Pts',(4.97827150468608,-3.18034042122053,18.8378865374679));
#7762=CARTESIAN_POINT('Ctrl Pts',(4.94146034302869,-3.18606459145615,18.8401655620948));
#7763=CARTESIAN_POINT('Ctrl Pts',(4.93125474143186,-3.18760139832158,18.840799530006));
#7764=CARTESIAN_POINT('Ctrl Pts',(4.91371750308837,-3.19015614888042,18.8418928565044));
#7765=CARTESIAN_POINT('Ctrl Pts',(4.90638934317869,-3.19119791433405,18.8423508904925));
#7766=CARTESIAN_POINT('Ctrl Pts',(4.89104354812957,-3.19332555166944,18.8433126299002));
#7767=CARTESIAN_POINT('Ctrl Pts',(4.88302535938324,-3.19440648357651,18.8438166198042));
#7768=CARTESIAN_POINT('Ctrl Pts',(4.86336909043711,-3.19698102011017,18.8450556216426));
#7769=CARTESIAN_POINT('Ctrl Pts',(4.85172682485273,-3.19844127130076,18.8457924663105));
#7770=CARTESIAN_POINT('Ctrl Pts',(4.8093689262314,-3.20351928690994,18.8484835548272));
#7771=CARTESIAN_POINT('Ctrl Pts',(4.77861068689287,-3.20675829185713,18.8504572325396));
#7772=CARTESIAN_POINT('Ctrl Pts',(4.70121818108527,-3.21378349008913,18.8554644493983));
#7773=CARTESIAN_POINT('Ctrl Pts',(4.6545401249802,-3.216997646603,18.8585218473489));
#7774=CARTESIAN_POINT('Ctrl Pts',(4.27363471350332,-3.23490492109894,18.8836915536146));
#7775=CARTESIAN_POINT('Ctrl Pts',(3.93902101098271,-3.19849399258761,18.906900344412));
#7776=CARTESIAN_POINT('Ctrl Pts',(3.55291754202133,-3.09418390780742,18.9326539648519));
#7777=CARTESIAN_POINT('Ctrl Pts',(3.49042217883087,-3.07524532503367,18.9367998591109));
#7778=CARTESIAN_POINT('Ctrl Pts',(3.40672109736123,-3.04707675217856,18.9423248363451));
#7779=CARTESIAN_POINT('Ctrl Pts',(3.38497961444894,-3.03949961818888,18.9437574399099));
#7780=CARTESIAN_POINT('Ctrl Pts',(3.34925324939164,-3.02661762234632,18.9461078309039));
#7781=CARTESIAN_POINT('Ctrl Pts',(3.33522105625367,-3.0214473366213,18.9470300391507));
#7782=CARTESIAN_POINT('Ctrl Pts',(3.30790869940422,-3.01116738226655,18.9488233570551));
#7783=CARTESIAN_POINT('Ctrl Pts',(3.29462540522846,-3.00606707124693,18.9496947538756));
#7784=CARTESIAN_POINT('Ctrl Pts',(3.26333241909884,-2.99381327201624,18.9517459861798));
#7785=CARTESIAN_POINT('Ctrl Pts',(3.24535248127419,-2.98658494069769,18.952923282763));
#7786=CARTESIAN_POINT('Ctrl Pts',(3.18557894507538,-2.96192609491856,18.9568338210127));
#7787=CARTESIAN_POINT('Ctrl Pts',(3.14408651938923,-2.94377652757285,18.9595427977026));
#7788=CARTESIAN_POINT('Ctrl Pts',(3.04576102040916,-2.89827476731839,18.9659596879517));
#7789=CARTESIAN_POINT('Ctrl Pts',(2.98932062613632,-2.8701167165736,18.9696407473141));
#7790=CARTESIAN_POINT('Ctrl Pts',(2.62460320862054,-2.67458738133287,18.9935192532195));
#7791=CARTESIAN_POINT('Ctrl Pts',(2.34466244250546,-2.45954024522084,19.0120208142239));
#7792=CARTESIAN_POINT('Ctrl Pts',(2.08611660375009,-2.18364397895329,19.0346758970734));
#7793=CARTESIAN_POINT('Ctrl Pts',(2.06759245105464,-2.16336317465537,19.0363374809732));
#7794=CARTESIAN_POINT('Ctrl Pts',(2.04242232926372,-2.13508867829872,19.03865295371));
#7795=CARTESIAN_POINT('Ctrl Pts',(2.03555184824896,-2.12729526129635,19.039291071974));
#7796=CARTESIAN_POINT('Ctrl Pts',(2.02383940043123,-2.11387921477343,19.0403896635026));
#7797=CARTESIAN_POINT('Ctrl Pts',(2.01897889721417,-2.10827277611714,19.0408487832938));
#7798=CARTESIAN_POINT('Ctrl Pts',(2.00886963138116,-2.09653036547292,19.0418105698564));
#7799=CARTESIAN_POINT('Ctrl Pts',(2.00362453591578,-2.09039141581821,19.0423135075052));
#7800=CARTESIAN_POINT('Ctrl Pts',(1.99086799162813,-2.07534682412467,19.0435461928208));
#7801=CARTESIAN_POINT('Ctrl Pts',(1.98338169825066,-2.06642008300027,19.044277731418));
#7802=CARTESIAN_POINT('Ctrl Pts',(1.95655462912258,-2.03407659224649,19.0469280719851));
#7803=CARTESIAN_POINT('Ctrl Pts',(1.93749737641811,-2.01042812468135,19.0488655657819));
#7804=CARTESIAN_POINT('Ctrl Pts',(1.89063860099345,-1.95056796563532,19.0537615591165));
#7805=CARTESIAN_POINT('Ctrl Pts',(1.86326753713745,-1.91402893803081,19.0567426691068));
#7806=CARTESIAN_POINT('Ctrl Pts',(1.74511466782522,-1.74911260872656,19.070122807827));
#7807=CARTESIAN_POINT('Ctrl Pts',(1.66302589472062,-1.61477831263553,19.0808133521838));
#7808=CARTESIAN_POINT('Ctrl Pts',(1.49390897990924,-1.28624381846734,19.1057799670569));
#7809=CARTESIAN_POINT('Ctrl Pts',(1.41561998982431,-1.08832453837688,19.119913206994));
#7810=CARTESIAN_POINT('Ctrl Pts',(1.34705079505857,-0.84796711067773,19.1357780272142));
#7811=CARTESIAN_POINT('Ctrl Pts',(1.33737180656961,-0.811641966334892,19.1381437790465));
#7812=CARTESIAN_POINT('Ctrl Pts',(1.32342020451585,-0.755340225812226,19.1417627794148));
#7813=CARTESIAN_POINT('Ctrl Pts',(1.31869849407533,-0.73547936308691,19.1430303312957));
#7814=CARTESIAN_POINT('Ctrl Pts',(1.31099644737121,-0.701657358663538,19.145173862704));
#7815=CARTESIAN_POINT('Ctrl Pts',(1.30791962556671,-0.687719037720674,19.1460529120865));
#7816=CARTESIAN_POINT('Ctrl Pts',(1.30187626068711,-0.659451031255482,19.1478271367258));
#7817=CARTESIAN_POINT('Ctrl Pts',(1.29891450926542,-0.645120656984942,19.1487221402857));
#7818=CARTESIAN_POINT('Ctrl Pts',(1.2918428951659,-0.609688968004864,19.1509243581212));
#7819=CARTESIAN_POINT('Ctrl Pts',(1.28784632917964,-0.588565565301257,19.1522279450183));
#7820=CARTESIAN_POINT('Ctrl Pts',(1.27362923061179,-0.509076373733218,19.1571000174714));
#7821=CARTESIAN_POINT('Ctrl Pts',(1.264807218163,-0.450470290566245,19.1606243420331));
#7822=CARTESIAN_POINT('Ctrl Pts',(1.24658513511028,-0.301639059924374,19.1694312479794));
#7823=CARTESIAN_POINT('Ctrl Pts',(1.2393681539368,-0.211197664560141,19.1746500614103));
#7824=CARTESIAN_POINT('Ctrl Pts',(1.23076599840026,0.0185765508398514,19.1877145216239));
#7825=CARTESIAN_POINT('Ctrl Pts',(1.2345799297012,0.157914209373653,19.1954526268538));
#7826=CARTESIAN_POINT('Ctrl Pts',(1.26255608127138,0.460635451149534,19.2124828429316));
#7827=CARTESIAN_POINT('Ctrl Pts',(1.29027651959695,0.623279101294859,19.2217751700751));
#7828=CARTESIAN_POINT('Ctrl Pts',(1.33687171770365,0.809296453501305,19.233269792944));
#7829=CARTESIAN_POINT('Ctrl Pts',(1.34377101459511,0.835439463856024,19.2349058713996));
#7830=CARTESIAN_POINT('Ctrl Pts',(1.35376076551621,0.871450124478345,19.2371919910161));
#7831=CARTESIAN_POINT('Ctrl Pts',(1.35657121447973,0.881395155964502,19.2378267948465));
#7832=CARTESIAN_POINT('Ctrl Pts',(1.36147758098768,0.898443021810753,19.2389211808651));
#7833=CARTESIAN_POINT('Ctrl Pts',(1.36355025781861,0.905552538120719,19.23937943265));
#7834=CARTESIAN_POINT('Ctrl Pts',(1.36793771408795,0.92041121814292,19.2403411765516));
#7835=CARTESIAN_POINT('Ctrl Pts',(1.37025717397582,0.928158862933251,19.2408449503942));
#7836=CARTESIAN_POINT('Ctrl Pts',(1.37600827936483,0.947109252538608,19.2420826608993));
#7837=CARTESIAN_POINT('Ctrl Pts',(1.37947188506063,0.958302109489029,19.2428184217461));
#7838=CARTESIAN_POINT('Ctrl Pts',(1.39226582107709,0.998861987740441,19.2455011456527));
#7839=CARTESIAN_POINT('Ctrl Pts',(1.40195584896868,1.02811266019896,19.2474673890269));
#7840=CARTESIAN_POINT('Ctrl Pts',(1.42733448872995,1.10119392812346,19.2524516952861));
#7841=CARTESIAN_POINT('Ctrl Pts',(1.44355589047861,1.14483104180327,19.2554933570124));
#7842=CARTESIAN_POINT('Ctrl Pts',(1.58189040738712,1.49363700090604,19.2802570552746));
#7843=CARTESIAN_POINT('Ctrl Pts',(1.74909751177648,1.7788659225165,19.3030546684332));
#7844=CARTESIAN_POINT('Ctrl Pts',(2.00089291534823,2.08834568149386,19.328811022667));
#7845=CARTESIAN_POINT('Ctrl Pts',(2.0469498138578,2.14132204965114,19.3332751884546));
#7846=CARTESIAN_POINT('Ctrl Pts',(2.11080115673308,2.21009484705856,19.3391497368552));
#7847=CARTESIAN_POINT('Ctrl Pts',(2.12709024478052,2.22725650298233,19.3406226838635));
#7848=CARTESIAN_POINT('Ctrl Pts',(2.15407656800868,2.25506849510468,19.3430218012453));
#7849=CARTESIAN_POINT('Ctrl Pts',(2.16466201690661,2.26582558802671,19.3439527626723));
#7850=CARTESIAN_POINT('Ctrl Pts',(2.1853282032757,2.28653388050096,19.3457510509876));
#7851=CARTESIAN_POINT('Ctrl Pts',(2.19539973392539,2.29649373861153,19.3466187516621));
#7852=CARTESIAN_POINT('Ctrl Pts',(2.2191269330718,2.31965044247967,19.3486429673614));
#7853=CARTESIAN_POINT('Ctrl Pts',(2.23283432096202,2.33279372014201,19.3497971333116));
#7854=CARTESIAN_POINT('Ctrl Pts',(2.27797333916505,2.37531571030506,19.3535493649714));
#7855=CARTESIAN_POINT('Ctrl Pts',(2.30987799878461,2.4041870582627,19.3561258341601));
#7856=CARTESIAN_POINT('Ctrl Pts',(2.38686016802551,2.47109566320175,19.3621755648519));
#7857=CARTESIAN_POINT('Ctrl Pts',(2.43242300171203,2.5085519497695,19.3656260383219));
#7858=CARTESIAN_POINT('Ctrl Pts',(2.70253068673412,2.71844868103846,19.3854192919508));
#7859=CARTESIAN_POINT('Ctrl Pts',(2.94796248030909,2.86193205947185,19.4007085830358));
#7860=CARTESIAN_POINT('Ctrl Pts',(3.2309808820318,2.98074927247887,19.4183296450099));
#7861=CARTESIAN_POINT('Ctrl Pts',(3.25309689062051,2.98974629025681,19.4197073812968));
#7862=CARTESIAN_POINT('Ctrl Pts',(3.33936965777885,3.02373059828085,19.4250920785058));
#7863=CARTESIAN_POINT('Ctrl Pts',(3.40421618554404,3.04690338070842,19.4291612278102));
#7864=CARTESIAN_POINT('Ctrl Pts',(3.48500511511073,3.07288660394029,19.4343143775769));
#7865=CARTESIAN_POINT('Ctrl Pts',(3.50029665751029,3.07767909158117,19.4352933961573));
#7866=CARTESIAN_POINT('Ctrl Pts',(3.52434583995685,3.0850197660745,19.4368397395733));
#7867=CARTESIAN_POINT('Ctrl Pts',(3.53307987509124,3.08764522955952,19.43740269666));
#7868=CARTESIAN_POINT('Ctrl Pts',(3.54927811117731,3.09243956759608,19.4384494910594));
#7869=CARTESIAN_POINT('Ctrl Pts',(3.55673912169654,3.09461854373629,19.4389327372406));
#7870=CARTESIAN_POINT('Ctrl Pts',(3.57394291717288,3.09957541059197,19.4400494818632));
#7871=CARTESIAN_POINT('Ctrl Pts',(3.5836909375287,3.10233435690301,19.4406840495841));
#7872=CARTESIAN_POINT('Ctrl Pts',(3.61408931549002,3.11078328819564,19.4426681333856));
#7873=CARTESIAN_POINT('Ctrl Pts',(3.63478302094563,3.11631325415694,19.4440263065033));
#7874=CARTESIAN_POINT('Ctrl Pts',(3.68345540603113,3.12880145871449,19.447235876117));
#7875=CARTESIAN_POINT('Ctrl Pts',(3.71147504787871,3.13559124898457,19.4490951792185));
#7876=CARTESIAN_POINT('Ctrl Pts',(3.8117468809298,3.1584695423951,19.4557813877245));
#7877=CARTESIAN_POINT('Ctrl Pts',(3.88445432883449,3.17244295745975,19.4606889497949));
#7878=CARTESIAN_POINT('Ctrl Pts',(4.2062636485862,3.22286831318564,19.4825006955638));
#7879=CARTESIAN_POINT('Ctrl Pts',(4.45870276160217,3.23256933229992,19.4997585902873));
#7880=CARTESIAN_POINT('Ctrl Pts',(4.80751678769213,3.20507570916502,19.5226416266125));
#7881=CARTESIAN_POINT('Ctrl Pts',(4.90493597665786,3.19290236554748,19.5289392361525));
#7882=CARTESIAN_POINT('Ctrl Pts',(5.02788771375879,3.17179865046942,19.5367693448369));
#7883=CARTESIAN_POINT('Ctrl Pts',(5.0540626374201,3.1669714150774,19.53842956906));
#7884=CARTESIAN_POINT('Ctrl Pts',(5.09561494365793,3.15877473337479,19.5410550758631));
#7885=CARTESIAN_POINT('Ctrl Pts',(5.11103218066666,3.15561601170437,19.5420270074152));
#7886=CARTESIAN_POINT('Ctrl Pts',(5.13873880317185,3.14972761978986,19.5437698850695));
#7887=CARTESIAN_POINT('Ctrl Pts',(5.15103642098971,3.14703865095611,19.5445421110312));
#7888=CARTESIAN_POINT('Ctrl Pts',(5.17988700871665,3.14055289769689,19.5463507464063));
#7889=CARTESIAN_POINT('Ctrl Pts',(5.19642644978054,3.1366971660958,19.5473852475298));
#7890=CARTESIAN_POINT('Ctrl Pts',(5.24449311352943,3.12509035378476,19.5503853628957));
#7891=CARTESIAN_POINT('Ctrl Pts',(5.27593520739811,3.11699325954761,19.552339856268));
#7892=CARTESIAN_POINT('Ctrl Pts',(5.51334540361283,3.05201361495254,19.5670484419043));
#7893=CARTESIAN_POINT('Ctrl Pts',(5.71332795076684,2.97524724648285,19.5791074001547));
#7894=CARTESIAN_POINT('Ctrl Pts',(6.10364171832906,2.77898258731845,19.6035518423707));
#7895=CARTESIAN_POINT('Ctrl Pts',(6.29204193627464,2.6583013428099,19.6158758171254));
#7896=CARTESIAN_POINT('Ctrl Pts',(6.48575271537412,2.5037444153385,19.6307654613275));
#7897=CARTESIAN_POINT('Ctrl Pts',(6.50488815946412,2.48811321326056,19.6322631243497));
#7898=CARTESIAN_POINT('Ctrl Pts',(6.5314812282206,2.46587539012949,19.6343854701012));
#7899=CARTESIAN_POINT('Ctrl Pts',(6.53909136526391,2.45945141569425,19.6349976155408));
#7900=CARTESIAN_POINT('Ctrl Pts',(6.55223512660553,2.4482515760214,19.6360634662144));
#7901=CARTESIAN_POINT('Ctrl Pts',(6.55778255483201,2.44349192342877,19.6365159964752));
#7902=CARTESIAN_POINT('Ctrl Pts',(6.5688662864211,2.43391650599394,19.63742564692));
#7903=CARTESIAN_POINT('Ctrl Pts',(6.57440241677802,2.4291006348124,19.6378827771027));
#7904=CARTESIAN_POINT('Ctrl Pts',(6.58810309283819,2.41709999615866,19.6390208744963));
#7905=CARTESIAN_POINT('Ctrl Pts',(6.59624774730844,2.40989277842168,19.6397034794654));
#7906=CARTESIAN_POINT('Ctrl Pts',(6.62430453059871,2.38481092206498,19.6420754299712));
#7907=CARTESIAN_POINT('Ctrl Pts',(6.64402981069565,2.36673015301993,19.6437790587012));
#7908=CARTESIAN_POINT('Ctrl Pts',(6.69205800368811,2.32159273968159,19.6480118762703));
#7909=CARTESIAN_POINT('Ctrl Pts',(6.72009682115932,2.29426237771427,19.6505574892609));
#7910=CARTESIAN_POINT('Ctrl Pts',(6.83198874344166,2.18114950111979,19.6609992481329));
#7911=CARTESIAN_POINT('Ctrl Pts',(6.91151600031204,2.09123121786874,19.6690834558953));
#7912=CARTESIAN_POINT('Ctrl Pts',(7.15005330590126,1.78911772960194,19.6951138797229));
#7913=CARTESIAN_POINT('Ctrl Pts',(7.28802045389854,1.56163615300294,19.7129654140903));
#7914=CARTESIAN_POINT('Ctrl Pts',(7.41249373904646,1.28434640594354,19.7322207066652));
#7915=CARTESIAN_POINT('Ctrl Pts',(7.4277642035746,1.24861242055775,19.7346606520895));
#7916=CARTESIAN_POINT('Ctrl Pts',(7.44917336138777,1.19589475783665,19.7382014265732));
#7917=CARTESIAN_POINT('Ctrl Pts',(7.45582110338722,1.17912283033489,19.7393193256318));
#7918=CARTESIAN_POINT('Ctrl Pts',(7.4674016762598,1.14917385464136,19.7413005508085));
#7919=CARTESIAN_POINT('Ctrl Pts',(7.47238966869084,1.13601877640831,19.7421657083397));
#7920=CARTESIAN_POINT('Ctrl Pts',(7.48264437499337,1.10842990715336,19.7439696643334));
#7921=CARTESIAN_POINT('Ctrl Pts',(7.48789434626524,1.09399023909491,19.7449078868439));
#7922=CARTESIAN_POINT('Ctrl Pts',(7.50138495162219,1.05604240740201,19.747358350578));
#7923=CARTESIAN_POINT('Ctrl Pts',(7.50945674196058,1.03247499774353,19.7488649860863));
#7924=CARTESIAN_POINT('Ctrl Pts',(7.54547170056723,0.923204248036363,19.7557834829227));
#7925=CARTESIAN_POINT('Ctrl Pts',(7.5700860779861,0.836441642686329,19.7610859848423));
#7926=CARTESIAN_POINT('Ctrl Pts',(7.64962599100909,0.503458342021578,19.7808852707807));
#7927=CARTESIAN_POINT('Ctrl Pts',(7.67921910621825,0.252160529432019,19.7946332277895));
#7928=CARTESIAN_POINT('Ctrl Pts',(7.67921910621823,5.28268401245313E-12,
19.808946496524));
#7929=CARTESIAN_POINT('Ctrl Pts',(7.67921910621823,-6.1812332959659E-13,
19.5612501365773));
#7930=CARTESIAN_POINT('Ctrl Pts',(7.67921910621824,0.0284028134448205,19.5594599908969));
#7931=CARTESIAN_POINT('Ctrl Pts',(7.67884362626994,0.0568051021141802,19.5576814802244));
#7932=CARTESIAN_POINT('Ctrl Pts',(7.67761897452903,0.103112508301193,19.5548000166224));
#7933=CARTESIAN_POINT('Ctrl Pts',(7.67699584377862,0.121021555604613,19.5536900801427));
#7934=CARTESIAN_POINT('Ctrl Pts',(7.67561927970105,0.152925139774606,19.5517204798415));
#7935=CARTESIAN_POINT('Ctrl Pts',(7.67492387973481,0.166921593822558,19.5508590253468));
#7936=CARTESIAN_POINT('Ctrl Pts',(7.67326251877794,0.196470055880185,19.5490457541829));
#7937=CARTESIAN_POINT('Ctrl Pts',(7.67227501624166,0.212020528141493,19.5480946339856));
#7938=CARTESIAN_POINT('Ctrl Pts',(7.66934537366983,0.253406518687992,19.5455713599666));
#7939=CARTESIAN_POINT('Ctrl Pts',(7.66720438560732,0.279227145878171,19.5440054488619));
#7940=CARTESIAN_POINT('Ctrl Pts',(7.65507507029223,0.406806685643112,19.5363060465622));
#7941=CARTESIAN_POINT('Ctrl Pts',(7.64055891975178,0.508081580129581,19.5303156947538));
#7942=CARTESIAN_POINT('Ctrl Pts',(7.57968009677215,0.824708082173789,19.5117654486567));
#7943=CARTESIAN_POINT('Ctrl Pts',(7.51606598448357,1.03607783163774,19.4996820645383));
#7944=CARTESIAN_POINT('Ctrl Pts',(7.37915361851138,1.36473161287488,19.4795795335781));
#7945=CARTESIAN_POINT('Ctrl Pts',(7.31903328111939,1.48670593372855,19.4717828342671));
#7946=CARTESIAN_POINT('Ctrl Pts',(7.24300181497109,1.61914730139673,19.4625396856323));
#7947=CARTESIAN_POINT('Ctrl Pts',(7.23448274576251,1.63372051199936,19.4615115163708));
#7948=CARTESIAN_POINT('Ctrl Pts',(7.22067260852757,1.65692457062143,19.4598554855769));
#7949=CARTESIAN_POINT('Ctrl Pts',(7.21545455007141,1.66559879594775,19.4592321446015));
#7950=CARTESIAN_POINT('Ctrl Pts',(7.20611294479588,1.68096344046085,19.4581201369868));
#7951=CARTESIAN_POINT('Ctrl Pts',(7.20200567928381,1.68766354811799,19.4576325282135));
#7952=CARTESIAN_POINT('Ctrl Pts',(7.19312142660486,1.70203799921369,19.4565805265562));
#7953=CARTESIAN_POINT('Ctrl Pts',(7.18833672829888,1.70970715743046,19.4560156515672));
#7954=CARTESIAN_POINT('Ctrl Pts',(7.17494340626888,1.73097489109188,19.454439346266));
#7955=CARTESIAN_POINT('Ctrl Pts',(7.1662652205259,1.74452904461202,19.4534235223688));
#7956=CARTESIAN_POINT('Ctrl Pts',(7.11464894778162,1.82383226277776,19.4474164184023));
#7957=CARTESIAN_POINT('Ctrl Pts',(7.06942417959728,1.88805397283022,19.4422930748145));
#7958=CARTESIAN_POINT('Ctrl Pts',(6.89503696942675,2.1174139224218,19.4232028274105));
#7959=CARTESIAN_POINT('Ctrl Pts',(6.75219512034282,2.27149716107704,19.4088336427382));
#7960=CARTESIAN_POINT('Ctrl Pts',(6.47067612865167,2.52128759044676,19.3836595480727));
#7961=CARTESIAN_POINT('Ctrl Pts',(6.33753648553057,2.622121576431,19.3727560120323));
#7962=CARTESIAN_POINT('Ctrl Pts',(6.17425368615352,2.72691678961993,19.3605416897803));
#7963=CARTESIAN_POINT('Ctrl Pts',(6.15115129476806,2.7413338712202,19.3588381531205));
#7964=CARTESIAN_POINT('Ctrl Pts',(6.11294209067534,2.76451073104742,19.3560601364328));
#7965=CARTESIAN_POINT('Ctrl Pts',(6.09794226200795,2.77344338834173,19.3549793730167));
#7966=CARTESIAN_POINT('Ctrl Pts',(6.07081270686615,2.7893023086204,19.3530419576122));
#7967=CARTESIAN_POINT('Ctrl Pts',(6.05870922482919,2.79627238334953,19.3521837328245));
#7968=CARTESIAN_POINT('Ctrl Pts',(6.03276225934852,2.81099077154585,19.3503567607638));
#7969=CARTESIAN_POINT('Ctrl Pts',(6.01890606480431,2.81871601741629,19.3493888583142));
#7970=CARTESIAN_POINT('Ctrl Pts',(5.98113818119996,2.8394086812677,19.3467711719543));
#7971=CARTESIAN_POINT('Ctrl Pts',(5.95711812001484,2.85217637141784,19.3451284965258));
#7972=CARTESIAN_POINT('Ctrl Pts',(5.82515080698649,2.92019392826158,19.3362189774638));
#7973=CARTESIAN_POINT('Ctrl Pts',(5.71430642120297,2.96962493182002,19.3291581123835));
#7974=CARTESIAN_POINT('Ctrl Pts',(5.44905878241921,3.07038700212826,19.3129521507839));
#7975=CARTESIAN_POINT('Ctrl Pts',(5.29304319525379,3.11651347471885,19.3039428106329));
#7976=CARTESIAN_POINT('Ctrl Pts',(5.0517760840782,3.16841240823839,19.2901080260325));
#7977=CARTESIAN_POINT('Ctrl Pts',(4.96867978540304,3.18290223988415,19.285357048519));
#7978=CARTESIAN_POINT('Ctrl Pts',(4.7961623552028,3.20605381663788,19.2753609849281));
#7979=CARTESIAN_POINT('Ctrl Pts',(4.7067583357602,3.21426894372378,19.2701081000082));
#7980=CARTESIAN_POINT('Ctrl Pts',(4.6014022833881,3.21952793714187,19.2637133667542));
#7981=CARTESIAN_POINT('Ctrl Pts',(4.58566227810978,3.22019795439139,19.2627526420184));
#7982=CARTESIAN_POINT('Ctrl Pts',(4.56002857035624,3.22110088775643,19.2611783906873));
#7983=CARTESIAN_POINT('Ctrl Pts',(4.55013738545256,3.22140369080439,19.2605686035396));
#7984=CARTESIAN_POINT('Ctrl Pts',(4.53242193643426,3.22186436300611,19.2594720208778));
#7985=CARTESIAN_POINT('Ctrl Pts',(4.52459831095192,3.22203929448222,19.2589861795267));
#7986=CARTESIAN_POINT('Ctrl Pts',(4.50745303428729,3.22236017733644,19.2579180030989));
#7987=CARTESIAN_POINT('Ctrl Pts',(4.49813148891168,3.22249417596578,19.2573350356344));
#7988=CARTESIAN_POINT('Ctrl Pts',(4.47139727390988,3.22276246922788,19.2556569673354));
#7989=CARTESIAN_POINT('Ctrl Pts',(4.45398423262307,3.22279608061584,19.2545565357168));
#7990=CARTESIAN_POINT('Ctrl Pts',(4.32762242154845,3.22201592298449,19.2465211332876));
#7991=CARTESIAN_POINT('Ctrl Pts',(4.21878769952972,3.21581881108584,19.239333251583));
#7992=CARTESIAN_POINT('Ctrl Pts',(3.88297921849647,3.17955827093561,19.2167184685112));
#7993=CARTESIAN_POINT('Ctrl Pts',(3.6587069476032,3.13082621787041,19.2010442730002));
#7994=CARTESIAN_POINT('Ctrl Pts',(3.32892572613319,3.02139517416331,19.1781380637038));
#7995=CARTESIAN_POINT('Ctrl Pts',(3.21850152632271,2.97785574094803,19.1704813730009));
#7996=CARTESIAN_POINT('Ctrl Pts',(3.08548787489987,2.91672744617726,19.1612816023624));
#7997=CARTESIAN_POINT('Ctrl Pts',(3.06040853826933,2.90480696434155,19.15954779632));
#7998=CARTESIAN_POINT('Ctrl Pts',(3.02099160519675,2.88544323898276,19.1568233537176));
#7999=CARTESIAN_POINT('Ctrl Pts',(3.00655098183327,2.87821399292753,19.1558253557429));
#8000=CARTESIAN_POINT('Ctrl Pts',(2.97974789858912,2.86454295425033,19.153972988634));
#8001=CARTESIAN_POINT('Ctrl Pts',(2.96737177343201,2.85812893427789,19.1531176739155));
#8002=CARTESIAN_POINT('Ctrl Pts',(2.93993540028403,2.84368324200678,19.1512213564351));
#8003=CARTESIAN_POINT('Ctrl Pts',(2.92489648808655,2.83561178494986,19.1501817867059));
#8004=CARTESIAN_POINT('Ctrl Pts',(2.8810704172853,2.81163973676643,19.1471513865489));
#8005=CARTESIAN_POINT('Ctrl Pts',(2.85246114196138,2.7954172513468,19.1451720324541));
#8006=CARTESIAN_POINT('Ctrl Pts',(2.78809754152416,2.75760725675333,19.1407127803965));
#8007=CARTESIAN_POINT('Ctrl Pts',(2.75250415606485,2.7357567754428,19.1382423714925));
#8008=CARTESIAN_POINT('Ctrl Pts',(2.63552980961425,2.66077834018514,19.1300951050013));
#8009=CARTESIAN_POINT('Ctrl Pts',(2.55612543648521,2.60466068879597,19.1245193731635));
#8010=CARTESIAN_POINT('Ctrl Pts',(2.37396676754032,2.46315191822,19.1114506277655));
#8011=CARTESIAN_POINT('Ctrl Pts',(2.27374693985957,2.37479641840688,19.1040346741214));
#8012=CARTESIAN_POINT('Ctrl Pts',(2.12224360462592,2.22351279194915,19.0920343033402));
#8013=CARTESIAN_POINT('Ctrl Pts',(2.06735221619393,2.16442541186132,19.0874942082041));
#8014=CARTESIAN_POINT('Ctrl Pts',(1.95307594700382,2.03176425318163,19.0774610189337));
#8015=CARTESIAN_POINT('Ctrl Pts',(1.89459891611928,1.95751396894585,19.071943188041));
#8016=CARTESIAN_POINT('Ctrl Pts',(1.83016477499899,1.86785907174852,19.0652520520684));
#8017=CARTESIAN_POINT('Ctrl Pts',(1.82095301426016,1.85483876861369,19.0642796320921));
#8018=CARTESIAN_POINT('Ctrl Pts',(1.80614955796381,1.83358199981329,19.0626900151264));
#8019=CARTESIAN_POINT('Ctrl Pts',(1.8004985903824,1.82538688248569,19.0620766794753));
#8020=CARTESIAN_POINT('Ctrl Pts',(1.79047113697588,1.81069977894365,19.0609763453953));
#8021=CARTESIAN_POINT('Ctrl Pts',(1.78608023266023,1.80421787023806,19.0604903299256));
#8022=CARTESIAN_POINT('Ctrl Pts',(1.77653848302074,1.79002107927728,19.0594249220416));
#8023=CARTESIAN_POINT('Ctrl Pts',(1.77139738636968,1.78230004870439,19.0588449215007));
#8024=CARTESIAN_POINT('Ctrl Pts',(1.75682193545894,1.7602040687787,19.0571837057389));
#8025=CARTESIAN_POINT('Ctrl Pts',(1.74746935884358,1.74577591596484,19.0560973206201));
#8026=CARTESIAN_POINT('Ctrl Pts',(1.68307586287662,1.64467306830056,19.0484770270223));
#8027=CARTESIAN_POINT('Ctrl Pts',(1.63209426850302,1.55549414585811,19.0417181555772));
#8028=CARTESIAN_POINT('Ctrl Pts',(1.51923625788486,1.33417828896631,19.0251146507008));
#8029=CARTESIAN_POINT('Ctrl Pts',(1.46190063927246,1.19996987354799,19.0151905873257));
#8030=CARTESIAN_POINT('Ctrl Pts',(1.34652797073386,0.869534611765488,18.9916125838002));
#8031=CARTESIAN_POINT('Ctrl Pts',(1.29767767003671,0.670736596291064,18.9781351894585));
#8032=CARTESIAN_POINT('Ctrl Pts',(1.26399286815807,0.441544956596039,18.9635498492786));
#8033=CARTESIAN_POINT('Ctrl Pts',(1.26035846307727,0.414419244593152,18.9618376356025));
#8034=CARTESIAN_POINT('Ctrl Pts',(1.25496723760914,0.369877761204898,18.9590484201937));
#8035=CARTESIAN_POINT('Ctrl Pts',(1.25300604329656,0.35248857680413,18.9579650488734));
#8036=CARTESIAN_POINT('Ctrl Pts',(1.24973399716544,0.321189462773992,18.9560247902201));
#8037=CARTESIAN_POINT('Ctrl Pts',(1.24837179016518,0.307285455418795,18.9551663106272));
#8038=CARTESIAN_POINT('Ctrl Pts',(1.24565840944089,0.277602272062222,18.9533407302291));
#8039=CARTESIAN_POINT('Ctrl Pts',(1.24433304174656,0.261821063545848,18.952374460107));
#8040=CARTESIAN_POINT('Ctrl Pts',(1.24105709782643,0.219034749994791,18.9497659731991));
#8041=CARTESIAN_POINT('Ctrl Pts',(1.2393303900664,0.192013422287832,18.9481307784456));
#8042=CARTESIAN_POINT('Ctrl Pts',(1.23184263457491,0.0459316960763701,18.9393518022687));
#8043=CARTESIAN_POINT('Ctrl Pts',(1.2323493970452,-0.0733639267330349,18.9324065843272));
#8044=CARTESIAN_POINT('Ctrl Pts',(1.24881839190477,-0.34877783578518,18.9166364767785));
#8045=CARTESIAN_POINT('Ctrl Pts',(1.26956607212594,-0.504301731685991,18.9079330095582));
#8046=CARTESIAN_POINT('Ctrl Pts',(1.33561694647016,-0.821141560418656,18.8898066780825));
#8047=CARTESIAN_POINT('Ctrl Pts',(1.38233454330533,-0.981669399701871,18.8803982146996));
#8048=CARTESIAN_POINT('Ctrl Pts',(1.45078014272268,-1.16304667717598,18.868776835227));
#8049=CARTESIAN_POINT('Ctrl Pts',(1.4606097308252,-1.18813728742322,18.8671461459863));
#8050=CARTESIAN_POINT('Ctrl Pts',(1.47463770315148,-1.22266331602778,18.8648663045421));
#8051=CARTESIAN_POINT('Ctrl Pts',(1.47856884446939,-1.23220701386692,18.8642322788332));
#8052=CARTESIAN_POINT('Ctrl Pts',(1.48539756755589,-1.24856167606506,18.8631389112664));
#8053=CARTESIAN_POINT('Ctrl Pts',(1.48827292118004,-1.25538191452222,18.8626808946013));
#8054=CARTESIAN_POINT('Ctrl Pts',(1.49433993559444,-1.26963529319562,18.8617192633322));
#8055=CARTESIAN_POINT('Ctrl Pts',(1.4975361092922,-1.27706637094985,18.8612153647438));
#8056=CARTESIAN_POINT('Ctrl Pts',(1.5054351826832,-1.29524280598295,18.8599767125325));
#8057=CARTESIAN_POINT('Ctrl Pts',(1.51016880833146,-1.3059746126881,18.8592401279763));
#8058=CARTESIAN_POINT('Ctrl Pts',(1.52758759172565,-1.34488876800186,18.856550722299));
#8059=CARTESIAN_POINT('Ctrl Pts',(1.54061894688311,-1.37291311039747,18.8545784968055));
#8060=CARTESIAN_POINT('Ctrl Pts',(1.57436636151043,-1.44283958007649,18.8495756689546));
#8061=CARTESIAN_POINT('Ctrl Pts',(1.59559438249457,-1.48448565403595,18.8465212560641));
#8062=CARTESIAN_POINT('Ctrl Pts',(1.77556520152065,-1.81935345055736,18.8214289343213));
#8063=CARTESIAN_POINT('Ctrl Pts',(1.9780413249982,-2.08680739637278,18.798298446561));
#8064=CARTESIAN_POINT('Ctrl Pts',(2.26563234168041,-2.36447377002062,18.7725442661621));
#8065=CARTESIAN_POINT('Ctrl Pts',(2.31467651749506,-2.40898889116164,18.7683378607335));
#8066=CARTESIAN_POINT('Ctrl Pts',(2.38266895772846,-2.46698320627207,18.7627463906983));
#8067=CARTESIAN_POINT('Ctrl Pts',(2.40043904753291,-2.48181257119949,18.7613061350128));
#8068=CARTESIAN_POINT('Ctrl Pts',(2.42997088242678,-2.50592236094837,18.7589465747357));
#8069=CARTESIAN_POINT('Ctrl Pts',(2.44164009658245,-2.51531429530023,18.758022779417));
#8070=CARTESIAN_POINT('Ctrl Pts',(2.46450903369547,-2.5334590297333,18.7562287613204));
#8071=CARTESIAN_POINT('Ctrl Pts',(2.47570200084537,-2.54221975256697,18.7553582343435));
#8072=CARTESIAN_POINT('Ctrl Pts',(2.50222665807577,-2.56269904202215,18.7533127457653));
#8073=CARTESIAN_POINT('Ctrl Pts',(2.51760647078688,-2.57435460496161,18.7521402836861));
#8074=CARTESIAN_POINT('Ctrl Pts',(2.56904525256626,-2.6126149211951,18.7482627808874));
#8075=CARTESIAN_POINT('Ctrl Pts',(2.6055552952843,-2.63860642957818,18.7455814365296));
#8076=CARTESIAN_POINT('Ctrl Pts',(2.69400860160376,-2.69883664266446,18.7392414632741));
#8077=CARTESIAN_POINT('Ctrl Pts',(2.74642497978504,-2.73234990690381,18.7356088055959));
#8078=CARTESIAN_POINT('Ctrl Pts',(3.0837497800168,-2.93451198513313,18.7129035866159));
#8079=CARTESIAN_POINT('Ctrl Pts',(3.39219217606696,-3.05989792512018,18.6953187470104));
#8080=CARTESIAN_POINT('Ctrl Pts',(3.75671554730795,-3.1461667447413,18.6731889307832));
#8081=CARTESIAN_POINT('Ctrl Pts',(3.79935984609438,-3.15534898672469,18.6705768903142));
#8082=CARTESIAN_POINT('Ctrl Pts',(3.85577291121581,-3.16630281564717,18.6670754944602));
#8083=CARTESIAN_POINT('Ctrl Pts',(3.86938749318509,-3.16885540893573,18.6662269686365));
#8084=CARTESIAN_POINT('Ctrl Pts',(3.89142656585196,-3.17284060566614,18.6648471053794));
#8085=CARTESIAN_POINT('Ctrl Pts',(3.89984120809032,-3.17432763911187,18.6643187886612));
#8086=CARTESIAN_POINT('Ctrl Pts',(3.91616047543904,-3.17714469268053,18.6632911423174));
#8087=CARTESIAN_POINT('Ctrl Pts',(3.9240642674348,-3.17847870795283,18.6627920390091));
#8088=CARTESIAN_POINT('Ctrl Pts',(3.94316171485472,-3.18162877818692,18.6615828478592));
#8089=CARTESIAN_POINT('Ctrl Pts',(3.95436008541971,-3.18341525446944,18.660871123889));
#8090=CARTESIAN_POINT('Ctrl Pts',(3.99360126614107,-3.18946319742835,18.6583682968408));
#8091=CARTESIAN_POINT('Ctrl Pts',(4.02168980010099,-3.19341337003237,18.6565610616655));
#8092=CARTESIAN_POINT('Ctrl Pts',(4.09114501240988,-3.20224776979922,18.6520595007502));
#8093=CARTESIAN_POINT('Ctrl Pts',(4.13256046724244,-3.20670162922516,18.649346712081));
#8094=CARTESIAN_POINT('Ctrl Pts',(4.30685694327721,-3.22203481229416,18.6378410092712));
#8095=CARTESIAN_POINT('Ctrl Pts',(4.44025521368895,-3.22546514583296,18.6288241015408));
#8096=CARTESIAN_POINT('Ctrl Pts',(4.67216988319575,-3.2170396986303,18.6131238551325));
#8097=CARTESIAN_POINT('Ctrl Pts',(4.77065164042923,-3.20891910176094,18.6064479200548));
#8098=CARTESIAN_POINT('Ctrl Pts',(5.02973886243387,-3.17551166064296,18.5889929843748));
#8099=CARTESIAN_POINT('Ctrl Pts',(5.18908686061228,-3.14257819092676,18.578380896443));
#8100=CARTESIAN_POINT('Ctrl Pts',(5.37135960031064,-3.09027966229791,18.5664442057519));
#8101=CARTESIAN_POINT('Ctrl Pts',(5.39733207173869,-3.08247140452727,18.5647477379578));
#8102=CARTESIAN_POINT('Ctrl Pts',(5.43982506973266,-3.06910935044628,18.5619788477785));
#8103=CARTESIAN_POINT('Ctrl Pts',(5.456404191201,-3.06374786836112,18.5609002118603));
#8104=CARTESIAN_POINT('Ctrl Pts',(5.48619032871492,-3.05384786034121,18.5589651105043));
#8105=CARTESIAN_POINT('Ctrl Pts',(5.49941277458038,-3.04935748388561,18.5581070881436));
#8106=CARTESIAN_POINT('Ctrl Pts',(5.52761502782939,-3.03957502938459,18.5562789541222));
#8107=CARTESIAN_POINT('Ctrl Pts',(5.54258577479633,-3.03425782375398,18.5553096989619));
#8108=CARTESIAN_POINT('Ctrl Pts',(5.58184263461627,-3.01998707422332,18.5527708216865));
#8109=CARTESIAN_POINT('Ctrl Pts',(5.60606156715453,-3.01085116536941,18.5512072804521));
#8110=CARTESIAN_POINT('Ctrl Pts',(5.72081351659151,-2.96597771025322,18.5438088551703));
#8111=CARTESIAN_POINT('Ctrl Pts',(5.80981170062668,-2.92644101777471,18.53810221279));
#8112=CARTESIAN_POINT('Ctrl Pts',(6.08107114380992,-2.79090964207324,18.5206326629969));
#8113=CARTESIAN_POINT('Ctrl Pts',(6.25600715633322,-2.68144991614729,18.5092828111469));
#8114=CARTESIAN_POINT('Ctrl Pts',(6.54122512580693,-2.46242533557525,18.489062015714));
#8115=CARTESIAN_POINT('Ctrl Pts',(6.65627179950778,-2.36021229459978,18.4803049468223));
#8116=CARTESIAN_POINT('Ctrl Pts',(6.77654386822955,-2.23689870377663,18.469880098456));
#8117=CARTESIAN_POINT('Ctrl Pts',(6.78940000652789,-2.2234873711176,18.4687479413034));
#8118=CARTESIAN_POINT('Ctrl Pts',(6.80878187051918,-2.20291535449392,18.4670123469773));
#8119=CARTESIAN_POINT('Ctrl Pts',(6.81539269116201,-2.19583490154854,18.4664151787582));
#8120=CARTESIAN_POINT('Ctrl Pts',(6.82728087634721,-2.18298653960332,18.4653316422684));
#8121=CARTESIAN_POINT('Ctrl Pts',(6.83256928120214,-2.17722911910111,18.464846125054));
#8122=CARTESIAN_POINT('Ctrl Pts',(6.84424036793362,-2.1644297836629,18.4637667897289));
#8123=CARTESIAN_POINT('Ctrl Pts',(6.85061279840961,-2.15737893342536,18.4631722456997));
#8124=CARTESIAN_POINT('Ctrl Pts',(6.868571778697,-2.13733044898643,18.4614820778406));
#8125=CARTESIAN_POINT('Ctrl Pts',(6.88008410594439,-2.12426718011805,18.4603812254201));
#8126=CARTESIAN_POINT('Ctrl Pts',(6.96367984521711,-2.02784530129074,18.4522629875831));
#8127=CARTESIAN_POINT('Ctrl Pts',(7.0315442423832,-1.94093925228313,18.4449877250534));
#8128=CARTESIAN_POINT('Ctrl Pts',(7.19396226978649,-1.7094018381902,18.4260422844694));
#8129=CARTESIAN_POINT('Ctrl Pts',(7.2815902684104,-1.5603257326243,18.414261610783));
#8130=CARTESIAN_POINT('Ctrl Pts',(7.43054058563359,-1.25283052626814,18.3913955725114));
#8131=CARTESIAN_POINT('Ctrl Pts',(7.49215259885276,-1.09513780678663,18.3803367662456));
#8132=CARTESIAN_POINT('Ctrl Pts',(7.54901462110506,-0.907206656555523,18.3679754710214));
#8133=CARTESIAN_POINT('Ctrl Pts',(7.5565829108954,-0.880997247951465,18.3662688514602));
#8134=CARTESIAN_POINT('Ctrl Pts',(7.56845146465908,-0.837847625456554,18.3634868554092));
#8135=CARTESIAN_POINT('Ctrl Pts',(7.57294821698209,-0.820963345194926,18.362405164962));
#8136=CARTESIAN_POINT('Ctrl Pts',(7.58079235911721,-0.790516841477836,18.3604667397016));
#8137=CARTESIAN_POINT('Ctrl Pts',(7.58418928022844,-0.776967945348729,18.3596084251712));
#8138=CARTESIAN_POINT('Ctrl Pts',(7.59125350125708,-0.747994456986186,18.3577819518879));
#8139=CARTESIAN_POINT('Ctrl Pts',(7.59489529453537,-0.732563980546522,18.3568146329101));
#8140=CARTESIAN_POINT('Ctrl Pts',(7.60209524151769,-0.701017919631405,18.354847777982));
#8141=CARTESIAN_POINT('Ctrl Pts',(7.60564377269254,-0.684900607586468,18.3538485726264));
#8142=CARTESIAN_POINT('Ctrl Pts',(7.61424658985375,-0.644345884572817,18.3513481536081));
#8143=CARTESIAN_POINT('Ctrl Pts',(7.61914119440518,-0.619875446692365,18.3498519651881));
#8144=CARTESIAN_POINT('Ctrl Pts',(7.66064905192815,-0.399052284398737,18.3364563363126));
#8145=CARTESIAN_POINT('Ctrl Pts',(7.67921910620918,-0.199750373277688,18.3251566808499));
#8146=CARTESIAN_POINT('Ctrl Pts',(7.67921910621823,-1.45987597011121E-10,
18.3139723139554));
#8147=CARTESIAN_POINT('Origin',(4.45646910621825,-5.13094777615093E-16,
-2.31077344927308));
#8148=CARTESIAN_POINT('',(7.67921904541622,-0.000626018863251772,17.0671267778236));
#8149=CARTESIAN_POINT('',(7.67921910621823,1.77253683985415E-10,17.3115866477388));
#8150=CARTESIAN_POINT('',(7.67921910621823,-3.51191647465084E-13,-2.31077344927308));
#8151=CARTESIAN_POINT('Ctrl Pts',(7.67921910621823,1.77258589750817E-10,
17.3115866477388));
#8152=CARTESIAN_POINT('Ctrl Pts',(7.67921910622848,-0.186420830783714,17.3241302593115));
#8153=CARTESIAN_POINT('Ctrl Pts',(7.66304408358115,-0.372522916221347,17.336428873084));
#8154=CARTESIAN_POINT('Ctrl Pts',(7.62644079621295,-0.581422353333308,17.3498435584536));
#8155=CARTESIAN_POINT('Ctrl Pts',(7.62172382977166,-0.606576511156904,17.351452896662));
#8156=CARTESIAN_POINT('Ctrl Pts',(7.61342130711023,-0.648113788347165,17.3541009479764));
#8157=CARTESIAN_POINT('Ctrl Pts',(7.61000667899512,-0.66452951440673,17.3551450134735));
#8158=CARTESIAN_POINT('Ctrl Pts',(7.6030750777652,-0.696595792055698,17.3571798672976));
#8159=CARTESIAN_POINT('Ctrl Pts',(7.5995690681753,-0.712248188271752,17.3581709731876));
#8160=CARTESIAN_POINT('Ctrl Pts',(7.59279576613295,-0.741462898034154,17.3600170071803));
#8161=CARTESIAN_POINT('Ctrl Pts',(7.58955700422825,-0.75503137674913,17.3608728258405));
#8162=CARTESIAN_POINT('Ctrl Pts',(7.58212511123354,-0.785295100588523,17.3627784000746));
#8163=CARTESIAN_POINT('Ctrl Pts',(7.57788609335654,-0.80197871978988,17.3638266540774));
#8164=CARTESIAN_POINT('Ctrl Pts',(7.56680151022728,-0.844184880978747,17.3664733104739));
#8165=CARTESIAN_POINT('Ctrl Pts',(7.55977526634653,-0.869658965258959,17.368065872046));
#8166=CARTESIAN_POINT('Ctrl Pts',(7.51283540917338,-1.03202439684236,17.3781904264158));
#8167=CARTESIAN_POINT('Ctrl Pts',(7.46418491208713,-1.16623413737935,17.3864305006333));
#8168=CARTESIAN_POINT('Ctrl Pts',(7.36008960238266,-1.40306098963202,17.4010965748994));
#8169=CARTESIAN_POINT('Ctrl Pts',(7.3076722618481,-1.50672943085777,17.4075665322756));
#8170=CARTESIAN_POINT('Ctrl Pts',(7.16179562435811,-1.7602395622959,17.4239294390725));
#8171=CARTESIAN_POINT('Ctrl Pts',(7.06142110399511,-1.90563505192807,17.4338212469983));
#8172=CARTESIAN_POINT('Ctrl Pts',(6.93068215346667,-2.0652567904974,17.4461581226165));
#8173=CARTESIAN_POINT('Ctrl Pts',(6.91136961550979,-2.08817603594508,17.4479686638805));
#8174=CARTESIAN_POINT('Ctrl Pts',(6.88405247088113,-2.11969204555891,17.4505188087015));
#8175=CARTESIAN_POINT('Ctrl Pts',(6.8763156199805,-2.12852019025575,17.4512398951258));
#8176=CARTESIAN_POINT('Ctrl Pts',(6.86316444797489,-2.14336197855872,17.452464027224));
#8177=CARTESIAN_POINT('Ctrl Pts',(6.85777529809564,-2.14939796460141,17.4529652179073));
#8178=CARTESIAN_POINT('Ctrl Pts',(6.84741375375233,-2.1609155529316,17.4539281423202));
#8179=CARTESIAN_POINT('Ctrl Pts',(6.84244512575294,-2.16640041683573,17.4543895770759));
#8180=CARTESIAN_POINT('Ctrl Pts',(6.83050516873597,-2.17949002490294,17.4554975858097));
#8181=CARTESIAN_POINT('Ctrl Pts',(6.82351618001147,-2.18707844816694,17.4561454645131));
#8182=CARTESIAN_POINT('Ctrl Pts',(6.79816967737895,-2.21433507795057,17.4584921841782));
#8183=CARTESIAN_POINT('Ctrl Pts',(6.77960305237923,-2.23380616010508,17.460205743448));
#8184=CARTESIAN_POINT('Ctrl Pts',(6.63766692459036,-2.37897309807701,17.4732492449244));
#8185=CARTESIAN_POINT('Ctrl Pts',(6.50443354318551,-2.49458757580444,17.4851617202718));
#8186=CARTESIAN_POINT('Ctrl Pts',(6.34242047661592,-2.61341181388632,17.4987544719417));
#8187=CARTESIAN_POINT('Ctrl Pts',(6.32223270782824,-2.62786226201846,17.5004339739429));
#8188=CARTESIAN_POINT('Ctrl Pts',(6.17041707209726,-2.73390084889562,17.5129517060931));
#8189=CARTESIAN_POINT('Ctrl Pts',(6.03227208164215,-2.81579231687521,17.5237020720199));
#8190=CARTESIAN_POINT('Ctrl Pts',(5.83729536214465,-2.91251011829875,17.5378531217607));
#8191=CARTESIAN_POINT('Ctrl Pts',(5.78532771960922,-2.93658505229964,17.5415344416708));
#8192=CARTESIAN_POINT('Ctrl Pts',(5.69438281561168,-2.97580786713871,17.5478223068354));
#8193=CARTESIAN_POINT('Ctrl Pts',(5.65570273264038,-2.991605219019,17.5504496919431));
#8194=CARTESIAN_POINT('Ctrl Pts',(5.59968004556968,-3.0132242038267,17.5541897869111));
#8195=CARTESIAN_POINT('Ctrl Pts',(5.58257927845958,-3.01965681102916,17.5553228306677));
#8196=CARTESIAN_POINT('Ctrl Pts',(5.55206995970538,-3.0308379415139,17.557329289839));
#8197=CARTESIAN_POINT('Ctrl Pts',(5.53868305267685,-3.03564372782525,17.5582045935896));
#8198=CARTESIAN_POINT('Ctrl Pts',(5.51114686843535,-3.04532368080307,17.5599948007428));
#8199=CARTESIAN_POINT('Ctrl Pts',(5.4969945618617,-3.05018823861609,17.5609093681771));
#8200=CARTESIAN_POINT('Ctrl Pts',(5.46093768559787,-3.06230187379469,17.5632257896918));
#8201=CARTESIAN_POINT('Ctrl Pts',(5.43898797996414,-3.06941469963751,17.5646231405301));
#8202=CARTESIAN_POINT('Ctrl Pts',(5.35428866523754,-3.09585992022371,17.569968181992));
#8203=CARTESIAN_POINT('Ctrl Pts',(5.29102773750733,-3.11350949590961,17.5738611954626));
#8204=CARTESIAN_POINT('Ctrl Pts',(4.90278901022853,-3.20914181941009,17.597248442036));
#8205=CARTESIAN_POINT('Ctrl Pts',(4.56790416102437,-3.23810679314254,17.6150524391799));
#8206=CARTESIAN_POINT('Ctrl Pts',(4.18792085897161,-3.21188209951904,17.637171667383));
#8207=CARTESIAN_POINT('Ctrl Pts',(4.14134200844061,-3.20764699781071,17.6399205202443));
#8208=CARTESIAN_POINT('Ctrl Pts',(4.06415002123486,-3.19893096325816,17.6445623167685));
#8209=CARTESIAN_POINT('Ctrl Pts',(4.03347865215829,-3.19501995107382,17.6464294604565));
#8210=CARTESIAN_POINT('Ctrl Pts',(3.99125406113507,-3.18901711692318,17.6490372343265));
#8211=CARTESIAN_POINT('Ctrl Pts',(3.97964783001051,-3.18730241283627,17.649757934463));
#8212=CARTESIAN_POINT('Ctrl Pts',(3.96005437429916,-3.18429826378558,17.650981602362));
#8213=CARTESIAN_POINT('Ctrl Pts',(3.9520620295563,-3.18304202266579,17.6514827184227));
#8214=CARTESIAN_POINT('Ctrl Pts',(3.93676652502225,-3.18057881238802,17.6524456554492));
#8215=CARTESIAN_POINT('Ctrl Pts',(3.92946266984737,-3.1793767578132,17.6529071784147));
#8216=CARTESIAN_POINT('Ctrl Pts',(3.91198415150622,-3.17643829409671,17.654015605431));
#8217=CARTESIAN_POINT('Ctrl Pts',(3.90181363655509,-3.17467815774732,17.6546638163495));
#8218=CARTESIAN_POINT('Ctrl Pts',(3.86512649035585,-3.1681473084216,17.6570132941445));
#8219=CARTESIAN_POINT('Ctrl Pts',(3.83866231254647,-3.16309312426167,17.6587293245425));
#8220=CARTESIAN_POINT('Ctrl Pts',(3.64138543984744,-3.12284670258013,17.671664996519));
#8221=CARTESIAN_POINT('Ctrl Pts',(3.47363262213271,-3.07417535280573,17.6834558230224));
#8222=CARTESIAN_POINT('Ctrl Pts',(3.14246145812883,-2.94820029907648,17.7074269182828));
#8223=CARTESIAN_POINT('Ctrl Pts',(2.97990245470859,-2.87023775754521,17.7195606389978));
#8224=CARTESIAN_POINT('Ctrl Pts',(2.77201839537422,-2.74817651579871,17.7352757873257));
#8225=CARTESIAN_POINT('Ctrl Pts',(2.72023385177468,-2.71575703577067,17.7392110544193));
#8226=CARTESIAN_POINT('Ctrl Pts',(2.63262073791459,-2.6573761422031,17.7459042697384));
#8227=CARTESIAN_POINT('Ctrl Pts',(2.59634885542461,-2.63211394047536,17.7486862558223));
#8228=CARTESIAN_POINT('Ctrl Pts',(2.5450859248808,-2.59482181831947,17.7526358336519));
#8229=CARTESIAN_POINT('Ctrl Pts',(2.52966618264017,-2.58339243127525,17.7538262466253));
#8230=CARTESIAN_POINT('Ctrl Pts',(2.50301939509041,-2.56327005079055,17.7558878869497));
#8231=CARTESIAN_POINT('Ctrl Pts',(2.49174611659163,-2.55463944842961,17.7567615147971));
#8232=CARTESIAN_POINT('Ctrl Pts',(2.46866660798003,-2.53672708615607,17.7585531931258));
#8233=CARTESIAN_POINT('Ctrl Pts',(2.45686746986413,-2.52743672314683,17.7594708740152));
#8234=CARTESIAN_POINT('Ctrl Pts',(2.4269151950109,-2.50351196458591,17.7618050976878));
#8235=CARTESIAN_POINT('Ctrl Pts',(2.40885495882912,-2.48876225913214,17.7632169956674));
#8236=CARTESIAN_POINT('Ctrl Pts',(2.33911369912581,-2.43053181889291,17.7686886278154));
#8237=CARTESIAN_POINT('Ctrl Pts',(2.2886424201401,-2.38562512967248,17.7726902158919));
#8238=CARTESIAN_POINT('Ctrl Pts',(1.99869771392132,-2.11084112312122,17.7960321724947));
#8239=CARTESIAN_POINT('Ctrl Pts',(1.79453086865377,-1.84670966079781,17.8137236163597));
#8240=CARTESIAN_POINT('Ctrl Pts',(1.61175235161855,-1.51521716828888,17.8357084465921));
#8241=CARTESIAN_POINT('Ctrl Pts',(1.59010546486741,-1.47385736307143,17.8384522625202));
#8242=CARTESIAN_POINT('Ctrl Pts',(1.55564563536271,-1.40438387922067,17.8430863442203));
#8243=CARTESIAN_POINT('Ctrl Pts',(1.54232452801917,-1.37652900700457,17.8449509196504));
#8244=CARTESIAN_POINT('Ctrl Pts',(1.52449979469413,-1.33783818730869,17.8475556761839));
#8245=CARTESIAN_POINT('Ctrl Pts',(1.51965160308294,-1.32716163392025,17.8482759875876));
#8246=CARTESIAN_POINT('Ctrl Pts',(1.51155750145409,-1.30907548998749,17.8494991884379));
#8247=CARTESIAN_POINT('Ctrl Pts',(1.50828096963643,-1.30167957190674,17.8500002294915));
#8248=CARTESIAN_POINT('Ctrl Pts',(1.50205903236507,-1.28749116139494,17.8509631795987));
#8249=CARTESIAN_POINT('Ctrl Pts',(1.4991091378223,-1.28070074173037,17.8514247916337));
#8250=CARTESIAN_POINT('Ctrl Pts',(1.49210058904709,-1.26441429320765,17.8525336407789));
#8251=CARTESIAN_POINT('Ctrl Pts',(1.4880641595107,-1.25490887159543,17.8531821869194));
#8252=CARTESIAN_POINT('Ctrl Pts',(1.47364702426217,-1.22049907019421,17.8555344705486));
#8253=CARTESIAN_POINT('Ctrl Pts',(1.46353381447304,-1.19548474761618,17.8572530177058));
#8254=CARTESIAN_POINT('Ctrl Pts',(1.39346545725631,-1.01571200390295,17.8696497279452));
#8255=CARTESIAN_POINT('Ctrl Pts',(1.34523547499512,-0.856666250735065,17.8808458304981));
#8256=CARTESIAN_POINT('Ctrl Pts',(1.27555594069633,-0.540986327088179,17.9027136101999));
#8257=CARTESIAN_POINT('Ctrl Pts',(1.25293717047129,-0.385051760889612,17.9133527290673));
#8258=CARTESIAN_POINT('Ctrl Pts',(1.2333471343102,-0.108940420664665,17.9315949290285));
#8259=CARTESIAN_POINT('Ctrl Pts',(1.23152306440408,0.0105874729040621,17.9393014113896));
#8260=CARTESIAN_POINT('Ctrl Pts',(1.23743273313204,0.157023417474341,17.9485039317567));
#8261=CARTESIAN_POINT('Ctrl Pts',(1.23886649681224,0.184078909287284,17.9501944273286));
#8262=CARTESIAN_POINT('Ctrl Pts',(1.24167900192721,0.22692088750235,17.9528564762268));
#8263=CARTESIAN_POINT('Ctrl Pts',(1.24283325991198,0.242720344189877,17.9538350008638));
#8264=CARTESIAN_POINT('Ctrl Pts',(1.24522468973586,0.272437259254777,17.955669675151));
#8265=CARTESIAN_POINT('Ctrl Pts',(1.2464359603021,0.286356376670746,17.956526614417));
#8266=CARTESIAN_POINT('Ctrl Pts',(1.24936786985855,0.317687489166557,17.9584503135568));
#8267=CARTESIAN_POINT('Ctrl Pts',(1.25113987271493,0.33509432203065,17.9595154378778));
#8268=CARTESIAN_POINT('Ctrl Pts',(1.2560454368601,0.379676389091274,17.9622345930253));
#8269=CARTESIAN_POINT('Ctrl Pts',(1.2593834291921,0.406828055700854,17.963882203253));
#8270=CARTESIAN_POINT('Ctrl Pts',(1.29053669609954,0.636090529680842,17.9777305180821));
#8271=CARTESIAN_POINT('Ctrl Pts',(1.33714061063732,0.835191021539577,17.9892963366749));
#8272=CARTESIAN_POINT('Ctrl Pts',(1.45920127007577,1.1976340710183,18.0107191484895));
#8273=CARTESIAN_POINT('Ctrl Pts',(1.53007234596313,1.36166624933642,18.0205835818753));
#8274=CARTESIAN_POINT('Ctrl Pts',(1.63711278150622,1.56196110220808,18.033749924833));
#8275=CARTESIAN_POINT('Ctrl Pts',(1.66105345875509,1.60441373940812,18.0366101428136));
#8276=CARTESIAN_POINT('Ctrl Pts',(1.70222774360734,1.67370484823327,18.041422128217));
#8277=CARTESIAN_POINT('Ctrl Pts',(1.71891419068282,1.70086046234113,18.0433456105338));
#8278=CARTESIAN_POINT('Ctrl Pts',(1.74236458308648,1.73778454982884,18.0460194931395));
#8279=CARTESIAN_POINT('Ctrl Pts',(1.7487844834652,1.74777071653791,18.0467486167704));
#8280=CARTESIAN_POINT('Ctrl Pts',(1.75968706003402,1.76452544993902,18.0479824264597));
#8281=CARTESIAN_POINT('Ctrl Pts',(1.76414048133063,1.77131308403381,18.0484851887683));
#8282=CARTESIAN_POINT('Ctrl Pts',(1.77268758470191,1.7842333575583,18.0494479351513));
#8283=CARTESIAN_POINT('Ctrl Pts',(1.77677674311759,1.79036889104188,18.0499076003301));
#8284=CARTESIAN_POINT('Ctrl Pts',(1.78657916328238,1.80496801343385,18.0510071675534));
#8285=CARTESIAN_POINT('Ctrl Pts',(1.79231162628024,1.81341852654092,18.0516483311739));
#8286=CARTESIAN_POINT('Ctrl Pts',(1.81289648258903,1.84345542798716,18.0539436907664));
#8287=CARTESIAN_POINT('Ctrl Pts',(1.82797140842111,1.86488709641623,18.0556117910376));
#8288=CARTESIAN_POINT('Ctrl Pts',(1.96077779876963,2.04888529092708,18.0701813412165));
#8289=CARTESIAN_POINT('Ctrl Pts',(2.09318804749009,2.2002944137908,18.0838390809187));
#8290=CARTESIAN_POINT('Ctrl Pts',(2.35581890646096,2.44936598455359,18.108308221133));
#8291=CARTESIAN_POINT('Ctrl Pts',(2.48100889545633,2.55140980236907,18.1191227658204));
#8292=CARTESIAN_POINT('Ctrl Pts',(2.66045001376294,2.67651513657042,18.1333472322813));
#8293=CARTESIAN_POINT('Ctrl Pts',(2.70844767165986,2.70810627057053,18.1370410058114));
#8294=CARTESIAN_POINT('Ctrl Pts',(2.79309806424371,2.76063263788371,18.1433661548506));
#8295=CARTESIAN_POINT('Ctrl Pts',(2.82936362209553,2.78216171327825,18.1460181919573));
#8296=CARTESIAN_POINT('Ctrl Pts',(2.88242826343463,2.81227095310713,18.1498178017836));
#8297=CARTESIAN_POINT('Ctrl Pts',(2.89889530364076,2.82142452710083,18.1509858758511));
#8298=CARTESIAN_POINT('Ctrl Pts',(2.92786111434785,2.83719493948615,18.1530216300262));
#8299=CARTESIAN_POINT('Ctrl Pts',(2.94032480097321,2.84387481673461,18.1538915391528));
#8300=CARTESIAN_POINT('Ctrl Pts',(2.96460580694255,2.856683155031,18.155574697084));
#8301=CARTESIAN_POINT('Ctrl Pts',(2.9764179060678,2.86282084756358,18.1563882592165));
#8302=CARTESIAN_POINT('Ctrl Pts',(3.00807495259627,2.87902188451017,18.1585548810051));
#8303=CARTESIAN_POINT('Ctrl Pts',(3.02798688440838,2.88895330800317,18.1599033056961));
#8304=CARTESIAN_POINT('Ctrl Pts',(3.10176861641895,2.92480387814324,18.1648487421524));
#8305=CARTESIAN_POINT('Ctrl Pts',(3.15625558582648,2.94942988063635,18.168401227318));
#8306=CARTESIAN_POINT('Ctrl Pts',(3.52629583588521,3.10442464018978,18.1919431062201));
#8307=CARTESIAN_POINT('Ctrl Pts',(3.86009815043818,3.18543169748073,18.2101076606996));
#8308=CARTESIAN_POINT('Ctrl Pts',(4.24725345507066,3.21629586340303,18.2326569091821));
#8309=CARTESIAN_POINT('Ctrl Pts',(4.29421804560129,3.21900674499806,18.2354211642744));
#8310=CARTESIAN_POINT('Ctrl Pts',(4.37225484965584,3.22179914761503,18.2400865422355));
#8311=CARTESIAN_POINT('Ctrl Pts',(4.40330010815037,3.22246096704296,18.2419615284009));
#8312=CARTESIAN_POINT('Ctrl Pts',(4.44610043648753,3.22275474736778,18.2445785140417));
#8313=CARTESIAN_POINT('Ctrl Pts',(4.45785225870054,3.22277112869508,18.2453003986375));
#8314=CARTESIAN_POINT('Ctrl Pts',(4.47769799622732,3.22269024504698,18.2465254901713));
#8315=CARTESIAN_POINT('Ctrl Pts',(4.48579207778506,3.22262676132734,18.2470268353177));
#8316=CARTESIAN_POINT('Ctrl Pts',(4.50128328850569,3.22244689358093,18.2479897348765));
#8317=CARTESIAN_POINT('Ctrl Pts',(4.50868038289312,3.22233553076978,18.2484509883077));
#8318=CARTESIAN_POINT('Ctrl Pts',(4.52638107799941,3.22200808352567,18.2495581365008));
#8319=CARTESIAN_POINT('Ctrl Pts',(4.53668407920401,3.22176804339415,18.2502053315818));
#8320=CARTESIAN_POINT('Ctrl Pts',(4.57380187564839,3.22072511475752,18.2525464466231));
#8321=CARTESIAN_POINT('Ctrl Pts',(4.6006067126288,3.21963685611386,18.2542549934808));
#8322=CARTESIAN_POINT('Ctrl Pts',(4.80916559087941,3.20855994778415,18.2676719831817));
#8323=CARTESIAN_POINT('Ctrl Pts',(4.98977627395893,3.18352372355826,18.2800022053041));
#8324=CARTESIAN_POINT('Ctrl Pts',(5.33736362501278,3.10492298519491,18.3041104649829));
#8325=CARTESIAN_POINT('Ctrl Pts',(5.50405278947946,3.05272046722543,18.3158488470475));
#8326=CARTESIAN_POINT('Ctrl Pts',(5.74974893418431,2.95326330277609,18.3331158729495));
#8327=CARTESIAN_POINT('Ctrl Pts',(5.83231819952626,2.91571238762201,18.338916852701));
#8328=CARTESIAN_POINT('Ctrl Pts',(5.93546206766403,2.86344551062101,18.3461639569532));
#8329=CARTESIAN_POINT('Ctrl Pts',(5.95759191940309,2.85190650764038,18.3477190117708));
#8330=CARTESIAN_POINT('Ctrl Pts',(5.99313477734857,2.83284530850656,18.3502174052531));
#8331=CARTESIAN_POINT('Ctrl Pts',(6.00663155622794,2.82548231606796,18.3511663209502));
#8332=CARTESIAN_POINT('Ctrl Pts',(6.03237465478157,2.81119851853907,18.3529768058081));
#8333=CARTESIAN_POINT('Ctrl Pts',(6.04462933227762,2.80429358571775,18.353838914319));
#8334=CARTESIAN_POINT('Ctrl Pts',(6.07247998116988,2.78835993841448,18.3557989695407));
#8335=CARTESIAN_POINT('Ctrl Pts',(6.08804630553277,2.77928015091319,18.3568950488875));
#8336=CARTESIAN_POINT('Ctrl Pts',(6.1368385592051,2.75026857462006,18.3603331596537));
#8337=CARTESIAN_POINT('Ctrl Pts',(6.16978242951311,2.72986746585732,18.3626581336002));
#8338=CARTESIAN_POINT('Ctrl Pts',(6.42599016402845,2.56474049801035,18.3807897360878));
#8339=CARTESIAN_POINT('Ctrl Pts',(6.6309173361166,2.39346940108887,18.3954839606383));
#8340=CARTESIAN_POINT('Ctrl Pts',(6.92775042164736,2.07543469982288,18.419876075711));
#8341=CARTESIAN_POINT('Ctrl Pts',(7.0331205750862,1.94306779650924,18.4294342190971));
#8342=CARTESIAN_POINT('Ctrl Pts',(7.13875264781814,1.78658014987017,18.440845502285));
#8343=CARTESIAN_POINT('Ctrl Pts',(7.14973381822924,1.76998270475036,18.44205722001));
#8344=CARTESIAN_POINT('Ctrl Pts',(7.16591065360235,1.74503317587486,18.4438824795525));
#8345=CARTESIAN_POINT('Ctrl Pts',(7.17122317378577,1.73675692895483,18.4444885692249));
#8346=CARTESIAN_POINT('Ctrl Pts',(7.18028893838699,1.72249036412953,18.4455346341585));
#8347=CARTESIAN_POINT('Ctrl Pts',(7.18406047435073,1.71651182919033,18.4459733918043));
#8348=CARTESIAN_POINT('Ctrl Pts',(7.19262104145066,1.70284239772997,18.4469775238051));
#8349=CARTESIAN_POINT('Ctrl Pts',(7.19739724115002,1.69514382828959,18.4475437068857));
#8350=CARTESIAN_POINT('Ctrl Pts',(7.21039331357081,1.67399744150392,18.4491004764101));
#8351=CARTESIAN_POINT('Ctrl Pts',(7.21854697087583,1.66050950616903,18.4500951823816));
#8352=CARTESIAN_POINT('Ctrl Pts',(7.25990987014407,1.59093859332788,18.4552326238555));
#8353=CARTESIAN_POINT('Ctrl Pts',(7.29150885086439,1.53392113941218,18.4594651813617));
#8354=CARTESIAN_POINT('Ctrl Pts',(7.33699852857038,1.44562598211644,18.4660095916498));
#8355=CARTESIAN_POINT('Ctrl Pts',(7.35215779216634,1.41501630349278,18.4682766470177));
#8356=CARTESIAN_POINT('Ctrl Pts',(7.48610796830902,1.13337291816072,18.4890865528718));
#8357=CARTESIAN_POINT('Ctrl Pts',(7.57249072918749,0.868155303675707,18.5081892131244));
#8358=CARTESIAN_POINT('Ctrl Pts',(7.64009809065663,0.508352915344718,18.5320130836027));
#8359=CARTESIAN_POINT('Ctrl Pts',(7.65283313618465,0.420922318484652,18.5376596092375));
#8360=CARTESIAN_POINT('Ctrl Pts',(7.66451877335594,0.308459403168151,18.5447447508743));
#8361=CARTESIAN_POINT('Ctrl Pts',(7.66679266168259,0.283817889359796,18.5462864146476));
#8362=CARTESIAN_POINT('Ctrl Pts',(7.67001513608912,0.243873782052595,18.548768613953));
#8363=CARTESIAN_POINT('Ctrl Pts',(7.67113870729234,0.228586693745645,18.5497145953185));
#8364=CARTESIAN_POINT('Ctrl Pts',(7.67308499922083,0.199243534041357,18.5515229323804));
#8365=CARTESIAN_POINT('Ctrl Pts',(7.67392475307572,0.185188982965779,18.552385801271));
#8366=CARTESIAN_POINT('Ctrl Pts',(7.67563430860804,0.153039605947283,18.5543523147175));
#8367=CARTESIAN_POINT('Ctrl Pts',(7.67644370459281,0.134941942603784,18.5554540476084));
#8368=CARTESIAN_POINT('Ctrl Pts',(7.67852384032242,0.0776032069004583,18.5589287054524));
#8369=CARTESIAN_POINT('Ctrl Pts',(7.67923017083788,0.0383443493416745,18.5612840410069));
#8370=CARTESIAN_POINT('Ctrl Pts',(7.67921897520336,-0.000918943050559805,
18.563618782904));
#8371=CARTESIAN_POINT('',(7.67921766478722,0.00291592938798334,18.3138092652699));
#8372=CARTESIAN_POINT('Ctrl Pts',(7.67921910621823,-1.45987529487438E-10,
18.3139723139554));
#8373=CARTESIAN_POINT('Ctrl Pts',(7.67921910621828,0.000972342785896192,
18.3139178708026));
#8374=CARTESIAN_POINT('Ctrl Pts',(7.67921866616676,0.00194469629559445,
18.3138634295123));
#8375=CARTESIAN_POINT('Ctrl Pts',(7.67921778603496,0.00291706008692861,
18.3138089900028));
#8376=CARTESIAN_POINT('Ctrl Pts',(7.67921778706881,0.00291591766745765,
18.3138090539631));
#8377=CARTESIAN_POINT('Ctrl Pts',(7.67902220457112,0.219078823587967,18.3017067902972));
#8378=CARTESIAN_POINT('Ctrl Pts',(7.65707889795432,0.434655820836481,18.2897863540716));
#8379=CARTESIAN_POINT('Ctrl Pts',(7.60880514919697,0.670446050244141,18.2754737311236));
#8380=CARTESIAN_POINT('Ctrl Pts',(7.60360584464707,0.694442732277932,18.2740017270286));
#8381=CARTESIAN_POINT('Ctrl Pts',(7.59513947807702,0.731468530665847,18.2717033529349));
#8382=CARTESIAN_POINT('Ctrl Pts',(7.59206418507794,0.744541068146832,18.2708866133773));
#8383=CARTESIAN_POINT('Ctrl Pts',(7.58614991284442,0.768994929362721,18.2693482721318));
#8384=CARTESIAN_POINT('Ctrl Pts',(7.58333031306333,0.780380763472973,18.2686277203827));
#8385=CARTESIAN_POINT('Ctrl Pts',(7.57846130622866,0.799592210917159,18.2674042705642));
#8386=CARTESIAN_POINT('Ctrl Pts',(7.57644444096982,0.807426101546395,18.2669032232013));
#8387=CARTESIAN_POINT('Ctrl Pts',(7.57252575545191,0.822413098394386,18.2659403930044));
#8388=CARTESIAN_POINT('Ctrl Pts',(7.57062875634282,0.829567367105543,18.2654789079425));
#8389=CARTESIAN_POINT('Ctrl Pts',(7.56602742070546,0.846682457257635,18.2643705415024));
#8390=CARTESIAN_POINT('Ctrl Pts',(7.56329986360912,0.85663687332996,18.2637223532187));
#8391=CARTESIAN_POINT('Ctrl Pts',(7.55327919942814,0.892530587111473,18.2613727282853));
#8392=CARTESIAN_POINT('Ctrl Pts',(7.5457088918796,0.918390460999878,18.2596565244853));
#8393=CARTESIAN_POINT('Ctrl Pts',(7.48794461673195,1.10691080639361,18.246988664533));
#8394=CARTESIAN_POINT('Ctrl Pts',(7.42526105832655,1.26544805290942,18.2354923274378));
#8395=CARTESIAN_POINT('Ctrl Pts',(7.29434462630614,1.53257348785622,18.2153676248116));
#8396=CARTESIAN_POINT('Ctrl Pts',(7.23160392027629,1.64345636269755,18.206761026444));
#8397=CARTESIAN_POINT('Ctrl Pts',(7.08615438131089,1.86831876536636,18.1889721971483));
#8398=CARTESIAN_POINT('Ctrl Pts',(7.00220115682713,1.98119085147181,18.1798438399361));
#8399=CARTESIAN_POINT('Ctrl Pts',(6.89244629127531,2.11020489532854,18.1691845424563));
#8400=CARTESIAN_POINT('Ctrl Pts',(6.87346167709424,2.13192320349972,18.1673814204658));
#8401=CARTESIAN_POINT('Ctrl Pts',(6.84505988469014,2.16354761042593,18.1647421610638));
#8402=CARTESIAN_POINT('Ctrl Pts',(6.83586759705272,2.17365291631261,18.1638966949583));
#8403=CARTESIAN_POINT('Ctrl Pts',(6.81709601361245,2.19402720247581,18.1621876219829));
#8404=CARTESIAN_POINT('Ctrl Pts',(6.80751328993501,2.20429263421184,18.1613241877605));
#8405=CARTESIAN_POINT('Ctrl Pts',(6.78724524961101,2.22572211320399,18.1595166326087));
#8406=CARTESIAN_POINT('Ctrl Pts',(6.77654609366499,2.23687262515404,18.15857313812));
#8407=CARTESIAN_POINT('Ctrl Pts',(6.74810491163968,2.26609003721838,18.1560927149251));
#8408=CARTESIAN_POINT('Ctrl Pts',(6.73022922821239,2.28402576273897,18.1545616513924));
#8409=CARTESIAN_POINT('Ctrl Pts',(6.65155945073906,2.36112078272651,18.1479405916881));
#8410=CARTESIAN_POINT('Ctrl Pts',(6.58865157296379,2.4180803777475,18.1429457569334));
#8411=CARTESIAN_POINT('Ctrl Pts',(6.31176948151111,2.64956388523367,18.1220375232401));
#8412=CARTESIAN_POINT('Ctrl Pts',(6.07811950043421,2.7986724024515,18.10708729565));
#8413=CARTESIAN_POINT('Ctrl Pts',(5.73727478898837,2.95901699600314,18.0855554388898));
#8414=CARTESIAN_POINT('Ctrl Pts',(5.64426619493235,2.99756213033704,18.0796916195761));
#8415=CARTESIAN_POINT('Ctrl Pts',(5.53311088446696,3.03764183810505,18.0725292580392));
#8416=CARTESIAN_POINT('Ctrl Pts',(5.5165563622763,3.04345863011925,18.0714586069918));
#8417=CARTESIAN_POINT('Ctrl Pts',(5.49110846461714,3.05216749199089,18.0698055558867));
#8418=CARTESIAN_POINT('Ctrl Pts',(5.48224833056234,3.05515662100498,18.0692286815634));
#8419=CARTESIAN_POINT('Ctrl Pts',(5.46595113524696,3.06057589529458,18.0681649226179));
#8420=CARTESIAN_POINT('Ctrl Pts',(5.4585181170781,3.06301755688028,18.0676787194975));
#8421=CARTESIAN_POINT('Ctrl Pts',(5.44169634814991,3.06847553180218,18.0665760672837));
#8422=CARTESIAN_POINT('Ctrl Pts',(5.43230266207107,3.07147581347142,18.0659587119084));
#8423=CARTESIAN_POINT('Ctrl Pts',(5.40797556983524,3.07912286413166,18.0643560486737));
#8424=CARTESIAN_POINT('Ctrl Pts',(5.39302203928985,3.08370406225967,18.0633671444802));
#8425=CARTESIAN_POINT('Ctrl Pts',(5.2939231292201,3.11327694979502,18.0567914066732));
#8426=CARTESIAN_POINT('Ctrl Pts',(5.20882724713966,3.13492854096393,18.0510403580686));
#8427=CARTESIAN_POINT('Ctrl Pts',(4.84349384724895,3.21215221840393,18.0261977317667));
#8428=CARTESIAN_POINT('Ctrl Pts',(4.55735162783163,3.2338171590074,18.0065091569289));
#8429=CARTESIAN_POINT('Ctrl Pts',(4.18289842369977,3.21236057737842,17.9820903032113));
#8430=CARTESIAN_POINT('Ctrl Pts',(4.09393743207977,3.20354095965228,17.9763753043247));
#8431=CARTESIAN_POINT('Ctrl Pts',(3.9808574037683,3.187558310022,17.9692183985274));
#8432=CARTESIAN_POINT('Ctrl Pts',(3.95630465989973,3.18379805474869,17.9676708537229));
#8433=CARTESIAN_POINT('Ctrl Pts',(3.91665490350325,3.17725569056913,17.9651816097251));
#8434=CARTESIAN_POINT('Ctrl Pts',(3.90153036724323,3.17464897361847,17.9642344067374));
#8435=CARTESIAN_POINT('Ctrl Pts',(3.87257519088137,3.16944529300161,17.9624253061553));
#8436=CARTESIAN_POINT('Ctrl Pts',(3.85874184493001,3.16686559562092,17.9615628836103));
#8437=CARTESIAN_POINT('Ctrl Pts',(3.82718417983331,3.1607664515855,17.9595995422138));
#8438=CARTESIAN_POINT('Ctrl Pts',(3.80947157588261,3.15718835301531,17.9585005143452));
#8439=CARTESIAN_POINT('Ctrl Pts',(3.75360868578368,3.14541370073778,17.9550429803124));
#8440=CARTESIAN_POINT('Ctrl Pts',(3.71557579329625,3.13667298521232,17.9527018148995));
#8441=CARTESIAN_POINT('Ctrl Pts',(3.42213901394682,3.063600118789,17.9347170930903));
#8442=CARTESIAN_POINT('Ctrl Pts',(3.17533609678247,2.96887128092349,17.9201593579953));
#8443=CARTESIAN_POINT('Ctrl Pts',(2.83596270779622,2.78831852162408,17.8986121307256));
#8444=CARTESIAN_POINT('Ctrl Pts',(2.73242371016655,2.72551360085741,17.8917844149911));
#8445=CARTESIAN_POINT('Ctrl Pts',(2.60022057258223,2.63476904710498,17.8824082052472));
#8446=CARTESIAN_POINT('Ctrl Pts',(2.56818412795226,2.61190469154603,17.8800812907266));
#8447=CARTESIAN_POINT('Ctrl Pts',(2.5147440117586,2.57226749424362,17.8760913002418));
#8448=CARTESIAN_POINT('Ctrl Pts',(2.49311870978285,2.55579958414268,17.8744456716623));
#8449=CARTESIAN_POINT('Ctrl Pts',(2.46292076423575,2.53219408545717,17.872099464602));
#8450=CARTESIAN_POINT('Ctrl Pts',(2.45417226063277,2.52528200640435,17.8714139445679));
#8451=CARTESIAN_POINT('Ctrl Pts',(2.43922269831306,2.51334402810182,17.8702321644941));
#8452=CARTESIAN_POINT('Ctrl Pts',(2.43300402619923,2.50834015688915,17.8697374624734));
#8453=CARTESIAN_POINT('Ctrl Pts',(2.42094245123594,2.49856073438672,17.8687717638766));
#8454=CARTESIAN_POINT('Ctrl Pts',(2.41509767778883,2.49378772051554,17.8683009701457));
#8455=CARTESIAN_POINT('Ctrl Pts',(2.39915331634107,2.48067347350706,17.8670090030699));
#8456=CARTESIAN_POINT('Ctrl Pts',(2.38908786531271,2.47229123131293,17.8661849455991));
#8457=CARTESIAN_POINT('Ctrl Pts',(2.35020441156416,2.43950662138524,17.8629695050356));
#8458=CARTESIAN_POINT('Ctrl Pts',(2.32176630714562,2.41466088535133,17.86054888641));
#8459=CARTESIAN_POINT('Ctrl Pts',(2.13208175656911,2.24296783296895,17.8439673343767));
#8460=CARTESIAN_POINT('Ctrl Pts',(1.98567366264413,2.08058705567431,17.8290320257688));
#8461=CARTESIAN_POINT('Ctrl Pts',(1.7752746792486,1.79341521202182,17.8050485566151));
#8462=CARTESIAN_POINT('Ctrl Pts',(1.70097776999226,1.67702597657883,17.79586790053));
#8463=CARTESIAN_POINT('Ctrl Pts',(1.59632712291983,1.48724895090778,17.7818272118218));
#8464=CARTESIAN_POINT('Ctrl Pts',(1.56083122172959,1.41689963434564,17.7768060278843));
#8465=CARTESIAN_POINT('Ctrl Pts',(1.51800495768735,1.32367411810515,17.7703829241998));
#8466=CARTESIAN_POINT('Ctrl Pts',(1.50830346973981,1.30192325116869,17.7689001576579));
#8467=CARTESIAN_POINT('Ctrl Pts',(1.49283651507568,1.26618646566647,17.7664892402141));
#8468=CARTESIAN_POINT('Ctrl Pts',(1.48692696672514,1.25226426737094,17.7655562060874));
#8469=CARTESIAN_POINT('Ctrl Pts',(1.47567917383837,1.22523839398297,17.7637567709461));
#8470=CARTESIAN_POINT('Ctrl Pts',(1.4703287970387,1.21214017631349,17.7628899753721));
#8471=CARTESIAN_POINT('Ctrl Pts',(1.45815513908929,1.18176809877748,17.7608920834409));
#8472=CARTESIAN_POINT('Ctrl Pts',(1.45139453105396,1.1644695379604,17.7597631140323));
#8473=CARTESIAN_POINT('Ctrl Pts',(1.4299005674612,1.10803826772325,17.7561083681613));
#8474=CARTESIAN_POINT('Ctrl Pts',(1.41577879806514,1.06867610361099,17.7536029297105));
#8475=CARTESIAN_POINT('Ctrl Pts',(1.33882591074292,0.840292977266851,17.7392969084463));
#8476=CARTESIAN_POINT('Ctrl Pts',(1.29285791951042,0.646040299189059,17.7280666575537));
#8477=CARTESIAN_POINT('Ctrl Pts',(1.24177440756993,0.282766235200084,17.7075407972883));
#8478=CARTESIAN_POINT('Ctrl Pts',(1.23142063369164,0.115209047531944,17.6982406204294));
#8479=CARTESIAN_POINT('Ctrl Pts',(1.23491218439861,-0.099588574865565,17.6857698812959));
#8480=CARTESIAN_POINT('Ctrl Pts',(1.23671692944911,-0.146773165160949,17.6829956328373));
#8481=CARTESIAN_POINT('Ctrl Pts',(1.2414307941622,-0.224979417776491,17.6783150012011));
#8482=CARTESIAN_POINT('Ctrl Pts',(1.24375444266111,-0.256030102910681,17.6764349754495));
#8483=CARTESIAN_POINT('Ctrl Pts',(1.24757526952819,-0.298757917447027,17.6738121190046));
#8484=CARTESIAN_POINT('Ctrl Pts',(1.24868716037419,-0.310468881436922,17.6730895229081));
#8485=CARTESIAN_POINT('Ctrl Pts',(1.25067247219531,-0.330228784207575,17.6718636154967));
#8486=CARTESIAN_POINT('Ctrl Pts',(1.25151216779087,-0.33828113992184,17.671362172308));
#8487=CARTESIAN_POINT('Ctrl Pts',(1.25317682238448,-0.353681754737367,17.6703994048724));
#8488=CARTESIAN_POINT('Ctrl Pts',(1.25399674267614,-0.361030466090661,17.6699383835343));
#8489=CARTESIAN_POINT('Ctrl Pts',(1.25601859844113,-0.378602796511614,17.6688322184066));
#8490=CARTESIAN_POINT('Ctrl Pts',(1.25724423375604,-0.388823531853105,17.6681857789811));
#8491=CARTESIAN_POINT('Ctrl Pts',(1.26183070545722,-0.425580198028187,17.6658504379682));
#8492=CARTESIAN_POINT('Ctrl Pts',(1.26547280382327,-0.452079093527858,17.6641470018324));
#8493=CARTESIAN_POINT('Ctrl Pts',(1.29707206589123,-0.662531810227149,17.6504766306551));
#8494=CARTESIAN_POINT('Ctrl Pts',(1.34058069505014,-0.843780325644675,17.6378602622274));
#8495=CARTESIAN_POINT('Ctrl Pts',(1.45375320281548,-1.18288293458307,17.6136778585585));
#8496=CARTESIAN_POINT('Ctrl Pts',(1.52092979962837,-1.34094567840818,17.6021452578269));
#8497=CARTESIAN_POINT('Ctrl Pts',(1.62792381585929,-1.5456346646578,17.5871051655424));
#8498=CARTESIAN_POINT('Ctrl Pts',(1.65693103694159,-1.59757387770947,17.583276644109));
#8499=CARTESIAN_POINT('Ctrl Pts',(1.70951460006085,-1.68589259241211,17.5767457805));
#8500=CARTESIAN_POINT('Ctrl Pts',(1.73241700917572,-1.72265299977992,17.574020923687));
#8501=CARTESIAN_POINT('Ctrl Pts',(1.76644492888785,-1.77489434223392,17.5701372479022));
#8502=CARTESIAN_POINT('Ctrl Pts',(1.77697688180983,-1.79075443458514,17.5689566412206));
#8503=CARTESIAN_POINT('Ctrl Pts',(1.79559236605462,-1.81825557749611,17.5669064672318));
#8504=CARTESIAN_POINT('Ctrl Pts',(1.80361320342808,-1.82993823411243,17.5660345744349));
#8505=CARTESIAN_POINT('Ctrl Pts',(1.82032296617973,-1.8539358748889,17.5642414173779));
#8506=CARTESIAN_POINT('Ctrl Pts',(1.82902175739814,-1.86624359104744,17.5633205572675));
#8507=CARTESIAN_POINT('Ctrl Pts',(1.8515456418621,-1.89764245389676,17.5609679044192));
#8508=CARTESIAN_POINT('Ctrl Pts',(1.86549457261731,-1.91664398086319,17.5595409055754));
#8509=CARTESIAN_POINT('Ctrl Pts',(1.92137920327115,-1.99104604014653,17.553938313669));
#8510=CARTESIAN_POINT('Ctrl Pts',(1.96489507265508,-2.04523960035997,17.549824562917));
#8511=CARTESIAN_POINT('Ctrl Pts',(2.22469752876772,-2.34817975736258,17.5265287183775));
#8512=CARTESIAN_POINT('Ctrl Pts',(2.47633822250584,-2.56394151868802,17.5089533273866));
#8513=CARTESIAN_POINT('Ctrl Pts',(2.79586405862106,-2.76236828748259,17.4871071519419));
#8514=CARTESIAN_POINT('Ctrl Pts',(2.83596485755118,-2.7860820577079,17.4843686844615));
#8515=CARTESIAN_POINT('Ctrl Pts',(2.90343386677729,-2.82403072669977,17.4797428349941));
#8516=CARTESIAN_POINT('Ctrl Pts',(2.93051863454886,-2.8387572984458,17.4778810282201));
#8517=CARTESIAN_POINT('Ctrl Pts',(2.96818340877761,-2.85854168429103,17.4752795717097));
#8518=CARTESIAN_POINT('Ctrl Pts',(2.97858693377309,-2.86393420883834,17.4745597272107));
#8519=CARTESIAN_POINT('Ctrl Pts',(2.99621952325265,-2.87295216092306,17.4733371270332));
#8520=CARTESIAN_POINT('Ctrl Pts',(3.00343337450779,-2.87660739833033,17.4728362160438));
#8521=CARTESIAN_POINT('Ctrl Pts',(3.01727804234486,-2.88355708536792,17.4718733616419));
#8522=CARTESIAN_POINT('Ctrl Pts',(3.02390656422465,-2.88685589241467,17.4714117142145));
#8523=CARTESIAN_POINT('Ctrl Pts',(3.03981106022875,-2.89470279525032,17.4703025785089));
#8524=CARTESIAN_POINT('Ctrl Pts',(3.04909758371662,-2.89922915322747,17.4696537793842));
#8525=CARTESIAN_POINT('Ctrl Pts',(3.08274736120653,-2.91543067326408,17.4672990189206));
#8526=CARTESIAN_POINT('Ctrl Pts',(3.10723466031358,-2.92684364842147,17.4655782058228));
#8527=CARTESIAN_POINT('Ctrl Pts',(3.28247572896301,-3.0058531191887,17.4532271512054));
#8528=CARTESIAN_POINT('Ctrl Pts',(3.43807472845809,-3.06207053171948,17.4420837889553));
#8529=CARTESIAN_POINT('Ctrl Pts',(3.63264751888794,-3.11589187379188,17.4284281942839));
#8530=CARTESIAN_POINT('Ctrl Pts',(3.66818020068284,-3.12507036535704,17.4259447738114));
#8531=CARTESIAN_POINT('Ctrl Pts',(3.85898907870392,-3.17089698573329,17.4126808919315));
#8532=CARTESIAN_POINT('Ctrl Pts',(4.01668296255306,-3.19658693281915,17.4019879880243));
#8533=CARTESIAN_POINT('Ctrl Pts',(4.2614399572273,-3.21799600106738,17.3860154573004));
#8534=CARTESIAN_POINT('Ctrl Pts',(4.34750688112334,-3.22205898574124,17.3805125245574));
#8535=CARTESIAN_POINT('Ctrl Pts',(4.45818015856971,-3.22284298054387,17.373578590175));
#8536=CARTESIAN_POINT('Ctrl Pts',(4.48272188194024,-3.22273651579276,17.3720498664936));
#8537=CARTESIAN_POINT('Ctrl Pts',(4.52254084771386,-3.22210887974095,17.369583383438));
#8538=CARTESIAN_POINT('Ctrl Pts',(4.53781944168036,-3.22175933981559,17.3686403034034));
#8539=CARTESIAN_POINT('Ctrl Pts',(4.56718031021658,-3.22087863184655,17.3668341624359));
#8540=CARTESIAN_POINT('Ctrl Pts',(4.58126268649436,-3.22036375337563,17.3659706136328));
#8541=CARTESIAN_POINT('Ctrl Pts',(4.61353120282899,-3.21897197010636,17.3639979208628));
#8542=CARTESIAN_POINT('Ctrl Pts',(4.63171430059792,-3.21803327973238,17.3628907319167));
#8543=CARTESIAN_POINT('Ctrl Pts',(4.68958626687517,-3.21455370787104,17.3593801653059));
#8544=CARTESIAN_POINT('Ctrl Pts',(4.72923742370364,-3.21143220472174,17.3569949096965));
#8545=CARTESIAN_POINT('Ctrl Pts',(5.02331932522896,-3.18279460040851,17.3394310924527));
#8546=CARTESIAN_POINT('Ctrl Pts',(5.27396187208866,-3.12781403392186,17.3252646958498));
#8547=CARTESIAN_POINT('Ctrl Pts',(5.63441523565642,-3.00240168649888,17.3038890654157));
#8548=CARTESIAN_POINT('Ctrl Pts',(5.75080522490167,-2.95409247797503,17.296798655125));
#8549=CARTESIAN_POINT('Ctrl Pts',(5.90030753851901,-2.88150509558005,17.2870897457788));
#8550=CARTESIAN_POINT('Ctrl Pts',(5.93621866209718,-2.86322929491492,17.2847093826322));
#8551=CARTESIAN_POINT('Ctrl Pts',(5.99619368212348,-2.83127731533167,17.2806361880545));
#8552=CARTESIAN_POINT('Ctrl Pts',(6.02044184046601,-2.81795531828166,17.2789617692416));
#8553=CARTESIAN_POINT('Ctrl Pts',(6.05428516475463,-2.79879036087014,17.276581419683));
#8554=CARTESIAN_POINT('Ctrl Pts',(6.06402663050121,-2.79320647973406,17.2758911426017));
#8555=CARTESIAN_POINT('Ctrl Pts',(6.08065452762133,-2.7835594496884,17.2747037602563));
#8556=CARTESIAN_POINT('Ctrl Pts',(6.08755549184291,-2.77952130672651,17.2742082521505));
#8557=CARTESIAN_POINT('Ctrl Pts',(6.1009210053411,-2.77163347562565,17.2732431625058));
#8558=CARTESIAN_POINT('Ctrl Pts',(6.10738716690114,-2.7677867919894,17.2727737975309));
#8559=CARTESIAN_POINT('Ctrl Pts',(6.12497710498134,-2.7572390654458,17.2714903885631));
#8560=CARTESIAN_POINT('Ctrl Pts',(6.13607380042161,-2.75049345822574,17.2706735240382));
#8561=CARTESIAN_POINT('Ctrl Pts',(6.17858499059505,-2.72429800399969,17.2675171843821));
#8562=CARTESIAN_POINT('Ctrl Pts',(6.20970358930844,-2.70437632555377,17.2651497808155));
#8563=CARTESIAN_POINT('Ctrl Pts',(6.42270387977984,-2.5627952617542,17.2485838177806));
#8564=CARTESIAN_POINT('Ctrl Pts',(6.59211552015056,-2.42342820268489,17.233598352804));
#8565=CARTESIAN_POINT('Ctrl Pts',(6.84331554104593,-2.16983124576322,17.2095497425833));
#8566=CARTESIAN_POINT('Ctrl Pts',(6.93413517870308,-2.06552205300968,17.2003534785003));
#8567=CARTESIAN_POINT('Ctrl Pts',(7.06583416808997,-1.89302624096835,17.1862924756662));
#8568=CARTESIAN_POINT('Ctrl Pts',(7.11136860825697,-1.82861825969781,17.1812659963406));
#8569=CARTESIAN_POINT('Ctrl Pts',(7.16752747256039,-1.74265534651719,17.1748372435296));
#8570=CARTESIAN_POINT('Ctrl Pts',(7.18033584657732,-1.72256644347301,17.1733539461284));
#8571=CARTESIAN_POINT('Ctrl Pts',(7.20091045736917,-1.68949342297908,17.1709423870277));
#8572=CARTESIAN_POINT('Ctrl Pts',(7.20880993584666,-1.67659366758962,17.1700092371288));
#8573=CARTESIAN_POINT('Ctrl Pts',(7.22392173916218,-1.65152161558649,17.1682097292093));
#8574=CARTESIAN_POINT('Ctrl Pts',(7.23114528870851,-1.6393565245945,17.1673429755271));
#8575=CARTESIAN_POINT('Ctrl Pts',(7.24766323351348,-1.61111689879409,17.1653453955555));
#8576=CARTESIAN_POINT('Ctrl Pts',(7.25689934362201,-1.59500872273912,17.1642166940894));
#8577=CARTESIAN_POINT('Ctrl Pts',(7.28646769057199,-1.54239158409041,17.1605637460476));
#8578=CARTESIAN_POINT('Ctrl Pts',(7.30622968094536,-1.50556590502938,17.158059809029));
#8579=CARTESIAN_POINT('Ctrl Pts',(7.41986887847896,-1.28354460694213,17.1432540232464));
#8580=CARTESIAN_POINT('Ctrl Pts',(7.49638975284808,-1.09000943486189,17.1315784981138));
#8581=CARTESIAN_POINT('Ctrl Pts',(7.61036373587296,-0.693562947500273,17.1085083507381));
#8582=CARTESIAN_POINT('Ctrl Pts',(7.64805616436984,-0.491764102507658,17.0971512371842));
#8583=CARTESIAN_POINT('Ctrl Pts',(7.6692386096317,-0.255500116449311,17.0829964143166));
#8584=CARTESIAN_POINT('Ctrl Pts',(7.67164570852725,-0.22317577015947,17.0810409566029));
#8585=CARTESIAN_POINT('Ctrl Pts',(7.67427227269532,-0.178894157323701,17.0783296688662));
#8586=CARTESIAN_POINT('Ctrl Pts',(7.67491342058057,-0.166962638465749,17.0775958997524));
#8587=CARTESIAN_POINT('Ctrl Pts',(7.67587942940681,-0.146904327247348,17.076356519675));
#8588=CARTESIAN_POINT('Ctrl Pts',(7.676239910841,-0.138779227190497,17.0758528727562));
#8589=CARTESIAN_POINT('Ctrl Pts',(7.67686790054002,-0.123301654468929,17.0748902681147));
#8590=CARTESIAN_POINT('Ctrl Pts',(7.67714099376114,-0.115949483331574,17.0744316406517));
#8591=CARTESIAN_POINT('Ctrl Pts',(7.67773096357435,-0.0984512680055124,
17.0733369479978));
#8592=CARTESIAN_POINT('Ctrl Pts',(7.67802508056954,-0.0883046061388677,
17.0726996457262));
#8593=CARTESIAN_POINT('Ctrl Pts',(7.67889809343006,-0.0523170574305221,
17.0704307528381));
#8594=CARTESIAN_POINT('Ctrl Pts',(7.67921402492626,-0.0264715562262677,
17.06878565696));
#8595=CARTESIAN_POINT('Ctrl Pts',(7.67921904541626,-0.000626018462678653,
17.0671267777979));
#8596=CARTESIAN_POINT('Origin',(4.45646910621825,-5.13094777615093E-16,
-2.31077344927308));
#8597=CARTESIAN_POINT('',(7.67921910621823,-2.74841093364834E-11,15.8122671767608));
#8598=CARTESIAN_POINT('',(7.67921901097264,-0.000783521410691963,16.0578089001723));
#8599=CARTESIAN_POINT('',(7.67921910621823,-3.51191647465084E-13,-2.31077344927308));
#8600=CARTESIAN_POINT('',(7.67921774902577,0.00295766498587945,17.311387620665));
#8601=CARTESIAN_POINT('Ctrl Pts',(7.6792190109727,-0.000783520933934101,
16.0578089001435));
#8602=CARTESIAN_POINT('Ctrl Pts',(7.67921491899289,-0.0176145039721776,
16.0588276805675));
#8603=CARTESIAN_POINT('Ctrl Pts',(7.67907897611209,-0.0344447885085603,
16.0598528746788));
#8604=CARTESIAN_POINT('Ctrl Pts',(7.67865038393961,-0.0613805116184825,
16.0615050578984));
#8605=CARTESIAN_POINT('Ctrl Pts',(7.6784419992823,-0.0714872271008963,16.0621275601583));
#8606=CARTESIAN_POINT('Ctrl Pts',(7.67798711827065,-0.0894483808643351,
16.0632386841219));
#8607=CARTESIAN_POINT('Ctrl Pts',(7.67775944040108,-0.0973031149845316,
16.0637262548862));
#8608=CARTESIAN_POINT('Ctrl Pts',(7.67720772453566,-0.114202549861549,16.0647789061789));
#8609=CARTESIAN_POINT('Ctrl Pts',(7.67687432041597,-0.123246588449949,16.065344474249));
#8610=CARTESIAN_POINT('Ctrl Pts',(7.67584024310604,-0.148416969419151,16.0669244641013));
#8611=CARTESIAN_POINT('Ctrl Pts',(7.67505651110471,-0.164539374364985,16.0679433113746));
#8612=CARTESIAN_POINT('Ctrl Pts',(7.66970318492263,-0.259888642933266,16.0740065108407));
#8613=CARTESIAN_POINT('Ctrl Pts',(7.6623298918754,-0.338924387070562,16.0791857297162));
#8614=CARTESIAN_POINT('Ctrl Pts',(7.62421756467202,-0.630569443723733,16.0986801740901));
#8615=CARTESIAN_POINT('Ctrl Pts',(7.57516724304894,-0.840222401023601,16.1134122761078));
#8616=CARTESIAN_POINT('Ctrl Pts',(7.45350925688677,-1.19573261401036,16.1385094717261));
#8617=CARTESIAN_POINT('Ctrl Pts',(7.3900524302319,-1.34392284283161,16.1490192470493));
#8618=CARTESIAN_POINT('Ctrl Pts',(7.30328453056901,-1.51079205072159,16.160858081982));
#8619=CARTESIAN_POINT('Ctrl Pts',(7.29049079432192,-1.53465690761307,16.1625518163035));
#8620=CARTESIAN_POINT('Ctrl Pts',(7.26897798259115,-1.57359923656831,16.1653172388882));
#8621=CARTESIAN_POINT('Ctrl Pts',(7.26043496188212,-1.5887719270955,16.1663951132472));
#8622=CARTESIAN_POINT('Ctrl Pts',(7.24481966077702,-1.61598692630935,16.1683294721022));
#8623=CARTESIAN_POINT('Ctrl Pts',(7.23779132982529,-1.62805382568155,16.1691875072791));
#8624=CARTESIAN_POINT('Ctrl Pts',(7.22259419896889,-1.65376004166844,16.1710163338651));
#8625=CARTESIAN_POINT('Ctrl Pts',(7.21440243324587,-1.66738540295784,16.1719862636914));
#8626=CARTESIAN_POINT('Ctrl Pts',(7.19184339508827,-1.70428671664892,16.1746150715596));
#8627=CARTESIAN_POINT('Ctrl Pts',(7.17727988634051,-1.7274416000197,16.1762667371265));
#8628=CARTESIAN_POINT('Ctrl Pts',(7.09519107377515,-1.854342550025,16.1853354552417));
#8629=CARTESIAN_POINT('Ctrl Pts',(7.0220227803968,-1.95432323047479,16.1925372813961));
#8630=CARTESIAN_POINT('Ctrl Pts',(6.84826378034748,-2.16512110206393,16.208126209407));
#8631=CARTESIAN_POINT('Ctrl Pts',(6.74534957900526,-2.27364446777784,16.2164290720521));
#8632=CARTESIAN_POINT('Ctrl Pts',(6.51061621612745,-2.48902010157701,16.2342667571056));
#8633=CARTESIAN_POINT('Ctrl Pts',(6.37715500206396,-2.59339412895388,16.2437929356195));
#8634=CARTESIAN_POINT('Ctrl Pts',(6.21368521430928,-2.70167254249933,16.2555472990377));
#8635=CARTESIAN_POINT('Ctrl Pts',(6.19104605459125,-2.71626318314095,16.2571771699683));
#8636=CARTESIAN_POINT('Ctrl Pts',(6.15948311670992,-2.73604958968973,16.2594561077038));
#8637=CARTESIAN_POINT('Ctrl Pts',(6.15071255162724,-2.74148923363464,16.2600900652648));
#8638=CARTESIAN_POINT('Ctrl Pts',(6.13560723047503,-2.75075762466987,16.2611833786475));
#8639=CARTESIAN_POINT('Ctrl Pts',(6.12928506965769,-2.75460688663026,16.2616414099417));
#8640=CARTESIAN_POINT('Ctrl Pts',(6.11602457029854,-2.76261808558821,16.2626031493102));
#8641=CARTESIAN_POINT('Ctrl Pts',(6.10908377317528,-2.76677570154484,16.2631071419028));
#8642=CARTESIAN_POINT('Ctrl Pts',(6.09203882948686,-2.77689879638773,16.2643461597925));
#8643=CARTESIAN_POINT('Ctrl Pts',(6.08191767322952,-2.78283527918043,16.2650830179291));
#8644=CARTESIAN_POINT('Ctrl Pts',(6.04500058880823,-2.80421859373254,16.2677742105272));
#8645=CARTESIAN_POINT('Ctrl Pts',(6.01801601511951,-2.81933419085409,16.2697479807669));
#8646=CARTESIAN_POINT('Ctrl Pts',(5.94967408228979,-2.85633429467298,16.2747554829605));
#8647=CARTESIAN_POINT('Ctrl Pts',(5.90805069298341,-2.87771040174079,16.2778130769657));
#8648=CARTESIAN_POINT('Ctrl Pts',(5.5650595794132,-3.04452223994572,16.3029879822869));
#8649=CARTESIAN_POINT('Ctrl Pts',(5.24315974360506,-3.14313291685941,16.3262020408946));
#8650=CARTESIAN_POINT('Ctrl Pts',(4.84721290872578,-3.19963914254381,16.3519556504451));
#8651=CARTESIAN_POINT('Ctrl Pts',(4.78237768933826,-3.20689194468982,16.3560975010557));
#8652=CARTESIAN_POINT('Ctrl Pts',(4.69442392759861,-3.21403558476308,16.3616180247218));
#8653=CARTESIAN_POINT('Ctrl Pts',(4.67146504238629,-3.21565297081346,16.3630501076816));
#8654=CARTESIAN_POINT('Ctrl Pts',(4.63356461364472,-3.21791521236215,16.3653998703246));
#8655=CARTESIAN_POINT('Ctrl Pts',(4.61863269892055,-3.2187022406429,16.3663219661153));
#8656=CARTESIAN_POINT('Ctrl Pts',(4.58948111051868,-3.22003537942379,16.3681152252426));
#8657=CARTESIAN_POINT('Ctrl Pts',(4.57526225164126,-3.22059128683993,16.3689866745974));
#8658=CARTESIAN_POINT('Ctrl Pts',(4.54166707317465,-3.22168194808148,16.3710382793572));
#8659=CARTESIAN_POINT('Ctrl Pts',(4.52228855360779,-3.2221361072898,16.3722158932403));
#8660=CARTESIAN_POINT('Ctrl Pts',(4.45759824733044,-3.2230683482113,16.3761286368861));
#8661=CARTESIAN_POINT('Ctrl Pts',(4.41227941174319,-3.22276564906168,16.3788394633201));
#8662=CARTESIAN_POINT('Ctrl Pts',(4.30388834749897,-3.21975470141702,16.385261517645));
#8663=CARTESIAN_POINT('Ctrl Pts',(4.24085903161981,-3.21614897381777,16.3889458313074));
#8664=CARTESIAN_POINT('Ctrl Pts',(3.85027391676939,-3.18226960371922,16.4115671507917));
#8665=CARTESIAN_POINT('Ctrl Pts',(3.52891645917528,-3.10385270046426,16.4290497005579));
#8666=CARTESIAN_POINT('Ctrl Pts',(3.18435944694149,-2.9613833180992,16.4510698935684));
#8667=CARTESIAN_POINT('Ctrl Pts',(3.14404313847831,-2.94373772429456,16.4537045261762));
#8668=CARTESIAN_POINT('Ctrl Pts',(3.09148671883608,-2.91944067165926,16.4572321280126));
#8669=CARTESIAN_POINT('Ctrl Pts',(3.07890851981518,-2.91352665473817,16.4580835067525));
#8670=CARTESIAN_POINT('Ctrl Pts',(3.05864991386217,-2.90384095236538,16.4594669192179));
#8671=CARTESIAN_POINT('Ctrl Pts',(3.05094542771825,-2.90011964517514,16.459995904293));
#8672=CARTESIAN_POINT('Ctrl Pts',(3.03605578319789,-2.89285460039557,16.4610239479468));
#8673=CARTESIAN_POINT('Ctrl Pts',(3.02886891249811,-2.88931469879349,16.46152277358));
#8674=CARTESIAN_POINT('Ctrl Pts',(3.01156531959131,-2.88071147408355,16.4627299793861));
#8675=CARTESIAN_POINT('Ctrl Pts',(3.00146196346637,-2.87562162932976,16.4634399820211));
#8676=CARTESIAN_POINT('Ctrl Pts',(2.96627685460063,-2.85766326082043,16.4659299885911));
#8677=CARTESIAN_POINT('Ctrl Pts',(2.94133812734378,-2.84451933548115,16.4677259100044));
#8678=CARTESIAN_POINT('Ctrl Pts',(2.88028716338874,-2.81131188963385,16.4721935582341));
#8679=CARTESIAN_POINT('Ctrl Pts',(2.84438281915184,-2.79087827402263,16.4748834102314));
#8680=CARTESIAN_POINT('Ctrl Pts',(2.69593574253986,-2.70257486529262,16.4862385244467));
#8681=CARTESIAN_POINT('Ctrl Pts',(2.58721013952809,-2.62854631929875,16.4951225665968));
#8682=CARTESIAN_POINT('Ctrl Pts',(2.40432756615846,-2.48692833352997,16.5107710290758));
#8683=CARTESIAN_POINT('Ctrl Pts',(2.32822561469016,-2.42212268483333,16.5175260758181));
#8684=CARTESIAN_POINT('Ctrl Pts',(2.13566062501915,-2.24204728690098,16.5351478272682));
#8685=CARTESIAN_POINT('Ctrl Pts',(2.02474934220106,-2.12124522009336,16.5458466548834));
#8686=CARTESIAN_POINT('Ctrl Pts',(1.90669806434585,-1.97117292032354,16.5578663316139));
#8687=CARTESIAN_POINT('Ctrl Pts',(1.89017807050392,-1.94961674190697,16.5595651932827));
#8688=CARTESIAN_POINT('Ctrl Pts',(1.86350165986471,-1.91388124257981,16.5623372368716));
#8689=CARTESIAN_POINT('Ctrl Pts',(1.85318462124812,-1.89982407027428,16.5634166554299));
#8690=CARTESIAN_POINT('Ctrl Pts',(1.83481014416316,-1.87435773124241,16.5653526918951));
#8691=CARTESIAN_POINT('Ctrl Pts',(1.82671188677445,-1.86297868869068,16.5662108720084));
#8692=CARTESIAN_POINT('Ctrl Pts',(1.80956361804907,-1.83854864281835,16.5680388454591));
#8693=CARTESIAN_POINT('Ctrl Pts',(1.80053556451908,-1.82548262426834,16.5690077857424));
#8694=CARTESIAN_POINT('Ctrl Pts',(1.77626545503593,-1.78979605603409,16.57163101249));
#8695=CARTESIAN_POINT('Ctrl Pts',(1.7612131813262,-1.7670475666259,16.573278139314));
#8696=CARTESIAN_POINT('Ctrl Pts',(1.68016425333615,-1.64111283404236,16.5822649008892));
#8697=CARTESIAN_POINT('Ctrl Pts',(1.61979865577896,-1.53441377099373,16.589394103827));
#8698=CARTESIAN_POINT('Ctrl Pts',(1.49644110327114,-1.28408189946112,16.6053266455819));
#8699=CARTESIAN_POINT('Ctrl Pts',(1.43755833075741,-1.13877639725991,16.614018535334));
#8700=CARTESIAN_POINT('Ctrl Pts',(1.38684647765155,-0.981635108186533,16.6232699458685));
#8701=CARTESIAN_POINT('Ctrl Pts',(1.38425471873931,-0.973493361195649,16.623748903725));
#8702=CARTESIAN_POINT('Ctrl Pts',(1.36000183104895,-0.896243861082445,16.6282904877374));
#8703=CARTESIAN_POINT('Ctrl Pts',(1.34064433330498,-0.826436890287925,16.6323728992154));
#8704=CARTESIAN_POINT('Ctrl Pts',(1.31760300182023,-0.730960160716594,16.6379944089174));
#8705=CARTESIAN_POINT('Ctrl Pts',(1.31185206768902,-0.705809327432867,16.6394788068208));
#8706=CARTESIAN_POINT('Ctrl Pts',(1.29089341995096,-0.608804009030981,16.6452267605403));
#8707=CARTESIAN_POINT('Ctrl Pts',(1.27784283678885,-0.536511894026225,16.6495579506666));
#8708=CARTESIAN_POINT('Ctrl Pts',(1.26492277517286,-0.44767890112563,16.6550065264959));
#8709=CARTESIAN_POINT('Ctrl Pts',(1.26269475730998,-0.431497119722543,16.6560041328377));
#8710=CARTESIAN_POINT('Ctrl Pts',(1.25940556124783,-0.406185571052742,16.6575735223661));
#8711=CARTESIAN_POINT('Ctrl Pts',(1.25826023038957,-0.397066758091685,16.6581407233909));
#8712=CARTESIAN_POINT('Ctrl Pts',(1.25621033275057,-0.380161533656425,16.6591958037145));
#8713=CARTESIAN_POINT('Ctrl Pts',(1.25529515518352,-0.372376609991201,16.6596830853476));
#8714=CARTESIAN_POINT('Ctrl Pts',(1.25326895626629,-0.354581169288587,16.6608001527638));
#8715=CARTESIAN_POINT('Ctrl Pts',(1.25217646003025,-0.344568770241947,16.6614309491695));
#8716=CARTESIAN_POINT('Ctrl Pts',(1.2489392959599,-0.313553505739142,16.6633917042396));
#8717=CARTESIAN_POINT('Ctrl Pts',(1.24695411542745,-0.292535046970126,16.6647300387172));
#8718=CARTESIAN_POINT('Ctrl Pts',(1.24279173168614,-0.243302368684655,16.6678849016947));
#8719=CARTESIAN_POINT('Ctrl Pts',(1.24077938528471,-0.215076297795103,16.6697089915932));
#8720=CARTESIAN_POINT('Ctrl Pts',(1.23496653061059,-0.114974445106646,16.6762239787322));
#8721=CARTESIAN_POINT('Ctrl Pts',(1.23320255836729,-0.0430051241223538,
16.6809915057223));
#8722=CARTESIAN_POINT('Ctrl Pts',(1.23586096321087,0.252837590994247,16.7007863128731));
#8723=CARTESIAN_POINT('Ctrl Pts',(1.26119837873316,0.475922231887378,16.7161232468502));
#8724=CARTESIAN_POINT('Ctrl Pts',(1.33649777901908,0.817090503063733,16.73921193732));
#8725=CARTESIAN_POINT('Ctrl Pts',(1.3706708412395,0.937930545330958,16.7473271362832));
#8726=CARTESIAN_POINT('Ctrl Pts',(1.42104743404263,1.08310995181859,16.7569880328314));
#8727=CARTESIAN_POINT('Ctrl Pts',(1.4306358121081,1.10961473177599,16.7587483672855));
#8728=CARTESIAN_POINT('Ctrl Pts',(1.44629694242589,1.15119285542561,16.7615051098234));
#8729=CARTESIAN_POINT('Ctrl Pts',(1.45213792204609,1.16635140387094,16.7625091714518));
#8730=CARTESIAN_POINT('Ctrl Pts',(1.46320198621567,1.1944302817629,16.7643674101083));
#8731=CARTESIAN_POINT('Ctrl Pts',(1.46839471712496,1.20736208511777,16.7652225794241));
#8732=CARTESIAN_POINT('Ctrl Pts',(1.48009071404442,1.23595172653589,16.7671119407984));
#8733=CARTESIAN_POINT('Ctrl Pts',(1.48663401916398,1.25159281579153,16.7681447543351));
#8734=CARTESIAN_POINT('Ctrl Pts',(1.50601174020839,1.29690553630237,16.7711349302513));
#8735=CARTESIAN_POINT('Ctrl Pts',(1.51916978412621,1.32643712454552,16.7730812867879));
#8736=CARTESIAN_POINT('Ctrl Pts',(1.62094443247679,1.54591326767384,16.7875394114354));
#8737=CARTESIAN_POINT('Ctrl Pts',(1.72746040481548,1.72701327297481,16.7993848451652));
#8738=CARTESIAN_POINT('Ctrl Pts',(1.98489644326414,2.0807097893377,16.8238695613919));
#8739=CARTESIAN_POINT('Ctrl Pts',(2.13810542493385,2.2501521667208,16.8364299771638));
#8740=CARTESIAN_POINT('Ctrl Pts',(2.32610370919936,2.41831751652797,16.8515891434468));
#8741=CARTESIAN_POINT('Ctrl Pts',(2.34452634094959,2.43442272624639,16.8530726225572));
#8742=CARTESIAN_POINT('Ctrl Pts',(2.37067070633125,2.45675822220885,16.8551780374351));
#8743=CARTESIAN_POINT('Ctrl Pts',(2.37824105586183,2.46316546177386,16.8557876971535));
#8744=CARTESIAN_POINT('Ctrl Pts',(2.39198996927544,2.47469348651566,16.8568952167836));
#8745=CARTESIAN_POINT('Ctrl Pts',(2.39815837816735,2.47982638583456,16.8573922052445));
#8746=CARTESIAN_POINT('Ctrl Pts',(2.41080481654098,2.49027013514356,16.8584114864115));
#8747=CARTESIAN_POINT('Ctrl Pts',(2.4172844671751,2.49557883789633,16.8589339166768));
#8748=CARTESIAN_POINT('Ctrl Pts',(2.43393955250154,2.5091159826995,16.8602770538247));
#8749=CARTESIAN_POINT('Ctrl Pts',(2.44414442840857,2.51730772605329,16.8611003025124));
#8750=CARTESIAN_POINT('Ctrl Pts',(2.48673433922446,2.55107138848306,16.86453628635));
#8751=CARTESIAN_POINT('Ctrl Pts',(2.51955760066113,2.57608107967437,16.8671847029899));
#8752=CARTESIAN_POINT('Ctrl Pts',(2.60927894634575,2.64176013822776,16.8744051995576));
#8753=CARTESIAN_POINT('Ctrl Pts',(2.66703406841434,2.68121784923661,16.8790330463247));
#8754=CARTESIAN_POINT('Ctrl Pts',(2.90633382545134,2.83352803699428,16.8979958404373));
#8755=CARTESIAN_POINT('Ctrl Pts',(3.09763113592772,2.93008008421822,16.9126328085388));
#8756=CARTESIAN_POINT('Ctrl Pts',(3.42539847577577,3.05645630560851,16.9359402172646));
#8757=CARTESIAN_POINT('Ctrl Pts',(3.55676772965079,3.09767298171816,16.9448651093177));
#8758=CARTESIAN_POINT('Ctrl Pts',(3.71589013979323,3.13661438758767,16.9551692861969));
#8759=CARTESIAN_POINT('Ctrl Pts',(3.74147096200509,3.14254431015215,16.9568109132848));
#8760=CARTESIAN_POINT('Ctrl Pts',(3.78388719923026,3.15183211617565,16.9595089632226));
#8761=CARTESIAN_POINT('Ctrl Pts',(3.80068168535266,3.1553692314905,16.9605710683739));
#8762=CARTESIAN_POINT('Ctrl Pts',(3.83117310908494,3.16153712164049,16.9624884552676));
#8763=CARTESIAN_POINT('Ctrl Pts',(3.84486029919415,3.16421344608838,16.9633451698897));
#8764=CARTESIAN_POINT('Ctrl Pts',(3.87436357327933,3.1697837806709,16.9651834881935));
#8765=CARTESIAN_POINT('Ctrl Pts',(3.89018486237877,3.17264845791358,16.9661641390154));
#8766=CARTESIAN_POINT('Ctrl Pts',(3.93379659584765,3.18020837732226,16.9688535580683));
#8767=CARTESIAN_POINT('Ctrl Pts',(3.96162862690468,3.18465772928577,16.9705545290887));
#8768=CARTESIAN_POINT('Ctrl Pts',(4.12750874490642,3.20894888438156,16.9806069581989));
#8769=CARTESIAN_POINT('Ctrl Pts',(4.2666764764671,3.2201790951297,16.9886806596702));
#8770=CARTESIAN_POINT('Ctrl Pts',(4.60205663584287,3.22541645961004,17.0077236362952));
#8771=CARTESIAN_POINT('Ctrl Pts',(4.79782855491159,3.21060393429043,17.0184902924625));
#8772=CARTESIAN_POINT('Ctrl Pts',(4.99797654072554,3.17693826758358,17.0300083129923));
#8773=CARTESIAN_POINT('Ctrl Pts',(5.0049104941181,3.17574858906294,17.0304080232));
#8774=CARTESIAN_POINT('Ctrl Pts',(5.12233761275765,3.1552052232168,17.0371894357207));
#8775=CARTESIAN_POINT('Ctrl Pts',(5.23173856450615,3.13012023375716,17.0436904259202));
#8776=CARTESIAN_POINT('Ctrl Pts',(5.35551541183524,3.0948517389064,17.0514838283109));
#8777=CARTESIAN_POINT('Ctrl Pts',(5.37139867645919,3.09019342448474,17.0524923502591));
#8778=CARTESIAN_POINT('Ctrl Pts',(5.3969482886031,3.08248587878171,17.0541293637971));
#8779=CARTESIAN_POINT('Ctrl Pts',(5.40663759181386,3.079512969267,17.0547536072247));
#8780=CARTESIAN_POINT('Ctrl Pts',(5.42380067694891,3.07415821400138,17.055865717006));
#8781=CARTESIAN_POINT('Ctrl Pts',(5.43127999164253,3.07179472431323,17.0563525125577));
#8782=CARTESIAN_POINT('Ctrl Pts',(5.4474615219152,3.06661625300323,17.0574104523252));
#8783=CARTESIAN_POINT('Ctrl Pts',(5.45616026659733,3.06379157093752,17.0579821354754));
#8784=CARTESIAN_POINT('Ctrl Pts',(5.48059778168218,3.05574099670985,17.0595962881212));
#8785=CARTESIAN_POINT('Ctrl Pts',(5.49630814662072,3.05043067871627,17.0606434895841));
#8786=CARTESIAN_POINT('Ctrl Pts',(5.59415427940313,3.01651365814902,17.0672219763189));
#8787=CARTESIAN_POINT('Ctrl Pts',(5.67513792586523,2.98471534237057,17.0729150331263));
#8788=CARTESIAN_POINT('Ctrl Pts',(6.00657120860778,2.83883996430468,17.0969889751586));
#8789=CARTESIAN_POINT('Ctrl Pts',(6.24322709943132,2.696174500723,17.1159506978192));
#8790=CARTESIAN_POINT('Ctrl Pts',(6.53602593173005,2.46399209950647,17.1403930355583));
#8791=CARTESIAN_POINT('Ctrl Pts',(6.61034199618662,2.39930167728656,17.1467137827531));
#8792=CARTESIAN_POINT('Ctrl Pts',(6.70085850170048,2.31290804866073,17.1545678442539));
#8793=CARTESIAN_POINT('Ctrl Pts',(6.71990319911003,2.29427408470581,17.1562298506081));
#8794=CARTESIAN_POINT('Ctrl Pts',(6.74983050238031,2.26425681348666,17.1588575094436));
#8795=CARTESIAN_POINT('Ctrl Pts',(6.76086421660871,2.2530265422505,17.1598298297017));
#8796=CARTESIAN_POINT('Ctrl Pts',(6.78057078306631,2.23267270142353,17.1615730456373));
#8797=CARTESIAN_POINT('Ctrl Pts',(6.78927325487103,2.22357837890843,17.1623452243043));
#8798=CARTESIAN_POINT('Ctrl Pts',(6.80708943077453,2.20474026614787,17.1639311145326));
#8799=CARTESIAN_POINT('Ctrl Pts',(6.81619636841305,2.19499038900004,17.1647445276665));
#8800=CARTESIAN_POINT('Ctrl Pts',(6.84248303574186,2.16649523370265,17.1671007451851));
#8801=CARTESIAN_POINT('Ctrl Pts',(6.8595020469077,2.14760257305164,17.1686367461373));
#8802=CARTESIAN_POINT('Ctrl Pts',(6.94732801149363,2.04775637483486,17.1766224599676));
#8803=CARTESIAN_POINT('Ctrl Pts',(7.0142775468229,1.96349273402446,17.1829121363089));
#8804=CARTESIAN_POINT('Ctrl Pts',(7.16599305054544,1.75157787881706,17.1978739101318));
#8805=CARTESIAN_POINT('Ctrl Pts',(7.24611658206469,1.62093028059307,17.2064034615225));
#8806=CARTESIAN_POINT('Ctrl Pts',(7.40135874376193,1.3219424323807,17.2252468936189));
#8807=CARTESIAN_POINT('Ctrl Pts',(7.47194111602398,1.15187592294832,17.2355408039456));
#8808=CARTESIAN_POINT('Ctrl Pts',(7.53574442367407,0.95126042667185,17.2481630464968));
#8809=CARTESIAN_POINT('Ctrl Pts',(7.5435325092681,0.925673981602462,17.2497817417243));
#8810=CARTESIAN_POINT('Ctrl Pts',(7.55387580989565,0.890109683910482,17.2520476952803));
#8811=CARTESIAN_POINT('Ctrl Pts',(7.55670323230842,0.880211278117644,17.252680073126));
#8812=CARTESIAN_POINT('Ctrl Pts',(7.56148014415612,0.86317941506813,17.2537713855274));
#8813=CARTESIAN_POINT('Ctrl Pts',(7.56345261391421,0.856052409973881,17.2542290065089));
#8814=CARTESIAN_POINT('Ctrl Pts',(7.56753345450884,0.841107454072355,17.2551907445052));
#8815=CARTESIAN_POINT('Ctrl Pts',(7.56963690535174,0.833288292193715,17.255695151277));
#8816=CARTESIAN_POINT('Ctrl Pts',(7.57472458335335,0.814087701768747,17.2569366367466));
#8817=CARTESIAN_POINT('Ctrl Pts',(7.57767597202928,0.802697762290085,17.2576755646251));
#8818=CARTESIAN_POINT('Ctrl Pts',(7.58387513030834,0.778222902142665,17.2592682943036));
#8819=CARTESIAN_POINT('Ctrl Pts',(7.58710328473699,0.765133289675284,17.2601231166666));
#8820=CARTESIAN_POINT('Ctrl Pts',(7.59601060132286,0.728015367292673,17.262554857176));
#8821=CARTESIAN_POINT('Ctrl Pts',(7.60149577315092,0.703942014637659,17.2641411485596));
#8822=CARTESIAN_POINT('Ctrl Pts',(7.65470592180679,0.457366147888939,17.2804662012447));
#8823=CARTESIAN_POINT('Ctrl Pts',(7.67900893588414,0.230485891480088,17.2960755674744));
#8824=CARTESIAN_POINT('Ctrl Pts',(7.67921774902577,0.00295766498587945,
17.311387620665));
#8825=CARTESIAN_POINT('Ctrl Pts',(7.67921775054129,0.00295601317713016,
17.3113877318274));
#8826=CARTESIAN_POINT('Ctrl Pts',(7.67921865433409,0.00197066675129393,
17.3114540430529));
#8827=CARTESIAN_POINT('Ctrl Pts',(7.67921910621818,0.000985328982374648,
17.3115203483787));
#8828=CARTESIAN_POINT('Ctrl Pts',(7.67921910621823,1.77253683985415E-10,
17.3115866477388));
#8829=CARTESIAN_POINT('',(7.67921808440022,-0.00256634505910285,15.8124366820589));
#8830=CARTESIAN_POINT('Ctrl Pts',(7.67921904541626,-0.000626018462678653,
17.0671267777979));
#8831=CARTESIAN_POINT('Ctrl Pts',(7.67922641406151,0.0373078484470186,17.0646920170307));
#8832=CARTESIAN_POINT('Ctrl Pts',(7.67856402138696,0.075237246115982,17.0622278733309));
#8833=CARTESIAN_POINT('Ctrl Pts',(7.67323678195464,0.226882242818845,17.0522795707411));
#8834=CARTESIAN_POINT('Ctrl Pts',(7.66321943395884,0.340321869569866,17.0446232903118));
#8835=CARTESIAN_POINT('Ctrl Pts',(7.60856111414402,0.72532554062384,17.0183407329052));
#8836=CARTESIAN_POINT('Ctrl Pts',(7.53517991272287,0.991654912655422,16.9997719067977));
#8837=CARTESIAN_POINT('Ctrl Pts',(7.41426989485969,1.2802158947923,16.9799671985172));
#8838=CARTESIAN_POINT('Ctrl Pts',(7.39909439897466,1.31472233668693,16.9776016405544));
#8839=CARTESIAN_POINT('Ctrl Pts',(7.37577552032328,1.36531761791377,16.9741358388106));
#8840=CARTESIAN_POINT('Ctrl Pts',(7.3680973423903,1.38161614519426,16.9730197946706));
#8841=CARTESIAN_POINT('Ctrl Pts',(7.35419959433934,1.41048653855108,16.9710433609457));
#8842=CARTESIAN_POINT('Ctrl Pts',(7.34803392117042,1.42308368974656,16.9701811349579));
#8843=CARTESIAN_POINT('Ctrl Pts',(7.33486864043715,1.44954296880113,16.9683702607652));
#8844=CARTESIAN_POINT('Ctrl Pts',(7.32785066294614,1.46339559446265,16.9674222804288));
#8845=CARTESIAN_POINT('Ctrl Pts',(7.30896822931891,1.50000835669644,16.9649166483615));
#8846=CARTESIAN_POINT('Ctrl Pts',(7.2969313865771,1.52267869536871,16.9633650827658));
#8847=CARTESIAN_POINT('Ctrl Pts',(7.23708751791692,1.63220976509306,16.9558648204866));
#8848=CARTESIAN_POINT('Ctrl Pts',(7.18555782115261,1.71698137789989,16.9500501588548));
#8849=CARTESIAN_POINT('Ctrl Pts',(7.02031498388442,1.96253632921389,16.93299963691));
#8850=CARTESIAN_POINT('Ctrl Pts',(6.89570686350565,2.11541409271351,16.9221247996718));
#8851=CARTESIAN_POINT('Ctrl Pts',(6.64392977320399,2.37226752492125,16.901933322919));
#8852=CARTESIAN_POINT('Ctrl Pts',(6.52129668612906,2.4797399633072,16.892689240058));
#8853=CARTESIAN_POINT('Ctrl Pts',(6.37763035591441,2.58757419174573,16.8818159626182));
#8854=CARTESIAN_POINT('Ctrl Pts',(6.36409314120027,2.59757026060535,16.8807909451575));
#8855=CARTESIAN_POINT('Ctrl Pts',(6.34230079643208,2.61339980887416,16.8791390273104));
#8856=CARTESIAN_POINT('Ctrl Pts',(6.3340952266952,2.61930140879531,16.8785166120754));
#8857=CARTESIAN_POINT('Ctrl Pts',(6.31946177290653,2.62972196712906,16.8774056316543));
#8858=CARTESIAN_POINT('Ctrl Pts',(6.31304494880182,2.63425614543059,16.8769181170332));
#8859=CARTESIAN_POINT('Ctrl Pts',(6.29920189307179,2.64396205158955,16.8758655769903));
#8860=CARTESIAN_POINT('Ctrl Pts',(6.29177056694333,2.64912589310753,16.8753000640578));
#8861=CARTESIAN_POINT('Ctrl Pts',(6.27102449420952,2.66341262622154,16.8737202085112));
#8862=CARTESIAN_POINT('Ctrl Pts',(6.25766302559902,2.67246674687792,16.8727014409875));
#8863=CARTESIAN_POINT('Ctrl Pts',(6.17820650817433,2.72544226456296,16.8666383823714));
#8864=CARTESIAN_POINT('Ctrl Pts',(6.11058068254245,2.76700702524492,16.8614592249629));
#8865=CARTESIAN_POINT('Ctrl Pts',(5.85448428938577,2.91166684309748,16.8419645268294));
#8866=CARTESIAN_POINT('Ctrl Pts',(5.65738124971003,2.99834352835722,16.8272320737738));
#8867=CARTESIAN_POINT('Ctrl Pts',(5.30004442139763,3.11454768893864,16.8021344607464));
#8868=CARTESIAN_POINT('Ctrl Pts',(5.14344046603789,3.15279408585368,16.7916246017548));
#8869=CARTESIAN_POINT('Ctrl Pts',(4.95790383448904,3.18361646477717,16.7797858096471));
#8870=CARTESIAN_POINT('Ctrl Pts',(4.93114006569536,3.18771675868674,16.7780921921655));
#8871=CARTESIAN_POINT('Ctrl Pts',(4.8870857183136,3.19389887380402,16.7753269828155));
#8872=CARTESIAN_POINT('Ctrl Pts',(4.86982471785276,3.19617863081447,16.7742492054875));
#8873=CARTESIAN_POINT('Ctrl Pts',(4.8386889941141,3.20003444918757,16.7723150365975));
#8874=CARTESIAN_POINT('Ctrl Pts',(4.82482099829171,3.20166041485179,16.7714570945202));
#8875=CARTESIAN_POINT('Ctrl Pts',(4.79514333238217,3.20494461853492,16.769628484665));
#8876=CARTESIAN_POINT('Ctrl Pts',(4.77933103136297,3.20657612271916,16.7686586781367));
#8877=CARTESIAN_POINT('Ctrl Pts',(4.73628349514404,3.21069609002996,16.7660302544208));
#8878=CARTESIAN_POINT('Ctrl Pts',(4.70902723647941,3.21295501610915,16.764378847195));
#8879=CARTESIAN_POINT('Ctrl Pts',(4.5583050755029,3.22351658916916,16.7553128179693));
#8880=CARTESIAN_POINT('Ctrl Pts',(4.43446163323033,3.22505045876536,16.7481132726778));
#8881=CARTESIAN_POINT('Ctrl Pts',(4.16157060515671,3.21270524461674,16.7325247338358));
#8882=CARTESIAN_POINT('Ctrl Pts',(4.01296221363759,3.19558188573533,16.7242201881454));
#8883=CARTESIAN_POINT('Ctrl Pts',(3.69973414324459,3.13721224565233,16.7063796869382));
#8884=CARTESIAN_POINT('Ctrl Pts',(3.53611007594965,3.09316564909594,16.6968524006383));
#8885=CARTESIAN_POINT('Ctrl Pts',(3.35134576716687,3.02746516622017,16.6850968248043));
#8886=CARTESIAN_POINT('Ctrl Pts',(3.32608481046238,3.01812427901765,16.6834670082483));
#8887=CARTESIAN_POINT('Ctrl Pts',(3.29131125786159,3.00476808555454,16.6811881776379));
#8888=CARTESIAN_POINT('Ctrl Pts',(3.28169566036188,3.00102172663583,16.6805542721145));
#8889=CARTESIAN_POINT('Ctrl Pts',(3.26521517066546,2.99450937551738,16.6794610568537));
#8890=CARTESIAN_POINT('Ctrl Pts',(3.25834143881846,2.99176577108572,16.6790030714752));
#8891=CARTESIAN_POINT('Ctrl Pts',(3.24397417543344,2.98597371920525,16.6780414406995));
#8892=CARTESIAN_POINT('Ctrl Pts',(3.23648262181709,2.98292071328848,16.6775375109211));
#8893=CARTESIAN_POINT('Ctrl Pts',(3.21815508496292,2.97537116785434,16.6762986724637));
#8894=CARTESIAN_POINT('Ctrl Pts',(3.20733206849318,2.97084362643378,16.6755619316185));
#8895=CARTESIAN_POINT('Ctrl Pts',(3.16807305158767,2.95416813190016,16.6728713185009));
#8896=CARTESIAN_POINT('Ctrl Pts',(3.13978855706311,2.94167059891326,16.6708980196557));
#8897=CARTESIAN_POINT('Ctrl Pts',(3.06918152884888,2.90925052600755,16.665891882294));
#8898=CARTESIAN_POINT('Ctrl Pts',(3.02710560509746,2.88881030585627,16.6628351956092));
#8899=CARTESIAN_POINT('Ctrl Pts',(2.68805127607453,2.7148790933123,16.6376829799644));
#8900=CARTESIAN_POINT('Ctrl Pts',(2.41613355028699,2.51693835727205,16.6144918129322));
#8901=CARTESIAN_POINT('Ctrl Pts',(2.13312914806322,2.23439000998588,16.5887378609379));
#8902=CARTESIAN_POINT('Ctrl Pts',(2.08819818628284,2.18671011517095,16.5845781627209));
#8903=CARTESIAN_POINT('Ctrl Pts',(2.02945986120961,2.12044216232553,16.5790380798669));
#8904=CARTESIAN_POINT('Ctrl Pts',(2.01435605574204,2.10302941780383,16.5776037947891));
#8905=CARTESIAN_POINT('Ctrl Pts',(1.98976024570209,2.07405128203211,16.5752514422341));
#8906=CARTESIAN_POINT('Ctrl Pts',(1.98015984364921,2.06257939754902,16.5743289382351));
#8907=CARTESIAN_POINT('Ctrl Pts',(1.96158721152768,2.04006965747755,16.5725356103906));
#8908=CARTESIAN_POINT('Ctrl Pts',(1.95260751073425,2.02903844140608,16.5716644953924));
#8909=CARTESIAN_POINT('Ctrl Pts',(1.93158060697397,2.00285554035508,16.5696148065946));
#8910=CARTESIAN_POINT('Ctrl Pts',(1.91959621498516,1.98765394577629,16.5684387618598));
#8911=CARTESIAN_POINT('Ctrl Pts',(1.88010806687893,1.93662624876962,16.5645364598637));
#8912=CARTESIAN_POINT('Ctrl Pts',(1.85321979075694,1.90032911275274,16.5618343266463));
#8913=CARTESIAN_POINT('Ctrl Pts',(1.79076293463419,1.81220248180522,16.5554364330263));
#8914=CARTESIAN_POINT('Ctrl Pts',(1.75592973124965,1.75987357654044,16.5517673084653));
#8915=CARTESIAN_POINT('Ctrl Pts',(1.53979864105369,1.41364205541139,16.5282127079555));
#8916=CARTESIAN_POINT('Ctrl Pts',(1.40524808344095,1.0933087138168,16.5099635909658));
#8917=CARTESIAN_POINT('Ctrl Pts',(1.31662246469314,0.726970786267712,16.4874714180596));
#8918=CARTESIAN_POINT('Ctrl Pts',(1.30962058478797,0.696037116993631,16.4855583468564));
#8919=CARTESIAN_POINT('Ctrl Pts',(1.30055572149833,0.653052466898911,16.4828745708855));
#8920=CARTESIAN_POINT('Ctrl Pts',(1.29810282509281,0.641084424641773,16.4821246228284));
#8921=CARTESIAN_POINT('Ctrl Pts',(1.29427852376111,0.621870297003964,16.4809158472514));
#8922=CARTESIAN_POINT('Ctrl Pts',(1.29286381304861,0.614632811139181,16.4804594489211));
#8923=CARTESIAN_POINT('Ctrl Pts',(1.28994446143114,0.599420634049377,16.4794977705213));
#8924=CARTESIAN_POINT('Ctrl Pts',(1.28844509031062,0.591445054350981,16.4789921854979));
#8925=CARTESIAN_POINT('Ctrl Pts',(1.28482857373238,0.57179941378067,16.4777435425726));
#8926=CARTESIAN_POINT('Ctrl Pts',(1.28274571153156,0.560123236981401,16.4769985875384));
#8927=CARTESIAN_POINT('Ctrl Pts',(1.27531578931681,0.517099963512778,16.4742438794933));
#8928=CARTESIAN_POINT('Ctrl Pts',(1.27036852724751,0.485686854722369,16.4722135024611));
#8929=CARTESIAN_POINT('Ctrl Pts',(1.25903963461298,0.406106944184073,16.4670304563079));
#8930=CARTESIAN_POINT('Ctrl Pts',(1.25328109350122,0.357860505628887,16.4638518828767));
#8931=CARTESIAN_POINT('Ctrl Pts',(1.23158769793012,0.133020067484351,16.4489239582926));
#8932=CARTESIAN_POINT('Ctrl Pts',(1.22915353331832,-0.0445635137069391,
16.4368243235861));
#8933=CARTESIAN_POINT('Ctrl Pts',(1.25543118670765,-0.42609201261151,16.4110572820287));
#8934=CARTESIAN_POINT('Ctrl Pts',(1.28903556867776,-0.628959367318881,16.3975156666417));
#8935=CARTESIAN_POINT('Ctrl Pts',(1.3487584313166,-0.853818267286595,16.3828661723043));
#8936=CARTESIAN_POINT('Ctrl Pts',(1.35614478696317,-0.880261587718025,16.3811483898693));
#8937=CARTESIAN_POINT('Ctrl Pts',(1.36879846741136,-0.923425538789335,16.3783519896799));
#8938=CARTESIAN_POINT('Ctrl Pts',(1.37386577871841,-0.940202873933742,16.3772669467542));
#8939=CARTESIAN_POINT('Ctrl Pts',(1.38321870183408,-0.970280757814361,16.3753248618623));
#8940=CARTESIAN_POINT('Ctrl Pts',(1.38745440601782,-0.983596246811233,16.3744662151625));
#8941=CARTESIAN_POINT('Ctrl Pts',(1.39666986875715,-1.01192708686171,16.3726415082342));
#8942=CARTESIAN_POINT('Ctrl Pts',(1.40167386871266,-1.02693421092204,16.3716762697239));
#8943=CARTESIAN_POINT('Ctrl Pts',(1.41551567054076,-1.06744953137409,16.3690735943346));
#8944=CARTESIAN_POINT('Ctrl Pts',(1.42456392449426,-1.09288486874238,16.3674431251106));
#8945=CARTESIAN_POINT('Ctrl Pts',(1.47484581757222,-1.2287982856096,16.3587450092682));
#8946=CARTESIAN_POINT('Ctrl Pts',(1.52180227840496,-1.33707056967685,16.3518714117494));
#8947=CARTESIAN_POINT('Ctrl Pts',(1.64318873995305,-1.57957478895859,16.3363637561783));
#8948=CARTESIAN_POINT('Ctrl Pts',(1.72147424354537,-1.7115514171787,16.3278430505824));
#8949=CARTESIAN_POINT('Ctrl Pts',(1.83584925075604,-1.87635576206542,16.3166133813224));
#8950=CARTESIAN_POINT('Ctrl Pts',(1.86369827092408,-1.91465366338749,16.3139577287342));
#8951=CARTESIAN_POINT('Ctrl Pts',(1.97571474945083,-2.06177076008277,16.3035219680895));
#8952=CARTESIAN_POINT('Ctrl Pts',(2.06596138160749,-2.16575724238562,16.2956334840394));
#8953=CARTESIAN_POINT('Ctrl Pts',(2.17556917385983,-2.27683026385919,16.2861887481779));
#8954=CARTESIAN_POINT('Ctrl Pts',(2.18869057571657,-2.2898997907435,16.2850600790611));
#8955=CARTESIAN_POINT('Ctrl Pts',(2.2088364926239,-2.30962308412409,16.2833287797662));
#8956=CARTESIAN_POINT('Ctrl Pts',(2.21577978402201,-2.31635975447106,16.2827323718179));
#8957=CARTESIAN_POINT('Ctrl Pts',(2.22838840867981,-2.32848342987639,16.2816496051689));
#8958=CARTESIAN_POINT('Ctrl Pts',(2.2340431208246,-2.33388119117334,16.2811640912687));
#8959=CARTESIAN_POINT('Ctrl Pts',(2.24662453340216,-2.34580371626504,16.2800840115047));
#8960=CARTESIAN_POINT('Ctrl Pts',(2.25356043847634,-2.35231832611619,16.2794887136877));
#8961=CARTESIAN_POINT('Ctrl Pts',(2.2739446666903,-2.37129517350995,16.2777398226892));
#8962=CARTESIAN_POINT('Ctrl Pts',(2.2874703543471,-2.38367323829133,16.2765801975406));
#8963=CARTESIAN_POINT('Ctrl Pts',(2.41116174664401,-2.49494526825097,16.2659889793383));
#8964=CARTESIAN_POINT('Ctrl Pts',(2.52790257640491,-2.58624346523975,16.2560963959517));
#8965=CARTESIAN_POINT('Ctrl Pts',(2.84934969901315,-2.80373582047553,16.2299067850006));
#8966=CARTESIAN_POINT('Ctrl Pts',(3.06265755433671,-2.91566243922233,16.2135905008431));
#8967=CARTESIAN_POINT('Ctrl Pts',(3.35563057078021,-3.02981624967571,16.1932506727074));
#8968=CARTESIAN_POINT('Ctrl Pts',(3.42573815898686,-3.0543783574797,16.1885202448652));
#8969=CARTESIAN_POINT('Ctrl Pts',(3.51968190060118,-3.08368773874728,16.1823570932969));
#8970=CARTESIAN_POINT('Ctrl Pts',(3.54280766752579,-3.09061857321385,16.1808537023805));
#8971=CARTESIAN_POINT('Ctrl Pts',(3.58061305738885,-3.10148748678316,16.1784178519824));
#8972=CARTESIAN_POINT('Ctrl Pts',(3.59524617456329,-3.10558263833907,16.1774803146664));
#8973=CARTESIAN_POINT('Ctrl Pts',(3.62353336297406,-3.11328363999004,16.1756779682489));
#8974=CARTESIAN_POINT('Ctrl Pts',(3.6371832167726,-3.11690353023258,16.1748127221981));
#8975=CARTESIAN_POINT('Ctrl Pts',(3.66898453856791,-3.12511378101737,16.1728070366949));
#8976=CARTESIAN_POINT('Ctrl Pts',(3.68715320815639,-3.12963594695978,16.1716688173208));
#8977=CARTESIAN_POINT('Ctrl Pts',(3.74573563746546,-3.14367607750028,16.1680225862752));
#8978=CARTESIAN_POINT('Ctrl Pts',(3.78629524026609,-3.15257173912639,16.1655344785044));
#8979=CARTESIAN_POINT('Ctrl Pts',(3.88223293692778,-3.17167780810815,16.1597265159112));
#8980=CARTESIAN_POINT('Ctrl Pts',(3.93772972516147,-3.18122574904888,16.1564269864891));
#8981=CARTESIAN_POINT('Ctrl Pts',(4.14760198313647,-3.2116945939568,16.1441327759674));
#8982=CARTESIAN_POINT('Ctrl Pts',(4.30318056163093,-3.22286958099581,16.1354020817183));
#8983=CARTESIAN_POINT('Ctrl Pts',(4.66805769108854,-3.22258723559974,16.1149984210397));
#8984=CARTESIAN_POINT('Ctrl Pts',(4.87661252494764,-3.20207650358121,16.1033947757592));
#8985=CARTESIAN_POINT('Ctrl Pts',(5.10688501374531,-3.15653875206495,16.0893056471989));
#8986=CARTESIAN_POINT('Ctrl Pts',(5.13202950220742,-3.15125305290691,16.0877493940194));
#8987=CARTESIAN_POINT('Ctrl Pts',(5.16699051503377,-3.14346614676949,16.0855573089383));
#8988=CARTESIAN_POINT('Ctrl Pts',(5.17686324906427,-3.14121829245557,16.084935122761));
#8989=CARTESIAN_POINT('Ctrl Pts',(5.19388465584204,-3.1372583418769,16.0838567097469));
#8990=CARTESIAN_POINT('Ctrl Pts',(5.20103843492549,-3.13556822740279,16.0834017264841));
#8991=CARTESIAN_POINT('Ctrl Pts',(5.21610198429949,-3.13195493526759,16.0824398750062));
#8992=CARTESIAN_POINT('Ctrl Pts',(5.22401031822904,-3.13002624736643,16.0819326827216));
#8993=CARTESIAN_POINT('Ctrl Pts',(5.24354246690118,-3.12518426487896,16.0806746544945));
#8994=CARTESIAN_POINT('Ctrl Pts',(5.25515742218511,-3.12223607817374,16.0799218590965));
#8995=CARTESIAN_POINT('Ctrl Pts',(5.29836265679485,-3.11101257513069,16.077104784977));
#8996=CARTESIAN_POINT('Ctrl Pts',(5.32984184554701,-3.10232233328631,16.0750186812156));
#8997=CARTESIAN_POINT('Ctrl Pts',(5.56138182832711,-3.03459951166415,16.0594527609299));
#8998=CARTESIAN_POINT('Ctrl Pts',(5.75540933622093,-2.9567498010121,16.0452124171109));
#8999=CARTESIAN_POINT('Ctrl Pts',(6.12115497022625,-2.76700914860504,16.0173949068354));
#9000=CARTESIAN_POINT('Ctrl Pts',(6.29251561768555,-2.6564029695707,16.0038770104438));
#9001=CARTESIAN_POINT('Ctrl Pts',(6.48516421461196,-2.50444874309693,15.9883020570688));
#9002=CARTESIAN_POINT('Ctrl Pts',(6.5175012381913,-2.47790519690094,15.9856717093837));
#9003=CARTESIAN_POINT('Ctrl Pts',(6.56343901095801,-2.43867595575881,15.9819099321802));
#9004=CARTESIAN_POINT('Ctrl Pts',(6.57746011071931,-2.42649124842,15.9807582653019));
#9005=CARTESIAN_POINT('Ctrl Pts',(6.60197444646242,-2.40481279769704,15.9787382092371));
#9006=CARTESIAN_POINT('Ctrl Pts',(6.61251186465673,-2.3953699904015,15.9778677379683));
#9007=CARTESIAN_POINT('Ctrl Pts',(6.62701260150798,-2.38220235652645,15.9766667455594));
#9008=CARTESIAN_POINT('Ctrl Pts',(6.63102907483247,-2.37853654078653,15.9763337546958));
#9009=CARTESIAN_POINT('Ctrl Pts',(6.63516905759745,-2.37473874706899,15.9759901715923));
#9010=CARTESIAN_POINT('Ctrl Pts',(6.63530183483533,-2.37461692398534,15.9759791518434));
#9011=CARTESIAN_POINT('Ctrl Pts',(6.6355505740188,-2.37438866741806,15.9759585072144));
#9012=CARTESIAN_POINT('Ctrl Pts',(6.63566653838777,-2.3742822365719,15.9759488822222));
#9013=CARTESIAN_POINT('Ctrl Pts',(6.63601831946668,-2.37395932821101,15.975919683675));
#9014=CARTESIAN_POINT('Ctrl Pts',(6.63625411176207,-2.37374282401828,15.9759001112467));
#9015=CARTESIAN_POINT('Ctrl Pts',(6.6367195680249,-2.37331531482025,15.975861472739));
#9016=CARTESIAN_POINT('Ctrl Pts',(6.63694923362345,-2.37310431160528,15.9758424065845));
#9017=CARTESIAN_POINT('Ctrl Pts',(6.63740284295748,-2.37268744064295,15.9758047470573));
#9018=CARTESIAN_POINT('Ctrl Pts',(6.63762678818554,-2.37248157451798,15.9757861536155));
#9019=CARTESIAN_POINT('Ctrl Pts',(6.63806933446912,-2.37207463938442,15.9757494083159));
#9020=CARTESIAN_POINT('Ctrl Pts',(6.63828793686706,-2.37187357187125,15.9757312563967));
#9021=CARTESIAN_POINT('Ctrl Pts',(6.63872014902901,-2.37147591868992,15.9756953650982));
#9022=CARTESIAN_POINT('Ctrl Pts',(6.63893376004545,-2.3712793343615,15.9756776256607));
#9023=CARTESIAN_POINT('Ctrl Pts',(6.65118788630558,-2.35999891192853,15.9746599190801));
#9024=CARTESIAN_POINT('Ctrl Pts',(6.66314399515584,-2.34882339435336,15.9736638447136));
#9025=CARTESIAN_POINT('Ctrl Pts',(6.69956824020663,-2.31425360994013,15.9706191685637));
#9026=CARTESIAN_POINT('Ctrl Pts',(6.72375381992902,-2.29056404702819,15.9685833007541));
#9027=CARTESIAN_POINT('Ctrl Pts',(6.7784411270563,-2.23528327040371,15.9639427127593));
#9028=CARTESIAN_POINT('Ctrl Pts',(6.80867974004409,-2.20344066359967,15.9613491415253));
#9029=CARTESIAN_POINT('Ctrl Pts',(6.90884871479582,-2.0935453657806,15.9526457062803));
#9030=CARTESIAN_POINT('Ctrl Pts',(6.97562262876506,-2.01270115083615,15.9466538201267));
#9031=CARTESIAN_POINT('Ctrl Pts',(7.09678512877229,-1.85050934541222,15.9352175767197));
#9032=CARTESIAN_POINT('Ctrl Pts',(7.15164262398297,-1.76965921483505,15.929769300325));
#9033=CARTESIAN_POINT('Ctrl Pts',(7.29928061992343,-1.52923912603593,15.9139890834805));
#9034=CARTESIAN_POINT('Ctrl Pts',(7.38212834925727,-1.36405654697205,15.9036608613047));
#9035=CARTESIAN_POINT('Ctrl Pts',(7.46028614308617,-1.16786834777868,15.8909987464818));
#9036=CARTESIAN_POINT('Ctrl Pts',(7.46987694698813,-1.14289384828441,15.8893796186732));
#9037=CARTESIAN_POINT('Ctrl Pts',(7.48272608057905,-1.10814812602912,15.8871132042093));
#9038=CARTESIAN_POINT('Ctrl Pts',(7.48625044451607,-1.09847557074047,15.88648080724));
#9039=CARTESIAN_POINT('Ctrl Pts',(7.49222655331929,-1.08182667940829,15.8853895028788));
#9040=CARTESIAN_POINT('Ctrl Pts',(7.49470076718004,-1.0748584156261,15.8849319093865));
#9041=CARTESIAN_POINT('Ctrl Pts',(7.49983361350887,-1.0602431717831,15.8839702802484));
#9042=CARTESIAN_POINT('Ctrl Pts',(7.50248743093015,-1.0525946361421,15.8834659552202));
#9043=CARTESIAN_POINT('Ctrl Pts',(7.50892633163067,-1.03380888742789,15.8822247615977));
#9044=CARTESIAN_POINT('Ctrl Pts',(7.5126792901654,-1.02266085784129,15.8814860452424));
#9045=CARTESIAN_POINT('Ctrl Pts',(7.52614200752061,-0.98193432200351,15.8787801314));
#9046=CARTESIAN_POINT('Ctrl Pts',(7.5354837229138,-0.952237132554293,15.8767932248743));
#9047=CARTESIAN_POINT('Ctrl Pts',(7.55790404277916,-0.877181349564938,15.8717450753413));
#9048=CARTESIAN_POINT('Ctrl Pts',(7.57041869710981,-0.831662958558692,15.8686595037599));
#9049=CARTESIAN_POINT('Ctrl Pts',(7.64633250482876,-0.529755630087821,15.8481056545554));
#9050=CARTESIAN_POINT('Ctrl Pts',(7.67900776168187,-0.266684111778894,15.8298838378527));
#9051=CARTESIAN_POINT('Ctrl Pts',(7.67921808440022,-0.00256634505910285,
15.8124366820589));
#9052=CARTESIAN_POINT('Ctrl Pts',(7.67921808747992,-0.00256247473102081,
15.8124364263919));
#9053=CARTESIAN_POINT('Ctrl Pts',(7.67921876664087,-0.0017083140070543,
15.8123800020577));
#9054=CARTESIAN_POINT('Ctrl Pts',(7.67921910621822,-0.000854155705641013,
15.8123235855046));
#9055=CARTESIAN_POINT('Ctrl Pts',(7.67921910621823,-2.74841093364834E-11,
15.8122671767608));
#9056=CARTESIAN_POINT('Origin',(4.45646910621825,-5.13094777615093E-16,
-2.31077344927308));
#9057=CARTESIAN_POINT('',(7.67921910621823,-1.84544675223763E-11,14.5621759541225));
#9058=CARTESIAN_POINT('',(7.67921910621823,2.3786865083016E-11,14.8122635502411));
#9059=CARTESIAN_POINT('',(7.67921910621823,-3.51191647465084E-13,-2.31077344927308));
#9060=CARTESIAN_POINT('',(7.67921816783712,-0.00245933620175732,14.8124033118825));
#9061=CARTESIAN_POINT('Ctrl Pts',(7.67921910621823,2.3786865083016E-11,
14.8122635502411));
#9062=CARTESIAN_POINT('Ctrl Pts',(7.67921910621823,-0.000819775054184794,
14.8123101427297));
#9063=CARTESIAN_POINT('Ctrl Pts',(7.67921879342738,-0.00163955385536296,
14.8123567299308));
#9064=CARTESIAN_POINT('Ctrl Pts',(7.67921816783712,-0.00245933620180352,
14.8124033118825));
#9065=CARTESIAN_POINT('Ctrl Pts',(7.67921817065546,-0.00245564023983482,
14.8124031018693));
#9066=CARTESIAN_POINT('Ctrl Pts',(7.67916398677161,-0.0735658371379256,
14.8164437511175));
#9067=CARTESIAN_POINT('Ctrl Pts',(7.67675624121047,-0.144657283957908,14.8204417577807));
#9068=CARTESIAN_POINT('Ctrl Pts',(7.65693647847182,-0.440237452401183,14.8370364533687));
#9069=CARTESIAN_POINT('Ctrl Pts',(7.61838122542217,-0.662635818713972,14.8494220805179));
#9070=CARTESIAN_POINT('Ctrl Pts',(7.54779577275092,-0.911565043813883,14.8648442997905));
#9071=CARTESIAN_POINT('Ctrl Pts',(7.53810318523207,-0.943812792510002,14.8668740737785));
#9072=CARTESIAN_POINT('Ctrl Pts',(7.52423546229692,-0.98745845462968,14.8696722761627));
#9073=CARTESIAN_POINT('Ctrl Pts',(7.52049821901749,-0.998994594656731,14.8704167681455));
#9074=CARTESIAN_POINT('Ctrl Pts',(7.51413420502902,-1.01826738091487,14.8716691762343));
#9075=CARTESIAN_POINT('Ctrl Pts',(7.51154291478027,-1.02601575870491,14.8721750353399));
#9076=CARTESIAN_POINT('Ctrl Pts',(7.50657224872985,-1.04069306414792,14.873137854759));
#9077=CARTESIAN_POINT('Ctrl Pts',(7.504198657536,-1.04762388919386,14.8735944597521));
#9078=CARTESIAN_POINT('Ctrl Pts',(7.49852091192929,-1.0640201532557,14.8746791691481));
#9079=CARTESIAN_POINT('Ctrl Pts',(7.49519620189542,-1.07347832158151,14.8753084595267));
#9080=CARTESIAN_POINT('Ctrl Pts',(7.48339423735058,-1.10655848395182,14.8775215847288));
#9081=CARTESIAN_POINT('Ctrl Pts',(7.47468547390956,-1.13009614451067,14.8791180971225));
#9082=CARTESIAN_POINT('Ctrl Pts',(7.38664412992046,-1.35977137215666,14.8948945341084));
#9083=CARTESIAN_POINT('Ctrl Pts',(7.2865986428985,-1.55732365816941,14.9099930932462));
#9084=CARTESIAN_POINT('Ctrl Pts',(7.08712282114353,-1.8675308530798,14.9348850835941));
#9085=CARTESIAN_POINT('Ctrl Pts',(6.99861212849077,-1.98633520196457,14.9447662312501));
#9086=CARTESIAN_POINT('Ctrl Pts',(6.86667537881657,-2.14009490638359,14.9579145561792));
#9087=CARTESIAN_POINT('Ctrl Pts',(6.83006004188112,-2.18063456779403,14.9614205251225));
#9088=CARTESIAN_POINT('Ctrl Pts',(6.76471952787671,-2.24938112752681,14.9674359063435));
#9089=CARTESIAN_POINT('Ctrl Pts',(6.7364645212211,-2.27801593685362,14.9699639235607));
#9090=CARTESIAN_POINT('Ctrl Pts',(6.69467183484033,-2.31881361055144,14.9736004166451));
#9091=CARTESIAN_POINT('Ctrl Pts',(6.68155647049997,-2.33140177959777,14.9747274430352));
#9092=CARTESIAN_POINT('Ctrl Pts',(6.65803514022487,-2.35359833533061,14.9767239242144));
#9093=CARTESIAN_POINT('Ctrl Pts',(6.64767111715006,-2.36325027951491,14.9775952442196));
#9094=CARTESIAN_POINT('Ctrl Pts',(6.62612832506414,-2.38304937996144,14.9793893634656));
#9095=CARTESIAN_POINT('Ctrl Pts',(6.61494118668094,-2.39318694699945,14.9803117437174));
#9096=CARTESIAN_POINT('Ctrl Pts',(6.586021710273,-2.41902546387145,14.9826727183195));
#9097=CARTESIAN_POINT('Ctrl Pts',(6.56818658696452,-2.43461040324936,14.9841064524206));
#9098=CARTESIAN_POINT('Ctrl Pts',(6.49667708818337,-2.49572078105314,14.989769350504));
#9099=CARTESIAN_POINT('Ctrl Pts',(6.44168728269488,-2.53968121904806,14.9939349224885));
#9100=CARTESIAN_POINT('Ctrl Pts',(6.12210599978859,-2.7784355454532,15.01721009849));
#9101=CARTESIAN_POINT('Ctrl Pts',(5.83043737062552,-2.93363660032036,15.0347322344474));
#9102=CARTESIAN_POINT('Ctrl Pts',(5.47644648393849,-3.05743844316518,15.0565147558549));
#9103=CARTESIAN_POINT('Ctrl Pts',(5.43218856466564,-3.07184875875863,15.0592507877455));
#9104=CARTESIAN_POINT('Ctrl Pts',(5.35814160150145,-3.09419673881673,15.0638729440253));
#9105=CARTESIAN_POINT('Ctrl Pts',(5.32852189574028,-3.10267473658088,15.0657335470274));
#9106=CARTESIAN_POINT('Ctrl Pts',(5.28747778554708,-3.1137885927299,15.0683336358798));
#9107=CARTESIAN_POINT('Ctrl Pts',(5.27615270024326,-3.11678899208406,15.0690533451905));
#9108=CARTESIAN_POINT('Ctrl Pts',(5.25698295075369,-3.12175600446902,15.0702758228254));
#9109=CARTESIAN_POINT('Ctrl Pts',(5.2491466463116,-3.12375499718228,15.070776747878));
#9110=CARTESIAN_POINT('Ctrl Pts',(5.23412019655623,-3.12752796768631,15.0717397190164));
#9111=CARTESIAN_POINT('Ctrl Pts',(5.22693134139263,-3.12930668815255,15.0722014696066));
#9112=CARTESIAN_POINT('Ctrl Pts',(5.209695343519,-3.1335083555683,15.0733109749551));
#9113=CARTESIAN_POINT('Ctrl Pts',(5.19964262458101,-3.13590776231487,15.0739600421062));
#9114=CARTESIAN_POINT('Ctrl Pts',(5.16324526498061,-3.14441032879497,15.0763167312534));
#9115=CARTESIAN_POINT('Ctrl Pts',(5.13683643246793,-3.15022999866435,15.078039235676));
#9116=CARTESIAN_POINT('Ctrl Pts',(4.94902443312715,-3.18914613116777,15.0903631142691));
#9117=CARTESIAN_POINT('Ctrl Pts',(4.78537925197181,-3.21015133415179,15.1014746765021));
#9118=CARTESIAN_POINT('Ctrl Pts',(4.48179962305897,-3.22565733684048,15.122036005141));
#9119=CARTESIAN_POINT('Ctrl Pts',(4.3424133502767,-3.22374042586903,15.131457439967));
#9120=CARTESIAN_POINT('Ctrl Pts',(4.11318825098388,-3.20569766475699,15.1467016091323));
#9121=CARTESIAN_POINT('Ctrl Pts',(4.02312898995123,-3.19477040685419,15.1526286579963));
#9122=CARTESIAN_POINT('Ctrl Pts',(3.87518073051021,-3.17044660910166,15.1622457337651));
#9123=CARTESIAN_POINT('Ctrl Pts',(3.81699100714112,-3.15922401578979,15.1659975467593));
#9124=CARTESIAN_POINT('Ctrl Pts',(3.73815318799753,-3.14175140790295,15.1710415994763));
#9125=CARTESIAN_POINT('Ctrl Pts',(3.71721248781034,-3.13689007705289,15.1723776313622));
#9126=CARTESIAN_POINT('Ctrl Pts',(3.68210168877383,-3.12836807024229,15.1746117886382));
#9127=CARTESIAN_POINT('Ctrl Pts',(3.66790528539886,-3.12481980150151,15.1755134896691));
#9128=CARTESIAN_POINT('Ctrl Pts',(3.63990958932302,-3.11761958146123,15.1772886055435));
#9129=CARTESIAN_POINT('Ctrl Pts',(3.62610942759744,-3.11397240093494,15.1781621509356));
#9130=CARTESIAN_POINT('Ctrl Pts',(3.59263237828971,-3.10488653676805,15.180277876917));
#9131=CARTESIAN_POINT('Ctrl Pts',(3.57298189287824,-3.09935229881371,15.1815169389064));
#9132=CARTESIAN_POINT('Ctrl Pts',(3.51730052904785,-3.08309795347374,15.1850208001341));
#9133=CARTESIAN_POINT('Ctrl Pts',(3.4814020997098,-3.07193344900454,15.187271214329));
#9134=CARTESIAN_POINT('Ctrl Pts',(3.25867460225429,-2.99836671792159,15.2011958885521));
#9135=CARTESIAN_POINT('Ctrl Pts',(3.07769267005492,-2.91957230184472,15.2123094245236));
#9136=CARTESIAN_POINT('Ctrl Pts',(2.71679310047202,-2.72135312549109,15.2353514374189));
#9137=CARTESIAN_POINT('Ctrl Pts',(2.53939296715385,-2.59942900765162,15.2472123668693));
#9138=CARTESIAN_POINT('Ctrl Pts',(2.3502247670444,-2.43945574961192,15.261987120572));
#9139=CARTESIAN_POINT('Ctrl Pts',(2.32532299546861,-2.41773150531196,15.2639799050779));
#9140=CARTESIAN_POINT('Ctrl Pts',(2.29181148491297,-2.38757615299691,15.2667349022613));
#9141=CARTESIAN_POINT('Ctrl Pts',(2.28290754403098,-2.37947318298986,15.2674741218123));
#9142=CARTESIAN_POINT('Ctrl Pts',(2.26805092895519,-2.36580005546202,15.2687201365073));
#9143=CARTESIAN_POINT('Ctrl Pts',(2.26207350663044,-2.36025675956711,15.269224920633));
#9144=CARTESIAN_POINT('Ctrl Pts',(2.25075312463964,-2.34967837588233,15.2701876575358));
#9145=CARTESIAN_POINT('Ctrl Pts',(2.24540622322211,-2.34464760387622,15.2706452672557));
#9146=CARTESIAN_POINT('Ctrl Pts',(2.23275363500033,-2.33266131671862,15.2717348951321));
#9147=CARTESIAN_POINT('Ctrl Pts',(2.22546337364863,-2.32568973217038,15.2723681242489));
#9148=CARTESIAN_POINT('Ctrl Pts',(2.19988690652591,-2.30100035787233,15.2746084055066));
#9149=CARTESIAN_POINT('Ctrl Pts',(2.18177860318924,-2.28310071890812,15.276228534302));
#9150=CARTESIAN_POINT('Ctrl Pts',(2.01306099467025,-2.11232756960067,15.291631139164));
#9151=CARTESIAN_POINT('Ctrl Pts',(1.8778746534446,-1.94499561999119,15.3062799670444));
#9152=CARTESIAN_POINT('Ctrl Pts',(1.63873268111013,-1.57979345273465,15.335760523392));
#9153=CARTESIAN_POINT('Ctrl Pts',(1.53662570504871,-1.38200353901985,15.3504889999615));
#9154=CARTESIAN_POINT('Ctrl Pts',(1.44400241626756,-1.14550545677039,15.3664998642962));
#9155=CARTESIAN_POINT('Ctrl Pts',(1.43279408778,-1.11558406697368,15.3684991252655));
#9156=CARTESIAN_POINT('Ctrl Pts',(1.41634800651187,-1.06961023670867,15.371531765673));
#9157=CARTESIAN_POINT('Ctrl Pts',(1.41078860101692,-1.05367577409899,15.3725757628642));
#9158=CARTESIAN_POINT('Ctrl Pts',(1.40091075172541,-1.0246322121648,15.3744659844511));
#9159=CARTESIAN_POINT('Ctrl Pts',(1.39655089369322,-1.01153772542836,15.3753135592133));
#9160=CARTESIAN_POINT('Ctrl Pts',(1.38723785354293,-0.982955475485766,15.3771537046914));
#9161=CARTESIAN_POINT('Ctrl Pts',(1.38231748019399,-0.967457360575087,15.3781451787012));
#9162=CARTESIAN_POINT('Ctrl Pts',(1.3691694997775,-0.924930750841023,15.3808489745612));
#9163=CARTESIAN_POINT('Ctrl Pts',(1.36117956201714,-0.897829865947965,15.3825535311901));
#9164=CARTESIAN_POINT('Ctrl Pts',(1.31930693117452,-0.748595398889713,15.3918441941649));
#9165=CARTESIAN_POINT('Ctrl Pts',(1.29229332272023,-0.624642692087423,15.3992051302605));
#9166=CARTESIAN_POINT('Ctrl Pts',(1.23810632496545,-0.279191222249639,15.4191270217043));
#9167=CARTESIAN_POINT('Ctrl Pts',(1.22650555388356,-0.0559962116658821,
15.4313123565139));
#9168=CARTESIAN_POINT('Ctrl Pts',(1.24350940002346,0.272487247807755,15.4500777972967));
#9169=CARTESIAN_POINT('Ctrl Pts',(1.25421206541333,0.378027060073327,15.4562438562687));
#9170=CARTESIAN_POINT('Ctrl Pts',(1.27268806453745,0.499955667475999,15.4637212285154));
#9171=CARTESIAN_POINT('Ctrl Pts',(1.27542016680174,0.517054161047396,15.4647780004967));
#9172=CARTESIAN_POINT('Ctrl Pts',(1.27983162273718,0.543303228168585,15.466414079682));
#9173=CARTESIAN_POINT('Ctrl Pts',(1.28141308503983,0.552470231326708,15.4669880367354));
#9174=CARTESIAN_POINT('Ctrl Pts',(1.28439842666182,0.569338605951417,15.4680491655432));
#9175=CARTESIAN_POINT('Ctrl Pts',(1.28579069763014,0.577041826573964,15.4685356811352));
#9176=CARTESIAN_POINT('Ctrl Pts',(1.28901156523218,0.594498751472163,15.4696425879379));
#9177=CARTESIAN_POINT('Ctrl Pts',(1.2908571447149,0.604249073216228,15.4702639161204));
#9178=CARTESIAN_POINT('Ctrl Pts',(1.29576630894026,0.629544621579493,15.4718835763839));
#9179=CARTESIAN_POINT('Ctrl Pts',(1.29889951367914,0.645075846705851,15.4728856281999));
#9180=CARTESIAN_POINT('Ctrl Pts',(1.3209783302041,0.750503478900806,15.4797364699548));
#9181=CARTESIAN_POINT('Ctrl Pts',(1.34364436939426,0.839569415432615,15.4857648979553));
#9182=CARTESIAN_POINT('Ctrl Pts',(1.45116918186101,1.19735947953262,15.5106570506489));
#9183=CARTESIAN_POINT('Ctrl Pts',(1.56731088601597,1.45543868967549,15.5300570237345));
#9184=CARTESIAN_POINT('Ctrl Pts',(1.74650013688679,1.74517910261711,15.5522316704088));
#9185=CARTESIAN_POINT('Ctrl Pts',(1.77882599492155,1.79438289729783,15.5560191474207));
#9186=CARTESIAN_POINT('Ctrl Pts',(1.83704714393673,1.87792220657212,15.5624874975784));
#9187=CARTESIAN_POINT('Ctrl Pts',(1.86231436145487,1.91267474411123,15.5651903114901));
#9188=CARTESIAN_POINT('Ctrl Pts',(1.89973544563385,1.96203739895868,15.5690486229272));
#9189=CARTESIAN_POINT('Ctrl Pts',(1.91133454074299,1.97706040231578,15.5702255144003));
#9190=CARTESIAN_POINT('Ctrl Pts',(1.93181970906803,2.00311346668988,15.5722714590117));
#9191=CARTESIAN_POINT('Ctrl Pts',(1.94064694636333,2.0141889209122,15.5731428086271));
#9192=CARTESIAN_POINT('Ctrl Pts',(1.95903325834408,2.03694860674731,15.5749368931426));
#9193=CARTESIAN_POINT('Ctrl Pts',(1.96860200889535,2.04862460177561,15.5758592097129));
#9194=CARTESIAN_POINT('Ctrl Pts',(1.99338998167762,2.07844159879424,15.5782198226448));
#9195=CARTESIAN_POINT('Ctrl Pts',(2.00872790470422,2.09648308114642,15.5796532616922));
#9196=CARTESIAN_POINT('Ctrl Pts',(2.07040961426932,2.16743741313799,15.5853133263687));
#9197=CARTESIAN_POINT('Ctrl Pts',(2.11828329299251,2.21899820097414,15.5894764437169));
#9198=CARTESIAN_POINT('Ctrl Pts',(2.39914382956457,2.5022980747393,15.6127525369564));
#9199=CARTESIAN_POINT('Ctrl Pts',(2.66476548795755,2.69885961722462,15.6302771501956));
#9200=CARTESIAN_POINT('Ctrl Pts',(2.99666883167572,2.87354607291331,15.6520626329592));
#9201=CARTESIAN_POINT('Ctrl Pts',(3.0383189194704,2.89432781418454,15.6547987805471));
#9202=CARTESIAN_POINT('Ctrl Pts',(3.10826234086195,2.92735466362218,15.6594211141058));
#9203=CARTESIAN_POINT('Ctrl Pts',(3.13630846254418,2.94010927095211,15.6612817761825));
#9204=CARTESIAN_POINT('Ctrl Pts',(3.17526538630308,2.95715604202562,15.6638819344545));
#9205=CARTESIAN_POINT('Ctrl Pts',(3.18602417479616,2.96179413450565,15.6646016527264));
#9206=CARTESIAN_POINT('Ctrl Pts',(3.20425177444704,2.96953442835968,15.6658241411236));
#9207=CARTESIAN_POINT('Ctrl Pts',(3.2117075407422,2.97266742347229,15.6663250679011));
#9208=CARTESIAN_POINT('Ctrl Pts',(3.22601311531618,2.97861552754672,15.6672880387195));
#9209=CARTESIAN_POINT('Ctrl Pts',(3.23286094785519,2.98143513742272,15.6677497872422));
#9210=CARTESIAN_POINT('Ctrl Pts',(3.24928852999123,2.98813310159381,15.6688592828029));
#9211=CARTESIAN_POINT('Ctrl Pts',(3.25887726665417,2.9919889965436,15.6695083421836));
#9212=CARTESIAN_POINT('Ctrl Pts',(3.2936214155095,3.0057667995058,15.6718649652339));
#9213=CARTESIAN_POINT('Ctrl Pts',(3.3188821243309,3.01541780722588,15.673587410236));
#9214=CARTESIAN_POINT('Ctrl Pts',(3.49891374656644,3.0816159371021,15.685912244743));
#9215=CARTESIAN_POINT('Ctrl Pts',(3.65768640977057,3.1265324128846,15.697024925187));
#9216=CARTESIAN_POINT('Ctrl Pts',(3.95570321320723,3.18665160919139,15.7175893014402));
#9217=CARTESIAN_POINT('Ctrl Pts',(4.09387694156978,3.20531527989227,15.7270126673056));
#9218=CARTESIAN_POINT('Ctrl Pts',(4.323258641263,3.22127138336444,15.7422567663711));
#9219=CARTESIAN_POINT('Ctrl Pts',(4.41391757009788,3.22374410640866,15.7481819746428));
#9220=CARTESIAN_POINT('Ctrl Pts',(4.56379553996563,3.22150700926882,15.757796432196));
#9221=CARTESIAN_POINT('Ctrl Pts',(4.62299141574046,3.21899012709779,15.7615474245602));
#9222=CARTESIAN_POINT('Ctrl Pts',(4.70352972195975,3.21333792889785,15.7665905678146));
#9223=CARTESIAN_POINT('Ctrl Pts',(4.72495669281635,3.21161860203254,15.767926490416));
#9224=CARTESIAN_POINT('Ctrl Pts',(4.76093836755449,3.20836876600046,15.7701605166629));
#9225=CARTESIAN_POINT('Ctrl Pts',(4.77550250593776,3.20695328479521,15.7710621950245));
#9226=CARTESIAN_POINT('Ctrl Pts',(4.80425394586561,3.20396114408532,15.7728373051744));
#9227=CARTESIAN_POINT('Ctrl Pts',(4.81844140237559,3.20238932277656,15.7737108672417));
#9228=CARTESIAN_POINT('Ctrl Pts',(4.85289422398696,3.19834042691797,15.7758267007739));
#9229=CARTESIAN_POINT('Ctrl Pts',(4.87314756679253,3.1957649241662,15.777065852861));
#9230=CARTESIAN_POINT('Ctrl Pts',(4.93062448544956,3.18790020372233,15.7805701413381));
#9231=CARTESIAN_POINT('Ctrl Pts',(4.96778258405081,3.18215174611032,15.7828208874788));
#9232=CARTESIAN_POINT('Ctrl Pts',(5.21316504250359,3.13978107849448,15.7976033829535));
#9233=CARTESIAN_POINT('Ctrl Pts',(5.41745873030948,3.08339525977471,15.8094782179626));
#9234=CARTESIAN_POINT('Ctrl Pts',(5.80274165822397,2.93500252859362,15.8325659842394));
#9235=CARTESIAN_POINT('Ctrl Pts',(5.98348285575964,2.84515349319922,15.8437480808564));
#9236=CARTESIAN_POINT('Ctrl Pts',(6.18199055873875,2.72208181252755,15.857688050087));
#9237=CARTESIAN_POINT('Ctrl Pts',(6.20909121548159,2.70471241350369,15.8596302339857));
#9238=CARTESIAN_POINT('Ctrl Pts',(6.2458620876556,2.68036048827521,15.8623260277433));
#9239=CARTESIAN_POINT('Ctrl Pts',(6.25576143949166,2.67372524358928,15.8630579042713));
#9240=CARTESIAN_POINT('Ctrl Pts',(6.27234954527477,2.66247288219343,15.8642950368265));
#9241=CARTESIAN_POINT('Ctrl Pts',(6.27905816691606,2.65788501087693,15.8647983454083));
#9242=CARTESIAN_POINT('Ctrl Pts',(6.29181241666764,2.64909168023801,15.8657610664351));
#9243=CARTESIAN_POINT('Ctrl Pts',(6.29786110274209,2.64489079360161,15.866220153304));
#9244=CARTESIAN_POINT('Ctrl Pts',(6.31223395401858,2.63483547095914,15.8673169395816));
#9245=CARTESIAN_POINT('Ctrl Pts',(6.32054483272826,2.62896230643553,15.8679558863853));
#9246=CARTESIAN_POINT('Ctrl Pts',(6.34998446106017,2.60794801412565,15.8702357492567));
#9247=CARTESIAN_POINT('Ctrl Pts',(6.37095704520445,2.59259118943021,15.8718903340276));
#9248=CARTESIAN_POINT('Ctrl Pts',(6.55531774909965,2.45413934154408,15.8866906939704));
#9249=CARTESIAN_POINT('Ctrl Pts',(6.70681294335107,2.31601053395622,15.9006226174699));
#9250=CARTESIAN_POINT('Ctrl Pts',(6.95076845518491,2.04689358348651,15.9251721949746));
#9251=CARTESIAN_POINT('Ctrl Pts',(7.04853299112394,1.92159232861858,15.9358060395362));
#9252=CARTESIAN_POINT('Ctrl Pts',(7.18434943544674,1.71818436432412,15.9517045869608));
#9253=CARTESIAN_POINT('Ctrl Pts',(7.22915534981766,1.64490176510289,15.9571899674633));
#9254=CARTESIAN_POINT('Ctrl Pts',(7.28292755144546,1.54849969638027,15.9641055038649));
#9255=CARTESIAN_POINT('Ctrl Pts',(7.29462621547439,1.52695216979027,15.9656327383442));
#9256=CARTESIAN_POINT('Ctrl Pts',(7.31321419106842,1.49176355521575,15.9680974879967));
#9257=CARTESIAN_POINT('Ctrl Pts',(7.32025420768364,1.47820360232922,15.9690403089542));
#9258=CARTESIAN_POINT('Ctrl Pts',(7.3336031132064,1.45203861313983,15.9708463948364));
#9259=CARTESIAN_POINT('Ctrl Pts',(7.33992624175181,1.43944127553771,15.971710144428));
#9260=CARTESIAN_POINT('Ctrl Pts',(7.35423364050562,1.41046456113806,15.9736839093621));
#9261=CARTESIAN_POINT('Ctrl Pts',(7.36216209700713,1.39405804715089,15.974791963404));
#9262=CARTESIAN_POINT('Ctrl Pts',(7.38698202081989,1.34156589152543,15.9783077808639));
#9263=CARTESIAN_POINT('Ctrl Pts',(7.4033440510622,1.30523302658718,15.9806973455743));
#9264=CARTESIAN_POINT('Ctrl Pts',(7.5193582668769,1.03430624520518,15.99821559639));
#9265=CARTESIAN_POINT('Ctrl Pts',(7.59154100052254,0.788934775008786,16.0123398231549));
#9266=CARTESIAN_POINT('Ctrl Pts',(7.66416188569981,0.359695869536868,16.0367207869367));
#9267=CARTESIAN_POINT('Ctrl Pts',(7.67926286618053,0.179600130261551,16.0468902667977));
#9268=CARTESIAN_POINT('Ctrl Pts',(7.6792190109727,-0.000783520933935085,
16.0578089001435));
#9269=CARTESIAN_POINT('Ctrl Pts',(7.67921910621823,-2.74841093364834E-11,
15.8122671767608));
#9270=CARTESIAN_POINT('Ctrl Pts',(7.67921910621895,0.0842650733278685,15.8067022814364));
#9271=CARTESIAN_POINT('Ctrl Pts',(7.67591422296171,0.168504703978227,15.801214720458));
#9272=CARTESIAN_POINT('Ctrl Pts',(7.66563399803438,0.299298265355216,15.7928221212079));
#9273=CARTESIAN_POINT('Ctrl Pts',(7.66093664709852,0.345986854884521,15.7898514449779));
#9274=CARTESIAN_POINT('Ctrl Pts',(7.65302786761198,0.410431366001335,15.7857844094348));
#9275=CARTESIAN_POINT('Ctrl Pts',(7.65068464403456,0.428286049699491,15.7846611645038));
#9276=CARTESIAN_POINT('Ctrl Pts',(7.64628536217112,0.459760257945463,15.7826871631853));
#9277=CARTESIAN_POINT('Ctrl Pts',(7.64429143132403,0.473387868997891,15.7818344736633));
#9278=CARTESIAN_POINT('Ctrl Pts',(7.64018893903769,0.500224444763774,15.7801591172514));
#9279=CARTESIAN_POINT('Ctrl Pts',(7.63808538195312,0.513433882381725,15.7793363103066));
#9280=CARTESIAN_POINT('Ctrl Pts',(7.63343583664471,0.54150464592363,15.7775915504833));
#9281=CARTESIAN_POINT('Ctrl Pts',(7.63086766532932,0.556362011489941,15.7766703214067));
#9282=CARTESIAN_POINT('Ctrl Pts',(7.62401251917557,0.594426801702553,15.7743155707005));
#9283=CARTESIAN_POINT('Ctrl Pts',(7.61957467945073,0.617606406591507,15.7728868599203));
#9284=CARTESIAN_POINT('Ctrl Pts',(7.60102989959306,0.709020207630493,15.7672709705227));
#9285=CARTESIAN_POINT('Ctrl Pts',(7.58496580574802,0.776840836270749,15.7631460077259));
#9286=CARTESIAN_POINT('Ctrl Pts',(7.54167806563526,0.936344328961776,15.7534995467753));
#9287=CARTESIAN_POINT('Ctrl Pts',(7.51254823862863,1.02744207392575,15.7480348531459));
#9288=CARTESIAN_POINT('Ctrl Pts',(7.43390192305887,1.24026101818886,15.7352108874529));
#9289=CARTESIAN_POINT('Ctrl Pts',(7.38091148706979,1.36051118353049,15.7279206843769));
#9290=CARTESIAN_POINT('Ctrl Pts',(7.24567551781377,1.62273230924428,15.7113667334707));
#9291=CARTESIAN_POINT('Ctrl Pts',(7.15964302471967,1.76231927900727,15.7020852857202));
#9292=CARTESIAN_POINT('Ctrl Pts',(7.0514954424338,1.91111627420558,15.6909718891952));
#9293=CARTESIAN_POINT('Ctrl Pts',(7.039443945683,1.92737334999577,15.689740095815));
#9294=CARTESIAN_POINT('Ctrl Pts',(7.02126984890355,1.95141300962047,15.6878904860991));
#9295=CARTESIAN_POINT('Ctrl Pts',(7.0152629300453,1.95928296702558,15.6872804180134));
#9296=CARTESIAN_POINT('Ctrl Pts',(7.00490123341382,1.97272940774302,15.6862299938113));
#9297=CARTESIAN_POINT('Ctrl Pts',(7.0005642163603,1.97831941111292,15.6857908864));
#9298=CARTESIAN_POINT('Ctrl Pts',(6.99066122321391,1.99099700843951,15.6847894581584));
#9299=CARTESIAN_POINT('Ctrl Pts',(6.98508401189751,1.99807543090164,15.6842263536444));
#9300=CARTESIAN_POINT('Ctrl Pts',(6.96980018926268,2.01730670473776,15.6826858336296));
#9301=CARTESIAN_POINT('Ctrl Pts',(6.96003531502426,2.02941264642906,15.6817044342856));
#9302=CARTESIAN_POINT('Ctrl Pts',(6.91040666148698,2.0900361528138,15.6767328374561));
#9303=CARTESIAN_POINT('Ctrl Pts',(6.86922116389314,2.13744870580446,15.6726592925865));
#9304=CARTESIAN_POINT('Ctrl Pts',(6.78609401677653,2.22767892795889,15.6645855040948));
#9305=CARTESIAN_POINT('Ctrl Pts',(6.74428883167371,2.27059153463945,15.6605919620065));
#9306=CARTESIAN_POINT('Ctrl Pts',(6.56128389896565,2.44825685468741,15.643469474081));
#9307=CARTESIAN_POINT('Ctrl Pts',(6.40918306970307,2.57121039353712,15.6301415999972));
#9308=CARTESIAN_POINT('Ctrl Pts',(6.16913421937717,2.73160046180395,15.6109759102717));
#9309=CARTESIAN_POINT('Ctrl Pts',(6.08914780985128,2.7801484985049,15.6048554815705));
#9310=CARTESIAN_POINT('Ctrl Pts',(5.97148072336591,2.84473436462652,15.5962396788252));
#9311=CARTESIAN_POINT('Ctrl Pts',(5.93543569516697,2.86363962000486,15.5936500060045));
#9312=CARTESIAN_POINT('Ctrl Pts',(5.87046681988051,2.8961610955757,15.589069118269));
#9313=CARTESIAN_POINT('Ctrl Pts',(5.84168080312052,2.91003905448762,15.5870691243747));
#9314=CARTESIAN_POINT('Ctrl Pts',(5.79746827482951,2.93054951192893,15.5840413399687));
#9315=CARTESIAN_POINT('Ctrl Pts',(5.78218910390708,2.93749310073453,15.5830028820373));
#9316=CARTESIAN_POINT('Ctrl Pts',(5.76674005434707,2.94436879842505,15.5819606821606));
#9317=CARTESIAN_POINT('Ctrl Pts',(5.76662395001161,2.94442046316999,15.581952850152));
#9318=CARTESIAN_POINT('Ctrl Pts',(5.76638363535373,2.94452738267807,15.5819366402476));
#9319=CARTESIAN_POINT('Ctrl Pts',(5.76625942459416,2.94458263644781,15.5819282623862));
#9320=CARTESIAN_POINT('Ctrl Pts',(5.76600230474415,2.94469699385462,15.5819109210194));
#9321=CARTESIAN_POINT('Ctrl Pts',(5.76586939511761,2.9447560963666,15.5819019575512));
#9322=CARTESIAN_POINT('Ctrl Pts',(5.76559423873709,2.94487843113088,15.581883402115));
#9323=CARTESIAN_POINT('Ctrl Pts',(5.76545199140813,2.94494166207284,15.5818738101925));
#9324=CARTESIAN_POINT('Ctrl Pts',(5.76515747047517,2.94507255522234,15.581853951636));
#9325=CARTESIAN_POINT('Ctrl Pts',(5.76500519620537,2.94514021592632,15.5818436850538));
#9326=CARTESIAN_POINT('Ctrl Pts',(5.76468987762537,2.94528029355213,15.5818224273288));
#9327=CARTESIAN_POINT('Ctrl Pts',(5.76452683253783,2.94535270875038,15.5818114362448));
#9328=CARTESIAN_POINT('Ctrl Pts',(5.76418916926002,2.94550264568189,15.581788675722));
#9329=CARTESIAN_POINT('Ctrl Pts',(5.76401455018736,2.94558016542695,15.5817769063515));
#9330=CARTESIAN_POINT('Ctrl Pts',(5.7636528715537,2.94574068920268,15.5817525311862));
#9331=CARTESIAN_POINT('Ctrl Pts',(5.76346581097887,2.9458236909438,15.5817399254702));
#9332=CARTESIAN_POINT('Ctrl Pts',(5.76307831220833,2.94599558611335,15.5817138149134));
#9333=CARTESIAN_POINT('Ctrl Pts',(5.76287787282165,2.94608447691495,15.5817003101619));
#9334=CARTESIAN_POINT('Ctrl Pts',(5.76246260363558,2.94626858966093,15.5816723338166));
#9335=CARTESIAN_POINT('Ctrl Pts',(5.76224777249714,2.946363808563,15.5816578623279));
#9336=CARTESIAN_POINT('Ctrl Pts',(5.76180262511463,2.94656105153108,15.5816278793665));
#9337=CARTESIAN_POINT('Ctrl Pts',(5.76157230729521,2.9466630721026,15.5816123680128));
#9338=CARTESIAN_POINT('Ctrl Pts',(5.76109500319871,2.94687442969405,15.5815802263163));
#9339=CARTESIAN_POINT('Ctrl Pts',(5.76084801514135,2.94698376266537,15.5815635961131));
#9340=CARTESIAN_POINT('Ctrl Pts',(5.76033609148587,2.94721029639146,15.5815291313911));
#9341=CARTESIAN_POINT('Ctrl Pts',(5.76007115381155,2.94732749248152,15.581511297032));
#9342=CARTESIAN_POINT('Ctrl Pts',(5.7470510905882,2.95308486314133,15.5806349601208));
#9343=CARTESIAN_POINT('Ctrl Pts',(5.73425934784724,2.95864228580718,15.579779299626));
#9344=CARTESIAN_POINT('Ctrl Pts',(5.70561996261436,2.97086439389849,15.5778751900898));
#9345=CARTESIAN_POINT('Ctrl Pts',(5.68975418130527,2.97748569272211,15.5768282328901));
#9346=CARTESIAN_POINT('Ctrl Pts',(5.64943271995649,2.9939355390484,15.5741869292169));
#9347=CARTESIAN_POINT('Ctrl Pts',(5.62490777208991,3.00359174022535,15.5725983827072));
#9348=CARTESIAN_POINT('Ctrl Pts',(5.47281146318484,3.06133169274663,15.5628522427458));
#9349=CARTESIAN_POINT('Ctrl Pts',(5.34240645678249,3.10158425330213,15.5549595961868));
#9350=CARTESIAN_POINT('Ctrl Pts',(5.00100358647835,3.18366601698323,15.5350179954092));
#9351=CARTESIAN_POINT('Ctrl Pts',(4.78769233542449,3.21286967120153,15.5232619013929));
#9352=CARTESIAN_POINT('Ctrl Pts',(4.46963093309053,3.22438492671661,15.5050854832484));
#9353=CARTESIAN_POINT('Ctrl Pts',(4.36608115169072,3.22314395226207,15.4990592922793));
#9354=CARTESIAN_POINT('Ctrl Pts',(4.245588507109,3.21588924404218,15.4917392925464));
#9355=CARTESIAN_POINT('Ctrl Pts',(4.22840382921732,3.21471623265909,15.4906879652083));
#9356=CARTESIAN_POINT('Ctrl Pts',(4.20197411440329,3.21269918115946,15.4890586000215));
#9357=CARTESIAN_POINT('Ctrl Pts',(4.19272164290768,3.21195283278537,15.4884858445347));
#9358=CARTESIAN_POINT('Ctrl Pts',(4.17567192684417,3.21050335583172,15.4874258711806));
#9359=CARTESIAN_POINT('Ctrl Pts',(4.16787390269243,3.20981177924335,15.4869392995582));
#9360=CARTESIAN_POINT('Ctrl Pts',(4.15017427637304,3.20817704771718,15.4858308932224));
#9361=CARTESIAN_POINT('Ctrl Pts',(4.14027452628728,3.20721646817218,15.4852081098509));
#9362=CARTESIAN_POINT('Ctrl Pts',(4.11453934901997,3.20459905614654,15.4835820514084));
#9363=CARTESIAN_POINT('Ctrl Pts',(4.09871168692683,3.20287069276456,15.4825750089276));
#9364=CARTESIAN_POINT('Ctrl Pts',(3.98973828446636,3.19015310143718,15.4755963594086));
#9365=CARTESIAN_POINT('Ctrl Pts',(3.89710632796835,3.17522036171682,15.4694376110368));
#9366=CARTESIAN_POINT('Ctrl Pts',(3.53108585644918,3.09970301145523,15.4445203084541));
#9367=CARTESIAN_POINT('Ctrl Pts',(3.26538928753086,3.00763378006678,15.4252525225651));
#9368=CARTESIAN_POINT('Ctrl Pts',(2.96243440968215,2.85612045319719,15.4032067467837));
#9369=CARTESIAN_POINT('Ctrl Pts',(2.91065529717274,2.82843138130871,15.3994295612968));
#9370=CARTESIAN_POINT('Ctrl Pts',(2.82241784803954,2.77809866740508,15.3929769716587));
#9371=CARTESIAN_POINT('Ctrl Pts',(2.78560316788573,2.75611375322189,15.3902797679413));
#9372=CARTESIAN_POINT('Ctrl Pts',(2.73315350411069,2.7233546359667,15.3864280131561));
#9373=CARTESIAN_POINT('Ctrl Pts',(2.71715904636012,2.71316746221537,15.3852521669152));
#9374=CARTESIAN_POINT('Ctrl Pts',(2.68938066882154,2.69512828705432,15.3832075077371));
#9375=CARTESIAN_POINT('Ctrl Pts',(2.67755698112068,2.68733877481257,15.38233640583));
#9376=CARTESIAN_POINT('Ctrl Pts',(2.65323081725135,2.67108165899843,15.3805423428934));
#9377=CARTESIAN_POINT('Ctrl Pts',(2.64073572875639,2.66260358859132,15.3796198034592));
#9378=CARTESIAN_POINT('Ctrl Pts',(2.60878153733425,2.64059273145671,15.3772576082841));
#9379=CARTESIAN_POINT('Ctrl Pts',(2.58941108920564,2.62693238067609,15.3758228237256));
#9380=CARTESIAN_POINT('Ctrl Pts',(2.51299407515785,2.57176960231916,15.3701490248023));
#9381=CARTESIAN_POINT('Ctrl Pts',(2.45716381579259,2.52861098679474,15.3659739288738));
#9382=CARTESIAN_POINT('Ctrl Pts',(2.14974972054736,2.27441704651301,15.3427019931669));
#9383=CARTESIAN_POINT('Ctrl Pts',(1.93020425142487,2.02777595095433,15.3251892232104));
#9384=CARTESIAN_POINT('Ctrl Pts',(1.72640961500678,1.71320111798867,15.3034178980689));
#9385=CARTESIAN_POINT('Ctrl Pts',(1.70195892173451,1.67360572222976,15.3006823438617));
#9386=CARTESIAN_POINT('Ctrl Pts',(1.66276178985039,1.60694302366897,15.2960609581086));
#9387=CARTESIAN_POINT('Ctrl Pts',(1.64753049301144,1.58016776312746,15.2942006386201));
#9388=CARTESIAN_POINT('Ctrl Pts',(1.62704028672539,1.54291521021326,15.2916009297953));
#9389=CARTESIAN_POINT('Ctrl Pts',(1.62145071305986,1.53262046544368,15.2908813108477));
#9390=CARTESIAN_POINT('Ctrl Pts',(1.61209782512665,1.51516829658132,15.2896589815691));
#9391=CARTESIAN_POINT('Ctrl Pts',(1.60830502975869,1.50802663885232,15.2891581140091));
#9392=CARTESIAN_POINT('Ctrl Pts',(1.6010906341844,1.49431796358418,15.2881952516157));
#9393=CARTESIAN_POINT('Ctrl Pts',(1.59766473139471,1.48775331917547,15.2877335521962));
#9394=CARTESIAN_POINT('Ctrl Pts',(1.5895119862195,1.47199905822171,15.2866241703193));
#9395=CARTESIAN_POINT('Ctrl Pts',(1.58480669625066,1.46279846584081,15.285975175754));
#9396=CARTESIAN_POINT('Ctrl Pts',(1.56795010939538,1.42944279101816,15.2836187565137));
#9397=CARTESIAN_POINT('Ctrl Pts',(1.55605906122965,1.40515840653327,15.2818964526451));
#9398=CARTESIAN_POINT('Ctrl Pts',(1.47386999824014,1.2318194203206,15.2695703299018));
#9399=CARTESIAN_POINT('Ctrl Pts',(1.41479711571852,1.07772802551118,15.258456065562));
#9400=CARTESIAN_POINT('Ctrl Pts',(1.32800902907146,0.786296812171222,15.2378876730981));
#9401=CARTESIAN_POINT('Ctrl Pts',(1.29694487400604,0.650335241337894,15.2284618734336));
#9402=CARTESIAN_POINT('Ctrl Pts',(1.26035818069816,0.423324305142609,15.2132177361621));
#9403=CARTESIAN_POINT('Ctrl Pts',(1.2497186671456,0.333290381493073,15.2072947245123));
#9404=CARTESIAN_POINT('Ctrl Pts',(1.23842372552297,0.18387052768763,15.1976834727894));
#9405=CARTESIAN_POINT('Ctrl Pts',(1.23558820930995,0.124705389878211,15.1939335383011));
#9406=CARTESIAN_POINT('Ctrl Pts',(1.23394789713065,0.0440056078309579,15.1888916571596));
#9407=CARTESIAN_POINT('Ctrl Pts',(1.23372608710336,0.022514555349209,15.1875559641337));
#9408=CARTESIAN_POINT('Ctrl Pts',(1.23371462666001,-0.0136080604199647,
15.1853222826256));
#9409=CARTESIAN_POINT('Ctrl Pts',(1.23380961358421,-0.028238636685241,15.1844207208913));
#9410=CARTESIAN_POINT('Ctrl Pts',(1.23419408043649,-0.0571395324266167,
15.1826458122114));
#9411=CARTESIAN_POINT('Ctrl Pts',(1.23447873509014,-0.071409569521203,15.1817723352036));
#9412=CARTESIAN_POINT('Ctrl Pts',(1.23540090362008,-0.106084609192493,15.1796566613541));
#9413=CARTESIAN_POINT('Ctrl Pts',(1.23613752408481,-0.126486524131578,15.1784175837259));
#9414=CARTESIAN_POINT('Ctrl Pts',(1.23878143162324,-0.184437054822519,15.1749133950307));
#9415=CARTESIAN_POINT('Ctrl Pts',(1.24115200196418,-0.221961917583025,15.1726626744533));
#9416=CARTESIAN_POINT('Ctrl Pts',(1.26118947499137,-0.470060513455625,15.1578865352414));
#9417=CARTESIAN_POINT('Ctrl Pts',(1.29887326188963,-0.678506233941155,15.1460172901386));
#9418=CARTESIAN_POINT('Ctrl Pts',(1.41183853977395,-1.07561864602565,15.1229297176025));
#9419=CARTESIAN_POINT('Ctrl Pts',(1.48503205391908,-1.26383240288843,15.1117423904982));
#9420=CARTESIAN_POINT('Ctrl Pts',(1.58972850894977,-1.47273635848952,15.0977960627004));
#9421=CARTESIAN_POINT('Ctrl Pts',(1.60458301744071,-1.50129930081596,15.0958535504836));
#9422=CARTESIAN_POINT('Ctrl Pts',(1.62551873410921,-1.54012323530385,15.0931574200188));
#9423=CARTESIAN_POINT('Ctrl Pts',(1.63123324774054,-1.55058115650156,15.0924255436778));
#9424=CARTESIAN_POINT('Ctrl Pts',(1.64094190856478,-1.56811677064882,15.0911884506177));
#9425=CARTESIAN_POINT('Ctrl Pts',(1.64490513200767,-1.57521161241637,15.0906851816082));
#9426=CARTESIAN_POINT('Ctrl Pts',(1.65251033542968,-1.5887060750483,15.0897225699942));
#9427=CARTESIAN_POINT('Ctrl Pts',(1.65614748294632,-1.59510833012601,15.089263553099));
#9428=CARTESIAN_POINT('Ctrl Pts',(1.66584804882955,-1.61204822646685,15.088042982752));
#9429=CARTESIAN_POINT('Ctrl Pts',(1.67194914113431,-1.62256399669117,15.0872790611312));
#9430=CARTESIAN_POINT('Ctrl Pts',(1.69399197097058,-1.66006628005071,15.0845330333729));
#9431=CARTESIAN_POINT('Ctrl Pts',(1.71026715505651,-1.68685347632025,15.0825312300784));
#9432=CARTESIAN_POINT('Ctrl Pts',(1.91071337332961,-2.00617560505691,15.0582177944138));
#9433=CARTESIAN_POINT('Ctrl Pts',(2.1404070534296,-2.26749335729481,15.0340251349315));
#9434=CARTESIAN_POINT('Ctrl Pts',(2.45578973674155,-2.52732103489233,15.0073554035512));
#9435=CARTESIAN_POINT('Ctrl Pts',(2.5054709995015,-2.56586764738827,15.0033012270454));
#9436=CARTESIAN_POINT('Ctrl Pts',(2.59273778996224,-2.62957485938873,14.9964280145181));
#9437=CARTESIAN_POINT('Ctrl Pts',(2.62978213844828,-2.65544222578176,14.9935831812708));
#9438=CARTESIAN_POINT('Ctrl Pts',(2.68346117704979,-2.69127018339964,14.9895614587708));
#9439=CARTESIAN_POINT('Ctrl Pts',(2.69965945746288,-2.70187198090747,14.9883605837713));
#9440=CARTESIAN_POINT('Ctrl Pts',(2.72792374800866,-2.72000934353825,14.9862868210935));
#9441=CARTESIAN_POINT('Ctrl Pts',(2.73994580118056,-2.72761207613919,14.985411451434));
#9442=CARTESIAN_POINT('Ctrl Pts',(2.76471278104889,-2.7430460881605,14.9836215745742));
#9443=CARTESIAN_POINT('Ctrl Pts',(2.77746269929537,-2.75086873603203,14.9827074000755));
#9444=CARTESIAN_POINT('Ctrl Pts',(2.80999427006611,-2.77051788077464,14.9803929080917));
#9445=CARTESIAN_POINT('Ctrl Pts',(2.82984937697306,-2.78222159658008,14.9789970796022));
#9446=CARTESIAN_POINT('Ctrl Pts',(2.90658767378477,-2.82635315558743,14.9736644679125));
#9447=CARTESIAN_POINT('Ctrl Pts',(2.96433078833044,-2.85725895431166,14.9697820308718));
#9448=CARTESIAN_POINT('Ctrl Pts',(3.32247991218538,-3.03512963210773,14.9463899944093));
#9449=CARTESIAN_POINT('Ctrl Pts',(3.64325821590194,-3.13633417607138,14.9285747587303));
#9450=CARTESIAN_POINT('Ctrl Pts',(4.02008067259177,-3.19341050709871,14.9064421129961));
#9451=CARTESIAN_POINT('Ctrl Pts',(4.06647367522107,-3.19940754882225,14.9036928030104));
#9452=CARTESIAN_POINT('Ctrl Pts',(4.14372488350597,-3.20768839261889,14.8990503451401));
#9453=CARTESIAN_POINT('Ctrl Pts',(4.17451595613227,-3.21054139265349,14.8971830082216));
#9454=CARTESIAN_POINT('Ctrl Pts',(4.21703837289087,-3.21386498274025,14.8945750542911));
#9455=CARTESIAN_POINT('Ctrl Pts',(4.22873943842849,-3.21471528939506,14.8938543723607));
#9456=CARTESIAN_POINT('Ctrl Pts',(4.24851629089258,-3.21604394157425,14.8926307661192));
#9457=CARTESIAN_POINT('Ctrl Pts',(4.25658985448087,-3.2165558118103,14.8921296936226));
#9458=CARTESIAN_POINT('Ctrl Pts',(4.27205319839246,-3.21747775621718,14.8911668677404));
#9459=CARTESIAN_POINT('Ctrl Pts',(4.27944258868239,-3.21789278073207,14.8907054124554));
#9460=CARTESIAN_POINT('Ctrl Pts',(4.2971386335242,-3.21882554029774,14.8895971871766));
#9461=CARTESIAN_POINT('Ctrl Pts',(4.30744639851509,-3.21931922682238,14.8889491110005));
#9462=CARTESIAN_POINT('Ctrl Pts',(4.34466342420592,-3.22092259996151,14.8866004204136));
#9463=CARTESIAN_POINT('Ctrl Pts',(4.37158312577784,-3.22174442899836,14.8848850541916));
#9464=CARTESIAN_POINT('Ctrl Pts',(4.56786252687139,-3.22527502584141,14.8722726155126));
#9465=CARTESIAN_POINT('Ctrl Pts',(4.73717708900132,-3.21496496372012,14.8608360994689));
#9466=CARTESIAN_POINT('Ctrl Pts',(5.05310408032427,-3.17057545326413,14.8392539426337));
#9467=CARTESIAN_POINT('Ctrl Pts',(5.199708300608,-3.13944634936555,14.8291373703244));
#9468=CARTESIAN_POINT('Ctrl Pts',(5.46218627721138,-3.06428781011458,14.8111190377832));
#9469=CARTESIAN_POINT('Ctrl Pts',(5.57871160574097,-3.02355832609254,14.8031532030418));
#9470=CARTESIAN_POINT('Ctrl Pts',(5.71786186011325,-2.96576338706664,14.7936901044114));
#9471=CARTESIAN_POINT('Ctrl Pts',(5.74296188909585,-2.95496202025116,14.7919848855101));
#9472=CARTESIAN_POINT('Ctrl Pts',(5.782437464662,-2.93737603721723,14.7893051412287));
#9473=CARTESIAN_POINT('Ctrl Pts',(5.79690495793689,-2.93080224742148,14.7883234850033));
#9474=CARTESIAN_POINT('Ctrl Pts',(5.82399288132301,-2.91825140470405,14.7864861402352));
#9475=CARTESIAN_POINT('Ctrl Pts',(5.83662418452835,-2.91229883529384,14.7856296360118));
#9476=CARTESIAN_POINT('Ctrl Pts',(5.86492411355093,-2.89873687043178,14.7837110694565));
#9477=CARTESIAN_POINT('Ctrl Pts',(5.88057061663662,-2.89108212581976,14.7826506062509));
#9478=CARTESIAN_POINT('Ctrl Pts',(5.92039992286234,-2.87119461632867,14.7799513276929));
#9479=CARTESIAN_POINT('Ctrl Pts',(5.94449218191281,-2.85878284492059,14.7783187724842));
#9480=CARTESIAN_POINT('Ctrl Pts',(6.11130550442123,-2.77016428376176,14.7670103771462));
#9481=CARTESIAN_POINT('Ctrl Pts',(6.24827579829929,-2.68360428669593,14.757717259926));
#9482=CARTESIAN_POINT('Ctrl Pts',(6.55001980411922,-2.45946846696826,14.7365140861951));
#9483=CARTESIAN_POINT('Ctrl Pts',(6.70870252099457,-2.31503184665385,14.7247919159305));
#9484=CARTESIAN_POINT('Ctrl Pts',(6.88739626311304,-2.11648964026712,14.7093604353198));
#9485=CARTESIAN_POINT('Ctrl Pts',(6.92192467792707,-2.07616556722218,14.7062548041627));
#9486=CARTESIAN_POINT('Ctrl Pts',(6.97686161792159,-2.00870357477332,14.7010703204091));
#9487=CARTESIAN_POINT('Ctrl Pts',(6.99786589367853,-1.98206221511699,14.6990256433661));
#9488=CARTESIAN_POINT('Ctrl Pts',(7.02582199529364,-1.94542827489513,14.6962100995476));
#9489=CARTESIAN_POINT('Ctrl Pts',(7.03314433129875,-1.93571955997157,14.6954635551285));
#9490=CARTESIAN_POINT('Ctrl Pts',(7.04529794709878,-1.91941388284454,14.6942086935522));
#9491=CARTESIAN_POINT('Ctrl Pts',(7.05015946581625,-1.91283944355455,14.693702451636));
#9492=CARTESIAN_POINT('Ctrl Pts',(7.05932510815806,-1.90034517006326,14.6927396914844));
#9493=CARTESIAN_POINT('Ctrl Pts',(7.06363418534541,-1.89442903795944,14.6922835333995));
#9494=CARTESIAN_POINT('Ctrl Pts',(7.07378290543782,-1.88039518146651,14.6912008966535));
#9495=CARTESIAN_POINT('Ctrl Pts',(7.07960495222912,-1.87226490893535,14.6905732421793));
#9496=CARTESIAN_POINT('Ctrl Pts',(7.09982085610025,-1.84375475980464,14.6883710878591));
#9497=CARTESIAN_POINT('Ctrl Pts',(7.11401538606175,-1.82323552237407,14.6867840688754));
#9498=CARTESIAN_POINT('Ctrl Pts',(7.25253334520598,-1.61794305703171,14.6709019690701));
#9499=CARTESIAN_POINT('Ctrl Pts',(7.35761598225156,-1.42093211674223,14.6556723181389));
#9500=CARTESIAN_POINT('Ctrl Pts',(7.52210694239558,-1.01669585332977,14.6262221739974));
#9501=CARTESIAN_POINT('Ctrl Pts',(7.58278629138018,-0.811157564302041,14.6120634215929));
#9502=CARTESIAN_POINT('Ctrl Pts',(7.62872200634747,-0.56919517407018,14.5965321715331));
#9503=CARTESIAN_POINT('Ctrl Pts',(7.63429525706737,-0.537208234686814,14.5944999931617));
#9504=CARTESIAN_POINT('Ctrl Pts',(7.64204608195944,-0.488370007483515,14.5914281901282));
#9505=CARTESIAN_POINT('Ctrl Pts',(7.64457523520442,-0.471577417362987,14.5903775195629));
#9506=CARTESIAN_POINT('Ctrl Pts',(7.64874768915267,-0.442304685051345,14.5885554096294));
#9507=CARTESIAN_POINT('Ctrl Pts',(7.65045080476814,-0.429833574697313,14.5877820986514));
#9508=CARTESIAN_POINT('Ctrl Pts',(7.65411850280738,-0.401750517229236,14.5860472468449));
#9509=CARTESIAN_POINT('Ctrl Pts',(7.65604190868923,-0.38613344458636,14.585087021143));
#9510=CARTESIAN_POINT('Ctrl Pts',(7.66090994278541,-0.344070496015452,14.5825125617611));
#9511=CARTESIAN_POINT('Ctrl Pts',(7.66364159074693,-0.317600850537358,14.5809050343077));
#9512=CARTESIAN_POINT('Ctrl Pts',(7.67482275501954,-0.194320799569486,14.5734726957604));
#9513=CARTESIAN_POINT('Ctrl Pts',(7.67921910621768,-0.0971890396789468,
14.5677751526768));
#9514=CARTESIAN_POINT('Ctrl Pts',(7.67921910621823,-1.84544675223763E-11,
14.5621759541225));
#9515=CARTESIAN_POINT('Origin',(4.45646910621825,-5.13094777615093E-16,
-2.31077344927308));
#9516=CARTESIAN_POINT('',(7.67921910621823,-2.34781276219209E-11,13.3169799747702));
#9517=CARTESIAN_POINT('',(7.67921910621823,1.97331828652831E-11,13.5632093210196));
#9518=CARTESIAN_POINT('',(7.67921910621823,-3.51191647465084E-13,-2.31077344927308));
#9519=CARTESIAN_POINT('Ctrl Pts',(7.67921910621823,1.97331828652831E-11,
13.5632093210196));
#9520=CARTESIAN_POINT('Ctrl Pts',(7.67921910621822,-0.0872823144129474,
13.568890915301));
#9521=CARTESIAN_POINT('Ctrl Pts',(7.67567332283278,-0.174534833379368,13.5744749122219));
#9522=CARTESIAN_POINT('Ctrl Pts',(7.66650491624969,-0.287135839366412,13.5815600653288));
#9523=CARTESIAN_POINT('Ctrl Pts',(7.66411522062897,-0.312703306593041,13.583160841812));
#9524=CARTESIAN_POINT('Ctrl Pts',(7.65979000297505,-0.353686357435978,13.5857145189396));
#9525=CARTESIAN_POINT('Ctrl Pts',(7.6580481884606,-0.369120848326992,13.5866734535385));
#9526=CARTESIAN_POINT('Ctrl Pts',(7.65452124211246,-0.398468098647805,13.5884916497737));
#9527=CARTESIAN_POINT('Ctrl Pts',(7.65275673681869,-0.412382931066173,13.5893515379531));
#9528=CARTESIAN_POINT('Ctrl Pts',(7.64851855997497,-0.444142289377875,13.5913093328706));
#9529=CARTESIAN_POINT('Ctrl Pts',(7.64598598158508,-0.461978582462665,13.5924053585139));
#9530=CARTESIAN_POINT('Ctrl Pts',(7.63769445834384,-0.517051740537311,13.595779447273));
#9531=CARTESIAN_POINT('Ctrl Pts',(7.6314318304972,-0.554210358562995,13.5980416257949));
#9532=CARTESIAN_POINT('Ctrl Pts',(7.59762418271365,-0.735358737667528,13.6090114158656));
#9533=CARTESIAN_POINT('Ctrl Pts',(7.56092703528893,-0.877471202577492,13.6174257117409));
#9534=CARTESIAN_POINT('Ctrl Pts',(7.45762995869177,-1.18821533969688,13.6359094813931));
#9535=CARTESIAN_POINT('Ctrl Pts',(7.38624228015617,-1.35471305534666,13.6458690665646));
#9536=CARTESIAN_POINT('Ctrl Pts',(7.24888199481941,-1.61275477940762,13.6625025044014));
#9537=CARTESIAN_POINT('Ctrl Pts',(7.19142734031945,-1.70837519428772,13.6689657509572));
#9538=CARTESIAN_POINT('Ctrl Pts',(7.11990623727849,-1.814522909026,13.6767164889205));
#9539=CARTESIAN_POINT('Ctrl Pts',(7.11056557345264,-1.82815826858343,13.6777235505348));
#9540=CARTESIAN_POINT('Ctrl Pts',(7.09533277420137,-1.8500320755244,13.6793586503808));
#9541=CARTESIAN_POINT('Ctrl Pts',(7.08950582657601,-1.8583158400676,13.6799824564271));
#9542=CARTESIAN_POINT('Ctrl Pts',(7.07909719814258,-1.87296582292038,13.6810940907671));
#9543=CARTESIAN_POINT('Ctrl Pts',(7.07453120105153,-1.87934295650837,13.6815808517866));
#9544=CARTESIAN_POINT('Ctrl Pts',(7.06458744256367,-1.89312441388107,13.6826390744354));
#9545=CARTESIAN_POINT('Ctrl Pts',(7.05920149663022,-1.90052240235201,13.6832110776686));
#9546=CARTESIAN_POINT('Ctrl Pts',(7.04395270755118,-1.92128133477971,13.6848270253689));
#9547=CARTESIAN_POINT('Ctrl Pts',(7.03401815580536,-1.93458890313138,13.6858757181601));
#9548=CARTESIAN_POINT('Ctrl Pts',(6.97047713496943,-2.01834533800077,13.6925543542624));
#9549=CARTESIAN_POINT('Ctrl Pts',(6.91409443833061,-2.0866310235974,13.6983519820784));
#9550=CARTESIAN_POINT('Ctrl Pts',(6.66069352322214,-2.36899282757778,13.7235884407757));
#9551=CARTESIAN_POINT('Ctrl Pts',(6.43794545911826,-2.55822758520408,13.7436454060561));
#9552=CARTESIAN_POINT('Ctrl Pts',(6.1221650285876,-2.76018289956538,13.7680056350018));
#9553=CARTESIAN_POINT('Ctrl Pts',(6.04976318727673,-2.80260032591528,13.7733654656271));
#9554=CARTESIAN_POINT('Ctrl Pts',(5.95352273291203,-2.85404714757985,13.780206794908));
#9555=CARTESIAN_POINT('Ctrl Pts',(5.93112294350223,-2.86568504902897,13.7817799180098));
#9556=CARTESIAN_POINT('Ctrl Pts',(5.89480748850041,-2.88401431121457,13.7843001608354));
#9557=CARTESIAN_POINT('Ctrl Pts',(5.88097678090408,-2.8908707593447,13.7852530364967));
#9558=CARTESIAN_POINT('Ctrl Pts',(5.85446553563167,-2.9037770089866,13.7870665023599));
#9559=CARTESIAN_POINT('Ctrl Pts',(5.84179369279982,-2.90984376457854,13.7879276667447));
#9560=CARTESIAN_POINT('Ctrl Pts',(5.812617034622,-2.92357855136183,13.789897791958));
#9561=CARTESIAN_POINT('Ctrl Pts',(5.79608603267887,-2.93119007591118,13.7910047842005));
#9562=CARTESIAN_POINT('Ctrl Pts',(5.7442456253661,-2.95452927572253,13.7944481923671));
#9563=CARTESIAN_POINT('Ctrl Pts',(5.70871638456807,-2.96976237277451,13.7967677452789));
#9564=CARTESIAN_POINT('Ctrl Pts',(5.53002626094137,-3.04259820800698,13.8082469337431));
#9565=CARTESIAN_POINT('Ctrl Pts',(5.38312525025187,-3.09050887185996,13.8170794854008));
#9566=CARTESIAN_POINT('Ctrl Pts',(4.98413433007395,-3.1896117236503,13.8402389650523));
#9567=CARTESIAN_POINT('Ctrl Pts',(4.72845711729497,-3.22149686421932,13.8542000824417));
#9568=CARTESIAN_POINT('Ctrl Pts',(4.43528713460996,-3.2228866225644,13.8716218407371));
#9569=CARTESIAN_POINT('Ctrl Pts',(4.39882946673899,-3.22244073265954,13.8738144113679));
#9570=CARTESIAN_POINT('Ctrl Pts',(4.34947596861523,-3.22099936655052,13.8768272266492));
#9571=CARTESIAN_POINT('Ctrl Pts',(4.33656558512677,-3.2205446097503,13.8776194948264));
#9572=CARTESIAN_POINT('Ctrl Pts',(4.31615380471127,-3.21970271849754,13.8788791466167));
#9573=CARTESIAN_POINT('Ctrl Pts',(4.30865026646491,-3.21936695131815,13.8793437119217));
#9574=CARTESIAN_POINT('Ctrl Pts',(4.29315179479551,-3.2186191305319,13.8803065055505));
#9575=CARTESIAN_POINT('Ctrl Pts',(4.285157194394,-3.21820351671839,13.8808049409972));
#9576=CARTESIAN_POINT('Ctrl Pts',(4.26590199833611,-3.21713054983919,13.8820096480538));
#9577=CARTESIAN_POINT('Ctrl Pts',(4.25464319797041,-3.21644385792047,13.8827175255939));
#9578=CARTESIAN_POINT('Ctrl Pts',(4.21546791356717,-3.21384799981331,13.8851921332886));
#9579=CARTESIAN_POINT('Ctrl Pts',(4.1875737559046,-3.21163442938975,13.8869745266135));
#9580=CARTESIAN_POINT('Ctrl Pts',(4.11898393503,-3.20529162027661,13.8914018059873));
#9581=CARTESIAN_POINT('Ctrl Pts',(4.07833203372368,-3.20075032674342,13.894064420926));
#9582=CARTESIAN_POINT('Ctrl Pts',(3.90967964896791,-3.17865225502166,13.9052429966878));
#9583=CARTESIAN_POINT('Ctrl Pts',(3.78271202267294,-3.15418080149188,13.9139716859022));
#9584=CARTESIAN_POINT('Ctrl Pts',(3.41468177254106,-3.0600083179504,13.9396714385325));
#9585=CARTESIAN_POINT('Ctrl Pts',(3.17983557867515,-2.96971770234912,13.956509610083));
#9586=CARTESIAN_POINT('Ctrl Pts',(2.92223568691936,-2.8344064197869,13.9749596834051));
#9587=CARTESIAN_POINT('Ctrl Pts',(2.88701639955016,-2.81505779217045,13.9774843074672));
#9588=CARTESIAN_POINT('Ctrl Pts',(2.83631091692538,-2.78595391949007,13.9811236388135));
#9589=CARTESIAN_POINT('Ctrl Pts',(2.8205324800884,-2.77671805864701,13.982256793438));
#9590=CARTESIAN_POINT('Ctrl Pts',(2.79272218323632,-2.76012004511184,13.9842555100907));
#9591=CARTESIAN_POINT('Ctrl Pts',(2.78065857237513,-2.75281229869889,13.9851230161558));
#9592=CARTESIAN_POINT('Ctrl Pts',(2.75565150762454,-2.73743851693216,13.9869225177319));
#9593=CARTESIAN_POINT('Ctrl Pts',(2.74271653094874,-2.72935931327512,13.9878540024717));
#9594=CARTESIAN_POINT('Ctrl Pts',(2.70924498137342,-2.70812117474639,13.9902665023559));
#9595=CARTESIAN_POINT('Ctrl Pts',(2.6887993378901,-2.69482023141235,13.9917422327826));
#9596=CARTESIAN_POINT('Ctrl Pts',(2.59818717011898,-2.63439733689004,13.9982945228518));
#9597=CARTESIAN_POINT('Ctrl Pts',(2.52973610666055,-2.5847558562676,14.003275811716));
#9598=CARTESIAN_POINT('Ctrl Pts',(2.34182948526469,-2.43686604809397,14.0171407075722));
#9599=CARTESIAN_POINT('Ctrl Pts',(2.22737876835255,-2.3326332230422,14.0258092319487));
#9600=CARTESIAN_POINT('Ctrl Pts',(1.9755638832424,-2.06777304689273,14.0462465174096));
#9601=CARTESIAN_POINT('Ctrl Pts',(1.84564662558299,-1.90109383463384,14.0579403396425));
#9602=CARTESIAN_POINT('Ctrl Pts',(1.71926191110106,-1.70131419510654,14.0721308791342));
#9603=CARTESIAN_POINT('Ctrl Pts',(1.70583135091994,-1.67951334187961,14.0736818892604));
#9604=CARTESIAN_POINT('Ctrl Pts',(1.68746187484791,-1.64888409401837,14.0758677795365));
#9605=CARTESIAN_POINT('Ctrl Pts',(1.68230220318664,-1.64018833999965,14.0764891153684));
#9606=CARTESIAN_POINT('Ctrl Pts',(1.67346394745453,-1.62513194472003,14.0775664912129));
#9607=CARTESIAN_POINT('Ctrl Pts',(1.66976600188284,-1.61878267756716,14.078021293668));
#9608=CARTESIAN_POINT('Ctrl Pts',(1.66201448473906,-1.60536826899351,14.0789832951336));
#9609=CARTESIAN_POINT('Ctrl Pts',(1.65796594985724,-1.59830034405348,14.0794908214991));
#9610=CARTESIAN_POINT('Ctrl Pts',(1.64801652968044,-1.58077696921104,14.080750600314));
#9611=CARTESIAN_POINT('Ctrl Pts',(1.64214723363691,-1.57030382024321,14.081504823357));
#9612=CARTESIAN_POINT('Ctrl Pts',(1.62045746967877,-1.53108848997792,14.0843330285229));
#9613=CARTESIAN_POINT('Ctrl Pts',(1.60501827907145,-1.50213912565454,14.0864290521794));
#9614=CARTESIAN_POINT('Ctrl Pts',(1.49360584154234,-1.28532571022899,14.1021596815978));
#9615=CARTESIAN_POINT('Ctrl Pts',(1.41585033477799,-1.08869063139299,14.1165700249028));
#9616=CARTESIAN_POINT('Ctrl Pts',(1.30264064159823,-0.69271164662861,14.1443671150533));
#9617=CARTESIAN_POINT('Ctrl Pts',(1.26559002447791,-0.494770768667403,14.157706669747));
#9618=CARTESIAN_POINT('Ctrl Pts',(1.24339255104212,-0.252993440710904,14.1731184079337));
#9619=CARTESIAN_POINT('Ctrl Pts',(1.24037988709977,-0.211274771900807,14.1757482061316));
#9620=CARTESIAN_POINT('Ctrl Pts',(1.23720302558135,-0.150958562652312,14.1795094239339));
#9621=CARTESIAN_POINT('Ctrl Pts',(1.2363864109681,-0.132401074333798,14.1806610707089));
#9622=CARTESIAN_POINT('Ctrl Pts',(1.23523044362633,-0.0996958830725559,
14.1826811787533));
#9623=CARTESIAN_POINT('Ctrl Pts',(1.23482375146724,-0.0855512059513194,
14.1835517214522));
#9624=CARTESIAN_POINT('Ctrl Pts',(1.23417510248544,-0.0562823048112054,
14.1853467873184));
#9625=CARTESIAN_POINT('Ctrl Pts',(1.2339464350297,-0.0411581126778235,14.1862708739258));
#9626=CARTESIAN_POINT('Ctrl Pts',(1.23363186519905,-0.00221677478436835,
14.1886415319656));
#9627=CARTESIAN_POINT('Ctrl Pts',(1.23370348643724,0.0216009887060091,14.1900831643403));
#9628=CARTESIAN_POINT('Ctrl Pts',(1.23514912816945,0.124173905957879,14.1962581319088));
#9629=CARTESIAN_POINT('Ctrl Pts',(1.23914608551795,0.202868489030255,14.2009095787873));
#9630=CARTESIAN_POINT('Ctrl Pts',(1.25806380988224,0.418741700692692,14.2135087402557));
#9631=CARTESIAN_POINT('Ctrl Pts',(1.27891322663128,0.555233070420645,14.2212900489046));
#9632=CARTESIAN_POINT('Ctrl Pts',(1.35513367409847,0.9029902144834,14.2412310431853));
#9633=CARTESIAN_POINT('Ctrl Pts',(1.42331623848131,1.11069070407474,14.2532403999187));
#9634=CARTESIAN_POINT('Ctrl Pts',(1.5272913634106,1.34441942648955,14.2684247357883));
#9635=CARTESIAN_POINT('Ctrl Pts',(1.5432576493015,1.37867493237495,14.2706956182593));
#9636=CARTESIAN_POINT('Ctrl Pts',(1.56556566102557,1.42441796698323,14.2738001353051));
#9637=CARTESIAN_POINT('Ctrl Pts',(1.57138119976016,1.4361605176657,14.2746035790639));
#9638=CARTESIAN_POINT('Ctrl Pts',(1.58065897591155,1.4546101279565,14.2758767031226));
#9639=CARTESIAN_POINT('Ctrl Pts',(1.584073516023,1.4613411992434,14.2763434587789));
#9640=CARTESIAN_POINT('Ctrl Pts',(1.59114792633489,1.47516637024125,14.2773069599709));
#9641=CARTESIAN_POINT('Ctrl Pts',(1.59481051882663,1.4822588867892,14.2778038887315));
#9642=CARTESIAN_POINT('Ctrl Pts',(1.6036514997011,1.49922431882597,14.2789987788665));
#9643=CARTESIAN_POINT('Ctrl Pts',(1.6088548181716,1.50908406396157,14.2796982811521));
#9644=CARTESIAN_POINT('Ctrl Pts',(1.62691489610489,1.54288002658651,14.2821129069378));
#9645=CARTESIAN_POINT('Ctrl Pts',(1.64002274789877,1.56667980193364,14.2838427232106));
#9646=CARTESIAN_POINT('Ctrl Pts',(1.6728397651505,1.62452223360079,14.2881140279753));
#9647=CARTESIAN_POINT('Ctrl Pts',(1.69287397612027,1.65837464753388,14.2906717569573));
#9648=CARTESIAN_POINT('Ctrl Pts',(1.7769848521379,1.79474114538311,14.3011882588007));
#9649=CARTESIAN_POINT('Ctrl Pts',(1.84618332021367,1.89397367822122,14.309337550426));
#9650=CARTESIAN_POINT('Ctrl Pts',(2.08341938738767,2.19640280943998,14.3353319242764));
#9651=CARTESIAN_POINT('Ctrl Pts',(2.27089900362723,2.38304115681519,14.3530775343362));
#9652=CARTESIAN_POINT('Ctrl Pts',(2.50678977521358,2.56634032846529,14.3720047737299));
#9653=CARTESIAN_POINT('Ctrl Pts',(2.53488662616988,2.5874452852819,14.3742133498339));
#9654=CARTESIAN_POINT('Ctrl Pts',(2.5777100126057,2.61852970877647,14.3775123641553));
#9655=CARTESIAN_POINT('Ctrl Pts',(2.5921824736702,2.62885316052389,14.3786160207957));
#9656=CARTESIAN_POINT('Ctrl Pts',(2.61747801353977,2.64658294391563,14.3805258060782));
#9657=CARTESIAN_POINT('Ctrl Pts',(2.62826213955876,2.65404386043874,14.3813340100135));
#9658=CARTESIAN_POINT('Ctrl Pts',(2.65087756232357,2.66948692053903,14.3830165861445));
#9659=CARTESIAN_POINT('Ctrl Pts',(2.66271696903669,2.67745672663395,14.3838904788468));
#9660=CARTESIAN_POINT('Ctrl Pts',(2.6909622973422,2.69619888839839,14.3859591177908));
#9661=CARTESIAN_POINT('Ctrl Pts',(2.70741456777154,2.70690062356626,14.3871512024184));
#9662=CARTESIAN_POINT('Ctrl Pts',(2.76340019145648,2.74259413411238,14.3911655337118));
#9663=CARTESIAN_POINT('Ctrl Pts',(2.80338056406409,2.76687613409256,14.3939616750454));
#9664=CARTESIAN_POINT('Ctrl Pts',(3.04430364074229,2.90611328492733,14.4104269685823));
#9665=CARTESIAN_POINT('Ctrl Pts',(3.25662871095167,3.00001693761937,14.4233125400605));
#9666=CARTESIAN_POINT('Ctrl Pts',(3.64921270157713,3.12522841372324,14.4463650118354));
#9667=CARTESIAN_POINT('Ctrl Pts',(3.82551000751064,3.16553150731771,14.4564878544845));
#9668=CARTESIAN_POINT('Ctrl Pts',(4.0308060223305,3.19462816425958,14.4689188765829));
#9669=CARTESIAN_POINT('Ctrl Pts',(4.05742956440232,3.19806277399873,14.4705434350207));
#9670=CARTESIAN_POINT('Ctrl Pts',(4.09433116658667,3.20235537320779,14.472816209741));
#9671=CARTESIAN_POINT('Ctrl Pts',(4.10457592083184,3.20349730810074,14.4734494258226));
#9672=CARTESIAN_POINT('Ctrl Pts',(4.12218275386761,3.20537438325845,14.4745417997836));
#9673=CARTESIAN_POINT('Ctrl Pts',(4.12954228431856,3.20613336477755,14.4749996382791));
#9674=CARTESIAN_POINT('Ctrl Pts',(4.14495826731517,3.2076695700567,14.4759613758462));
#9675=CARTESIAN_POINT('Ctrl Pts',(4.15301508878348,3.20844179122328,14.4764655618908));
#9676=CARTESIAN_POINT('Ctrl Pts',(4.17277411163566,3.21026054256094,14.4777057335754));
#9677=CARTESIAN_POINT('Ctrl Pts',(4.18447922540539,3.21127343833726,14.4784435596951));
#9678=CARTESIAN_POINT('Ctrl Pts',(4.22711989960889,3.21472852366581,14.4811422412636));
#9679=CARTESIAN_POINT('Ctrl Pts',(4.25808367459332,3.21678777574895,14.4831226705108));
#9680=CARTESIAN_POINT('Ctrl Pts',(4.33600568986535,3.22084072156798,14.488150720113));
#9681=CARTESIAN_POINT('Ctrl Pts',(4.38298586218097,3.22225482416824,14.491222436927));
#9682=CARTESIAN_POINT('Ctrl Pts',(4.77014741194583,3.2254374548829,14.5167819394477));
#9683=CARTESIAN_POINT('Ctrl Pts',(5.10864669690037,3.17436463155494,14.5403858485047));
#9684=CARTESIAN_POINT('Ctrl Pts',(5.49079332467771,3.05286328757666,14.5661432515988));
#9685=CARTESIAN_POINT('Ctrl Pts',(5.54810227181103,3.03284333120434,14.5699910357038));
#9686=CARTESIAN_POINT('Ctrl Pts',(5.62572727920928,3.00324055275362,14.5751851623551));
#9687=CARTESIAN_POINT('Ctrl Pts',(5.6465564439084,2.99504768944647,14.5765771713108));
#9688=CARTESIAN_POINT('Ctrl Pts',(5.67965814263576,2.98162774304877,14.5787869829935));
#9689=CARTESIAN_POINT('Ctrl Pts',(5.69198621008855,2.97654042665313,14.5796094557429));
#9690=CARTESIAN_POINT('Ctrl Pts',(5.71730803757016,2.96590666364735,14.5812978638825));
#9691=CARTESIAN_POINT('Ctrl Pts',(5.73029763350956,2.96035099969067,14.5821634650598));
#9692=CARTESIAN_POINT('Ctrl Pts',(5.7594995317123,2.94763352243498,14.5841084590075));
#9693=CARTESIAN_POINT('Ctrl Pts',(5.77569021482703,2.94042298970787,14.5851861650754));
#9694=CARTESIAN_POINT('Ctrl Pts',(5.82715044061085,2.9169945383745,14.5886100426635));
#9695=CARTESIAN_POINT('Ctrl Pts',(5.86218761109995,2.90027242464741,14.5909389301721));
#9696=CARTESIAN_POINT('Ctrl Pts',(5.94348495925571,2.85965235148318,14.5963436891206));
#9697=CARTESIAN_POINT('Ctrl Pts',(5.98948563832835,2.83525809175234,14.5994025733774));
#9698=CARTESIAN_POINT('Ctrl Pts',(6.15408612860223,2.7427922610927,14.6103815486283));
#9699=CARTESIAN_POINT('Ctrl Pts',(6.26891874587849,2.66830344494869,14.6180989555965));
#9700=CARTESIAN_POINT('Ctrl Pts',(6.55074403205544,2.45887895294038,14.6377694321812));
#9701=CARTESIAN_POINT('Ctrl Pts',(6.70960348816129,2.31418194151873,14.6495754499166));
#9702=CARTESIAN_POINT('Ctrl Pts',(6.88103364429328,2.12352867794647,14.6647409153597));
#9703=CARTESIAN_POINT('Ctrl Pts',(6.90854439162075,2.09170114012658,14.6672622685669));
#9704=CARTESIAN_POINT('Ctrl Pts',(6.94415327203489,2.04883667509095,14.6706585851679));
#9705=CARTESIAN_POINT('Ctrl Pts',(6.95281663386567,2.03827212018418,14.6714957055672));
#9706=CARTESIAN_POINT('Ctrl Pts',(6.96676269838553,2.02104328456586,14.6728615701919));
#9707=CARTESIAN_POINT('Ctrl Pts',(6.97208676148357,2.014412491411,14.673387405667));
#9708=CARTESIAN_POINT('Ctrl Pts',(6.98239284779177,2.00147231888601,14.6744140713768));
#9709=CARTESIAN_POINT('Ctrl Pts',(6.9873775846459,1.99516527134056,14.6749147031086));
#9710=CARTESIAN_POINT('Ctrl Pts',(6.99941336172188,1.97981905774341,14.6761332759717));
#9711=CARTESIAN_POINT('Ctrl Pts',(7.00643983398527,1.97076083434401,14.6768529147233));
#9712=CARTESIAN_POINT('Ctrl Pts',(7.0311616626226,1.93853696858531,14.6794136829932));
#9713=CARTESIAN_POINT('Ctrl Pts',(7.04859028609062,1.91516970235062,14.6812719259126));
#9714=CARTESIAN_POINT('Ctrl Pts',(7.09105582808355,1.85659278422195,14.6859268063001));
#9715=CARTESIAN_POINT('Ctrl Pts',(7.11570576171344,1.82111065313819,14.688743466472));
#9716=CARTESIAN_POINT('Ctrl Pts',(7.26461568675241,1.59729145278992,14.7064420458323));
#9717=CARTESIAN_POINT('Ctrl Pts',(7.36952265379383,1.3968349644446,14.7219424101969));
#9718=CARTESIAN_POINT('Ctrl Pts',(7.48827060509728,1.09711361525992,14.7435037122974));
#9719=CARTESIAN_POINT('Ctrl Pts',(7.51984179616873,1.00559879559793,14.7498970662721));
#9720=CARTESIAN_POINT('Ctrl Pts',(7.56977246922604,0.836530558452999,14.7613300555828));
#9721=CARTESIAN_POINT('Ctrl Pts',(7.58946666073998,0.759453290113551,14.7664044723514));
#9722=CARTESIAN_POINT('Ctrl Pts',(7.6115247142054,0.657536273701604,14.7729387032276));
#9723=CARTESIAN_POINT('Ctrl Pts',(7.61648037024327,0.633291960173989,14.7744803292275));
#9724=CARTESIAN_POINT('Ctrl Pts',(7.62405286212141,0.593940782413684,14.7769624828522));
#9725=CARTESIAN_POINT('Ctrl Pts',(7.62684192522217,0.578868469647898,14.7779084559418));
#9726=CARTESIAN_POINT('Ctrl Pts',(7.63198637842811,0.549914396956638,14.7797167870231));
#9727=CARTESIAN_POINT('Ctrl Pts',(7.63435853079836,0.536036011064709,14.7805796581345));
#9728=CARTESIAN_POINT('Ctrl Pts',(7.63886555511494,0.508585439083418,14.782278835495));
#9729=CARTESIAN_POINT('Ctrl Pts',(7.64100473704754,0.495014274410429,14.7831152608139));
#9730=CARTESIAN_POINT('Ctrl Pts',(7.64573174625454,0.463726151964611,14.7850355122205));
#9731=CARTESIAN_POINT('Ctrl Pts',(7.64825885707549,0.446000377970389,14.7861174202155));
#9732=CARTESIAN_POINT('Ctrl Pts',(7.6572019822485,0.379297344009631,14.7901671597348));
#9733=CARTESIAN_POINT('Ctrl Pts',(7.66263964684926,0.330194287256672,14.7931046605912));
#9734=CARTESIAN_POINT('Ctrl Pts',(7.67512411768421,0.187548556376506,14.8015302425086));
#9735=CARTESIAN_POINT('Ctrl Pts',(7.67921910621824,0.0937987030144953,14.806932435509));
#9736=CARTESIAN_POINT('Ctrl Pts',(7.67921910621823,2.3786865083016E-11,
14.8122635502411));
#9737=CARTESIAN_POINT('Ctrl Pts',(7.67921910621823,-1.84544675223763E-11,
14.5621759541225));
#9738=CARTESIAN_POINT('Ctrl Pts',(7.67921910621823,0.000668280097381219,
14.5621374535563));
#9739=CARTESIAN_POINT('Ctrl Pts',(7.67921889835307,0.00133656291538531,
14.5620989575348));
#9740=CARTESIAN_POINT('Ctrl Pts',(7.67909503873809,0.200438155357122,14.5506312262009));
#9741=CARTESIAN_POINT('Ctrl Pts',(7.66064549735702,0.398434351142203,14.5396726513469));
#9742=CARTESIAN_POINT('Ctrl Pts',(7.59450626321197,0.751444354318352,14.5195032484083));
#9743=CARTESIAN_POINT('Ctrl Pts',(7.55313980900694,0.906952413113773,14.5103727338205));
#9744=CARTESIAN_POINT('Ctrl Pts',(7.49482381008865,1.07461718896952,14.499627873536));
#9745=CARTESIAN_POINT('Ctrl Pts',(7.48916459758958,1.09048587261971,14.4986016757321));
#9746=CARTESIAN_POINT('Ctrl Pts',(7.47990966549629,1.11580779055098,14.4969482174958));
#9747=CARTESIAN_POINT('Ctrl Pts',(7.4763933298234,1.12528997071433,14.4963254554595));
#9748=CARTESIAN_POINT('Ctrl Pts',(7.4700656187829,1.14211005158411,14.4952140904344));
#9749=CARTESIAN_POINT('Ctrl Pts',(7.46727196151491,1.1494544251454,14.4947265407459));
#9750=CARTESIAN_POINT('Ctrl Pts',(7.46120453016421,1.16523148696397,14.4936742033071));
#9751=CARTESIAN_POINT('Ctrl Pts',(7.45792216103014,1.17366048803549,14.4931089300761));
#9752=CARTESIAN_POINT('Ctrl Pts',(7.44869059052325,1.19707481208954,14.4915304087946));
#9753=CARTESIAN_POINT('Ctrl Pts',(7.44266444810608,1.21202923719652,14.4905127476183));
#9754=CARTESIAN_POINT('Ctrl Pts',(7.40643337908578,1.3000293753218,14.4844708098356));
#9755=CARTESIAN_POINT('Ctrl Pts',(7.37366389448707,1.37198321574115,14.4793127284117));
#9756=CARTESIAN_POINT('Ctrl Pts',(7.24302226894476,1.63295050469672,14.4599721949457));
#9757=CARTESIAN_POINT('Ctrl Pts',(7.12914480878979,1.81334320822728,14.4453784097787));
#9758=CARTESIAN_POINT('Ctrl Pts',(6.89801354792347,2.10988108581692,14.4202523384195));
#9759=CARTESIAN_POINT('Ctrl Pts',(6.78807410901351,2.23077781869281,14.4095932249652));
#9760=CARTESIAN_POINT('Ctrl Pts',(6.64970414225297,2.36147711178539,14.3976115866561));
#9761=CARTESIAN_POINT('Ctrl Pts',(6.62974004158838,2.37986293442126,14.3959138685314));
#9762=CARTESIAN_POINT('Ctrl Pts',(6.59657628207801,2.40963952479686,14.3931433638542));
#9763=CARTESIAN_POINT('Ctrl Pts',(6.58351253480578,2.42117897637548,14.3920643514368));
#9764=CARTESIAN_POINT('Ctrl Pts',(6.55981500428074,2.44177161036826,14.3901288409292));
#9765=CARTESIAN_POINT('Ctrl Pts',(6.5492148540294,2.45086266625679,14.3892707831063));
#9766=CARTESIAN_POINT('Ctrl Pts',(6.52643290943104,2.47014567776588,14.3874428564832));
#9767=CARTESIAN_POINT('Ctrl Pts',(6.5142341506277,2.48031708701237,14.3864738421072));
#9768=CARTESIAN_POINT('Ctrl Pts',(6.48087453751981,2.50771704520668,14.3838498863127));
#9769=CARTESIAN_POINT('Ctrl Pts',(6.45956897233869,2.52476793486275,14.3822021125532));
#9770=CARTESIAN_POINT('Ctrl Pts',(6.34128348057619,2.61699215112238,14.3732017676736));
#9771=CARTESIAN_POINT('Ctrl Pts',(6.2402822093321,2.68685482957355,14.3660604271901));
#9772=CARTESIAN_POINT('Ctrl Pts',(6.00739120865093,2.82900978486206,14.3504845664106));
#9773=CARTESIAN_POINT('Ctrl Pts',(5.87393719635609,2.89817905703745,14.342139651112));
#9774=CARTESIAN_POINT('Ctrl Pts',(5.58045190647431,3.02515431194848,14.3242352231939));
#9775=CARTESIAN_POINT('Ctrl Pts',(5.41969959233771,3.08010858363322,14.3146850043082));
#9776=CARTESIAN_POINT('Ctrl Pts',(5.2293016041149,3.12882930852328,14.3029033625162));
#9777=CARTESIAN_POINT('Ctrl Pts',(5.20312827659499,3.13517828639295,14.3012735630718));
#9778=CARTESIAN_POINT('Ctrl Pts',(5.16682087539358,3.14350511734529,14.298994752286));
#9779=CARTESIAN_POINT('Ctrl Pts',(5.15675145022703,3.14576361010987,14.2983608491235));
#9780=CARTESIAN_POINT('Ctrl Pts',(5.1394421296764,3.14955872910914,14.2972676368545));
#9781=CARTESIAN_POINT('Ctrl Pts',(5.13220739548798,3.1511188648941,14.2968096520904));
#9782=CARTESIAN_POINT('Ctrl Pts',(5.11705348761897,3.1543321455049,14.295848021324));
#9783=CARTESIAN_POINT('Ctrl Pts',(5.10913341072838,3.15598040387741,14.2953440909324));
#9784=CARTESIAN_POINT('Ctrl Pts',(5.08971250748114,3.15994588523639,14.2941052488143));
#9785=CARTESIAN_POINT('Ctrl Pts',(5.07820513617605,3.16223014689314,14.2933685048975));
#9786=CARTESIAN_POINT('Ctrl Pts',(5.03632261131575,3.17030655896598,14.2906778680443));
#9787=CARTESIAN_POINT('Ctrl Pts',(5.0058780464719,3.17572407766685,14.2887045480987));
#9788=CARTESIAN_POINT('Ctrl Pts',(4.92919639643872,3.18823374560923,14.2836983456709));
#9789=CARTESIAN_POINT('Ctrl Pts',(4.8828749841513,3.19475869056921,14.2806416142801));
#9790=CARTESIAN_POINT('Ctrl Pts',(4.50445092510337,3.2396881446224,14.2554882161959));
#9791=CARTESIAN_POINT('Ctrl Pts',(4.16833193024383,3.22721804051266,14.2322958511351));
#9792=CARTESIAN_POINT('Ctrl Pts',(3.7758054286254,3.15073045182821,14.2065419024282));
#9793=CARTESIAN_POINT('Ctrl Pts',(3.71192576680821,3.13624961335846,14.2023831248437));
#9794=CARTESIAN_POINT('Ctrl Pts',(3.62621624185979,3.11405345719717,14.1968440555202));
#9795=CARTESIAN_POINT('Ctrl Pts',(3.60396686911272,3.10803615376427,14.1954098886343));
#9796=CARTESIAN_POINT('Ctrl Pts',(3.56738673451449,3.09772075038639,14.1930576787443));
#9797=CARTESIAN_POINT('Ctrl Pts',(3.55301823141858,3.09356070570831,14.192135200289));
#9798=CARTESIAN_POINT('Ctrl Pts',(3.5250441141134,3.08524996810971,14.1903418859184));
#9799=CARTESIAN_POINT('Ctrl Pts',(3.51143600937368,3.08110894609963,14.1894707591095));
#9800=CARTESIAN_POINT('Ctrl Pts',(3.47937377395767,3.07111982952666,14.1874209863259));
#9801=CARTESIAN_POINT('Ctrl Pts',(3.46094390837154,3.0651952468612,14.1862448700069));
#9802=CARTESIAN_POINT('Ctrl Pts',(3.39968995235336,3.04489341262478,14.1823420712968));
#9803=CARTESIAN_POINT('Ctrl Pts',(3.35711372971005,3.02978153228021,14.1796395215578));
#9804=CARTESIAN_POINT('Ctrl Pts',(3.25608422394308,2.99151215891566,14.1732404660703));
#9805=CARTESIAN_POINT('Ctrl Pts',(3.19796254262301,2.96752940763584,14.1695706095977));
#9806=CARTESIAN_POINT('Ctrl Pts',(2.82507814161248,2.80073848069028,14.145996914924));
#9807=CARTESIAN_POINT('Ctrl Pts',(2.53439989466032,2.60981708533835,14.1277329016664));
#9808=CARTESIAN_POINT('Ctrl Pts',(2.25642222333436,2.35518600960463,14.1052314380284));
#9809=CARTESIAN_POINT('Ctrl Pts',(2.23353566643227,2.33359683354842,14.1033333515255));
#9810=CARTESIAN_POINT('Ctrl Pts',(2.20223543237642,2.30319264931507,14.1006673415672));
#9811=CARTESIAN_POINT('Ctrl Pts',(2.19354936152978,2.29465902788125,14.0999198183001));
#9812=CARTESIAN_POINT('Ctrl Pts',(2.17968624278577,2.28088395737702,14.0987139416052));
#9813=CARTESIAN_POINT('Ctrl Pts',(2.17447834595029,2.27567352705129,14.0982579956657));
#9814=CARTESIAN_POINT('Ctrl Pts',(2.16356562943253,2.26468037345803,14.0972962760922));
#9815=CARTESIAN_POINT('Ctrl Pts',(2.15786476281457,2.25889389202919,14.096790191477));
#9816=CARTESIAN_POINT('Ctrl Pts',(2.14386711522806,2.24457817417296,14.0955386179663));
#9817=CARTESIAN_POINT('Ctrl Pts',(2.13559563195884,2.23602447544034,14.0947912124938));
#9818=CARTESIAN_POINT('Ctrl Pts',(2.10520951288517,2.20425136708127,14.0920171389705));
#9819=CARTESIAN_POINT('Ctrl Pts',(2.08339522677425,2.18074894135581,14.0899694777593));
#9820=CARTESIAN_POINT('Ctrl Pts',(1.92835283495276,2.00862708802443,14.0750291528445));
#9821=CARTESIAN_POINT('Ctrl Pts',(1.80884515799611,1.84825070333104,14.0614328501973));
#9822=CARTESIAN_POINT('Ctrl Pts',(1.59383510024042,1.49565709925879,14.0335264710804));
#9823=CARTESIAN_POINT('Ctrl Pts',(1.5010814572475,1.30283377865261,14.0193147045042));
#9824=CARTESIAN_POINT('Ctrl Pts',(1.41521590396304,1.06691542992767,14.0033794686006));
#9825=CARTESIAN_POINT('Ctrl Pts',(1.40298226732136,1.03138154481074,14.0010144689211));
#9826=CARTESIAN_POINT('Ctrl Pts',(1.38506717777146,0.976229633878805,13.9973964776238));
#9827=CARTESIAN_POINT('Ctrl Pts',(1.37894630676164,0.956758879604003,13.9961291927427));
#9828=CARTESIAN_POINT('Ctrl Pts',(1.36886027581244,0.92357617507163,13.9939860482907));
#9829=CARTESIAN_POINT('Ctrl Pts',(1.36480054965817,0.909893833129339,13.993107120556));
#9830=CARTESIAN_POINT('Ctrl Pts',(1.35676299688425,0.88213019738672,13.9913330896865));
#9831=CARTESIAN_POINT('Ctrl Pts',(1.35278991035701,0.868047872911373,13.9904381585538));
#9832=CARTESIAN_POINT('Ctrl Pts',(1.34321670461973,0.833210158616637,13.9882360259451));
#9833=CARTESIAN_POINT('Ctrl Pts',(1.33772803572621,0.812424675982848,13.9869324522086));
#9834=CARTESIAN_POINT('Ctrl Pts',(1.317891595552,0.734139424707712,13.982059855971));
#9835=CARTESIAN_POINT('Ctrl Pts',(1.30492219573072,0.676300391067899,13.9785350100107));
#9836=CARTESIAN_POINT('Ctrl Pts',(1.27615686629611,0.529111721636741,13.9697263455005));
#9837=CARTESIAN_POINT('Ctrl Pts',(1.26252443902447,0.439390921102984,13.9645063327866));
#9838=CARTESIAN_POINT('Ctrl Pts',(1.23760916997616,0.210809062254648,13.9514419591284));
#9839=CARTESIAN_POINT('Ctrl Pts',(1.23150739452777,0.0715740310489558,13.9437050295382));
#9840=CARTESIAN_POINT('Ctrl Pts',(1.23788548569985,-0.23234013637818,13.92667648119));
#9841=CARTESIAN_POINT('Ctrl Pts',(1.25396853637502,-0.396534319980223,13.9173846255518));
#9842=CARTESIAN_POINT('Ctrl Pts',(1.28721481952918,-0.585385226616336,13.9058905525115));
#9843=CARTESIAN_POINT('Ctrl Pts',(1.29223732115812,-0.611952366562802,13.904254493684));
#9844=CARTESIAN_POINT('Ctrl Pts',(1.29964051032992,-0.648581195326102,13.9019684414169));
#9845=CARTESIAN_POINT('Ctrl Pts',(1.30173639977978,-0.6587001555527,13.9013336853142));
#9846=CARTESIAN_POINT('Ctrl Pts',(1.30541759048237,-0.676052319841705,13.9002393919425));
#9847=CARTESIAN_POINT('Ctrl Pts',(1.30697923714229,-0.683290535545815,13.8997811849379));
#9848=CARTESIAN_POINT('Ctrl Pts',(1.31029845498599,-0.698421926569698,13.8988195495288));
#9849=CARTESIAN_POINT('Ctrl Pts',(1.31206080017165,-0.70631392026081,13.8983158395494));
#9850=CARTESIAN_POINT('Ctrl Pts',(1.31644891143079,-0.725622472868669,13.8970783148354));
#9851=CARTESIAN_POINT('Ctrl Pts',(1.31910724697604,-0.737031445070224,13.8963426766312));
#9852=CARTESIAN_POINT('Ctrl Pts',(1.32898178079829,-0.778389101116496,13.8936605726701));
#9853=CARTESIAN_POINT('Ctrl Pts',(1.3365648444778,-0.808247362285659,13.8916948365096));
#9854=CARTESIAN_POINT('Ctrl Pts',(1.35667509513097,-0.882927138720909,13.8867120039979));
#9855=CARTESIAN_POINT('Ctrl Pts',(1.36974709336806,-0.927593672279187,13.8836713238479));
#9856=CARTESIAN_POINT('Ctrl Pts',(1.48281013137566,-1.28502378130988,13.8589309884121));
#9857=CARTESIAN_POINT('Ctrl Pts',(1.62910408500653,-1.58114236493716,13.8361569272549));
#9858=CARTESIAN_POINT('Ctrl Pts',(1.85811725982171,-1.90778690595023,13.8103996454192));
#9859=CARTESIAN_POINT('Ctrl Pts',(1.90045430153217,-1.96414682636604,13.805916464426));
#9860=CARTESIAN_POINT('Ctrl Pts',(1.95945165665872,-2.03754331424302,13.8000214080405));
#9861=CARTESIAN_POINT('Ctrl Pts',(1.97449872822753,-2.0558458093323,13.7985464028389));
#9862=CARTESIAN_POINT('Ctrl Pts',(1.99946250488216,-2.0855368752841,13.7961448658852));
#9863=CARTESIAN_POINT('Ctrl Pts',(2.00925962390741,-2.09702438212829,13.7952135234316));
#9864=CARTESIAN_POINT('Ctrl Pts',(2.02840087277306,-2.11915141176225,13.7934151387024));
#9865=CARTESIAN_POINT('Ctrl Pts',(2.03773509197325,-2.12979901180117,13.7925477180528));
#9866=CARTESIAN_POINT('Ctrl Pts',(2.05973658409488,-2.15456504856732,13.7905251193534));
#9867=CARTESIAN_POINT('Ctrl Pts',(2.07245901084021,-2.16863395252972,13.7893722800737));
#9868=CARTESIAN_POINT('Ctrl Pts',(2.11436088600907,-2.21415611636309,13.7856285533746));
#9869=CARTESIAN_POINT('Ctrl Pts',(2.14404505419226,-2.24513997052017,13.7830591256843));
#9870=CARTESIAN_POINT('Ctrl Pts',(2.21582687870698,-2.31713018133583,13.7770286625279));
#9871=CARTESIAN_POINT('Ctrl Pts',(2.2584452823529,-2.35759659762561,13.773590214167));
#9872=CARTESIAN_POINT('Ctrl Pts',(2.51085191031132,-2.5844605145735,13.7539501353106));
#9873=CARTESIAN_POINT('Ctrl Pts',(2.74314070948067,-2.74396680762048,13.7387821065838));
#9874=CARTESIAN_POINT('Ctrl Pts',(3.07613032813164,-2.91366764626532,13.7173533130667));
#9875=CARTESIAN_POINT('Ctrl Pts',(3.16091017783334,-2.95234110590285,13.711909767744));
#9876=CARTESIAN_POINT('Ctrl Pts',(3.26197101875949,-2.99324983167174,13.7053017956754));
#9877=CARTESIAN_POINT('Ctrl Pts',(3.27674891231762,-2.9991049458972,13.7043326047753));
#9878=CARTESIAN_POINT('Ctrl Pts',(3.30083567030626,-3.00844273627513,13.7027472291953));
#9879=CARTESIAN_POINT('Ctrl Pts',(3.31011859319263,-3.01199216977737,13.7021348720278));
#9880=CARTESIAN_POINT('Ctrl Pts',(3.32674254625061,-3.01826054956571,13.7010355757096));
#9881=CARTESIAN_POINT('Ctrl Pts',(3.3340772395925,-3.02099575320679,13.7005496115846));
#9882=CARTESIAN_POINT('Ctrl Pts',(3.35013702053118,-3.0269180960205,13.6994834551387));
#9883=CARTESIAN_POINT('Ctrl Pts',(3.35886582151306,-3.03009420120151,13.6989026480833));
#9884=CARTESIAN_POINT('Ctrl Pts',(3.38384726229506,-3.03906196641303,13.6972368580765));
#9885=CARTESIAN_POINT('Ctrl Pts',(3.40013256191121,-3.04476080018153,13.6961466617832));
#9886=CARTESIAN_POINT('Ctrl Pts',(3.51519340614459,-3.08399068982933,13.6884179401053));
#9887=CARTESIAN_POINT('Ctrl Pts',(3.61549084426952,-3.11283626087745,13.6815473107918));
#9888=CARTESIAN_POINT('Ctrl Pts',(3.92819197838124,-3.1865533499662,13.6600649581354));
#9889=CARTESIAN_POINT('Ctrl Pts',(4.14389397697756,-3.2148882277126,13.6452036680957));
#9890=CARTESIAN_POINT('Ctrl Pts',(4.4022998077223,-3.22256211297559,13.6280718044847));
#9891=CARTESIAN_POINT('Ctrl Pts',(4.44381554531811,-3.2229925501364,13.6253380233406));
#9892=CARTESIAN_POINT('Ctrl Pts',(4.5820523133432,-3.22175457106555,13.6163022463906));
#9893=CARTESIAN_POINT('Ctrl Pts',(4.67869446175065,-3.2165342668205,13.6100964425014));
#9894=CARTESIAN_POINT('Ctrl Pts',(4.80134393976071,-3.20435355041761,13.6023609886958));
#9895=CARTESIAN_POINT('Ctrl Pts',(4.82769114735343,-3.201408219916,13.6007074247587));
#9896=CARTESIAN_POINT('Ctrl Pts',(4.86959270277683,-3.19619983044423,13.5980900288976));
#9897=CARTESIAN_POINT('Ctrl Pts',(4.88517157619495,-3.19414756521506,13.5971196175894));
#9898=CARTESIAN_POINT('Ctrl Pts',(4.91320464959167,-3.19024586970708,13.5953781578395));
#9899=CARTESIAN_POINT('Ctrl Pts',(4.92566411906265,-3.1884372524484,13.5946058412056));
#9900=CARTESIAN_POINT('Ctrl Pts',(4.95493424703653,-3.18401311100888,13.5927953098236));
#9901=CARTESIAN_POINT('Ctrl Pts',(4.97173553092693,-3.18133737861027,13.5917590175383));
#9902=CARTESIAN_POINT('Ctrl Pts',(5.02068476036917,-3.17314388920715,13.5887479980086));
#9903=CARTESIAN_POINT('Ctrl Pts',(5.05277166652581,-3.16727087881588,13.5867845198453));
#9904=CARTESIAN_POINT('Ctrl Pts',(5.29897716113582,-3.11833251213573,13.5717860605839));
#9905=CARTESIAN_POINT('Ctrl Pts',(5.50831444020005,-3.05408824374727,13.5594805031201));
#9906=CARTESIAN_POINT('Ctrl Pts',(5.91001419956551,-2.88455552524536,13.5350919147166));
#9907=CARTESIAN_POINT('Ctrl Pts',(6.10135336698419,-2.77988908263454,13.5230537413206));
#9908=CARTESIAN_POINT('Ctrl Pts',(6.30137955911803,-2.64254696934178,13.5084815170903));
#9909=CARTESIAN_POINT('Ctrl Pts',(6.32192818433605,-2.62808131610801,13.5069588001555));
#9910=CARTESIAN_POINT('Ctrl Pts',(6.35043871295164,-2.60750787196009,13.5048066233857));
#9911=CARTESIAN_POINT('Ctrl Pts',(6.35854503259861,-2.60160053383523,13.504190169292));
#9912=CARTESIAN_POINT('Ctrl Pts',(6.37252461160565,-2.59131289971176,13.5031189575797));
#9913=CARTESIAN_POINT('Ctrl Pts',(6.37841080942031,-2.58695019876686,13.5026654043984));
#9914=CARTESIAN_POINT('Ctrl Pts',(6.39069585492202,-2.57777976310625,13.5017134087303));
#9915=CARTESIAN_POINT('Ctrl Pts',(6.39709173639391,-2.57296821308916,13.5012146920526));
#9916=CARTESIAN_POINT('Ctrl Pts',(6.41247952024194,-2.5613021420518,13.5000075039506));
#9917=CARTESIAN_POINT('Ctrl Pts',(6.42145334776341,-2.55442406897991,13.4992974168503));
#9918=CARTESIAN_POINT('Ctrl Pts',(6.44095531016407,-2.53931303540811,13.4977412734762));
#9919=CARTESIAN_POINT('Ctrl Pts',(6.45146875418697,-2.5310615512356,13.4968940165852));
#9920=CARTESIAN_POINT('Ctrl Pts',(6.48101781920159,-2.50757146273953,13.4944897567835));
#9921=CARTESIAN_POINT('Ctrl Pts',(6.49993185008024,-2.49218219043527,13.4929236241527));
#9922=CARTESIAN_POINT('Ctrl Pts',(6.56305320578506,-2.43962227858665,13.487609685616));
#9923=CARTESIAN_POINT('Ctrl Pts',(6.60643361362268,-2.40147981221747,13.4838109813724));
#9924=CARTESIAN_POINT('Ctrl Pts',(6.84336442457945,-2.18159023073843,13.4623293720801));
#9925=CARTESIAN_POINT('Ctrl Pts',(7.01491172105647,-1.97762541223175,13.4440443299091));
#9926=CARTESIAN_POINT('Ctrl Pts',(7.21824865472653,-1.66442997305387,13.4195268783202));
#9927=CARTESIAN_POINT('Ctrl Pts',(7.27241290310834,-1.57105641319643,13.4125838106318));
#9928=CARTESIAN_POINT('Ctrl Pts',(7.33417509311794,-1.45108826908946,13.4041091031588));
#9929=CARTESIAN_POINT('Ctrl Pts',(7.3462507122496,-1.42688866167521,13.4024212026745));
#9930=CARTESIAN_POINT('Ctrl Pts',(7.36497677984122,-1.38814846469177,13.3997525998214));
#9931=CARTESIAN_POINT('Ctrl Pts',(7.37182590555821,-1.37370586182128,13.3987650311547));
#9932=CARTESIAN_POINT('Ctrl Pts',(7.38445212800718,-1.34656142494925,13.3969223483472));
#9933=CARTESIAN_POINT('Ctrl Pts',(7.39025470693223,-1.33387192255277,13.3960663710962));
#9934=CARTESIAN_POINT('Ctrl Pts',(7.40306065038044,-1.30537910464537,13.3941563237535));
#9935=CARTESIAN_POINT('Ctrl Pts',(7.41001968722926,-1.28955624867551,13.3931037898284));
#9936=CARTESIAN_POINT('Ctrl Pts',(7.43027196280166,-1.24248432210975,13.3899961361588));
#9937=CARTESIAN_POINT('Ctrl Pts',(7.44319922745701,-1.21107969815745,13.3879534210041));
#9938=CARTESIAN_POINT('Ctrl Pts',(7.52870715791737,-0.99365098824755,13.3740077225398));
#9939=CARTESIAN_POINT('Ctrl Pts',(7.58436220790903,-0.801428459235842,13.3626990609833));
#9940=CARTESIAN_POINT('Ctrl Pts',(7.66002300390259,-0.40574215963851,13.3401367438679));
#9941=CARTESIAN_POINT('Ctrl Pts',(7.67921910621675,-0.203083804950041,13.3289292504702));
#9942=CARTESIAN_POINT('Ctrl Pts',(7.67921910621823,-2.34794475528766E-11,
13.3169799747702));
#9943=CARTESIAN_POINT('Origin',(4.45646910621825,-5.13094777615093E-16,
-2.31077344927308));
#9944=CARTESIAN_POINT('',(7.67921910621823,-1.80065651569973E-10,12.0641237905203));
#9945=CARTESIAN_POINT('',(7.67921910621823,3.33464896044866E-11,12.3083142504469));
#9946=CARTESIAN_POINT('',(7.67921910621823,-3.51191647465084E-13,-2.31077344927308));
#9947=CARTESIAN_POINT('Ctrl Pts',(7.67921910621823,3.33546384956307E-11,
12.3083142504469));
#9948=CARTESIAN_POINT('Ctrl Pts',(7.67921910622113,-0.280383095796685,12.3267276928725));
#9949=CARTESIAN_POINT('Ctrl Pts',(7.64263159215061,-0.559592506371846,12.3461293237484));
#9950=CARTESIAN_POINT('Ctrl Pts',(7.53881732225561,-0.948797846265927,12.3727036979257));
#9951=CARTESIAN_POINT('Ctrl Pts',(7.50057450373251,-1.06513681324748,12.3806045998136));
#9952=CARTESIAN_POINT('Ctrl Pts',(7.44582673239986,-1.20440944008838,12.3900026642943));
#9953=CARTESIAN_POINT('Ctrl Pts',(7.43552883995388,-1.22966023471888,12.3917043587878));
#9954=CARTESIAN_POINT('Ctrl Pts',(7.41872874207879,-1.26940441635969,12.3943799193372));
#9955=CARTESIAN_POINT('Ctrl Pts',(7.41243793317796,-1.28398521447319,12.3953608775295));
#9956=CARTESIAN_POINT('Ctrl Pts',(7.4004121269501,-1.31130168704837,12.3971977069326));
#9957=CARTESIAN_POINT('Ctrl Pts',(7.39470163099574,-1.32404768185387,12.3980543874791));
#9958=CARTESIAN_POINT('Ctrl Pts',(7.38167499036028,-1.35262419376029,12.3999743765636));
#9959=CARTESIAN_POINT('Ctrl Pts',(7.3743128118175,-1.36843333869575,12.4010360767259));
#9960=CARTESIAN_POINT('Ctrl Pts',(7.35515518848157,-1.40871376966487,12.4037404772194));
#9961=CARTESIAN_POINT('Ctrl Pts',(7.34317785921788,-1.43309739084182,12.4053768769742));
#9962=CARTESIAN_POINT('Ctrl Pts',(7.25672026003652,-1.60362588695045,12.4168224247787));
#9963=CARTESIAN_POINT('Ctrl Pts',(7.17148211227494,-1.74405754107698,12.4262373645221));
#9964=CARTESIAN_POINT('Ctrl Pts',(7.01756403963998,-1.9588113864248,12.4411339624225));
#9965=CARTESIAN_POINT('Ctrl Pts',(6.95545297765951,-2.03745656534628,12.4467152953346));
#9966=CARTESIAN_POINT('Ctrl Pts',(6.80388689882243,-2.21199189525644,12.4596539543624));
#9967=CARTESIAN_POINT('Ctrl Pts',(6.71204870215988,-2.30556590073623,12.467015678508));
#9968=CARTESIAN_POINT('Ctrl Pts',(6.58415928554667,-2.42089905136426,12.4770672170594));
#9969=CARTESIAN_POINT('Ctrl Pts',(6.55301305340035,-2.44792174795321,12.4795012765369));
#9970=CARTESIAN_POINT('Ctrl Pts',(6.50653588881959,-2.48670795793105,12.4831279841435));
#9971=CARTESIAN_POINT('Ctrl Pts',(6.49160286495506,-2.49894394229083,12.4842924397806));
#9972=CARTESIAN_POINT('Ctrl Pts',(6.46471989572811,-2.52057082669988,12.4863891634543));
#9973=CARTESIAN_POINT('Ctrl Pts',(6.45281162415638,-2.53001285693807,12.4873180908032));
#9974=CARTESIAN_POINT('Ctrl Pts',(6.4338005774955,-2.5448688702918,12.4888021183337));
#9975=CARTESIAN_POINT('Ctrl Pts',(6.4267411422943,-2.55033829395978,12.4893534110466));
#9976=CARTESIAN_POINT('Ctrl Pts',(6.41365960180178,-2.56038672068573,12.4903755895942));
#9977=CARTESIAN_POINT('Ctrl Pts',(6.40764402390254,-2.56497392424168,12.4908458898465));
#9978=CARTESIAN_POINT('Ctrl Pts',(6.39361876202776,-2.57559105601253,12.4919429370439));
#9979=CARTESIAN_POINT('Ctrl Pts',(6.3855970887134,-2.58160479113828,12.4925707823596));
#9980=CARTESIAN_POINT('Ctrl Pts',(6.36455276852032,-2.59722856976623,12.4942186348895));
#9981=CARTESIAN_POINT('Ctrl Pts',(6.35148574021324,-2.60677798014992,12.4952425715615));
#9982=CARTESIAN_POINT('Ctrl Pts',(6.25654681305502,-2.67506847618704,12.5026840260521));
#9983=CARTESIAN_POINT('Ctrl Pts',(6.17203916718867,-2.73003413698777,12.5093171424033));
#9984=CARTESIAN_POINT('Ctrl Pts',(5.9053557404573,-2.8862149346065,12.5299684545301));
#9985=CARTESIAN_POINT('Ctrl Pts',(5.71582050451688,-2.97381082121707,12.5442290818051));
#9986=CARTESIAN_POINT('Ctrl Pts',(5.42789978566637,-3.07437503110044,12.5645038317668));
#9987=CARTESIAN_POINT('Ctrl Pts',(5.33525869693962,-3.10212685741149,12.5708380402753));
#9988=CARTESIAN_POINT('Ctrl Pts',(5.20114628508984,-3.13581007976809,12.5797207759354));
#9989=CARTESIAN_POINT('Ctrl Pts',(5.16059571678796,-3.14516373637219,12.582370196098));
#9990=CARTESIAN_POINT('Ctrl Pts',(5.08778282902986,-3.16048033496879,12.5870635923237));
#9991=CARTESIAN_POINT('Ctrl Pts',(5.05558975562851,-3.16674083869105,12.5891166147838));
#9992=CARTESIAN_POINT('Ctrl Pts',(5.00652182547518,-3.17550787457755,12.592213300854));
#9993=CARTESIAN_POINT('Ctrl Pts',(4.98971411624229,-3.1783734885362,12.593268284443));
#9994=CARTESIAN_POINT('Ctrl Pts',(4.95912468727175,-3.18333932259374,12.5951781101941));
#9995=CARTESIAN_POINT('Ctrl Pts',(4.94535066443466,-3.18548374782396,12.5960343319193));
#9996=CARTESIAN_POINT('Ctrl Pts',(4.91557345614374,-3.18992195878262,12.5978774412759));
#9997=CARTESIAN_POINT('Ctrl Pts',(4.89956599667714,-3.192184842359,12.5988633320907));
#9998=CARTESIAN_POINT('Ctrl Pts',(4.8559488113597,-3.19801634126479,12.601536735067));
#9999=CARTESIAN_POINT('Ctrl Pts',(4.82830839654391,-3.20134786762485,12.603216773561));
#10000=CARTESIAN_POINT('Ctrl Pts',(4.68162062536532,-3.21710279522244,12.6120630033188));
#10001=CARTESIAN_POINT('Ctrl Pts',(4.56198647919039,-3.22324591996066,12.6190299901467));
#10002=CARTESIAN_POINT('Ctrl Pts',(4.21408862251111,-3.22171386894985,12.6388991770143));
#10003=CARTESIAN_POINT('Ctrl Pts',(3.98666505872358,-3.19647719283489,12.651364339304));
#10004=CARTESIAN_POINT('Ctrl Pts',(3.69213172208375,-3.13165995818053,12.6685534509104));
#10005=CARTESIAN_POINT('Ctrl Pts',(3.62100730242283,-3.113439889655,12.6727926536621));
#10006=CARTESIAN_POINT('Ctrl Pts',(3.52305722303507,-3.08474987867242,12.6788307043833));
#10007=CARTESIAN_POINT('Ctrl Pts',(3.49565248640691,-3.07632424576494,12.6805422377958));
#10008=CARTESIAN_POINT('Ctrl Pts',(3.44806417995651,-3.06099525360632,12.6835590326797));
#10009=CARTESIAN_POINT('Ctrl Pts',(3.42782960132389,-3.05425492575899,12.68485602953));
#10010=CARTESIAN_POINT('Ctrl Pts',(3.39810118291132,-3.04402319012996,12.68678469638));
#10011=CARTESIAN_POINT('Ctrl Pts',(3.38855402880637,-3.04068696582291,12.6874076204511));
#10012=CARTESIAN_POINT('Ctrl Pts',(3.37163195638336,-3.03468407264001,12.6885182973413));
#10013=CARTESIAN_POINT('Ctrl Pts',(3.36425086854456,-3.03203535300356,12.6890049900022));
#10014=CARTESIAN_POINT('Ctrl Pts',(3.34826797920018,-3.02623392208214,12.6900637887849));
#10015=CARTESIAN_POINT('Ctrl Pts',(3.33967006666442,-3.02307151576813,12.6906364419256));
#10016=CARTESIAN_POINT('Ctrl Pts',(3.31590097740323,-3.01421374644525,12.692227855125));
#10017=CARTESIAN_POINT('Ctrl Pts',(3.3007593369409,-3.00844063751657,12.6932510318437));
#10018=CARTESIAN_POINT('Ctrl Pts',(3.21902205422988,-2.97656824496834,12.6988228599169));
#10019=CARTESIAN_POINT('Ctrl Pts',(3.15327069599096,-2.94837344077278,12.703479833281));
#10020=CARTESIAN_POINT('Ctrl Pts',(3.06343515286575,-2.906258994978,12.7100368782526));
#10021=CARTESIAN_POINT('Ctrl Pts',(3.03850610157407,-2.89417791309808,12.7118778132383));
#10022=CARTESIAN_POINT('Ctrl Pts',(2.76593378100132,-2.7577173343064,12.7322214904861));
#10023=CARTESIAN_POINT('Ctrl Pts',(2.53511957275793,-2.602185422782,12.7512800949521));
#10024=CARTESIAN_POINT('Ctrl Pts',(2.28317822030604,-2.3804078249608,12.7731215823635));
#10025=CARTESIAN_POINT('Ctrl Pts',(2.24035733189057,-2.34059479120643,12.7768823059954));
#10026=CARTESIAN_POINT('Ctrl Pts',(2.16814624449462,-2.26969654170508,12.7833098209696));
#10027=CARTESIAN_POINT('Ctrl Pts',(2.13824899115032,-2.2391515559859,12.7859981838682));
#10028=CARTESIAN_POINT('Ctrl Pts',(2.09599081180354,-2.19422389211145,12.7898398023908));
#10029=CARTESIAN_POINT('Ctrl Pts',(2.0831363424598,-2.18031371232119,12.7910141961165));
#10030=CARTESIAN_POINT('Ctrl Pts',(2.06088939508232,-2.15580978024384,12.7930572502876));
#10031=CARTESIAN_POINT('Ctrl Pts',(2.05144281222413,-2.14526606656641,12.7939281880721));
#10032=CARTESIAN_POINT('Ctrl Pts',(2.03205694964629,-2.12333972603486,12.7957227642804));
#10033=CARTESIAN_POINT('Ctrl Pts',(2.02212762386339,-2.11194873436338,12.7966459751391));
#10034=CARTESIAN_POINT('Ctrl Pts',(1.99680008638921,-2.08247685910075,12.799011665166));
#10035=CARTESIAN_POINT('Ctrl Pts',(1.98152078101579,-2.06429464697946,12.8004492457636));
#10036=CARTESIAN_POINT('Ctrl Pts',(1.92141222366032,-1.9911392796657,12.8061490001547));
#10037=CARTESIAN_POINT('Ctrl Pts',(1.87820039708457,-1.93485932107359,12.8103464884415));
#10038=CARTESIAN_POINT('Ctrl Pts',(1.80439232553842,-1.83186158480249,12.8177375603417));
#10039=CARTESIAN_POINT('Ctrl Pts',(1.77308719436076,-1.78569035762233,12.8209527577885));
#10040=CARTESIAN_POINT('Ctrl Pts',(1.61945999993934,-1.54593845630854,12.8372226771492));
#10041=CARTESIAN_POINT('Ctrl Pts',(1.51682907237625,-1.34054343587287,12.8497296651616));
#10042=CARTESIAN_POINT('Ctrl Pts',(1.3987369121024,-1.02385495744705,12.8689894033766));
#10043=CARTESIAN_POINT('Ctrl Pts',(1.36585505957918,-0.91983957267185,12.8753217721624));
#10044=CARTESIAN_POINT('Ctrl Pts',(1.33390847275518,-0.79751865796829,12.8829863052737));
#10045=CARTESIAN_POINT('Ctrl Pts',(1.32964405612803,-0.780631792002036,
12.8840491732649));
#10046=CARTESIAN_POINT('Ctrl Pts',(1.32330726809734,-0.754653163071605,
12.8856927250864));
#10047=CARTESIAN_POINT('Ctrl Pts',(1.32113705499851,-0.745585289473953,
12.8862679820854));
#10048=CARTESIAN_POINT('Ctrl Pts',(1.31721758402831,-0.728888674859578,
12.8873303038784));
#10049=CARTESIAN_POINT('Ctrl Pts',(1.31545673762614,-0.721262862141284,
12.8878167013743));
#10050=CARTESIAN_POINT('Ctrl Pts',(1.31153222360232,-0.703979765194318,
12.888921784122));
#10051=CARTESIAN_POINT('Ctrl Pts',(1.3093852645857,-0.694318941891138,12.8895413929244));
#10052=CARTESIAN_POINT('Ctrl Pts',(1.30393587446378,-0.669253315526627,
12.8911536405293));
#10053=CARTESIAN_POINT('Ctrl Pts',(1.30070189317633,-0.653834116257114,
12.8921499447888));
#10054=CARTESIAN_POINT('Ctrl Pts',(1.2798059829733,-0.550437114123183,12.8988583280191));
#10055=CARTESIAN_POINT('Ctrl Pts',(1.26571366128599,-0.461785948136937,
12.9047418643186));
#10056=CARTESIAN_POINT('Ctrl Pts',(1.22252704560661,-0.090826657060951,
12.929606447947));
#10057=CARTESIAN_POINT('Ctrl Pts',(1.22707809586845,0.194176743933125,12.9491546877146));
#10058=CARTESIAN_POINT('Ctrl Pts',(1.28203216841671,0.563034906910546,12.9734317401019));
#10059=CARTESIAN_POINT('Ctrl Pts',(1.2988140034172,0.650595809980168,12.9791308336188));
#10060=CARTESIAN_POINT('Ctrl Pts',(1.32488349736597,0.761514967831724,12.9862711637016));
#10061=CARTESIAN_POINT('Ctrl Pts',(1.33084067171668,0.785608309902471,12.9878174324361));
#10062=CARTESIAN_POINT('Ctrl Pts',(1.34093042815405,0.824482710904736,12.9903052006832));
#10063=CARTESIAN_POINT('Ctrl Pts',(1.34489122514292,0.839306915314272,12.9912521910129));
#10064=CARTESIAN_POINT('Ctrl Pts',(1.35268787498126,0.867673742781844,12.9930612604975));
#10065=CARTESIAN_POINT('Ctrl Pts',(1.35650686044375,0.881220596665855,12.9939238618749));
#10066=CARTESIAN_POINT('Ctrl Pts',(1.36543472480635,0.912113468790976,12.9958881256814));
#10067=CARTESIAN_POINT('Ctrl Pts',(1.37060111974435,0.929442476837498,12.996987891866));
#10068=CARTESIAN_POINT('Ctrl Pts',(1.38739370247584,0.984083857658635,13.0004498078648));
#10069=CARTESIAN_POINT('Ctrl Pts',(1.39955314018012,1.02122957660542,13.0027945547021));
#10070=CARTESIAN_POINT('Ctrl Pts',(1.49870176107478,1.30646112754162,13.0207531970528));
#10071=CARTESIAN_POINT('Ctrl Pts',(1.61507331208986,1.54327973948428,13.0352860904291));
#10072=CARTESIAN_POINT('Ctrl Pts',(1.85236789918476,1.90628884204277,13.0595939793505));
#10073=CARTESIAN_POINT('Ctrl Pts',(1.95700802932465,2.04155797881894,13.0692447930298));
#10074=CARTESIAN_POINT('Ctrl Pts',(2.08559318563472,2.18299845060467,13.0807909941339));
#10075=CARTESIAN_POINT('Ctrl Pts',(2.09947772797619,2.19798236119644,13.0820342101143));
#10076=CARTESIAN_POINT('Ctrl Pts',(2.12032764428936,2.22005842546125,13.0838977238906));
#10077=CARTESIAN_POINT('Ctrl Pts',(2.12718520532033,2.2272523084491,13.0845101030516));
#10078=CARTESIAN_POINT('Ctrl Pts',(2.13898481636893,2.23951652377176,13.0855631408545));
#10079=CARTESIAN_POINT('Ctrl Pts',(2.14391046066186,2.24460246003662,13.0860025331292));
#10080=CARTESIAN_POINT('Ctrl Pts',(2.15512677522783,2.25610766908877,13.0870027149876));
#10081=CARTESIAN_POINT('Ctrl Pts',(2.16142744088259,2.26251675986647,13.0875642751017));
#10082=CARTESIAN_POINT('Ctrl Pts',(2.17862900576883,2.27986855168398,13.0890964190707));
#10083=CARTESIAN_POINT('Ctrl Pts',(2.18958173758774,2.29075921300148,13.0900709167299));
#10084=CARTESIAN_POINT('Ctrl Pts',(2.24450311933146,2.3445897548294,13.0949502089249));
#10085=CARTESIAN_POINT('Ctrl Pts',(2.28961262461102,2.386341659838,13.0989348041721));
#10086=CARTESIAN_POINT('Ctrl Pts',(2.36456371250586,2.45183603102268,13.1054805861793));
#10087=CARTESIAN_POINT('Ctrl Pts',(2.39368405170251,2.4763856195491,13.1080065352424));
#10088=CARTESIAN_POINT('Ctrl Pts',(2.56236217141639,2.61354805183486,13.1225114644826));
#10089=CARTESIAN_POINT('Ctrl Pts',(2.71069190499138,2.71487345370927,13.1347604085088));
#10090=CARTESIAN_POINT('Ctrl Pts',(3.00744471482028,2.88316365151822,13.1576296300736));
#10091=CARTESIAN_POINT('Ctrl Pts',(3.15403622994852,2.95228490901848,13.1682621382635));
#10092=CARTESIAN_POINT('Ctrl Pts',(3.34218049738266,3.02424277043986,13.1810294593323));
#10093=CARTESIAN_POINT('Ctrl Pts',(3.3793991329058,3.0376971433638,13.1835151711712));
#10094=CARTESIAN_POINT('Ctrl Pts',(3.4342448814686,3.05638882207109,13.1871215543392));
#10095=CARTESIAN_POINT('Ctrl Pts',(3.45168288746346,3.06216584696773,13.1882599280882));
#10096=CARTESIAN_POINT('Ctrl Pts',(3.48256472845279,3.07210446405868,13.1902616581366));
#10097=CARTESIAN_POINT('Ctrl Pts',(3.49598808410393,3.07632764692806,13.191127018138));
#10098=CARTESIAN_POINT('Ctrl Pts',(3.5241144939772,3.08497458178052,13.1929305465105));
#10099=CARTESIAN_POINT('Ctrl Pts',(3.53882239549219,3.0893814624092,13.1938681448824));
#10100=CARTESIAN_POINT('Ctrl Pts',(3.57742767059103,3.10064861478459,13.1963150959281));
#10101=CARTESIAN_POINT('Ctrl Pts',(3.60137420508863,3.10733783821667,13.1978188728869));
#10102=CARTESIAN_POINT('Ctrl Pts',(3.70326173620357,3.13453204926887,13.2041604505742));
#10103=CARTESIAN_POINT('Ctrl Pts',(3.78188345793262,3.15238771197374,13.2089130075183));
#10104=CARTESIAN_POINT('Ctrl Pts',(4.0915723936306,3.21060177606796,13.2272053979618));
#10105=CARTESIAN_POINT('Ctrl Pts',(4.32608151635074,3.22863984625599,13.2400819056559));
#10106=CARTESIAN_POINT('Ctrl Pts',(4.70633942201599,3.2163613540936,13.2615140518314));
#10107=CARTESIAN_POINT('Ctrl Pts',(4.8516956392506,3.20174963588584,13.2698575940307));
#10108=CARTESIAN_POINT('Ctrl Pts',(5.01358619258606,3.17428308527813,13.2798014026489));
#10109=CARTESIAN_POINT('Ctrl Pts',(5.03160419382584,3.17106798236126,13.2809173807437));
#10110=CARTESIAN_POINT('Ctrl Pts',(5.05894059214937,3.16594947926375,13.2826259376557));
#10111=CARTESIAN_POINT('Ctrl Pts',(5.06827990273194,3.16415795125306,13.2832124008005));
#10112=CARTESIAN_POINT('Ctrl Pts',(5.08528306823281,3.16081820025487,13.2842853484006));
#10113=CARTESIAN_POINT('Ctrl Pts',(5.09294935231818,3.15928339767642,13.2847710708786));
#10114=CARTESIAN_POINT('Ctrl Pts',(5.11009774708293,3.15578531032237,13.2858619591544));
#10115=CARTESIAN_POINT('Ctrl Pts',(5.1195765482943,3.15380719758422,13.2864679414813));
#10116=CARTESIAN_POINT('Ctrl Pts',(5.14719490018595,3.14791356559026,13.2882420361841));
#10117=CARTESIAN_POINT('Ctrl Pts',(5.16530937330319,3.14388412269432,13.2894162853379));
#10118=CARTESIAN_POINT('Ctrl Pts',(5.32122019252144,3.10778688446259,13.2996090789624));
#10119=CARTESIAN_POINT('Ctrl Pts',(5.45678715339439,3.06683690000413,13.309046941385));
#10120=CARTESIAN_POINT('Ctrl Pts',(5.62939744916173,3.00203255164949,13.3214786776704));
#10121=CARTESIAN_POINT('Ctrl Pts',(5.66928023713543,2.98614290450023,13.3243817022453));
#10122=CARTESIAN_POINT('Ctrl Pts',(5.85031651510964,2.90979122506909,13.3376737535657));
#10123=CARTESIAN_POINT('Ctrl Pts',(5.98736445408275,2.84008127699621,13.3480463773411));
#10124=CARTESIAN_POINT('Ctrl Pts',(6.22004580104891,2.69997171070097,13.3659368928106));
#10125=CARTESIAN_POINT('Ctrl Pts',(6.31775185058082,2.63356833100348,13.3735498445784));
#10126=CARTESIAN_POINT('Ctrl Pts',(6.43307136596196,2.54556286702816,13.382658052534));
#10127=CARTESIAN_POINT('Ctrl Pts',(6.45433247337631,2.52891060354138,13.3843430088537));
#10128=CARTESIAN_POINT('Ctrl Pts',(6.48771493705192,2.50208078932814,13.3869983730876));
#10129=CARTESIAN_POINT('Ctrl Pts',(6.49997458904939,2.49207810020211,13.3879756928641));
#10130=CARTESIAN_POINT('Ctrl Pts',(6.52292226370886,2.47307181113204,13.3898093081554));
#10131=CARTESIAN_POINT('Ctrl Pts',(6.53362631379439,2.46408822485294,13.3906663834845));
#10132=CARTESIAN_POINT('Ctrl Pts',(6.55762212135739,2.44368179230383,13.392591958317));
#10133=CARTESIAN_POINT('Ctrl Pts',(6.57087988256129,2.43221951781021,13.39365880857));
#10134=CARTESIAN_POINT('Ctrl Pts',(6.60466178773215,2.40252768377527,13.3963854087311));
#10135=CARTESIAN_POINT('Ctrl Pts',(6.62504797110731,2.38414279039983,13.3980386770825));
#10136=CARTESIAN_POINT('Ctrl Pts',(6.80378346179067,2.21876400114542,13.4126123459492));
#10137=CARTESIAN_POINT('Ctrl Pts',(6.94721913518784,2.05644818125776,13.4248123958923));
#10138=CARTESIAN_POINT('Ctrl Pts',(7.17167490327287,1.74417835955314,13.4463312502281));
#10139=CARTESIAN_POINT('Ctrl Pts',(7.25911965845381,1.59988827985571,13.4556754827386));
#10140=CARTESIAN_POINT('Ctrl Pts',(7.35617056744006,1.40715669141018,13.4682007101432));
#10141=CARTESIAN_POINT('Ctrl Pts',(7.37652603064583,1.36441402459769,13.4709819276123));
#10142=CARTESIAN_POINT('Ctrl Pts',(7.40872192624013,1.29278542145264,13.4756732593142));
#10143=CARTESIAN_POINT('Ctrl Pts',(7.4210977422972,1.26414704251688,13.4775568634157));
#10144=CARTESIAN_POINT('Ctrl Pts',(7.43756830341546,1.22446059674141,13.4801839681871));
#10145=CARTESIAN_POINT('Ctrl Pts',(7.4420215607347,1.21356199176158,13.4809071498913));
#10146=CARTESIAN_POINT('Ctrl Pts',(7.44943709289846,1.19512584303349,13.4821338013944));
#10147=CARTESIAN_POINT('Ctrl Pts',(7.45243090820416,1.1876009553603,13.4826353983371));
#10148=CARTESIAN_POINT('Ctrl Pts',(7.45810355712397,1.17318491683476,13.4835982609504));
#10149=CARTESIAN_POINT('Ctrl Pts',(7.46078708789358,1.16629571221425,13.4840592223917));
#10150=CARTESIAN_POINT('Ctrl Pts',(7.46714823561781,1.14979763364853,13.4851649827836));
#10151=CARTESIAN_POINT('Ctrl Pts',(7.47080356363207,1.14018033251333,13.4858110749508));
#10152=CARTESIAN_POINT('Ctrl Pts',(7.48378092911438,1.10553781239608,13.4881433469418));
#10153=CARTESIAN_POINT('Ctrl Pts',(7.49283758792597,1.08041522740317,13.4898440107271));
#10154=CARTESIAN_POINT('Ctrl Pts',(7.56284092930072,0.878395494069324,13.5035776530195));
#10155=CARTESIAN_POINT('Ctrl Pts',(7.60858387781865,0.696623788770225,13.5162674048535));
#10156=CARTESIAN_POINT('Ctrl Pts',(7.66541976647591,0.343368413608132,13.540470057364));
#10157=CARTESIAN_POINT('Ctrl Pts',(7.67910509069768,0.17290148099393,13.5519513694079));
#10158=CARTESIAN_POINT('Ctrl Pts',(7.67921886993575,0.0014255959816308,
13.5631165164725));
#10159=CARTESIAN_POINT('Ctrl Pts',(7.67921910621823,0.000712797000042185,
13.563162921892));
#10160=CARTESIAN_POINT('Ctrl Pts',(7.67921910621823,1.97331828652831E-11,
13.5632093210196));
#10161=CARTESIAN_POINT('',(7.67921877062999,0.00147072563195245,13.3168934255997));
#10162=CARTESIAN_POINT('Ctrl Pts',(7.67921910621823,-2.34781276219209E-11,
13.3169799747702));
#10163=CARTESIAN_POINT('Ctrl Pts',(7.67921910621823,0.000490239403011727,
13.3169511295057));
#10164=CARTESIAN_POINT('Ctrl Pts',(7.67921899435662,0.000980481300954709,
13.316922279787));
#10165=CARTESIAN_POINT('Ctrl Pts',(7.67921877062999,0.0014707256322326,
13.3168934255997));
#10166=CARTESIAN_POINT('Ctrl Pts',(7.6792187687556,0.00147482719786989,
13.3168931841947));
#10167=CARTESIAN_POINT('Ctrl Pts',(7.67920381324451,0.0341551767246361,
13.3149697234694));
#10168=CARTESIAN_POINT('Ctrl Pts',(7.67869176533755,0.066832409103204,13.3130272302896));
#10169=CARTESIAN_POINT('Ctrl Pts',(7.67701596931515,0.121087280003743,13.3097618798408));
#10170=CARTESIAN_POINT('Ctrl Pts',(7.67613197904975,0.142671496439738,13.3084522487079));
#10171=CARTESIAN_POINT('Ctrl Pts',(7.67457495974107,0.173183093420942,13.306583935171));
#10172=CARTESIAN_POINT('Ctrl Pts',(7.67408159372043,0.182119587732629,13.3060346618699));
#10173=CARTESIAN_POINT('Ctrl Pts',(7.67311364949827,0.19841843143695,13.305028911093));
#10174=CARTESIAN_POINT('Ctrl Pts',(7.67265100068669,0.205781463906846,13.3045730869004));
#10175=CARTESIAN_POINT('Ctrl Pts',(7.67166754783189,0.220618859610453,13.3036514575909));
#10176=CARTESIAN_POINT('Ctrl Pts',(7.67114596244545,0.228092976882592,13.3031856038319));
#10177=CARTESIAN_POINT('Ctrl Pts',(7.66985949858511,0.245645916032934,13.3020878355876));
#10178=CARTESIAN_POINT('Ctrl Pts',(7.66907326560881,0.255722971971126,13.3014547504164));
#10179=CARTESIAN_POINT('Ctrl Pts',(7.6664827713951,0.287025448232298,13.2994796438253));
#10180=CARTESIAN_POINT('Ctrl Pts',(7.66451549984509,0.308236303210312,13.2981290732907));
#10181=CARTESIAN_POINT('Ctrl Pts',(7.65607497150492,0.390376983252589,13.2928554920203));
#10182=CARTESIAN_POINT('Ctrl Pts',(7.64807519898021,0.451133451762505,13.2888622700012));
#10183=CARTESIAN_POINT('Ctrl Pts',(7.61248406997233,0.672482481119379,13.2740595272985));
#10184=CARTESIAN_POINT('Ctrl Pts',(7.57445842254818,0.831145153881467,13.2629676725312));
#10185=CARTESIAN_POINT('Ctrl Pts',(7.45784536113904,1.19391894370988,13.2372407243241));
#10186=CARTESIAN_POINT('Ctrl Pts',(7.37016663932756,1.39430994304863,13.2227739788541));
#10187=CARTESIAN_POINT('Ctrl Pts',(7.24686129349354,1.61272823893366,13.2069549707656));
#10188=CARTESIAN_POINT('Ctrl Pts',(7.23039973895362,1.64088083106302,13.2049136678247));
#10189=CARTESIAN_POINT('Ctrl Pts',(7.20470477867923,1.68333229679738,13.2018310000153));
#10190=CARTESIAN_POINT('Ctrl Pts',(7.19578111571957,1.6978152623848,13.2007784693871));
#10191=CARTESIAN_POINT('Ctrl Pts',(7.17933882447423,1.72403372313035,13.1988713202093));
#10192=CARTESIAN_POINT('Ctrl Pts',(7.17185799443414,1.73579231952181,13.1980153399034));
#10193=CARTESIAN_POINT('Ctrl Pts',(7.15551989687925,1.76110892453041,13.1961707906214));
#10194=CARTESIAN_POINT('Ctrl Pts',(7.14663620508639,1.77464948926502,13.1951832330464));
#10195=CARTESIAN_POINT('Ctrl Pts',(7.12213343558818,1.8113899065014,13.192500470571));
#10196=CARTESIAN_POINT('Ctrl Pts',(7.10631360892998,1.8344546590993,13.1908128297048));
#10197=CARTESIAN_POINT('Ctrl Pts',(7.02009683401578,1.95671277920615,13.181843496809));
#10198=CARTESIAN_POINT('Ctrl Pts',(6.94442300520664,2.05207265756611,13.1747679709686));
#10199=CARTESIAN_POINT('Ctrl Pts',(6.6961399381897,2.33095796738833,13.1534577150527));
#10200=CARTESIAN_POINT('Ctrl Pts',(6.50730971249028,2.49870532792051,13.1397892186547));
#10201=CARTESIAN_POINT('Ctrl Pts',(6.25442653781677,2.67519687004011,13.1220223134124));
#10202=CARTESIAN_POINT('Ctrl Pts',(6.20710910792218,2.70639762280815,13.1187148839667));
#10203=CARTESIAN_POINT('Ctrl Pts',(6.13856035875061,2.7490481796493,13.1139107569189));
#10204=CARTESIAN_POINT('Ctrl Pts',(6.11798303048373,2.76153368330714,13.1124670407894));
#10205=CARTESIAN_POINT('Ctrl Pts',(6.08586864287728,2.78053055028302,13.110208339515));
#10206=CARTESIAN_POINT('Ctrl Pts',(6.07442760828103,2.78720348439878,13.1094025820518));
#10207=CARTESIAN_POINT('Ctrl Pts',(6.05302258814588,2.79951166725186,13.107892471534));
#10208=CARTESIAN_POINT('Ctrl Pts',(6.04306903576269,2.80516474562825,13.1071892087795));
#10209=CARTESIAN_POINT('Ctrl Pts',(6.02615221544345,2.81465374401116,13.1059918275921));
#10210=CARTESIAN_POINT('Ctrl Pts',(6.0192043684039,2.81851720954874,13.1054994495111));
#10211=CARTESIAN_POINT('Ctrl Pts',(6.00578195545449,2.82591607735439,13.1045469326737));
#10212=CARTESIAN_POINT('Ctrl Pts',(5.99930943693048,2.82945501685345,13.1040870398865));
#10213=CARTESIAN_POINT('Ctrl Pts',(5.98207452954156,2.83880172167028,13.1028610427401));
#10214=CARTESIAN_POINT('Ctrl Pts',(5.97129125984596,2.84457043404316,13.1020925320432));
#10215=CARTESIAN_POINT('Ctrl Pts',(5.93235403518063,2.86511644726083,13.0993130402351));
#10216=CARTESIAN_POINT('Ctrl Pts',(5.90401558841697,2.87953773805855,13.097281748021));
#10217=CARTESIAN_POINT('Ctrl Pts',(5.56561613348809,3.04549001940456,13.0729670581777));
#10218=CARTESIAN_POINT('Ctrl Pts',(5.23335666464999,3.1466996842052,13.0488180794679));
#10219=CARTESIAN_POINT('Ctrl Pts',(4.82905732106831,3.20175649558625,13.0221877117035));
#10220=CARTESIAN_POINT('Ctrl Pts',(4.76655263534069,3.20841326552862,13.0181350829883));
#10221=CARTESIAN_POINT('Ctrl Pts',(4.65886056695671,3.21670559904264,13.0112642092798));
#10222=CARTESIAN_POINT('Ctrl Pts',(4.61376173223752,3.2192260834208,13.0084201903498));
#10223=CARTESIAN_POINT('Ctrl Pts',(4.54927820309124,3.22147151244244,13.0043994024005));
#10224=CARTESIAN_POINT('Ctrl Pts',(4.52992749134325,3.22197084496574,13.0031986628876));
#10225=CARTESIAN_POINT('Ctrl Pts',(4.49635149315902,3.22253460324911,13.0011250584373));
#10226=CARTESIAN_POINT('Ctrl Pts',(4.48212827316133,3.22267924115812,13.0002497125702));
#10227=CARTESIAN_POINT('Ctrl Pts',(4.45294571398415,3.222782790176,12.9984598167093));
#10228=CARTESIAN_POINT('Ctrl Pts',(4.43798666812938,3.22273171987286,12.9975455998804));
#10229=CARTESIAN_POINT('Ctrl Pts',(4.39997950722119,3.22233731826011,12.9952308652837));
#10230=CARTESIAN_POINT('Ctrl Pts',(4.37693348163165,3.22185086466744,12.9938348384292));
#10231=CARTESIAN_POINT('Ctrl Pts',(4.28842649284819,3.21903240249337,12.988500519426));
#10232=CARTESIAN_POINT('Ctrl Pts',(4.22303456711213,3.21495211817029,12.9846166192997));
#10233=CARTESIAN_POINT('Ctrl Pts',(3.82487465482195,3.17789417989429,12.9612252041445));
#10234=CARTESIAN_POINT('Ctrl Pts',(3.49884225918399,3.09529230279362,12.9434114911611));
#10235=CARTESIAN_POINT('Ctrl Pts',(3.14834390018076,2.94569412298596,12.9212806630537));
#10236=CARTESIAN_POINT('Ctrl Pts',(3.10573094069481,2.9263990494975,12.9185314203321));
#10237=CARTESIAN_POINT('Ctrl Pts',(3.03567049819908,2.89281956792869,12.9138890654744));
#10238=CARTESIAN_POINT('Ctrl Pts',(3.00798081011377,2.87905457277214,12.9120217628384));
#10239=CARTESIAN_POINT('Ctrl Pts',(2.97006541102245,2.85952080884865,12.9094138491821));
#10240=CARTESIAN_POINT('Ctrl Pts',(2.95966578189501,2.85409092352391,12.9086931724371));
#10241=CARTESIAN_POINT('Ctrl Pts',(2.94214561115178,2.84482114719977,12.9074695724265));
#10242=CARTESIAN_POINT('Ctrl Pts',(2.93500933157743,2.841010939726,12.9069685009313));
#10243=CARTESIAN_POINT('Ctrl Pts',(2.92137187678723,2.83366350071366,12.906005674878));
#10244=CARTESIAN_POINT('Ctrl Pts',(2.91486843024113,2.83013068466764,12.9055442184075));
#10245=CARTESIAN_POINT('Ctrl Pts',(2.89932614673029,2.82161830578856,12.9044359875086));
#10246=CARTESIAN_POINT('Ctrl Pts',(2.89029901177816,2.81661770361597,12.903787906869));
#10247=CARTESIAN_POINT('Ctrl Pts',(2.85779971090961,2.79841010176745,12.9014391791299));
#10248=CARTESIAN_POINT('Ctrl Pts',(2.83447004431859,2.7849527583687,12.8997237796098));
#10249=CARTESIAN_POINT('Ctrl Pts',(2.66584667633639,2.68484764025082,12.8871249561621));
#10250=CARTESIAN_POINT('Ctrl Pts',(2.52741954039008,2.58717848896796,12.8757034219781));
#10251=CARTESIAN_POINT('Ctrl Pts',(2.27798024077954,2.37999320192958,12.8537674463824));
#10252=CARTESIAN_POINT('Ctrl Pts',(2.16595314362284,2.27238306191774,12.8432842875182));
#10253=CARTESIAN_POINT('Ctrl Pts',(1.98270926928234,2.06898544425127,12.8252476824585));
#10254=CARTESIAN_POINT('Ctrl Pts',(1.90823076345392,1.97653118871277,12.8175957438341));
#10255=CARTESIAN_POINT('Ctrl Pts',(1.82323786911562,1.85820933382615,12.8084483277612));
#10256=CARTESIAN_POINT('Ctrl Pts',(1.80773973075249,1.83605050135093,12.8067611715887));
#10257=CARTESIAN_POINT('Ctrl Pts',(1.78361391579044,1.80061468314072,12.8041032200917));
#10258=CARTESIAN_POINT('Ctrl Pts',(1.77480230591938,1.78746504653802,12.8031254888156));
#10259=CARTESIAN_POINT('Ctrl Pts',(1.7583960480067,1.7625874538957,12.8012916207077));
#10260=CARTESIAN_POINT('Ctrl Pts',(1.75078012239798,1.75087403676891,12.8004346999934));
#10261=CARTESIAN_POINT('Ctrl Pts',(1.73379112888625,1.72436910719446,12.7985101535118));
#10262=CARTESIAN_POINT('Ctrl Pts',(1.7244619111404,1.70954990888216,12.7974441706748));
#10263=CARTESIAN_POINT('Ctrl Pts',(1.70084292389648,1.67134465608744,12.7947211088799));
#10264=CARTESIAN_POINT('Ctrl Pts',(1.68672965839136,1.64785074475509,12.7930704834745));
#10265=CARTESIAN_POINT('Ctrl Pts',(1.56633419568821,1.44151451785189,12.7787725176692));
#10266=CARTESIAN_POINT('Ctrl Pts',(1.47798439372229,1.24879489861585,12.7668123694457));
#10267=CARTESIAN_POINT('Ctrl Pts',(1.35364031562009,0.887504212192018,12.7454246640629));
#10268=CARTESIAN_POINT('Ctrl Pts',(1.31102808707795,0.72208242657127,12.7359741007249));
#10269=CARTESIAN_POINT('Ctrl Pts',(1.2733007208603,0.505912383712873,12.7232538653564));
#10270=CARTESIAN_POINT('Ctrl Pts',(1.26599196824303,0.457562516161085,12.7203845244984));
#10271=CARTESIAN_POINT('Ctrl Pts',(1.25573093626501,0.377377089863857,12.7155586696377));
#10272=CARTESIAN_POINT('Ctrl Pts',(1.25214725977861,0.345629323396932,12.7136306506186));
#10273=CARTESIAN_POINT('Ctrl Pts',(1.24787919925338,0.30200920164946,12.7109514988501));
#10274=CARTESIAN_POINT('Ctrl Pts',(1.24678753001809,0.290177390756196,12.7102217536085));
#10275=CARTESIAN_POINT('Ctrl Pts',(1.24506006218668,0.270250704656202,12.7089872333189));
#10276=CARTESIAN_POINT('Ctrl Pts',(1.24438936907204,0.262158828956796,12.7084843876311));
#10277=CARTESIAN_POINT('Ctrl Pts',(1.24316823701675,0.246717261086248,12.7075217583553));
#10278=CARTESIAN_POINT('Ctrl Pts',(1.24261241919079,0.239368075555769,12.7070622953139));
#10279=CARTESIAN_POINT('Ctrl Pts',(1.24120391249241,0.2198544909123,12.7058389567956));
#10280=CARTESIAN_POINT('Ctrl Pts',(1.24039505798525,0.207687188476975,12.7050726936982));
#10281=CARTESIAN_POINT('Ctrl Pts',(1.23773990807846,0.164002115223861,12.7023097672006));
#10282=CARTESIAN_POINT('Ctrl Pts',(1.23628780042375,0.132463312770913,12.7002930985489));
#10283=CARTESIAN_POINT('Ctrl Pts',(1.22448456204126,-0.244311594846807,
12.6759790780607));
#10284=CARTESIAN_POINT('Ctrl Pts',(1.26922898318824,-0.589041015268961,
12.6518085214495));
#10285=CARTESIAN_POINT('Ctrl Pts',(1.38581085210585,-0.980370320995771,
12.625158704807));
#10286=CARTESIAN_POINT('Ctrl Pts',(1.40551539561215,-1.04007229488903,12.6211053095696));
#10287=CARTESIAN_POINT('Ctrl Pts',(1.44236004250517,-1.14162355173332,12.6142332775771));
#10288=CARTESIAN_POINT('Ctrl Pts',(1.45865702174169,-1.18375707821254,12.6113888553529));
#10289=CARTESIAN_POINT('Ctrl Pts',(1.4831962438025,-1.24343908603298,12.6073676045592));
#10290=CARTESIAN_POINT('Ctrl Pts',(1.49071872181435,-1.26127592487877,12.6061667979425));
#10291=CARTESIAN_POINT('Ctrl Pts',(1.50404672723625,-1.29209983173182,12.6040931151261));
#10292=CARTESIAN_POINT('Ctrl Pts',(1.50977830782964,-1.30511808970727,12.603217757476));
#10293=CARTESIAN_POINT('Ctrl Pts',(1.52171391878816,-1.3317482142607,12.6014278710306));
#10294=CARTESIAN_POINT('Ctrl Pts',(1.52792691538541,-1.34535570192071,12.6005136751708));
#10295=CARTESIAN_POINT('Ctrl Pts',(1.54395320699319,-1.37981880262653,12.5981990607555));
#10296=CARTESIAN_POINT('Ctrl Pts',(1.55389600868042,-1.40061352522789,12.5968031321633));
#10297=CARTESIAN_POINT('Ctrl Pts',(1.59294297434135,-1.48007580164221,12.59146965895));
#10298=CARTESIAN_POINT('Ctrl Pts',(1.62361084589942,-1.53796009082808,12.5875864836286));
#10299=CARTESIAN_POINT('Ctrl Pts',(1.82150488730791,-1.88544335459233,12.5641947607128));
#10300=CARTESIAN_POINT('Ctrl Pts',(2.0311709514052,-2.14844655108265,12.5463802934115));
#10301=CARTESIAN_POINT('Ctrl Pts',(2.31196539467383,-2.40611913816037,12.5242485648804));
#10302=CARTESIAN_POINT('Ctrl Pts',(2.34711166352935,-2.43698917163063,12.5214992888348));
#10303=CARTESIAN_POINT('Ctrl Pts',(2.40658716930032,-2.48697764356547,12.5168568829425));
#10304=CARTESIAN_POINT('Ctrl Pts',(2.43054301448473,-2.50653088262194,12.5149895633222));
#10305=CARTESIAN_POINT('Ctrl Pts',(2.46397008586001,-2.53302247447593,12.5123816297132));
#10306=CARTESIAN_POINT('Ctrl Pts',(2.47320425305622,-2.54025898574482,12.5116609503992));
#10307=CARTESIAN_POINT('Ctrl Pts',(2.4888721994674,-2.55239993338525,12.5104373473017));
#10308=CARTESIAN_POINT('Ctrl Pts',(2.49528542216456,-2.55733094515154,12.5099362753104));
#10309=CARTESIAN_POINT('Ctrl Pts',(2.50760133950425,-2.56672685862988,12.5089734493419));
#10310=CARTESIAN_POINT('Ctrl Pts',(2.51350094753726,-2.57119565002111,12.5085119934587));
#10311=CARTESIAN_POINT('Ctrl Pts',(2.52766341740478,-2.58184675647691,12.5074037653441));
#10312=CARTESIAN_POINT('Ctrl Pts',(2.53594062357905,-2.58800973717229,12.5067556869159));
#10313=CARTESIAN_POINT('Ctrl Pts',(2.56592626462596,-2.6101131553157,12.5044069775835));
#10314=CARTESIAN_POINT('Ctrl Pts',(2.58780403541401,-2.62582056938119,12.5026915945608));
#10315=CARTESIAN_POINT('Ctrl Pts',(2.74860490422625,-2.73824224349261,12.4900861121656));
#10316=CARTESIAN_POINT('Ctrl Pts',(2.89474768326844,-2.8241434324512,12.4786572505607));
#10317=CARTESIAN_POINT('Ctrl Pts',(3.18637835362486,-2.96597844620731,12.4567191528118));
#10318=CARTESIAN_POINT('Ctrl Pts',(3.33053632435742,-3.02364693790833,12.4462411388403));
#10319=CARTESIAN_POINT('Ctrl Pts',(3.59129349320956,-3.10671099593496,12.4282113290634));
#10320=CARTESIAN_POINT('Ctrl Pts',(3.70620321469813,-3.13644525442325,12.4205612013085));
#10321=CARTESIAN_POINT('Ctrl Pts',(3.84901240458805,-3.16509793537076,12.4114156115129));
#10322=CARTESIAN_POINT('Ctrl Pts',(3.87558803885065,-3.17008293929334,12.409728562755));
#10323=CARTESIAN_POINT('Ctrl Pts',(3.91781629810821,-3.17745515259895,12.4070707408858));
#10324=CARTESIAN_POINT('Ctrl Pts',(3.93342872877015,-3.18006240069309,12.4060930329751));
#10325=CARTESIAN_POINT('Ctrl Pts',(3.96285706663703,-3.18475429442643,12.4042591853959));
#10326=CARTESIAN_POINT('Ctrl Pts',(3.97666850011975,-3.18686431301914,12.4034022620349));
#10327=CARTESIAN_POINT('Ctrl Pts',(4.00782061276383,-3.19141641518297,12.4014776791398));
#10328=CARTESIAN_POINT('Ctrl Pts',(4.02516844051225,-3.19380712635601,12.4004116628017));
#10329=CARTESIAN_POINT('Ctrl Pts',(4.06971536768892,-3.19957657568628,12.397688456489));
#10330=CARTESIAN_POINT('Ctrl Pts',(4.09693997644385,-3.20275000468555,12.3960377212503));
#10331=CARTESIAN_POINT('Ctrl Pts',(4.33403374495199,-3.22732542235886,12.3817714188112));
#10332=CARTESIAN_POINT('Ctrl Pts',(4.54550260105667,-3.22842202195993,12.3698392355282));
#10333=CARTESIAN_POINT('Ctrl Pts',(4.91798138865993,-3.19370093934476,12.3488981862817));
#10334=CARTESIAN_POINT('Ctrl Pts',(5.07898401990814,-3.16625772812626,12.3398564251453));
#10335=CARTESIAN_POINT('Ctrl Pts',(5.31514417693471,-3.10728943927905,12.325802516139));
#10336=CARTESIAN_POINT('Ctrl Pts',(5.39232009816608,-3.084923204585,12.3210766100853));
#10337=CARTESIAN_POINT('Ctrl Pts',(5.48394688357945,-3.05461441152921,12.3152161762111));
#10338=CARTESIAN_POINT('Ctrl Pts',(5.49928201198969,-3.04941322299876,12.3142267885455));
#10339=CARTESIAN_POINT('Ctrl Pts',(5.52313552910312,-3.04112189900822,12.3126734865469));
#10340=CARTESIAN_POINT('Ctrl Pts',(5.53168142742914,-3.03811094628702,12.3121141075238));
#10341=CARTESIAN_POINT('Ctrl Pts',(5.54761242537416,-3.03242238627542,12.3110657385685));
#10342=CARTESIAN_POINT('Ctrl Pts',(5.55500053250379,-3.02975378082513,12.3105772774782));
#10343=CARTESIAN_POINT('Ctrl Pts',(5.57185613235565,-3.02359573250288,12.3094577242184));
#10344=CARTESIAN_POINT('Ctrl Pts',(5.5813170353997,-3.02008882343736,12.3088256171271));
#10345=CARTESIAN_POINT('Ctrl Pts',(5.60645625573877,-3.01063586056169,12.3071364030628));
#10346=CARTESIAN_POINT('Ctrl Pts',(5.62210466530556,-3.00461186255643,12.3060749417688));
#10347=CARTESIAN_POINT('Ctrl Pts',(5.7565902080672,-2.95163172675197,12.2968706456738));
#10348=CARTESIAN_POINT('Ctrl Pts',(5.87257240794169,-2.89777310594636,12.2883833695715));
#10349=CARTESIAN_POINT('Ctrl Pts',(6.1708839703949,-2.73705376730441,12.2655890021648));
#10350=CARTESIAN_POINT('Ctrl Pts',(6.34646159466809,-2.6188974861744,12.2511835575357));
#10351=CARTESIAN_POINT('Ctrl Pts',(6.59984640436162,-2.40953727643423,12.2295372133662));
#10352=CARTESIAN_POINT('Ctrl Pts',(6.68631071990159,-2.3297527877283,12.221956470714));
#10353=CARTESIAN_POINT('Ctrl Pts',(6.78702288341076,-2.22606472267618,12.2128809011621));
#10354=CARTESIAN_POINT('Ctrl Pts',(6.80557219741457,-2.20648131556224,12.2111979965357));
#10355=CARTESIAN_POINT('Ctrl Pts',(6.83460386556999,-2.17505004780455,12.2085451760659));
#10356=CARTESIAN_POINT('Ctrl Pts',(6.84524829377783,-2.1633542593425,12.207568369822));
#10357=CARTESIAN_POINT('Ctrl Pts',(6.86513526886889,-2.1411772774605,12.2057353128842));
#10358=CARTESIAN_POINT('Ctrl Pts',(6.87439653775097,-2.13071343971381,12.2048782858412));
#10359=CARTESIAN_POINT('Ctrl Pts',(6.8951242350167,-2.10698508113077,12.2029522902023));
#10360=CARTESIAN_POINT('Ctrl Pts',(6.90655112002233,-2.0936864889109,12.2018849751087));
#10361=CARTESIAN_POINT('Ctrl Pts',(6.93560703155391,-2.05930760673307,12.1991561646069));
#10362=CARTESIAN_POINT('Ctrl Pts',(6.95307621695464,-2.03809363790473,12.1975011699074));
#10363=CARTESIAN_POINT('Ctrl Pts',(7.09807638440555,-1.85734815055128,12.1836334219675));
#10364=CARTESIAN_POINT('Ctrl Pts',(7.21045377309074,-1.68624278667474,12.1720567753647));
#10365=CARTESIAN_POINT('Ctrl Pts',(7.38905693971152,-1.34823458912725,12.1506434341339));
#10366=CARTESIAN_POINT('Ctrl Pts',(7.45903448048918,-1.18422980717912,12.140798669982));
#10367=CARTESIAN_POINT('Ctrl Pts',(7.53044644192222,-0.969097934124585,
12.1276565582434));
#10368=CARTESIAN_POINT('Ctrl Pts',(7.54473358000822,-0.922555974668644,
12.1247993016484));
#10369=CARTESIAN_POINT('Ctrl Pts',(7.56661394311815,-0.845062629067053,
12.1199918723882));
#10370=CARTESIAN_POINT('Ctrl Pts',(7.5748123556431,-0.814289234928381,12.1180699183353));
#10371=CARTESIAN_POINT('Ctrl Pts',(7.58543782081593,-0.771889357120676,
12.115397874579));
#10372=CARTESIAN_POINT('Ctrl Pts',(7.58825893293793,-0.760362326530088,
12.1146690249373));
#10373=CARTESIAN_POINT('Ctrl Pts',(7.59290221207841,-0.740925647767541,
12.1134355851471));
#10374=CARTESIAN_POINT('Ctrl Pts',(7.5947583121602,-0.733024079335304,12.1129329166605));
#10375=CARTESIAN_POINT('Ctrl Pts',(7.59824348841837,-0.717931513197416,
12.111970276808));
#10376=CARTESIAN_POINT('Ctrl Pts',(7.59987776802665,-0.710741801622296,
12.1115106238061));
#10377=CARTESIAN_POINT('Ctrl Pts',(7.60371683245668,-0.693580284382329,
12.1104109929231));
#10378=CARTESIAN_POINT('Ctrl Pts',(7.60589890169122,-0.683603553226435,
12.1097697527912));
#10379=CARTESIAN_POINT('Ctrl Pts',(7.61351266386181,-0.647982021254438,
12.1074735972572));
#10380=CARTESIAN_POINT('Ctrl Pts',(7.6186786751694,-0.622282303269627,12.1058047643183));
#10381=CARTESIAN_POINT('Ctrl Pts',(7.66039724929173,-0.400790100694894,
12.0913335325743));
#10382=CARTESIAN_POINT('Ctrl Pts',(7.67903638184453,-0.202077454925135,
12.0777860519143));
#10383=CARTESIAN_POINT('Ctrl Pts',(7.67921866061281,-0.00195693911181231,
12.0642560913868));
#10384=CARTESIAN_POINT('Ctrl Pts',(7.67921910621818,-0.000978464247689706,
12.0641899395814));
#10385=CARTESIAN_POINT('Ctrl Pts',(7.67921910621823,-1.80065651569973E-10,
12.0641237905203));
#10386=CARTESIAN_POINT('Origin',(4.45646910621825,-5.13094777615093E-16,
-2.31077344927308));
#10387=CARTESIAN_POINT('',(7.67921909946346,0.000172060260772193,10.8112112210413));
#10388=CARTESIAN_POINT('',(7.67921910621823,4.13684814843145E-12,11.0603093566956));
#10389=CARTESIAN_POINT('',(7.67921910621823,-3.51191647465084E-13,-2.31077344927308));
#10390=CARTESIAN_POINT('',(7.67921883037524,0.00133339637767557,12.3082266921078));
#10391=CARTESIAN_POINT('Ctrl Pts',(7.67921910621823,4.13684814843145E-12,
11.0603093566956));
#10392=CARTESIAN_POINT('Ctrl Pts',(7.67921910621823,-0.000978691749929005,
11.0603640893182));
#10393=CARTESIAN_POINT('Ctrl Pts',(7.6792186604013,-0.00195739598008107,
11.0604188236236));
#10394=CARTESIAN_POINT('Ctrl Pts',(7.67904758692959,-0.189731801402226,
11.0709203693113));
#10395=CARTESIAN_POINT('Ctrl Pts',(7.66263724333298,-0.376135903192157,
11.0813693796804));
#10396=CARTESIAN_POINT('Ctrl Pts',(7.62554174357558,-0.586353128666877,
11.0941687338931));
#10397=CARTESIAN_POINT('Ctrl Pts',(7.62057205216903,-0.612604125605327,
11.0957857537902));
#10398=CARTESIAN_POINT('Ctrl Pts',(7.61323707430009,-0.648875527346521,
11.0980497544362));
#10399=CARTESIAN_POINT('Ctrl Pts',(7.61114912889885,-0.658951744915312,
11.0986818887872));
#10400=CARTESIAN_POINT('Ctrl Pts',(7.60747807361002,-0.676250486208489,
11.0997728929118));
#10401=CARTESIAN_POINT('Ctrl Pts',(7.60591828335012,-0.68347795191097,11.1002304507979));
#10402=CARTESIAN_POINT('Ctrl Pts',(7.60259803063439,-0.698610002476913,
11.1011921894131));
#10403=CARTESIAN_POINT('Ctrl Pts',(7.60083263348986,-0.706513374217232,
11.1016966607099));
#10404=CARTESIAN_POINT('Ctrl Pts',(7.59642807764261,-0.725888271816524,
11.102938529704));
#10405=CARTESIAN_POINT('Ctrl Pts',(7.59375583437939,-0.737352087267582,
11.1036777791226));
#10406=CARTESIAN_POINT('Ctrl Pts',(7.58377558417166,-0.779130369775862,
11.1063875035056));
#10407=CARTESIAN_POINT('Ctrl Pts',(7.57609076160968,-0.809351900783152,
11.1083777567132));
#10408=CARTESIAN_POINT('Ctrl Pts',(7.55564617089128,-0.885131161045326,
11.1134361643206));
#10409=CARTESIAN_POINT('Ctrl Pts',(7.54231972362599,-0.930527356070157,
11.1165287636591));
#10410=CARTESIAN_POINT('Ctrl Pts',(7.47706380636555,-1.13597345241519,11.1307621369488));
#10411=CARTESIAN_POINT('Ctrl Pts',(7.4136496190919,-1.29209444827668,11.1422265556533));
#10412=CARTESIAN_POINT('Ctrl Pts',(7.24954036859994,-1.61994659645458,11.1669649109007));
#10413=CARTESIAN_POINT('Ctrl Pts',(7.14453799737394,-1.78879369389825,11.1801285828953));
#10414=CARTESIAN_POINT('Ctrl Pts',(6.99939537129697,-1.98025042203995,11.1953789822275));
#10415=CARTESIAN_POINT('Ctrl Pts',(6.97348954364359,-2.01307578225376,11.1980080857866));
#10416=CARTESIAN_POINT('Ctrl Pts',(6.93516356939034,-2.05974179764837,11.2017685004541));
#10417=CARTESIAN_POINT('Ctrl Pts',(6.92325183129595,-2.07399265310841,11.2029200267265));
#10418=CARTESIAN_POINT('Ctrl Pts',(6.90204912210327,-2.09891785632107,11.2049399947677));
#10419=CARTESIAN_POINT('Ctrl Pts',(6.89280988842858,-2.10963536772769,11.2058105170673));
#10420=CARTESIAN_POINT('Ctrl Pts',(6.87354844187395,-2.13168333783996,11.2076056087064));
#10421=CARTESIAN_POINT('Ctrl Pts',(6.86351642726592,-2.14300480031042,11.208529741018));
#10422=CARTESIAN_POINT('Ctrl Pts',(6.83748225095625,-2.17197177008911,11.2109006582316));
#10423=CARTESIAN_POINT('Ctrl Pts',(6.82136331771991,-2.18951144789662,11.2123425019607));
#10424=CARTESIAN_POINT('Ctrl Pts',(6.75109062967667,-2.26429658693185,11.218519729137));
#10425=CARTESIAN_POINT('Ctrl Pts',(6.69503938127266,-2.31972661717589,11.2231731475022));
#10426=CARTESIAN_POINT('Ctrl Pts',(6.53537825877686,-2.46643548092471,11.2357796146883));
#10427=CARTESIAN_POINT('Ctrl Pts',(6.42784844943309,-2.55320089576116,11.2435659992456));
#10428=CARTESIAN_POINT('Ctrl Pts',(6.13667874027008,-2.75875007111114,11.2635291721455));
#10429=CARTESIAN_POINT('Ctrl Pts',(5.94595913438762,-2.86621754563971,11.275555351935));
#10430=CARTESIAN_POINT('Ctrl Pts',(5.71154865503173,-2.96855104290203,11.290741840794));
#10431=CARTESIAN_POINT('Ctrl Pts',(5.67697098965047,-2.98293393263337,11.2929925309254));
#10432=CARTESIAN_POINT('Ctrl Pts',(5.63001147617826,-3.00151400845297,11.2960734256265));
#10433=CARTESIAN_POINT('Ctrl Pts',(5.61784181895103,-3.00624374355983,11.2968740184334));
#10434=CARTESIAN_POINT('Ctrl Pts',(5.59860120598885,-3.01358733997101,11.2981437043337));
#10435=CARTESIAN_POINT('Ctrl Pts',(5.59154908833675,-3.01625062294471,11.2986099000534));
#10436=CARTESIAN_POINT('Ctrl Pts',(5.57700487189572,-3.02168512123565,11.2995732058822));
#10437=CARTESIAN_POINT('Ctrl Pts',(5.56951179144285,-3.02445323148031,11.3000705052422));
#10438=CARTESIAN_POINT('Ctrl Pts',(5.55150579438006,-3.03102907209611,11.3012678365657));
#10439=CARTESIAN_POINT('Ctrl Pts',(5.54098325279889,-3.0348099844112,11.3019694256215));
#10440=CARTESIAN_POINT('Ctrl Pts',(5.50463489484315,-3.04765733281829,11.3043988921674));
#10441=CARTESIAN_POINT('Ctrl Pts',(5.47871418307278,-3.05644918587328,11.3061416995402));
#10442=CARTESIAN_POINT('Ctrl Pts',(5.41491064716071,-3.07718785343146,11.3104514079697));
#10443=CARTESIAN_POINT('Ctrl Pts',(5.37691354786026,-3.08876626081083,11.3130349096823));
#10444=CARTESIAN_POINT('Ctrl Pts',(5.22051589591655,-3.13328145452372,11.3237115703974));
#10445=CARTESIAN_POINT('Ctrl Pts',(5.10049698743856,-3.16013365532247,11.3320005480398));
#10446=CARTESIAN_POINT('Ctrl Pts',(4.72235662512426,-3.22229685985559,11.3579195217586));
#10447=CARTESIAN_POINT('Ctrl Pts',(4.46124441515921,-3.23325226299835,11.3754404989111));
#10448=CARTESIAN_POINT('Ctrl Pts',(4.16241650436121,-3.2095479040965,11.3944371762699));
#10449=CARTESIAN_POINT('Ctrl Pts',(4.12326515513776,-3.20571989235086,11.3969076814506));
#10450=CARTESIAN_POINT('Ctrl Pts',(4.06618514457591,-3.19908184221559,11.4004840681602));
#10451=CARTESIAN_POINT('Ctrl Pts',(4.04819573555253,-3.19683579187826,11.4016075110291));
#10452=CARTESIAN_POINT('Ctrl Pts',(4.0162684177267,-3.19257563687982,11.4035950748661));
#10453=CARTESIAN_POINT('Ctrl Pts',(4.00232308227447,-3.19062176421459,11.4044610681076));
#10454=CARTESIAN_POINT('Ctrl Pts',(3.97323172784513,-3.18635119673012,11.4062633159448));
#10455=CARTESIAN_POINT('Ctrl Pts',(3.95808849479013,-3.18401775931291,11.4071990187233));
#10456=CARTESIAN_POINT('Ctrl Pts',(3.91856225998225,-3.17763821995725,11.4096352968336));
#10457=CARTESIAN_POINT('Ctrl Pts',(3.89420786100196,-3.17341941385261,11.4111303872281));
#10458=CARTESIAN_POINT('Ctrl Pts',(3.78338083700313,-3.15290540173152,11.4179091869772));
#10459=CARTESIAN_POINT('Ctrl Pts',(3.69754517663288,-3.13335232264249,11.4230890407422));
#10460=CARTESIAN_POINT('Ctrl Pts',(3.34676165286698,-3.03818126721864,11.4441297859574));
#10461=CARTESIAN_POINT('Ctrl Pts',(3.0912781516922,-2.93227525318054,11.4590455379355));
#10462=CARTESIAN_POINT('Ctrl Pts',(2.83184276159427,-2.7833913837344,11.4761535701754));
#10463=CARTESIAN_POINT('Ctrl Pts',(2.81143444126037,-2.77137858590893,11.4775144258895));
#10464=CARTESIAN_POINT('Ctrl Pts',(2.72529584922079,-2.71938876111501,11.4833303972237));
#10465=CARTESIAN_POINT('Ctrl Pts',(2.6608810191872,-2.67729294076745,11.487859785427));
#10466=CARTESIAN_POINT('Ctrl Pts',(2.58451951153603,-2.62339401083963,11.4935312901317));
#10467=CARTESIAN_POINT('Ctrl Pts',(2.57107353285406,-2.61374729582814,11.4945417496268));
#10468=CARTESIAN_POINT('Ctrl Pts',(2.55023763166598,-2.59855430705072,11.4961270654055));
#10469=CARTESIAN_POINT('Ctrl Pts',(2.54279604115322,-2.59307892597518,11.4966971886456));
#10470=CARTESIAN_POINT('Ctrl Pts',(2.52908845097391,-2.58290199957926,11.4977548527623));
#10471=CARTESIAN_POINT('Ctrl Pts',(2.52281595714934,-2.57820953851906,11.4982417705361));
#10472=CARTESIAN_POINT('Ctrl Pts',(2.50857047234511,-2.56747124502946,11.4993542976546));
#10473=CARTESIAN_POINT('Ctrl Pts',(2.50060852705559,-2.56141114826782,11.4999808849298));
#10474=CARTESIAN_POINT('Ctrl Pts',(2.47620531938287,-2.54265694787415,11.5019157958421));
#10475=CARTESIAN_POINT('Ctrl Pts',(2.45985882884333,-2.52984117445728,11.5032321891396));
#10476=CARTESIAN_POINT('Ctrl Pts',(2.42199608070531,-2.49956096045932,11.5063267764986));
#10477=CARTESIAN_POINT('Ctrl Pts',(2.40057918344838,-2.48197542362974,11.5081121610438));
#10478=CARTESIAN_POINT('Ctrl Pts',(2.32605653766171,-2.41915808436957,11.5144410230817));
#10479=CARTESIAN_POINT('Ctrl Pts',(2.2741974848701,-2.37248243873286,11.5190568512391));
#10480=CARTESIAN_POINT('Ctrl Pts',(2.07052539828312,-2.17683678891236,11.5379351860183));
#10481=CARTESIAN_POINT('Ctrl Pts',(1.93210077453762,-2.01467599240331,11.5524984109024));
#10482=CARTESIAN_POINT('Ctrl Pts',(1.73140636231103,-1.72609953531858,11.5758291490185));
#10483=CARTESIAN_POINT('Ctrl Pts',(1.65958750919274,-1.60712439048832,11.5848402089506));
#10484=CARTESIAN_POINT('Ctrl Pts',(1.58355731945138,-1.46054309564896,11.5952268862625));
#10485=CARTESIAN_POINT('Ctrl Pts',(1.57174199827352,-1.43706570734369,11.5968700235363));
#10486=CARTESIAN_POINT('Ctrl Pts',(1.55268457107457,-1.39801564115407,11.5995700282398));
#10487=CARTESIAN_POINT('Ctrl Pts',(1.54527755670816,-1.38252527635991,11.6006325923202));
#10488=CARTESIAN_POINT('Ctrl Pts',(1.53207895050924,-1.35434644216353,11.6025504687986));
#10489=CARTESIAN_POINT('Ctrl Pts',(1.52624530070121,-1.34167825035857,11.6034072175087));
#10490=CARTESIAN_POINT('Ctrl Pts',(1.51386611533915,-1.31433006817151,11.6052452383843));
#10491=CARTESIAN_POINT('Ctrl Pts',(1.50734777256357,-1.29963812811037,11.6062255604608));
#10492=CARTESIAN_POINT('Ctrl Pts',(1.48971303192609,-1.25907459335024,11.6089131165678));
#10493=CARTESIAN_POINT('Ctrl Pts',(1.47882520381993,-1.23310474115358,11.6106125716609));
#10494=CARTESIAN_POINT('Ctrl Pts',(1.41624538143159,-1.07817416417145,11.6206317981295));
#10495=CARTESIAN_POINT('Ctrl Pts',(1.37259289356336,-0.946115242427954,
11.6286760763592));
#10496=CARTESIAN_POINT('Ctrl Pts',(1.28980684874658,-0.627994041516914,
11.6473414407405));
#10497=CARTESIAN_POINT('Ctrl Pts',(1.25833077457372,-0.440494492926915,
11.6577824273708));
#10498=CARTESIAN_POINT('Ctrl Pts',(1.23373667137521,-0.126075299624717,
11.6756424952873));
#10499=CARTESIAN_POINT('Ctrl Pts',(1.23127269959557,-0.000380615296982113,
11.6828823604304));
#10500=CARTESIAN_POINT('Ctrl Pts',(1.23679864356387,0.141844133949329,11.6914988498626));
#10501=CARTESIAN_POINT('Ctrl Pts',(1.23757863459981,0.15856150566911,11.6925183421518));
#10502=CARTESIAN_POINT('Ctrl Pts',(1.2390370478985,0.185337916165719,11.6941630826639));
#10503=CARTESIAN_POINT('Ctrl Pts',(1.23963254275298,0.195401409026146,11.6947839077818));
#10504=CARTESIAN_POINT('Ctrl Pts',(1.24077603574011,0.213301064458868,11.6958931752251));
#10505=CARTESIAN_POINT('Ctrl Pts',(1.24130547906815,0.221138229832411,11.6963805798441));
#10506=CARTESIAN_POINT('Ctrl Pts',(1.24250789712175,0.238019218530842,11.6974342263589));
#10507=CARTESIAN_POINT('Ctrl Pts',(1.24319038174068,0.247062008491229,11.6980009656996));
#10508=CARTESIAN_POINT('Ctrl Pts',(1.24520044188864,0.27227635048743,11.6995874803384));
#10509=CARTESIAN_POINT('Ctrl Pts',(1.24661197599933,0.28844067589552,11.7006117389568));
#10510=CARTESIAN_POINT('Ctrl Pts',(1.25579314380662,0.385147208826615,11.7067798460935));
#10511=CARTESIAN_POINT('Ctrl Pts',(1.26647125483765,0.465377637834308,11.7120638974129));
#10512=CARTESIAN_POINT('Ctrl Pts',(1.30762353524697,0.70516721361332,11.7281997086415));
#10513=CARTESIAN_POINT('Ctrl Pts',(1.34714905757414,0.862911292366838,11.739264962974));
#10514=CARTESIAN_POINT('Ctrl Pts',(1.46497644901045,1.21721302943449,11.764441969432));
#10515=CARTESIAN_POINT('Ctrl Pts',(1.55107007936994,1.41043310090803,11.7783901046834));
#10516=CARTESIAN_POINT('Ctrl Pts',(1.6690102569144,1.61769647661509,11.7934051510063));
#10517=CARTESIAN_POINT('Ctrl Pts',(1.68286876840089,1.64134395165133,11.7951199783696));
#10518=CARTESIAN_POINT('Ctrl Pts',(1.70607413426041,1.67980705473906,11.7979126286919));
#10519=CARTESIAN_POINT('Ctrl Pts',(1.71524286721299,1.69472799259804,11.798996846783));
#10520=CARTESIAN_POINT('Ctrl Pts',(1.73194509131987,1.7214185124042,11.8009381139648));
#10521=CARTESIAN_POINT('Ctrl Pts',(1.73943431278229,1.73321514637385,11.8017967610808));
#10522=CARTESIAN_POINT('Ctrl Pts',(1.75557159269913,1.75827210365081,11.8036221638665));
#10523=CARTESIAN_POINT('Ctrl Pts',(1.76424113675216,1.77151820296095,11.8045880925586));
#10524=CARTESIAN_POINT('Ctrl Pts',(1.78798410413118,1.80721794278911,11.8071943451218));
#10525=CARTESIAN_POINT('Ctrl Pts',(1.80324332580989,1.82954691793712,11.8088276690067));
#10526=CARTESIAN_POINT('Ctrl Pts',(1.8869591174586,1.94879854200651,11.8175726274125));
#10527=CARTESIAN_POINT('Ctrl Pts',(1.96045186665671,2.04208221883733,11.8244876130443));
#10528=CARTESIAN_POINT('Ctrl Pts',(2.14157176600435,2.24754556426695,11.8401459484117));
#10529=CARTESIAN_POINT('Ctrl Pts',(2.25249498917068,2.35641910651263,11.8487713625466));
#10530=CARTESIAN_POINT('Ctrl Pts',(2.49970191536184,2.56627252074296,11.8669283903286));
#10531=CARTESIAN_POINT('Ctrl Pts',(2.63696350998806,2.66534761487728,11.876446943503));
#10532=CARTESIAN_POINT('Ctrl Pts',(2.80434943085274,2.76719055605803,11.8881926546349));
#10533=CARTESIAN_POINT('Ctrl Pts',(2.82753273765578,2.78090078839968,11.8898225452397));
#10534=CARTESIAN_POINT('Ctrl Pts',(2.85983290088742,2.79946010972262,11.8921015057698));
#10535=CARTESIAN_POINT('Ctrl Pts',(2.86880602333693,2.8045587900115,11.8927354660463));
#10536=CARTESIAN_POINT('Ctrl Pts',(2.88425633767143,2.81324001119805,11.89382878287));
#10537=CARTESIAN_POINT('Ctrl Pts',(2.89072173162477,2.81684353604128,11.894286814871));
#10538=CARTESIAN_POINT('Ctrl Pts',(2.90428023565949,2.82433934489387,11.8952485542498));
#10539=CARTESIAN_POINT('Ctrl Pts',(2.91137563640776,2.82822721673375,11.8957525461371));
#10540=CARTESIAN_POINT('Ctrl Pts',(2.92879687160709,2.83768792987388,11.8969915598155));
#10541=CARTESIAN_POINT('Ctrl Pts',(2.93913858890091,2.84323114342978,11.8977284144185));
#10542=CARTESIAN_POINT('Ctrl Pts',(2.97684959418558,2.86318009722167,11.9004195797089));
#10543=CARTESIAN_POINT('Ctrl Pts',(3.00439465755385,2.87724760854169,11.9023933256723));
#10544=CARTESIAN_POINT('Ctrl Pts',(3.07410665991517,2.91159418514974,11.9074007530025));
#10545=CARTESIAN_POINT('Ctrl Pts',(3.11651989023072,2.93135502564482,11.9104582955685));
#10546=CARTESIAN_POINT('Ctrl Pts',(3.4656478501972,3.08485794785006,11.9356318364543));
#10547=CARTESIAN_POINT('Ctrl Pts',(3.79107840754225,3.17102644228206,11.9588445125763));
#10548=CARTESIAN_POINT('Ctrl Pts',(4.18889971442039,3.21228580812286,11.984598124893));
#10549=CARTESIAN_POINT('Ctrl Pts',(4.25398196640656,3.21704420846337,11.9887410366056));
#10550=CARTESIAN_POINT('Ctrl Pts',(4.34216371387288,3.22080449791538,11.994262728989));
#10551=CARTESIAN_POINT('Ctrl Pts',(4.3651699440188,3.22153873849655,11.9956949485987));
#10552=CARTESIAN_POINT('Ctrl Pts',(4.40313192585424,3.22234329203948,11.9980448761718));
#10553=CARTESIAN_POINT('Ctrl Pts',(4.41808351676838,3.2225560825376,11.9989670014789));
#10554=CARTESIAN_POINT('Ctrl Pts',(4.44726502520892,3.2227682690688,12.0007602760201));
#10555=CARTESIAN_POINT('Ctrl Pts',(4.46149450482491,3.22277749570648,12.001631711573));
#10556=CARTESIAN_POINT('Ctrl Pts',(4.49510514568959,3.22257668185406,12.0036832185075));
#10557=CARTESIAN_POINT('Ctrl Pts',(4.51448540914642,3.22228604378204,12.0048607490557));
#10558=CARTESIAN_POINT('Ctrl Pts',(4.57915408971273,3.22073260235598,12.0087729133907));
#10559=CARTESIAN_POINT('Ctrl Pts',(4.6244195651695,3.21868964796209,12.0114832539261));
#10560=CARTESIAN_POINT('Ctrl Pts',(4.73259156779437,3.21151921904056,12.0179039516255));
#10561=CARTESIAN_POINT('Ctrl Pts',(4.79542079024282,3.20549711656875,12.0215874103393));
#10562=CARTESIAN_POINT('Ctrl Pts',(5.19165243688261,3.15573739974705,12.0446297194061));
#10563=CARTESIAN_POINT('Ctrl Pts',(5.51659325538989,3.06190208872768,12.0624557908975));
#10564=CARTESIAN_POINT('Ctrl Pts',(5.85575968986766,2.90337153703621,12.0846699154591));
#10565=CARTESIAN_POINT('Ctrl Pts',(5.89011608816558,2.88656135560115,12.0869674869881));
#10566=CARTESIAN_POINT('Ctrl Pts',(5.93588472811248,2.86314867231562,12.0901032031835));
#10567=CARTESIAN_POINT('Ctrl Pts',(5.94756891320646,2.85708107233618,12.0909103830337));
#10568=CARTESIAN_POINT('Ctrl Pts',(5.96590310900927,2.84741702361747,12.0921880139532));
#10569=CARTESIAN_POINT('Ctrl Pts',(5.97257835379497,2.84386839741559,12.0926555044932));
#10570=CARTESIAN_POINT('Ctrl Pts',(5.98612980002014,2.83660304253335,12.0936094161364));
#10571=CARTESIAN_POINT('Ctrl Pts',(5.99300498945145,2.83288477234763,12.0940959461785));
#10572=CARTESIAN_POINT('Ctrl Pts',(6.00928205416367,2.82400505459335,12.0952538266617));
#10573=CARTESIAN_POINT('Ctrl Pts',(6.01867177874385,2.81882163357949,12.0959265503405));
#10574=CARTESIAN_POINT('Ctrl Pts',(6.03870017181669,2.80763452802438,12.0973714406658));
#10575=CARTESIAN_POINT('Ctrl Pts',(6.04933090070736,2.80161704749301,12.0981444229905));
#10576=CARTESIAN_POINT('Ctrl Pts',(6.07849629427805,2.7848884405216,12.1002812902777));
#10577=CARTESIAN_POINT('Ctrl Pts',(6.09695850697849,2.77405304528776,12.1016520884313));
#10578=CARTESIAN_POINT('Ctrl Pts',(6.15630956149059,2.73842048441058,12.1061144379651));
#10579=CARTESIAN_POINT('Ctrl Pts',(6.1967532842698,2.71289786619919,12.1092414831599));
#10580=CARTESIAN_POINT('Ctrl Pts',(6.37984055542981,2.59157898589117,12.1237488907221));
#10581=CARTESIAN_POINT('Ctrl Pts',(6.51524493031847,2.48537287449146,12.1354633572611));
#10582=CARTESIAN_POINT('Ctrl Pts',(6.79735182520336,2.22515669248053,12.1613456969005));
#10583=CARTESIAN_POINT('Ctrl Pts',(6.93863271240567,2.06638515019245,12.1753626016913));
#10584=CARTESIAN_POINT('Ctrl Pts',(7.07942216527227,1.87269474230708,12.1904394314919));
#10585=CARTESIAN_POINT('Ctrl Pts',(7.09524969724317,1.85032575909946,12.1921538182579));
#10586=CARTESIAN_POINT('Ctrl Pts',(7.12072119413416,1.81333531969423,12.19494590011));
#10587=CARTESIAN_POINT('Ctrl Pts',(7.1305344164181,1.79883265085385,12.1960299859318));
#10588=CARTESIAN_POINT('Ctrl Pts',(7.14796495644493,1.77261470307994,12.1979711086328));
#10589=CARTESIAN_POINT('Ctrl Pts',(7.1556251440065,1.76092858764597,12.1988297425504));
#10590=CARTESIAN_POINT('Ctrl Pts',(7.1718021871384,1.73589587020527,12.2006552145705));
#10591=CARTESIAN_POINT('Ctrl Pts',(7.18029720731496,1.72253554453937,12.2016212249853));
#10592=CARTESIAN_POINT('Ctrl Pts',(7.20303866731209,1.68618056162621,12.2042279379456));
#10593=CARTESIAN_POINT('Ctrl Pts',(7.21709481641753,1.66306794696448,12.2058616361951));
#10594=CARTESIAN_POINT('Ctrl Pts',(7.29128521373943,1.53754318610722,12.2146130112867));
#10595=CARTESIAN_POINT('Ctrl Pts',(7.34601833158008,1.43203743172263,12.221533680445));
#10596=CARTESIAN_POINT('Ctrl Pts',(7.50209949664125,1.08558063208721,12.2432565024709));
#10597=CARTESIAN_POINT('Ctrl Pts',(7.58003042799952,0.835282469259103,12.2574077007351));
#10598=CARTESIAN_POINT('Ctrl Pts',(7.63798520752686,0.517579001566154,12.2760516264132));
#10599=CARTESIAN_POINT('Ctrl Pts',(7.64731980758917,0.456512386987226,12.2796696021478));
#10600=CARTESIAN_POINT('Ctrl Pts',(7.65832034987787,0.367487389848901,12.2850418986793));
#10601=CARTESIAN_POINT('Ctrl Pts',(7.66138615378078,0.339713065685527,12.2867317287733));
#10602=CARTESIAN_POINT('Ctrl Pts',(7.66521301089827,0.300357594063791,12.2891500471769));
#10603=CARTESIAN_POINT('Ctrl Pts',(7.66627334392751,0.288805948951008,12.2898627781235));
#10604=CARTESIAN_POINT('Ctrl Pts',(7.6679582024821,0.2692937171048,12.2910719534643));
#10605=CARTESIAN_POINT('Ctrl Pts',(7.66861556138497,0.261335934111689,12.2915665805529));
#10606=CARTESIAN_POINT('Ctrl Pts',(7.66981775725156,0.246092238856737,12.29251704469));
#10607=CARTESIAN_POINT('Ctrl Pts',(7.67036740132274,0.238806803366017,12.29297259082));
#10608=CARTESIAN_POINT('Ctrl Pts',(7.67149353305973,0.223171569119474,12.2939529109828));
#10609=CARTESIAN_POINT('Ctrl Pts',(7.67206227469203,0.214821287746002,12.2944781046257));
#10610=CARTESIAN_POINT('Ctrl Pts',(7.67335950428873,0.194614582118339,12.2957528141746));
#10611=CARTESIAN_POINT('Ctrl Pts',(7.67405497275093,0.182756259358044,12.296504043653));
#10612=CARTESIAN_POINT('Ctrl Pts',(7.67768381420142,0.114419421775526,12.3008503987718));
#10613=CARTESIAN_POINT('Ctrl Pts',(7.67919543476754,0.0578793639106088,
12.304513948662));
#10614=CARTESIAN_POINT('Ctrl Pts',(7.67921883037524,0.00133339637767557,
12.3082266921078));
#10615=CARTESIAN_POINT('Ctrl Pts',(7.6792188285542,0.00133779050316054,
12.3082264035946));
#10616=CARTESIAN_POINT('Ctrl Pts',(7.67921901366479,0.000891857374298317,
12.308255683033));
#10617=CARTESIAN_POINT('Ctrl Pts',(7.67921910621823,0.000445927208297339,
12.3082849653206));
#10618=CARTESIAN_POINT('Ctrl Pts',(7.67921910621823,3.33464896044866E-11,
12.3083142504469));
#10619=CARTESIAN_POINT('Ctrl Pts',(7.67921910621823,-1.80070125477272E-10,
12.0641237905203));
#10620=CARTESIAN_POINT('Ctrl Pts',(7.67921910623054,0.220223674247331,12.0492355694953));
#10621=CARTESIAN_POINT('Ctrl Pts',(7.6566461785926,0.439904518120074,12.0345467987471));
#10622=CARTESIAN_POINT('Ctrl Pts',(7.60348141468906,0.695784317002951,12.0179601641892));
#10623=CARTESIAN_POINT('Ctrl Pts',(7.59436437097806,0.735809650992355,12.0153791528641));
#10624=CARTESIAN_POINT('Ctrl Pts',(7.5803823102935,0.792195940043441,12.0117608083892));
#10625=CARTESIAN_POINT('Ctrl Pts',(7.57614852599569,0.808707889004498,12.0107033809678));
#10626=CARTESIAN_POINT('Ctrl Pts',(7.56814013939585,0.838941864390323,12.0087709310081));
#10627=CARTESIAN_POINT('Ctrl Pts',(7.56440529012875,0.852673887028682,12.0078946503945));
#10628=CARTESIAN_POINT('Ctrl Pts',(7.55663175939393,0.880525260543539,12.0061200941527));
#10629=CARTESIAN_POINT('Ctrl Pts',(7.552587279485,0.894642654354233,12.0052220302843));
#10630=CARTESIAN_POINT('Ctrl Pts',(7.54231194754444,0.929604655910437,12.0030012414111));
#10631=CARTESIAN_POINT('Ctrl Pts',(7.53596619612086,0.950414944436179,12.0016822836236));
#10632=CARTESIAN_POINT('Ctrl Pts',(7.5109721779184,1.02950094478521,11.9966793787643));
#10633=CARTESIAN_POINT('Ctrl Pts',(7.49087576490687,1.08730776049391,11.9930428097661));
#10634=CARTESIAN_POINT('Ctrl Pts',(7.43545603159794,1.23318820622243,11.9838868717474));
#10635=CARTESIAN_POINT('Ctrl Pts',(7.39786705934426,1.32033946090253,11.9784383134237));
#10636=CARTESIAN_POINT('Ctrl Pts',(7.26736789938451,1.58956253537082,11.9614708766129));
#10637=CARTESIAN_POINT('Ctrl Pts',(7.16097357143027,1.76451448333438,11.9502648967615));
#10638=CARTESIAN_POINT('Ctrl Pts',(7.00963137616278,1.9671925982126,11.9358484172731));
#10639=CARTESIAN_POINT('Ctrl Pts',(6.97964616158735,2.00550778828141,11.9330511638447));
#10640=CARTESIAN_POINT('Ctrl Pts',(6.9089977411522,2.09168921400619,11.92655564984));
#10641=CARTESIAN_POINT('Ctrl Pts',(6.8677812061394,2.13907299375599,11.9228334040076));
#10642=CARTESIAN_POINT('Ctrl Pts',(6.81466414182491,2.1966510065224,11.9180735088394));
#10643=CARTESIAN_POINT('Ctrl Pts',(6.80403562790972,2.20800608567754,11.9171228345294));
#10644=CARTESIAN_POINT('Ctrl Pts',(6.78711986355854,2.22581801149646,11.9156116990101));
#10645=CARTESIAN_POINT('Ctrl Pts',(6.7808868500872,2.23232634718757,11.9150552874418));
#10646=CARTESIAN_POINT('Ctrl Pts',(6.76971150626549,2.2438977745161,11.9140582081819));
#10647=CARTESIAN_POINT('Ctrl Pts',(6.76477970281994,2.24897083353874,11.9136183538537));
#10648=CARTESIAN_POINT('Ctrl Pts',(6.75290665460124,2.26110375058687,11.912559858883));
#10649=CARTESIAN_POINT('Ctrl Pts',(6.74594959421759,2.26814785088999,11.911939994256));
#10650=CARTESIAN_POINT('Ctrl Pts',(6.72467346626776,2.28949253943776,11.9100457466175));
#10651=CARTESIAN_POINT('Ctrl Pts',(6.71025236808401,2.30369009788425,11.9087637634295));
#10652=CARTESIAN_POINT('Ctrl Pts',(6.57792824521665,2.43153135117997,11.8970262685726));
#10653=CARTESIAN_POINT('Ctrl Pts',(6.4516689512312,2.53615840650527,11.8860213886354));
#10654=CARTESIAN_POINT('Ctrl Pts',(6.15469770637899,2.74630112738081,11.8614278720506));
#10655=CARTESIAN_POINT('Ctrl Pts',(5.98094434977684,2.84642618032661,11.8478781345625));
#10656=CARTESIAN_POINT('Ctrl Pts',(5.7156013817188,2.96801649833694,11.8288419701231));
#10657=CARTESIAN_POINT('Ctrl Pts',(5.63058958983003,3.0026621195026,11.8229643458874));
#10658=CARTESIAN_POINT('Ctrl Pts',(5.51970978380955,3.04241912504131,11.8155747419029));
#10659=CARTESIAN_POINT('Ctrl Pts',(5.49510576315501,3.05090623087821,11.8139519136509));
#10660=CARTESIAN_POINT('Ctrl Pts',(5.45558650835282,3.06400482378726,11.8113716504733));
#10661=CARTESIAN_POINT('Ctrl Pts',(5.44073629958786,3.06880746368696,11.8104079557328));
#10662=CARTESIAN_POINT('Ctrl Pts',(5.41249211727007,3.0777156779338,11.8085860262564));
#10663=CARTESIAN_POINT('Ctrl Pts',(5.39910516402675,3.08184215432441,11.8077271237873));
#10664=CARTESIAN_POINT('Ctrl Pts',(5.36857705916762,3.09103479594336,11.80577878941));
#10665=CARTESIAN_POINT('Ctrl Pts',(5.35141971937201,3.09604593757507,11.8046911722217));
#10666=CARTESIAN_POINT('Ctrl Pts',(5.29867032934833,3.11097730641304,11.8013692753442));
#10667=CARTESIAN_POINT('Ctrl Pts',(5.26294788974635,3.1204286310937,11.799150165121));
#10668=CARTESIAN_POINT('Ctrl Pts',(5.09016954695058,3.16297636604587,11.7885520867415));
#10669=CARTESIAN_POINT('Ctrl Pts',(4.95119657956384,3.18767108367891,11.7804431528228));
#10670=CARTESIAN_POINT('Ctrl Pts',(4.58726014989438,3.22795634216087,11.7597424254733));
#10671=CARTESIAN_POINT('Ctrl Pts',(4.36151944620187,3.22920725055079,11.7474447921891));
#10672=CARTESIAN_POINT('Ctrl Pts',(4.06116664416522,3.19933418790658,11.7299949288011));
#10673=CARTESIAN_POINT('Ctrl Pts',(3.98512666545837,3.18901827998858,11.7254776524982));
#10674=CARTESIAN_POINT('Ctrl Pts',(3.89323889988093,3.1731943998788,11.7198198290195));
#10675=CARTESIAN_POINT('Ctrl Pts',(3.87696610934467,3.17026295672794,11.7188101978106));
#10676=CARTESIAN_POINT('Ctrl Pts',(3.85164090077474,3.16549928043924,11.7172259452684));
#10677=CARTESIAN_POINT('Ctrl Pts',(3.84257231951007,3.16375308500252,11.716656047468));
#10678=CARTESIAN_POINT('Ctrl Pts',(3.82582614007766,3.16045382328994,11.715598646352));
#10679=CARTESIAN_POINT('Ctrl Pts',(3.81814658605979,3.15891172334973,11.7151117645995));
#10680=CARTESIAN_POINT('Ctrl Pts',(3.80066751894192,3.15533548256719,11.7139991226772));
#10681=CARTESIAN_POINT('Ctrl Pts',(3.79087185604669,3.1532836890576,11.7133723830575));
#10682=CARTESIAN_POINT('Ctrl Pts',(3.76076054193737,3.14683003359098,11.7114363318822));
#10683=CARTESIAN_POINT('Ctrl Pts',(3.74047825306778,3.14227731311064,11.7101189364605));
#10684=CARTESIAN_POINT('Ctrl Pts',(3.69323668938031,3.13119199119303,11.7070215542541));
#10685=CARTESIAN_POINT('Ctrl Pts',(3.66631520671211,3.12450695535757,11.7052343593985));
#10686=CARTESIAN_POINT('Ctrl Pts',(3.57190394239094,3.09976496004786,11.6988966574035));
#10687=CARTESIAN_POINT('Ctrl Pts',(3.50492129018556,3.07986264111225,11.6942735954374));
#10688=CARTESIAN_POINT('Ctrl Pts',(3.23623886210338,2.99042841080317,11.6753436950448));
#10689=CARTESIAN_POINT('Ctrl Pts',(3.04100674687627,2.90311892647591,11.6607353114752));
#10690=CARTESIAN_POINT('Ctrl Pts',(2.73602052805816,2.72859507165688,11.6374175157297));
#10691=CARTESIAN_POINT('Ctrl Pts',(2.62072147831916,2.6523977438883,11.6284579607456));
#10692=CARTESIAN_POINT('Ctrl Pts',(2.48971916744451,2.55317484496912,11.6181211032822));
#10693=CARTESIAN_POINT('Ctrl Pts',(2.46898057113399,2.53706454374651,11.6164793686601));
#10694=CARTESIAN_POINT('Ctrl Pts',(2.43501735358665,2.51000894529688,11.6137812414612));
#10695=CARTESIAN_POINT('Ctrl Pts',(2.42167944198256,2.49920850155493,11.6127191650596));
#10696=CARTESIAN_POINT('Ctrl Pts',(2.39766152151381,2.4794401271263,11.6108018957496));
#10697=CARTESIAN_POINT('Ctrl Pts',(2.38695230920184,2.47050850057202,11.6099452696033));
#10698=CARTESIAN_POINT('Ctrl Pts',(2.36402317226441,2.45113157301568,11.6081072144645));
#10699=CARTESIAN_POINT('Ctrl Pts',(2.35182270974581,2.44066374890149,11.6071267375644));
#10700=CARTESIAN_POINT('Ctrl Pts',(2.31845542800445,2.41159883067978,11.6044379903333));
#10701=CARTESIAN_POINT('Ctrl Pts',(2.29745306211572,2.39281449468743,11.6027375117796));
#10702=CARTESIAN_POINT('Ctrl Pts',(2.17407128205378,2.27951565041241,11.5926933473035));
#10703=CARTESIAN_POINT('Ctrl Pts',(2.07765619194766,2.1787123070302,11.5846268638287));
#10704=CARTESIAN_POINT('Ctrl Pts',(1.86552823064782,1.92599740819466,11.5658940719076));
#10705=CARTESIAN_POINT('Ctrl Pts',(1.75619065494535,1.76944470664022,11.5554096703205));
#10706=CARTESIAN_POINT('Ctrl Pts',(1.59940400760066,1.49625307534337,11.5375651204653));
#10707=CARTESIAN_POINT('Ctrl Pts',(1.54378671469099,1.38487125356914,11.5303919072017));
#10708=CARTESIAN_POINT('Ctrl Pts',(1.48816131788502,1.2552074855191,11.5218502635722));
#10709=CARTESIAN_POINT('Ctrl Pts',(1.48169114895505,1.23979556217569,11.5208320030074));
#10710=CARTESIAN_POINT('Ctrl Pts',(1.47151393111779,1.21501508765922,11.5191889054141));
#10711=CARTESIAN_POINT('Ctrl Pts',(1.46773032463518,1.20567804562248,11.5185684780571));
#10712=CARTESIAN_POINT('Ctrl Pts',(1.46107519190689,1.18903092595743,11.5174596974215));
#10713=CARTESIAN_POINT('Ctrl Pts',(1.45818652740502,1.18172789624985,11.516972379024));
#10714=CARTESIAN_POINT('Ctrl Pts',(1.45201887750108,1.16596683977823,11.5159186562171));
#10715=CARTESIAN_POINT('Ctrl Pts',(1.4487489533227,1.15750564811413,11.5153517525427));
#10716=CARTESIAN_POINT('Ctrl Pts',(1.43972446679359,1.13385761871625,11.5137641485953));
#10717=CARTESIAN_POINT('Ctrl Pts',(1.43404900964207,1.11864116371261,11.5127389547059));
#10718=CARTESIAN_POINT('Ctrl Pts',(1.40068398725088,1.02707854151743,11.5065509939708));
#10719=CARTESIAN_POINT('Ctrl Pts',(1.37577564988708,0.94975706260412,11.5012469955488));
#10720=CARTESIAN_POINT('Ctrl Pts',(1.30995361568709,0.715444949027674,11.4851035086846));
#10721=CARTESIAN_POINT('Ctrl Pts',(1.27794155792669,0.556220906086365,11.4740526136909));
#10722=CARTESIAN_POINT('Ctrl Pts',(1.2321857967585,0.185975661357574,11.4488974658969));
#10723=CARTESIAN_POINT('Ctrl Pts',(1.22692197046327,-0.0253815361453739,
11.4349569508367));
#10724=CARTESIAN_POINT('Ctrl Pts',(1.24435981001886,-0.26310166646629,11.4199489368552));
#10725=CARTESIAN_POINT('Ctrl Pts',(1.24671333211472,-0.290407580425181,
11.41823423667));
#10726=CARTESIAN_POINT('Ctrl Pts',(1.25114104351235,-0.33510624733189,11.4154418129523));
#10727=CARTESIAN_POINT('Ctrl Pts',(1.25300916797354,-0.35251755986187,11.4143576950389));
#10728=CARTESIAN_POINT('Ctrl Pts',(1.2566227920913,-0.383792034940419,11.4124166210896));
#10729=CARTESIAN_POINT('Ctrl Pts',(1.25831669986068,-0.397660603501415,
11.4115580672226));
#10730=CARTESIAN_POINT('Ctrl Pts',(1.26212193619423,-0.427216880753332,
11.4097328787171));
#10731=CARTESIAN_POINT('Ctrl Pts',(1.264258768027,-0.442900978287249,11.4087670707483));
#10732=CARTESIAN_POINT('Ctrl Pts',(1.27035851962529,-0.485332880446873,
11.406161187575));
#10733=CARTESIAN_POINT('Ctrl Pts',(1.27454270339344,-0.512047956223543,
11.4045281100179));
#10734=CARTESIAN_POINT('Ctrl Pts',(1.29889139434481,-0.655661396283384,
11.3957855121279));
#10735=CARTESIAN_POINT('Ctrl Pts',(1.32516328904076,-0.771438434329466,
11.3888725168799));
#10736=CARTESIAN_POINT('Ctrl Pts',(1.40038725642705,-1.03467216221648,11.3732211608344));
#10737=CARTESIAN_POINT('Ctrl Pts',(1.45372761201006,-1.18056276128543,11.364600531952));
#10738=CARTESIAN_POINT('Ctrl Pts',(1.58676839199512,-1.47633202276641,11.3464411885921));
#10739=CARTESIAN_POINT('Ctrl Pts',(1.66820167335284,-1.62489666084929,11.336915467499));
#10740=CARTESIAN_POINT('Ctrl Pts',(1.77566523256052,-1.78889170212943,11.3251616676655));
#10741=CARTESIAN_POINT('Ctrl Pts',(1.79070808459254,-1.81123190095604,11.3235318469473));
#10742=CARTESIAN_POINT('Ctrl Pts',(1.81189935885067,-1.84186723491647,11.3212530115149));
#10743=CARTESIAN_POINT('Ctrl Pts',(1.81781076837829,-1.85032597916519,11.3206191054174));
#10744=CARTESIAN_POINT('Ctrl Pts',(1.82803128458814,-1.86480212271782,11.3195258894289));
#10745=CARTESIAN_POINT('Ctrl Pts',(1.83232072458879,-1.87083339922545,11.3190679039009));
#10746=CARTESIAN_POINT('Ctrl Pts',(1.84134220619562,-1.88342621456326,11.3181062731231));
#10747=CARTESIAN_POINT('Ctrl Pts',(1.84607821012626,-1.88998475481941,11.3176023434937));
#10748=CARTESIAN_POINT('Ctrl Pts',(1.85774280189033,-1.90601070213575,11.3163635059266));
#10749=CARTESIAN_POINT('Ctrl Pts',(1.86469845193362,-1.91545818723699,11.3156267658286));
#10750=CARTESIAN_POINT('Ctrl Pts',(1.89017440807326,-1.94966798776422,11.3129361584839));
#10751=CARTESIAN_POINT('Ctrl Pts',(1.90899861926493,-1.97420052027516,11.3109628647708));
#10752=CARTESIAN_POINT('Ctrl Pts',(1.95717746703219,-2.03515275411314,11.3059567432344));
#10753=CARTESIAN_POINT('Ctrl Pts',(1.98697688944659,-2.07121055852537,11.3029000674229));
#10754=CARTESIAN_POINT('Ctrl Pts',(2.23606312980758,-2.35958992983217,11.2777481393411));
#10755=CARTESIAN_POINT('Ctrl Pts',(2.49262234709484,-2.57706247502939,11.2545572636626));
#10756=CARTESIAN_POINT('Ctrl Pts',(2.83401623413867,-2.78532841998298,11.2288033108617));
#10757=CARTESIAN_POINT('Ctrl Pts',(2.89096202238079,-2.81772892592821,11.224643388743));
#10758=CARTESIAN_POINT('Ctrl Pts',(2.96923153900141,-2.85915604308597,11.2191030593982));
#10759=CARTESIAN_POINT('Ctrl Pts',(2.98971930407134,-2.86972018188014,11.2176687455785));
#10760=CARTESIAN_POINT('Ctrl Pts',(3.02368719361504,-2.88677628452276,11.2153163583304));
#10761=CARTESIAN_POINT('Ctrl Pts',(3.03710205444235,-2.89339567123651,11.2143938481195));
#10762=CARTESIAN_POINT('Ctrl Pts',(3.06336153212007,-2.90612648750706,11.2126005169973));
#10763=CARTESIAN_POINT('Ctrl Pts',(3.07620146085871,-2.91224674638006,11.2117294048702));
#10764=CARTESIAN_POINT('Ctrl Pts',(3.10660948320878,-2.92649470117636,11.2096797364911));
#10765=CARTESIAN_POINT('Ctrl Pts',(3.12421123765801,-2.93454957954183,11.2085037091601));
#10766=CARTESIAN_POINT('Ctrl Pts',(3.18311983945182,-2.96086793377446,11.2046015279199));
#10767=CARTESIAN_POINT('Ctrl Pts',(3.22473900220289,-2.97842215443572,11.2018994959622));
#10768=CARTESIAN_POINT('Ctrl Pts',(3.32511899383177,-3.01829649873181,11.1955018847928));
#10769=CARTESIAN_POINT('Ctrl Pts',(3.38419138395671,-3.03978420454166,11.1918329381576));
#10770=CARTESIAN_POINT('Ctrl Pts',(3.77159633858511,-3.16800347026377,11.1682829642504));
#10771=CARTESIAN_POINT('Ctrl Pts',(4.11456495857461,-3.22309192692174,11.1500374569534));
#10772=CARTESIAN_POINT('Ctrl Pts',(4.49145464435115,-3.22271677207613,11.1275475132918));
#10773=CARTESIAN_POINT('Ctrl Pts',(4.52322871360484,-3.2222151330177,11.125630791769));
#10774=CARTESIAN_POINT('Ctrl Pts',(4.56720963865016,-3.22087000448166,11.1229426981498));
#10775=CARTESIAN_POINT('Ctrl Pts',(4.57942803175382,-3.22042670197447,11.1221921701828));
#10776=CARTESIAN_POINT('Ctrl Pts',(4.59901322797788,-3.21960450152842,11.1209827009971));
#10777=CARTESIAN_POINT('Ctrl Pts',(4.60638190657565,-3.21926981202584,11.1205261941671));
#10778=CARTESIAN_POINT('Ctrl Pts',(4.62185321793741,-3.21851386335856,11.1195645237478));
#10779=CARTESIAN_POINT('Ctrl Pts',(4.62995547006626,-3.21808729988793,11.1190590566389));
#10780=CARTESIAN_POINT('Ctrl Pts',(4.64988859051627,-3.21696237536811,11.1178111072399));
#10781=CARTESIAN_POINT('Ctrl Pts',(4.66171731068068,-3.2162293428344,11.1170667324173));
#10782=CARTESIAN_POINT('Ctrl Pts',(4.70520670843476,-3.21329339198362,11.1143165930574));
#10783=CARTESIAN_POINT('Ctrl Pts',(4.73683724621753,-3.21068814229316,11.1122902910883));
#10784=CARTESIAN_POINT('Ctrl Pts',(4.81665020025041,-3.20292601077256,11.1071199351535));
#10785=CARTESIAN_POINT('Ctrl Pts',(4.86476334008476,-3.19714885221963,11.103950127269));
#10786=CARTESIAN_POINT('Ctrl Pts',(5.08730863716374,-3.16532174860641,11.0890945311827));
#10787=CARTESIAN_POINT('Ctrl Pts',(5.25954232120868,-3.126066361025,11.0770612481191));
#10788=CARTESIAN_POINT('Ctrl Pts',(5.62438551802157,-3.01075414149152,11.0512764874949));
#10789=CARTESIAN_POINT('Ctrl Pts',(5.81468190077913,-2.92983866604257,11.0376553469737));
#10790=CARTESIAN_POINT('Ctrl Pts',(6.02221814101125,-2.81699142197774,11.0227804948697));
#10791=CARTESIAN_POINT('Ctrl Pts',(6.04827422450781,-2.80235031241455,11.0209116022635));
#10792=CARTESIAN_POINT('Ctrl Pts',(6.08861467606917,-2.77893848804436,11.0180152102385));
#10793=CARTESIAN_POINT('Ctrl Pts',(6.10304015938343,-2.77041550410005,11.0169788774665));
#10794=CARTESIAN_POINT('Ctrl Pts',(6.12909592291001,-2.75474561532282,11.0151056958175));
#10795=CARTESIAN_POINT('Ctrl Pts',(6.14074843466152,-2.74763662552363,11.0142674948921));
#10796=CARTESIAN_POINT('Ctrl Pts',(6.16592703566354,-2.73205524634707,11.012455086251));
#10797=CARTESIAN_POINT('Ctrl Pts',(6.17943610946637,-2.72355594795934,11.0114818940404));
#10798=CARTESIAN_POINT('Ctrl Pts',(6.20720905344388,-2.70579312608946,11.0094792104312));
#10799=CARTESIAN_POINT('Ctrl Pts',(6.22146387079355,-2.6965163270345,11.0084502453134));
#10800=CARTESIAN_POINT('Ctrl Pts',(6.29281827183956,-2.64927181028644,11.0032932267952));
#10801=CARTESIAN_POINT('Ctrl Pts',(6.34877175810351,-2.60959978934597,10.9992290454581));
#10802=CARTESIAN_POINT('Ctrl Pts',(6.49246358577995,-2.50066584478156,10.9886913692953));
#10803=CARTESIAN_POINT('Ctrl Pts',(6.57794065420054,-2.42857251610717,10.9823210782168));
#10804=CARTESIAN_POINT('Ctrl Pts',(6.85242546700345,-2.17149198577975,10.9611273833903));
#10805=CARTESIAN_POINT('Ctrl Pts',(7.0223557567631,-1.96778337828671,10.9467807596889));
#10806=CARTESIAN_POINT('Ctrl Pts',(7.18290855974081,-1.71862718751688,10.9290996327766));
#10807=CARTESIAN_POINT('Ctrl Pts',(7.19991957875737,-1.69133995103716,10.9271606304123));
#10808=CARTESIAN_POINT('Ctrl Pts',(7.22286060953618,-1.65328355438285,10.9244462478727));
#10809=CARTESIAN_POINT('Ctrl Pts',(7.22914216457237,-1.64272717181336,10.9236922499977));
#10810=CARTESIAN_POINT('Ctrl Pts',(7.23910431644646,-1.62576548768821,10.9224786281062));
#10811=CARTESIAN_POINT('Ctrl Pts',(7.24282357833584,-1.61938287235636,10.9220214696629));
#10812=CARTESIAN_POINT('Ctrl Pts',(7.2505763285439,-1.60597261801255,10.921059832261));
#10813=CARTESIAN_POINT('Ctrl Pts',(7.25460528627269,-1.59894250445306,10.920555058309));
#10814=CARTESIAN_POINT('Ctrl Pts',(7.26443525670486,-1.58163929210865,10.9193112006158));
#10815=CARTESIAN_POINT('Ctrl Pts',(7.27020641674,-1.57134944867043,10.9185702514656));
#10816=CARTESIAN_POINT('Ctrl Pts',(7.29111549839727,-1.53358450546202,10.9158469576761));
#10817=CARTESIAN_POINT('Ctrl Pts',(7.30590799905327,-1.50592145516734,10.9138445805711));
#10818=CARTESIAN_POINT('Ctrl Pts',(7.34216750077239,-1.43566606181642,10.9087485431914));
#10819=CARTESIAN_POINT('Ctrl Pts',(7.36309669245342,-1.39280575584128,10.9056300007568));
#10820=CARTESIAN_POINT('Ctrl Pts',(7.45464594297158,-1.19426709515922,10.8911902089749));
#10821=CARTESIAN_POINT('Ctrl Pts',(7.51375933613255,-1.0335915424067,10.8795374249385));
#10822=CARTESIAN_POINT('Ctrl Pts',(7.60187594792293,-0.718905664837764,
10.8574962158966));
#10823=CARTESIAN_POINT('Ctrl Pts',(7.63296332552938,-0.565954231945592,
10.8471144209096));
#10824=CARTESIAN_POINT('Ctrl Pts',(7.66177825343877,-0.342041428854369,
10.8325427447077));
#10825=CARTESIAN_POINT('Ctrl Pts',(7.66844056163603,-0.272469536252241,
10.8280987125428));
#10826=CARTESIAN_POINT('Ctrl Pts',(7.67429102637126,-0.17965099168277,10.8222771897009));
#10827=CARTESIAN_POINT('Ctrl Pts',(7.67549736894351,-0.156555029264165,
10.8208373831447));
#10828=CARTESIAN_POINT('Ctrl Pts',(7.67708334470026,-0.118286674984217,
10.8184657677264));
#10829=CARTESIAN_POINT('Ctrl Pts',(7.67760459210728,-0.103121310616642,
10.8175295663393));
#10830=CARTESIAN_POINT('Ctrl Pts',(7.67838502949849,-0.0745352632944399,
10.8157715506668));
#10831=CARTESIAN_POINT('Ctrl Pts',(7.67866751960757,-0.0611155914426918,
10.8149490269002));
#10832=CARTESIAN_POINT('Ctrl Pts',(7.67900178879491,-0.0385312124607307,
10.8135693095553));
#10833=CARTESIAN_POINT('Ctrl Pts',(7.67909832803428,-0.0293674311609509,
10.8130107342684));
#10834=CARTESIAN_POINT('Ctrl Pts',(7.67919852553884,-0.0133846288352081,
10.8120386483023));
#10835=CARTESIAN_POINT('Ctrl Pts',(7.67921963167649,-0.00656581911898159,
10.8116246026049));
#10836=CARTESIAN_POINT('Ctrl Pts',(7.67921909628439,0.000253038698648237,
10.8112112210413));
#10837=CARTESIAN_POINT('Origin',(4.45646910621825,-5.13094777615093E-16,
-2.31077344927308));
#10838=CARTESIAN_POINT('',(7.67921910621823,-1.20018596680688E-11,9.56539764702567));
#10839=CARTESIAN_POINT('',(7.67921908851299,0.000264017416110453,9.81380927132941));
#10840=CARTESIAN_POINT('',(7.67921910621823,-3.51191647465084E-13,-2.31077344927308));
#10841=CARTESIAN_POINT('Ctrl Pts',(7.67921907731647,0.000431608942485311,
9.81380931041028));
#10842=CARTESIAN_POINT('Ctrl Pts',(7.67921999593717,-0.00642757427997835,
9.81423341595552));
#10843=CARTESIAN_POINT('Ctrl Pts',(7.67919901631219,-0.0132867957832829,
9.8146568350422));
#10844=CARTESIAN_POINT('Ctrl Pts',(7.67908726875781,-0.0311627145954824,
9.81575854209838));
#10845=CARTESIAN_POINT('Ctrl Pts',(7.67896190832854,-0.0421791588647937,
9.8164357403265));
#10846=CARTESIAN_POINT('Ctrl Pts',(7.6785598212312,-0.0665358320184445,
9.81792919613046));
#10847=CARTESIAN_POINT('Ctrl Pts',(7.67825673277487,-0.0798754686210316,
9.81874461760427));
#10848=CARTESIAN_POINT('Ctrl Pts',(7.67724587273198,-0.114810363339683,
9.82087374072973));
#10849=CARTESIAN_POINT('Ctrl Pts',(7.676403751909,-0.136401288975939,9.82218323111384));
#10850=CARTESIAN_POINT('Ctrl Pts',(7.67247659054794,-0.216416741788965,
9.8270140149127));
#10851=CARTESIAN_POINT('Ctrl Pts',(7.66801786859589,-0.274764496649009,
9.83049256274217));
#10852=CARTESIAN_POINT('Ctrl Pts',(7.65687582983732,-0.382031733374004,
9.83682556887203));
#10853=CARTESIAN_POINT('Ctrl Pts',(7.65065256122217,-0.430980066625157,
9.83969154504362));
#10854=CARTESIAN_POINT('Ctrl Pts',(7.60275977378607,-0.749105943252482,
9.85821572193964));
#10855=CARTESIAN_POINT('Ctrl Pts',(7.52823663255914,-1.01219235733315,9.87295000215523));
#10856=CARTESIAN_POINT('Ctrl Pts',(7.38643664285754,-1.34514943407498,9.89374760571939));
#10857=CARTESIAN_POINT('Ctrl Pts',(7.34793301146621,-1.42603302969453,9.89899372328385));
#10858=CARTESIAN_POINT('Ctrl Pts',(7.29833761037256,-1.51992708460718,9.90543784929495));
#10859=CARTESIAN_POINT('Ctrl Pts',(7.29044516328324,-1.53459265547766,9.90645494356437));
#10860=CARTESIAN_POINT('Ctrl Pts',(7.27803574020009,-1.55722934100019,9.90804233239676));
#10861=CARTESIAN_POINT('Ctrl Pts',(7.27359771370477,-1.56524371728423,9.90860776396864));
#10862=CARTESIAN_POINT('Ctrl Pts',(7.26529732416374,-1.58008325894628,9.90966130530712));
#10863=CARTESIAN_POINT('Ctrl Pts',(7.26144416700374,-1.5869133457858,9.91014883292004));
#10864=CARTESIAN_POINT('Ctrl Pts',(7.2525648634924,-1.60251937807423,9.91126876450845));
#10865=CARTESIAN_POINT('Ctrl Pts',(7.247522327569,-1.61128574437785,9.91190219956568));
#10866=CARTESIAN_POINT('Ctrl Pts',(7.23415518826596,-1.6342732739089,9.91357435620706));
#10867=CARTESIAN_POINT('Ctrl Pts',(7.22576274584919,-1.64845437162698,9.91461719224971));
#10868=CARTESIAN_POINT('Ctrl Pts',(7.16048343881514,-1.75685440318819,9.9226718941789));
#10869=CARTESIAN_POINT('Ctrl Pts',(7.09891775007986,-1.84815881476174,9.92994028631981));
#10870=CARTESIAN_POINT('Ctrl Pts',(6.88754774358668,-2.12942226747186,9.95351278466168));
#10871=CARTESIAN_POINT('Ctrl Pts',(6.72097057431804,-2.30578354131053,9.97007775942203));
#10872=CARTESIAN_POINT('Ctrl Pts',(6.45483559886048,-2.53061292137835,9.99292498399827));
#10873=CARTESIAN_POINT('Ctrl Pts',(6.37007609874208,-2.59530014581036,9.99977477048405));
#10874=CARTESIAN_POINT('Ctrl Pts',(6.2606443924544,-2.67053498375984,10.0081073214428));
#10875=CARTESIAN_POINT('Ctrl Pts',(6.23884891337553,-2.68513088160387,10.0097431269656));
#10876=CARTESIAN_POINT('Ctrl Pts',(6.20578566355649,-2.7066925358365,10.0121896787153));
#10877=CARTESIAN_POINT('Ctrl Pts',(6.19464958698807,-2.71385731496079,10.0130078399992));
#10878=CARTESIAN_POINT('Ctrl Pts',(6.17194538963449,-2.72826776365378,10.0146641699982));
#10879=CARTESIAN_POINT('Ctrl Pts',(6.16037475621262,-2.73550898630452,10.0155021622287));
#10880=CARTESIAN_POINT('Ctrl Pts',(6.13509826111924,-2.75110511622994,10.0173197094045));
#10881=CARTESIAN_POINT('Ctrl Pts',(6.12137523194765,-2.75943160945997,10.018298206435));
#10882=CARTESIAN_POINT('Ctrl Pts',(6.08333762719452,-2.78212399350229,10.020988083634));
#10883=CARTESIAN_POINT('Ctrl Pts',(6.05889519153959,-2.79627355914039,10.0226916144835));
#10884=CARTESIAN_POINT('Ctrl Pts',(5.92225013319539,-2.87299630020352,10.0320832132331));
#10885=CARTESIAN_POINT('Ctrl Pts',(5.80656326373418,-2.92914202500443,10.0395394944507));
#10886=CARTESIAN_POINT('Ctrl Pts',(5.48328746815852,-3.06280054959406,10.0594566277609));
#10887=CARTESIAN_POINT('Ctrl Pts',(5.27059749632247,-3.12606645338749,10.0715583081962));
#10888=CARTESIAN_POINT('Ctrl Pts',(4.98300132281416,-3.18024704468283,10.0882581043715));
#10889=CARTESIAN_POINT('Ctrl Pts',(4.91247621747375,-3.191122637554,10.0923832836022));
#10890=CARTESIAN_POINT('Ctrl Pts',(4.80011499180572,-3.20464904221776,10.0990828012916));
#10891=CARTESIAN_POINT('Ctrl Pts',(4.75848570554201,-3.20883991113459,10.1015924755917));
#10892=CARTESIAN_POINT('Ctrl Pts',(4.70367986426045,-3.21328140379905,10.1049463944504));
#10893=CARTESIAN_POINT('Ctrl Pts',(4.69056467201822,-3.21426349125607,10.1057527423508));
#10894=CARTESIAN_POINT('Ctrl Pts',(4.6690726628246,-3.21574061487841,10.1070807815817));
#10895=CARTESIAN_POINT('Ctrl Pts',(4.66069912534194,-3.21628326954639,10.1075998576704));
#10896=CARTESIAN_POINT('Ctrl Pts',(4.64432358831088,-3.21728029470964,10.1086183820768));
#10897=CARTESIAN_POINT('Ctrl Pts',(4.63632186690846,-3.21773752516636,10.1091176691765));
#10898=CARTESIAN_POINT('Ctrl Pts',(4.61845220994846,-3.21869176236602,10.1102361335892));
#10899=CARTESIAN_POINT('Ctrl Pts',(4.60858353533303,-3.21917324502341,10.1108561574953));
#10900=CARTESIAN_POINT('Ctrl Pts',(4.57448175627935,-3.22067987760433,10.1130064138393));
#10901=CARTESIAN_POINT('Ctrl Pts',(4.55024007181425,-3.22147680173744,10.1145484250521));
#10902=CARTESIAN_POINT('Ctrl Pts',(4.29616469113471,-3.22695917221954,10.1308352988315));
#10903=CARTESIAN_POINT('Ctrl Pts',(4.06648349227644,-3.20731360671786,10.1465799268687));
#10904=CARTESIAN_POINT('Ctrl Pts',(3.70099283993351,-3.13618846072786,10.1716873463901));
#10905=CARTESIAN_POINT('Ctrl Pts',(3.56306871174581,-3.09972026253991,10.1811864651691));
#10906=CARTESIAN_POINT('Ctrl Pts',(3.35180460885189,-3.02858017083324,10.1956401664037));
#10907=CARTESIAN_POINT('Ctrl Pts',(3.27659185432677,-3.00007883328078,10.2007681317039));
#10908=CARTESIAN_POINT('Ctrl Pts',(3.18042427302851,-2.95945981174252,10.2073051036386));
#10909=CARTESIAN_POINT('Ctrl Pts',(3.15843467449651,-2.94988126161821,10.2087985632167));
#10910=CARTESIAN_POINT('Ctrl Pts',(3.12272162497368,-2.93384817300427,10.2112224742302));
#10911=CARTESIAN_POINT('Ctrl Pts',(3.10893349353527,-2.92754081629147,10.212157908962));
#10912=CARTESIAN_POINT('Ctrl Pts',(3.08237725562864,-2.91516534221846,10.2139590087169));
#10913=CARTESIAN_POINT('Ctrl Pts',(3.06960358064444,-2.90911007188638,10.2148250901254));
#10914=CARTESIAN_POINT('Ctrl Pts',(3.04021798882582,-2.8949425001514,10.2168171160729));
#10915=CARTESIAN_POINT('Ctrl Pts',(3.02363510516452,-2.88677086970675,10.2179409746657));
#10916=CARTESIAN_POINT('Ctrl Pts',(2.97021676268909,-2.85987393827861,10.2215611171192));
#10917=CARTESIAN_POINT('Ctrl Pts',(2.93366996804725,-2.84058233292023,10.2240376089029));
#10918=CARTESIAN_POINT('Ctrl Pts',(2.69654880882918,-2.70952339772059,10.2401256202899));
#10919=CARTESIAN_POINT('Ctrl Pts',(2.50803521632308,-2.5772963129953,10.2529493327028));
#10920=CARTESIAN_POINT('Ctrl Pts',(2.22666211390671,-2.33127640734139,10.273849764921));
#10921=CARTESIAN_POINT('Ctrl Pts',(2.12465760471318,-2.22924605974608,10.281909257287));
#10922=CARTESIAN_POINT('Ctrl Pts',(2.00118547724504,-2.08796426713745,10.2928372009946));
#10923=CARTESIAN_POINT('Ctrl Pts',(1.9732083609513,-2.0546114457606,10.2954021874568));
#10924=CARTESIAN_POINT('Ctrl Pts',(1.92753504017212,-1.99786623534622,10.299761361581));
#10925=CARTESIAN_POINT('Ctrl Pts',(1.90946660175892,-1.97477976225421,10.301533596026));
#10926=CARTESIAN_POINT('Ctrl Pts',(1.88475906339256,-1.94230714134396,10.3040296423266));
#10927=CARTESIAN_POINT('Ctrl Pts',(1.87785085165892,-1.93312634445691,10.3047356939684));
#10928=CARTESIAN_POINT('Ctrl Pts',(1.86618998578101,-1.91745569565183,10.3059418280298));
#10929=CARTESIAN_POINT('Ctrl Pts',(1.86141218419524,-1.91098452024827,10.3064401824557));
#10930=CARTESIAN_POINT('Ctrl Pts',(1.8516383609433,-1.89764235847253,10.3074684035336));
#10931=CARTESIAN_POINT('Ctrl Pts',(1.84664523367791,-1.89076944194156,10.3079984452521));
#10932=CARTESIAN_POINT('Ctrl Pts',(1.83371533825434,-1.87282296342465,10.3093832873325));
#10933=CARTESIAN_POINT('Ctrl Pts',(1.82582160950704,-1.86171880592062,10.3102409320988));
#10934=CARTESIAN_POINT('Ctrl Pts',(1.7940193695222,-1.81637629599524,10.3137451130285));
#10935=CARTESIAN_POINT('Ctrl Pts',(1.77070812026272,-1.7817264079612,10.316427719854));
#10936=CARTESIAN_POINT('Ctrl Pts',(1.5683226537705,-1.46790074628903,10.3406982428882));
#10937=CARTESIAN_POINT('Ctrl Pts',(1.43265990537807,-1.1630787726175,10.3638322221651));
#10938=CARTESIAN_POINT('Ctrl Pts',(1.32938882984028,-0.781965047806497,
10.3896074013916));
#10939=CARTESIAN_POINT('Ctrl Pts',(1.31467511713148,-0.720577389254914,
10.3936779065262));
#10940=CARTESIAN_POINT('Ctrl Pts',(1.29251065704203,-0.614440780181416,
10.4005758452427));
#10941=CARTESIAN_POINT('Ctrl Pts',(1.28418447367038,-0.569895679828085,
10.403429321022));
#10942=CARTESIAN_POINT('Ctrl Pts',(1.27364143085589,-0.506064457583524,
10.4074610393373));
#10943=CARTESIAN_POINT('Ctrl Pts',(1.27065532822734,-0.48691256357353,10.4086634290249));
#10944=CARTESIAN_POINT('Ctrl Pts',(1.2657769651137,-0.453655922467149,10.4107390351009));
#10945=CARTESIAN_POINT('Ctrl Pts',(1.26380503151451,-0.439563592348429,
10.4116147447373));
#10946=CARTESIAN_POINT('Ctrl Pts',(1.25995249102548,-0.410636904172278,
10.4134046293212));
#10947=CARTESIAN_POINT('Ctrl Pts',(1.25808165901963,-0.395801576177258,
10.4143184761931));
#10948=CARTESIAN_POINT('Ctrl Pts',(1.25359350737592,-0.358099393691755,
10.4166307673093));
#10949=CARTESIAN_POINT('Ctrl Pts',(1.25111774396813,-0.335216294423932,
10.4180247409525));
#10950=CARTESIAN_POINT('Ctrl Pts',(1.24256620056765,-0.24738709997588,10.4233407297769));
#10951=CARTESIAN_POINT('Ctrl Pts',(1.23821726657937,-0.182286117020922,
10.4272088475887));
#10952=CARTESIAN_POINT('Ctrl Pts',(1.22368624262764,0.217382098415956,10.4506066745609));
#10953=CARTESIAN_POINT('Ctrl Pts',(1.26370030415009,0.551659280171078,10.4684365865389));
#10954=CARTESIAN_POINT('Ctrl Pts',(1.36711407729092,0.918799311953891,10.4905867484897));
#10955=CARTESIAN_POINT('Ctrl Pts',(1.38077800369832,0.963550974159175,10.4933367455716));
#10956=CARTESIAN_POINT('Ctrl Pts',(1.40508433819549,1.03736453542189,10.4979802944308));
#10957=CARTESIAN_POINT('Ctrl Pts',(1.41518016259921,1.06660001078157,10.499848021295));
#10958=CARTESIAN_POINT('Ctrl Pts',(1.42968405265914,1.10671924354929,10.5024564802682));
#10959=CARTESIAN_POINT('Ctrl Pts',(1.43373352358236,1.11773200368874,10.5031772686164));
#10960=CARTESIAN_POINT('Ctrl Pts',(1.44067665639394,1.13630054256862,10.5044010425109));
#10961=CARTESIAN_POINT('Ctrl Pts',(1.44353884711287,1.14386811978149,10.5049021756046));
#10962=CARTESIAN_POINT('Ctrl Pts',(1.44907402817738,1.15833811758942,10.5058651097169));
#10963=CARTESIAN_POINT('Ctrl Pts',(1.4517423455711,1.16524222431301,10.5063266125128));
#10964=CARTESIAN_POINT('Ctrl Pts',(1.4581880719486,1.18175078468853,10.5074349439068));
#10965=CARTESIAN_POINT('Ctrl Pts',(1.46198785217983,1.19134633502655,10.5080830788828));
#10966=CARTESIAN_POINT('Ctrl Pts',(1.47587014289994,1.22591712827557,10.5104319241996));
#10967=CARTESIAN_POINT('Ctrl Pts',(1.48621924417486,1.25078320764716,10.5121473876807));
#10968=CARTESIAN_POINT('Ctrl Pts',(1.56381781853494,1.43083588934329,10.5247438745543));
#10969=CARTESIAN_POINT('Ctrl Pts',(1.64287407995897,1.58063122515684,10.5361627636886));
#10970=CARTESIAN_POINT('Ctrl Pts',(1.81627938863639,1.85461212870683,10.5580975998598));
#10971=CARTESIAN_POINT('Ctrl Pts',(1.90861543588989,1.97955458261038,10.5685822459964));
#10972=CARTESIAN_POINT('Ctrl Pts',(2.0868038257101,2.18743624665154,10.5866209795249));
#10973=CARTESIAN_POINT('Ctrl Pts',(2.16892996767276,2.2731830674006,10.5942735960116));
#10974=CARTESIAN_POINT('Ctrl Pts',(2.27536116286318,2.37268138476804,10.6034218195368));
#10975=CARTESIAN_POINT('Ctrl Pts',(2.29534717572278,2.39089959792077,10.6051091371891));
#10976=CARTESIAN_POINT('Ctrl Pts',(2.32739302150087,2.41938074386109,10.6077673511515));
#10977=CARTESIAN_POINT('Ctrl Pts',(2.33930290370203,2.42980975458787,10.6087451846409));
#10978=CARTESIAN_POINT('Ctrl Pts',(2.36186908260158,2.4492781681474,10.6105792507942));
#10979=CARTESIAN_POINT('Ctrl Pts',(2.37250822472243,2.45833680727787,10.6114362674547));
#10980=CARTESIAN_POINT('Ctrl Pts',(2.39661382577828,2.47859244021172,10.6133610393574));
#10981=CARTESIAN_POINT('Ctrl Pts',(2.41011338371064,2.4897494927842,10.6144271512094));
#10982=CARTESIAN_POINT('Ctrl Pts',(2.4449724021288,2.5180845559845,10.6171505655273));
#10983=CARTESIAN_POINT('Ctrl Pts',(2.46646153845565,2.53510133360284,10.618801412554));
#10984=CARTESIAN_POINT('Ctrl Pts',(2.6552370322235,2.68070886380681,10.6330702431419));
#10985=CARTESIAN_POINT('Ctrl Pts',(2.83456647656753,2.79286318612986,10.6450045564167));
#10986=CARTESIAN_POINT('Ctrl Pts',(3.16975301107138,2.95924060008267,10.6659519200789));
#10987=CARTESIAN_POINT('Ctrl Pts',(3.32120117800465,3.02057999299012,10.6749977637266));
#10988=CARTESIAN_POINT('Ctrl Pts',(3.55305490134623,3.09457521741472,10.6890504051162));
#10989=CARTESIAN_POINT('Ctrl Pts',(3.63035588064386,3.11610135738314,10.6937701190569));
#10990=CARTESIAN_POINT('Ctrl Pts',(3.72411846779949,3.13847768454784,10.6996236759485));
#10991=CARTESIAN_POINT('Ctrl Pts',(3.73989260995214,3.14211676007866,10.7006127815641));
#10992=CARTESIAN_POINT('Ctrl Pts',(3.76453680844162,3.14760692434643,10.7021657742993));
#10993=CARTESIAN_POINT('Ctrl Pts',(3.77338863919336,3.14953976411872,10.702725129671));
#10994=CARTESIAN_POINT('Ctrl Pts',(3.7899311600375,3.15307888509004,10.7037735455463));
#10995=CARTESIAN_POINT('Ctrl Pts',(3.7976196769649,3.15469439313929,10.7042620778659));
#10996=CARTESIAN_POINT('Ctrl Pts',(3.81519923631034,3.15832113531748,10.7053819157759));
#10997=CARTESIAN_POINT('Ctrl Pts',(3.82509386346105,3.16031402493828,10.7060142375981));
#10998=CARTESIAN_POINT('Ctrl Pts',(3.85146027829207,3.16549575428454,10.7077042805933));
#10999=CARTESIAN_POINT('Ctrl Pts',(3.86794763690857,3.16860245291813,10.7087663620851));
#11000=CARTESIAN_POINT('Ctrl Pts',(4.01074615382345,3.1943569096528,10.7180062658649));
#11001=CARTESIAN_POINT('Ctrl Pts',(4.13826869446855,3.20956792258219,10.7265314288199));
#11002=CARTESIAN_POINT('Ctrl Pts',(4.45383763827683,3.22821744047018,10.7477988839086));
#11003=CARTESIAN_POINT('Ctrl Pts',(4.64195671198449,3.22288641439608,10.760605635627));
#11004=CARTESIAN_POINT('Ctrl Pts',(4.96576025145441,3.18525083861677,10.7822263357789));
#11005=CARTESIAN_POINT('Ctrl Pts',(5.10182333892039,3.16049475702027,10.7911851989636));
#11006=CARTESIAN_POINT('Ctrl Pts',(5.26317893870952,3.12027683551355,10.8016360746681));
#11007=CARTESIAN_POINT('Ctrl Pts',(5.29037441969082,3.11311906177195,10.80339183629));
#11008=CARTESIAN_POINT('Ctrl Pts',(5.33295382927633,3.1013142624892,10.8061325678051));
#11009=CARTESIAN_POINT('Ctrl Pts',(5.34840212674062,3.09690670287466,10.8071252251882));
#11010=CARTESIAN_POINT('Ctrl Pts',(5.37720007871632,3.08845698751825,10.8089726954126));
#11011=CARTESIAN_POINT('Ctrl Pts',(5.39055763936269,3.08444333865793,10.8098284111002));
#11012=CARTESIAN_POINT('Ctrl Pts',(5.42031027146503,3.07529233441839,10.8117319214297));
#11013=CARTESIAN_POINT('Ctrl Pts',(5.4366912417463,3.07011031019614,10.8127782299731));
#11014=CARTESIAN_POINT('Ctrl Pts',(5.47805735152002,3.05665954948261,10.8154165561771));
#11015=CARTESIAN_POINT('Ctrl Pts',(5.50298437994152,3.04821521355538,10.8170027980389));
#11016=CARTESIAN_POINT('Ctrl Pts',(5.65967679363376,2.99298501599292,10.8269561947725));
#11017=CARTESIAN_POINT('Ctrl Pts',(5.78839166253631,2.93796819542145,10.8350434064736));
#11018=CARTESIAN_POINT('Ctrl Pts',(6.10210698842642,2.77900544136473,10.8549977946015));
#11019=CARTESIAN_POINT('Ctrl Pts',(6.28116384389513,2.66485979021775,10.8665992928978));
#11020=CARTESIAN_POINT('Ctrl Pts',(6.50244831379754,2.490969994231,10.8826750217225));
#11021=CARTESIAN_POINT('Ctrl Pts',(6.55576630958784,2.44620368932329,10.8867038676878));
#11022=CARTESIAN_POINT('Ctrl Pts',(6.6382163040163,2.37229601826381,10.8932622917179));
#11023=CARTESIAN_POINT('Ctrl Pts',(6.66831281717414,2.34426028257049,10.8957304974198));
#11024=CARTESIAN_POINT('Ctrl Pts',(6.70725468058114,2.30656729856088,10.8990367075264));
#11025=CARTESIAN_POINT('Ctrl Pts',(6.71659082533019,2.29741990194421,10.8998381484173));
#11026=CARTESIAN_POINT('Ctrl Pts',(6.73181610960179,2.28231980434057,10.9011601640503));
#11027=CARTESIAN_POINT('Ctrl Pts',(6.73773825444993,2.27640039199073,10.9016781693041));
#11028=CARTESIAN_POINT('Ctrl Pts',(6.74929243240172,2.26476117804141,10.90269640893));
#11029=CARTESIAN_POINT('Ctrl Pts',(6.75492626945211,2.25904330696814,10.9031964947027));
#11030=CARTESIAN_POINT('Ctrl Pts',(6.76747929628213,2.2462074716817,10.9043186979078));
#11031=CARTESIAN_POINT('Ctrl Pts',(6.77438706980177,2.23907847393418,10.904941679839));
#11032=CARTESIAN_POINT('Ctrl Pts',(6.79824397242794,2.21422883537781,10.9071118543875));
#11033=CARTESIAN_POINT('Ctrl Pts',(6.81502322782553,2.19634724732291,10.9086711067592));
#11034=CARTESIAN_POINT('Ctrl Pts',(6.98524201374017,2.01074581529305,10.9248149443672));
#11035=CARTESIAN_POINT('Ctrl Pts',(7.12071984219153,1.82744233583162,10.9403755491017));
#11036=CARTESIAN_POINT('Ctrl Pts',(7.30868240230257,1.50722842270428,10.9654195617516));
#11037=CARTESIAN_POINT('Ctrl Pts',(7.37318573569044,1.37827066358377,10.9750248647329));
#11038=CARTESIAN_POINT('Ctrl Pts',(7.46012656534164,1.17077304174138,10.9896155046163));
#11039=CARTESIAN_POINT('Ctrl Pts',(7.48858171600869,1.09497152340598,10.9947784050595));
#11040=CARTESIAN_POINT('Ctrl Pts',(7.5217490012014,0.995366539106615,11.0013525290928));
#11041=CARTESIAN_POINT('Ctrl Pts',(7.52908811512436,0.9724751195583,11.0028494023457));
#11042=CARTESIAN_POINT('Ctrl Pts',(7.54064112010471,0.935003096531051,11.0052774403068));
#11043=CARTESIAN_POINT('Ctrl Pts',(7.54500925306155,0.920471387748938,11.0062136205683));
#11044=CARTESIAN_POINT('Ctrl Pts',(7.55324697706468,0.892347510280575,11.0080152048919));
#11045=CARTESIAN_POINT('Ctrl Pts',(7.55713010892174,0.878759703684791,11.0088810323424));
#11046=CARTESIAN_POINT('Ctrl Pts',(7.5658789399078,0.847365777339032,11.0108711256351));
#11047=CARTESIAN_POINT('Ctrl Pts',(7.57068131558189,0.829542410891683,11.0119933187065));
#11048=CARTESIAN_POINT('Ctrl Pts',(7.58569773872903,0.771842050558184,11.0156023696786));
#11049=CARTESIAN_POINT('Ctrl Pts',(7.59530125369099,0.731809378708541,11.0180696082588));
#11050=CARTESIAN_POINT('Ctrl Pts',(7.65404280643009,0.464460910628713,11.0343253648084));
#11051=CARTESIAN_POINT('Ctrl Pts',(7.67921910621825,0.232584571269279,11.0473022341681));
#11052=CARTESIAN_POINT('Ctrl Pts',(7.67921910621823,4.13155620826444E-12,
11.0603093566956));
#11053=CARTESIAN_POINT('Ctrl Pts',(7.67921909637197,0.000251920834644204,
10.8112112888099));
#11054=CARTESIAN_POINT('Ctrl Pts',(7.67921814033762,0.0124821902146477,
10.8104698495681));
#11055=CARTESIAN_POINT('Ctrl Pts',(7.67914756388822,0.0247125160183424,
10.8097305531979));
#11056=CARTESIAN_POINT('Ctrl Pts',(7.67874967167465,0.05942130752487,10.8076383569203));
#11057=CARTESIAN_POINT('Ctrl Pts',(7.67825677579211,0.0818974009304786,
10.8062905276175));
#11058=CARTESIAN_POINT('Ctrl Pts',(7.6747247277413,0.190906431148489,10.7997849037513));
#11059=CARTESIAN_POINT('Ctrl Pts',(7.66843420242991,0.277302262702642,10.7947260112625));
#11060=CARTESIAN_POINT('Ctrl Pts',(7.62986819249719,0.617188526220949,10.7750449003715));
#11061=CARTESIAN_POINT('Ctrl Pts',(7.57098767328278,0.866688250696628,10.7611596897908));
#11062=CARTESIAN_POINT('Ctrl Pts',(7.45931330519997,1.17214008832426,10.7425842695347));
#11063=CARTESIAN_POINT('Ctrl Pts',(7.43323512768143,1.23687045567647,10.7385461720994));
#11064=CARTESIAN_POINT('Ctrl Pts',(7.39389310644517,1.32605652627423,10.7327727756238));
#11065=CARTESIAN_POINT('Ctrl Pts',(7.38238121883419,1.3512675056706,10.7311167162734));
#11066=CARTESIAN_POINT('Ctrl Pts',(7.36167457304223,1.39510941406132,10.7281892017881));
#11067=CARTESIAN_POINT('Ctrl Pts',(7.3526219812279,1.41380605279516,10.7269253570229));
#11068=CARTESIAN_POINT('Ctrl Pts',(7.33894236877195,1.44137627471139,10.7250368680531));
#11069=CARTESIAN_POINT('Ctrl Pts',(7.33445353760921,1.45031833783466,10.7244204555405));
#11070=CARTESIAN_POINT('Ctrl Pts',(7.32637654746597,1.46622310537438,10.7233168422859));
#11071=CARTESIAN_POINT('Ctrl Pts',(7.32280455776994,1.47319380707129,10.72283064942));
#11072=CARTESIAN_POINT('Ctrl Pts',(7.31496459643249,1.48835695411372,10.7217675243059));
#11073=CARTESIAN_POINT('Ctrl Pts',(7.31068686693818,1.49654397189629,10.7211900043192));
#11074=CARTESIAN_POINT('Ctrl Pts',(7.29864963385638,1.51934232925502,10.7195722134272));
#11075=CARTESIAN_POINT('Ctrl Pts',(7.29081285459532,1.53391223808719,10.7185272929));
#11076=CARTESIAN_POINT('Ctrl Pts',(7.2459301501307,1.61583846034783,10.712591966948));
#11077=CARTESIAN_POINT('Ctrl Pts',(7.20659856426446,1.68190748079574,10.7075763979895));
#11078=CARTESIAN_POINT('Ctrl Pts',(7.15186361424725,1.76679054405747,10.7008858081471));
#11079=CARTESIAN_POINT('Ctrl Pts',(7.13855323434307,1.78693174696692,10.6992792594526));
#11080=CARTESIAN_POINT('Ctrl Pts',(7.07294695370399,1.88382229143512,10.6914643690124));
#11081=CARTESIAN_POINT('Ctrl Pts',(7.01757736195909,1.95843467110588,10.6851817318563));
#11082=CARTESIAN_POINT('Ctrl Pts',(6.84713068572379,2.16850543159649,10.6668799908397));
#11083=CARTESIAN_POINT('Ctrl Pts',(6.72396974789081,2.29698320623937,10.654909168971));
#11084=CARTESIAN_POINT('Ctrl Pts',(6.54539046221419,2.45483277018436,10.6393763213304));
#11085=CARTESIAN_POINT('Ctrl Pts',(6.49881868663857,2.49371315790049,10.6354694954964));
#11086=CARTESIAN_POINT('Ctrl Pts',(6.41664802486475,2.55846605256933,10.6288195190014));
#11087=CARTESIAN_POINT('Ctrl Pts',(6.38156696101045,2.58496585879209,10.6260527403455));
#11088=CARTESIAN_POINT('Ctrl Pts',(6.33100225439664,2.62156130129316,10.6221640571411));
#11089=CARTESIAN_POINT('Ctrl Pts',(6.3159583241122,2.63225341700168,10.6210192249988));
#11090=CARTESIAN_POINT('Ctrl Pts',(6.3004210598223,2.64309647869332,10.6198490599527));
#11091=CARTESIAN_POINT('Ctrl Pts',(6.30001893583932,2.64337697436172,10.6198187829466));
#11092=CARTESIAN_POINT('Ctrl Pts',(6.29921621884924,2.64393662552497,10.6197583608425));
#11093=CARTESIAN_POINT('Ctrl Pts',(6.29881562638652,2.64421578176337,10.6197282157169));
#11094=CARTESIAN_POINT('Ctrl Pts',(6.29801409780326,2.64477406315331,10.6196679161316));
#11095=CARTESIAN_POINT('Ctrl Pts',(6.29761316162423,2.64505318819942,10.6196377616764));
#11096=CARTESIAN_POINT('Ctrl Pts',(6.29680893663143,2.64561280470362,10.6195772923983));
#11097=CARTESIAN_POINT('Ctrl Pts',(6.29640564711696,2.64589329514308,10.6195469776147));
#11098=CARTESIAN_POINT('Ctrl Pts',(6.29559451797871,2.64645716552412,10.619486022813));
#11099=CARTESIAN_POINT('Ctrl Pts',(6.29518667695265,2.64674054342506,10.6194553828736));
#11100=CARTESIAN_POINT('Ctrl Pts',(6.29436398932019,2.64731188494822,10.6193935938853));
#11101=CARTESIAN_POINT('Ctrl Pts',(6.29394914049116,2.64759984536359,10.6193624449592));
#11102=CARTESIAN_POINT('Ctrl Pts',(6.29310963216011,2.64818228376005,10.6192994283009));
#11103=CARTESIAN_POINT('Ctrl Pts',(6.29268496947562,2.64847675713325,10.6192675607453));
#11104=CARTESIAN_POINT('Ctrl Pts',(6.29182255474529,2.64907447329488,10.6192028621032));
#11105=CARTESIAN_POINT('Ctrl Pts',(6.29138479830942,2.64937770976522,10.6191700312577));
#11106=CARTESIAN_POINT('Ctrl Pts',(6.29049227124517,2.6499956412216,10.6191031134801));
#11107=CARTESIAN_POINT('Ctrl Pts',(6.29003749471579,2.65031032768843,10.6190690268734));
#11108=CARTESIAN_POINT('Ctrl Pts',(6.28910610913606,2.65095445334739,10.6189992388471));
#11109=CARTESIAN_POINT('Ctrl Pts',(6.28862949218443,2.65128388111927,10.6189635378638));
#11110=CARTESIAN_POINT('Ctrl Pts',(6.28764834724949,2.65196163727851,10.618890069017));
#11111=CARTESIAN_POINT('Ctrl Pts',(6.28714380862485,2.65230995027918,10.6188523017408));
#11112=CARTESIAN_POINT('Ctrl Pts',(6.28639154319504,2.65282896690625,10.6187960101368));
#11113=CARTESIAN_POINT('Ctrl Pts',(6.28614389203217,2.65299977971444,10.6187774816517));
#11114=CARTESIAN_POINT('Ctrl Pts',(6.28553908936986,2.65341680619762,10.6187322398095));
#11115=CARTESIAN_POINT('Ctrl Pts',(6.28518191199602,2.65366298249474,10.6187055278757));
#11116=CARTESIAN_POINT('Ctrl Pts',(6.28427900984817,2.65428501818811,10.6186380196138));
#11117=CARTESIAN_POINT('Ctrl Pts',(6.28373321865466,2.65466078152906,10.6185972269422));
#11118=CARTESIAN_POINT('Ctrl Pts',(6.27258911918289,2.66232814517143,10.6177646198765));
#11119=CARTESIAN_POINT('Ctrl Pts',(6.26194724265096,2.66955647262255,10.6169752174111));
#11120=CARTESIAN_POINT('Ctrl Pts',(6.23771557691386,2.68580427280003,10.6151904192664));
#11121=CARTESIAN_POINT('Ctrl Pts',(6.22409995852453,2.69478473470162,10.6141965039965));
#11122=CARTESIAN_POINT('Ctrl Pts',(6.18576175291082,2.71965589403468,10.6114223956736));
#11123=CARTESIAN_POINT('Ctrl Pts',(6.16088873968896,2.73531260354452,10.609650886681));
#11124=CARTESIAN_POINT('Ctrl Pts',(5.99836490752757,2.83453797257349,10.5982500087928));
#11125=CARTESIAN_POINT('Ctrl Pts',(5.85482130878241,2.90803520114457,10.5889977944774));
#11126=CARTESIAN_POINT('Ctrl Pts',(5.50831813749511,3.05383360086019,10.5677875342344));
#11127=CARTESIAN_POINT('Ctrl Pts',(5.30244567930492,3.11714577108419,10.5560234979026));
#11128=CARTESIAN_POINT('Ctrl Pts',(5.01401086948633,3.17514787783862,10.5390279416438));
#11129=CARTESIAN_POINT('Ctrl Pts',(4.93565558614299,3.18791389076883,10.5343565614428));
#11130=CARTESIAN_POINT('Ctrl Pts',(4.84090049949899,3.19977977300703,10.5285573114725));
#11131=CARTESIAN_POINT('Ctrl Pts',(4.82487020626356,3.20166498818244,10.5275710720516));
#11132=CARTESIAN_POINT('Ctrl Pts',(4.79983154874142,3.20441908764935,10.5260216412684));
#11133=CARTESIAN_POINT('Ctrl Pts',(4.79083228635154,3.20537060498631,10.5254629485834));
#11134=CARTESIAN_POINT('Ctrl Pts',(4.77401200642193,3.20707745585063,10.5244151424474));
#11135=CARTESIAN_POINT('Ctrl Pts',(4.766192129019,3.20784210110908,10.5239265516702));
#11136=CARTESIAN_POINT('Ctrl Pts',(4.74830667786557,3.20952497307624,10.5228057732859));
#11137=CARTESIAN_POINT('Ctrl Pts',(4.73823953463086,3.21042444860722,10.5221725623958));
#11138=CARTESIAN_POINT('Ctrl Pts',(4.71140101003878,3.21269519995637,10.5204784630471));
#11139=CARTESIAN_POINT('Ctrl Pts',(4.69462308961619,3.21398247904009,10.5194131815238));
#11140=CARTESIAN_POINT('Ctrl Pts',(4.51530761655103,3.22632862276993,10.5079668885814));
#11141=CARTESIAN_POINT('Ctrl Pts',(4.35218195265447,3.22517760792805,10.4970302945412));
#11142=CARTESIAN_POINT('Ctrl Pts',(4.0864083979378,3.20311556665918,10.4790062374092));
#11143=CARTESIAN_POINT('Ctrl Pts',(3.98342645371507,3.18953378130472,10.4719685805042));
#11144=CARTESIAN_POINT('Ctrl Pts',(3.71625767697638,3.14107186327914,10.4537411317924));
#11145=CARTESIAN_POINT('Ctrl Pts',(3.55380623430455,3.09829949538152,10.4427021378335));
#11146=CARTESIAN_POINT('Ctrl Pts',(3.35737963528518,3.029808804846,10.429510996831));
#11147=CARTESIAN_POINT('Ctrl Pts',(3.31960746197088,3.01583900378104,10.4269807082249));
#11148=CARTESIAN_POINT('Ctrl Pts',(3.26488118156158,2.99442446693503,10.4233224703249));
#11149=CARTESIAN_POINT('Ctrl Pts',(3.24771482043455,2.98753623740773,10.4221760865794));
#11150=CARTESIAN_POINT('Ctrl Pts',(3.21757926070068,2.97514167545388,10.4201653077777));
#11151=CARTESIAN_POINT('Ctrl Pts',(3.20458521875577,2.96969742241077,10.4192988480017));
#11152=CARTESIAN_POINT('Ctrl Pts',(3.17756157993267,2.95816614888372,10.417497870999));
#11153=CARTESIAN_POINT('Ctrl Pts',(3.16353874408766,2.95206411117862,10.4165638898192));
#11154=CARTESIAN_POINT('Ctrl Pts',(3.12708407684098,2.93589127564845,10.414136999552));
#11155=CARTESIAN_POINT('Ctrl Pts',(3.10472286308955,2.92566305033427,10.412649497066));
#11156=CARTESIAN_POINT('Ctrl Pts',(3.01179839128535,2.88186569061529,10.4064702645387));
#11157=CARTESIAN_POINT('Ctrl Pts',(2.94234769378112,2.84599035929404,10.4018582890044));
#11158=CARTESIAN_POINT('Ctrl Pts',(2.59588690315103,2.65074639365128,10.3787449578783));
#11159=CARTESIAN_POINT('Ctrl Pts',(2.34242583966154,2.45336666498699,10.3616719260676));
#11160=CARTESIAN_POINT('Ctrl Pts',(2.09033280157612,2.18852618607789,10.3404268506277));
#11161=CARTESIAN_POINT('Ctrl Pts',(2.05923392549234,2.15441661484041,10.3377127261952));
#11162=CARTESIAN_POINT('Ctrl Pts',(2.00874133273874,2.09658861521045,10.3331241908187));
#11163=CARTESIAN_POINT('Ctrl Pts',(1.98893340906712,2.0732396151966,10.3312748298298));
#11164=CARTESIAN_POINT('Ctrl Pts',(1.96202936855526,2.04059416341122,10.3286880015695));
#11165=CARTESIAN_POINT('Ctrl Pts',(1.95464599152431,2.03153519230877,10.3279700488556));
#11166=CARTESIAN_POINT('Ctrl Pts',(1.94224097508167,2.01614477879654,10.3267497198601));
#11167=CARTESIAN_POINT('Ctrl Pts',(1.9371934901261,2.00983413070289,10.3262491721954));
#11168=CARTESIAN_POINT('Ctrl Pts',(1.92756264946095,1.99769983150096,10.3252862466478));
#11169=CARTESIAN_POINT('Ctrl Pts',(1.9229755713762,1.9918792609238,10.3248241599439));
#11170=CARTESIAN_POINT('Ctrl Pts',(1.91076251116181,1.97627160029268,10.3235846988326));
#11171=CARTESIAN_POINT('Ctrl Pts',(1.90317299506083,1.96645632120958,10.32280482275));
#11172=CARTESIAN_POINT('Ctrl Pts',(1.87561072898966,1.93038235394059,10.3199378212155));
#11173=CARTESIAN_POINT('Ctrl Pts',(1.85598558581657,1.90386219547677,10.3178287155303));
#11174=CARTESIAN_POINT('Ctrl Pts',(1.63663296470507,1.59772306212793,10.2935094510462));
#11175=CARTESIAN_POINT('Ctrl Pts',(1.48244106606708,1.2881802135927,10.2694733897782));
#11176=CARTESIAN_POINT('Ctrl Pts',(1.36134590021225,0.900150710269656,10.2429449133735));
#11177=CARTESIAN_POINT('Ctrl Pts',(1.34439737374029,0.839684067797136,10.2388963574241));
#11178=CARTESIAN_POINT('Ctrl Pts',(1.3183200539857,0.734965798778296,10.2320316385589));
#11179=CARTESIAN_POINT('Ctrl Pts',(1.30833551111386,0.690948187732318,10.2291897629372));
#11180=CARTESIAN_POINT('Ctrl Pts',(1.29539510715096,0.627776383626155,10.2251714349104));
#11181=CARTESIAN_POINT('Ctrl Pts',(1.29168259212148,0.608784331105901,10.2239710521369));
#11182=CARTESIAN_POINT('Ctrl Pts',(1.28553856506472,0.575777170220123,10.2218978642694));
#11183=CARTESIAN_POINT('Ctrl Pts',(1.28302839148411,0.561777435419149,10.2210225810147));
#11184=CARTESIAN_POINT('Ctrl Pts',(1.27806812888478,0.533018396231397,10.2192326349437));
#11185=CARTESIAN_POINT('Ctrl Pts',(1.27562796928626,0.518257712809005,10.2183183065131));
#11186=CARTESIAN_POINT('Ctrl Pts',(1.26968823921314,0.480704668525556,10.2160029323459));
#11187=CARTESIAN_POINT('Ctrl Pts',(1.26633030225269,0.457890517943861,10.2146063825791));
#11188=CARTESIAN_POINT('Ctrl Pts',(1.25436641683359,0.370074371341196,10.2092675608518));
#11189=CARTESIAN_POINT('Ctrl Pts',(1.24749969664378,0.30484895048233,10.2053798019695));
#11190=CARTESIAN_POINT('Ctrl Pts',(1.21778888700268,-0.0939127560540211,
10.1819900242355));
#11191=CARTESIAN_POINT('Ctrl Pts',(1.24496884967253,-0.429064027471083,
10.1641803265554));
#11192=CARTESIAN_POINT('Ctrl Pts',(1.33411196502905,-0.79949422194072,10.1420542915426));
#11193=CARTESIAN_POINT('Ctrl Pts',(1.34604308381342,-0.844721643567564,
10.1393052262906));
#11194=CARTESIAN_POINT('Ctrl Pts',(1.36748942152943,-0.919390096834596,
10.1346631432224));
#11195=CARTESIAN_POINT('Ctrl Pts',(1.37645224355946,-0.948983460419278,
10.1327959310387));
#11196=CARTESIAN_POINT('Ctrl Pts',(1.3894008882927,-0.989619999092187,10.1301881236437));
#11197=CARTESIAN_POINT('Ctrl Pts',(1.39302364291881,-1.00077823693333,10.1294674605805));
#11198=CARTESIAN_POINT('Ctrl Pts',(1.39924728787083,-1.01959686149254,10.1282438770101));
#11199=CARTESIAN_POINT('Ctrl Pts',(1.40181629092783,-1.02726782428499,10.1277428081568));
#11200=CARTESIAN_POINT('Ctrl Pts',(1.40679088936271,-1.04193815240546,10.126779981652));
#11201=CARTESIAN_POINT('Ctrl Pts',(1.40919175336887,-1.04893902205962,10.1263185220534));
#11202=CARTESIAN_POINT('Ctrl Pts',(1.41499800258247,-1.06568174864628,10.1252102763244));
#11203=CARTESIAN_POINT('Ctrl Pts',(1.41842608299683,-1.07541556893228,10.1245621839069));
#11204=CARTESIAN_POINT('Ctrl Pts',(1.43096977249069,-1.11049393869981,10.1222133581154));
#11205=CARTESIAN_POINT('Ctrl Pts',(1.44035598487733,-1.13573964248514,10.1204978707118));
#11206=CARTESIAN_POINT('Ctrl Pts',(1.51071959095196,-1.31796773368111,10.1079477400085));
#11207=CARTESIAN_POINT('Ctrl Pts',(1.58359761346543,-1.47006048735957,10.0965797370211));
#11208=CARTESIAN_POINT('Ctrl Pts',(1.74224129658463,-1.74384753375148,10.0751739999166));
#11209=CARTESIAN_POINT('Ctrl Pts',(1.82521192110522,-1.8666890527819,10.0651652034073));
#11210=CARTESIAN_POINT('Ctrl Pts',(1.9936839627957,-2.08245067727558,10.0470845675642));
#11211=CARTESIAN_POINT('Ctrl Pts',(2.07676303259264,-2.17690542105144,10.0389618091173));
#11212=CARTESIAN_POINT('Ctrl Pts',(2.18446713668157,-2.28579934459972,10.0293415409776));
#11213=CARTESIAN_POINT('Ctrl Pts',(2.20402626460562,-2.30507546809343,10.0276276947414));
#11214=CARTESIAN_POINT('Ctrl Pts',(2.23531070988738,-2.33512877377327,10.0249375453656));
#11215=CARTESIAN_POINT('Ctrl Pts',(2.24687327493903,-2.34607273728276,10.02395401751));
#11216=CARTESIAN_POINT('Ctrl Pts',(2.26872602069147,-2.36645148495767,10.0221149956874));
#11217=CARTESIAN_POINT('Ctrl Pts',(2.27899728961242,-2.37590591912105,10.0212586709671));
#11218=CARTESIAN_POINT('Ctrl Pts',(2.30218987238983,-2.39697735508031,10.0193428629521));
#11219=CARTESIAN_POINT('Ctrl Pts',(2.31514441889843,-2.4085572569366,10.0182849584729));
#11220=CARTESIAN_POINT('Ctrl Pts',(2.34843585625655,-2.43783513332583,10.0155966868537));
#11221=CARTESIAN_POINT('Ctrl Pts',(2.36890256207908,-2.45538394359089,10.0139724912624));
#11222=CARTESIAN_POINT('Ctrl Pts',(2.51033051776054,-2.57360203504729,10.002935807968));
#11223=CARTESIAN_POINT('Ctrl Pts',(2.63831121799681,-2.66555691806683,9.99388391983638));
#11224=CARTESIAN_POINT('Ctrl Pts',(2.95844616478623,-2.86174768094455,9.97268152184718));
#11225=CARTESIAN_POINT('Ctrl Pts',(3.15544972984387,-2.95651972997849,9.96075153270206));
#11226=CARTESIAN_POINT('Ctrl Pts',(3.4356038586933,-3.05783099988023,9.94354676086417));
#11227=CARTESIAN_POINT('Ctrl Pts',(3.51168780436764,-3.08218791204095,9.93884711582047));
#11228=CARTESIAN_POINT('Ctrl Pts',(3.60416150136919,-3.10804612571095,9.93301614895125));
#11229=CARTESIAN_POINT('Ctrl Pts',(3.61976456362276,-3.11228283680847,9.93202827122564));
#11230=CARTESIAN_POINT('Ctrl Pts',(3.64415508636642,-3.11870894708472,9.93047682585878));
#11231=CARTESIAN_POINT('Ctrl Pts',(3.65292126267374,-3.12097908065923,9.92991777594184));
#11232=CARTESIAN_POINT('Ctrl Pts',(3.66931052833491,-3.12514970186349,9.92886967730495));
#11233=CARTESIAN_POINT('Ctrl Pts',(3.67693110204434,-3.1270592864645,9.92838115447137));
#11234=CARTESIAN_POINT('Ctrl Pts',(3.6943629147211,-3.13135971927985,9.92726101568716));
#11235=CARTESIAN_POINT('Ctrl Pts',(3.7041784525157,-3.13373232815647,9.92662838081642));
#11236=CARTESIAN_POINT('Ctrl Pts',(3.73034939864135,-3.13992831951293,9.92493683146913));
#11237=CARTESIAN_POINT('Ctrl Pts',(3.74672357642959,-3.14366997893885,9.92387354417107));
#11238=CARTESIAN_POINT('Ctrl Pts',(3.88973381179413,-3.17517498538392,9.9145482829503));
#11239=CARTESIAN_POINT('Ctrl Pts',(4.01789618243485,-3.19539847881571,9.90593192464381));
#11240=CARTESIAN_POINT('Ctrl Pts',(4.20200696691789,-3.21316515352719,9.89348491067499));
#11241=CARTESIAN_POINT('Ctrl Pts',(4.25722913526284,-3.21706148196895,9.88974209664869));
#11242=CARTESIAN_POINT('Ctrl Pts',(4.46567809834205,-3.22638124944188,9.87562605688196));
#11243=CARTESIAN_POINT('Ctrl Pts',(4.61913720846135,-3.2222921182501,9.86527056314726));
#11244=CARTESIAN_POINT('Ctrl Pts',(4.88910718369397,-3.19575533144132,9.84740292646025));
#11245=CARTESIAN_POINT('Ctrl Pts',(5.00577176481852,-3.1777822506138,9.83979623955946));
#11246=CARTESIAN_POINT('Ctrl Pts',(5.14761683986571,-3.1478820167745,9.83069447803535));
#11247=CARTESIAN_POINT('Ctrl Pts',(5.17396257660983,-3.14198179059991,9.82901001734078));
#11248=CARTESIAN_POINT('Ctrl Pts',(5.21562399011704,-3.13210020200933,9.82635531884745));
#11249=CARTESIAN_POINT('Ctrl Pts',(5.23098938148993,-3.12833600666929,9.82537817399062));
#11250=CARTESIAN_POINT('Ctrl Pts',(5.25987309208869,-3.12103425665755,9.82354482049152));
#11251=CARTESIAN_POINT('Ctrl Pts',(5.27339727944072,-3.11752163829869,9.82268783274062));
#11252=CARTESIAN_POINT('Ctrl Pts',(5.30383138618866,-3.10940538498125,9.82076236937654));
#11253=CARTESIAN_POINT('Ctrl Pts',(5.32072754507335,-3.10475152812595,9.81969554338449));
#11254=CARTESIAN_POINT('Ctrl Pts',(5.36399133190121,-3.09245446065972,9.81696884373966));
#11255=CARTESIAN_POINT('Ctrl Pts',(5.39030110771465,-3.08461165212121,9.81531545346186));
#11256=CARTESIAN_POINT('Ctrl Pts',(5.61135516975866,-3.01562900693202,9.80145647819413));
#11257=CARTESIAN_POINT('Ctrl Pts',(5.79999452932515,-2.93644933080625,9.78988621295467));
#11258=CARTESIAN_POINT('Ctrl Pts',(6.10843308791325,-2.77099414210449,9.77028060140354));
#11259=CARTESIAN_POINT('Ctrl Pts',(6.23213520906258,-2.69339934632674,9.7621900674558));
#11260=CARTESIAN_POINT('Ctrl Pts',(6.43313875130678,-2.54743271769388,9.74799760587075));
#11261=CARTESIAN_POINT('Ctrl Pts',(6.51319389706793,-2.48324688826594,9.74202403291668));
#11262=CARTESIAN_POINT('Ctrl Pts',(6.60292824027595,-2.40398133360863,9.73476318390896));
#11263=CARTESIAN_POINT('Ctrl Pts',(6.61572025541774,-2.3924981737591,9.73371393261964));
#11264=CARTESIAN_POINT('Ctrl Pts',(6.63527187361856,-2.37466252205988,9.73208711346476));
#11265=CARTESIAN_POINT('Ctrl Pts',(6.64209715994522,-2.36838206348538,9.73151480210709));
#11266=CARTESIAN_POINT('Ctrl Pts',(6.65463365558372,-2.35674595092397,9.73045523153041));
#11267=CARTESIAN_POINT('Ctrl Pts',(6.66035254629726,-2.35139886912497,9.72996861473297));
#11268=CARTESIAN_POINT('Ctrl Pts',(6.67329932843229,-2.33920508862119,9.7288595636404));
#11269=CARTESIAN_POINT('Ctrl Pts',(6.68051497488574,-2.33234573950822,9.7282361759791));
#11270=CARTESIAN_POINT('Ctrl Pts',(6.69921018379128,-2.31440803080173,9.72660750658177));
#11271=CARTESIAN_POINT('Ctrl Pts',(6.71063931635709,-2.30327781949418,9.72559843812134));
#11272=CARTESIAN_POINT('Ctrl Pts',(6.78924499074979,-2.22558258470347,9.71856795432336));
#11273=CARTESIAN_POINT('Ctrl Pts',(6.85353977601534,-2.15617946684834,9.7123563157888));
#11274=CARTESIAN_POINT('Ctrl Pts',(7.03215585607542,-1.94549592777755,9.69393610501191));
#11275=CARTESIAN_POINT('Ctrl Pts',(7.13770172312054,-1.79725061730207,9.68152466652997));
#11276=CARTESIAN_POINT('Ctrl Pts',(7.30562919662112,-1.51339125927077,9.65941997303687));
#11277=CARTESIAN_POINT('Ctrl Pts',(7.37218754747625,-1.38081940793283,9.64966903169383));
#11278=CARTESIAN_POINT('Ctrl Pts',(7.44806036171018,-1.19951553175262,9.63714186858402));
#11279=CARTESIAN_POINT('Ctrl Pts',(7.46572189929812,-1.15449286927154,9.63409274466785));
#11280=CARTESIAN_POINT('Ctrl Pts',(7.48920682767043,-1.09041955082206,9.62983758079859));
#11281=CARTESIAN_POINT('Ctrl Pts',(7.49587653577505,-1.07168810271846,9.62860358436104));
#11282=CARTESIAN_POINT('Ctrl Pts',(7.5070499315085,-1.03936478505215,9.62649095010929));
#11283=CARTESIAN_POINT('Ctrl Pts',(7.51163711669378,-1.02580259617763,9.62560957075305));
#11284=CARTESIAN_POINT('Ctrl Pts',(7.52023498376673,-0.999813337354608,
9.62393002501564));
#11285=CARTESIAN_POINT('Ctrl Pts',(7.52426080021341,-0.987391610319358,
9.62313137485021));
#11286=CARTESIAN_POINT('Ctrl Pts',(7.53352168066227,-0.958213536596063,
9.62126479486707));
#11287=CARTESIAN_POINT('Ctrl Pts',(7.53869558262355,-0.941438099178831,
9.62019888017037));
#11288=CARTESIAN_POINT('Ctrl Pts',(7.55606754108163,-0.883433999148986,
9.61653748320085));
#11289=CARTESIAN_POINT('Ctrl Pts',(7.56757781208675,-0.842002951441,9.61396427375406));
#11290=CARTESIAN_POINT('Ctrl Pts',(7.6452990315115,-0.538850156262905,9.59541229192057));
#11291=CARTESIAN_POINT('Ctrl Pts',(7.67921910621722,-0.269971659946486,
9.5805624267731));
#11292=CARTESIAN_POINT('Ctrl Pts',(7.67921910621823,-1.20008863957466E-11,
9.56539764702567));
#11293=CARTESIAN_POINT('Origin',(4.45646910621825,-5.13094777615093E-16,
-2.31077344927308));
#11294=CARTESIAN_POINT('',(7.67921910621823,-4.32305015001326E-11,8.31612808864258));
#11295=CARTESIAN_POINT('',(7.67921910621823,1.63241365473312E-10,8.56014415614755));
#11296=CARTESIAN_POINT('',(7.67921910621823,-3.51191647465084E-13,-2.31077344927308));
#11297=CARTESIAN_POINT('Ctrl Pts',(7.67921910621823,1.63240393424857E-10,
8.56014415614755));
#11298=CARTESIAN_POINT('Ctrl Pts',(7.67921910623171,-0.266045158755238,
8.57813436331319));
#11299=CARTESIAN_POINT('Ctrl Pts',(7.64627463525177,-0.531126215526067,
8.59606011624979));
#11300=CARTESIAN_POINT('Ctrl Pts',(7.5716381018007,-0.826639474292601,8.61536623206872));
#11301=CARTESIAN_POINT('Ctrl Pts',(7.56150248251137,-0.863932076104476,
8.61779245718516));
#11302=CARTESIAN_POINT('Ctrl Pts',(7.54566539375373,-0.918317973315446,
8.6213172267283));
#11303=CARTESIAN_POINT('Ctrl Pts',(7.54048773856555,-0.935559030440784,
8.62243262266453));
#11304=CARTESIAN_POINT('Ctrl Pts',(7.53100827512552,-0.966190577496588,
8.6244109927897));
#11305=CARTESIAN_POINT('Ctrl Pts',(7.52676279586725,-0.979597877930699,
8.62527577996548));
#11306=CARTESIAN_POINT('Ctrl Pts',(7.51768969288889,-1.00761239587881,8.62708054229396));
#11307=CARTESIAN_POINT('Ctrl Pts',(7.51284495431674,-1.02221372941467,8.6280199304207));
#11308=CARTESIAN_POINT('Ctrl Pts',(7.49985317450248,-1.06045083175874,8.63047695265231));
#11309=CARTESIAN_POINT('Ctrl Pts',(7.49153523983137,-1.0840277542396,8.63198892486271));
#11310=CARTESIAN_POINT('Ctrl Pts',(7.45161767680612,-1.19311021973424,8.63897322441953));
#11311=CARTESIAN_POINT('Ctrl Pts',(7.41667211718725,-1.27735168005217,8.64433354406527));
#11312=CARTESIAN_POINT('Ctrl Pts',(7.3038937192333,-1.51963623994239,8.65978228322838));
#11313=CARTESIAN_POINT('Ctrl Pts',(7.21662746243491,-1.6729171288756,8.66958276301207));
#11314=CARTESIAN_POINT('Ctrl Pts',(7.01585930898204,-1.966710152776,8.68949065761058));
#11315=CARTESIAN_POINT('Ctrl Pts',(6.90221772390692,-2.10635335977743,8.69957173040615));
#11316=CARTESIAN_POINT('Ctrl Pts',(6.75893556217045,-2.25510213429688,8.71195409070326));
#11317=CARTESIAN_POINT('Ctrl Pts',(6.7400823156765,-2.27419172897672,8.71357781679368));
#11318=CARTESIAN_POINT('Ctrl Pts',(6.71366048793978,-2.30028494967422,8.71584962443154));
#11319=CARTESIAN_POINT('Ctrl Pts',(6.70629275556051,-2.30749156522323,8.7164827228139));
#11320=CARTESIAN_POINT('Ctrl Pts',(6.69357717926225,-2.31981028624362,8.71757494768917));
#11321=CARTESIAN_POINT('Ctrl Pts',(6.68824601297749,-2.32493959717168,8.71803275561443));
#11322=CARTESIAN_POINT('Ctrl Pts',(6.67704507023155,-2.33564241038036,8.71899449308323));
#11323=CARTESIAN_POINT('Ctrl Pts',(6.67117191769319,-2.34121219305574,8.71949870999025));
#11324=CARTESIAN_POINT('Ctrl Pts',(6.65672075497676,-2.35481386525024,8.72073906554134));
#11325=CARTESIAN_POINT('Ctrl Pts',(6.64811972410858,-2.36282102938297,8.72147704588266));
#11326=CARTESIAN_POINT('Ctrl Pts',(6.61663497186748,-2.39181207183875,8.72417692219809));
#11327=CARTESIAN_POINT('Ctrl Pts',(6.59349292670909,-2.41251125982059,8.72615841403667));
#11328=CARTESIAN_POINT('Ctrl Pts',(6.53455200237349,-2.46371691097859,8.731189744691));
#11329=CARTESIAN_POINT('Ctrl Pts',(6.49837832581934,-2.49377942678379,8.73426371750534));
#11330=CARTESIAN_POINT('Ctrl Pts',(6.19452092419874,-2.73525903413027,8.75988661147945));
#11331=CARTESIAN_POINT('Ctrl Pts',(5.89546083249698,-2.90376578648535,8.78355480818503));
#11332=CARTESIAN_POINT('Ctrl Pts',(5.51924250453308,-3.04306168929238,8.80931334935854));
#11333=CARTESIAN_POINT('Ctrl Pts',(5.46244827320802,-3.06230606349106,8.8131132733979));
#11334=CARTESIAN_POINT('Ctrl Pts',(5.38385879787382,-3.08651293633397,8.81825402052648));
#11335=CARTESIAN_POINT('Ctrl Pts',(5.36250276052255,-3.09284930179538,8.81963930404839));
#11336=CARTESIAN_POINT('Ctrl Pts',(5.32827778284383,-3.10261897587398,8.82184116021949));
#11337=CARTESIAN_POINT('Ctrl Pts',(5.31545058028242,-3.10619473211106,8.82266234201427));
#11338=CARTESIAN_POINT('Ctrl Pts',(5.28895939846442,-3.11340285848696,8.82435007186715));
#11339=CARTESIAN_POINT('Ctrl Pts',(5.2752929224201,-3.11702502620548,8.8252162735536));
#11340=CARTESIAN_POINT('Ctrl Pts',(5.24337661972674,-3.12525973931445,8.82722897336991));
#11341=CARTESIAN_POINT('Ctrl Pts',(5.22510922013725,-3.12980259306518,8.82837320324312));
#11342=CARTESIAN_POINT('Ctrl Pts',(5.16588216344047,-3.14398173403054,8.83205887573175));
#11343=CARTESIAN_POINT('Ctrl Pts',(5.12477229891581,-3.15297623187847,8.83457979436019));
#11344=CARTESIAN_POINT('Ctrl Pts',(5.02730602995478,-3.1723089970325,8.84047720225616));
#11345=CARTESIAN_POINT('Ctrl Pts',(4.97082618173617,-3.18195482449718,8.84383247538456));
#11346=CARTESIAN_POINT('Ctrl Pts',(4.75526211998063,-3.21287946272154,8.85644815557179));
#11347=CARTESIAN_POINT('Ctrl Pts',(4.59491957481742,-3.22377230872117,8.86542812234982));
#11348=CARTESIAN_POINT('Ctrl Pts',(4.41377157453322,-3.22253334753993,8.87555690556549));
#11349=CARTESIAN_POINT('Ctrl Pts',(4.39311736902046,-3.22219347823403,8.87671176831728));
#11350=CARTESIAN_POINT('Ctrl Pts',(4.19243617140399,-3.21696092972169,8.8879425841779));
#11351=CARTESIAN_POINT('Ctrl Pts',(4.01313653340017,-3.19718484463236,8.89804109646337));
#11352=CARTESIAN_POINT('Ctrl Pts',(3.81001409448675,-3.15736271749901,8.91044946079441));
#11353=CARTESIAN_POINT('Ctrl Pts',(3.78364280649666,-3.15184835847806,8.91207981103353));
#11354=CARTESIAN_POINT('Ctrl Pts',(3.74726884938306,-3.14376511455478,8.9143593040352));
#11355=CARTESIAN_POINT('Ctrl Pts',(3.73720393170334,-3.141477630318,8.91499332768923));
#11356=CARTESIAN_POINT('Ctrl Pts',(3.71994022354113,-3.13746674233525,8.91608672482675));
#11357=CARTESIAN_POINT('Ctrl Pts',(3.71273598971319,-3.13576679666831,8.91654477332416));
#11358=CARTESIAN_POINT('Ctrl Pts',(3.69766982462866,-3.1321568720545,8.91750651295192));
#11359=CARTESIAN_POINT('Ctrl Pts',(3.68980917701839,-3.13024209427628,8.91801048838225));
#11360=CARTESIAN_POINT('Ctrl Pts',(3.67056734597002,-3.1254781452905,8.91924940380384));
#11361=CARTESIAN_POINT('Ctrl Pts',(3.65919441464672,-3.12259639877303,8.91998617595629));
#11362=CARTESIAN_POINT('Ctrl Pts',(3.61790648575937,-3.1118943366093,8.9226767041511));
#11363=CARTESIAN_POINT('Ctrl Pts',(3.58808975881175,-3.10370597441035,8.9246498837514));
#11364=CARTESIAN_POINT('Ctrl Pts',(3.51347975900388,-3.08205711406361,8.92965556461399));
#11365=CARTESIAN_POINT('Ctrl Pts',(3.46885399001639,-3.06804838649118,8.93271190720616));
#11366=CARTESIAN_POINT('Ctrl Pts',(3.10800130231633,-2.94608268908611,8.95785368948979));
#11367=CARTESIAN_POINT('Ctrl Pts',(2.80998669748263,-2.79050925012496,8.98103418809206));
#11368=CARTESIAN_POINT('Ctrl Pts',(2.48839113237206,-2.55285964489084,9.00678788267015));
#11369=CARTESIAN_POINT('Ctrl Pts',(2.43681922827416,-2.51225768061364,9.01095551410693));
#11370=CARTESIAN_POINT('Ctrl Pts',(2.36883995428409,-2.45529105660766,9.01650442373908));
#11371=CARTESIAN_POINT('Ctrl Pts',(2.35131926185671,-2.44028560334203,9.01793981938467));
#11372=CARTESIAN_POINT('Ctrl Pts',(2.32270089967534,-2.41523802340159,9.02029358053654));
#11373=CARTESIAN_POINT('Ctrl Pts',(2.31150961047107,-2.40530460494819,9.02121639215117));
#11374=CARTESIAN_POINT('Ctrl Pts',(2.289816110687,-2.38577758210017,9.02301002776923));
#11375=CARTESIAN_POINT('Ctrl Pts',(2.2793074448476,-2.37619169781858,9.02388114506244));
#11376=CARTESIAN_POINT('Ctrl Pts',(2.25465375755024,-2.35340203371604,9.02593039078003));
#11377=CARTESIAN_POINT('Ctrl Pts',(2.24056340722253,-2.34013972239799,9.02710599428367));
#11378=CARTESIAN_POINT('Ctrl Pts',(2.19402215410672,-2.29553623059744,9.03100478054321));
#11379=CARTESIAN_POINT('Ctrl Pts',(2.16210910024029,-2.26363982599952,9.03370390214333));
#11380=CARTESIAN_POINT('Ctrl Pts',(2.0874332191019,-2.18580058223674,9.04009329732077));
#11381=CARTESIAN_POINT('Ctrl Pts',(2.04532149239832,-2.13925760351277,9.04375703498692));
#11382=CARTESIAN_POINT('Ctrl Pts',(1.78201150245087,-1.83057989472059,9.06717307026251));
#11383=CARTESIAN_POINT('Ctrl Pts',(1.60255103113114,-1.53584644364613,9.08531402281039));
#11384=CARTESIAN_POINT('Ctrl Pts',(1.46022465917345,-1.18733527438123,9.10774119880578));
#11385=CARTESIAN_POINT('Ctrl Pts',(1.44801278370199,-1.15604333573595,9.10976486374217));
#11386=CARTESIAN_POINT('Ctrl Pts',(1.4319320302784,-1.11285632961836,9.1125788556098));
#11387=CARTESIAN_POINT('Ctrl Pts',(1.42763953135996,-1.10111994292676,9.11334569224518));
#11388=CARTESIAN_POINT('Ctrl Pts',(1.42090440914674,-1.08236764478966,9.11457474753833));
#11389=CARTESIAN_POINT('Ctrl Pts',(1.41841754785586,-1.07536759979857,9.11503438431459));
#11390=CARTESIAN_POINT('Ctrl Pts',(1.41328059857458,-1.06074801447655,9.11599621385248));
#11391=CARTESIAN_POINT('Ctrl Pts',(1.41063490261845,-1.0531270779083,9.11649867113346));
#11392=CARTESIAN_POINT('Ctrl Pts',(1.40425077394034,-1.03451227992866,9.11772844880602));
#11393=CARTESIAN_POINT('Ctrl Pts',(1.40054311384935,-1.02350804817362,9.11845754089606));
#11394=CARTESIAN_POINT('Ctrl Pts',(1.38743321627117,-0.983891922355063,
9.12108926359253));
#11395=CARTESIAN_POINT('Ctrl Pts',(1.37837301648705,-0.955169575971337,
9.12301025198625));
#11396=CARTESIAN_POINT('Ctrl Pts',(1.35674321695494,-0.883093602061001,
9.12785574822883));
#11397=CARTESIAN_POINT('Ctrl Pts',(1.34467968281328,-0.839595782798345,
9.13080231114196));
#11398=CARTESIAN_POINT('Ctrl Pts',(1.29551571100217,-0.646677878181749,
9.14392772787879));
#11399=CARTESIAN_POINT('Ctrl Pts',(1.26823750831663,-0.494968703430431,
9.15438865258361));
#11400=CARTESIAN_POINT('Ctrl Pts',(1.22893725100035,-0.12661341600215,9.17942665836086));
#11401=CARTESIAN_POINT('Ctrl Pts',(1.22771743656247,0.090471240857646,9.19385490692827));
#11402=CARTESIAN_POINT('Ctrl Pts',(1.2518510976004,0.343438952699975,9.20998381864488));
#11403=CARTESIAN_POINT('Ctrl Pts',(1.2560692459071,0.380746399084559,9.21234653040841));
#11404=CARTESIAN_POINT('Ctrl Pts',(1.26358433561908,0.438201554196141,9.21596173385019));
#11405=CARTESIAN_POINT('Ctrl Pts',(1.26642229086129,0.458404959575393,9.21722848536505));
#11406=CARTESIAN_POINT('Ctrl Pts',(1.27157122891479,0.492693352333813,9.21937106890253));
#11407=CARTESIAN_POINT('Ctrl Pts',(1.27378425063996,0.506792214607541,9.22024996428723));
#11408=CARTESIAN_POINT('Ctrl Pts',(1.27845639667876,0.535319520210305,9.22202421197417));
#11409=CARTESIAN_POINT('Ctrl Pts',(1.2809203055303,0.549746847444394,9.22291939031988));
#11410=CARTESIAN_POINT('Ctrl Pts',(1.2872481709028,0.585336638259917,9.22512265418461));
#11411=CARTESIAN_POINT('Ctrl Pts',(1.29122592936376,0.606478344885927,9.226427104539));
#11412=CARTESIAN_POINT('Ctrl Pts',(1.30697438209144,0.685801753666355,9.23130640406682));
#11413=CARTESIAN_POINT('Ctrl Pts',(1.32014047879625,0.743696489950744,9.23483691795375));
#11414=CARTESIAN_POINT('Ctrl Pts',(1.3575002890913,0.889255213025787,9.24366292298356));
#11415=CARTESIAN_POINT('Ctrl Pts',(1.38381858613466,0.976321215388722,9.24889427254708));
#11416=CARTESIAN_POINT('Ctrl Pts',(1.47480778565485,1.23696993981106,9.2645786025982));
#11417=CARTESIAN_POINT('Ctrl Pts',(1.55077964248598,1.40618854585699,9.27477692940569));
#11418=CARTESIAN_POINT('Ctrl Pts',(1.70502975984947,1.6831802618863,9.29269784116597));
#11419=CARTESIAN_POINT('Ctrl Pts',(1.77620707446161,1.79435264594643,9.30027923709603));
#11420=CARTESIAN_POINT('Ctrl Pts',(1.86391059012287,1.91442972474918,9.3092798017825));
#11421=CARTESIAN_POINT('Ctrl Pts',(1.87394364872069,1.9279427025321,9.31030497078347));
#11422=CARTESIAN_POINT('Ctrl Pts',(1.89017138523617,1.94944498730195,9.31195712123199));
#11423=CARTESIAN_POINT('Ctrl Pts',(1.8962987615834,1.95748500665026,9.31257961611275));
#11424=CARTESIAN_POINT('Ctrl Pts',(1.90725636858591,1.97172354373008,9.3136907318954));
#11425=CARTESIAN_POINT('Ctrl Pts',(1.91207157520281,1.97793339555126,9.31417830191596));
#11426=CARTESIAN_POINT('Ctrl Pts',(1.92248150434882,1.99125746826845,9.31523095753061));
#11427=CARTESIAN_POINT('Ctrl Pts',(1.92808340188389,1.99836563140001,9.31579653070956));
#11428=CARTESIAN_POINT('Ctrl Pts',(1.94375989538178,2.01808586226907,9.31737654900322));
#11429=CARTESIAN_POINT('Ctrl Pts',(1.95389925840699,2.03064577346947,9.3183954198604));
#11430=CARTESIAN_POINT('Ctrl Pts',(2.01444756607069,2.1045064057208,9.32445907071313));
#11431=CARTESIAN_POINT('Ctrl Pts',(2.06700868473713,2.16399932389914,9.32963874012403));
#11432=CARTESIAN_POINT('Ctrl Pts',(2.26978689608714,2.37711743303975,9.34913649950054));
#11433=CARTESIAN_POINT('Ctrl Pts',(2.43305599542146,2.51755226466315,9.36387158596401));
#11434=CARTESIAN_POINT('Ctrl Pts',(2.74093952176487,2.73294150219422,9.38896817798124));
#11435=CARTESIAN_POINT('Ctrl Pts',(2.87952987834343,2.81518866994653,9.39947475373481));
#11436=CARTESIAN_POINT('Ctrl Pts',(3.04795702900409,2.89878325008511,9.41131052066808));
#11437=CARTESIAN_POINT('Ctrl Pts',(3.0723602282471,2.91051426528434,9.41300416302171));
#11438=CARTESIAN_POINT('Ctrl Pts',(3.1126952480273,2.92928191538089,9.41576946683301));
#11439=CARTESIAN_POINT('Ctrl Pts',(3.12854102844654,2.93649923566308,9.41684731348154));
#11440=CARTESIAN_POINT('Ctrl Pts',(3.15719932133499,2.94927289110232,9.41878164225623));
#11441=CARTESIAN_POINT('Ctrl Pts',(3.16999083872056,2.95487499517214,9.41963967485644));
#11442=CARTESIAN_POINT('Ctrl Pts',(3.19742244743444,2.96667689927876,9.42146851686997));
#11443=CARTESIAN_POINT('Ctrl Pts',(3.21207286133671,2.9728518822163,9.4224384645469));
#11444=CARTESIAN_POINT('Ctrl Pts',(3.25205272451414,2.98935561078739,9.42506737311239));
#11445=CARTESIAN_POINT('Ctrl Pts',(3.27746929624237,2.99947083771479,9.42671912057119));
#11446=CARTESIAN_POINT('Ctrl Pts',(3.41861780200445,3.05357338822391,9.43578932903667));
#11447=CARTESIAN_POINT('Ctrl Pts',(3.53668820235613,3.09118972042258,9.44299247588159));
#11448=CARTESIAN_POINT('Ctrl Pts',(3.80132963962856,3.15899012055374,9.45858169859357));
#11449=CARTESIAN_POINT('Ctrl Pts',(3.94842350481087,3.18595634035313,9.46688365126446));
#11450=CARTESIAN_POINT('Ctrl Pts',(4.26497726317687,3.22150103329119,9.48471988535488));
#11451=CARTESIAN_POINT('Ctrl Pts',(4.43430234091749,3.22710902719359,9.49424553703263));
#11452=CARTESIAN_POINT('Ctrl Pts',(4.63016688893988,3.21817837587943,9.50599930267023));
#11453=CARTESIAN_POINT('Ctrl Pts',(4.65705505683749,3.21661439212084,9.50762917500264));
#11454=CARTESIAN_POINT('Ctrl Pts',(4.69421431713357,3.2139852662894,9.50990811436239));
#11455=CARTESIAN_POINT('Ctrl Pts',(4.70450545833392,3.21320743783238,9.51054207211688));
#11456=CARTESIAN_POINT('Ctrl Pts',(4.72217056553544,3.21178689899271,9.51163538574469));
#11457=CARTESIAN_POINT('Ctrl Pts',(4.72954645462876,3.21116818450954,9.5120934170893));
#11458=CARTESIAN_POINT('Ctrl Pts',(4.74498026531459,3.20981998502131,9.51305515645851));
#11459=CARTESIAN_POINT('Ctrl Pts',(4.75303762487338,3.20908556037863,9.5135591490009));
#11460=CARTESIAN_POINT('Ctrl Pts',(4.77277326862014,3.20721170517433,9.51479816659046));
#11461=CARTESIAN_POINT('Ctrl Pts',(4.78444819446088,3.206038825815,9.51553502447527));
#11462=CARTESIAN_POINT('Ctrl Pts',(4.82687340356939,3.20154257311573,9.5182262151274));
#11463=CARTESIAN_POINT('Ctrl Pts',(4.85758074885276,3.19784043956469,9.52019998363712));
#11464=CARTESIAN_POINT('Ctrl Pts',(4.93459511234618,3.18742877891503,9.52520748049599));
#11465=CARTESIAN_POINT('Ctrl Pts',(4.98081723437808,3.18015177227774,9.52826507083558));
#11466=CARTESIAN_POINT('Ctrl Pts',(5.35619857844323,3.11264749751272,9.55343987891822));
#11467=CARTESIAN_POINT('Ctrl Pts',(5.67433219540271,3.00249483702527,9.57665383900076));
#11468=CARTESIAN_POINT('Ctrl Pts',(6.0274476628766,2.81467544986075,9.60240744874631));
#11469=CARTESIAN_POINT('Ctrl Pts',(6.0840911855857,2.78230459657241,9.60654937497545));
#11470=CARTESIAN_POINT('Ctrl Pts',(6.15895410478027,2.73645232010687,9.61204146543004));
#11471=CARTESIAN_POINT('Ctrl Pts',(6.17806766158924,2.72446782441143,9.61344534544333));
#11472=CARTESIAN_POINT('Ctrl Pts',(6.20946225631597,2.70432060666752,9.61575447174331));
#11473=CARTESIAN_POINT('Ctrl Pts',(6.22181568382887,2.69627268657626,9.61666392412165));
#11474=CARTESIAN_POINT('Ctrl Pts',(6.24528831253729,2.68075043441964,9.61839374398925));
#11475=CARTESIAN_POINT('Ctrl Pts',(6.25641695316132,2.67329100574122,9.61921464416099));
#11476=CARTESIAN_POINT('Ctrl Pts',(6.26827235891255,2.66523683945707,9.62009006891609));
#11477=CARTESIAN_POINT('Ctrl Pts',(6.26904560022436,2.66471103316141,9.62014717065128));
#11478=CARTESIAN_POINT('Ctrl Pts',(6.27061807886667,2.66364074206354,9.62026330243684));
#11479=CARTESIAN_POINT('Ctrl Pts',(6.27141730022208,2.6630962338653,9.62032233160112));
#11480=CARTESIAN_POINT('Ctrl Pts',(6.27305688328217,2.66197810771712,9.62044343781818));
#11481=CARTESIAN_POINT('Ctrl Pts',(6.27389721874535,2.661404451327,9.62050551341895));
#11482=CARTESIAN_POINT('Ctrl Pts',(6.27563407862643,2.66021757483399,9.62063382579028));
#11483=CARTESIAN_POINT('Ctrl Pts',(6.27653056508238,2.65960429918707,9.62070006046501));
#11484=CARTESIAN_POINT('Ctrl Pts',(6.2948981954135,2.647025587143,9.62205722674283));
#11485=CARTESIAN_POINT('Ctrl Pts',(6.31225160747897,2.63488848263993,9.62334166572541));
#11486=CARTESIAN_POINT('Ctrl Pts',(6.37581474063395,2.58949246836366,9.6280559916815));
#11487=CARTESIAN_POINT('Ctrl Pts',(6.42126200904066,2.55518068788699,9.63144542802615));
#11488=CARTESIAN_POINT('Ctrl Pts',(6.53285765499646,2.46618919740773,9.63983997420649));
#11489=CARTESIAN_POINT('Ctrl Pts',(6.5977769382923,2.41003752486692,9.64478906306018));
#11490=CARTESIAN_POINT('Ctrl Pts',(6.76636931785504,2.25201704023173,9.65794871897998));
#11491=CARTESIAN_POINT('Ctrl Pts',(6.8655215118462,2.14562059496171,9.6660214995519));
#11492=CARTESIAN_POINT('Ctrl Pts',(7.06237476122235,1.90346935274722,9.68349955097179));
#11493=CARTESIAN_POINT('Ctrl Pts',(7.15737231332272,1.76608273114505,9.69289979448135));
#11494=CARTESIAN_POINT('Ctrl Pts',(7.25486556595784,1.59869359353365,9.70451207683384));
#11495=CARTESIAN_POINT('Ctrl Pts',(7.2681368998726,1.57523587512892,9.70614302223234));
#11496=CARTESIAN_POINT('Ctrl Pts',(7.28608208116538,1.54256751548184,9.70842320453637));
#11497=CARTESIAN_POINT('Ctrl Pts',(7.29100860406667,1.53349599158762,9.70905731007857));
#11498=CARTESIAN_POINT('Ctrl Pts',(7.29939285755834,1.51787908070096,9.71015081099103));
#11499=CARTESIAN_POINT('Ctrl Pts',(7.30287181140591,1.51134509522469,9.71060888080686));
#11500=CARTESIAN_POINT('Ctrl Pts',(7.31010579137443,1.49764504630892,9.7115706207782));
#11501=CARTESIAN_POINT('Ctrl Pts',(7.31385636976276,1.49047678165576,9.7120745749631));
#11502=CARTESIAN_POINT('Ctrl Pts',(7.32297904085902,1.47288016108919,9.71331336351387));
#11503=CARTESIAN_POINT('Ctrl Pts',(7.32832123107935,1.46243650708679,9.71405002920095));
#11504=CARTESIAN_POINT('Ctrl Pts',(7.3475318437883,1.42436974928348,9.71673973492031));
#11505=CARTESIAN_POINT('Ctrl Pts',(7.3610592096519,1.39657763922609,9.71871218338841));
#11506=CARTESIAN_POINT('Ctrl Pts',(7.39403593651121,1.32627445428034,9.72371560995369));
#11507=CARTESIAN_POINT('Ctrl Pts',(7.41296354051476,1.28352757171271,9.72677040374641));
#11508=CARTESIAN_POINT('Ctrl Pts',(7.5593332846058,0.932528445929391,9.75187139471307));
#11509=CARTESIAN_POINT('Ctrl Pts',(7.63915824174214,0.606582303620659,9.77501056737986));
#11510=CARTESIAN_POINT('Ctrl Pts',(7.67298196595207,0.210372040167672,9.8006275531688));
#11511=CARTESIAN_POINT('Ctrl Pts',(7.67652483621499,0.146469788826136,9.80469393872761));
#11512=CARTESIAN_POINT('Ctrl Pts',(7.6786045497387,0.0652558286983623,9.8097819554415));
#11513=CARTESIAN_POINT('Ctrl Pts',(7.67890769140363,0.0480075293663571,
9.81085800952626));
#11514=CARTESIAN_POINT('Ctrl Pts',(7.6791688049711,0.0206493426565398,9.8125577449811));
#11515=CARTESIAN_POINT('Ctrl Pts',(7.67921772144553,0.0105408608178574,
9.81318425199337));
#11516=CARTESIAN_POINT('Ctrl Pts',(7.67921907723176,0.00043224100879341,
9.81380927132941));
#11517=CARTESIAN_POINT('',(7.6792185144777,-0.00195296268717014,8.31625837989182));
#11518=CARTESIAN_POINT('Ctrl Pts',(7.67921910621823,-1.20018596680688E-11,
9.56539764702567));
#11519=CARTESIAN_POINT('Ctrl Pts',(7.67921910621823,0.000928979248483444,
9.56534546463779));
#11520=CARTESIAN_POINT('Ctrl Pts',(7.67921870454109,0.00185797137808247,
9.56529327719194));
#11521=CARTESIAN_POINT('Ctrl Pts',(7.67908108221349,0.160998824745607,9.55635255496428));
#11522=CARTESIAN_POINT('Ctrl Pts',(7.66729393926749,0.318966012123944,9.54735584768415));
#11523=CARTESIAN_POINT('Ctrl Pts',(7.64121861529879,0.493795320519256,9.53665832976546));
#11524=CARTESIAN_POINT('Ctrl Pts',(7.63831687549237,0.512160121540664,9.53552529949506));
#11525=CARTESIAN_POINT('Ctrl Pts',(7.63366137680432,0.540056234942165,9.53378863017499));
#11526=CARTESIAN_POINT('Ctrl Pts',(7.63202320403941,0.549606793336955,9.53319127180097));
#11527=CARTESIAN_POINT('Ctrl Pts',(7.62898559348343,0.566849027923784,9.53210754245388));
#11528=CARTESIAN_POINT('Ctrl Pts',(7.62760121391902,0.574543153378958,9.53162202410102));
#11529=CARTESIAN_POINT('Ctrl Pts',(7.62447236094279,0.591576883365306,9.53054287359425));
#11530=CARTESIAN_POINT('Ctrl Pts',(7.62271459685533,0.60091373629595,9.52994851702363));
#11531=CARTESIAN_POINT('Ctrl Pts',(7.61745727106482,0.628175890443109,9.52820507911565));
#11532=CARTESIAN_POINT('Ctrl Pts',(7.61384665196991,0.646079039391844,9.52705002124847));
#11533=CARTESIAN_POINT('Ctrl Pts',(7.58048149277343,0.804556126150436,9.51674133023832));
#11534=CARTESIAN_POINT('Ctrl Pts',(7.54151157380808,0.943009835652374,9.50715272205079));
#11535=CARTESIAN_POINT('Ctrl Pts',(7.41696977463348,1.29374746990147,9.48205220968626));
#11536=CARTESIAN_POINT('Ctrl Pts',(7.31779480623073,1.50039525453802,9.4665017367109));
#11537=CARTESIAN_POINT('Ctrl Pts',(7.15162526328535,1.76914873444427,9.44593374946827));
#11538=CARTESIAN_POINT('Ctrl Pts',(7.10266214854912,1.84158048239401,9.44034332390495));
#11539=CARTESIAN_POINT('Ctrl Pts',(7.03562121897747,1.9325494825861,9.43325674475015));
#11540=CARTESIAN_POINT('Ctrl Pts',(7.02018593284587,1.95297957415063,9.43166062736506));
#11541=CARTESIAN_POINT('Ctrl Pts',(6.99500900985691,1.98549072806798,9.42911265003299));
#11542=CARTESIAN_POINT('Ctrl Pts',(6.98542098667627,1.99768883297143,9.428154802837));
#11543=CARTESIAN_POINT('Ctrl Pts',(6.9669968461074,2.02078321726404,9.42633758750628));
#11544=CARTESIAN_POINT('Ctrl Pts',(6.95817696770307,2.03169193765794,9.4254776013639));
#11545=CARTESIAN_POINT('Ctrl Pts',(6.93785154048757,2.05649806044339,9.42351809388139));
#11546=CARTESIAN_POINT('Ctrl Pts',(6.92629988962827,2.07035721062324,9.42242046693408));
#11547=CARTESIAN_POINT('Ctrl Pts',(6.89017039888718,2.11297099137802,9.4190359302423));
#11548=CARTESIAN_POINT('Ctrl Pts',(6.86520171802142,2.14139108476953,9.41676505221556));
#11549=CARTESIAN_POINT('Ctrl Pts',(6.74027412602419,2.27863671791143,9.40571825013802));
#11550=CARTESIAN_POINT('Ctrl Pts',(6.63340781961554,2.38094428309651,9.39724061723168));
#11551=CARTESIAN_POINT('Ctrl Pts',(6.36955494584345,2.60086922266454,9.37785829637783));
#11552=CARTESIAN_POINT('Ctrl Pts',(6.20813059345895,2.71221190874339,9.36710733478918));
#11553=CARTESIAN_POINT('Ctrl Pts',(6.00796732460519,2.82491209176933,9.35395477517526));
#11554=CARTESIAN_POINT('Ctrl Pts',(5.97805991253678,2.84113293260986,9.35199320792766));
#11555=CARTESIAN_POINT('Ctrl Pts',(5.89001273870715,2.88709797537025,9.34621301093907));
#11556=CARTESIAN_POINT('Ctrl Pts',(5.83122243176929,2.9155503890975,9.34234684049696));
#11557=CARTESIAN_POINT('Ctrl Pts',(5.75721662172873,2.94863055274336,9.33742280260646));
#11558=CARTESIAN_POINT('Ctrl Pts',(5.74277333751813,2.95495983679112,9.33645914857957));
#11559=CARTESIAN_POINT('Ctrl Pts',(5.71995876033456,2.96475860091453,9.33493190334445));
#11560=CARTESIAN_POINT('Ctrl Pts',(5.71161807211486,2.96829930035014,9.33437250629055));
#11561=CARTESIAN_POINT('Ctrl Pts',(5.69674516361641,2.97453909349972,9.33337293359196));
#11562=CARTESIAN_POINT('Ctrl Pts',(5.6902188654052,2.97725192850503,9.33293359736946));
#11563=CARTESIAN_POINT('Ctrl Pts',(5.67459404603141,2.98368661694464,9.33188007457149));
#11564=CARTESIAN_POINT('Ctrl Pts',(5.66548744366219,2.98738829931156,9.33126469738929));
#11565=CARTESIAN_POINT('Ctrl Pts',(5.63791107676984,2.99845089169941,9.32939745888321));
#11566=CARTESIAN_POINT('Ctrl Pts',(5.61939038516162,3.0056824404082,9.32813830207602));
#11567=CARTESIAN_POINT('Ctrl Pts',(5.50229806781728,3.05015783442555,9.32015095681529));
#11568=CARTESIAN_POINT('Ctrl Pts',(5.40202519605113,3.08271637719427,9.31319428078877));
#11569=CARTESIAN_POINT('Ctrl Pts',(5.07905714932123,3.17034331364465,9.29078539536379));
#11570=CARTESIAN_POINT('Ctrl Pts',(4.85196264475413,3.20660156158906,9.27508030286756));
#11571=CARTESIAN_POINT('Ctrl Pts',(4.616822210384,3.21876404643781,9.25956287856023));
#11572=CARTESIAN_POINT('Ctrl Pts',(4.61070230772222,3.21906309737384,9.25915947788318));
#11573=CARTESIAN_POINT('Ctrl Pts',(4.49241392159903,3.22450519353561,9.25137143399491));
#11574=CARTESIAN_POINT('Ctrl Pts',(4.38004385680494,3.22380052051984,9.2441349681423));
#11575=CARTESIAN_POINT('Ctrl Pts',(4.24061651282348,3.21562959926465,9.2353606021019));
#11576=CARTESIAN_POINT('Ctrl Pts',(4.21332549654666,3.21368127246703,9.23365268476979));
#11577=CARTESIAN_POINT('Ctrl Pts',(4.17006267615006,3.21003842805254,9.23095972401324));
#11578=CARTESIAN_POINT('Ctrl Pts',(4.15407351087644,3.2085716871511,9.22996760015403));
#11579=CARTESIAN_POINT('Ctrl Pts',(4.12421772103346,3.20560775471976,9.22812072759481));
#11580=CARTESIAN_POINT('Ctrl Pts',(4.11034862242366,3.20413992835018,9.22726507958984));
#11581=CARTESIAN_POINT('Ctrl Pts',(4.07940940498913,3.2006622679169,9.22536122264338));
#11582=CARTESIAN_POINT('Ctrl Pts',(4.06234487629347,3.19860580265221,9.2243145036489));
#11583=CARTESIAN_POINT('Ctrl Pts',(4.01209575932957,3.19214198894333,9.2212416203021));
#11584=CARTESIAN_POINT('Ctrl Pts',(3.97896183375215,3.18735393080534,9.21922743830035));
#11585=CARTESIAN_POINT('Ctrl Pts',(3.90373524086754,3.17528378692003,9.21467814508613));
#11586=CARTESIAN_POINT('Ctrl Pts',(3.86170031213639,3.16767930432509,9.21215310095929));
#11587=CARTESIAN_POINT('Ctrl Pts',(3.7212926299111,3.13938473560258,9.20376119053553));
#11588=CARTESIAN_POINT('Ctrl Pts',(3.62373618248316,3.11492842314315,9.19800269917268));
#11589=CARTESIAN_POINT('Ctrl Pts',(3.40256911854199,3.04834843071644,9.18493426390847));
#11590=CARTESIAN_POINT('Ctrl Pts',(3.28005828268848,3.00319687258149,9.17768701315366));
#11591=CARTESIAN_POINT('Ctrl Pts',(3.0835836036963,2.91691316400997,9.16565599881432));
#11592=CARTESIAN_POINT('Ctrl Pts',(3.00790311934487,2.88007854927287,9.16091418279482));
#11593=CARTESIAN_POINT('Ctrl Pts',(2.85518445675,2.79820521440139,9.15096023855335));
#11594=CARTESIAN_POINT('Ctrl Pts',(2.77840373927628,2.75284554436341,9.14574115564873));
#11595=CARTESIAN_POINT('Ctrl Pts',(2.69041031728837,2.69581181023556,9.13938419453255));
#11596=CARTESIAN_POINT('Ctrl Pts',(2.67727450207947,2.68716049020513,9.13842499582302));
#11597=CARTESIAN_POINT('Ctrl Pts',(2.65598477174093,2.67291442082524,9.13685275024214));
#11598=CARTESIAN_POINT('Ctrl Pts',(2.64779217954587,2.66737757144264,9.13624342704031));
#11599=CARTESIAN_POINT('Ctrl Pts',(2.63316200120205,2.65739157825737,9.13514733235075));
#11600=CARTESIAN_POINT('Ctrl Pts',(2.62671498926561,2.65295659002752,9.13466151125581));
#11601=CARTESIAN_POINT('Ctrl Pts',(2.61261755429364,2.64318293799529,9.13359296167823));
#11602=CARTESIAN_POINT('Ctrl Pts',(2.60497424168383,2.63783459502239,9.13300959757436));
#11603=CARTESIAN_POINT('Ctrl Pts',(2.58310667852573,2.62239108835879,9.13132927099558));
#11604=CARTESIAN_POINT('Ctrl Pts',(2.56894127601944,2.61221370956518,9.13022695600439));
#11605=CARTESIAN_POINT('Ctrl Pts',(2.46617285079706,2.53710561252241,9.12213244115718));
#11606=CARTESIAN_POINT('Ctrl Pts',(2.38086696761499,2.46780362593014,9.114883216524));
#11607=CARTESIAN_POINT('Ctrl Pts',(2.12866586809538,2.24057693872543,9.09214864491327));
#11608=CARTESIAN_POINT('Ctrl Pts',(1.97495576443553,2.06904829350985,9.07642041301047));
#11609=CARTESIAN_POINT('Ctrl Pts',(1.77242115453936,1.78765196040579,9.05357734024762));
#11610=CARTESIAN_POINT('Ctrl Pts',(1.70927570441868,1.68900764002873,9.04602532154727));
#11611=CARTESIAN_POINT('Ctrl Pts',(1.63800597973549,1.56305744109691,9.03693134391803));
#11612=CARTESIAN_POINT('Ctrl Pts',(1.62469144566678,1.53880418423814,9.03520392313672));
#11613=CARTESIAN_POINT('Ctrl Pts',(1.60411296453515,1.50014734094187,9.0324872429685));
#11614=CARTESIAN_POINT('Ctrl Pts',(1.59664223650824,1.4858559465593,9.03149069189127));
#11615=CARTESIAN_POINT('Ctrl Pts',(1.58291364085979,1.45910619690964,9.02963968737945));
#11616=CARTESIAN_POINT('Ctrl Pts',(1.57662876521555,1.44666220188011,9.02878429972129));
#11617=CARTESIAN_POINT('Ctrl Pts',(1.56281654165101,1.41886739591356,9.02688616956951));
#11618=CARTESIAN_POINT('Ctrl Pts',(1.55533016776276,1.40349660809365,9.0258448738598));
#11619=CARTESIAN_POINT('Ctrl Pts',(1.53374105391334,1.35825959221902,9.02280424365691));
#11620=CARTESIAN_POINT('Ctrl Pts',(1.51997442969955,1.32823473977894,9.02081650635699));
#11621=CARTESIAN_POINT('Ctrl Pts',(1.48975999653348,1.25957042538472,9.01633561077226));
#11622=CARTESIAN_POINT('Ctrl Pts',(1.47360078736609,1.22081014871945,9.01385207868912));
#11623=CARTESIAN_POINT('Ctrl Pts',(1.42227687165443,1.09059347651488,9.00564634477162));
#11624=CARTESIAN_POINT('Ctrl Pts',(1.39052424784582,0.997848125242633,9.00002697589843));
#11625=CARTESIAN_POINT('Ctrl Pts',(1.32586111105626,0.776525130115015,8.98696760051298));
#11626=CARTESIAN_POINT('Ctrl Pts',(1.29656636971623,0.647080421732769,8.97960075979825));
#11627=CARTESIAN_POINT('Ctrl Pts',(1.26215553017199,0.435019620977347,8.96755879082327));
#11628=CARTESIAN_POINT('Ctrl Pts',(1.25209532960429,0.353368032262696,8.96292675735798));
#11629=CARTESIAN_POINT('Ctrl Pts',(1.23736822778804,0.179127570220786,8.95289841079886));
#11630=CARTESIAN_POINT('Ctrl Pts',(1.23355060378722,0.0865458005470657,
8.94748415899529));
#11631=CARTESIAN_POINT('Ctrl Pts',(1.23375466895951,-0.0219365159964151,
8.94090896896696));
#11632=CARTESIAN_POINT('Ctrl Pts',(1.23390181612946,-0.0378099516884193,
8.93994106217947));
#11633=CARTESIAN_POINT('Ctrl Pts',(1.23433165877112,-0.0636119274055645,
8.93835737351153));
#11634=CARTESIAN_POINT('Ctrl Pts',(1.23454299988932,-0.0735415990230416,
8.9377454057285));
#11635=CARTESIAN_POINT('Ctrl Pts',(1.23500297903915,-0.0912952931957789,
8.93664652168846));
#11636=CARTESIAN_POINT('Ctrl Pts',(1.23523422697856,-0.0991195726215972,
8.93616057729858));
#11637=CARTESIAN_POINT('Ctrl Pts',(1.23580238771824,-0.116231778231468,
8.93509411985661));
#11638=CARTESIAN_POINT('Ctrl Pts',(1.2361509670397,-0.12551898385345,8.93451298942317));
#11639=CARTESIAN_POINT('Ctrl Pts',(1.23726241310558,-0.152066911768491,
8.93284536390891));
#11640=CARTESIAN_POINT('Ctrl Pts',(1.23812390864203,-0.169322878409737,
8.93175363800632));
#11641=CARTESIAN_POINT('Ctrl Pts',(1.24520168967922,-0.291376725418134,
8.92398055944772));
#11642=CARTESIAN_POINT('Ctrl Pts',(1.25639623687191,-0.395812937733077,
8.91706414910813));
#11643=CARTESIAN_POINT('Ctrl Pts',(1.30667914247089,-0.716312161538888,
8.89536709799072));
#11644=CARTESIAN_POINT('Ctrl Pts',(1.36275520070235,-0.929099397203223,
8.88033493726173));
#11645=CARTESIAN_POINT('Ctrl Pts',(1.48609837219437,-1.25703835319484,8.85713857048745));
#11646=CARTESIAN_POINT('Ctrl Pts',(1.53959816372505,-1.37663326723985,8.84866028843823));
#11647=CARTESIAN_POINT('Ctrl Pts',(1.6134158586213,-1.51788541816975,8.83863829944873));
#11648=CARTESIAN_POINT('Ctrl Pts',(1.62693454821042,-1.54293946088116,8.83686000024468));
#11649=CARTESIAN_POINT('Ctrl Pts',(1.64871703675081,-1.58205935714622,8.83408151332681));
#11650=CARTESIAN_POINT('Ctrl Pts',(1.65675843348644,-1.59624674087481,8.83307347065534));
#11651=CARTESIAN_POINT('Ctrl Pts',(1.67180157114896,-1.62232384028896,8.8312197086133));
#11652=CARTESIAN_POINT('Ctrl Pts',(1.67877261068145,-1.63423074004063,8.83037291119591));
#11653=CARTESIAN_POINT('Ctrl Pts',(1.6944097390735,-1.66055064123587,8.82850009316388));
#11654=CARTESIAN_POINT('Ctrl Pts',(1.70311265109821,-1.67494138031732,8.82747543901985));
#11655=CARTESIAN_POINT('Ctrl Pts',(1.72852904315753,-1.71623531232519,8.82453277910791));
#11656=CARTESIAN_POINT('Ctrl Pts',(1.74552726119505,-1.74296157598743,8.82262523867793));
#11657=CARTESIAN_POINT('Ctrl Pts',(1.88652935879342,-1.95760453343155,8.80726958512924));
#11658=CARTESIAN_POINT('Ctrl Pts',(2.02952215622663,-2.13231125178817,8.7946048573358));
#11659=CARTESIAN_POINT('Ctrl Pts',(2.34010307766225,-2.43966393757368,8.77016899421306));
#11660=CARTESIAN_POINT('Ctrl Pts',(2.50492532105668,-2.57340583191477,8.75842800160268));
#11661=CARTESIAN_POINT('Ctrl Pts',(2.70298346429899,-2.70408198943641,8.74418389645411));
#11662=CARTESIAN_POINT('Ctrl Pts',(2.72449118569299,-2.71790796241603,8.74263511190485));
#11663=CARTESIAN_POINT('Ctrl Pts',(2.75472452676728,-2.73683851359313,8.74045190722554));
#11664=CARTESIAN_POINT('Ctrl Pts',(2.76331373284463,-2.74216056029999,8.73983098896695));
#11665=CARTESIAN_POINT('Ctrl Pts',(2.77818978169496,-2.75128152444725,8.73875417118699));
#11666=CARTESIAN_POINT('Ctrl Pts',(2.7844649064416,-2.75509953926674,8.73829950656211));
#11667=CARTESIAN_POINT('Ctrl Pts',(2.79772659707692,-2.76310644206574,8.737337597468));
#11668=CARTESIAN_POINT('Ctrl Pts',(2.80471605401932,-2.76729033022415,8.7368300245143));
#11669=CARTESIAN_POINT('Ctrl Pts',(2.82205124340896,-2.77757810069329,8.735569790862));
#11670=CARTESIAN_POINT('Ctrl Pts',(2.83241531176789,-2.78365068170309,8.73481515603995));
#11671=CARTESIAN_POINT('Ctrl Pts',(2.87125690608195,-2.80611824627147,8.73198327799059));
#11672=CARTESIAN_POINT('Ctrl Pts',(2.89994963406066,-2.82213470074953,8.72988391942714));
#11673=CARTESIAN_POINT('Ctrl Pts',(3.11536615215668,-2.93809717043213,8.71409573711287));
#11674=CARTESIAN_POINT('Ctrl Pts',(3.31127969950151,-3.0198513671987,8.69962580070306));
#11675=CARTESIAN_POINT('Ctrl Pts',(3.70505476047866,-3.14030303706421,8.67183545717458));
#11676=CARTESIAN_POINT('Ctrl Pts',(3.90138712320724,-3.18088578870972,8.65855784381704));
#11677=CARTESIAN_POINT('Ctrl Pts',(4.14180448333265,-3.20762411232021,8.64320293557294));
#11678=CARTESIAN_POINT('Ctrl Pts',(4.18345330094341,-3.21143720239514,8.64057341405049));
#11679=CARTESIAN_POINT('Ctrl Pts',(4.24369109510046,-3.21577176280041,8.63681259202144));
#11680=CARTESIAN_POINT('Ctrl Pts',(4.26222750451843,-3.21694462740009,8.63566106843576));
#11681=CARTESIAN_POINT('Ctrl Pts',(4.29490093229314,-3.21872854892906,8.63364117886267));
#11682=CARTESIAN_POINT('Ctrl Pts',(4.30903363253705,-3.21940686117232,8.63277073186177));
#11683=CARTESIAN_POINT('Ctrl Pts',(4.33828138555654,-3.22061763558807,8.63097586696577));
#11684=CARTESIAN_POINT('Ctrl Pts',(4.35339666174785,-3.2211368141386,8.6300518855014));
#11685=CARTESIAN_POINT('Ctrl Pts',(4.39232011918263,-3.22219949176642,8.6276815078878));
#11686=CARTESIAN_POINT('Ctrl Pts',(4.41613194417036,-3.22258554846624,8.62624004953389));
#11687=CARTESIAN_POINT('Ctrl Pts',(4.51869826278476,-3.22311140355569,8.62006599642272));
#11688=CARTESIAN_POINT('Ctrl Pts',(4.59744261371916,-3.22062843877784,8.61541526334332));
#11689=CARTESIAN_POINT('Ctrl Pts',(4.81359696306451,-3.20586842908658,8.60281850345185));
#11690=CARTESIAN_POINT('Ctrl Pts',(4.95043414859862,-3.18765357362187,8.59503880545987));
#11691=CARTESIAN_POINT('Ctrl Pts',(5.29806979917756,-3.11844808992389,8.5751848008833));
#11692=CARTESIAN_POINT('Ctrl Pts',(5.50562206020022,-3.05487583790019,8.5632575008652));
#11693=CARTESIAN_POINT('Ctrl Pts',(5.7411787905244,-2.95586894980729,8.54810622880221));
#11694=CARTESIAN_POINT('Ctrl Pts',(5.77687233089303,-2.94009782790998,8.54576325528096));
#11695=CARTESIAN_POINT('Ctrl Pts',(5.82430658877819,-2.91810113794584,8.54257457692905));
#11696=CARTESIAN_POINT('Ctrl Pts',(5.83630945116774,-2.91244471850141,8.54176117690007));
#11697=CARTESIAN_POINT('Ctrl Pts',(5.85511333458684,-2.90344094808087,8.54047607343421));
#11698=CARTESIAN_POINT('Ctrl Pts',(5.86193821675647,-2.90014337457348,8.54000739085381));
#11699=CARTESIAN_POINT('Ctrl Pts',(5.87576635642736,-2.89340176701809,8.53905306794945));
#11700=CARTESIAN_POINT('Ctrl Pts',(5.88276875855161,-2.8899563606369,8.53856733150461));
#11701=CARTESIAN_POINT('Ctrl Pts',(5.89925924756005,-2.88176798014905,8.53741766891512));
#11702=CARTESIAN_POINT('Ctrl Pts',(5.90873652238066,-2.87700355020117,8.53675242885094));
#11703=CARTESIAN_POINT('Ctrl Pts',(5.92896577514654,-2.86670844625675,8.53532306453999));
#11704=CARTESIAN_POINT('Ctrl Pts',(5.93971046608167,-2.86116389145982,8.53455813576977));
#11705=CARTESIAN_POINT('Ctrl Pts',(5.96911069580212,-2.84578245441171,8.53244985369507));
#11706=CARTESIAN_POINT('Ctrl Pts',(5.98770093686906,-2.83582287642731,8.53109980657977));
#11707=CARTESIAN_POINT('Ctrl Pts',(6.04723101679982,-2.80317408374387,8.52672500247137));
#11708=CARTESIAN_POINT('Ctrl Pts',(6.08777324691131,-2.7797760262058,8.52366619160925));
#11709=CARTESIAN_POINT('Ctrl Pts',(6.41431278253724,-2.58171714974494,8.4984575836249));
#11710=CARTESIAN_POINT('Ctrl Pts',(6.67200624246284,-2.36429467617147,8.47520927718465));
#11711=CARTESIAN_POINT('Ctrl Pts',(6.93404981340766,-2.06201681177209,8.44945534797583));
#11712=CARTESIAN_POINT('Ctrl Pts',(6.97502514629658,-2.01176438373979,8.44533941364197));
#11713=CARTESIAN_POINT('Ctrl Pts',(7.0284249128865,-1.94208342591629,8.43984758741855));
#11714=CARTESIAN_POINT('Ctrl Pts',(7.04219570772101,-1.92371065671693,8.4384189906345));
#11715=CARTESIAN_POINT('Ctrl Pts',(7.06460096029538,-1.89314261959641,8.43607350344447));
#11716=CARTESIAN_POINT('Ctrl Pts',(7.07334887032411,-1.88103191322775,8.43515222794963));
#11717=CARTESIAN_POINT('Ctrl Pts',(7.09026642093851,-1.85726461894156,8.43335954003556));
#11718=CARTESIAN_POINT('Ctrl Pts',(7.098443660284,-1.84561388857948,8.43248784898087));
#11719=CARTESIAN_POINT('Ctrl Pts',(7.11759174077314,-1.8179441226612,8.43043408051115));
#11720=CARTESIAN_POINT('Ctrl Pts',(7.12849561901404,-1.80187925502417,8.42925456087466));
#11721=CARTESIAN_POINT('Ctrl Pts',(7.16447121463733,-1.74783104754734,8.42532809204456));
#11722=CARTESIAN_POINT('Ctrl Pts',(7.18888412320446,-1.709414307437,8.42260568762478));
#11723=CARTESIAN_POINT('Ctrl Pts',(7.2453806841808,-1.61620528356107,8.41615118502481));
#11724=CARTESIAN_POINT('Ctrl Pts',(7.2766754419555,-1.56095619535568,8.412446381932));
#11725=CARTESIAN_POINT('Ctrl Pts',(7.41819558545888,-1.2929425944155,8.39496273568616));
#11726=CARTESIAN_POINT('Ctrl Pts',(7.50609147992221,-1.06926399160712,8.38186764287226));
#11727=CARTESIAN_POINT('Ctrl Pts',(7.58606020599265,-0.772268420479377,
8.36444103141177));
#11728=CARTESIAN_POINT('Ctrl Pts',(7.60165288054581,-0.706085748941868,
8.36055045159957));
#11729=CARTESIAN_POINT('Ctrl Pts',(7.62726270620167,-0.57958427145637,8.35301918685649));
#11730=CARTESIAN_POINT('Ctrl Pts',(7.63767898783902,-0.519377124168955,
8.34939458018844));
#11731=CARTESIAN_POINT('Ctrl Pts',(7.64857245229546,-0.443656866994801,
8.34474539364199));
#11732=CARTESIAN_POINT('Ctrl Pts',(7.65065798754777,-0.428383655577541,
8.34380303184777));
#11733=CARTESIAN_POINT('Ctrl Pts',(7.65378488134748,-0.404190592809645,
8.34230221639636));
#11734=CARTESIAN_POINT('Ctrl Pts',(7.6548986933696,-0.395280119225564,8.34174772096573));
#11735=CARTESIAN_POINT('Ctrl Pts',(7.65689661803388,-0.378735224277724,
8.34071472768886));
#11736=CARTESIAN_POINT('Ctrl Pts',(7.6577906759714,-0.371102183949988,8.34023679040597));
#11737=CARTESIAN_POINT('Ctrl Pts',(7.6595268722726,-0.355806045237808,8.33927634923776));
#11738=CARTESIAN_POINT('Ctrl Pts',(7.66036882904639,-0.348143013255039,
8.33879384922559));
#11739=CARTESIAN_POINT('Ctrl Pts',(7.66225149399062,-0.330422577657364,
8.3376751077898));
#11740=CARTESIAN_POINT('Ctrl Pts',(7.66327237515316,-0.320363208981211,
8.3370378139275));
#11741=CARTESIAN_POINT('Ctrl Pts',(7.6658015915591,-0.294216968424916,8.33537589654803));
#11742=CARTESIAN_POINT('Ctrl Pts',(7.66723629441381,-0.278123471324824,
8.33434758398818));
#11743=CARTESIAN_POINT('Ctrl Pts',(7.67560750110016,-0.175501658053048,
8.32775910133968));
#11744=CARTESIAN_POINT('Ctrl Pts',(7.67916592121515,-0.0887415669224956,
8.32204787422042));
#11745=CARTESIAN_POINT('Ctrl Pts',(7.6792185144777,-0.00195296268717014,
8.31625837989182));
#11746=CARTESIAN_POINT('Ctrl Pts',(7.67921851169523,-0.00195754888720522,
8.31625868582799));
#11747=CARTESIAN_POINT('Ctrl Pts',(7.67921890804601,-0.0013050291805212,
8.31621515756297));
#11748=CARTESIAN_POINT('Ctrl Pts',(7.67921910621822,-0.000652512869385687,
8.31617162515749));
#11749=CARTESIAN_POINT('Ctrl Pts',(7.67921910621823,-4.32305015001326E-11,
8.31612808864258));
#11750=CARTESIAN_POINT('Origin',(4.45646910621825,-5.13094777615093E-16,
-2.31077344927308));
#11751=CARTESIAN_POINT('',(7.67921910621823,-4.71466720739905E-12,7.06143953130409));
#11752=CARTESIAN_POINT('',(7.67921910621823,3.2100258423573E-11,7.30846150265208));
#11753=CARTESIAN_POINT('',(7.67921910621823,-3.51191647465084E-13,-2.31077344927308));
#11754=CARTESIAN_POINT('',(7.6792190806041,-0.00206625803567177,7.30858154752831));
#11755=CARTESIAN_POINT('Ctrl Pts',(7.67921910621823,3.2100258423573E-11,
7.30846150265207));
#11756=CARTESIAN_POINT('Ctrl Pts',(7.67921910621824,-0.000687215974718567,
7.30850105516546));
#11757=CARTESIAN_POINT('Ctrl Pts',(7.67921888640636,-0.00137443588253173,
7.30854061414169));
#11758=CARTESIAN_POINT('Ctrl Pts',(7.6792184467751,-0.00206165958607078,
7.30858017961946));
#11759=CARTESIAN_POINT('Ctrl Pts',(7.67921844378978,-0.00206632091524094,
7.3085804479859));
#11760=CARTESIAN_POINT('Ctrl Pts',(7.67918020638304,-0.0617035129651612,
7.3120139379522));
#11761=CARTESIAN_POINT('Ctrl Pts',(7.67748658974212,-0.121325551268667,
7.31549377261651));
#11762=CARTESIAN_POINT('Ctrl Pts',(7.67242000325691,-0.211463230508943,
7.32087119381463));
#11763=CARTESIAN_POINT('Ctrl Pts',(7.67026365826296,-0.242035732280913,
7.32271546731949));
#11764=CARTESIAN_POINT('Ctrl Pts',(7.66679089382596,-0.282948839811236,
7.32521639024807));
#11765=CARTESIAN_POINT('Ctrl Pts',(7.66585977297981,-0.293321610761411,
7.32585328936783));
#11766=CARTESIAN_POINT('Ctrl Pts',(7.66414196846598,-0.311469816463751,
7.32697285839252));
#11767=CARTESIAN_POINT('Ctrl Pts',(7.66337724195445,-0.319247308115157,
7.32745434428977));
#11768=CARTESIAN_POINT('Ctrl Pts',(7.66181770050518,-0.334537018894052,
7.32840435288995));
#11769=CARTESIAN_POINT('Ctrl Pts',(7.66102474504478,-0.342049389227136,
7.32887277415009));
#11770=CARTESIAN_POINT('Ctrl Pts',(7.65925805141564,-0.358241281463178,
7.32988604944475));
#11771=CARTESIAN_POINT('Ctrl Pts',(7.65827544404199,-0.366919628846942,
7.33043138121957));
#11772=CARTESIAN_POINT('Ctrl Pts',(7.65554427546374,-0.390194491264422,
7.33189977082851));
#11773=CARTESIAN_POINT('Ctrl Pts',(7.65373111810975,-0.404783012952968,
7.33282631555129));
#11774=CARTESIAN_POINT('Ctrl Pts',(7.64514939637772,-0.470172437357681,
7.33700547659333));
#11775=CARTESIAN_POINT('Ctrl Pts',(7.63726979041701,-0.520817092241585,
7.34031311758333));
#11776=CARTESIAN_POINT('Ctrl Pts',(7.61659074472771,-0.63563234806109,7.34794181485242));
#11777=CARTESIAN_POINT('Ctrl Pts',(7.6030376960173,-0.699644529982602,7.35228830604115));
#11778=CARTESIAN_POINT('Ctrl Pts',(7.53514353935692,-0.978186076470445,
7.37149837338241));
#11779=CARTESIAN_POINT('Ctrl Pts',(7.46072994356382,-1.18722989462073,7.38664401679061));
#11780=CARTESIAN_POINT('Ctrl Pts',(7.31189390507405,-1.49938982229062,7.40947636014331));
#11781=CARTESIAN_POINT('Ctrl Pts',(7.25183399838337,-1.60859015487668,7.41752141132423));
#11782=CARTESIAN_POINT('Ctrl Pts',(7.17102722442641,-1.73725135190454,7.42706402989331));
#11783=CARTESIAN_POINT('Ctrl Pts',(7.15616147287261,-1.76026396790633,7.4287737602139));
#11784=CARTESIAN_POINT('Ctrl Pts',(7.13220263814914,-1.79633534285425,7.43145901354115));
#11785=CARTESIAN_POINT('Ctrl Pts',(7.12330345040149,-1.80952070810709,7.43244171590857));
#11786=CARTESIAN_POINT('Ctrl Pts',(7.10640998992296,-1.83415534870922,7.43428010288028));
#11787=CARTESIAN_POINT('Ctrl Pts',(7.09843825459297,-1.84561955967894,7.43513661089269));
#11788=CARTESIAN_POINT('Ctrl Pts',(7.08036672374754,-1.87125133572545,7.43705400370565));
#11789=CARTESIAN_POINT('Ctrl Pts',(7.07022615083744,-1.88538972069481,7.43811329921883));
#11790=CARTESIAN_POINT('Ctrl Pts',(7.04403919945474,-1.92128324234704,7.44080735050458));
#11791=CARTESIAN_POINT('Ctrl Pts',(7.02783250030479,-1.94292013403791,7.44243588926601));
#11792=CARTESIAN_POINT('Ctrl Pts',(6.91411423935617,-2.09082505716037,7.45360588244969));
#11793=CARTESIAN_POINT('Ctrl Pts',(6.80761068029022,-2.20991211346664,7.46277599905399));
#11794=CARTESIAN_POINT('Ctrl Pts',(6.50215932831748,-2.50425576562502,7.48671709111689));
#11795=CARTESIAN_POINT('Ctrl Pts',(6.28974365737954,-2.66368421642327,7.50106549903362));
#11796=CARTESIAN_POINT('Ctrl Pts',(6.03810119144741,-2.80806174922007,7.518295346561));
#11797=CARTESIAN_POINT('Ctrl Pts',(6.01578179550669,-2.82051674223762,7.51982600830751));
#11798=CARTESIAN_POINT('Ctrl Pts',(5.97631918044489,-2.84192668803427,7.52254084281685));
#11799=CARTESIAN_POINT('Ctrl Pts',(5.95923881759403,-2.85099538778073,7.52371863883487));
#11800=CARTESIAN_POINT('Ctrl Pts',(5.93348912295942,-2.8643713297818,7.52549990586779));
#11801=CARTESIAN_POINT('Ctrl Pts',(5.92487996514342,-2.86879430919172,7.52609639684756));
#11802=CARTESIAN_POINT('Ctrl Pts',(5.91622426249262,-2.87319203102394,7.52669718606732));
#11803=CARTESIAN_POINT('Ctrl Pts',(5.91619738017794,-2.87320568870586,7.52669905196951));
#11804=CARTESIAN_POINT('Ctrl Pts',(5.91614332399392,-2.87323315124092,7.52670280403155));
#11805=CARTESIAN_POINT('Ctrl Pts',(5.91611615016522,-2.87324695606307,7.52670469018881));
#11806=CARTESIAN_POINT('Ctrl Pts',(5.91606150714547,-2.87327471478184,7.52670848302596));
#11807=CARTESIAN_POINT('Ctrl Pts',(5.91603403793397,-2.87328866867825,7.52671038970751));
#11808=CARTESIAN_POINT('Ctrl Pts',(5.91597880022802,-2.87331672750524,7.5267142238661));
#11809=CARTESIAN_POINT('Ctrl Pts',(5.9159510318188,-2.87333083238168,7.52671615133745));
#11810=CARTESIAN_POINT('Ctrl Pts',(5.91589519186165,-2.87335919509461,7.526720027344));
#11811=CARTESIAN_POINT('Ctrl Pts',(5.91586712023358,-2.8733734529607,7.526721975885));
#11812=CARTESIAN_POINT('Ctrl Pts',(5.91581066986365,-2.87340212363845,7.52672589430751));
#11813=CARTESIAN_POINT('Ctrl Pts',(5.91578229109896,-2.87341653645034,7.52672786419085));
#11814=CARTESIAN_POINT('Ctrl Pts',(5.91572522238854,-2.8734455190511,7.52673182558112));
#11815=CARTESIAN_POINT('Ctrl Pts',(5.91569653241074,-2.87346008884462,7.52673381709053));
#11816=CARTESIAN_POINT('Ctrl Pts',(5.91563883706423,-2.87348938751146,7.52673782202595));
#11817=CARTESIAN_POINT('Ctrl Pts',(5.91560983180642,-2.87350411631655,7.52673983544451));
#11818=CARTESIAN_POINT('Ctrl Pts',(5.91555150177167,-2.87353373506692,7.5267438844856));
#11819=CARTESIAN_POINT('Ctrl Pts',(5.91552217695326,-2.87354862502103,7.52674592011126));
#11820=CARTESIAN_POINT('Ctrl Pts',(5.9154632035932,-2.87357856816732,7.52675001385919));
#11821=CARTESIAN_POINT('Ctrl Pts',(5.91543355502112,-2.87359362136243,7.52675207198385));
#11822=CARTESIAN_POINT('Ctrl Pts',(5.91537392983196,-2.87362389314725,7.5267562110306));
#11823=CARTESIAN_POINT('Ctrl Pts',(5.91534395319029,-2.87363911173661,7.52675829195469));
#11824=CARTESIAN_POINT('Ctrl Pts',(5.9152836674988,-2.87366971648641,7.52676247690405));
#11825=CARTESIAN_POINT('Ctrl Pts',(5.91525335839336,-2.87368510266194,7.52676458093347));
#11826=CARTESIAN_POINT('Ctrl Pts',(5.91519240325465,-2.87371604483886,7.52676881240812));
#11827=CARTESIAN_POINT('Ctrl Pts',(5.9151617572847,-2.87373160079465,7.52677093984926));
#11828=CARTESIAN_POINT('Ctrl Pts',(5.91510012389725,-2.87376288478576,7.526775218462));
#11829=CARTESIAN_POINT('Ctrl Pts',(5.91506913648204,-2.87377861280613,7.52677736963376));
#11830=CARTESIAN_POINT('Ctrl Pts',(5.915006815644,-2.87381024319937,7.52678169602523));
#11831=CARTESIAN_POINT('Ctrl Pts',(5.91497548220631,-2.87382614556565,7.52678387124629));
#11832=CARTESIAN_POINT('Ctrl Pts',(5.91491246465541,-2.87385812697718,7.52678824606137));
#11833=CARTESIAN_POINT('Ctrl Pts',(5.91488078054145,-2.87387420600834,7.52679044565577));
#11834=CARTESIAN_POINT('Ctrl Pts',(5.91481705688783,-2.87390654311663,7.52679486954826));
#11835=CARTESIAN_POINT('Ctrl Pts',(5.91478501735916,-2.87392280117334,7.52679709384592));
#11836=CARTESIAN_POINT('Ctrl Pts',(5.9147205781317,-2.8739554986955,7.52680156747532));
#11837=CARTESIAN_POINT('Ctrl Pts',(5.91468817833591,-2.87397193819497,7.52680381681412));
#11838=CARTESIAN_POINT('Ctrl Pts',(5.91462301360079,-2.87400500108034,7.52680834087211));
#11839=CARTESIAN_POINT('Ctrl Pts',(5.91459024874631,-2.87402162440758,7.52681061558574));
#11840=CARTESIAN_POINT('Ctrl Pts',(5.91452434893773,-2.87405505741602,7.5268151907385));
#11841=CARTESIAN_POINT('Ctrl Pts',(5.91449121396325,-2.87407186709156,7.5268174911794));
#11842=CARTESIAN_POINT('Ctrl Pts',(5.91442456887314,-2.87410567530606,7.52682211813778));
#11843=CARTESIAN_POINT('Ctrl Pts',(5.91439105878632,-2.87412267381402,7.52682444465363));
#11844=CARTESIAN_POINT('Ctrl Pts',(5.91432365834847,-2.87415686224275,7.52682912411869));
#11845=CARTESIAN_POINT('Ctrl Pts',(5.91428976800086,-2.874174052145,7.52683147706804));
#11846=CARTESIAN_POINT('Ctrl Pts',(5.9142216018802,-2.87420862592962,7.52683620975957));
#11847=CARTESIAN_POINT('Ctrl Pts',(5.91418732605847,-2.87422600981947,7.52683858950551));
#11848=CARTESIAN_POINT('Ctrl Pts',(5.91411838365043,-2.87426097423532,7.52684337616208));
#11849=CARTESIAN_POINT('Ctrl Pts',(5.91408371712026,-2.8742785547152,7.52684578306921));
#11850=CARTESIAN_POINT('Ctrl Pts',(5.91401398798716,-2.8743139149499,7.52685062441787));
#11851=CARTESIAN_POINT('Ctrl Pts',(5.91397892529484,-2.87433169473196,7.52685305886602));
#11852=CARTESIAN_POINT('Ctrl Pts',(5.91390839834184,-2.87436745630325,7.52685795567954));
#11853=CARTESIAN_POINT('Ctrl Pts',(5.91387293412571,-2.87438543805134,7.52686041804222));
#11854=CARTESIAN_POINT('Ctrl Pts',(5.91380159858358,-2.87442160630858,7.52686537107079));
#11855=CARTESIAN_POINT('Ctrl Pts',(5.91376572723567,-2.87443979280982,7.52686786173863));
#11856=CARTESIAN_POINT('Ctrl Pts',(5.91369357179188,-2.87447637337453,7.5268728717703));
#11857=CARTESIAN_POINT('Ctrl Pts',(5.91365728772179,-2.87449476740542,7.52687539113275));
#11858=CARTESIAN_POINT('Ctrl Pts',(5.9135843010979,-2.87453176587839,7.52688045895323));
#11859=CARTESIAN_POINT('Ctrl Pts',(5.91354759857372,-2.87455037028544,7.52688300740962));
#11860=CARTESIAN_POINT('Ctrl Pts',(5.91347376934107,-2.8745877923401,7.52688813381515));
#11861=CARTESIAN_POINT('Ctrl Pts',(5.91343664250006,-2.87460661003437,7.52689071177393));
#11862=CARTESIAN_POINT('Ctrl Pts',(5.91336195868054,-2.87464446161903,7.52689589759898));
#11863=CARTESIAN_POINT('Ctrl Pts',(5.91332440173229,-2.87466349547306,7.52689850546361));
#11864=CARTESIAN_POINT('Ctrl Pts',(5.91324885164239,-2.874701782383,7.52690375152228));
#11865=CARTESIAN_POINT('Ctrl Pts',(5.91321085854592,-2.87472103539445,7.52690638971367));
#11866=CARTESIAN_POINT('Ctrl Pts',(5.9131344301249,-2.87475976361232,7.52691169684635));
#11867=CARTESIAN_POINT('Ctrl Pts',(5.91309599476147,-2.87477923881632,7.52691436579084));
#11868=CARTESIAN_POINT('Ctrl Pts',(5.9130186756693,-2.87481841446236,7.52691973485741));
#11869=CARTESIAN_POINT('Ctrl Pts',(5.91297979187752,-2.87483811491365,7.52692243498437));
#11870=CARTESIAN_POINT('Ctrl Pts',(5.91290156963042,-2.87487774417691,7.52692786685476));
#11871=CARTESIAN_POINT('Ctrl Pts',(5.91286223115425,-2.87489767297615,7.52693059860015));
#11872=CARTESIAN_POINT('Ctrl Pts',(5.91278309312252,-2.87493776211543,7.52693609415454));
#11873=CARTESIAN_POINT('Ctrl Pts',(5.91274329358416,-2.87495792242288,7.52693885796286));
#11874=CARTESIAN_POINT('Ctrl Pts',(5.91266322700936,-2.87499847775797,7.52694441809044));
#11875=CARTESIAN_POINT('Ctrl Pts',(5.91262295988501,-2.87501887280566,7.52694721441635));
#11876=CARTESIAN_POINT('Ctrl Pts',(5.91254195146517,-2.87505990092728,7.5269528400442));
#11877=CARTESIAN_POINT('Ctrl Pts',(5.91250121027844,-2.875080533921,7.52695566933913));
#11878=CARTESIAN_POINT('Ctrl Pts',(5.91241924706806,-2.87512204123482,7.52696136136963));
#11879=CARTESIAN_POINT('Ctrl Pts',(5.91237802503446,-2.87514291553416,7.52696422410646));
#11880=CARTESIAN_POINT('Ctrl Pts',(5.91229509340215,-2.87518490878858,7.52696998348976));
#11881=CARTESIAN_POINT('Ctrl Pts',(5.91225338377053,-2.87520602773387,7.5269728801391));
#11882=CARTESIAN_POINT('Ctrl Pts',(5.91216947004982,-2.87524851369029,7.52697870782789));
#11883=CARTESIAN_POINT('Ctrl Pts',(5.91212726594579,-2.87526988068185,7.52698163886898));
#11884=CARTESIAN_POINT('Ctrl Pts',(5.91204235630175,-2.8753128661821,7.52698753582775));
#11885=CARTESIAN_POINT('Ctrl Pts',(5.91199965071389,-2.87533448468717,7.52699050174938));
#11886=CARTESIAN_POINT('Ctrl Pts',(5.9119137309574,-2.87537797674735,7.52699646896736));
#11887=CARTESIAN_POINT('Ctrl Pts',(5.91187051682151,-2.87539985025732,7.52699947026206));
#11888=CARTESIAN_POINT('Ctrl Pts',(5.91178357278943,-2.87544385587524,7.52700550872677));
#11889=CARTESIAN_POINT('Ctrl Pts',(5.91173984283814,-2.87546598798174,7.52700854590125));
#11890=CARTESIAN_POINT('Ctrl Pts',(5.91165185983416,-2.87551051441975,7.52701465663737));
#11891=CARTESIAN_POINT('Ctrl Pts',(5.91160760679998,-2.87553290871179,7.52701773019839));
#11892=CARTESIAN_POINT('Ctrl Pts',(5.91152199272508,-2.87557623131725,7.5270236765146));
#11893=CARTESIAN_POINT('Ctrl Pts',(5.91148063168748,-2.87559715979139,7.52702654926596));
#11894=CARTESIAN_POINT('Ctrl Pts',(5.90442868615588,-2.8791652171741,7.52751634990232));
#11895=CARTESIAN_POINT('Ctrl Pts',(5.89740538435486,-2.88268658207869,7.52800489810312));
#11896=CARTESIAN_POINT('Ctrl Pts',(5.88132808729335,-2.89067403331396,7.52912488672838));
#11897=CARTESIAN_POINT('Ctrl Pts',(5.87226594297745,-2.89512327775316,7.52975734441413));
#11898=CARTESIAN_POINT('Ctrl Pts',(5.84808164591235,-2.90685634952692,7.53144798854324));
#11899=CARTESIAN_POINT('Ctrl Pts',(5.83292346582989,-2.91406462960333,7.5325105400672));
#11900=CARTESIAN_POINT('Ctrl Pts',(5.7006482605295,-2.9757041137638,7.54180335861236));
#11901=CARTESIAN_POINT('Ctrl Pts',(5.5804255078002,-3.02316247948295,7.55038537350614));
#11902=CARTESIAN_POINT('Ctrl Pts',(5.27968466108615,-3.12145907507314,7.57167483474776));
#11903=CARTESIAN_POINT('Ctrl Pts',(5.09692751588153,-3.16401822938152,7.58444290431546));
#11904=CARTESIAN_POINT('Ctrl Pts',(4.82108046907848,-3.2033605936835,7.60292190032956));
#11905=CARTESIAN_POINT('Ctrl Pts',(4.73014240208535,-3.21240810900902,7.60889424641218));
#11906=CARTESIAN_POINT('Ctrl Pts',(4.5989436049025,-3.2198483055755,7.61732455134665));
#11907=CARTESIAN_POINT('Ctrl Pts',(4.55891111003898,-3.22137050923549,7.6198723556987));
#11908=CARTESIAN_POINT('Ctrl Pts',(4.48704260334128,-3.22276209130484,7.62440318758332));
#11909=CARTESIAN_POINT('Ctrl Pts',(4.45521778407727,-3.22290688458961,7.62639438847226));
#11910=CARTESIAN_POINT('Ctrl Pts',(4.40654629590824,-3.22240735903025,7.62941741368368));
#11911=CARTESIAN_POINT('Ctrl Pts',(4.38969885983033,-3.22210229911656,7.63045975220696));
#11912=CARTESIAN_POINT('Ctrl Pts',(4.35905913390518,-3.22130707872627,7.63234823771107));
#11913=CARTESIAN_POINT('Ctrl Pts',(4.34526621214669,-3.22086043222862,7.63319572265086));
#11914=CARTESIAN_POINT('Ctrl Pts',(4.31520614677569,-3.21969369026665,7.63503713135469));
#11915=CARTESIAN_POINT('Ctrl Pts',(4.29894067307012,-3.21893887652395,7.6360299473));
#11916=CARTESIAN_POINT('Ctrl Pts',(4.25437073889694,-3.21653192777853,7.63874106001821));
#11917=CARTESIAN_POINT('Ctrl Pts',(4.22608084949324,-3.2146294842955,7.64045152062713));
#11918=CARTESIAN_POINT('Ctrl Pts',(4.06960495898306,-3.20203046835265,7.64986036240773));
#11919=CARTESIAN_POINT('Ctrl Pts',(3.94211569634664,-3.18403973880444,7.65732633446367));
#11920=CARTESIAN_POINT('Ctrl Pts',(3.59907319593254,-3.11448164008162,7.67725560294875));
#11921=CARTESIAN_POINT('Ctrl Pts',(3.38723747971508,-3.04825535591424,7.6893597258122));
#11922=CARTESIAN_POINT('Ctrl Pts',(3.08691799803865,-2.91917508021386,7.70801264061929));
#11923=CARTESIAN_POINT('Ctrl Pts',(2.99208253731074,-2.87277229552128,7.71415091209754));
#11924=CARTESIAN_POINT('Ctrl Pts',(2.88455813027404,-2.81345209126844,7.72159702695786));
#11925=CARTESIAN_POINT('Ctrl Pts',(2.86948000446817,-2.80497457150385,7.72265275069675));
#11926=CARTESIAN_POINT('Ctrl Pts',(2.8464026799731,-2.791753952857,7.72428754469633));
#11927=CARTESIAN_POINT('Ctrl Pts',(2.83835428256579,-2.787096776688,7.72486127794301));
#11928=CARTESIAN_POINT('Ctrl Pts',(2.82356738299414,-2.77845475238457,7.72592220226524));
#11929=CARTESIAN_POINT('Ctrl Pts',(2.81682314219335,-2.77448012380268,7.72640873909922));
#11930=CARTESIAN_POINT('Ctrl Pts',(2.80155849066583,-2.76540900899988,7.72751596400573));
#11931=CARTESIAN_POINT('Ctrl Pts',(2.79304715648399,-2.76029772733014,7.72813759138408));
#11932=CARTESIAN_POINT('Ctrl Pts',(2.77100103982271,-2.74691945536921,7.72975854261043));
#11933=CARTESIAN_POINT('Ctrl Pts',(2.75750360660644,-2.73859184703327,7.7307615956832));
#11934=CARTESIAN_POINT('Ctrl Pts',(2.66592016021447,-2.68114933368016,7.73763754250189));
#11935=CARTESIAN_POINT('Ctrl Pts',(2.58991955152757,-2.62880519832061,7.74369153494054));
#11936=CARTESIAN_POINT('Ctrl Pts',(2.45029939372569,-2.52353484522955,7.75534358972921));
#11937=CARTESIAN_POINT('Ctrl Pts',(2.3862622701084,-2.47127251457562,7.76091947144446));
#11938=CARTESIAN_POINT('Ctrl Pts',(2.22491934130544,-2.32892041412423,7.77547060486515));
#11939=CARTESIAN_POINT('Ctrl Pts',(2.13103174148922,-2.2351798280881,7.78444642351581));
#11940=CARTESIAN_POINT('Ctrl Pts',(1.97822316920715,-2.06252772218843,7.79978315762799));
#11941=CARTESIAN_POINT('Ctrl Pts',(1.9166431221908,-1.98620502305204,7.80620995802105));
#11942=CARTESIAN_POINT('Ctrl Pts',(1.83377796619093,-1.87333199146408,7.81520790277436));
#11943=CARTESIAN_POINT('Ctrl Pts',(1.80958614019447,-1.83899222202472,7.81788285931309));
#11944=CARTESIAN_POINT('Ctrl Pts',(1.76757732791114,-1.77681454085119,7.82261699510284));
#11945=CARTESIAN_POINT('Ctrl Pts',(1.74950455849487,-1.74915750459717,7.82468544725825));
#11946=CARTESIAN_POINT('Ctrl Pts',(1.72272723230812,-1.70677043338548,7.82780048587873));
#11947=CARTESIAN_POINT('Ctrl Pts',(1.71370983839016,-1.69224157915713,7.82885859756701));
#11948=CARTESIAN_POINT('Ctrl Pts',(1.69755052014457,-1.66573712999991,7.83077173601058));
#11949=CARTESIAN_POINT('Ctrl Pts',(1.6903699147922,-1.65378572485089,7.83162816576033));
#11950=CARTESIAN_POINT('Ctrl Pts',(1.67505134751849,-1.62791059094059,7.83346912942253));
#11951=CARTESIAN_POINT('Ctrl Pts',(1.66693985842808,-1.61397157069171,7.8344526860514));
#11952=CARTESIAN_POINT('Ctrl Pts',(1.64519805344523,-1.57595623186843,7.83711340459795));
#11953=CARTESIAN_POINT('Ctrl Pts',(1.63177239035655,-1.55176400028695,7.83878321308081));
#11954=CARTESIAN_POINT('Ctrl Pts',(1.56347530074076,-1.42487257312192,7.84742519107584));
#11955=CARTESIAN_POINT('Ctrl Pts',(1.51388445119901,-1.31942215157096,7.85420960525952));
#11956=CARTESIAN_POINT('Ctrl Pts',(1.38368678183428,-0.9984857233354,7.87401250631363));
#11957=CARTESIAN_POINT('Ctrl Pts',(1.3203121997983,-0.776839055453567,7.88656885806303));
#11958=CARTESIAN_POINT('Ctrl Pts',(1.26223768874595,-0.441756111965293,
7.90593875558007));
#11959=CARTESIAN_POINT('Ctrl Pts',(1.24900235386584,-0.33228689170426,7.9123361068974));
#11960=CARTESIAN_POINT('Ctrl Pts',(1.24019546835171,-0.204954002497827,
7.92007381077273));
#11961=CARTESIAN_POINT('Ctrl Pts',(1.23913257910733,-0.187531056072594,
7.92113897962062));
#11962=CARTESIAN_POINT('Ctrl Pts',(1.2377187398344,-0.160781624375865,7.92278535130385));
#11963=CARTESIAN_POINT('Ctrl Pts',(1.23726666439664,-0.151460507343538,
7.9233610982383));
#11964=CARTESIAN_POINT('Ctrl Pts',(1.23650991752259,-0.134319151317417,
7.92442387195206));
#11965=CARTESIAN_POINT('Ctrl Pts',(1.23619324114858,-0.126499645035582,
7.92491022724559));
#11966=CARTESIAN_POINT('Ctrl Pts',(1.23554097158206,-0.10879916617651,7.92601463282506));
#11967=CARTESIAN_POINT('Ctrl Pts',(1.23522236523769,-0.0989178178291134,
7.92663360166204));
#11968=CARTESIAN_POINT('Ctrl Pts',(1.23451489317406,-0.0733197131773398,
7.92824309285351));
#11969=CARTESIAN_POINT('Ctrl Pts',(1.23419556495815,-0.0576015065964676,
7.92923726057324));
#11970=CARTESIAN_POINT('Ctrl Pts',(1.23283769636146,0.0468754824732806,
7.93588165931194));
#11971=CARTESIAN_POINT('Ctrl Pts',(1.23535174813176,0.135634740869622,7.94169968024144));
#11972=CARTESIAN_POINT('Ctrl Pts',(1.26132431000045,0.508124649788423,7.96655106455441));
#11973=CARTESIAN_POINT('Ctrl Pts',(1.3186644953888,0.788266175328424,7.98616575056507));
#11974=CARTESIAN_POINT('Ctrl Pts',(1.4413368717694,1.14151496394501,8.01051003475562));
#11975=CARTESIAN_POINT('Ctrl Pts',(1.47409728168568,1.22455689598729,8.01621672730507));
#11976=CARTESIAN_POINT('Ctrl Pts',(1.5203274404603,1.32883637393786,8.02336502965246));
#11977=CARTESIAN_POINT('Ctrl Pts',(1.53065206413788,1.35141728633027,8.02491195998822));
#11978=CARTESIAN_POINT('Ctrl Pts',(1.54777897483766,1.38775890729739,8.02740052833206));
#11979=CARTESIAN_POINT('Ctrl Pts',(1.55442026339144,1.4015939469134,8.02834766363145));
#11980=CARTESIAN_POINT('Ctrl Pts',(1.56734123721506,1.42802513734399,8.03015683888255));
#11981=CARTESIAN_POINT('Ctrl Pts',(1.57360509450719,1.44062859066464,8.03101940235089));
#11982=CARTESIAN_POINT('Ctrl Pts',(1.58810281202865,1.4693260901403,8.03298334545138));
#11983=CARTESIAN_POINT('Ctrl Pts',(1.59638997514467,1.4853927902967,8.0340828310382));
#11984=CARTESIAN_POINT('Ctrl Pts',(1.6230067431694,1.53594723462193,8.03754293156664));
#11985=CARTESIAN_POINT('Ctrl Pts',(1.64182870891379,1.57017276203312,8.03988617000821));
#11986=CARTESIAN_POINT('Ctrl Pts',(1.79223939164411,1.83227699111076,8.05785837035122));
#11987=CARTESIAN_POINT('Ctrl Pts',(1.95066497013704,2.04360432280226,8.07240389583344));
#11988=CARTESIAN_POINT('Ctrl Pts',(2.21698782117833,2.32067176489093,8.09394482351849));
#11989=CARTESIAN_POINT('Ctrl Pts',(2.30579273130685,2.40320218412119,8.10077976953727));
#11990=CARTESIAN_POINT('Ctrl Pts',(2.4293382507474,2.50567539337132,8.11016519909149));
#11991=CARTESIAN_POINT('Ctrl Pts',(2.46010912082101,2.53025991095954,8.11249365982654));
#11992=CARTESIAN_POINT('Ctrl Pts',(2.51287651295211,2.57085686763634,8.1164860939486));
#11993=CARTESIAN_POINT('Ctrl Pts',(2.53463990663532,2.58716632998767,8.11813259316799));
#11994=CARTESIAN_POINT('Ctrl Pts',(2.5656150363775,2.6097725637616,8.12047987779021));
#11995=CARTESIAN_POINT('Ctrl Pts',(2.57465771893149,2.61630041129315,8.12116558733931));
#11996=CARTESIAN_POINT('Ctrl Pts',(2.59023089661888,2.6274200726489,8.12234763207773));
#11997=CARTESIAN_POINT('Ctrl Pts',(2.5967450034474,2.63203486937701,8.12284240796897));
#11998=CARTESIAN_POINT('Ctrl Pts',(2.60945017514427,2.64096489562136,8.12380820106755));
#11999=CARTESIAN_POINT('Ctrl Pts',(2.61563930681297,2.6452826235604,8.12427901506673));
#12000=CARTESIAN_POINT('Ctrl Pts',(2.63261176668727,2.65703472289611,8.12557093494879));
#12001=CARTESIAN_POINT('Ctrl Pts',(2.64342520256819,2.66442506055483,8.12639492415659));
#12002=CARTESIAN_POINT('Ctrl Pts',(2.68557725377455,2.69285805718569,8.12960941123526));
#12003=CARTESIAN_POINT('Ctrl Pts',(2.71723824940221,2.71341449249602,8.13202912134047));
#12004=CARTESIAN_POINT('Ctrl Pts',(2.9342345175239,2.84894484384315,8.14861014994374));
#12005=CARTESIAN_POINT('Ctrl Pts',(3.13045713424751,2.94539784774797,8.16354602207032));
#12006=CARTESIAN_POINT('Ctrl Pts',(3.46421289675029,3.06929472137217,8.18753027230061));
#12007=CARTESIAN_POINT('Ctrl Pts',(3.59648062561646,3.10894986088775,8.19671114121583));
#12008=CARTESIAN_POINT('Ctrl Pts',(3.80764083140854,3.15774347995749,8.21075221561559));
#12009=CARTESIAN_POINT('Ctrl Pts',(3.88501603441871,3.17265899957625,8.21577357468115));
#12010=CARTESIAN_POINT('Ctrl Pts',(3.98640183300925,3.18837287213575,8.22219696813252));
#12011=CARTESIAN_POINT('Ctrl Pts',(4.00997804591508,3.19175979595857,8.22367985372211));
#12012=CARTESIAN_POINT('Ctrl Pts',(4.04858499230612,3.19686985914933,8.22609098274487));
#12013=CARTESIAN_POINT('Ctrl Pts',(4.06359381253402,3.19874903091438,8.22702411003635));
#12014=CARTESIAN_POINT('Ctrl Pts',(4.09266808050719,3.20218153814956,8.22882373855212));
#12015=CARTESIAN_POINT('Ctrl Pts',(4.10673159485959,3.20374803516124,8.22969063431562));
#12016=CARTESIAN_POINT('Ctrl Pts',(4.13927872823666,3.20715650421183,8.23168877857485));
#12017=CARTESIAN_POINT('Ctrl Pts',(4.1577689783552,3.20893141627922,8.23281789943001));
#12018=CARTESIAN_POINT('Ctrl Pts',(4.21793631374609,3.21418242347375,8.23647324008585));
#12019=CARTESIAN_POINT('Ctrl Pts',(4.25966696016786,3.21700725859855,8.23897911424938));
#12020=CARTESIAN_POINT('Ctrl Pts',(4.50190175096816,3.22867320150942,8.25337507169849));
#12021=CARTESIAN_POINT('Ctrl Pts',(4.70283233463573,3.21958265723146,8.26468506574211));
#12022=CARTESIAN_POINT('Ctrl Pts',(5.11079804496556,3.16268445186581,8.28773024144073));
#12023=CARTESIAN_POINT('Ctrl Pts',(5.31656451498272,3.11302629196946,8.29941041425671));
#12024=CARTESIAN_POINT('Ctrl Pts',(5.54696446468353,3.03282290172023,8.31396256820595));
#12025=CARTESIAN_POINT('Ctrl Pts',(5.57779452658766,3.02155986071374,8.31594218524855));
#12026=CARTESIAN_POINT('Ctrl Pts',(5.61966022357567,3.00553625378433,8.31868178756917));
#12027=CARTESIAN_POINT('Ctrl Pts',(5.63085035083276,3.00118150568075,8.31941911094992));
#12028=CARTESIAN_POINT('Ctrl Pts',(5.64959024471379,2.99376783750807,8.32066282950014));
#12029=CARTESIAN_POINT('Ctrl Pts',(5.65715335538297,2.99074259131064,8.32116723011931));
#12030=CARTESIAN_POINT('Ctrl Pts',(5.6715163033913,2.98493414579692,8.32212995161071));
#12031=CARTESIAN_POINT('Ctrl Pts',(5.67831823436919,2.98215630904535,8.32258793389401));
#12032=CARTESIAN_POINT('Ctrl Pts',(5.69445694871588,2.97550094534822,8.32367937508729));
#12033=CARTESIAN_POINT('Ctrl Pts',(5.70378503718952,2.97160272174388,8.32431405417834));
#12034=CARTESIAN_POINT('Ctrl Pts',(5.73666564368688,2.95767976753859,8.32656440058392));
#12035=CARTESIAN_POINT('Ctrl Pts',(5.76011621206759,2.94741868593203,8.32819329414516));
#12036=CARTESIAN_POINT('Ctrl Pts',(5.97573646161604,2.84999486250812,8.34337631647785));
#12037=CARTESIAN_POINT('Ctrl Pts',(6.15901774324404,2.74444139178069,8.35776824686605));
#12038=CARTESIAN_POINT('Ctrl Pts',(6.5143542283234,2.49042519431466,8.38727555731693));
#12039=CARTESIAN_POINT('Ctrl Pts',(6.68377496669091,2.3401394133331,8.40227131845801));
#12040=CARTESIAN_POINT('Ctrl Pts',(6.85747211421996,2.14995478200649,8.41850437641143));
#12041=CARTESIAN_POINT('Ctrl Pts',(6.87848903416943,2.12625035985636,8.42048632743801));
#12042=CARTESIAN_POINT('Ctrl Pts',(6.91012524069904,2.08949085486792,8.42349831389009));
#12043=CARTESIAN_POINT('Ctrl Pts',(6.92099701478286,2.07665660712555,8.42453874523332));
#12044=CARTESIAN_POINT('Ctrl Pts',(6.94060418750484,2.05313927056341,8.42642523986893));
#12045=CARTESIAN_POINT('Ctrl Pts',(6.94937234057136,2.04248413456387,8.42727262684278));
#12046=CARTESIAN_POINT('Ctrl Pts',(6.96835372211582,2.01911347263982,8.42911551416144));
#12047=CARTESIAN_POINT('Ctrl Pts',(6.97853944706148,2.00637602410008,8.43010989376353));
#12048=CARTESIAN_POINT('Ctrl Pts',(7.00623826510674,1.97119385912471,8.43282953838485));
#12049=CARTESIAN_POINT('Ctrl Pts',(7.02355159699357,1.9485932253829,8.43454688414816));
#12050=CARTESIAN_POINT('Ctrl Pts',(7.11876933368087,1.82082501074837,8.44409646428369));
#12051=CARTESIAN_POINT('Ctrl Pts',(7.1905151353312,1.71121134777246,8.45168749756149));
#12052=CARTESIAN_POINT('Ctrl Pts',(7.36420963234959,1.40689148490349,8.47162362218473));
#12053=CARTESIAN_POINT('Ctrl Pts',(7.45325094019838,1.20564944144229,8.48362897184219));
#12054=CARTESIAN_POINT('Ctrl Pts',(7.54309826241073,0.929447941818175,8.50020645125321));
#12055=CARTESIAN_POINT('Ctrl Pts',(7.56281332800213,0.861264970790674,8.504310451108));
#12056=CARTESIAN_POINT('Ctrl Pts',(7.58715373160293,0.765321537309864,8.51017070011551));
#12057=CARTESIAN_POINT('Ctrl Pts',(7.59369160941581,0.738063774908442,8.51184510428537));
#12058=CARTESIAN_POINT('Ctrl Pts',(7.60449467943694,0.690283827154938,8.51480219077887));
#12059=CARTESIAN_POINT('Ctrl Pts',(7.60891683439086,0.66979850714309,8.51607704978918));
#12060=CARTESIAN_POINT('Ctrl Pts',(7.61516187107677,0.639436018637407,8.51797892254679));
#12061=CARTESIAN_POINT('Ctrl Pts',(7.61713897306658,0.629590653664814,8.51859753561515));
#12062=CARTESIAN_POINT('Ctrl Pts',(7.62057693334679,0.61204626401379,8.51970355782792));
#12063=CARTESIAN_POINT('Ctrl Pts',(7.62205576479485,0.604350954379263,8.52018994162952));
#12064=CARTESIAN_POINT('Ctrl Pts',(7.62521206953694,0.58759719240185,8.52125166951141));
#12065=CARTESIAN_POINT('Ctrl Pts',(7.62687874837235,0.578537055053457,8.5218275876985));
#12066=CARTESIAN_POINT('Ctrl Pts',(7.63140984296587,0.553298147141996,8.52343657092831));
#12067=CARTESIAN_POINT('Ctrl Pts',(7.63418936528196,0.537104691961789,8.52447420680797));
#12068=CARTESIAN_POINT('Ctrl Pts',(7.64896042166707,0.446917874928872,8.53027994021497));
#12069=CARTESIAN_POINT('Ctrl Pts',(7.65849043901687,0.372550488443372,8.53516703147698));
#12070=CARTESIAN_POINT('Ctrl Pts',(7.66699191607319,0.280981187684177,8.54125397867788));
#12071=CARTESIAN_POINT('Ctrl Pts',(7.66843079228126,0.26402509759489,8.54238404061981));
#12072=CARTESIAN_POINT('Ctrl Pts',(7.67598553012433,0.165767519409022,8.54894685044929));
#12073=CARTESIAN_POINT('Ctrl Pts',(7.67914849102628,0.0842710249388068,
8.55444595359864));
#12074=CARTESIAN_POINT('Ctrl Pts',(7.67921871651019,0.0018301419827333,
8.56002040187424));
#12075=CARTESIAN_POINT('Ctrl Pts',(7.67921910621818,0.000915065319246332,
8.5600822786385));
#12076=CARTESIAN_POINT('Ctrl Pts',(7.67921910621823,1.63241365473312E-10,
8.56014415614755));
#12077=CARTESIAN_POINT('Ctrl Pts',(7.67921910621823,-4.32286151319516E-11,
8.31612808864259));
#12078=CARTESIAN_POINT('Ctrl Pts',(7.67921910622028,0.152894774448002,8.30592674797713));
#12079=CARTESIAN_POINT('Ctrl Pts',(7.6683387014842,0.305598992240482,8.29551152918883));
#12080=CARTESIAN_POINT('Ctrl Pts',(7.6272739193954,0.592287328368467,8.27600540816731));
#12081=CARTESIAN_POINT('Ctrl Pts',(7.59929648326779,0.726257753529316,8.26690949802179));
#12082=CARTESIAN_POINT('Ctrl Pts',(7.54203676515252,0.933554726933015,8.25297924861768));
#12083=CARTESIAN_POINT('Ctrl Pts',(7.51843640605665,1.00827087518957,8.24798693863413));
#12084=CARTESIAN_POINT('Ctrl Pts',(7.48415433602558,1.10444768529297,8.24159465152635));
#12085=CARTESIAN_POINT('Ctrl Pts',(7.4759260392699,1.12674860479593,8.24011479010671));
#12086=CARTESIAN_POINT('Ctrl Pts',(7.46206317765897,1.1630779327418,8.23770738401184));
#12087=CARTESIAN_POINT('Ctrl Pts',(7.45657542378966,1.17716103214207,8.23677498330327));
#12088=CARTESIAN_POINT('Ctrl Pts',(7.44575760007654,1.20435549483327,8.23497594434296));
#12089=CARTESIAN_POINT('Ctrl Pts',(7.44043984567187,1.21747135227674,8.23410891757477));
#12090=CARTESIAN_POINT('Ctrl Pts',(7.4279349260634,1.24773967039451,8.23210930921201));
#12091=CARTESIAN_POINT('Ctrl Pts',(7.42068530394154,1.26486590561796,8.23097886625832));
#12092=CARTESIAN_POINT('Ctrl Pts',(7.39659943288182,1.32042090748783,8.22731422220286));
#12093=CARTESIAN_POINT('Ctrl Pts',(7.3791605492576,1.35858480921884,8.22480051620933));
#12094=CARTESIAN_POINT('Ctrl Pts',(7.27274319629282,1.57993308830166,8.2102227037136));
#12095=CARTESIAN_POINT('Ctrl Pts',(7.1673059260598,1.75469793342222,8.19875771206775));
#12096=CARTESIAN_POINT('Ctrl Pts',(6.95438750816694,2.04211719908581,8.17874959744835));
#12097=CARTESIAN_POINT('Ctrl Pts',(6.85395957507722,2.15913700917035,8.17018921603032));
#12098=CARTESIAN_POINT('Ctrl Pts',(6.70845988300255,2.30595594055005,8.15824427225181));
#12099=CARTESIAN_POINT('Ctrl Pts',(6.6704504084308,2.34247336420976,8.15515993018695));
#12100=CARTESIAN_POINT('Ctrl Pts',(6.6146693449649,2.39349400703087,8.15065443385224));
#12101=CARTESIAN_POINT('Ctrl Pts',(6.59761017182726,2.4087666361266,8.14927923258981));
#12102=CARTESIAN_POINT('Ctrl Pts',(6.5707670866307,2.43228808361965,8.1471167813232));
#12103=CARTESIAN_POINT('Ctrl Pts',(6.56109399440802,2.44066288939511,8.14633781778985));
#12104=CARTESIAN_POINT('Ctrl Pts',(6.54311147480594,2.4560454679067,8.14488968315624));
#12105=CARTESIAN_POINT('Ctrl Pts',(6.53481592518202,2.46306926557597,8.14422163290536));
#12106=CARTESIAN_POINT('Ctrl Pts',(6.52040969160513,2.475142350857,8.14306114787766));
#12107=CARTESIAN_POINT('Ctrl Pts',(6.51431552608102,2.48021138365959,8.14257013286076));
#12108=CARTESIAN_POINT('Ctrl Pts',(6.50249414975144,2.4899706589433,8.14161733695782));
#12109=CARTESIAN_POINT('Ctrl Pts',(6.49676939396589,2.49466372370422,8.14115578426719));
#12110=CARTESIAN_POINT('Ctrl Pts',(6.48302091996156,2.50585552717981,8.14004709731872));
#12111=CARTESIAN_POINT('Ctrl Pts',(6.47498209743747,2.51233546214467,8.1393986545137));
#12112=CARTESIAN_POINT('Ctrl Pts',(6.44583006920326,2.53560410015474,8.13704689884219));
#12113=CARTESIAN_POINT('Ctrl Pts',(6.42453808279569,2.55216566599599,8.13532878378228));
#12114=CARTESIAN_POINT('Ctrl Pts',(6.27208697801919,2.66770471378783,8.12303870143831));
#12115=CARTESIAN_POINT('Ctrl Pts',(6.13374605277013,2.75678226366342,8.11195887552769));
#12116=CARTESIAN_POINT('Ctrl Pts',(5.8497801566302,2.91031511352275,8.09012365574392));
#12117=CARTESIAN_POINT('Ctrl Pts',(5.7049431817029,2.9753267497044,8.07940108838415));
#12118=CARTESIAN_POINT('Ctrl Pts',(5.44322473042737,3.07030928418576,8.06104957621094));
#12119=CARTESIAN_POINT('Ctrl Pts',(5.32834455960816,3.10488724798534,8.05331454530127));
#12120=CARTESIAN_POINT('Ctrl Pts',(5.18543114207754,3.13934184155351,8.04408339348481));
#12121=CARTESIAN_POINT('Ctrl Pts',(5.15899048265322,3.14536430890173,8.04239134876867));
#12122=CARTESIAN_POINT('Ctrl Pts',(5.11698346033278,3.15437623401253,8.03972749817557));
#12123=CARTESIAN_POINT('Ctrl Pts',(5.10146610631022,3.15758571093394,8.03874870381919));
#12124=CARTESIAN_POINT('Ctrl Pts',(5.072225475103,3.16340904581196,8.03691389956197));
#12125=CARTESIAN_POINT('Ctrl Pts',(5.05850770076668,3.16604836307615,8.03605709713987));
#12126=CARTESIAN_POINT('Ctrl Pts',(5.02758159219517,3.17179031847486,8.03413419705184));
#12127=CARTESIAN_POINT('Ctrl Pts',(5.01036420957287,3.17484228415048,8.03306973028545));
#12128=CARTESIAN_POINT('Ctrl Pts',(4.96618270092223,3.18230357902081,8.03035320643503));
#12129=CARTESIAN_POINT('Ctrl Pts',(4.939185466422,3.18651047422589,8.02870754946587));
#12130=CARTESIAN_POINT('Ctrl Pts',(4.70087441575128,3.22054748427962,8.01429858010636));
#12131=CARTESIAN_POINT('Ctrl Pts',(4.48712808632995,3.22966504285192,8.00223656807286));
#12132=CARTESIAN_POINT('Ctrl Pts',(4.10348530604978,3.20791170107139,7.98073046126447));
#12133=CARTESIAN_POINT('Ctrl Pts',(3.93399610626441,3.18469916452879,7.97126329965214));
#12134=CARTESIAN_POINT('Ctrl Pts',(3.72058703479672,3.13797195970881,7.95858633430621));
#12135=CARTESIAN_POINT('Ctrl Pts',(3.67424988293245,3.12674320585354,7.95578607917916));
#12136=CARTESIAN_POINT('Ctrl Pts',(3.59787452101686,3.1064314512102,7.95106567799243));
#12137=CARTESIAN_POINT('Ctrl Pts',(3.56768833987926,3.09792989033976,7.94917246547854));
#12138=CARTESIAN_POINT('Ctrl Pts',(3.52632540868807,3.08562626099909,7.94653413009217));
#12139=CARTESIAN_POINT('Ctrl Pts',(3.51503724998766,3.08220096208138,7.94580955543328));
#12140=CARTESIAN_POINT('Ctrl Pts',(3.49602794043152,3.07631857596444,7.94458126721166));
#12141=CARTESIAN_POINT('Ctrl Pts',(3.48829665050208,3.07389416015902,7.94407943867261));
#12142=CARTESIAN_POINT('Ctrl Pts',(3.47353393773413,3.06920357631316,7.94311672195272));
#12143=CARTESIAN_POINT('Ctrl Pts',(3.4665010388713,3.06694234724588,7.94265614161233));
#12144=CARTESIAN_POINT('Ctrl Pts',(3.44779319335072,3.06085631805267,7.9414259060653));
#12145=CARTESIAN_POINT('Ctrl Pts',(3.43613237391788,3.05698894964509,7.94065381460934));
#12146=CARTESIAN_POINT('Ctrl Pts',(3.39402305271583,3.04275541544234,7.93784727361805));
#12147=CARTESIAN_POINT('Ctrl Pts',(3.36370915505603,3.03200060045672,7.93579200578562));
#12148=CARTESIAN_POINT('Ctrl Pts',(3.01051345801012,2.90070873838357,7.91147604308592));
#12149=CARTESIAN_POINT('Ctrl Pts',(2.70880247699491,2.72958178960875,7.8873621280405));
#12150=CARTESIAN_POINT('Ctrl Pts',(2.39089588386221,2.47456491838673,7.86076337936925));
#12151=CARTESIAN_POINT('Ctrl Pts',(2.34304904065818,2.43382841231113,7.8567120042757));
#12152=CARTESIAN_POINT('Ctrl Pts',(2.26291194355601,2.36145363289537,7.84984302497023));
#12153=CARTESIAN_POINT('Ctrl Pts',(2.23004130218746,2.3304883289731,7.84699966567669));
#12154=CARTESIAN_POINT('Ctrl Pts',(2.18402482035561,2.28527659908884,7.84297963478266));
#12155=CARTESIAN_POINT('Ctrl Pts',(2.17034103651119,2.27158769185718,7.84177900504115));
#12156=CARTESIAN_POINT('Ctrl Pts',(2.14681666123005,2.24762662576877,7.83970552878154));
#12157=CARTESIAN_POINT('Ctrl Pts',(2.13691933887628,2.23741117201143,7.83883020218593));
#12158=CARTESIAN_POINT('Ctrl Pts',(2.11675196397681,2.21631790107348,7.83704029090279));
#12159=CARTESIAN_POINT('Ctrl Pts',(2.10648936097224,2.2054334161559,7.83612603975568));
#12160=CARTESIAN_POINT('Ctrl Pts',(2.08060539129778,2.17759514147273,7.83381110847673));
#12161=CARTESIAN_POINT('Ctrl Pts',(2.06508929793362,2.16054429412465,7.83241492081288));
#12162=CARTESIAN_POINT('Ctrl Pts',(2.00618139749804,2.0943974695644,7.82707921742073));
#12163=CARTESIAN_POINT('Ctrl Pts',(1.96410594502064,2.04414710025331,7.82319413091853));
#12164=CARTESIAN_POINT('Ctrl Pts',(1.71685983785065,1.72986920957065,7.79980321937745));
#12165=CARTESIAN_POINT('Ctrl Pts',(1.55230942071272,1.43656660179051,7.78199074100371));
#12166=CARTESIAN_POINT('Ctrl Pts',(1.41949591364359,1.07939759052762,7.7598613866478));
#12167=CARTESIAN_POINT('Ctrl Pts',(1.40415087593605,1.03520931207224,7.75711219847908));
#12168=CARTESIAN_POINT('Ctrl Pts',(1.38026803102447,0.961280735814901,7.75246992716725));
#12169=CARTESIAN_POINT('Ctrl Pts',(1.37118679470257,0.931722386840167,7.75060265233535));
#12170=CARTESIAN_POINT('Ctrl Pts',(1.35924892011026,0.890776244890207,7.74799477134266));
#12171=CARTESIAN_POINT('Ctrl Pts',(1.3560267805261,0.879495636640035,7.74727409880327));
#12172=CARTESIAN_POINT('Ctrl Pts',(1.35068700399735,0.86040719462833,7.7460505038462));
#12173=CARTESIAN_POINT('Ctrl Pts',(1.34853700450162,0.852608383955271,7.74554943316304));
#12174=CARTESIAN_POINT('Ctrl Pts',(1.34447629307104,0.837659280509856,7.74458660697104));
#12175=CARTESIAN_POINT('Ctrl Pts',(1.34256081524545,0.830510380490131,7.74412514953906));
#12176=CARTESIAN_POINT('Ctrl Pts',(1.33803347506568,0.813377695398469,7.74301691408169));
#12177=CARTESIAN_POINT('Ctrl Pts',(1.33544492848741,0.803387911429119,7.74236882982181));
#12178=CARTESIAN_POINT('Ctrl Pts',(1.32627397301453,0.767281815049695,7.74002007194676));
#12179=CARTESIAN_POINT('Ctrl Pts',(1.31997124311823,0.741096485203178,7.73830464541641));
#12180=CARTESIAN_POINT('Ctrl Pts',(1.27651707821088,0.550068861059934,7.72571811881177));
#12181=CARTESIAN_POINT('Ctrl Pts',(1.25205672688252,0.38262409411107,7.71431011086639));
#12182=CARTESIAN_POINT('Ctrl Pts',(1.23093908259382,0.0653811834219913,
7.69280154349986));
#12183=CARTESIAN_POINT('Ctrl Pts',(1.23136434704622,-0.0838073757847299,
7.68272999060841));
#12184=CARTESIAN_POINT('Ctrl Pts',(1.2510776512479,-0.356419311215628,7.66468579819657));
#12185=CARTESIAN_POINT('Ctrl Pts',(1.26720923235708,-0.479788574623397,
7.65665459465783));
#12186=CARTESIAN_POINT('Ctrl Pts',(1.2955451970621,-0.62883011445333,7.64712597316299));
#12187=CARTESIAN_POINT('Ctrl Pts',(1.30100198708793,-0.655663485905089,
7.64541712858252));
#12188=CARTESIAN_POINT('Ctrl Pts',(1.3101677163521,-0.697967069935794,7.64273301119939));
#12189=CARTESIAN_POINT('Ctrl Pts',(1.31365024797686,-0.713484481510536,
7.64175056816355));
#12190=CARTESIAN_POINT('Ctrl Pts',(1.32040566715821,-0.742575653386324,
7.6399125198569));
#12191=CARTESIAN_POINT('Ctrl Pts',(1.32365216819928,-0.756155101401115,
7.63905609256234));
#12192=CARTESIAN_POINT('Ctrl Pts',(1.33114260867385,-0.786609562489644,
7.63713869280799));
#12193=CARTESIAN_POINT('Ctrl Pts',(1.33543519358248,-0.803472248869386,
7.63607931089189));
#12194=CARTESIAN_POINT('Ctrl Pts',(1.34674681179853,-0.846449040028402,
7.63338468513084));
#12195=CARTESIAN_POINT('Ctrl Pts',(1.35395840339334,-0.872511393424122,
7.63175566390866));
#12196=CARTESIAN_POINT('Ctrl Pts',(1.40606210577076,-1.05199162360801,7.62056647556314));
#12197=CARTESIAN_POINT('Ctrl Pts',(1.46198871831191,-1.20198407748167,7.61137922158509));
#12198=CARTESIAN_POINT('Ctrl Pts',(1.61904192398505,-1.54327609479098,7.59017688995366));
#12199=CARTESIAN_POINT('Ctrl Pts',(1.72871845227857,-1.72975677040328,7.57836374178375));
#12200=CARTESIAN_POINT('Ctrl Pts',(1.88766714357632,-1.94684663133831,7.56282226068313));
#12201=CARTESIAN_POINT('Ctrl Pts',(1.92019644161005,-1.98903888688763,7.55970599223822));
#12202=CARTESIAN_POINT('Ctrl Pts',(1.97518321488984,-2.05681665238036,7.55450543614644));
#12203=CARTESIAN_POINT('Ctrl Pts',(1.99702770382565,-2.08288794567341,7.55245559214156));
#12204=CARTESIAN_POINT('Ctrl Pts',(2.02724406608525,-2.11781289031882,7.5496340212833));
#12205=CARTESIAN_POINT('Ctrl Pts',(2.03526037977817,-2.12697297256629,7.54888675112303));
#12206=CARTESIAN_POINT('Ctrl Pts',(2.04874955188261,-2.1422117098308,7.54763100784953));
#12207=CARTESIAN_POINT('Ctrl Pts',(2.05419409770233,-2.14831544302794,7.54712461634422));
#12208=CARTESIAN_POINT('Ctrl Pts',(2.06455321605354,-2.15984015072397,7.54616183730286));
#12209=CARTESIAN_POINT('Ctrl Pts',(2.06946312898463,-2.1652652411245,7.54570581157442));
#12210=CARTESIAN_POINT('Ctrl Pts',(2.0811213403259,-2.17805885801383,7.54462382834226));
#12211=CARTESIAN_POINT('Ctrl Pts',(2.0878854704134,-2.18541276465219,7.54399669834043));
#12212=CARTESIAN_POINT('Ctrl Pts',(2.11162699873649,-2.21098466382968,7.54179812622171));
#12213=CARTESIAN_POINT('Ctrl Pts',(2.12878077822029,-2.22903670955622,7.54021421677398));
#12214=CARTESIAN_POINT('Ctrl Pts',(2.30180286110789,-2.406944018976,7.52429980588636));
#12215=CARTESIAN_POINT('Ctrl Pts',(2.47366310376377,-2.55037895359194,7.50902976931343));
#12216=CARTESIAN_POINT('Ctrl Pts',(2.78052681236518,-2.7565903635249,7.48408255841565));
#12217=CARTESIAN_POINT('Ctrl Pts',(2.9075419699288,-2.82991267755118,7.47430532702304));
#12218=CARTESIAN_POINT('Ctrl Pts',(3.11256812964798,-2.93031338644525,7.45949384584328));
#12219=CARTESIAN_POINT('Ctrl Pts',(3.18736650189891,-2.96347547386831,7.45427515007964));
#12220=CARTESIAN_POINT('Ctrl Pts',(3.28575893153008,-3.00268831142673,7.44764186331407));
#12221=CARTESIAN_POINT('Ctrl Pts',(3.30826649823546,-3.01136683758988,7.44613969303666));
#12222=CARTESIAN_POINT('Ctrl Pts',(3.3451039708181,-3.02509766077058,7.44370531847486));
#12223=CARTESIAN_POINT('Ctrl Pts',(3.35937558334564,-3.03030264760154,7.44276804795086));
#12224=CARTESIAN_POINT('Ctrl Pts',(3.38698557456558,-3.04015164001144,7.44096587847708));
#12225=CARTESIAN_POINT('Ctrl Pts',(3.40031869737615,-3.04480924569405,7.44010054506261));
#12226=CARTESIAN_POINT('Ctrl Pts',(3.43110378217191,-3.05533672780294,7.43811372720588));
#12227=CARTESIAN_POINT('Ctrl Pts',(3.44857639593675,-3.06114502668276,7.43699429423566));
#12228=CARTESIAN_POINT('Ctrl Pts',(3.50502868465343,-3.07937531491875,7.43340316061855));
#12229=CARTESIAN_POINT('Ctrl Pts',(3.54419635048831,-3.09120524265147,7.43095080365681));
#12230=CARTESIAN_POINT('Ctrl Pts',(3.81365964326605,-3.1670240162034,7.41432395756224));
#12231=CARTESIAN_POINT('Ctrl Pts',(4.05022885863677,-3.20596765644971,7.40101379923618));
#12232=CARTESIAN_POINT('Ctrl Pts',(4.42608717966414,-3.22553128210508,7.37995976634447));
#12233=CARTESIAN_POINT('Ctrl Pts',(4.56353067942897,-3.22389631315354,7.37226130702679));
#12234=CARTESIAN_POINT('Ctrl Pts',(4.74267964850517,-3.21029525195857,7.36178605549637));
#12235=CARTESIAN_POINT('Ctrl Pts',(4.7848505594209,-3.20625597353815,7.35928762822203));
#12236=CARTESIAN_POINT('Ctrl Pts',(4.8554629321712,-3.19808484234549,7.35503132067655));
#12237=CARTESIAN_POINT('Ctrl Pts',(4.88395173418012,-3.19440154096533,7.35329408067575));
#12238=CARTESIAN_POINT('Ctrl Pts',(4.92366873938594,-3.18872575756332,7.35083939479156));
#12239=CARTESIAN_POINT('Ctrl Pts',(4.93494229071351,-3.18705363255897,7.35013894072391));
#12240=CARTESIAN_POINT('Ctrl Pts',(4.95413933561673,-3.18410212180901,7.34893950892251));
#12241=CARTESIAN_POINT('Ctrl Pts',(4.96206748666253,-3.18285284858524,7.34844221269011));
#12242=CARTESIAN_POINT('Ctrl Pts',(4.97737460761431,-3.18038220360127,7.34747817740011));
#12243=CARTESIAN_POINT('Ctrl Pts',(4.98475408340319,-3.17916474605474,7.34701168332264));
#12244=CARTESIAN_POINT('Ctrl Pts',(5.00471091697265,-3.17580088756422,7.34574552855238));
#12245=CARTESIAN_POINT('Ctrl Pts',(5.01727971856154,-3.17360548979258,7.34494317402932));
#12246=CARTESIAN_POINT('Ctrl Pts',(5.06460240635232,-3.16504972200412,7.3419044803148));
#12247=CARTESIAN_POINT('Ctrl Pts',(5.09926256045062,-3.15819286776999,7.33964272835365));
#12248=CARTESIAN_POINT('Ctrl Pts',(5.46692456952255,-3.07915521389287,7.31531447524016));
#12249=CARTESIAN_POINT('Ctrl Pts',(5.78659909684695,-2.95516948877348,7.29149814442993));
#12250=CARTESIAN_POINT('Ctrl Pts',(6.13506398475503,-2.75179263825539,7.26516849734931));
#12251=CARTESIAN_POINT('Ctrl Pts',(6.18824889739357,-2.71863625382783,7.26112816460795));
#12252=CARTESIAN_POINT('Ctrl Pts',(6.27796414239646,-2.65900431523359,7.25427587552249));
#12253=CARTESIAN_POINT('Ctrl Pts',(6.31496621374648,-2.63327494698932,7.25143832987609));
#12254=CARTESIAN_POINT('Ctrl Pts',(6.36706105545717,-2.59540555160179,7.247424972149));
#12255=CARTESIAN_POINT('Ctrl Pts',(6.38260163068106,-2.58389339914262,7.24622531066522));
#12256=CARTESIAN_POINT('Ctrl Pts',(6.40938819663329,-2.56367447575151,7.24415296493719));
#12257=CARTESIAN_POINT('Ctrl Pts',(6.42068179091017,-2.55503196280005,7.24327780812886));
#12258=CARTESIAN_POINT('Ctrl Pts',(6.4437414798932,-2.53714209511834,7.24148775973954));
#12259=CARTESIAN_POINT('Ctrl Pts',(6.45550112494956,-2.5278869630461,7.24057320501637));
#12260=CARTESIAN_POINT('Ctrl Pts',(6.48523023529931,-2.5041522269333,7.23825653430463));
#12261=CARTESIAN_POINT('Ctrl Pts',(6.50310961532524,-2.48956075712994,7.23685892454179));
#12262=CARTESIAN_POINT('Ctrl Pts',(6.57128501873422,-2.43269153521718,7.23151096617996));
#12263=CARTESIAN_POINT('Ctrl Pts',(6.62044243041523,-2.38906985816482,7.22761537674616));
#12264=CARTESIAN_POINT('Ctrl Pts',(6.91125386096917,-2.11466117313467,7.20422891638768));
#12265=CARTESIAN_POINT('Ctrl Pts',(7.11709970765209,-1.84899042296554,7.1864273639643));
#12266=CARTESIAN_POINT('Ctrl Pts',(7.30102871677801,-1.51551481530063,7.16431105229617));
#12267=CARTESIAN_POINT('Ctrl Pts',(7.32271934705333,-1.47408061462171,7.16156234747799));
#12268=CARTESIAN_POINT('Ctrl Pts',(7.35723942624506,-1.40449457136165,7.15692081640959));
#12269=CARTESIAN_POINT('Ctrl Pts',(7.37057930062141,-1.3766027260209,7.1550537879378));
#12270=CARTESIAN_POINT('Ctrl Pts',(7.38842410289604,-1.33786960600319,7.15244619636444));
#12271=CARTESIAN_POINT('Ctrl Pts',(7.39327462216904,-1.32718820700389,7.15172556109115));
#12272=CARTESIAN_POINT('Ctrl Pts',(7.40137122225159,-1.30909683830656,7.15050201091301));
#12273=CARTESIAN_POINT('Ctrl Pts',(7.40464797542145,-1.3017005640678,7.15000094742551));
#12274=CARTESIAN_POINT('Ctrl Pts',(7.41086925895172,-1.28751391401718,7.14903812000192));
#12275=CARTESIAN_POINT('Ctrl Pts',(7.41381829595241,-1.2807256180091,7.14857665404869));
#12276=CARTESIAN_POINT('Ctrl Pts',(7.42082342557149,-1.26444752390577,7.14746837819304));
#12277=CARTESIAN_POINT('Ctrl Pts',(7.42485733866612,-1.25494835194159,7.1468202618492));
#12278=CARTESIAN_POINT('Ctrl Pts',(7.43925521269443,-1.22058600593344,7.14447123678265));
#12279=CARTESIAN_POINT('Ctrl Pts',(7.44935265233791,-1.1956132837017,7.1427555707597));
#12280=CARTESIAN_POINT('Ctrl Pts',(7.52007427991809,-1.01419490974086,7.13024559021496));
#12281=CARTESIAN_POINT('Ctrl Pts',(7.56870678481348,-0.853366255022636,
7.11892184163296));
#12282=CARTESIAN_POINT('Ctrl Pts',(7.63604262722976,-0.545924068564765,
7.09763134699031));
#12283=CARTESIAN_POINT('Ctrl Pts',(7.65763179825853,-0.400354411450338,
7.08769347469783));
#12284=CARTESIAN_POINT('Ctrl Pts',(7.67583711996911,-0.169912452741478,
7.07241736234439));
#12285=CARTESIAN_POINT('Ctrl Pts',(7.67917671221306,-0.0857802343074928,
7.06693207621422));
#12286=CARTESIAN_POINT('Ctrl Pts',(7.67921897253183,-0.00107186857600834,
7.06150815186532));
#12287=CARTESIAN_POINT('Ctrl Pts',(7.67921910621823,-0.000535933988464888,
7.06147383960103));
#12288=CARTESIAN_POINT('Ctrl Pts',(7.67921910621823,-4.71466720739905E-12,
7.06143953130409));
#12289=CARTESIAN_POINT('Origin',(4.45646910621825,-5.13094777615093E-16,
-2.31077344927308));
#12290=CARTESIAN_POINT('',(7.67921910621823,-9.10779638672584E-11,5.81337971654115));
#12291=CARTESIAN_POINT('',(7.67921910621823,3.83865910396161E-12,6.06327685380577));
#12292=CARTESIAN_POINT('',(7.67921910621823,-3.51191647465084E-13,-2.31077344927308));
#12293=CARTESIAN_POINT('',(7.6792176224508,0.00276905877516891,5.81322441567618));
#12294=CARTESIAN_POINT('Ctrl Pts',(7.67921910621823,-9.10779638672584E-11,
5.81337971654115));
#12295=CARTESIAN_POINT('Ctrl Pts',(7.67921910621826,0.000923861410410587,
5.81332772766874));
#12296=CARTESIAN_POINT('Ctrl Pts',(7.67921870895504,0.00184773084885948,
5.81327574292358));
#12297=CARTESIAN_POINT('Ctrl Pts',(7.67921791440811,0.00277160796994168,
5.81322376224255));
#12298=CARTESIAN_POINT('',(7.15082074185096,-1.76821571819255,4.67690209133339));
#12299=CARTESIAN_POINT('Ctrl Pts',(7.6792179166238,0.00276903041849574,
5.81322390726497));
#12300=CARTESIAN_POINT('Ctrl Pts',(7.67900856449745,0.246424467231695,5.79951496557771));
#12301=CARTESIAN_POINT('Ctrl Pts',(7.65116821843853,0.489250992218867,5.78622294437281));
#12302=CARTESIAN_POINT('Ctrl Pts',(7.58979339265802,0.754462998349227,5.77011732124514));
#12303=CARTESIAN_POINT('Ctrl Pts',(7.58297494971163,0.782238196207692,5.76840989669069));
#12304=CARTESIAN_POINT('Ctrl Pts',(7.57043845281463,0.830521272702615,5.76539972955178));
#12305=CARTESIAN_POINT('Ctrl Pts',(7.56488505924565,0.851070434140909,5.76410520256966));
#12306=CARTESIAN_POINT('Ctrl Pts',(7.5563959368466,0.881290709280791,5.76217956363626));
#12307=CARTESIAN_POINT('Ctrl Pts',(7.55361749252557,0.891005912594745,5.7615571591039));
#12308=CARTESIAN_POINT('Ctrl Pts',(7.54860210507242,0.908235958343354,5.76044709417541));
#12309=CARTESIAN_POINT('Ctrl Pts',(7.54638336986067,0.915755906412577,5.75996049006881));
#12310=CARTESIAN_POINT('Ctrl Pts',(7.54151146076358,0.932048944867181,5.75890151687508));
#12311=CARTESIAN_POINT('Ctrl Pts',(7.53884833932929,0.940818698452763,5.75832859813902));
#12312=CARTESIAN_POINT('Ctrl Pts',(7.53136695194085,0.965082421935289,5.75673559457842));
#12313=CARTESIAN_POINT('Ctrl Pts',(7.52646910105616,0.980551298451076,5.75571107863792));
#12314=CARTESIAN_POINT('Ctrl Pts',(7.49924541920163,1.06432809565836,5.75011639906219));
#12315=CARTESIAN_POINT('Ctrl Pts',(7.47475796773551,1.1319066359539,5.74543688440981));
#12316=CARTESIAN_POINT('Ctrl Pts',(7.4354466989433,1.23002261276611,5.73845045926817));
#12317=CARTESIAN_POINT('Ctrl Pts',(7.42236478590468,1.26123979768473,5.73619816128619));
#12318=CARTESIAN_POINT('Ctrl Pts',(7.34076793638534,1.44765996886942,5.72259124765988));
#12319=CARTESIAN_POINT('Ctrl Pts',(7.26057646519738,1.5974612293486,5.71101510603924));
#12320=CARTESIAN_POINT('Ctrl Pts',(7.10402919691497,1.84146781002633,5.69157265587832));
#12321=CARTESIAN_POINT('Ctrl Pts',(7.03347524038021,1.93897458849221,5.68361820729284));
#12322=CARTESIAN_POINT('Ctrl Pts',(6.91232519687503,2.08807317405674,5.67121251013103));
#12323=CARTESIAN_POINT('Ctrl Pts',(6.8651667275426,2.1423015200399,5.66664262983613));
#12324=CARTESIAN_POINT('Ctrl Pts',(6.80112192807073,2.21115646302847,5.66075875143344));
#12325=CARTESIAN_POINT('Ctrl Pts',(6.78584445918166,2.22724499405994,5.65937776061662));
#12326=CARTESIAN_POINT('Ctrl Pts',(6.76127645552357,2.2525879613569,5.6571920901708));
#12327=CARTESIAN_POINT('Ctrl Pts',(6.75209369110902,2.26194544903647,5.65638277993084));
#12328=CARTESIAN_POINT('Ctrl Pts',(6.73300848548805,2.28115785967703,5.65471625633208));
#12329=CARTESIAN_POINT('Ctrl Pts',(6.72309853924008,2.29100496490285,5.65385939928364));
#12330=CARTESIAN_POINT('Ctrl Pts',(6.700633240538,2.31303935285052,5.65193573423835));
#12331=CARTESIAN_POINT('Ctrl Pts',(6.68804197297036,2.32518951243891,5.65087056273352));
#12332=CARTESIAN_POINT('Ctrl Pts',(6.6555095972262,2.35607450474447,5.64815100026633));
#12333=CARTESIAN_POINT('Ctrl Pts',(6.63542748435271,2.37465926160609,5.64650303422928));
#12334=CARTESIAN_POINT('Ctrl Pts',(6.46129972570706,2.53173470703194,5.63246704371628));
#12335=CARTESIAN_POINT('Ctrl Pts',(6.29446373181011,2.65533758430647,5.6207355687472));
#12336=CARTESIAN_POINT('Ctrl Pts',(5.96619680930918,2.85267550021613,5.59928750437024));
#12337=CARTESIAN_POINT('Ctrl Pts',(5.80834629009445,2.93077714346589,5.58955710524609));
#12338=CARTESIAN_POINT('Ctrl Pts',(5.59995643053094,3.01345234605205,5.57655570021058));
#12339=CARTESIAN_POINT('Ctrl Pts',(5.55459130081789,3.03027811864658,5.57371544604752));
#12340=CARTESIAN_POINT('Ctrl Pts',(5.47890323341279,3.05642781959852,5.56893395573933));
#12341=CARTESIAN_POINT('Ctrl Pts',(5.4487896005746,3.06633697192618,5.56702055168781));
#12342=CARTESIAN_POINT('Ctrl Pts',(5.40722980152017,3.07933629201336,5.5643585313215));
#12343=CARTESIAN_POINT('Ctrl Pts',(5.39590438844032,3.08281028274428,5.56363094806922));
#12344=CARTESIAN_POINT('Ctrl Pts',(5.37679148198509,3.088557932028,5.56239903538514));
#12345=CARTESIAN_POINT('Ctrl Pts',(5.36901395099259,3.09086481087599,5.56189661674324));
#12346=CARTESIAN_POINT('Ctrl Pts',(5.35414715794404,3.09521341811359,5.56093395870326));
#12347=CARTESIAN_POINT('Ctrl Pts',(5.34705946440774,3.09726020856029,5.56047403457025));
#12348=CARTESIAN_POINT('Ctrl Pts',(5.32820147412363,3.10263595416122,5.5592478437888));
#12349=CARTESIAN_POINT('Ctrl Pts',(5.31641928224329,3.1059222251656,5.55847916943823));
#12350=CARTESIAN_POINT('Ctrl Pts',(5.27392728363824,3.11751371499186,5.55569845687809));
#12351=CARTESIAN_POINT('Ctrl Pts',(5.24311470579462,3.12543087565918,5.55366608487108));
#12352=CARTESIAN_POINT('Ctrl Pts',(4.87672696202815,3.21381168402107,5.52935134168323));
#12353=CARTESIAN_POINT('Ctrl Pts',(4.53043031056119,3.24033771928698,5.50520394945881));
#12354=CARTESIAN_POINT('Ctrl Pts',(4.12385546154255,3.20615574976477,5.47857501192268));
#12355=CARTESIAN_POINT('Ctrl Pts',(4.06139989117354,3.1990604380419,5.47452243970827));
#12356=CARTESIAN_POINT('Ctrl Pts',(3.95448316596778,3.18373480180905,5.46765165137932));
#12357=CARTESIAN_POINT('Ctrl Pts',(3.90991600046186,3.17638744600244,5.46480766217799));
#12358=CARTESIAN_POINT('Ctrl Pts',(3.84648795812378,3.16455608733335,5.46078690834855));
#12359=CARTESIAN_POINT('Ctrl Pts',(3.82749184868448,3.16083531153208,5.45958617378364));
#12360=CARTESIAN_POINT('Ctrl Pts',(3.79459690432893,3.15408387046255,5.45751257511264));
#12361=CARTESIAN_POINT('Ctrl Pts',(3.78068264301221,3.15113194582629,5.45663723011539));
#12362=CARTESIAN_POINT('Ctrl Pts',(3.75217596959817,3.14488672378497,5.45484733356307));
#12363=CARTESIAN_POINT('Ctrl Pts',(3.7375860145647,3.14158374711049,5.45393311518984));
#12364=CARTESIAN_POINT('Ctrl Pts',(3.7005740931552,3.13293338618671,5.45161837173749));
#12365=CARTESIAN_POINT('Ctrl Pts',(3.67818529136058,3.12744675716123,5.45022233764159));
#12366=CARTESIAN_POINT('Ctrl Pts',(3.59240842939892,3.10544798636379,5.44488795629383));
#12367=CARTESIAN_POINT('Ctrl Pts',(3.52946796365262,3.08724437142873,5.4410040027396));
#12368=CARTESIAN_POINT('Ctrl Pts',(3.14889632712346,2.96448573140725,5.41761261028515));
#12369=CARTESIAN_POINT('Ctrl Pts',(2.84863116048766,2.81295929817016,5.39979895291815));
#12370=CARTESIAN_POINT('Ctrl Pts',(2.53905500581176,2.5907197039378,5.37766819119971));
#12371=CARTESIAN_POINT('Ctrl Pts',(2.50165799437472,2.56261946095399,5.37491895093606));
#12372=CARTESIAN_POINT('Ctrl Pts',(2.44057681596239,2.51460772485839,5.37027659984267));
#12373=CARTESIAN_POINT('Ctrl Pts',(2.41654328533991,2.49515054074021,5.36840929845948));
#12374=CARTESIAN_POINT('Ctrl Pts',(2.38378329971818,2.46783888225906,5.3658013862751));
#12375=CARTESIAN_POINT('Ctrl Pts',(2.37481339281279,2.46027735879909,5.36508070971974));
#12376=CARTESIAN_POINT('Ctrl Pts',(2.35972841357764,2.44741935006658,5.36385710993688));
#12377=CARTESIAN_POINT('Ctrl Pts',(2.35359152472814,2.44214841538127,5.36335603847808));
#12378=CARTESIAN_POINT('Ctrl Pts',(2.34187828697669,2.4320111032381,5.36239321241617));
#12379=CARTESIAN_POINT('Ctrl Pts',(2.33629876087939,2.42714854164853,5.36193175590002));
#12380=CARTESIAN_POINT('Ctrl Pts',(2.32297961733642,2.41545992736965,5.36082352478989));
#12381=CARTESIAN_POINT('Ctrl Pts',(2.31525599725014,2.40861588367227,5.36017544398369));
#12382=CARTESIAN_POINT('Ctrl Pts',(2.28749405493776,2.38377644948445,5.35782671487045));
#12383=CARTESIAN_POINT('Ctrl Pts',(2.26764926382681,2.3655676954434,5.35611131412028));
#12384=CARTESIAN_POINT('Ctrl Pts',(2.12483700205699,2.23119353115142,5.34351300104494));
#12385=CARTESIAN_POINT('Ctrl Pts',(2.01096767671065,2.10576466517582,5.33209202841541));
#12386=CARTESIAN_POINT('Ctrl Pts',(1.81610134889612,1.85388136914968,5.31054840223347));
#12387=CARTESIAN_POINT('Ctrl Pts',(1.73303842616976,1.72955172535244,5.30045479072259));
#12388=CARTESIAN_POINT('Ctrl Pts',(1.59741556759932,1.49240283905983,5.2824223537282));
#12389=CARTESIAN_POINT('Ctrl Pts',(1.54217909739774,1.38143894524199,5.27442231367824));
#12390=CARTESIAN_POINT('Ctrl Pts',(1.48270287028835,1.24240901512131,5.2649249198695));
#12391=CARTESIAN_POINT('Ctrl Pts',(1.47226460153038,1.21712338533716,5.26321779805227));
#12392=CARTESIAN_POINT('Ctrl Pts',(1.45627085619532,1.17693701592555,5.26053575851637));
#12393=CARTESIAN_POINT('Ctrl Pts',(1.45050173426947,1.16212325170144,5.2595536892911));
#12394=CARTESIAN_POINT('Ctrl Pts',(1.43987185727296,1.13421935804556,5.25771597549725));
#12395=CARTESIAN_POINT('Ctrl Pts',(1.43498612362419,1.12113920193156,5.25685951191735));
#12396=CARTESIAN_POINT('Ctrl Pts',(1.42420018748514,1.09168027551467,5.25494155910723));
#12397=CARTESIAN_POINT('Ctrl Pts',(1.41834735073865,1.07528453761948,5.25388166449026));
#12398=CARTESIAN_POINT('Ctrl Pts',(1.4037341917408,1.03327624595637,5.2511848328358));
#12399=CARTESIAN_POINT('Ctrl Pts',(1.39516307214433,1.00759897354941,5.24955413619682));
#12400=CARTESIAN_POINT('Ctrl Pts',(1.3379427952436,0.828705336911774,5.23830944602236));
#12401=CARTESIAN_POINT('Ctrl Pts',(1.30049031183233,0.672135497194382,5.22907291227796));
#12402=CARTESIAN_POINT('Ctrl Pts',(1.24062592285557,0.301154980856729,5.20787029317528));
#12403=CARTESIAN_POINT('Ctrl Pts',(1.22770315884033,0.0860245480225275,
5.19609954522581));
#12404=CARTESIAN_POINT('Ctrl Pts',(1.23946508786304,-0.208099123167737,
5.17909551831905));
#12405=CARTESIAN_POINT('Ctrl Pts',(1.24556704783773,-0.287273149991707,
5.17442298293));
#12406=CARTESIAN_POINT('Ctrl Pts',(1.25641861233058,-0.382171381155469,
5.16862243665321));
#12407=CARTESIAN_POINT('Ctrl Pts',(1.25837291890157,-0.398194525142885,
5.16763613000343));
#12408=CARTESIAN_POINT('Ctrl Pts',(1.26161058041794,-0.423176630674345,
5.166086616547));
#12409=CARTESIAN_POINT('Ctrl Pts',(1.26281147575432,-0.43214626611738,5.16552790919859));
#12410=CARTESIAN_POINT('Ctrl Pts',(1.26512558519124,-0.448894009152649,
5.16448009107429));
#12411=CARTESIAN_POINT('Ctrl Pts',(1.26622947939416,-0.456673208434475,
5.16399150310423));
#12412=CARTESIAN_POINT('Ctrl Pts',(1.26881837561255,-0.474449716181971,
5.16287075105305));
#12413=CARTESIAN_POINT('Ctrl Pts',(1.27032196582853,-0.484444121464008,
5.16223756386857));
#12414=CARTESIAN_POINT('Ctrl Pts',(1.27445396453041,-0.511058038332236,
5.1605435694887));
#12415=CARTESIAN_POINT('Ctrl Pts',(1.27716552152691,-0.527664068159161,
5.1594783700627));
#12416=CARTESIAN_POINT('Ctrl Pts',(1.30224565933314,-0.674042475043102,
5.15002080423962));
#12417=CARTESIAN_POINT('Ctrl Pts',(1.3324166059841,-0.80233851284325,5.14126301938515));
#12418=CARTESIAN_POINT('Ctrl Pts',(1.42372747532276,-1.10586336698008,5.11992547912634));
#12419=CARTESIAN_POINT('Ctrl Pts',(1.49232008490354,-1.27839110651048,5.10729690797321));
#12420=CARTESIAN_POINT('Ctrl Pts',(1.61611270294635,-1.52537333360888,5.08897846802543));
#12421=CARTESIAN_POINT('Ctrl Pts',(1.66028908507281,-1.60491992273071,5.08303307195462));
#12422=CARTESIAN_POINT('Ctrl Pts',(1.72862508160112,-1.71656039342291,5.0746366721406));
#12423=CARTESIAN_POINT('Ctrl Pts',(1.75010755754954,-1.75023427033121,5.07209662052985));
#12424=CARTESIAN_POINT('Ctrl Pts',(1.78978051114918,-1.80994403080671,5.06757826239652));
#12425=CARTESIAN_POINT('Ctrl Pts',(1.80774006623573,-1.8361263699208,5.06559184665267));
#12426=CARTESIAN_POINT('Ctrl Pts',(1.83580985791605,-1.8757787758011,5.06257460105723));
#12427=CARTESIAN_POINT('Ctrl Pts',(1.84564324511415,-1.8894415184518,5.06153331771169));
#12428=CARTESIAN_POINT('Ctrl Pts',(1.86373091063091,-1.91416211148822,5.0596460231123));
#12429=CARTESIAN_POINT('Ctrl Pts',(1.87194996682861,-1.92524511879044,5.05879868121817));
#12430=CARTESIAN_POINT('Ctrl Pts',(1.89002946375878,-1.94930002937856,5.05695675340985));
#12431=CARTESIAN_POINT('Ctrl Pts',(1.89991765084662,-1.96225067567429,5.05596328139648));
#12432=CARTESIAN_POINT('Ctrl Pts',(1.92731267690875,-1.99757157418712,5.05324829395977));
#12433=CARTESIAN_POINT('Ctrl Pts',(1.94501797830594,-2.01978656003651,5.05153465353216));
#12434=CARTESIAN_POINT('Ctrl Pts',(2.04518419433832,-2.1421120176429,5.04205902452874));
#12435=CARTESIAN_POINT('Ctrl Pts',(2.13334101396892,-2.23741375370434,5.0345336028333));
#12436=CARTESIAN_POINT('Ctrl Pts',(2.38623112363911,-2.47968761399129,5.01460042258944));
#12437=CARTESIAN_POINT('Ctrl Pts',(2.56067592803624,-2.61547271564878,5.002542619857));
#12438=CARTESIAN_POINT('Ctrl Pts',(2.83684889586298,-2.78819416487964,4.98395315847202));
#12439=CARTESIAN_POINT('Ctrl Pts',(2.92876067783844,-2.83959479756779,4.97782989872249));
#12440=CARTESIAN_POINT('Ctrl Pts',(3.03849435149316,-2.89409122290364,4.97040074552768));
#12441=CARTESIAN_POINT('Ctrl Pts',(3.05403861451872,-2.90165557867087,4.9693456718687));
#12442=CARTESIAN_POINT('Ctrl Pts',(3.07803374309955,-2.9130945617444,4.96771171290074));
#12443=CARTESIAN_POINT('Ctrl Pts',(3.08644204644958,-2.91705842012141,4.96713815675236));
#12444=CARTESIAN_POINT('Ctrl Pts',(3.10196211357278,-2.92429301611773,4.96607745456314));
#12445=CARTESIAN_POINT('Ctrl Pts',(3.10906875151037,-2.92757427187282,4.96559096164928));
#12446=CARTESIAN_POINT('Ctrl Pts',(3.12521728770776,-2.93495907154992,4.96448370544755));
#12447=CARTESIAN_POINT('Ctrl Pts',(3.13426618886665,-2.93904671537241,4.96386200191928));
#12448=CARTESIAN_POINT('Ctrl Pts',(3.15782257184258,-2.94955699380067,4.96224060591144));
#12449=CARTESIAN_POINT('Ctrl Pts',(3.17235865360718,-2.9559143429365,4.96123718040098));
#12450=CARTESIAN_POINT('Ctrl Pts',(3.27188421095465,-2.99856914547841,4.9543501293015));
#12451=CARTESIAN_POINT('Ctrl Pts',(3.35834654757568,-3.03130035770005,4.94828474923369));
#12452=CARTESIAN_POINT('Ctrl Pts',(3.524419695971,-3.0861313056986,4.93662991481701));
#12453=CARTESIAN_POINT('Ctrl Pts',(3.60371473570473,-3.10897598635012,4.93106316396087));
#12454=CARTESIAN_POINT('Ctrl Pts',(3.81256386908113,-3.16055311967138,4.91651475170433));
#12455=CARTESIAN_POINT('Ctrl Pts',(3.94317824868259,-3.18437523488754,4.90753252958415));
#12456=CARTESIAN_POINT('Ctrl Pts',(4.17212957111309,-3.21167524374345,4.89219568324045));
#12457=CARTESIAN_POINT('Ctrl Pts',(4.26985011691826,-3.21883256511799,4.88577470503153));
#12458=CARTESIAN_POINT('Ctrl Pts',(4.40971127060308,-3.22268415016564,4.87678407014721));
#12459=CARTESIAN_POINT('Ctrl Pts',(4.4516899698963,-3.22301983372493,4.87411078362877));
#12460=CARTESIAN_POINT('Ctrl Pts',(4.52668170766121,-3.22215424995194,4.86937935350788));
#12461=CARTESIAN_POINT('Ctrl Pts',(4.55969168690786,-3.22126575262239,4.86731195122749));
#12462=CARTESIAN_POINT('Ctrl Pts',(4.60976263878109,-3.21914754007146,4.86419823131219));
#12463=CARTESIAN_POINT('Ctrl Pts',(4.6268363177046,-3.21828911428826,4.86314040189775));
#12464=CARTESIAN_POINT('Ctrl Pts',(4.65781965598681,-3.21648408354677,4.86122765054649));
#12465=CARTESIAN_POINT('Ctrl Pts',(4.67173144895827,-3.2155830011184,4.86037132715108));
#12466=CARTESIAN_POINT('Ctrl Pts',(4.70172346486876,-3.2134448722957,4.85853045769639));
#12467=CARTESIAN_POINT('Ctrl Pts',(4.71780118531136,-3.21217733117724,4.85754688970649));
#12468=CARTESIAN_POINT('Ctrl Pts',(4.76143809421167,-3.20840726999045,4.85488581599801));
#12469=CARTESIAN_POINT('Ctrl Pts',(4.78897604549433,-3.20567036692459,4.85321566820236));
#12470=CARTESIAN_POINT('Ctrl Pts',(4.93286645481124,-3.18949542228666,4.8445321855694));
#12471=CARTESIAN_POINT('Ctrl Pts',(5.04846445734408,-3.17007591575075,4.83770903264517));
#12472=CARTESIAN_POINT('Ctrl Pts',(5.38683259219747,-3.0940723463552,4.81788441951594));
#12473=CARTESIAN_POINT('Ctrl Pts',(5.60487242015871,-3.01993770381107,4.8053406301921));
#12474=CARTESIAN_POINT('Ctrl Pts',(5.91273802771762,-2.87705512169928,4.78600568126638));
#12475=CARTESIAN_POINT('Ctrl Pts',(6.00986424974131,-2.82579611135214,4.77963281334741));
#12476=CARTESIAN_POINT('Ctrl Pts',(6.11916369786089,-2.76077315318956,4.77192275847928));
#12477=CARTESIAN_POINT('Ctrl Pts',(6.13407875526853,-2.75173536933379,4.77085853245698));
#12478=CARTESIAN_POINT('Ctrl Pts',(6.15685771003802,-2.73767842783556,4.76921335427777));
#12479=CARTESIAN_POINT('Ctrl Pts',(6.16477465327649,-2.7327452737155,4.76863784638903));
#12480=CARTESIAN_POINT('Ctrl Pts',(6.17929353614584,-2.72361061537892,4.76757535314304));
#12481=CARTESIAN_POINT('Ctrl Pts',(6.18590169278284,-2.71941937279797,4.76708903763024));
#12482=CARTESIAN_POINT('Ctrl Pts',(6.20082610241681,-2.70987712340869,4.76598452049958));
#12483=CARTESIAN_POINT('Ctrl Pts',(6.20913297903031,-2.70451191474658,4.76536539879232));
#12484=CARTESIAN_POINT('Ctrl Pts',(6.23059018547676,-2.6905128571153,4.76375513378521));
#12485=CARTESIAN_POINT('Ctrl Pts',(6.24370205034098,-2.68182091470453,4.76276033895619));
#12486=CARTESIAN_POINT('Ctrl Pts',(6.33073835208014,-2.62320221766511,4.75608725411832));
#12487=CARTESIAN_POINT('Ctrl Pts',(6.40261971842986,-2.5703248582892,4.75023949808361));
#12488=CARTESIAN_POINT('Ctrl Pts',(6.53766763384786,-2.46206594209395,4.73871810019295));
#12489=CARTESIAN_POINT('Ctrl Pts',(6.60105071111069,-2.4070572959987,4.73305891556851));
#12490=CARTESIAN_POINT('Ctrl Pts',(6.80107096415059,-2.21928666995304,4.71450728585569));
#12491=CARTESIAN_POINT('Ctrl Pts',(6.92811460428226,-2.07686633212499,4.70161997360154));
#12492=CARTESIAN_POINT('Ctrl Pts',(7.07969194710109,-1.87318941970666,4.68503221910502));
#12493=CARTESIAN_POINT('Ctrl Pts',(7.11603373663308,-1.82122306534099,4.68093942591495));
#12494=CARTESIAN_POINT('Ctrl Pts',(7.15082074185096,-1.76821571819255,4.67690209133339));
#12495=CARTESIAN_POINT('',(7.49128385400174,-1.0844431793025,4.88098201673873));
#12496=CARTESIAN_POINT('Ctrl Pts',(7.15082074206232,-1.76821571787049,4.67690209167091));
#12497=CARTESIAN_POINT('Ctrl Pts',(7.25658458800507,-1.60705608760082,4.73783237965716));
#12498=CARTESIAN_POINT('Ctrl Pts',(7.34968713435654,-1.43333021245007,4.79384230980414));
#12499=CARTESIAN_POINT('Ctrl Pts',(7.4495156664105,-1.19638506817819,4.85508770712984));
#12500=CARTESIAN_POINT('Ctrl Pts',(7.47117036804548,-1.14073078200022,4.86847594001313));
#12501=CARTESIAN_POINT('Ctrl Pts',(7.49128387097725,-1.08444313179653,4.88098177561639));
#12502=CARTESIAN_POINT('Ctrl Pts',(7.49128385400174,-1.0844431793025,4.88098201673873));
#12503=CARTESIAN_POINT('Ctrl Pts',(7.48571404110737,-1.10003030330939,4.88193244700284));
#12504=CARTESIAN_POINT('Ctrl Pts',(7.48002363766192,-1.11557592977363,4.88288021106361));
#12505=CARTESIAN_POINT('Ctrl Pts',(7.43245320196961,-1.24249495035342,4.89061991409293));
#12506=CARTESIAN_POINT('Ctrl Pts',(7.3845538648513,-1.35151629996845,4.89727582348624));
#12507=CARTESIAN_POINT('Ctrl Pts',(7.28641881897214,-1.54502488880185,4.90940738558587));
#12508=CARTESIAN_POINT('Ctrl Pts',(7.23814284012053,-1.63033968458306,4.91487864608455));
#12509=CARTESIAN_POINT('Ctrl Pts',(7.12794689546593,-1.8058991226053,4.92664895678325));
#12510=CARTESIAN_POINT('Ctrl Pts',(7.06516983124947,-1.89545270042632,4.93296302842427));
#12511=CARTESIAN_POINT('Ctrl Pts',(6.98349610672583,-2.00020158726413,4.94095829133831));
#12512=CARTESIAN_POINT('Ctrl Pts',(6.96881702021602,-2.01860836630284,4.94238748798571));
#12513=CARTESIAN_POINT('Ctrl Pts',(6.94728574912995,-2.04500875282901,4.9444754461981));
#12514=CARTESIAN_POINT('Ctrl Pts',(6.94059360715719,-2.05313268065134,4.94512326244438));
#12515=CARTESIAN_POINT('Ctrl Pts',(6.92881731193899,-2.0672866567847,4.94626154400089));
#12516=CARTESIAN_POINT('Ctrl Pts',(6.92375064219131,-2.0733310378899,4.94675074869134));
#12517=CARTESIAN_POINT('Ctrl Pts',(6.91291530063083,-2.08616130198916,4.94779590577731));
#12518=CARTESIAN_POINT('Ctrl Pts',(6.90714077465332,-2.09294177008912,4.94835226674887));
#12519=CARTESIAN_POINT('Ctrl Pts',(6.89125110948031,-2.11144355019793,4.94988124319343));
#12520=CARTESIAN_POINT('Ctrl Pts',(6.88107964378012,-2.12311586774513,4.95085784337695));
#12521=CARTESIAN_POINT('Ctrl Pts',(6.83126891493184,-2.17945165927551,4.95562808268873));
#12522=CARTESIAN_POINT('Ctrl Pts',(6.79048006076839,-2.22307793353713,4.95949688204261));
#12523=CARTESIAN_POINT('Ctrl Pts',(6.70601718748927,-2.30852855333303,4.96739110501676));
#12524=CARTESIAN_POINT('Ctrl Pts',(6.66232923793585,-2.35030871913189,4.97141637915219));
#12525=CARTESIAN_POINT('Ctrl Pts',(6.47053728010992,-2.52366551895702,4.98875975978848));
#12526=CARTESIAN_POINT('Ctrl Pts',(6.31163388546885,-2.64267475497599,5.00229395102239));
#12527=CARTESIAN_POINT('Ctrl Pts',(6.06307733348232,-2.79529627511069,5.02165740077742));
#12528=CARTESIAN_POINT('Ctrl Pts',(5.98124771099469,-2.84076116939327,5.02778089059002));
#12529=CARTESIAN_POINT('Ctrl Pts',(5.86113495670316,-2.90080830275744,5.03640059343862));
#12530=CARTESIAN_POINT('Ctrl Pts',(5.82437775179795,-2.91832163024682,5.0389911961664));
#12531=CARTESIAN_POINT('Ctrl Pts',(5.75821164430768,-2.94832220318836,5.04357185156247));
#12532=CARTESIAN_POINT('Ctrl Pts',(5.72893086897331,-2.96107727516808,5.04557071651636));
#12533=CARTESIAN_POINT('Ctrl Pts',(5.68396957509363,-2.97987285142317,5.04859814551216));
#12534=CARTESIAN_POINT('Ctrl Pts',(5.66842405960474,-2.98622919746436,5.04963735402027));
#12535=CARTESIAN_POINT('Ctrl Pts',(5.65271848491895,-2.9925081454706,5.05067982369156));
#12536=CARTESIAN_POINT('Ctrl Pts',(5.65260763972783,-2.99255245324175,5.05068718075502));
#12537=CARTESIAN_POINT('Ctrl Pts',(5.65237822650347,-2.99264414102675,5.05070240669615));
#12538=CARTESIAN_POINT('Ctrl Pts',(5.65225965809875,-2.99269152015981,5.0507102755449));
#12539=CARTESIAN_POINT('Ctrl Pts',(5.65201423163662,-2.99278957400101,5.05072656250885));
#12540=CARTESIAN_POINT('Ctrl Pts',(5.65188737315497,-2.99284024769696,5.05073498059069));
#12541=CARTESIAN_POINT('Ctrl Pts',(5.65162475457962,-2.99294513148158,5.05075240644048));
#12542=CARTESIAN_POINT('Ctrl Pts',(5.65148899402042,-2.99299934039864,5.05076141416866));
#12543=CARTESIAN_POINT('Ctrl Pts',(5.65120791024285,-2.99311155440975,5.05078006295485));
#12544=CARTESIAN_POINT('Ctrl Pts',(5.65106258648902,-2.99316955815702,5.05078970396717));
#12545=CARTESIAN_POINT('Ctrl Pts',(5.65076166185503,-2.99328964220238,5.05080966647131));
#12546=CARTESIAN_POINT('Ctrl Pts',(5.65060606034434,-2.99335172095695,5.05081998791156));
#12547=CARTESIAN_POINT('Ctrl Pts',(5.65028380753271,-2.99348025776264,5.05084136223761));
#12548=CARTESIAN_POINT('Ctrl Pts',(5.65011715552066,-2.99354671403099,5.0508524150631));
#12549=CARTESIAN_POINT('Ctrl Pts',(5.64977196567573,-2.9936843328999,5.05087530727756));
#12550=CARTESIAN_POINT('Ctrl Pts',(5.64959342701954,-2.99375549344836,5.05088714659736));
#12551=CARTESIAN_POINT('Ctrl Pts',(5.6492235588312,-2.99390287429107,5.05091167143675));
#12552=CARTESIAN_POINT('Ctrl Pts',(5.64903222835298,-2.99397909221836,5.05092435687643));
#12553=CARTESIAN_POINT('Ctrl Pts',(5.64863579626798,-2.99413696987474,5.05095063850953));
#12554=CARTESIAN_POINT('Ctrl Pts',(5.64843069359028,-2.99421862686485,5.05096423460941));
#12555=CARTESIAN_POINT('Ctrl Pts',(5.64800565500928,-2.99438779576479,5.05099240746333));
#12556=CARTESIAN_POINT('Ctrl Pts',(5.64778571784138,-2.99447530452345,5.05100698411128));
#12557=CARTESIAN_POINT('Ctrl Pts',(5.64732985908287,-2.99465662376272,5.05103719377547));
#12558=CARTESIAN_POINT('Ctrl Pts',(5.64709393602716,-2.99475043060383,5.05105282666945));
#12559=CARTESIAN_POINT('Ctrl Pts',(5.64660485738868,-2.99494482929023,5.05108523085489));
#12560=CARTESIAN_POINT('Ctrl Pts',(5.64635170012362,-2.99504541692232,5.05110200200428));
#12561=CARTESIAN_POINT('Ctrl Pts',(5.64582679973206,-2.99525389989982,5.05113677157762));
#12562=CARTESIAN_POINT('Ctrl Pts',(5.64555505466544,-2.99536179036708,5.05115476983681));
#12563=CARTESIAN_POINT('Ctrl Pts',(5.64499151126087,-2.99558544424274,5.0511920899189));
#12564=CARTESIAN_POINT('Ctrl Pts',(5.64469971067464,-2.99570120200272,5.05121141155123));
#12565=CARTESIAN_POINT('Ctrl Pts',(5.64420359141788,-2.99589792941442,5.05124425783134));
#12566=CARTESIAN_POINT('Ctrl Pts',(5.64399928140574,-2.99597892079054,5.05125778321113));
#12567=CARTESIAN_POINT('Ctrl Pts',(5.63080417725614,-3.0012080847289,5.05213122177585));
#12568=CARTESIAN_POINT('Ctrl Pts',(5.61777988694038,-3.00627179529985,5.05298828167137));
#12569=CARTESIAN_POINT('Ctrl Pts',(5.588350868476,-3.01749370465314,5.05491364613198));
#12570=CARTESIAN_POINT('Ctrl Pts',(5.57192794068415,-3.0236031797876,5.05598030298161));
#12571=CARTESIAN_POINT('Ctrl Pts',(5.52966112792642,-3.03893556429234,5.05870606860748));
#12572=CARTESIAN_POINT('Ctrl Pts',(5.50374748444482,-3.04796301615364,5.06035870267325));
#12573=CARTESIAN_POINT('Ctrl Pts',(5.27865337527585,-3.12316860292018,5.07456242624772));
#12574=CARTESIAN_POINT('Ctrl Pts',(5.07355614975767,-3.17007704354512,5.08643785947386));
#12575=CARTESIAN_POINT('Ctrl Pts',(4.69325033171447,-3.21871839381532,5.10790194083449));
#12576=CARTESIAN_POINT('Ctrl Pts',(4.51968673807162,-3.22679539393264,5.11750902559948));
#12577=CARTESIAN_POINT('Ctrl Pts',(4.29830491589749,-3.21922519160031,5.13035859274909));
#12578=CARTESIAN_POINT('Ctrl Pts',(4.25032413907847,-3.21650906014664,5.13318031983141));
#12579=CARTESIAN_POINT('Ctrl Pts',(4.17097825415433,-3.210234818078,5.13793356555996));
#12580=CARTESIAN_POINT('Ctrl Pts',(4.13957151720611,-3.20728676023203,5.13983767126595));
#12581=CARTESIAN_POINT('Ctrl Pts',(4.0964594566348,-3.2026005726158,5.14248883434007));
#12582=CARTESIAN_POINT('Ctrl Pts',(4.08471177505838,-3.20125816705427,5.14321508312299));
#12583=CARTESIAN_POINT('Ctrl Pts',(4.06492087715667,-3.19888625896635,5.14444542706746));
#12584=CARTESIAN_POINT('Ctrl Pts',(4.05687353249974,-3.19789097515882,5.14494762314535));
#12585=CARTESIAN_POINT('Ctrl Pts',(4.04150640209735,-3.19593148003164,5.1459104150595));
#12586=CARTESIAN_POINT('Ctrl Pts',(4.03418604038425,-3.19497246945622,5.14637069905288));
#12587=CARTESIAN_POINT('Ctrl Pts',(4.01471992001893,-3.1923542241563,5.1475989322333));
#12588=CARTESIAN_POINT('Ctrl Pts',(4.00258036454496,-3.19065084815349,5.1483693030879));
#12589=CARTESIAN_POINT('Ctrl Pts',(3.95880582563907,-3.18425370047042,5.1511624375862));
#12590=CARTESIAN_POINT('Ctrl Pts',(3.92723255635927,-3.17915851512183,5.15320576550251));
#12591=CARTESIAN_POINT('Ctrl Pts',(3.55657512066857,-3.1136688143604,5.17749168822863));
#12592=CARTESIAN_POINT('Ctrl Pts',(3.22919235477271,-2.99976506171877,5.20158973399491));
#12593=CARTESIAN_POINT('Ctrl Pts',(2.87049842934907,-2.80620638166001,5.22819534149876));
#12594=CARTESIAN_POINT('Ctrl Pts',(2.81586992099581,-2.77462293108618,5.23226418374168));
#12595=CARTESIAN_POINT('Ctrl Pts',(2.7236692116218,-2.71764122591282,5.23915961113898));
#12596=CARTESIAN_POINT('Ctrl Pts',(2.68564255018691,-2.69301744349551,5.24201221334999));
#12597=CARTESIAN_POINT('Ctrl Pts',(2.63210419473049,-2.65672464268397,5.24604292947481));
#12598=CARTESIAN_POINT('Ctrl Pts',(2.61616051621262,-2.64570547816168,5.24724517412552));
#12599=CARTESIAN_POINT('Ctrl Pts',(2.58868504033778,-2.62634778873017,5.24932061074586));
#12600=CARTESIAN_POINT('Ctrl Pts',(2.57710741394206,-2.61807556500095,5.25019629483684));
#12601=CARTESIAN_POINT('Ctrl Pts',(2.55347595359909,-2.60095332947705,5.25198619935437));
#12602=CARTESIAN_POINT('Ctrl Pts',(2.54142815547933,-2.59209554798012,5.25290009121145));
#12603=CARTESIAN_POINT('Ctrl Pts',(2.51099163143338,-2.56938997346372,5.25521264031282));
#12604=CARTESIAN_POINT('Ctrl Pts',(2.4926886250003,-2.55542828197969,5.25660682491963));
#12605=CARTESIAN_POINT('Ctrl Pts',(2.42308022284281,-2.50114082246641,5.26192462495208));
#12606=CARTESIAN_POINT('Ctrl Pts',(2.37285240423198,-2.45945483241195,5.26579429457234));
#12607=CARTESIAN_POINT('Ctrl Pts',(2.07300568255103,-2.19481672237145,5.28919145986583));
#12608=CARTESIAN_POINT('Ctrl Pts',(1.85815003519757,-1.93566962973461,5.3070197553109));
#12609=CARTESIAN_POINT('Ctrl Pts',(1.66310396235734,-1.60792342042298,5.32916798777171));
#12610=CARTESIAN_POINT('Ctrl Pts',(1.64005659331291,-1.56720345762136,5.33191791364714));
#12611=CARTESIAN_POINT('Ctrl Pts',(1.60325995589937,-1.49875671423385,5.33656135345852));
#12612=CARTESIAN_POINT('Ctrl Pts',(1.58900851383478,-1.47130681190826,5.33842904403346));
#12613=CARTESIAN_POINT('Ctrl Pts',(1.5698987229574,-1.43316665633793,5.3410374603754));
#12614=CARTESIAN_POINT('Ctrl Pts',(1.56469993956813,-1.42264764410637,5.34175824323515));
#12615=CARTESIAN_POINT('Ctrl Pts',(1.55601370249326,-1.40482791621343,5.34298201053466));
#12616=CARTESIAN_POINT('Ctrl Pts',(1.55249602504105,-1.39754190105146,5.34348314256849));
#12617=CARTESIAN_POINT('Ctrl Pts',(1.54581278685394,-1.38356501145322,5.34444607686191));
#12618=CARTESIAN_POINT('Ctrl Pts',(1.54264278620235,-1.3768763650167,5.34490758091258));
#12619=CARTESIAN_POINT('Ctrl Pts',(1.53510797396376,-1.3608354838305,5.34601591825508));
#12620=CARTESIAN_POINT('Ctrl Pts',(1.53076502248097,-1.35147315426463,5.34666405795526));
#12621=CARTESIAN_POINT('Ctrl Pts',(1.5152506293183,-1.31760270414943,5.34901294258131));
#12622=CARTESIAN_POINT('Ctrl Pts',(1.50434191621799,-1.29297639532269,5.35072844129238));
#12623=CARTESIAN_POINT('Ctrl Pts',(1.42729501356592,-1.11298449445733,5.36330735817016));
#12624=CARTESIAN_POINT('Ctrl Pts',(1.37315556569585,-0.952783833335006,
5.37470692547687));
#12625=CARTESIAN_POINT('Ctrl Pts',(1.29538305061416,-0.644822100003465,
5.39619415002161));
#12626=CARTESIAN_POINT('Ctrl Pts',(1.26898159577177,-0.498186387000548,
5.40625281619682));
#12627=CARTESIAN_POINT('Ctrl Pts',(1.2392680533715,-0.22639783085076,5.42430436075756));
#12628=CARTESIAN_POINT('Ctrl Pts',(1.23291987206655,-0.101860118708508,
5.43235423357902));
#12629=CARTESIAN_POINT('Ctrl Pts',(1.23399276566092,0.0501447910228232,
5.44190168109828));
#12630=CARTESIAN_POINT('Ctrl Pts',(1.23453554598781,0.0775401410268698,
5.44361167635798));
#12631=CARTESIAN_POINT('Ctrl Pts',(1.23594557320512,0.120825494280249,5.4462972492166));
#12632=CARTESIAN_POINT('Ctrl Pts',(1.23658122801304,0.136721223832147,5.44728000905953));
#12633=CARTESIAN_POINT('Ctrl Pts',(1.23799577568304,0.166559142551229,5.44911844753835));
#12634=CARTESIAN_POINT('Ctrl Pts',(1.23874763001121,0.180502184459306,5.44997495004527));
#12635=CARTESIAN_POINT('Ctrl Pts',(1.24063971945123,0.211805519475726,5.4518922581791));
#12636=CARTESIAN_POINT('Ctrl Pts',(1.24182996340243,0.229162437617779,5.45295147514225));
#12637=CARTESIAN_POINT('Ctrl Pts',(1.24522806081473,0.273457489370556,5.45564518853079));
#12638=CARTESIAN_POINT('Ctrl Pts',(1.24763437132642,0.300379362240641,5.45727347066482));
#12639=CARTESIAN_POINT('Ctrl Pts',(1.26656614121557,0.485844734863518,5.46843517751405));
#12640=CARTESIAN_POINT('Ctrl Pts',(1.29449640024636,0.643011548987624,5.4775979383425));
#12641=CARTESIAN_POINT('Ctrl Pts',(1.38745149982558,1.00697475131792,5.49879981854309));
#12642=CARTESIAN_POINT('Ctrl Pts',(1.46189717919662,1.21053465676384,5.51063372901266));
#12643=CARTESIAN_POINT('Ctrl Pts',(1.59085055762625,1.47671291787271,5.52771749959235));
#12644=CARTESIAN_POINT('Ctrl Pts',(1.62818519816741,1.54701603770678,5.53240094293972));
#12645=CARTESIAN_POINT('Ctrl Pts',(1.67617882998829,1.62983572407868,5.53821380031675));
#12646=CARTESIAN_POINT('Ctrl Pts',(1.68438298130972,1.64375089317014,5.53920081332505));
#12647=CARTESIAN_POINT('Ctrl Pts',(1.69734751885659,1.66536710188411,5.54075123291304));
#12648=CARTESIAN_POINT('Ctrl Pts',(1.70203646386184,1.67311097417702,5.54131013210037));
#12649=CARTESIAN_POINT('Ctrl Pts',(1.71085621268371,1.68753937666373,5.54235817379593));
#12650=CARTESIAN_POINT('Ctrl Pts',(1.71497889110163,1.69422864589296,5.54284679222001));
#12651=CARTESIAN_POINT('Ctrl Pts',(1.72445914163435,1.70948566105769,5.54396744401497));
#12652=CARTESIAN_POINT('Ctrl Pts',(1.72983257044811,1.71804332520261,5.54460049917335));
#12653=CARTESIAN_POINT('Ctrl Pts',(1.74425576261011,1.74077544674501,5.54629378771886));
#12654=CARTESIAN_POINT('Ctrl Pts',(1.75337624469967,1.75490436527744,5.54735840716286));
#12655=CARTESIAN_POINT('Ctrl Pts',(1.83449568079927,1.87843711404869,5.55676966787602));
#12656=CARTESIAN_POINT('Ctrl Pts',(1.91298386988069,1.98341772779215,5.56547783271349));
#12657=CARTESIAN_POINT('Ctrl Pts',(2.11776787485982,2.22511409491698,5.58680076541084));
#12658=CARTESIAN_POINT('Ctrl Pts',(2.24995562244796,2.3562601943199,5.5994675741388));
#12659=CARTESIAN_POINT('Ctrl Pts',(2.46265403886111,2.53359648609577,5.61783067491177));
#12660=CARTESIAN_POINT('Ctrl Pts',(2.53503946247744,2.58892258944724,5.62378406187063));
#12661=CARTESIAN_POINT('Ctrl Pts',(2.64243608428466,2.66401945770731,5.63219056559815));
#12662=CARTESIAN_POINT('Ctrl Pts',(2.67562001170284,2.68631573072059,5.63473296499141));
#12663=CARTESIAN_POINT('Ctrl Pts',(2.73590734365723,2.7252145150741,5.63925512966341));
#12664=CARTESIAN_POINT('Ctrl Pts',(2.76285728065968,2.74204413392283,5.6412430231258));
#12665=CARTESIAN_POINT('Ctrl Pts',(2.80446553164012,2.76718002684345,5.64426210178119));
#12666=CARTESIAN_POINT('Ctrl Pts',(2.81894682166643,2.77577410755926,5.64530375881303));
#12667=CARTESIAN_POINT('Ctrl Pts',(2.84541686439616,2.7912038013422,5.64719153226137));
#12668=CARTESIAN_POINT('Ctrl Pts',(2.85738335612172,2.7980766179167,5.64803898153647));
#12669=CARTESIAN_POINT('Ctrl Pts',(2.88357315024145,2.81289553643384,5.64988091535598));
#12670=CARTESIAN_POINT('Ctrl Pts',(2.89781336100139,2.82081110149895,5.65087428748169));
#12671=CARTESIAN_POINT('Ctrl Pts',(2.93703400434898,2.84222460546706,5.65358843416815));
#12672=CARTESIAN_POINT('Ctrl Pts',(2.96213411581703,2.85550113835663,5.65530134306269));
#12673=CARTESIAN_POINT('Ctrl Pts',(3.10260011386277,2.92744022131947,5.66475983340365));
#12674=CARTESIAN_POINT('Ctrl Pts',(3.22124967784707,2.97944727213506,5.67226992560713));
#12675=CARTESIAN_POINT('Ctrl Pts',(3.54983521765312,3.10045943900629,5.69220181741328));
#12676=CARTESIAN_POINT('Ctrl Pts',(3.76422940900722,3.15525455092874,5.70427132166275));
#12677=CARTESIAN_POINT('Ctrl Pts',(4.086712805333,3.20320017475117,5.72287688337272));
#12678=CARTESIAN_POINT('Ctrl Pts',(4.19157952393162,3.21357120854047,5.72900402321083));
#12679=CARTESIAN_POINT('Ctrl Pts',(4.31402348958662,3.21964684228138,5.73643761746604));
#12680=CARTESIAN_POINT('Ctrl Pts',(4.33129946695436,3.22036474236261,5.73749291885307));
#12681=CARTESIAN_POINT('Ctrl Pts',(4.35787204032969,3.22125482087648,5.73912719501438));
#12682=CARTESIAN_POINT('Ctrl Pts',(4.36716530346022,3.22152585402803,5.73970083806339));
#12683=CARTESIAN_POINT('Ctrl Pts',(4.38428572892534,3.22195102548173,5.74076168005068));
#12684=CARTESIAN_POINT('Ctrl Pts',(4.39211239867391,3.22211686018867,5.74124822552181));
#12685=CARTESIAN_POINT('Ctrl Pts',(4.40986821501686,3.22242835871814,5.7423555789701));
#12686=CARTESIAN_POINT('Ctrl Pts',(4.41979742226745,3.22255664830897,5.7429773271956));
#12687=CARTESIAN_POINT('Ctrl Pts',(4.44559249720182,3.22277070176415,5.74459879993989));
#12688=CARTESIAN_POINT('Ctrl Pts',(4.46145847336754,3.22278518976129,5.74560225752012));
#12689=CARTESIAN_POINT('Ctrl Pts',(4.5697223890258,3.22208459893676,5.75248837229417));
#12690=CARTESIAN_POINT('Ctrl Pts',(4.66204432515844,3.2175131728796,5.75855272137907));
#12691=CARTESIAN_POINT('Ctrl Pts',(4.83618207946392,3.20136567169928,5.77020711636286));
#12692=CARTESIAN_POINT('Ctrl Pts',(4.9180061548293,3.19059662434563,5.77577450191839));
#12693=CARTESIAN_POINT('Ctrl Pts',(5.1300548718705,3.15436037967675,5.79032284188314));
#12694=CARTESIAN_POINT('Ctrl Pts',(5.25928824997423,3.12397051426465,5.7993043595104));
#12695=CARTESIAN_POINT('Ctrl Pts',(5.48005337302454,3.05744722787013,5.81464106667898));
#12696=CARTESIAN_POINT('Ctrl Pts',(5.57249081982316,3.02493086279902,5.82106256223416));
#12697=CARTESIAN_POINT('Ctrl Pts',(5.70223427046989,2.97253239714415,5.83005391239988));
#12698=CARTESIAN_POINT('Ctrl Pts',(5.74084812251682,2.95605319656,5.83272741093062));
#12699=CARTESIAN_POINT('Ctrl Pts',(5.80924295328493,2.92527108393362,5.83745922189585));
#12700=CARTESIAN_POINT('Ctrl Pts',(5.83914620930727,2.91125611287085,5.83952679422523));
#12701=CARTESIAN_POINT('Ctrl Pts',(5.88419686780973,2.88929113934443,5.84264078670076));
#12702=CARTESIAN_POINT('Ctrl Pts',(5.89950440546051,2.88167642046806,5.84369872032235));
#12703=CARTESIAN_POINT('Ctrl Pts',(5.92718401559389,2.8676313573661,5.84561166982905));
#12704=CARTESIAN_POINT('Ctrl Pts',(5.93957624948928,2.86124189080065,5.84646808737535));
#12705=CARTESIAN_POINT('Ctrl Pts',(5.96621428233791,2.84728769445016,5.84830917142137));
#12706=CARTESIAN_POINT('Ctrl Pts',(5.98044558904795,2.83969600597366,5.84929285953522));
#12707=CARTESIAN_POINT('Ctrl Pts',(6.01893970269511,2.81878859612649,5.85195429228117));
#12708=CARTESIAN_POINT('Ctrl Pts',(6.0430892866359,2.80526647395741,5.8536246767173));
#12709=CARTESIAN_POINT('Ctrl Pts',(6.16853935120409,2.73288469023007,5.86231035910533));
#12710=CARTESIAN_POINT('Ctrl Pts',(6.26675468142661,2.66884126879553,5.86913536228855));
#12711=CARTESIAN_POINT('Ctrl Pts',(6.54649661368538,2.46386495974867,5.88895982267156));
#12712=CARTESIAN_POINT('Ctrl Pts',(6.71667538330973,2.30874578757954,5.90150195518993));
#12713=CARTESIAN_POINT('Ctrl Pts',(6.94169305425103,2.05470799049169,5.92083457579292));
#12714=CARTESIAN_POINT('Ctrl Pts',(7.01021269064341,1.96889600901355,5.92720684464008));
#12715=CARTESIAN_POINT('Ctrl Pts',(7.08438773944989,1.86560054685676,5.93491630263972));
#12716=CARTESIAN_POINT('Ctrl Pts',(7.09444517964552,1.85135192449132,5.93598058869225));
#12717=CARTESIAN_POINT('Ctrl Pts',(7.10970393636753,1.82935768230533,5.93762587848579));
#12718=CARTESIAN_POINT('Ctrl Pts',(7.11498827056967,1.82166968503891,5.9382014374876));
#12719=CARTESIAN_POINT('Ctrl Pts',(7.12464422717785,1.80749006593233,5.93926403770364));
#12720=CARTESIAN_POINT('Ctrl Pts',(7.12902565175454,1.80100536410118,5.93975040903788));
#12721=CARTESIAN_POINT('Ctrl Pts',(7.13889064768162,1.78628946614509,5.94085507371115));
#12722=CARTESIAN_POINT('Ctrl Pts',(7.14435994029868,1.77804899846363,5.94147428751529));
#12723=CARTESIAN_POINT('Ctrl Pts',(7.15843168451342,1.75663409877361,5.94308483364394));
#12724=CARTESIAN_POINT('Ctrl Pts',(7.16697562524646,1.74342178451079,5.94407981901744));
#12725=CARTESIAN_POINT('Ctrl Pts',(7.22333561207384,1.65485121888495,5.9507558755446));
#12726=CARTESIAN_POINT('Ctrl Pts',(7.26809614297793,1.5776036327733,5.95660657303239));
#12727=CARTESIAN_POINT('Ctrl Pts',(7.3485491223689,1.42443330833082,5.96812352231471));
#12728=CARTESIAN_POINT('Ctrl Pts',(7.38460019395792,1.3487714698252,5.97377503997865));
#12729=CARTESIAN_POINT('Ctrl Pts',(7.49283878168835,1.09675323013322,5.99232203063751));
#12730=CARTESIAN_POINT('Ctrl Pts',(7.55235583180524,0.915373080372865,6.00521257966433));
#12731=CARTESIAN_POINT('Ctrl Pts',(7.61010129434065,0.666991465606748,6.02187337043636));
#12732=CARTESIAN_POINT('Ctrl Pts',(7.62281307446264,0.603771789738278,6.02603446623604));
#12733=CARTESIAN_POINT('Ctrl Pts',(7.64133921587721,0.49481344717113,6.03306899415619));
#12734=CARTESIAN_POINT('Ctrl Pts',(7.64808438469772,0.449255193559716,6.03596985672517));
#12735=CARTESIAN_POINT('Ctrl Pts',(7.65629381970488,0.384213302008736,6.04005588300774));
#12736=CARTESIAN_POINT('Ctrl Pts',(7.65856076712176,0.364838430654508,6.04126609215879));
#12737=CARTESIAN_POINT('Ctrl Pts',(7.66217922042267,0.331275274173806,6.04335084558643));
#12738=CARTESIAN_POINT('Ctrl Pts',(7.66361276032533,0.317096571861515,6.04422794399757));
#12739=CARTESIAN_POINT('Ctrl Pts',(7.6663538376426,0.288062404375125,6.0460168158811));
#12740=CARTESIAN_POINT('Ctrl Pts',(7.66765240828835,0.273206423953281,6.04692828761155));
#12741=CARTESIAN_POINT('Ctrl Pts',(7.67067776633357,0.235587281066092,6.04922693339431));
#12742=CARTESIAN_POINT('Ctrl Pts',(7.67226591368866,0.212813561422698,6.05060974414237));
#12743=CARTESIAN_POINT('Ctrl Pts',(7.67734907811268,0.126754805073478,6.05580405820949));
#12744=CARTESIAN_POINT('Ctrl Pts',(7.67921910621824,0.0633859825749122,
6.0595649876271));
#12745=CARTESIAN_POINT('Ctrl Pts',(7.67921910621823,3.83865910396161E-12,
6.06327685380577));
#12746=CARTESIAN_POINT('Origin',(6.37917532067789,0.,0.));
#12747=CARTESIAN_POINT('',(6.37917532067789,3.3456130901271,3.71576009063693));
#12748=CARTESIAN_POINT('',(6.37917546296132,2.5863715564937,3.37286375486987));
#12749=CARTESIAN_POINT('Ctrl Pts',(6.37917532067789,3.3456130901271,3.71576009063693));
#12750=CARTESIAN_POINT('Ctrl Pts',(6.37917532067789,3.24255076195948,3.66678682150482));
#12751=CARTESIAN_POINT('Ctrl Pts',(6.37917532320414,3.13881135649388,3.61831280819208));
#12752=CARTESIAN_POINT('Ctrl Pts',(6.37917532320414,2.89069148427495,3.50485012599878));
#12753=CARTESIAN_POINT('Ctrl Pts',(6.37917532067789,2.74467927191424,3.44009994888136));
#12754=CARTESIAN_POINT('Ctrl Pts',(6.37917532067789,2.59448758938272,3.3763047103935));
#12755=CARTESIAN_POINT('Ctrl Pts',(6.37917532067789,2.59043006761928,3.3745833507138));
#12756=CARTESIAN_POINT('Ctrl Pts',(6.37917532067789,2.5863715767527,3.3728637070571));
#12757=CARTESIAN_POINT('',(6.37917532067789,-3.03681439448832,3.9721226483366));
#12758=CARTESIAN_POINT('Origin',(6.37917532067789,0.,0.));
#12759=CARTESIAN_POINT('',(6.37917568135534,-2.58637139413976,3.74329856950612));
#12760=CARTESIAN_POINT('Ctrl Pts',(6.37917532067789,-2.58637143681758,3.74329848378769));
#12761=CARTESIAN_POINT('Ctrl Pts',(6.37917532067789,-2.7320504532865,3.8158297039793));
#12762=CARTESIAN_POINT('Ctrl Pts',(6.37917532045944,-2.87765867009868,3.88989647023702));
#12763=CARTESIAN_POINT('Ctrl Pts',(6.37917532045944,-3.02751940626012,3.96731715398979));
#12764=CARTESIAN_POINT('Ctrl Pts',(6.37917532067789,-3.03216640106086,3.96971905726743));
#12765=CARTESIAN_POINT('Ctrl Pts',(6.37917532067789,-3.03681439448831,3.9721226483366));
#12766=CARTESIAN_POINT('',(6.3791877629001,-2.58636241268454,3.49716578845862));
#12767=CARTESIAN_POINT('',(6.37917532067789,-2.58637166226708,-2.31077344927308));
#12768=CARTESIAN_POINT('',(6.37917532067789,-3.43098962587739,3.11492912548425));
#12769=CARTESIAN_POINT('Ctrl Pts',(6.37917532067789,-3.42636936949566,3.11682231207784));
#12770=CARTESIAN_POINT('Ctrl Pts',(6.37917532067789,-3.28944284185674,3.18199139775366));
#12771=CARTESIAN_POINT('Ctrl Pts',(6.37917532239532,-3.1510759240114,3.24655917840321));
#12772=CARTESIAN_POINT('Ctrl Pts',(6.37917532239532,-2.87198388415713,3.37336255932108));
#12773=CARTESIAN_POINT('Ctrl Pts',(6.37917532067789,-2.72904836859129,3.43653015731865));
#12774=CARTESIAN_POINT('Ctrl Pts',(6.37917532067789,-2.58636419175174,3.49716997456519));
#12775=CARTESIAN_POINT('',(6.37998521093114,-3.43053564256519,2.93155396442585));
#12776=CARTESIAN_POINT('',(6.37917532067789,-3.43098962587739,7.61832735979826E-16));
#12777=CARTESIAN_POINT('',(6.37918196868372,-2.58636672013265,2.49808050559515));
#12778=CARTESIAN_POINT('Ctrl Pts',(6.37917532067789,-2.58636751268136,2.49807891470192));
#12779=CARTESIAN_POINT('Ctrl Pts',(6.37917532067789,-2.72887860212156,2.56907486702406));
#12780=CARTESIAN_POINT('Ctrl Pts',(6.37917532053929,-2.87210044244327,2.64173957575438));
#12781=CARTESIAN_POINT('Ctrl Pts',(6.37917532053929,-3.15213081145752,2.78567562114608));
#12782=CARTESIAN_POINT('Ctrl Pts',(6.37917532067789,-3.29129959195667,2.85812191577848));
#12783=CARTESIAN_POINT('Ctrl Pts',(6.37917532067789,-3.42919155682922,2.9305834788995));
#12784=CARTESIAN_POINT('',(6.3791823737616,-2.58636641899648,2.24798337798073));
#12785=CARTESIAN_POINT('',(6.37917532067789,-2.58637166226708,-2.31077344927308));
#12786=CARTESIAN_POINT('',(6.37611478183885,-3.42549916664848,1.86508717508508));
#12787=CARTESIAN_POINT('Ctrl Pts',(6.37917532067789,-3.42379086727351,1.86491054275556));
#12788=CARTESIAN_POINT('Ctrl Pts',(6.37917532067789,-3.28673462067467,1.93071771383031));
#12789=CARTESIAN_POINT('Ctrl Pts',(6.37917532283357,-3.14809308263519,1.99603457995718));
#12790=CARTESIAN_POINT('Ctrl Pts',(6.37917532283357,-2.86996050619901,2.12368388664866));
#12791=CARTESIAN_POINT('Ctrl Pts',(6.37917532067789,-2.72795486563548,2.18712975387996));
#12792=CARTESIAN_POINT('Ctrl Pts',(6.37917532067789,-2.58636741807969,2.2479857024477));
#12793=CARTESIAN_POINT('',(6.37607929534711,-3.42544344211231,1.6817486560154));
#12794=CARTESIAN_POINT('',(6.37917532067789,-3.43098962587739,7.61832735979826E-16));
#12795=CARTESIAN_POINT('',(6.37917539807422,-2.58637160473072,1.24811343365893));
#12796=CARTESIAN_POINT('Ctrl Pts',(6.37917532067789,-2.58637161380091,1.24811341563195));
#12797=CARTESIAN_POINT('Ctrl Pts',(6.37917532067789,-2.72753521492361,1.31913928723047));
#12798=CARTESIAN_POINT('Ctrl Pts',(6.37917532051029,-2.86970473769156,1.39195767065841));
#12799=CARTESIAN_POINT('Ctrl Pts',(6.37917532051029,-3.1477213348857,1.53611018972745));
#12800=CARTESIAN_POINT('Ctrl Pts',(6.37917532067789,-3.2864602980215,1.60891634068854));
#12801=CARTESIAN_POINT('Ctrl Pts',(6.37917532067789,-3.42371299993736,1.68156992689594));
#12802=CARTESIAN_POINT('',(6.37917532113595,-2.58637166192656,1.00259120688551));
#12803=CARTESIAN_POINT('',(6.37917532067789,-2.58637166226708,-2.31077344927308));
#12804=CARTESIAN_POINT('',(6.3791753206778,-3.43420595741608,0.615284103491457));
#12805=CARTESIAN_POINT('Ctrl Pts',(6.37917532067789,-3.43420595741604,0.615284103491447));
#12806=CARTESIAN_POINT('Ctrl Pts',(6.37917532067789,-3.29741891646025,0.681127228409223));
#12807=CARTESIAN_POINT('Ctrl Pts',(6.37917532352613,-3.15892390364414,0.746478675402509));
#12808=CARTESIAN_POINT('Ctrl Pts',(6.37917532352613,-2.8774597106866,0.875641799826454));
#12809=CARTESIAN_POINT('Ctrl Pts',(6.37917532067789,-2.73164810422721,0.940615345270336));
#12810=CARTESIAN_POINT('Ctrl Pts',(6.37917532067789,-2.58637166199141,1.00259120703754));
#12811=CARTESIAN_POINT('',(6.38006015424921,-3.4304936204481,0.431770922268101));
#12812=CARTESIAN_POINT('',(6.37917532067789,-3.43098962587739,7.61832735979826E-16));
#12813=CARTESIAN_POINT('',(6.37917530233775,-2.60059989070202,1.86049092798513E-15));
#12814=CARTESIAN_POINT('Ctrl Pts',(6.37917532067789,-2.60059988642247,8.5336713043227E-9));
#12815=CARTESIAN_POINT('Ctrl Pts',(6.37917532067789,-2.74096448551843,0.0703914931049154));
#12816=CARTESIAN_POINT('Ctrl Pts',(6.37917532047357,-2.88242584110287,0.142797521996279));
#12817=CARTESIAN_POINT('Ctrl Pts',(6.37917532047357,-3.15734889890005,0.285445038517132));
#12818=CARTESIAN_POINT('Ctrl Pts',(6.37917532067789,-3.29408671125374,0.357340193452045));
#12819=CARTESIAN_POINT('Ctrl Pts',(6.37917532067789,-3.42919755846904,0.429047307451443));
#12820=CARTESIAN_POINT('',(6.37917532067381,3.40970963171873,-2.08166817117217E-15));
#12821=CARTESIAN_POINT('',(6.37917532067789,0.,0.));
#12822=CARTESIAN_POINT('',(6.37917532067789,3.43058507618661,0.00996756904321544));
#12823=CARTESIAN_POINT('Ctrl Pts',(6.37917532067789,3.43058507618662,0.00996756904321605));
#12824=CARTESIAN_POINT('Ctrl Pts',(6.37917532067789,3.42363017407561,0.0066432490635038));
#12825=CARTESIAN_POINT('Ctrl Pts',(6.37917532067789,3.41667162062538,0.00332067317801396));
#12826=CARTESIAN_POINT('Ctrl Pts',(6.37917532067789,3.40970963171769,2.18790263684099E-12));
#12827=CARTESIAN_POINT('',(6.37857781428809,3.43132439655042,0.193274600733303));
#12828=CARTESIAN_POINT('',(6.37917532067789,3.43098962587739,-7.61832735979826E-16));
#12829=CARTESIAN_POINT('',(6.38046276496377,2.58541407971855,0.629099045079643));
#12830=CARTESIAN_POINT('Ctrl Pts',(6.37917532067789,2.58599310446573,0.630264828345792));
#12831=CARTESIAN_POINT('Ctrl Pts',(6.37917532067789,2.72634555194803,0.560554151602523));
#12832=CARTESIAN_POINT('Ctrl Pts',(6.3791753205559,2.86720337116213,0.489210445502158));
#12833=CARTESIAN_POINT('Ctrl Pts',(6.3791753205559,3.14680320597834,0.345567079807686));
#12834=CARTESIAN_POINT('Ctrl Pts',(6.37917532067789,3.28758563896518,0.272204329161614));
#12835=CARTESIAN_POINT('Ctrl Pts',(6.37917532067789,3.42894278019802,0.19775621643526));
#12836=CARTESIAN_POINT('Ctrl Pts',(6.37917532067789,3.43079831146947,0.196778831244402));
#12837=CARTESIAN_POINT('Ctrl Pts',(6.37917532067789,3.43265378674765,0.195801337563912));
#12838=CARTESIAN_POINT('',(6.37917532099386,2.58637166203218,0.87851513268152));
#12839=CARTESIAN_POINT('',(6.37917532067789,2.58637166226708,-2.31077344927308));
#12840=CARTESIAN_POINT('',(6.37917532067788,3.4309896258774,1.26003777205275));
#12841=CARTESIAN_POINT('Ctrl Pts',(6.37917532067789,3.42328500954886,1.25880755392709));
#12842=CARTESIAN_POINT('Ctrl Pts',(6.37917532067789,3.29045367565351,1.19543400654417));
#12843=CARTESIAN_POINT('Ctrl Pts',(6.37917532244034,3.15626185421106,1.13259854029751));
#12844=CARTESIAN_POINT('Ctrl Pts',(6.37917532244034,2.87827578392745,1.00567409785647));
#12845=CARTESIAN_POINT('Ctrl Pts',(6.37917532067789,2.73212479642037,0.940755725708482));
#12846=CARTESIAN_POINT('Ctrl Pts',(6.37917532067789,2.58637166207725,0.878515132575993));
#12847=CARTESIAN_POINT('',(6.37730370004177,3.42771650614571,1.44343144191856));
#12848=CARTESIAN_POINT('',(6.37917532067789,3.43098962587739,-7.61832735979826E-16));
#12849=CARTESIAN_POINT('',(6.37917532696298,2.58637165759475,1.87594439571473));
#12850=CARTESIAN_POINT('Ctrl Pts',(6.37917532067789,2.58637165834049,1.87594439720601));
#12851=CARTESIAN_POINT('Ctrl Pts',(6.37917532067789,2.72296207022395,1.80763974829727));
#12852=CARTESIAN_POINT('Ctrl Pts',(6.37917532052268,2.86026107377465,1.73779740731373));
#12853=CARTESIAN_POINT('Ctrl Pts',(6.37917532052268,3.13594275047174,1.59584166551277));
#12854=CARTESIAN_POINT('Ctrl Pts',(6.37917532067789,3.27670524567701,1.52244549425824));
#12855=CARTESIAN_POINT('Ctrl Pts',(6.37917532067789,3.41959079935358,1.44725503297199));
#12856=CARTESIAN_POINT('Ctrl Pts',(6.37917532067789,3.42311930708574,1.44539779726455));
#12857=CARTESIAN_POINT('Ctrl Pts',(6.37917532067789,3.42664762619326,1.44354022985285));
#12858=CARTESIAN_POINT('',(6.37918119522423,2.5863672951246,2.12518466390817));
#12859=CARTESIAN_POINT('',(6.37917532067789,2.58637166226708,-2.31077344927308));
#12860=CARTESIAN_POINT('',(6.37707234371275,3.42716806216857,2.50981808392763));
#12861=CARTESIAN_POINT('Ctrl Pts',(6.37917532067789,3.42600824378348,2.50993925709623));
#12862=CARTESIAN_POINT('Ctrl Pts',(6.37917532067789,3.29337096368447,2.44609345245295));
#12863=CARTESIAN_POINT('Ctrl Pts',(6.37917532292,3.15924007754082,2.38271294856361));
#12864=CARTESIAN_POINT('Ctrl Pts',(6.37917532292,2.88260140945533,2.25527329380387));
#12865=CARTESIAN_POINT('Ctrl Pts',(6.37917532067789,2.73745665096598,2.19022396547602));
#12866=CARTESIAN_POINT('Ctrl Pts',(6.37917532067789,2.59068646954243,2.12704004536091));
#12867=CARTESIAN_POINT('Ctrl Pts',(6.37917532067789,2.58852740148246,2.12611114721521));
#12868=CARTESIAN_POINT('Ctrl Pts',(6.37917532067789,2.58636812502947,2.12518273374011));
#12869=CARTESIAN_POINT('',(6.37692902980926,3.42691262734832,2.69315322924028));
#12870=CARTESIAN_POINT('',(6.37917532067789,3.43098962587739,-7.61832735979826E-16));
#12871=CARTESIAN_POINT('',(6.37918160141763,2.58636699315934,3.1286030352177));
#12872=CARTESIAN_POINT('Ctrl Pts',(6.37917532067789,2.58636772558512,3.12860448938999));
#12873=CARTESIAN_POINT('Ctrl Pts',(6.37917532067789,2.72377271853466,3.05939745007247));
#12874=CARTESIAN_POINT('Ctrl Pts',(6.37917532049074,2.86217419915329,2.98842182782831));
#12875=CARTESIAN_POINT('Ctrl Pts',(6.37917532049074,3.13736378955755,2.84554807880643));
#12876=CARTESIAN_POINT('Ctrl Pts',(6.37917532067789,3.27707963871674,2.77209788112412));
#12877=CARTESIAN_POINT('Ctrl Pts',(6.37917532067789,3.41866961320406,2.69699822902537));
#12878=CARTESIAN_POINT('Ctrl Pts',(6.37917532067789,3.42217110366622,2.69514060888361));
#12879=CARTESIAN_POINT('Ctrl Pts',(6.37917532067789,3.42567240795605,2.69328266938512));
#12880=CARTESIAN_POINT('',(6.37917532067789,2.58637166226708,-2.31077344927308));
#12881=CARTESIAN_POINT('Origin',(206.833344075386,0.,0.));
#12882=CARTESIAN_POINT('',(6.62837333988161,3.27892070654281,3.77474224288293));
#12883=CARTESIAN_POINT('Ctrl Pts',(6.62603580309594,3.28236130364179,3.77175082320597));
#12884=CARTESIAN_POINT('Ctrl Pts',(6.54400502547545,3.30474507000467,3.75227137931291));
#12885=CARTESIAN_POINT('Ctrl Pts',(6.46198795242467,3.32574102461171,3.73365259200797));
#12886=CARTESIAN_POINT('Ctrl Pts',(6.37917532067789,3.3456130901271,3.71576009063693));
#12887=CARTESIAN_POINT('',(6.97215211287823,3.02321484681493,3.97983001953316));
#12888=CARTESIAN_POINT('Ctrl Pts',(6.96745972433549,3.02711333050602,3.97952068524248));
#12889=CARTESIAN_POINT('Ctrl Pts',(6.86017306897531,3.11610761504228,3.91182514943145));
#12890=CARTESIAN_POINT('Ctrl Pts',(6.74689823309609,3.20041018982336,3.84293949843672));
#12891=CARTESIAN_POINT('Ctrl Pts',(6.6284029078717,3.27890112099087,3.77475925573603));
#12892=CARTESIAN_POINT('',(6.63714354025222,2.37292574162162,4.40103865535663));
#12893=CARTESIAN_POINT('Ctrl Pts',(6.63711855526384,2.3729338705341,4.40104360874464));
#12894=CARTESIAN_POINT('Ctrl Pts',(6.66436682263207,2.49766393078106,4.33379224498954));
#12895=CARTESIAN_POINT('Ctrl Pts',(6.70730912100586,2.61378897659334,4.26444374464064));
#12896=CARTESIAN_POINT('Ctrl Pts',(6.82251116401291,2.83139221157415,4.123048075617));
#12897=CARTESIAN_POINT('Ctrl Pts',(6.8922421142993,2.93018531660515,4.05305893528313));
#12898=CARTESIAN_POINT('Ctrl Pts',(6.97154264924743,3.02268510374038,3.98288533237325));
#12899=CARTESIAN_POINT('Ctrl Pts',(6.97215682679145,3.02340044689291,3.98234234385051));
#12900=CARTESIAN_POINT('Ctrl Pts',(6.97277153762443,3.02411535324729,3.98179938347652));
#12901=CARTESIAN_POINT('',(7.19099309084831,1.70543136478218,4.70016067061871));
#12902=CARTESIAN_POINT('Ctrl Pts',(7.19099319326954,1.70543120055785,4.70016004197344));
#12903=CARTESIAN_POINT('Ctrl Pts',(7.05768222863756,1.91918479186951,4.6226005459991));
#12904=CARTESIAN_POINT('Ctrl Pts',(6.90177096221566,2.11235490214046,4.53573987292431));
#12905=CARTESIAN_POINT('Ctrl Pts',(6.70347989827123,2.31064596608489,4.43420714472505));
#12906=CARTESIAN_POINT('Ctrl Pts',(6.67075041713426,2.3420417073132,4.41769984393852));
#12907=CARTESIAN_POINT('Ctrl Pts',(6.63714132687621,2.37292777567092,4.40104689493868));
#12908=CARTESIAN_POINT('Ctrl Pts',(7.49128360962441,-1.08444291718913,4.88098182329727));
#12909=CARTESIAN_POINT('Ctrl Pts',(7.57445070748278,-0.991695767530693,
4.90158812612276));
#12910=CARTESIAN_POINT('Ctrl Pts',(7.65099179058753,-0.8924678343991,4.92086171312852));
#12911=CARTESIAN_POINT('Ctrl Pts',(7.8082523458007,-0.646879580013778,4.9600116730167));
#12912=CARTESIAN_POINT('Ctrl Pts',(7.88168782814486,-0.496205002355483,
4.97788797884683));
#12913=CARTESIAN_POINT('Ctrl Pts',(7.96978192849634,-0.221548058095216,
4.99642020088847));
#12914=CARTESIAN_POINT('Ctrl Pts',(7.99463425444134,-0.103359142162303,
5.00038423568684));
#12915=CARTESIAN_POINT('Ctrl Pts',(8.01211326010161,0.0803660628211763,
4.99975359834527));
#12916=CARTESIAN_POINT('Ctrl Pts',(8.01439868802338,0.143739735844232,4.99833648163297));
#12917=CARTESIAN_POINT('Ctrl Pts',(8.01259138727451,0.221360495872097,4.99511777741445));
#12918=CARTESIAN_POINT('Ctrl Pts',(8.01207221978763,0.235554826120059,4.99446850150878));
#12919=CARTESIAN_POINT('Ctrl Pts',(8.01099445753803,0.257172126518868,4.99338741634105));
#12920=CARTESIAN_POINT('Ctrl Pts',(8.01057226899669,0.264601754000765,4.99299922061733));
#12921=CARTESIAN_POINT('Ctrl Pts',(8.01000948285326,0.27342443630196,4.99251850621268));
#12922=CARTESIAN_POINT('Ctrl Pts',(8.00991855247719,0.274821229604134,4.9924418122137));
#12923=CARTESIAN_POINT('Ctrl Pts',(8.00977582860952,0.27697036175503,4.99232290488944));
#12924=CARTESIAN_POINT('Ctrl Pts',(8.00972532729969,0.277722806958215,4.99228110289905));
#12925=CARTESIAN_POINT('Ctrl Pts',(8.00963608199596,0.279038673397197,4.99220770173184));
#12926=CARTESIAN_POINT('Ctrl Pts',(8.00959757004527,0.279602114059626,4.99217617640346));
#12927=CARTESIAN_POINT('Ctrl Pts',(8.00951618108859,0.280783714389569,4.99210986348361));
#12928=CARTESIAN_POINT('Ctrl Pts',(8.00947324372347,0.281401868345432,4.99207505670626));
#12929=CARTESIAN_POINT('Ctrl Pts',(8.00936645504332,0.2829265290089,4.99198892262566));
#12930=CARTESIAN_POINT('Ctrl Pts',(8.00930219348069,0.283832998435099,4.99193746487618));
#12931=CARTESIAN_POINT('Ctrl Pts',(8.00904765528153,0.287380903063516,4.99173509080762));
#12932=CARTESIAN_POINT('Ctrl Pts',(8.00885163576263,0.290021809101788,4.99158234885387));
#12933=CARTESIAN_POINT('Ctrl Pts',(8.00857581971104,0.293617630215502,4.99137151526392));
#12934=CARTESIAN_POINT('Ctrl Pts',(8.00850167515199,0.294573070581933,4.99131521965872));
#12935=CARTESIAN_POINT('Ctrl Pts',(7.99573391015604,0.457219192837101,4.98168507297965));
#12936=CARTESIAN_POINT('Ctrl Pts',(7.9588726805899,0.614067202363164,4.96447590138363));
#12937=CARTESIAN_POINT('Ctrl Pts',(7.89447382037831,0.782155205343506,4.93847758919872));
#12938=CARTESIAN_POINT('Ctrl Pts',(7.88733759678773,0.799921002710326,4.93563026557539));
#12939=CARTESIAN_POINT('Ctrl Pts',(7.87214710745916,0.836083527033064,4.9296365821974));
#12940=CARTESIAN_POINT('Ctrl Pts',(7.86406639597203,0.854463551329238,4.92648302627241));
#12941=CARTESIAN_POINT('Ctrl Pts',(7.84683912384043,0.891993396233924,4.91983046092911));
#12942=CARTESIAN_POINT('Ctrl Pts',(7.83765954684862,0.911122334981121,4.91632265681671));
#12943=CARTESIAN_POINT('Ctrl Pts',(7.81806182513801,0.950278649661944,4.90890955196389));
#12944=CARTESIAN_POINT('Ctrl Pts',(7.80760352455399,0.970280169205902,4.90499384152793));
#12945=CARTESIAN_POINT('Ctrl Pts',(7.78524190471491,1.01131140639185,4.89670483459671));
#12946=CARTESIAN_POINT('Ctrl Pts',(7.77329998295004,1.03229105411954,4.8923232138641));
#12947=CARTESIAN_POINT('Ctrl Pts',(7.74771939462743,1.07542623486743,4.88303000318918));
#12948=CARTESIAN_POINT('Ctrl Pts',(7.73403417106869,1.09752525896396,4.87810821733423));
#12949=CARTESIAN_POINT('Ctrl Pts',(7.7047137303281,1.14299094381945,4.86766474399873));
#12950=CARTESIAN_POINT('Ctrl Pts',(7.68900907462563,1.16631315349381,4.86212652513195));
#12951=CARTESIAN_POINT('Ctrl Pts',(7.65532437253361,1.21435424181897,4.85036168180865));
#12952=CARTESIAN_POINT('Ctrl Pts',(7.63726195561945,1.23901925752238,4.84411614483842));
#12953=CARTESIAN_POINT('Ctrl Pts',(7.5984706626884,1.28988258743456,4.83083404018334));
#12954=CARTESIAN_POINT('Ctrl Pts',(7.57764365710047,1.31601533654054,4.82377594525967));
#12955=CARTESIAN_POINT('Ctrl Pts',(7.53284793993454,1.36996136284253,4.80874897585579));
#12956=CARTESIAN_POINT('Ctrl Pts',(7.50876158839627,1.39769425420913,4.80075575890809));
#12957=CARTESIAN_POINT('Ctrl Pts',(7.45686085092974,1.45500289392553,4.78371753530002));
#12958=CARTESIAN_POINT('Ctrl Pts',(7.4289043609337,1.48447885289504,4.77464531538174));
#12959=CARTESIAN_POINT('Ctrl Pts',(7.36852762470939,1.54545586007504,4.75528163768685));
#12960=CARTESIAN_POINT('Ctrl Pts',(7.335933276171,1.5768317599979,4.74496009493226));
#12961=CARTESIAN_POINT('Ctrl Pts',(7.26623678847155,1.64098942714486,4.7231778702185));
#12962=CARTESIAN_POINT('Ctrl Pts',(7.22896040182095,1.67365483176265,4.7116899453092));
#12963=CARTESIAN_POINT('Ctrl Pts',(7.19099262183641,1.70543064890463,4.70016024213821));
#12964=CARTESIAN_POINT('',(7.44179868886595,-2.56052656361313,4.29510059109848));
#12965=CARTESIAN_POINT('Ctrl Pts',(7.43760018588873,-2.55681065102966,4.29682665402984));
#12966=CARTESIAN_POINT('Ctrl Pts',(7.37455140393809,-2.44222979000476,4.36500756740177));
#12967=CARTESIAN_POINT('Ctrl Pts',(7.32043150814391,-2.32265920674659,4.42999823940972));
#12968=CARTESIAN_POINT('Ctrl Pts',(7.22351087100368,-2.05881741292851,4.55904201498614));
#12969=CARTESIAN_POINT('Ctrl Pts',(7.18339207724428,-1.91623224743013,4.62094087013212));
#12970=CARTESIAN_POINT('Ctrl Pts',(7.15082074146671,-1.76821571833791,4.67690209149419));
#12971=CARTESIAN_POINT('',(7.19731080507723,-2.82068711164422,4.12982512801404));
#12972=CARTESIAN_POINT('Ctrl Pts',(7.19924459195077,-2.81880677501399,4.1296886523242));
#12973=CARTESIAN_POINT('Ctrl Pts',(7.21211560828053,-2.8062829268458,4.13823707111259));
#12974=CARTESIAN_POINT('Ctrl Pts',(7.22487457054161,-2.79369647649002,4.14674469164499));
#12975=CARTESIAN_POINT('Ctrl Pts',(7.30716927425948,-2.71140177277215,4.2018239446048));
#12976=CARTESIAN_POINT('Ctrl Pts',(7.37554087547359,-2.63778413144905,4.24855436104107));
#12977=CARTESIAN_POINT('Ctrl Pts',(7.44191783873706,-2.56038763969479,4.29469616323415));
#12978=CARTESIAN_POINT('Ctrl Pts',(6.37917532067789,-3.03681439448832,3.9721226483366));
#12979=CARTESIAN_POINT('Ctrl Pts',(6.6575480987566,-2.98017745787073,4.01542339194582));
#12980=CARTESIAN_POINT('Ctrl Pts',(6.93157288344106,-2.90736320883569,4.06919443434768));
#12981=CARTESIAN_POINT('Ctrl Pts',(7.19690031496509,-2.8203511405513,4.12863408938004));
#12982=CARTESIAN_POINT('Origin',(4.45646910621825,0.,0.));
#12983=CARTESIAN_POINT('',(6.32992046864336,-2.62554739444332,-0.00153646747546771));
#12984=CARTESIAN_POINT('Ctrl Pts',(6.33207202947621,-2.6273817546684,8.65193333643433E-16));
#12985=CARTESIAN_POINT('Ctrl Pts',(6.34786150147485,-2.61859153627079,1.51541797368282E-15));
#12986=CARTESIAN_POINT('Ctrl Pts',(6.3635632560086,-2.6096640634631,1.86847043519414E-15));
#12987=CARTESIAN_POINT('Ctrl Pts',(6.37917529771412,-2.60059988273836,2.16580225975704E-15));
#12988=CARTESIAN_POINT('',(6.28979540306975,-2.65047774028998,5.88524282705277E-16));
#12989=CARTESIAN_POINT('Ctrl Pts',(6.28979540306975,-2.65047774028998,5.55111512312578E-16));
#12990=CARTESIAN_POINT('Ctrl Pts',(6.30271977741102,-2.64153799520552,-0.000512155825155562));
#12991=CARTESIAN_POINT('Ctrl Pts',(6.31557876201817,-2.63250371485126,-0.0010243116503117));
#12992=CARTESIAN_POINT('Ctrl Pts',(6.32837098102566,-2.62337586586299,-0.00153646747546782));
#12993=CARTESIAN_POINT('',(2.58488257447922,-2.62360084935056,5.82556414075021E-16));
#12994=CARTESIAN_POINT('Origin',(4.45646910621825,0.,0.));
#12995=CARTESIAN_POINT('',(2.70777160956256,3.52286049471024,6.63097267454378E-5));
#12996=CARTESIAN_POINT('Ctrl Pts',(2.70366602788722,3.52819471846405,1.72691722033491E-15));
#12997=CARTESIAN_POINT('Ctrl Pts',(2.6303277955966,3.48382721479545,-2.31975679365046E-15));
#12998=CARTESIAN_POINT('Ctrl Pts',(2.55868989239216,3.4369761734182,-1.18643451332771E-15));
#12999=CARTESIAN_POINT('Ctrl Pts',(2.48889033901316,3.38764193337989,-1.40339129206524E-15));
#13000=CARTESIAN_POINT('Ctrl Pts',(2.3907080577368,3.31824681553872,-1.82822104457045E-15));
#13001=CARTESIAN_POINT('Ctrl Pts',(2.29616136391543,3.24393985163692,-1.17259527911366E-15));
#13002=CARTESIAN_POINT('Ctrl Pts',(2.20540600264083,3.16513659897062,-2.1163626406917E-15));
#13003=CARTESIAN_POINT('Ctrl Pts',(2.11354814395808,3.08537604328003,-3.07159490148268E-15));
#13004=CARTESIAN_POINT('Ctrl Pts',(2.02557385752853,3.00100846009477,-3.8205868856292E-15));
#13005=CARTESIAN_POINT('Ctrl Pts',(1.9416867490807,2.91243153502283,-1.7277845820729E-15));
#13006=CARTESIAN_POINT('Ctrl Pts',(1.85792069011407,2.82398242685893,3.61997798186831E-16));
#13007=CARTESIAN_POINT('Ctrl Pts',(1.77822967842939,2.7313352228696,-2.48459787165829E-15));
#13008=CARTESIAN_POINT('Ctrl Pts',(1.70286389222234,2.63486608936521,-2.63677968348475E-15));
#13009=CARTESIAN_POINT('Ctrl Pts',(1.6781146665661,2.60318677605715,-2.68675437613003E-15));
#13010=CARTESIAN_POINT('Ctrl Pts',(1.65383227076774,2.5710952091118,-2.8599034388E-15));
#13011=CARTESIAN_POINT('Ctrl Pts',(1.63002677982222,2.53860449291447,-1.94289029309402E-16));
#13012=CARTESIAN_POINT('Ctrl Pts',(1.61755917530988,2.52158819189391,1.2749127461642E-15));
#13013=CARTESIAN_POINT('Ctrl Pts',(1.60522051376831,2.50445961085367,1.310626938495E-16));
#13014=CARTESIAN_POINT('Ctrl Pts',(1.59302690140008,2.48724166221798,-4.16333634234434E-17));
#13015=CARTESIAN_POINT('Ctrl Pts',(1.52372019925809,2.3893773705255,-1.0764802561769E-15));
#13016=CARTESIAN_POINT('Ctrl Pts',(1.458998168726,2.28849803957527,-1.59975950272218E-16));
#13017=CARTESIAN_POINT('Ctrl Pts',(1.39902498721045,2.18499850267992,-8.18789480661053E-16));
#13018=CARTESIAN_POINT('Ctrl Pts',(1.33917053664773,2.0817038673476,-1.476298735435E-15));
#13019=CARTESIAN_POINT('Ctrl Pts',(1.2840458525211,1.97579849696066,-2.5027159982132E-15));
#13020=CARTESIAN_POINT('Ctrl Pts',(1.23386201766705,1.86765533743376,-1.80411241501588E-15));
#13021=CARTESIAN_POINT('Ctrl Pts',(1.1847518022553,1.76182576352577,-1.12045456865919E-15));
#13022=CARTESIAN_POINT('Ctrl Pts',(1.14037317863941,1.65385230743519,-3.75898551344171E-16));
#13023=CARTESIAN_POINT('Ctrl Pts',(1.10097264016064,1.54407841972287,9.99200722162641E-16));
#13024=CARTESIAN_POINT('Ctrl Pts',(1.06978322653079,1.45718155684214,2.08772747025844E-15));
#13025=CARTESIAN_POINT('Ctrl Pts',(1.04171411204053,1.36915624453442,3.10028998944715E-15));
#13026=CARTESIAN_POINT('Ctrl Pts',(1.01691072758221,1.28017498851225,-9.43689570931383E-16));
#13027=CARTESIAN_POINT('Ctrl Pts',(1.01127765022899,1.25996652466321,-1.83529644040914E-15));
#13028=CARTESIAN_POINT('Ctrl Pts',(1.00581310158324,1.23970877167875,1.26058758656943E-15));
#13029=CARTESIAN_POINT('Ctrl Pts',(1.0005189403258,1.21940378536753,3.33066907387547E-16));
#13030=CARTESIAN_POINT('Ctrl Pts',(0.995361168747364,1.19962190185401,1.86042795644021E-17));
#13031=CARTESIAN_POINT('Ctrl Pts',(0.990366678191223,1.17980083040635,-4.01805598180605E-16));
#13032=CARTESIAN_POINT('Ctrl Pts',(0.985540360826723,1.15995762053482,-2.4980018054066E-16));
#13033=CARTESIAN_POINT('Ctrl Pts',(0.95842730415821,1.04848337773237,6.04128641609991E-16));
#13034=CARTESIAN_POINT('Ctrl Pts',(0.93658062937845,0.936170584254423,7.41469670808834E-16));
#13035=CARTESIAN_POINT('Ctrl Pts',(0.920192761507513,0.823356814344894,
5.55111512312578E-16));
#13036=CARTESIAN_POINT('Ctrl Pts',(0.904246281723449,0.713581551608195,
3.73772693226398E-16));
#13037=CARTESIAN_POINT('Ctrl Pts',(0.893468511491124,0.60333123086173,1.04581915629055E-15));
#13038=CARTESIAN_POINT('Ctrl Pts',(0.888084984187708,0.492918270951998,
7.21644966006352E-16));
#13039=CARTESIAN_POINT('Ctrl Pts',(0.882770527429912,0.38392190706839,4.01629923978879E-16));
#13040=CARTESIAN_POINT('Ctrl Pts',(0.882712683316618,0.27476643868936,2.31398886448546E-16));
#13041=CARTESIAN_POINT('Ctrl Pts',(0.888177025122092,0.165763420734776,
-5.55111512312578E-17));
#13042=CARTESIAN_POINT('Ctrl Pts',(0.893809155355859,0.0534133491527256,
2.12453188764699E-16));
#13043=CARTESIAN_POINT('Ctrl Pts',(0.905308962289794,-0.0587755777626049,
-8.65920908799369E-16));
#13044=CARTESIAN_POINT('Ctrl Pts',(0.922516988147342,-0.170434870117333,
8.88178419700125E-16));
#13045=CARTESIAN_POINT('Ctrl Pts',(0.92494514034144,-0.186190643496979,
1.10894341647542E-15));
#13046=CARTESIAN_POINT('Ctrl Pts',(0.92748542236121,-0.20192551582943,5.94353309524359E-16));
#13047=CARTESIAN_POINT('Ctrl Pts',(0.930136948334951,-0.21763816265144,
4.71844785465692E-16));
#13048=CARTESIAN_POINT('Ctrl Pts',(0.94852451933544,-0.326600855043117,
9.40525687969926E-16));
#13049=CARTESIAN_POINT('Ctrl Pts',(0.972258635131026,-0.434502143524435,
1.05264572258918E-15));
#13050=CARTESIAN_POINT('Ctrl Pts',(1.00109425852612,-0.541025619578607,
3.88578058618805E-16));
#13051=CARTESIAN_POINT('Ctrl Pts',(1.03041848882312,-0.649354088883701,
-1.43096128522812E-15));
#13052=CARTESIAN_POINT('Ctrl Pts',(1.06501902951245,-0.756258472851647,
2.29070670693008E-15));
#13053=CARTESIAN_POINT('Ctrl Pts',(1.10468717429828,-0.861384907347987,
1.77635683940025E-15));
#13054=CARTESIAN_POINT('Ctrl Pts',(1.14402738445883,-0.965642266718928,
2.1288356987997E-15));
#13055=CARTESIAN_POINT('Ctrl Pts',(1.18835237636573,-1.068151643539,-9.6169310269721E-16));
#13056=CARTESIAN_POINT('Ctrl Pts',(1.237498022929,-1.16853612940548,-5.55111512312578E-16));
#13057=CARTESIAN_POINT('Ctrl Pts',(1.27435271733458,-1.24381521938361,-8.96320816629977E-16));
#13058=CARTESIAN_POINT('Ctrl Pts',(1.31391921578064,-1.31789876864352,1.35933570826783E-15));
#13059=CARTESIAN_POINT('Ctrl Pts',(1.35613997129588,-1.39061245421914,2.1094237467878E-15));
#13060=CARTESIAN_POINT('Ctrl Pts',(1.37023011538891,-1.41487886761685,1.71588219329404E-15));
#13061=CARTESIAN_POINT('Ctrl Pts',(1.38461938163405,-1.43899786663544,1.51548447731389E-15));
#13062=CARTESIAN_POINT('Ctrl Pts',(1.39928390362746,-1.46292781003586,1.33226762955019E-15));
#13063=CARTESIAN_POINT('Ctrl Pts',(1.45676275832064,-1.55672328050179,6.14133443199526E-16));
#13064=CARTESIAN_POINT('Ctrl Pts',(1.51852300092247,-1.64771721479925,-1.19127808284468E-16));
#13065=CARTESIAN_POINT('Ctrl Pts',(1.58438368534009,-1.73555731024463,-5.55111512312578E-17));
#13066=CARTESIAN_POINT('Ctrl Pts',(1.65182969073821,-1.82551178921746,9.63681121344935E-18));
#13067=CARTESIAN_POINT('Ctrl Pts',(1.72357639497341,-1.91215970296754,2.66635203942124E-15));
#13068=CARTESIAN_POINT('Ctrl Pts',(1.79946346354604,-1.99507596845891,9.43689570931383E-16));
#13069=CARTESIAN_POINT('Ctrl Pts',(1.82652314050868,-2.02464210405154,3.29425628605202E-16));
#13070=CARTESIAN_POINT('Ctrl Pts',(1.85410952977247,-2.05373327548512,1.97952276092729E-15));
#13071=CARTESIAN_POINT('Ctrl Pts',(1.88221618809976,-2.08232847206164,1.94289029309402E-15));
#13072=CARTESIAN_POINT('Ctrl Pts',(1.90343708486131,-2.10391822162776,1.91523229800409E-15));
#13073=CARTESIAN_POINT('Ctrl Pts',(1.92495870310435,-2.12522891105285,6.33416430339438E-16));
#13074=CARTESIAN_POINT('Ctrl Pts',(1.94674902241761,-2.14622370228633,6.66133814775094E-16));
#13075=CARTESIAN_POINT('Ctrl Pts',(2.02283382172196,-2.21953077293877,7.80372417374885E-16));
#13076=CARTESIAN_POINT('Ctrl Pts',(2.10225777717469,-2.28905888221851,5.24876442197073E-16));
#13077=CARTESIAN_POINT('Ctrl Pts',(2.18487568646623,-2.35446233376722,2.77555756156289E-16));
#13078=CARTESIAN_POINT('Ctrl Pts',(2.26524307769197,-2.41808419037438,3.69721042132366E-17));
#13079=CARTESIAN_POINT('Ctrl Pts',(2.34863333307708,-2.47780335795739,-1.51150751606644E-15));
#13080=CARTESIAN_POINT('Ctrl Pts',(2.43493194849077,-2.53325667596464,-1.38777878078145E-15));
#13081=CARTESIAN_POINT('Ctrl Pts',(2.48398201129342,-2.56477501166252,-1.31745433574685E-15));
#13082=CARTESIAN_POINT('Ctrl Pts',(2.53397193040965,-2.59491440821501,-1.7272141774891E-15));
#13083=CARTESIAN_POINT('Ctrl Pts',(2.58488257447923,-2.62360084935056,-4.32986979603811E-15));
#13084=CARTESIAN_POINT('',(6.20516358154937,3.52286199445083,-5.04676743606953E-16));
#13085=CARTESIAN_POINT('Origin',(4.45646910621825,0.,0.));
#13086=CARTESIAN_POINT('Ctrl Pts',(6.37917532067248,3.40970963171683,-2.72004641033163E-15));
#13087=CARTESIAN_POINT('Ctrl Pts',(6.3222949445991,3.44902614310676,-3.07858945357474E-15));
#13088=CARTESIAN_POINT('Ctrl Pts',(6.26428052451075,3.48676815608406,-3.47743989805006E-15));
#13089=CARTESIAN_POINT('Ctrl Pts',(6.20516358154926,3.52286199445089,-3.88578058618805E-15));
#13090=CARTESIAN_POINT('Origin',(4.45646910621825,0.,0.));
#13091=CARTESIAN_POINT('',(8.38922139765086,0.00345161095399406,5.40416349472619));
#13092=CARTESIAN_POINT('Ctrl Pts',(8.38946759139483,0.00345189784424339,
5.40416349114816));
#13093=CARTESIAN_POINT('Ctrl Pts',(8.38934348094969,0.144859962266585,5.3970221751716));
#13094=CARTESIAN_POINT('Ctrl Pts',(8.38158931939786,0.285932740914827,5.38988085919504));
#13095=CARTESIAN_POINT('Ctrl Pts',(8.36633566017505,0.425948976110962,5.38273954321849));
#13096=CARTESIAN_POINT('Ctrl Pts',(8.35085549509945,0.568044351551121,5.37549218384331));
#13097=CARTESIAN_POINT('Ctrl Pts',(8.32765150846094,0.709051616527048,5.36824482446814));
#13098=CARTESIAN_POINT('Ctrl Pts',(8.29690900814658,0.848239565026732,5.36099746509296));
#13099=CARTESIAN_POINT('Ctrl Pts',(8.27698189787658,0.938460385377871,5.35629976881066));
#13100=CARTESIAN_POINT('Ctrl Pts',(8.25388842308756,1.02791726940828,5.35160207252836));
#13101=CARTESIAN_POINT('Ctrl Pts',(8.22768967185264,1.11641589263869,5.34690437624606));
#13102=CARTESIAN_POINT('Ctrl Pts',(8.19493248239052,1.22706873033696,5.34103068685625));
#13103=CARTESIAN_POINT('Ctrl Pts',(8.15724654742994,1.33646292603361,5.33515699746645));
#13104=CARTESIAN_POINT('Ctrl Pts',(8.11474561481755,1.44412672111228,5.32928330807664));
#13105=CARTESIAN_POINT('Ctrl Pts',(8.07229955490193,1.55165151211699,5.32341720217164));
#13106=CARTESIAN_POINT('Ctrl Pts',(8.02505101045592,1.6574499646389,5.31755109626664));
#13107=CARTESIAN_POINT('Ctrl Pts',(7.97316383541589,1.76106421848653,5.31168499036164));
#13108=CARTESIAN_POINT('Ctrl Pts',(7.92132979218209,1.86457237265819,5.30582489127436));
#13109=CARTESIAN_POINT('Ctrl Pts',(7.86486675018913,1.96590040970343,5.29996479218708));
#13110=CARTESIAN_POINT('Ctrl Pts',(7.80398685317266,2.06460987448604,5.2941046930998));
#13111=CARTESIAN_POINT('Ctrl Pts',(7.74091054835004,2.16688055158362,5.28803317500541));
#13112=CARTESIAN_POINT('Ctrl Pts',(7.67309283703732,2.26633972471172,5.28196165691101));
#13113=CARTESIAN_POINT('Ctrl Pts',(7.60082223596538,2.36252669729877,5.27589013881662));
#13114=CARTESIAN_POINT('Ctrl Pts',(7.53114837535926,2.45525759507398,5.27003677522061));
#13115=CARTESIAN_POINT('Ctrl Pts',(7.45733637921637,2.54494703243881,5.2641834116246));
#13116=CARTESIAN_POINT('Ctrl Pts',(7.37968871760434,2.63121190777325,5.2583300480286));
#13117=CARTESIAN_POINT('Ctrl Pts',(7.30205271452735,2.71746383072702,5.25247756329543));
#13118=CARTESIAN_POINT('Ctrl Pts',(7.22058246743452,2.80029190705686,5.24662507856226));
#13119=CARTESIAN_POINT('Ctrl Pts',(7.13561968331908,2.87934735404054,5.24077259382909));
#13120=CARTESIAN_POINT('Ctrl Pts',(7.05064910925681,2.95841004934754,5.23491957250164));
#13121=CARTESIAN_POINT('Ctrl Pts',(6.96218566408682,3.03369914624373,5.22906655117418));
#13122=CARTESIAN_POINT('Ctrl Pts',(6.87060620880603,3.10490435438986,5.22321352984672));
#13123=CARTESIAN_POINT('Ctrl Pts',(6.7789962100083,3.17613331084803,5.21735855642361));
#13124=CARTESIAN_POINT('Ctrl Pts',(6.6842684605794,3.24327541671102,5.21150358300051));
#13125=CARTESIAN_POINT('Ctrl Pts',(6.58683044030583,3.30606255025893,5.2056486095774));
#13126=CARTESIAN_POINT('Ctrl Pts',(6.48928198655146,3.36892084495818,5.19978700029395));
#13127=CARTESIAN_POINT('Ctrl Pts',(6.38901747841869,3.42741409186869,5.1939253910105));
#13128=CARTESIAN_POINT('Ctrl Pts',(6.28647081930378,3.48131910776706,5.18806378172705));
#13129=CARTESIAN_POINT('Ctrl Pts',(6.18385501222344,3.53526047221357,5.1821982199174));
#13130=CARTESIAN_POINT('Ctrl Pts',(6.07895436284824,3.58460726962324,5.17633265810775));
#13131=CARTESIAN_POINT('Ctrl Pts',(5.97222306208261,3.62918433608456,5.17046709629811));
#13132=CARTESIAN_POINT('Ctrl Pts',(5.86533569397726,3.67382658515048,5.16459295759845));
#13133=CARTESIAN_POINT('Ctrl Pts',(5.75661271854766,3.71368504222688,5.15871881889879));
#13134=CARTESIAN_POINT('Ctrl Pts',(5.646523851029,3.74863424520897,5.15284468019913));
#13135=CARTESIAN_POINT('Ctrl Pts',(5.61868417351413,3.75747232813555,5.15135920641089));
#13136=CARTESIAN_POINT('Ctrl Pts',(5.59075719728958,3.76599671884015,5.14987373262265));
#13137=CARTESIAN_POINT('Ctrl Pts',(5.5627506075966,3.77420590849361,5.14838825883441));
#13138=CARTESIAN_POINT('Ctrl Pts',(5.45201017581034,3.80666574086897,5.14251456944487));
#13139=CARTESIAN_POINT('Ctrl Pts',(5.33965547096268,3.83430158792593,5.13664088005533));
#13140=CARTESIAN_POINT('Ctrl Pts',(5.22614457931037,3.85695328803972,5.13076719066579));
#13141=CARTESIAN_POINT('Ctrl Pts',(5.11278024088333,3.87957574268059,5.12490108476107));
#13142=CARTESIAN_POINT('Ctrl Pts',(4.9982630856897,3.89722676737455,5.11903497885635));
#13143=CARTESIAN_POINT('Ctrl Pts',(4.88306668401858,3.90979583950555,5.11316887295164));
#13144=CARTESIAN_POINT('Ctrl Pts',(4.76798824199548,3.92235204106678,5.10730877386465));
#13145=CARTESIAN_POINT('Ctrl Pts',(4.65223234524747,3.9298365964174,5.10144867477766));
#13146=CARTESIAN_POINT('Ctrl Pts',(4.53628243620288,3.93219008090361,5.09558857569067));
#13147=CARTESIAN_POINT('Ctrl Pts',(4.41614931893485,3.93462847374153,5.08951705759617));
#13148=CARTESIAN_POINT('Ctrl Pts',(4.29580836896058,3.93155848245691,5.08344553950168));
#13149=CARTESIAN_POINT('Ctrl Pts',(4.17580312088828,3.92297280192952,5.07737402140718));
#13150=CARTESIAN_POINT('Ctrl Pts',(4.06010975731343,3.91469561176703,5.07152065781149));
#13151=CARTESIAN_POINT('Ctrl Pts',(3.9447288341557,3.90129230922499,5.0656672942158));
#13152=CARTESIAN_POINT('Ctrl Pts',(3.83014624661306,3.88280937924282,5.05981393062012));
#13153=CARTESIAN_POINT('Ctrl Pts',(3.71558086326044,3.8643292244104,5.05396144588728));
#13154=CARTESIAN_POINT('Ctrl Pts',(3.60181398494459,3.84077102442487,5.04810896115444));
#13155=CARTESIAN_POINT('Ctrl Pts',(3.48932393913495,3.812232839923,5.04225647642161));
#13156=CARTESIAN_POINT('Ctrl Pts',(3.37682357949849,3.7836920388528,5.0364034550945));
#13157=CARTESIAN_POINT('Ctrl Pts',(3.26560068557013,3.75017044719279,5.03055043376739));
#13158=CARTESIAN_POINT('Ctrl Pts',(3.15612029668761,3.71181653285184,5.02469741244029));
#13159=CARTESIAN_POINT('Ctrl Pts',(3.04660339398123,3.6734498267398,5.01884243901754));
#13160=CARTESIAN_POINT('Ctrl Pts',(2.93883054162971,3.6302477297295,5.01298746559479));
#13161=CARTESIAN_POINT('Ctrl Pts',(2.83324794308609,3.58240729894856,5.00713249217205));
#13162=CARTESIAN_POINT('Ctrl Pts',(2.72754568022847,3.53451264718414,5.00127088288896));
#13163=CARTESIAN_POINT('Ctrl Pts',(2.62403900236968,3.48196933969022,4.99540927360588));
#13164=CARTESIAN_POINT('Ctrl Pts',(2.52315067528165,3.42502099914743,4.98954766432279));
#13165=CARTESIAN_POINT('Ctrl Pts',(2.42219431845377,3.3680342579204,4.98368210251352));
#13166=CARTESIAN_POINT('Ctrl Pts',(2.32386017762171,3.30663678729406,4.97781654070425));
#13167=CARTESIAN_POINT('Ctrl Pts',(2.22854166560395,3.24111528942705,4.97195097889498));
#13168=CARTESIAN_POINT('Ctrl Pts',(2.13308377454302,3.17549798305983,4.96607684019571));
#13169=CARTESIAN_POINT('Ctrl Pts',(2.04065064124075,3.10574486231773,4.96020270149644));
#13170=CARTESIAN_POINT('Ctrl Pts',(1.95160232958478,3.03218261839848,4.95432856279716));
#13171=CARTESIAN_POINT('Ctrl Pts',(1.92908346513302,3.01357992769296,4.95284308900569));
#13172=CARTESIAN_POINT('Ctrl Pts',(1.90678087325711,2.99473382365849,4.95135761521422));
#13173=CARTESIAN_POINT('Ctrl Pts',(1.88469998808044,2.97564994631302,4.94987214142275));
#13174=CARTESIAN_POINT('Ctrl Pts',(1.79739029480277,2.90019067625882,4.94399845202725));
#13175=CARTESIAN_POINT('Ctrl Pts',(1.7132591214716,2.82075979155518,4.93812476263176));
#13176=CARTESIAN_POINT('Ctrl Pts',(1.63268938607396,2.73765540053927,4.93225107323626));
#13177=CARTESIAN_POINT('Ctrl Pts',(1.5522236737737,2.65465830509925,4.92638496732557));
#13178=CARTESIAN_POINT('Ctrl Pts',(1.47531054014492,2.56799742922099,4.92051886141487));
#13179=CARTESIAN_POINT('Ctrl Pts',(1.40229958516729,2.47801080237423,4.91465275550418));
#13180=CARTESIAN_POINT('Ctrl Pts',(1.32936339247731,2.38811632068681,4.90879265641119));
#13181=CARTESIAN_POINT('Ctrl Pts',(1.26032168925582,2.29490318082625,4.90293255731821));
#13182=CARTESIAN_POINT('Ctrl Pts',(1.19548648924436,2.19874540858966,4.89707245822522));
#13183=CARTESIAN_POINT('Ctrl Pts',(1.12831218320644,2.09911848341626,4.89100094013297));
#13184=CARTESIAN_POINT('Ctrl Pts',(1.06565394748279,1.99633076737082,4.88492942204071));
#13185=CARTESIAN_POINT('Ctrl Pts',(1.00781257590287,1.89083503667377,4.87885790394846));
#13186=CARTESIAN_POINT('Ctrl Pts',(0.952049490965552,1.78912985177413,4.87300454034678));
#13187=CARTESIAN_POINT('Ctrl Pts',(0.900763295417265,1.68490829873013,4.86715117674511));
#13188=CARTESIAN_POINT('Ctrl Pts',(0.854178336007027,1.57860387901811,4.86129781314343));
#13189=CARTESIAN_POINT('Ctrl Pts',(0.807600371171798,1.47231542055725,4.85544532840462));
#13190=CARTESIAN_POINT('Ctrl Pts',(0.765722404711504,1.3639450955676,4.84959284366581));
#13191=CARTESIAN_POINT('Ctrl Pts',(0.728721341374304,1.2539480059799,4.84374035892699));
#13192=CARTESIAN_POINT('Ctrl Pts',(0.691716885536518,1.14394083113633,4.83788733759393));
#13193=CARTESIAN_POINT('Ctrl Pts',(0.659590353436437,1.03230698679914,4.83203431626086));
#13194=CARTESIAN_POINT('Ctrl Pts',(0.632469088573365,0.919517735039361,
4.8261812949278));
#13195=CARTESIAN_POINT('Ctrl Pts',(0.60533877824483,0.806690865886492,4.82032632149911));
#13196=CARTESIAN_POINT('Ctrl Pts',(0.583217151127083,0.69270822453654,4.81447134807043));
#13197=CARTESIAN_POINT('Ctrl Pts',(0.566180509705361,0.578051585796435,
4.80861637464174));
#13198=CARTESIAN_POINT('Ctrl Pts',(0.549124559439059,0.463264998484746,
4.80275476535279));
#13199=CARTESIAN_POINT('Ctrl Pts',(0.537165158581018,0.347803297992415,
4.79689315606384));
#13200=CARTESIAN_POINT('Ctrl Pts',(0.53032677442703,0.232153807888215,4.79103154677488));
#13201=CARTESIAN_POINT('Ctrl Pts',(0.523483779100426,0.11642633448417,4.78516598495977));
#13202=CARTESIAN_POINT('Ctrl Pts',(0.521768682541085,0.000511231401446904,
4.77930042314466));
#13203=CARTESIAN_POINT('Ctrl Pts',(0.525153839506122,-0.115105489513525,
4.77343486132955));
#13204=CARTESIAN_POINT('Ctrl Pts',(0.528543946400855,-0.230891270429573,
4.76756072262453));
#13205=CARTESIAN_POINT('Ctrl Pts',(0.537049160528772,-0.346377387971861,
4.76168658391951));
#13206=CARTESIAN_POINT('Ctrl Pts',(0.550590154771058,-0.461084175223764,
4.75581244521449));
#13207=CARTESIAN_POINT('Ctrl Pts',(0.554014451045886,-0.490091648180038,
4.75432697148003));
#13208=CARTESIAN_POINT('Ctrl Pts',(0.557760532846793,-0.519049342278175,
4.75284149774556));
#13209=CARTESIAN_POINT('Ctrl Pts',(0.561826606712647,-0.547949633675161,
4.7513560240111));
#13210=CARTESIAN_POINT('Ctrl Pts',(0.577904208319941,-0.662223841853587,
4.74548233462701));
#13211=CARTESIAN_POINT('Ctrl Pts',(0.599042294759102,-0.775980164860141,
4.73960864524293));
#13212=CARTESIAN_POINT('Ctrl Pts',(0.62519794673883,-0.888735226342029,
4.73373495585884));
#13213=CARTESIAN_POINT('Ctrl Pts',(0.651319829314674,-1.00134471044683,
4.72786884995955));
#13214=CARTESIAN_POINT('Ctrl Pts',(0.682446302012626,-1.11295510504555,
4.72200274406025));
#13215=CARTESIAN_POINT('Ctrl Pts',(0.718482837491725,-1.2230893895427,4.71613663816096));
#13216=CARTESIAN_POINT('Ctrl Pts',(0.754482472017684,-1.3331108979359,4.71027653907936));
#13217=CARTESIAN_POINT('Ctrl Pts',(0.795382040814186,-1.4416589124362,4.70441643999776));
#13218=CARTESIAN_POINT('Ctrl Pts',(0.841036392686699,-1.54826848250744,
4.69855634091616));
#13219=CARTESIAN_POINT('Ctrl Pts',(0.888337849491357,-1.65872428281689,
4.69248482281963));
#13220=CARTESIAN_POINT('Ctrl Pts',(0.940743548349913,-1.76709868859664,
4.6864133047231));
#13221=CARTESIAN_POINT('Ctrl Pts',(0.998036081046421,-1.87289348613337,
4.68034178662657));
#13222=CARTESIAN_POINT('Ctrl Pts',(1.05327004717428,-1.97488699189445,4.67448842303615));
#13223=CARTESIAN_POINT('Ctrl Pts',(1.11304550150352,-2.0744826794852,4.66863505944574));
#13224=CARTESIAN_POINT('Ctrl Pts',(1.17711978984902,-2.17125702329979,4.66278169585532));
#13225=CARTESIAN_POINT('Ctrl Pts',(1.24118445765626,-2.2680168367731,4.65692921112771));
#13226=CARTESIAN_POINT('Ctrl Pts',(1.30954644805187,-2.36195580438726,4.65107672640009));
#13227=CARTESIAN_POINT('Ctrl Pts',(1.38191923705951,-2.45267855661029,4.64522424167247));
#13228=CARTESIAN_POINT('Ctrl Pts',(1.45429866168086,-2.54340962689245,4.63937122035053));
#13229=CARTESIAN_POINT('Ctrl Pts',(1.53068935828223,-2.63092357259591,4.63351819902859));
#13230=CARTESIAN_POINT('Ctrl Pts',(1.61076435577023,-2.71485791032929,4.62766517770664));
#13231=CARTESIAN_POINT('Ctrl Pts',(1.69086605981718,-2.79882024178618,4.62181020428899));
#13232=CARTESIAN_POINT('Ctrl Pts',(1.77465422310562,-2.87920029255102,4.61595523087134));
#13233=CARTESIAN_POINT('Ctrl Pts',(1.86176537078853,-2.955672770343,4.61010025745369));
#13234=CARTESIAN_POINT('Ctrl Pts',(1.94897524777021,-3.03223191986768,4.60423864817558));
#13235=CARTESIAN_POINT('Ctrl Pts',(2.03951531555244,-3.10487438422178,4.59837703889748));
#13236=CARTESIAN_POINT('Ctrl Pts',(2.13298933627094,-3.17331542060439,4.59251542961937));
#13237=CARTESIAN_POINT('Ctrl Pts',(2.22652638720913,-3.24180260728122,4.58664986781502));
#13238=CARTESIAN_POINT('Ctrl Pts',(2.32300098752248,-3.30608249623343,4.58078430601067));
#13239=CARTESIAN_POINT('Ctrl Pts',(2.42198975089452,-3.3659148463325,4.57491874420632));
#13240=CARTESIAN_POINT('Ctrl Pts',(2.52112326011971,-3.42583468600379,4.56904460551183));
#13241=CARTESIAN_POINT('Ctrl Pts',(2.62277790813312,-3.4812938105796,4.56317046681735));
#13242=CARTESIAN_POINT('Ctrl Pts',(2.72650762307617,-3.53209884726416,4.55729632812286));
#13243=CARTESIAN_POINT('Ctrl Pts',(2.75273917566813,-3.54494661217376,4.55581085428172));
#13244=CARTESIAN_POINT('Ctrl Pts',(2.77910334170824,-3.55749699254563,4.55432538044058));
#13245=CARTESIAN_POINT('Ctrl Pts',(2.80559274256743,-3.56974736248086,4.55283990659944));
#13246=CARTESIAN_POINT('Ctrl Pts',(2.91033407718839,-3.6181863627979,4.54696621721354));
#13247=CARTESIAN_POINT('Ctrl Pts',(3.01738356579454,-3.66209224752273,4.54109252782763));
#13248=CARTESIAN_POINT('Ctrl Pts',(3.12631175648758,-3.70123903915398,4.53521883844173));
#13249=CARTESIAN_POINT('Ctrl Pts',(3.23509931065145,-3.74033528859897,4.52935273254072));
#13250=CARTESIAN_POINT('Ctrl Pts',(3.34576035796865,-3.77468452576842,4.52348662663971));
#13251=CARTESIAN_POINT('Ctrl Pts',(3.45784281011898,-3.80410758532656,4.51762052073871));
#13252=CARTESIAN_POINT('Ctrl Pts',(3.56981049126493,-3.83350051604621,4.51176042165547));
#13253=CARTESIAN_POINT('Ctrl Pts',(3.68319628490271,-3.85797719849322,4.50590032257224));
#13254=CARTESIAN_POINT('Ctrl Pts',(3.79753080160516,-3.87740755024715,4.50004022348901));
#13255=CARTESIAN_POINT('Ctrl Pts',(3.91599024696327,-3.89753890478704,4.49396870539313));
#13256=CARTESIAN_POINT('Ctrl Pts',(4.03546773832967,-3.91225278090741,4.48789718729724));
#13257=CARTESIAN_POINT('Ctrl Pts',(4.15542676375039,-3.92146178204524,4.48182566920136));
#13258=CARTESIAN_POINT('Ctrl Pts',(4.27107556538731,-3.93033989640244,4.47597230560955));
#13259=CARTESIAN_POINT('Ctrl Pts',(4.38717144554922,-3.93410188254922,4.47011894201775));
#13260=CARTESIAN_POINT('Ctrl Pts',(4.50322696720433,-3.93272204744195,4.46426557842595));
#13261=CARTESIAN_POINT('Ctrl Pts',(4.61926506351249,-3.93134241951228,4.45841309369704));
#13262=CARTESIAN_POINT('Ctrl Pts',(4.73526240035798,-3.924822510319,4.45256060896812));
#13263=CARTESIAN_POINT('Ctrl Pts',(4.85073141824768,-3.91318875462368,4.44670812423921));
#13264=CARTESIAN_POINT('Ctrl Pts',(4.96621102309533,-3.90155393226923,4.44085510291606));
#13265=CARTESIAN_POINT('Ctrl Pts',(5.08116180160703,-3.88480437275884,4.43500208159291));
#13266=CARTESIAN_POINT('Ctrl Pts',(5.19510190200478,-3.86301832677358,4.42914906026976));
#13267=CARTESIAN_POINT('Ctrl Pts',(5.30908000362576,-3.84122501472138,4.423294086851));
#13268=CARTESIAN_POINT('Ctrl Pts',(5.42204635128827,-3.81439195360396,4.41743911343223));
#13269=CARTESIAN_POINT('Ctrl Pts',(5.53353055616425,-3.78264823014779,4.41158414001347));
#13270=CARTESIAN_POINT('Ctrl Pts',(5.64514111406658,-3.75086852925848,4.4057225307344));
#13271=CARTESIAN_POINT('Ctrl Pts',(5.75526577879248,-3.71416717062201,4.39986092145532));
#13272=CARTESIAN_POINT('Ctrl Pts',(5.86345047441672,-3.6727227542441,4.39399931217625));
#13273=CARTESIAN_POINT('Ctrl Pts',(5.97170811977554,-3.63125039159192,4.388133750371));
#13274=CARTESIAN_POINT('Ctrl Pts',(6.07802281329685,-3.5850287670336,4.38226818856575));
#13275=CARTESIAN_POINT('Ctrl Pts',(6.18196315672575,-3.53428341841217,4.37640262676049));
#13276=CARTESIAN_POINT('Ctrl Pts',(6.2860554864301,-3.48346386764478,4.37052848806524));
#13277=CARTESIAN_POINT('Ctrl Pts',(6.38776617555163,-3.42810758808792,4.36465434936999));
#13278=CARTESIAN_POINT('Ctrl Pts',(6.48669091161503,-3.36848458819265,4.35878021067474));
#13279=CARTESIAN_POINT('Ctrl Pts',(6.51170736323199,-3.3534069043747,4.35729473684576));
#13280=CARTESIAN_POINT('Ctrl Pts',(6.53654581130273,-3.33805656945364,4.35580926301677));
#13281=CARTESIAN_POINT('Ctrl Pts',(6.56120004923896,-3.32243836022448,4.35432378918779));
#13282=CARTESIAN_POINT('Ctrl Pts',(6.65867343535823,-3.2606899605123,4.34845079629802));
#13283=CARTESIAN_POINT('Ctrl Pts',(6.75358948814569,-3.19454559946926,4.34257780340824));
#13284=CARTESIAN_POINT('Ctrl Pts',(6.84552565595133,-3.12424355679538,4.33670481051846));
#13285=CARTESIAN_POINT('Ctrl Pts',(6.93735750783295,-3.05402128275573,4.33083848145528));
#13286=CARTESIAN_POINT('Ctrl Pts',(7.02621586872288,-2.97965095039595,4.3249721523921));
#13287=CARTESIAN_POINT('Ctrl Pts',(7.11170505525854,-2.90141535374102,4.31910582332892));
#13288=CARTESIAN_POINT('Ctrl Pts',(7.19709978829401,-2.82326619639196,4.3132459757324));
#13289=CARTESIAN_POINT('Ctrl Pts',(7.27913245113307,-2.74126054982594,4.30738612813589));
#13290=CARTESIAN_POINT('Ctrl Pts',(7.35743931745999,-2.6557222809413,4.30152628053938));
#13291=CARTESIAN_POINT('Ctrl Pts',(7.38606210988018,-2.62445626010418,4.29938438405908));
#13292=CARTESIAN_POINT('Ctrl Pts',(7.41418743616012,-2.59271864890061,4.29724248757878));
#13293=CARTESIAN_POINT('Ctrl Pts',(7.44179868886595,-2.56052656361313,4.29510059109848));
#13294=CARTESIAN_POINT('',(8.38744148431105,-0.00176345638553475,6.65416354772551));
#13295=CARTESIAN_POINT('Ctrl Pts',(8.38378142039597,-0.00176130459896508,
6.65416352203495));
#13296=CARTESIAN_POINT('Ctrl Pts',(8.38067961832936,0.766306874467471,6.61544270826197));
#13297=CARTESIAN_POINT('Ctrl Pts',(7.79186236069236,2.85135882026889,6.51054985535175));
#13298=CARTESIAN_POINT('Ctrl Pts',(4.40556007854754,4.64877272666142,6.33948496330435));
#13299=CARTESIAN_POINT('Ctrl Pts',(0.522470636039735,2.4773646541884,6.14096884589269));
#13300=CARTESIAN_POINT('Ctrl Pts',(0.242062159932001,-1.96276684409906,
5.94245272848103));
#13301=CARTESIAN_POINT('Ctrl Pts',(3.82112739871976,-4.60543380238081,5.74393661106939));
#13302=CARTESIAN_POINT('Ctrl Pts',(7.58197580057618,-3.18195140949412,5.56450687558735));
#13303=CARTESIAN_POINT('Ctrl Pts',(8.37950088367395,-0.928416374988517,
5.45124917924254));
#13304=CARTESIAN_POINT('Ctrl Pts',(8.38734236653861,0.00344942131385295,
5.40416352203495));
#13305=CARTESIAN_POINT('',(8.39081119622603,-0.00254965045452874,7.90416352203496));
#13306=CARTESIAN_POINT('Ctrl Pts',(8.38946828034982,-0.00254878017787342,
7.90416352203496));
#13307=CARTESIAN_POINT('Ctrl Pts',(8.38954213717047,0.111418998272305,7.89837421661825));
#13308=CARTESIAN_POINT('Ctrl Pts',(8.38465808761385,0.225581875715186,7.89258491120154));
#13309=CARTESIAN_POINT('Ctrl Pts',(8.37479171694471,0.339465636360686,7.88679560578483));
#13310=CARTESIAN_POINT('Ctrl Pts',(8.36493650012569,0.453220652360487,7.88101284512981));
#13311=CARTESIAN_POINT('Ctrl Pts',(8.35011019437028,0.566696758242774,7.8752300844748));
#13312=CARTESIAN_POINT('Ctrl Pts',(8.33034040981158,0.679418959991637,7.86944732381978));
#13313=CARTESIAN_POINT('Ctrl Pts',(8.31034793917893,0.793410860177514,7.86359942637671));
#13314=CARTESIAN_POINT('Ctrl Pts',(8.28529991712303,0.906631325987264,7.85775152893363));
#13315=CARTESIAN_POINT('Ctrl Pts',(8.25527900904773,1.01859330557622,7.85190363149055));
#13316=CARTESIAN_POINT('Ctrl Pts',(8.2256318969392,1.12916122552193,7.84612854731724));
#13317=CARTESIAN_POINT('Ctrl Pts',(8.19113515060747,1.23850139940321,7.84035346314393));
#13318=CARTESIAN_POINT('Ctrl Pts',(8.15191972961016,1.34615515081744,7.83457837897062));
#13319=CARTESIAN_POINT('Ctrl Pts',(8.11271233818502,1.45378685953663,7.82880447727741));
#13320=CARTESIAN_POINT('Ctrl Pts',(8.06878833770282,1.55973243241917,7.8230305755842));
#13321=CARTESIAN_POINT('Ctrl Pts',(8.02032802247892,1.66355000675945,7.81725667389099));
#13322=CARTESIAN_POINT('Ctrl Pts',(7.97186515694209,1.76737304468989,7.81148246833563));
#13323=CARTESIAN_POINT('Ctrl Pts',(7.91886568300501,1.86906747635069,7.80570826278026));
#13324=CARTESIAN_POINT('Ctrl Pts',(7.86155696974341,1.96821382011043,7.79993405722489));
#13325=CARTESIAN_POINT('Ctrl Pts',(7.80296975279677,2.06957202588276,7.79403103455498));
#13326=CARTESIAN_POINT('Ctrl Pts',(7.73987896152691,2.16826669075738,7.78812801188507));
#13327=CARTESIAN_POINT('Ctrl Pts',(7.67257493907625,2.26387991551159,7.78222498921515));
#13328=CARTESIAN_POINT('Ctrl Pts',(7.60664614522057,2.35753946742498,7.77644258349022));
#13329=CARTESIAN_POINT('Ctrl Pts',(7.53667497002743,2.44824200393647,7.77066017776528));
#13330=CARTESIAN_POINT('Ctrl Pts',(7.46297497751559,2.53562841241665,7.76487777204034));
#13331=CARTESIAN_POINT('Ctrl Pts',(7.38696898944648,2.62574905007182,7.75891444089794));
#13332=CARTESIAN_POINT('Ctrl Pts',(7.30699734734518,2.71234227061884,7.75295110975554));
#13333=CARTESIAN_POINT('Ctrl Pts',(7.22344370650432,2.79505645048034,7.74698777861314));
#13334=CARTESIAN_POINT('Ctrl Pts',(7.13989006566346,2.87777063034184,7.74102444747074));
#13335=CARTESIAN_POINT('Ctrl Pts',(7.05275483757312,2.95660549722653,7.73506111632834));
#13336=CARTESIAN_POINT('Ctrl Pts',(6.96245617822768,3.03125680121655,7.72909778518594));
#13337=CARTESIAN_POINT('Ctrl Pts',(6.87351490283744,3.10478593481108,7.72322409579537));
#13338=CARTESIAN_POINT('Ctrl Pts',(6.78118658365038,3.17451972307124,7.71735040640481));
#13339=CARTESIAN_POINT('Ctrl Pts',(6.68582891585312,3.24013021947958,7.71147671701425));
#13340=CARTESIAN_POINT('Ctrl Pts',(6.59059436376342,3.30565600657324,7.70561061110849));
#13341=CARTESIAN_POINT('Ctrl Pts',(6.49233857835877,3.36706885657886,7.69974450520274));
#13342=CARTESIAN_POINT('Ctrl Pts',(6.39145307221303,3.42408032197598,7.69387839929699));
#13343=CARTESIAN_POINT('Ctrl Pts',(6.29067087154033,3.48103340835884,7.68801830020895));
#13344=CARTESIAN_POINT('Ctrl Pts',(6.18726466387726,3.53359387279993,7.68215820112091));
#13345=CARTESIAN_POINT('Ctrl Pts',(6.08165519858878,3.58151632205766,7.67629810203288));
#13346=CARTESIAN_POINT('Ctrl Pts',(5.97223558472645,3.631167703956,7.67022658393877));
#13347=CARTESIAN_POINT('Ctrl Pts',(5.86045110676504,3.67583983813407,7.66415506584466));
#13348=CARTESIAN_POINT('Ctrl Pts',(5.74679829771543,3.71531150478264,7.65808354775055));
#13349=CARTESIAN_POINT('Ctrl Pts',(5.63722912492401,3.75336492290356,7.6522301841538));
#13350=CARTESIAN_POINT('Ctrl Pts',(5.52592399542495,3.78658500868859,7.64637682055705));
#13351=CARTESIAN_POINT('Ctrl Pts',(5.41334770981636,3.814822713833,7.6405234569603));
#13352=CARTESIAN_POINT('Ctrl Pts',(5.30078832715837,3.84305617918096,7.6346709722264));
#13353=CARTESIAN_POINT('Ctrl Pts',(5.18695856851517,3.86630865087859,7.6288184874925));
#13354=CARTESIAN_POINT('Ctrl Pts',(5.07233663553888,3.88448145655614,7.62296600275861));
#13355=CARTESIAN_POINT('Ctrl Pts',(4.95770419327007,3.90265592843602,7.61711298143043));
#13356=CARTESIAN_POINT('Ctrl Pts',(4.84227984035374,3.91574974375605,7.61125996010225));
#13357=CARTESIAN_POINT('Ctrl Pts',(4.72654946229429,3.92371579007219,7.60540693877406));
#13358=CARTESIAN_POINT('Ctrl Pts',(4.61078048591883,3.93168449321862,7.59955196535024));
#13359=CARTESIAN_POINT('Ctrl Pts',(4.49470569339517,3.93452199832943,7.59369699192642));
#13360=CARTESIAN_POINT('Ctrl Pts',(4.37881283913662,3.93223327184222,7.58784201850259));
#13361=CARTESIAN_POINT('Ctrl Pts',(4.26278863521375,3.92994195137751,7.58198040921844));
#13362=CARTESIAN_POINT('Ctrl Pts',(4.14694719442151,3.92251281121624,7.57611879993429));
#13363=CARTESIAN_POINT('Ctrl Pts',(4.03177311316667,3.91000285338591,7.57025719065014));
#13364=CARTESIAN_POINT('Ctrl Pts',(3.91652136918324,3.89748445999917,7.56439162883981));
#13365=CARTESIAN_POINT('Ctrl Pts',(3.80193828813998,3.87987848954146,7.55852606702948));
#13366=CARTESIAN_POINT('Ctrl Pts',(3.6884984975159,3.85729311100017,7.55266050521916));
#13367=CARTESIAN_POINT('Ctrl Pts',(3.5748928300947,3.83467470709597,7.54678636651883));
#13368=CARTESIAN_POINT('Ctrl Pts',(3.4624341892126,3.80706246196692,7.54091222781849));
#13369=CARTESIAN_POINT('Ctrl Pts',(3.35158234214481,3.77461444899679,7.53503808911816));
#13370=CARTESIAN_POINT('Ctrl Pts',(3.3235497196911,3.76640887623436,7.53355261533687));
#13371=CARTESIAN_POINT('Ctrl Pts',(3.29561975116823,3.75789429531127,7.53206714155557));
#13372=CARTESIAN_POINT('Ctrl Pts',(3.26779965546345,3.74907374385225,7.53058166777428));
#13373=CARTESIAN_POINT('Ctrl Pts',(3.15779663619547,3.71419653485921,7.52470797838371));
#13374=CARTESIAN_POINT('Ctrl Pts',(3.04914672673835,3.67441567358155,7.51883428899315));
#13375=CARTESIAN_POINT('Ctrl Pts',(2.94231941308688,3.62985395116528,7.51296059960258));
#13376=CARTESIAN_POINT('Ctrl Pts',(2.83563002353313,3.58534976211896,7.50709449369682));
#13377=CARTESIAN_POINT('Ctrl Pts',(2.73075892797452,3.53607714469623,7.50122838779105));
#13378=CARTESIAN_POINT('Ctrl Pts',(2.62816075381596,3.48220871984091,7.49536228188529));
#13379=CARTESIAN_POINT('Ctrl Pts',(2.52566763888122,3.42839545556665,7.48950218279727));
#13380=CARTESIAN_POINT('Ctrl Pts',(2.42544317948749,3.3699959354944,7.48364208370925));
#13381=CARTESIAN_POINT('Ctrl Pts',(2.32792167373385,3.30723068860702,7.47778198462123));
#13382=CARTESIAN_POINT('Ctrl Pts',(2.22688181453445,3.24220101480218,7.47171046652713));
#13383=CARTESIAN_POINT('Ctrl Pts',(2.12874404094721,3.1724848295905,7.46563894843301));
#13384=CARTESIAN_POINT('Ctrl Pts',(2.03396342098152,3.09837944819477,7.45956743033891));
#13385=CARTESIAN_POINT('Ctrl Pts',(1.94258834443801,3.02693673237616,7.45371406674216));
#13386=CARTESIAN_POINT('Ctrl Pts',(1.85433367634259,2.95141508308456,7.44786070314541));
#13387=CARTESIAN_POINT('Ctrl Pts',(1.76957663598028,2.87212427540636,7.44200733954866));
#13388=CARTESIAN_POINT('Ctrl Pts',(1.68483232160248,2.79284537297621,7.43615485481476));
#13389=CARTESIAN_POINT('Ctrl Pts',(1.60358489237179,2.70979871960467,7.43030237008087));
#13390=CARTESIAN_POINT('Ctrl Pts',(1.5261765011186,2.62333266066245,7.42444988534698));
#13391=CARTESIAN_POINT('Ctrl Pts',(1.44876101255519,2.53685867394349,7.4185968640188));
#13392=CARTESIAN_POINT('Ctrl Pts',(1.37518553727407,2.44696496624988,7.41274384269063));
#13393=CARTESIAN_POINT('Ctrl Pts',(1.30575306738485,2.35403429087981,7.40689082136246));
#13394=CARTESIAN_POINT('Ctrl Pts',(1.23629744042602,2.26107262133479,7.40103584793864));
#13395=CARTESIAN_POINT('Ctrl Pts',(1.17098781359953,2.16507230082266,7.39518087451482));
#13396=CARTESIAN_POINT('Ctrl Pts',(1.11008442987535,2.06644588555749,7.389325901091));
#13397=CARTESIAN_POINT('Ctrl Pts',(1.04911201998847,1.96770768991868,7.38346429180684));
#13398=CARTESIAN_POINT('Ctrl Pts',(0.992556037941512,1.86633781064936,7.37760268252269));
#13399=CARTESIAN_POINT('Ctrl Pts',(0.94063128880457,1.76277435925413,7.37174107323854));
#13400=CARTESIAN_POINT('Ctrl Pts',(0.888671526427721,1.6591410742626,7.36587551142817));
#13401=CARTESIAN_POINT('Ctrl Pts',(0.84134938352646,1.55331164806864,7.3600099496178));
#13402=CARTESIAN_POINT('Ctrl Pts',(0.798831264922408,1.44574355330421,7.35414438780743));
#13403=CARTESIAN_POINT('Ctrl Pts',(0.756250974400965,1.33801816760309,7.34827024910711));
#13404=CARTESIAN_POINT('Ctrl Pts',(0.718488861844663,1.22854942847929,7.34239611040679));
#13405=CARTESIAN_POINT('Ctrl Pts',(0.685661341161439,1.11780937506681,7.33652197170647));
#13406=CARTESIAN_POINT('Ctrl Pts',(0.677359797093927,1.08980502340366,7.33503649792519));
#13407=CARTESIAN_POINT('Ctrl Pts',(0.669373564680903,1.06171941638128,7.3335510241439));
#13408=CARTESIAN_POINT('Ctrl Pts',(0.661704004809934,1.0335602668125,7.33206555036262));
#13409=CARTESIAN_POINT('Ctrl Pts',(0.63137791423059,0.922216599792919,7.32619186097206));
#13410=CARTESIAN_POINT('Ctrl Pts',(0.605905934843882,0.809351645023374,
7.3203181715815));
#13411=CARTESIAN_POINT('Ctrl Pts',(0.585439397109298,0.69542648151754,7.31444448219094));
#13412=CARTESIAN_POINT('Ctrl Pts',(0.564999283597626,0.581648406100308,
7.30857837628518));
#13413=CARTESIAN_POINT('Ctrl Pts',(0.549551832338061,0.466813247020311,
7.30271227037941));
#13414=CARTESIAN_POINT('Ctrl Pts',(0.539198446437092,0.351396610708885,
7.29684616447365));
#13415=CARTESIAN_POINT('Ctrl Pts',(0.528855662271394,0.236098159562734,
7.2909860653856));
#13416=CARTESIAN_POINT('Ctrl Pts',(0.523596604588073,0.120219824582288,
7.28512596629756));
#13417=CARTESIAN_POINT('Ctrl Pts',(0.523471398282406,0.00424610072730045,
7.27926586720951));
#13418=CARTESIAN_POINT('Ctrl Pts',(0.523341674818871,-0.115911690505769,
7.27319434911541));
#13419=CARTESIAN_POINT('Ctrl Pts',(0.528723311878636,-0.23617143883278,
7.2671228310213));
#13420=CARTESIAN_POINT('Ctrl Pts',(0.539613169842923,-0.355989569624379,
7.2610513129272));
#13421=CARTESIAN_POINT('Ctrl Pts',(0.550111746507598,-0.471502539220414,
7.25519794933045));
#13422=CARTESIAN_POINT('Ctrl Pts',(0.565729486075797,-0.586604633741501,
7.24934458573369));
#13423=CARTESIAN_POINT('Ctrl Pts',(0.586410576273707,-0.700810940841733,
7.24349122213694));
#13424=CARTESIAN_POINT('Ctrl Pts',(0.607088561275496,-0.815000100249152,
7.23763873740305));
#13425=CARTESIAN_POINT('Ctrl Pts',(0.632828311656819,-0.928293333247116,
7.23178625266915));
#13426=CARTESIAN_POINT('Ctrl Pts',(0.663522594372679,-1.04021428478872,
7.22593376793525));
#13427=CARTESIAN_POINT('Ctrl Pts',(0.694219691342193,-1.15214549797904,
7.22008074660708));
#13428=CARTESIAN_POINT('Ctrl Pts',(0.729872114404692,-1.26270378114022,
7.21422772527889));
#13429=CARTESIAN_POINT('Ctrl Pts',(0.770322487864552,-1.37142703342161,
7.20837470395072));
#13430=CARTESIAN_POINT('Ctrl Pts',(0.810786352305245,-1.48018654700758,
7.20251973052688));
#13431=CARTESIAN_POINT('Ctrl Pts',(0.856051205102927,-1.58710942573772,
7.19666475710303));
#13432=CARTESIAN_POINT('Ctrl Pts',(0.905911452222711,-1.69175333475471,
7.19080978367919));
#13433=CARTESIAN_POINT('Ctrl Pts',(0.955828209528095,-1.79651584420114,
7.18494817439504));
#13434=CARTESIAN_POINT('Ctrl Pts',(1.01035057877626,-1.89899385540313,7.1790865651109));
#13435=CARTESIAN_POINT('Ctrl Pts',(1.06922685930345,-1.99876936156115,7.17322495582675));
#13436=CARTESIAN_POINT('Ctrl Pts',(1.12814284053891,-2.09861214707559,7.16735939401642));
#13437=CARTESIAN_POINT('Ctrl Pts',(1.19141835408643,-2.19574845358574,7.16149383220609));
#13438=CARTESIAN_POINT('Ctrl Pts',(1.25875919173999,-2.28979044954935,7.15562827039576));
#13439=CARTESIAN_POINT('Ctrl Pts',(1.32619849821487,-2.38396995797673,7.14975413169542));
#13440=CARTESIAN_POINT('Ctrl Pts',(1.39771473835196,-2.47504580212225,7.14387999299507));
#13441=CARTESIAN_POINT('Ctrl Pts',(1.47297436304945,-2.56266426156141,7.13800585429473));
#13442=CARTESIAN_POINT('Ctrl Pts',(1.49200629351248,-2.58482153957106,7.13652038051348));
#13443=CARTESIAN_POINT('Ctrl Pts',(1.51127743693832,-2.60675790802619,7.13503490673223));
#13444=CARTESIAN_POINT('Ctrl Pts',(1.53078204993991,-2.62846804217311,7.13354943295097));
#13445=CARTESIAN_POINT('Ctrl Pts',(1.60790494493833,-2.71431175494393,7.12767574356041));
#13446=CARTESIAN_POINT('Ctrl Pts',(1.68893764981593,-2.79690122454661,7.12180205416984));
#13447=CARTESIAN_POINT('Ctrl Pts',(1.77357475394073,-2.87585933148987,7.11592836477927));
#13448=CARTESIAN_POINT('Ctrl Pts',(1.85810258361284,-2.95471549609932,7.11006225887352));
#13449=CARTESIAN_POINT('Ctrl Pts',(1.94622525867404,-3.02994934254741,7.10419615296776));
#13450=CARTESIAN_POINT('Ctrl Pts',(2.03759809489637,-3.10121783023809,7.098330047062));
#13451=CARTESIAN_POINT('Ctrl Pts',(2.12887736649824,-3.17241333990514,7.09246994797397));
#13452=CARTESIAN_POINT('Ctrl Pts',(2.22339985551396,-3.23965131485787,7.08660984888595));
#13453=CARTESIAN_POINT('Ctrl Pts',(2.32078561020942,-3.30262698542774,7.08074974979792));
#13454=CARTESIAN_POINT('Ctrl Pts',(2.42168482076202,-3.36787467452139,7.07467823170381));
#13455=CARTESIAN_POINT('Ctrl Pts',(2.52565746761902,-3.42854639602888,7.0686067136097));
#13456=CARTESIAN_POINT('Ctrl Pts',(2.63224507873663,-3.48435011121998,7.0625351955156));
#13457=CARTESIAN_POINT('Ctrl Pts',(2.73500291180405,-3.53814875432703,7.05668183191885));
#13458=CARTESIAN_POINT('Ctrl Pts',(2.84019063022018,-3.58742298538917,7.0508284683221));
#13459=CARTESIAN_POINT('Ctrl Pts',(2.94737050197106,-3.63195682830333,7.04497510472535));
#13460=CARTESIAN_POINT('Ctrl Pts',(3.05453428102504,-3.6764839846109,7.03912261999144));
#13461=CARTESIAN_POINT('Ctrl Pts',(3.16368923724138,-3.71627200952159,7.03327013525753));
#13462=CARTESIAN_POINT('Ctrl Pts',(3.27437695368253,-3.75115277520304,7.02741765052361));
#13463=CARTESIAN_POINT('Ctrl Pts',(3.3850748187013,-3.78603673898243,7.02156462919542));
#13464=CARTESIAN_POINT('Ctrl Pts',(3.49730532924808,-3.81601242493366,7.01571160786723));
#13465=CARTESIAN_POINT('Ctrl Pts',(3.61059486349046,-3.84096156782253,7.00985858653904));
#13466=CARTESIAN_POINT('Ctrl Pts',(3.72392218197992,-3.86591903173227,7.00400361311522));
#13467=CARTESIAN_POINT('Ctrl Pts',(3.83830882323813,-3.88584653022775,6.99814863969141));
#13468=CARTESIAN_POINT('Ctrl Pts',(3.95327163533168,-3.9006770316566,6.99229366626759));
#13469=CARTESIAN_POINT('Ctrl Pts',(4.06836474300635,-3.91552434155392,6.98643205698344));
#13470=CARTESIAN_POINT('Ctrl Pts',(4.18403491491749,-3.92526307136835,6.98057044769929));
#13471=CARTESIAN_POINT('Ctrl Pts',(4.29979444734751,-3.92987812168109,6.97470883841514));
#13472=CARTESIAN_POINT('Ctrl Pts',(4.4156320372802,-3.93449628395615,6.96884327660481));
#13473=CARTESIAN_POINT('Ctrl Pts',(4.53155869559722,-3.93398388900966,6.96297771479449));
#13474=CARTESIAN_POINT('Ctrl Pts',(4.64708903134349,-3.92837791513816,6.95711215298416));
#13475=CARTESIAN_POINT('Ctrl Pts',(4.7627883007767,-3.92276374395788,6.95123801428382));
#13476=CARTESIAN_POINT('Ctrl Pts',(4.8780896812728,-3.91204116750255,6.94536387558348));
#13477=CARTESIAN_POINT('Ctrl Pts',(4.9925151186429,-3.89629871449349,6.93948973688314));
#13478=CARTESIAN_POINT('Ctrl Pts',(5.02145144374442,-3.89231770512498,6.93800426310187));
#13479=CARTESIAN_POINT('Ctrl Pts',(5.05033181643606,-3.88801592605609,6.93651878932059));
#13480=CARTESIAN_POINT('Ctrl Pts',(5.07914864874074,-3.8833953169004,6.93503331553931));
#13481=CARTESIAN_POINT('Ctrl Pts',(5.1930928491103,-3.86512503618743,6.92915962614875));
#13482=CARTESIAN_POINT('Ctrl Pts',(5.30642202853069,-3.84180515537933,6.92328593675819));
#13483=CARTESIAN_POINT('Ctrl Pts',(5.41865372452572,-3.81348787336377,6.91741224736763));
#13484=CARTESIAN_POINT('Ctrl Pts',(5.53074051885709,-3.78520715161968,6.9115461414619));
#13485=CARTESIAN_POINT('Ctrl Pts',(5.64173225068844,-3.75194195995854,6.90568003555618));
#13486=CARTESIAN_POINT('Ctrl Pts',(5.75115380371673,-3.71379597367212,6.89981392965046));
#13487=CARTESIAN_POINT('Ctrl Pts',(5.8604633104693,-3.67568904838949,6.89395383056241));
#13488=CARTESIAN_POINT('Ctrl Pts',(5.96820544875217,-3.632711404855,6.88809373147437));
#13489=CARTESIAN_POINT('Ctrl Pts',(6.07391814277246,-3.5850171009564,6.88223363238633));
#13490=CARTESIAN_POINT('Ctrl Pts',(6.18344470962372,-3.53560209538128,6.87616211429222));
#13491=CARTESIAN_POINT('Ctrl Pts',(6.29079219405587,-3.48112378161116,6.87009059619811));
#13492=CARTESIAN_POINT('Ctrl Pts',(6.39546665157674,-3.42180910032891,6.864019078104));
#13493=CARTESIAN_POINT('Ctrl Pts',(6.496380072185,-3.36462564294833,6.85816571450725));
#13494=CARTESIAN_POINT('Ctrl Pts',(6.59480885780615,-3.30294760704014,6.8523123509105));
#13495=CARTESIAN_POINT('Ctrl Pts',(6.6903342233379,-3.23702573955104,6.84645898731376));
#13496=CARTESIAN_POINT('Ctrl Pts',(6.78584524605742,-3.17111377000855,6.84060650257986));
#13497=CARTESIAN_POINT('Ctrl Pts',(6.87845337555303,-3.10095947046721,6.83475401784597));
#13498=CARTESIAN_POINT('Ctrl Pts',(6.96776882050604,-3.02685690857993,6.82890153311207));
#13499=CARTESIAN_POINT('Ctrl Pts',(7.05709245448592,-2.95274755248287,6.82304851178392));
#13500=CARTESIAN_POINT('Ctrl Pts',(7.14312248580832,-2.87468947822836,6.81719549045577));
#13501=CARTESIAN_POINT('Ctrl Pts',(7.22550278036893,-2.7930165612505,6.81134246912762));
#13502=CARTESIAN_POINT('Ctrl Pts',(7.30791055034922,-2.71131640477706,6.80548749570378));
#13503=CARTESIAN_POINT('Ctrl Pts',(7.38666586986888,-2.62599929897716,6.79963252227995));
#13504=CARTESIAN_POINT('Ctrl Pts',(7.46145049044606,-2.53743490171557,6.79377754885611));
#13505=CARTESIAN_POINT('Ctrl Pts',(7.53631986978456,-2.4487701280858,6.78791593957197));
#13506=CARTESIAN_POINT('Ctrl Pts',(7.60720930120241,-2.35685103299911,6.78205433028784));
#13507=CARTESIAN_POINT('Ctrl Pts',(7.67384170771563,-2.26207925217795,6.7761927210037));
#13508=CARTESIAN_POINT('Ctrl Pts',(7.74051904495014,-2.16724356604867,6.77032715919335));
#13509=CARTESIAN_POINT('Ctrl Pts',(7.80293341950909,-2.06955171119052,6.76446159738301));
#13510=CARTESIAN_POINT('Ctrl Pts',(7.86085276949195,-1.96943161171825,6.75859603557266));
#13511=CARTESIAN_POINT('Ctrl Pts',(7.91885681177011,-1.86916511210453,6.75272189687233));
#13512=CARTESIAN_POINT('Ctrl Pts',(7.9723525216318,-1.76646364660131,6.746847758172));
#13513=CARTESIAN_POINT('Ctrl Pts',(8.0211551327337,-1.6617769201567,6.74097361947167));
#13514=CARTESIAN_POINT('Ctrl Pts',(8.03349651637322,-1.63530335606152,6.73948814569033));
#13515=CARTESIAN_POINT('Ctrl Pts',(8.04553802238277,-1.60870291690999,6.73800267190899));
#13516=CARTESIAN_POINT('Ctrl Pts',(8.05727716712034,-1.58198303042179,6.73651719812766));
#13517=CARTESIAN_POINT('Ctrl Pts',(8.1084003026791,-1.46561983620379,6.73004806607504));
#13518=CARTESIAN_POINT('Ctrl Pts',(8.153931540328,-1.34665702084391,6.72357893402242));
#13519=CARTESIAN_POINT('Ctrl Pts',(8.19362510200889,-1.22562394849566,6.7171098019698));
#13520=CARTESIAN_POINT('Ctrl Pts',(8.23315965443665,-1.10507572501514,6.71066658474599));
#13521=CARTESIAN_POINT('Ctrl Pts',(8.26690307392798,-0.98247403906862,6.70422336752219));
#13522=CARTESIAN_POINT('Ctrl Pts',(8.29465845219617,-0.858365623974744,
6.69778015029838));
#13523=CARTESIAN_POINT('Ctrl Pts',(8.32234009544139,-0.734586915676805,
6.6913540501452));
#13524=CARTESIAN_POINT('Ctrl Pts',(8.34406534138423,-0.609309719422338,
6.68492794999202));
#13525=CARTESIAN_POINT('Ctrl Pts',(8.3596866062786,-0.483096416073087,6.67850184983884));
#13526=CARTESIAN_POINT('Ctrl Pts',(8.37524543826056,-0.357387544609839,
6.67210143263455));
#13527=CARTESIAN_POINT('Ctrl Pts',(8.38474888011412,-0.230750293069467,
6.66570101543027));
#13528=CARTESIAN_POINT('Ctrl Pts',(8.3881002700853,-0.103756403703388,6.65930059822598));
#13529=CARTESIAN_POINT('Ctrl Pts',(8.38899688933635,-0.0697808989274935,
6.6575882528023));
#13530=CARTESIAN_POINT('Ctrl Pts',(8.38945344844305,-0.0357799447000208,
6.65587590737861));
#13531=CARTESIAN_POINT('Ctrl Pts',(8.38946871033935,-0.00176464821109916,
6.65416356195493));
#13532=CARTESIAN_POINT('',(8.38972787904154,0.00332410110871984,9.15416352203496));
#13533=CARTESIAN_POINT('Ctrl Pts',(8.39162089400544,0.00332570094577824,
9.15416352203496));
#13534=CARTESIAN_POINT('Ctrl Pts',(8.39372334105807,0.236557087994407,9.14234588371248));
#13535=CARTESIAN_POINT('Ctrl Pts',(8.26865424024228,1.77349980320093,9.06435620625279));
#13536=CARTESIAN_POINT('Ctrl Pts',(6.24434514927126,4.29152407052596,8.92019448965587));
#13537=CARTESIAN_POINT('Ctrl Pts',(1.81949236073018,3.82884228416074,8.72167837224421));
#13538=CARTESIAN_POINT('Ctrl Pts',(-0.190467284909431,-0.140220433735275,
8.52316225483256));
#13539=CARTESIAN_POINT('Ctrl Pts',(2.05514902234277,-3.9808719456923,8.3246461374209));
#13540=CARTESIAN_POINT('Ctrl Pts',(6.49984858445665,-4.17591665399795,8.12613002000926));
#13541=CARTESIAN_POINT('Ctrl Pts',(8.31678720259861,-1.61356007833625,7.98596914821393));
#13542=CARTESIAN_POINT('Ctrl Pts',(8.39494635335579,-0.156602103613678,
7.91198031555583));
#13543=CARTESIAN_POINT('Ctrl Pts',(8.3937869499332,-0.00255157889176684,
7.90416352203496));
#13544=CARTESIAN_POINT('',(8.38946907025241,0.000531890299595265,10.4041635220091));
#13545=CARTESIAN_POINT('Ctrl Pts',(8.38946907025241,0.000531890299602342,
10.4041635220091));
#13546=CARTESIAN_POINT('Ctrl Pts',(8.38945241340615,0.123698971527209,10.3979671066763));
#13547=CARTESIAN_POINT('Ctrl Pts',(8.38364577828166,0.246730412162652,10.3917706913436));
#13548=CARTESIAN_POINT('Ctrl Pts',(8.37211282064582,0.369084409944182,10.3855742760109));
#13549=CARTESIAN_POINT('Ctrl Pts',(8.36036117144559,0.493758522654603,10.3792603623048));
#13550=CARTESIAN_POINT('Ctrl Pts',(8.34266391787132,0.617728875751,10.3729464485986));
#13551=CARTESIAN_POINT('Ctrl Pts',(8.3191423869568,0.74043509254254,10.3666325348925));
#13552=CARTESIAN_POINT('Ctrl Pts',(8.29595163295195,0.861415725088067,10.3604074120424));
#13553=CARTESIAN_POINT('Ctrl Pts',(8.26709952108454,0.981167248167593,10.3541822891922));
#13554=CARTESIAN_POINT('Ctrl Pts',(8.23275230602851,1.09916977525348,10.3479571663421));
#13555=CARTESIAN_POINT('Ctrl Pts',(8.19767023351702,1.21969696224706,10.341598857208));
#13556=CARTESIAN_POINT('Ctrl Pts',(8.15685541023361,1.3383991161203,10.3352405480739));
#13557=CARTESIAN_POINT('Ctrl Pts',(8.11053592485518,1.45474557395325,10.3288822389398));
#13558=CARTESIAN_POINT('Ctrl Pts',(8.06421643947676,1.57109203178621,10.3225239298057));
#13559=CARTESIAN_POINT('Ctrl Pts',(8.01239250780688,1.68508249127428,10.3161656206716));
#13560=CARTESIAN_POINT('Ctrl Pts',(7.95534068950908,1.79621453163031,10.3098073115375));
#13561=CARTESIAN_POINT('Ctrl Pts',(7.90263726588178,1.89887627276674,10.3039336221469));
#13562=CARTESIAN_POINT('Ctrl Pts',(7.84532387922023,1.99938744358075,10.2980599327564));
#13563=CARTESIAN_POINT('Ctrl Pts',(7.78359976553002,2.09730555138436,10.2921862433658));
#13564=CARTESIAN_POINT('Ctrl Pts',(7.72195534346928,2.19509723771183,10.28632013746));
#13565=CARTESIAN_POINT('Ctrl Pts',(7.65591173749817,2.29030217257148,10.2804540315543));
#13566=CARTESIAN_POINT('Ctrl Pts',(7.58571484446163,2.38250081000734,10.2745879256485));
#13567=CARTESIAN_POINT('Ctrl Pts',(7.51558983214928,2.47460503721305,10.2687278265605));
#13568=CARTESIAN_POINT('Ctrl Pts',(7.4413202409521,2.56370876344788,10.2628677274725));
#13569=CARTESIAN_POINT('Ctrl Pts',(7.3631958228677,2.64942046393477,10.2570076283844));
#13570=CARTESIAN_POINT('Ctrl Pts',(7.28225285400916,2.73822444703552,10.2509361102903));
#13571=CARTESIAN_POINT('Ctrl Pts',(7.19717190086365,2.8233866481401,10.2448645921962));
#13572=CARTESIAN_POINT('Ctrl Pts',(7.10832188785066,2.90450784549612,10.2387930741021));
#13573=CARTESIAN_POINT('Ctrl Pts',(7.02266432681241,2.98271429340066,10.2329397105053));
#13574=CARTESIAN_POINT('Ctrl Pts',(6.93350422654221,3.05716483048509,10.2270863469086));
#13575=CARTESIAN_POINT('Ctrl Pts',(6.84120983747266,3.12753907164982,10.2212329833118));
#13576=CARTESIAN_POINT('Ctrl Pts',(6.74892930609505,3.19790274635905,10.2153804985779));
#13577=CARTESIAN_POINT('Ctrl Pts',(6.65351575009993,3.26419109167856,10.209528013844));
#13578=CARTESIAN_POINT('Ctrl Pts',(6.55536961423406,3.32612472066983,10.2036755291101));
#13579=CARTESIAN_POINT('Ctrl Pts',(6.45721447968537,3.38806402814328,10.197822507782));
#13580=CARTESIAN_POINT('Ctrl Pts',(6.35632661662856,3.44564760508633,10.1919694864538));
#13581=CARTESIAN_POINT('Ctrl Pts',(6.25313387825276,3.49864040691955,10.1861164651256));
#13582=CARTESIAN_POINT('Ctrl Pts',(6.14990672310565,3.55165088287568,10.1802614917018));
#13583=CARTESIAN_POINT('Ctrl Pts',(6.04437353139222,3.60006735054361,10.174406518278));
#13584=CARTESIAN_POINT('Ctrl Pts',(5.93698442660608,3.64370187942111,10.1685515448541));
#13585=CARTESIAN_POINT('Ctrl Pts',(5.82947361006336,3.68738586243242,10.16268993557));
#13586=CARTESIAN_POINT('Ctrl Pts',(5.72010306507971,3.72627693362288,10.1568283262858));
#13587=CARTESIAN_POINT('Ctrl Pts',(5.60934054948644,3.76023622067773,10.1509667170017));
#13588=CARTESIAN_POINT('Ctrl Pts',(5.49850334591545,3.79421840672924,10.1451011551913));
#13589=CARTESIAN_POINT('Ctrl Pts',(5.38627270172141,3.82326208351065,10.139235593381));
#13590=CARTESIAN_POINT('Ctrl Pts',(5.27312740818583,3.84727932672265,10.1333700315706));
#13591=CARTESIAN_POINT('Ctrl Pts',(5.15981666848041,3.87133168903483,10.1274958928703));
#13592=CARTESIAN_POINT('Ctrl Pts',(5.04558901620855,3.89034288170041,10.12162175417));
#13593=CARTESIAN_POINT('Ctrl Pts',(4.93092928357524,3.90427669871161,10.1157476154696));
#13594=CARTESIAN_POINT('Ctrl Pts',(4.90193370902624,3.90780033356249,10.1142621416884));
#13595=CARTESIAN_POINT('Ctrl Pts',(4.87291050496303,3.91099952969373,10.1127766679071));
#13596=CARTESIAN_POINT('Ctrl Pts',(4.8438675031252,3.91387422920997,10.1112911941258));
#13597=CARTESIAN_POINT('Ctrl Pts',(4.7290290092294,3.92524103504814,10.1054175047352));
#13598=CARTESIAN_POINT('Ctrl Pts',(4.61349855164524,3.93156820814743,10.0995438153446));
#13599=CARTESIAN_POINT('Ctrl Pts',(4.49775596818432,3.93278328859206,10.0936701259541));
#13600=CARTESIAN_POINT('Ctrl Pts',(4.38216281927222,3.93399680025369,10.0878040200483));
#13601=CARTESIAN_POINT('Ctrl Pts',(4.2663584984788,3.93011134058082,10.0819379141426));
#13602=CARTESIAN_POINT('Ctrl Pts',(4.15082885658152,3.92110609876882,10.0760718082368));
#13603=CARTESIAN_POINT('Ctrl Pts',(4.0354175155657,3.9121100782097,10.0702117091488));
#13604=CARTESIAN_POINT('Ctrl Pts',(3.92028070342867,3.89800473537621,10.0643516100607));
#13605=CARTESIAN_POINT('Ctrl Pts',(3.8059044988267,3.87882130184022,10.0584915109727));
#13606=CARTESIAN_POINT('Ctrl Pts',(3.6874018616966,3.85894577378668,10.0524199928786));
#13607=CARTESIAN_POINT('Ctrl Pts',(3.56971620191733,3.83361882040805,10.0463484747845));
#13608=CARTESIAN_POINT('Ctrl Pts',(3.45338298609684,3.80293402988006,10.0402769566904));
#13609=CARTESIAN_POINT('Ctrl Pts',(3.34122971569198,3.77335176839842,10.0344235930936));
#13610=CARTESIAN_POINT('Ctrl Pts',(3.23033380679234,3.73879018073694,10.0285702294969));
#13611=CARTESIAN_POINT('Ctrl Pts',(3.12116411357318,3.69938502681421,10.0227168659001));
#13612=CARTESIAN_POINT('Ctrl Pts',(3.01201081181605,3.65998578944272,10.0168643811662));
#13613=CARTESIAN_POINT('Ctrl Pts',(2.90458359888168,3.61574457207698,10.0110118964323));
#13614=CARTESIAN_POINT('Ctrl Pts',(2.79933433071275,3.56684641326345,10.0051594116984));
#13615=CARTESIAN_POINT('Ctrl Pts',(2.69407541259906,3.51794377114529,9.99930639037026));
#13616=CARTESIAN_POINT('Ctrl Pts',(2.59099521091513,3.46438351286954,9.99345336904209));
#13617=CARTESIAN_POINT('Ctrl Pts',(2.49052317874863,3.40639774692646,9.98760034771391));
#13618=CARTESIAN_POINT('Ctrl Pts',(2.39001763721911,3.34839264161062,9.98174537429009));
#13619=CARTESIAN_POINT('Ctrl Pts',(2.29212235254894,3.28595930008548,9.97589040086627));
#13620=CARTESIAN_POINT('Ctrl Pts',(2.1972392604409,3.21937408574227,9.97003542744246));
#13621=CARTESIAN_POINT('Ctrl Pts',(2.10224863053523,3.15271340561115,9.9641738181583));
#13622=CARTESIAN_POINT('Ctrl Pts',(2.01027734556785,3.08189169799394,9.95831220887415));
#13623=CARTESIAN_POINT('Ctrl Pts',(1.92169567700385,3.00722673946423,9.95245059959));
#13624=CARTESIAN_POINT('Ctrl Pts',(1.83305427717017,2.93251143380463,9.94658503777966));
#13625=CARTESIAN_POINT('Ctrl Pts',(1.74780734801486,2.85394799620934,9.94071947596932));
#13626=CARTESIAN_POINT('Ctrl Pts',(1.6662883303241,2.77189109415048,9.93485391415898));
#13627=CARTESIAN_POINT('Ctrl Pts',(1.58465011183569,2.6897142047751,9.92897977545866));
#13628=CARTESIAN_POINT('Ctrl Pts',(1.50675096073738,2.6040339605629,9.92310563675833));
#13629=CARTESIAN_POINT('Ctrl Pts',(1.43288413337119,2.51523814219915,9.917231498058));
#13630=CARTESIAN_POINT('Ctrl Pts',(1.41420441861529,2.49278312933758,9.91574602427672));
#13631=CARTESIAN_POINT('Ctrl Pts',(1.39578235403901,2.47012901786274,9.91426055049544));
#13632=CARTESIAN_POINT('Ctrl Pts',(1.37762223395277,2.44728235746125,9.91277507671416));
#13633=CARTESIAN_POINT('Ctrl Pts',(1.30581557803848,2.35694472343405,9.9069013873236));
#13634=CARTESIAN_POINT('Ctrl Pts',(1.23786864496497,2.26329359404981,9.90102769793303));
#13635=CARTESIAN_POINT('Ctrl Pts',(1.17410244800949,2.16669289957748,9.89515400854246));
#13636=CARTESIAN_POINT('Ctrl Pts',(1.11041857920489,2.07021692567701,9.88928790263671));
#13637=CARTESIAN_POINT('Ctrl Pts',(1.05090493774002,1.97079930153077,9.88342179673096));
#13638=CARTESIAN_POINT('Ctrl Pts',(0.995842395424703,1.8688370096245,9.87755569082521));
#13639=CARTESIAN_POINT('Ctrl Pts',(0.940836236451232,1.76697912580616,9.87169559173717));
#13640=CARTESIAN_POINT('Ctrl Pts',(0.890272305795063,1.6625821185592,9.86583549264913));
#13641=CARTESIAN_POINT('Ctrl Pts',(0.84438786718391,1.55607137452501,9.85997539356109));
#13642=CARTESIAN_POINT('Ctrl Pts',(0.796848022706831,1.44571796583597,9.85390387546698));
#13643=CARTESIAN_POINT('Ctrl Pts',(0.754331944901039,1.33309580010854,9.84783235737288));
#13644=CARTESIAN_POINT('Ctrl Pts',(0.717051272429055,1.21870556917548,9.84176083927877));
#13645=CARTESIAN_POINT('Ctrl Pts',(0.681110124312961,1.10842547065824,9.83590747568202));
#13646=CARTESIAN_POINT('Ctrl Pts',(0.650034770690332,0.996502602800106,
9.83005411208527));
#13647=CARTESIAN_POINT('Ctrl Pts',(0.623965301743936,0.883404544186814,
9.82420074848851));
#13648=CARTESIAN_POINT('Ctrl Pts',(0.597899747040573,0.770323466866426,
9.81834826375461));
#13649=CARTESIAN_POINT('Ctrl Pts',(0.576838675290042,0.656067952121766,
9.81249577902071));
#13650=CARTESIAN_POINT('Ctrl Pts',(0.560871552553867,0.541118009203235,
9.8066432942868));
#13651=CARTESIAN_POINT('Ctrl Pts',(0.544902965846919,0.426157526918307,
9.80079027295863));
#13652=CARTESIAN_POINT('Ctrl Pts',(0.534029313444819,0.310502899128489,
9.79493725163045));
#13653=CARTESIAN_POINT('Ctrl Pts',(0.528288363365169,0.194640826853502,
9.78908423030227));
#13654=CARTESIAN_POINT('Ctrl Pts',(0.522545498567798,0.0787401123398783,
9.78322925687845));
#13655=CARTESIAN_POINT('Ctrl Pts',(0.521938760476017,-0.0373677718176726,
9.77737428345463));
#13656=CARTESIAN_POINT('Ctrl Pts',(0.526453811930776,-0.153195256671141,
9.7715193100308));
#13657=CARTESIAN_POINT('Ctrl Pts',(0.530973980616423,-0.26915401710119,
9.76565770074665));
#13658=CARTESIAN_POINT('Ctrl Pts',(0.540627508959133,-0.384831330861955,
9.75979609146249));
#13659=CARTESIAN_POINT('Ctrl Pts',(0.555348094493326,-0.499743786232803,
9.75393448217834));
#13660=CARTESIAN_POINT('Ctrl Pts',(0.570078606226456,-0.614733727916248,
9.74806892036799));
#13661=CARTESIAN_POINT('Ctrl Pts',(0.589882908261818,-0.728957378173498,
9.74220335855765));
#13662=CARTESIAN_POINT('Ctrl Pts',(0.614643732160975,-0.84194227548548,
9.73633779674731));
#13663=CARTESIAN_POINT('Ctrl Pts',(0.639440762457654,-0.95509238442866,
9.73046365804698));
#13664=CARTESIAN_POINT('Ctrl Pts',(0.66920867330973,-1.0669997276802,9.72458951934664));
#13665=CARTESIAN_POINT('Ctrl Pts',(0.703780586616563,-1.17720766003696,
9.71871538064631));
#13666=CARTESIAN_POINT('Ctrl Pts',(0.712523259101106,-1.20507744697188,
9.71722990686504));
#13667=CARTESIAN_POINT('Ctrl Pts',(0.721572910325626,-1.23283866169091,
9.71574443308376));
#13668=CARTESIAN_POINT('Ctrl Pts',(0.730926364523589,-1.2604841450039,9.71425895930249));
#13669=CARTESIAN_POINT('Ctrl Pts',(0.767910716169708,-1.36979673205834,
9.70838526991192));
#13670=CARTESIAN_POINT('Ctrl Pts',(0.809771816427867,-1.47766224106937,
9.70251158052135));
#13671=CARTESIAN_POINT('Ctrl Pts',(0.856377876187989,-1.58361363200093,
9.69663789113078));
#13672=CARTESIAN_POINT('Ctrl Pts',(0.902923763146497,-1.68942822973307,
9.69077178522503));
#13673=CARTESIAN_POINT('Ctrl Pts',(0.954202261794194,-1.79333324928329,
9.68490567931928));
#13674=CARTESIAN_POINT('Ctrl Pts',(1.01003204791259,-1.89487746388452,9.67903957341353));
#13675=CARTESIAN_POINT('Ctrl Pts',(1.06580466504125,-1.99631769850363,9.67317947432549));
#13676=CARTESIAN_POINT('Ctrl Pts',(1.12611910173288,-2.09540157676892,9.66731937523745));
#13677=CARTESIAN_POINT('Ctrl Pts',(1.19074652517804,-2.19169911796397,9.66145927614942));
#13678=CARTESIAN_POINT('Ctrl Pts',(1.25770555862236,-2.2914708547555,9.65538775805531));
#13679=CARTESIAN_POINT('Ctrl Pts',(1.32929447810303,-2.3882509957593,9.6493162399612));
#13680=CARTESIAN_POINT('Ctrl Pts',(1.4052072796758,-2.48159026954186,9.6432447218671));
#13681=CARTESIAN_POINT('Ctrl Pts',(1.47839247362007,-2.57157578862252,9.63739135827035));
#13682=CARTESIAN_POINT('Ctrl Pts',(1.55559589300616,-2.65836310329154,9.6315379946736));
#13683=CARTESIAN_POINT('Ctrl Pts',(1.63650057209977,-2.74158101587053,9.62568463107685));
#13684=CARTESIAN_POINT('Ctrl Pts',(1.71739310362806,-2.82478643355997,9.61983214634295));
#13685=CARTESIAN_POINT('Ctrl Pts',(1.80198550194642,-2.90442321865073,9.61397966160904));
#13686=CARTESIAN_POINT('Ctrl Pts',(1.88992291191788,-2.98015597452923,9.60812717687514));
#13687=CARTESIAN_POINT('Ctrl Pts',(1.97786838456911,-3.05589567408459,9.60227415554697));
#13688=CARTESIAN_POINT('Ctrl Pts',(2.06915916547981,-3.12773036324282,9.5964211342188));
#13689=CARTESIAN_POINT('Ctrl Pts',(2.16340675036543,-3.19536445999055,9.59056811289063));
#13690=CARTESIAN_POINT('Ctrl Pts',(2.25768576864082,-3.26302111401577,9.58471313946681));
#13691=CARTESIAN_POINT('Ctrl Pts',(2.35492321633055,-3.3264741491004,9.57885816604298));
#13692=CARTESIAN_POINT('Ctrl Pts',(2.45470161311127,-3.38547129710772,9.57300319261916));
#13693=CARTESIAN_POINT('Ctrl Pts',(2.55459309588865,-3.44453531080437,9.56714158333501));
#13694=CARTESIAN_POINT('Ctrl Pts',(2.65703091991477,-3.49913314718241,9.56127997405085));
#13695=CARTESIAN_POINT('Ctrl Pts',(2.76157292733018,-3.54905845863246,9.5554183647667));
#13696=CARTESIAN_POINT('Ctrl Pts',(2.86618542818888,-3.59901743508664,9.54955280295636));
#13697=CARTESIAN_POINT('Ctrl Pts',(2.97290455832861,-3.64429745186445,9.54368724114602));
#13698=CARTESIAN_POINT('Ctrl Pts',(3.08126973229157,-3.68474092467186,9.53782167933568));
#13699=CARTESIAN_POINT('Ctrl Pts',(3.18979336271725,-3.72524353575596,9.53194754063535));
#13700=CARTESIAN_POINT('Ctrl Pts',(3.29996744900717,-3.76089536180044,9.52607340193502));
#13701=CARTESIAN_POINT('Ctrl Pts',(3.41131780240822,-3.79158908007503,9.52019926323468));
#13702=CARTESIAN_POINT('Ctrl Pts',(3.43947648897517,-3.79935102034795,9.5187137894534));
#13703=CARTESIAN_POINT('Ctrl Pts',(3.46771035755175,-3.80679614594589,9.51722831567212));
#13704=CARTESIAN_POINT('Ctrl Pts',(3.49601167060103,-3.8139232444253,9.51574284189084));
#13705=CARTESIAN_POINT('Ctrl Pts',(3.60791746408699,-3.84210439662843,9.50986915250028));
#13706=CARTESIAN_POINT('Ctrl Pts',(3.72125099834294,-3.86540310393352,9.50399546310971));
#13707=CARTESIAN_POINT('Ctrl Pts',(3.8355483718316,-3.88367692291837,9.49812177371915));
#13708=CARTESIAN_POINT('Ctrl Pts',(3.94969817667328,-3.90192714868616,9.49225566781339));
#13709=CARTESIAN_POINT('Ctrl Pts',(4.06480894179248,-3.91516532321931,9.48638956190764));
#13710=CARTESIAN_POINT('Ctrl Pts',(4.18040320021251,-3.92329920035946,9.48052345600189));
#13711=CARTESIAN_POINT('Ctrl Pts',(4.29587909158459,-3.93142474851305,9.47466335691385));
#13712=CARTESIAN_POINT('Ctrl Pts',(4.41183708180411,-3.93445636685655,9.46880325782581));
#13713=CARTESIAN_POINT('Ctrl Pts',(4.52779180225849,-3.93235324875952,9.46294315873777));
#13714=CARTESIAN_POINT('Ctrl Pts',(4.64792990449177,-3.93017425495952,9.45687164064366));
#13715=CARTESIAN_POINT('Ctrl Pts',(4.76806405056415,-3.92248295906189,9.45080012254955));
#13716=CARTESIAN_POINT('Ctrl Pts',(4.88765082651595,-3.90929294426513,9.44472860445545));
#13717=CARTESIAN_POINT('Ctrl Pts',(5.0029407540364,-3.89657685724121,9.4388752408587));
#13718=CARTESIAN_POINT('Ctrl Pts',(5.11772152352217,-3.87875044681698,9.43302187726195));
#13719=CARTESIAN_POINT('Ctrl Pts',(5.23150938451202,-3.85587883199438,9.4271685136652));
#13720=CARTESIAN_POINT('Ctrl Pts',(5.34528016063744,-3.83301065126777,9.4213160289313));
#13721=CARTESIAN_POINT('Ctrl Pts',(5.45805791976276,-3.80509885377081,9.41546354419739));
#13722=CARTESIAN_POINT('Ctrl Pts',(5.56936845513688,-3.77225980536554,9.40961105946349));
#13723=CARTESIAN_POINT('Ctrl Pts',(5.6806891961926,-3.73941774606044,9.40375803813532));
#13724=CARTESIAN_POINT('Ctrl Pts',(5.79054204979292,-3.70164765469671,9.39790501680714));
#13725=CARTESIAN_POINT('Ctrl Pts',(5.89846802418478,-3.6591157566526,9.39205199547897));
#13726=CARTESIAN_POINT('Ctrl Pts',(6.0064299939734,-3.61656967339911,9.38619702205515));
#13727=CARTESIAN_POINT('Ctrl Pts',(6.11246342250275,-3.56925877688499,9.38034204863132));
#13728=CARTESIAN_POINT('Ctrl Pts',(6.21613000682399,-3.51739712214577,9.3744870752075));
#13729=CARTESIAN_POINT('Ctrl Pts',(6.31991408390305,-3.46547668888231,9.36862546592334));
#13730=CARTESIAN_POINT('Ctrl Pts',(6.4213255929435,-3.40899538788358,9.36276385663919));
#13731=CARTESIAN_POINT('Ctrl Pts',(6.51995144044893,-3.348212904867,9.35690224735504));
#13732=CARTESIAN_POINT('Ctrl Pts',(6.6186437920876,-3.28738943577575,9.3510366855447));
#13733=CARTESIAN_POINT('Ctrl Pts',(6.71454640096287,-3.22225924102633,9.34517112373436));
#13734=CARTESIAN_POINT('Ctrl Pts',(6.80727715999856,-3.15312392624864,9.33930556192402));
#13735=CARTESIAN_POINT('Ctrl Pts',(6.90014351414779,-3.08388751868411,9.33343142322368));
#13736=CARTESIAN_POINT('Ctrl Pts',(6.98982844338462,-3.01063456339955,9.32755728452334));
#13737=CARTESIAN_POINT('Ctrl Pts',(7.07598470134355,-2.93370534425244,9.32168314582301));
#13738=CARTESIAN_POINT('Ctrl Pts',(7.09777221246983,-2.91425120060912,9.32019767204173));
#13739=CARTESIAN_POINT('Ctrl Pts',(7.11933425862108,-2.89456213268461,9.31871219826045));
#13740=CARTESIAN_POINT('Ctrl Pts',(7.14066562637913,-2.87464398511472,9.31722672447918));
#13741=CARTESIAN_POINT('Ctrl Pts',(7.22376073689112,-2.79705399218563,9.31144014719928));
#13742=CARTESIAN_POINT('Ctrl Pts',(7.30364702188168,-2.71571004166237,9.30565356991938));
#13743=CARTESIAN_POINT('Ctrl Pts',(7.37995847202851,-2.63091218553458,9.29986699263949));
#13744=CARTESIAN_POINT('Ctrl Pts',(7.4600205031988,-2.54194665562505,9.29379601469763));
#13745=CARTESIAN_POINT('Ctrl Pts',(7.53614695790885,-2.44917930042223,9.28772503675578));
#13746=CARTESIAN_POINT('Ctrl Pts',(7.60795436220654,-2.35300439465982,9.28165405881392));
#13747=CARTESIAN_POINT('Ctrl Pts',(7.67622775464223,-2.26156275089337,9.27588186493577));
#13748=CARTESIAN_POINT('Ctrl Pts',(7.74059676747692,-2.1670413478874,9.27010967105763));
#13749=CARTESIAN_POINT('Ctrl Pts',(7.80077050348256,-2.06981573195683,9.26433747717948));
#13750=CARTESIAN_POINT('Ctrl Pts',(7.860907062838,-1.97265018413826,9.25856884948896));
#13751=CARTESIAN_POINT('Ctrl Pts',(7.91685327154823,-1.87278410434854,9.25280022179843));
#13752=CARTESIAN_POINT('Ctrl Pts',(7.96836070555525,-1.770623165585,9.24703159410791));
#13753=CARTESIAN_POINT('Ctrl Pts',(8.01984963901964,-1.6684989211907,9.24126503840456));
#13754=CARTESIAN_POINT('Ctrl Pts',(8.06690277522152,-1.56408183666917,9.23549848270121));
#13755=CARTESIAN_POINT('Ctrl Pts',(8.10931738031529,-1.45780262258862,9.22973192699786));
#13756=CARTESIAN_POINT('Ctrl Pts',(8.15172771930584,-1.35153409817726,9.22396595130042));
#13757=CARTESIAN_POINT('Ctrl Pts',(8.18950029855435,-1.24340421331412,9.21819997560299));
#13758=CARTESIAN_POINT('Ctrl Pts',(8.22248066516845,-1.13386328005343,9.21243399990555));
#13759=CARTESIAN_POINT('Ctrl Pts',(8.25547959033317,-1.02426070645439,9.20666477960647));
#13760=CARTESIAN_POINT('Ctrl Pts',(8.28368079446724,-0.913245907583533,
9.20089555930738));
#13761=CARTESIAN_POINT('Ctrl Pts',(8.30697991638799,-0.801283658117368,
9.19512633900829));
#13762=CARTESIAN_POINT('Ctrl Pts',(8.33028668955545,-0.689284641137116,
9.18935522414305));
#13763=CARTESIAN_POINT('Ctrl Pts',(8.34868810447865,-0.576337974560135,
9.18358410927781));
#13764=CARTESIAN_POINT('Ctrl Pts',(8.36213133903415,-0.462916324140246,
9.17781299441257));
#13765=CARTESIAN_POINT('Ctrl Pts',(8.37558884384286,-0.349374274447022,
9.17203575339739));
#13766=CARTESIAN_POINT('Ctrl Pts',(8.38407763076053,-0.235356659269688,
9.16625851238221));
#13767=CARTESIAN_POINT('Ctrl Pts',(8.38759692383704,-0.121338705876156,
9.16048127136704));
#13768=CARTESIAN_POINT('Ctrl Pts',(8.38887977444717,-0.0797769496096529,
9.15837535492301));
#13769=CARTESIAN_POINT('Ctrl Pts',(8.38950280738372,-0.0382151267219463,
9.15626943847898));
#13770=CARTESIAN_POINT('Ctrl Pts',(8.38946770166849,0.00332388122593439,
9.15416352203496));
#13771=CARTESIAN_POINT('',(8.38946746815912,-0.0035895640966767,11.654163522035));
#13772=CARTESIAN_POINT('Ctrl Pts',(8.38946746815912,-0.0035895640966767,
11.654163522035));
#13773=CARTESIAN_POINT('Ctrl Pts',(8.38957177719058,0.110699312995978,11.6483796262953));
#13774=CARTESIAN_POINT('Ctrl Pts',(8.38469020710796,0.225131832695754,11.6425957305555));
#13775=CARTESIAN_POINT('Ctrl Pts',(8.37481197693192,0.339231701831254,11.6368118348158));
#13776=CARTESIAN_POINT('Ctrl Pts',(8.36494112420078,0.453246356765222,11.6310322587134));
#13777=CARTESIAN_POINT('Ctrl Pts',(8.35008106722861,0.566928433243951,11.625252682611));
#13778=CARTESIAN_POINT('Ctrl Pts',(8.33027309159042,0.679802679396528,11.6194731065086));
#13779=CARTESIAN_POINT('Ctrl Pts',(8.31047288488467,0.792632654877085,11.6136957972273));
#13780=CARTESIAN_POINT('Ctrl Pts',(8.28572868845862,0.904655011542767,11.607918487946));
#13781=CARTESIAN_POINT('Ctrl Pts',(8.2561334371495,1.01540138479756,11.6021411786646));
#13782=CARTESIAN_POINT('Ctrl Pts',(8.22654219053135,1.12613277237115,11.5963646511418));
#13783=CARTESIAN_POINT('Ctrl Pts',(8.19210130352364,1.23558810919518,11.5905881236189));
#13784=CARTESIAN_POINT('Ctrl Pts',(8.1529542431634,1.3433118150093,11.584811596096));
#13785=CARTESIAN_POINT('Ctrl Pts',(8.11380242285544,1.45104861910472,11.5790343661968));
#13786=CARTESIAN_POINT('Ctrl Pts',(8.06994343806426,1.55705297462456,11.5732571362976));
#13787=CARTESIAN_POINT('Ctrl Pts',(8.02156948115232,1.66088780977071,11.5674799063984));
#13788=CARTESIAN_POINT('Ctrl Pts',(7.97314712098685,1.76482654263728,11.5616968957705));
#13789=CARTESIAN_POINT('Ctrl Pts',(7.92020094699321,1.86659103422067,11.5559138851425));
#13790=CARTESIAN_POINT('Ctrl Pts',(7.862969864933,1.96576742797205,11.5501308745146));
#13791=CARTESIAN_POINT('Ctrl Pts',(7.80570950282026,2.06499456145984,11.5443449052346));
#13792=CARTESIAN_POINT('Ctrl Pts',(7.74416009704854,2.16163060308781,11.5385589359547));
#13793=CARTESIAN_POINT('Ctrl Pts',(7.67860370651661,2.25529102724241,11.5327729666747));
#13794=CARTESIAN_POINT('Ctrl Pts',(7.61294154446378,2.34910256718346,11.5269776620613));
#13795=CARTESIAN_POINT('Ctrl Pts',(7.54325974405533,2.43992856386017,11.5211823574478));
#13796=CARTESIAN_POINT('Ctrl Pts',(7.46988061977961,2.52741766432378,11.5153870528343));
#13797=CARTESIAN_POINT('Ctrl Pts',(7.40875340098826,2.60029895636267,11.510559373892));
#13798=CARTESIAN_POINT('Ctrl Pts',(7.34506123463426,2.67086518116762,11.5057316949497));
#13799=CARTESIAN_POINT('Ctrl Pts',(7.27900868446959,2.73893397678818,11.5009040160074));
#13800=CARTESIAN_POINT('Ctrl Pts',(7.19864456586121,2.82175119960764,11.4950303266169));
#13801=CARTESIAN_POINT('Ctrl Pts',(7.11449855412747,2.90116636477368,11.4891566372263));
#13802=CARTESIAN_POINT('Ctrl Pts',(7.02689032355886,2.97681436529812,11.4832829478357));
#13803=CARTESIAN_POINT('Ctrl Pts',(6.93939520344638,3.05236469714703,11.47741684193));
#13804=CARTESIAN_POINT('Ctrl Pts',(6.84844706380809,3.1241572692394,11.4715507360242));
#13805=CARTESIAN_POINT('Ctrl Pts',(6.7544035142015,3.19186253723538,11.4656846301185));
#13806=CARTESIAN_POINT('Ctrl Pts',(6.66045626399169,3.25949847589943,11.4598245310304));
#13807=CARTESIAN_POINT('Ctrl Pts',(6.56342024182953,3.32305519551627,11.4539644319424));
#13808=CARTESIAN_POINT('Ctrl Pts',(6.46368682834724,3.38224274941515,11.4481043328544));
#13809=CARTESIAN_POINT('Ctrl Pts',(6.36035526083478,3.4435656552303,11.4420328147602));
#13810=CARTESIAN_POINT('Ctrl Pts',(6.25412833768368,3.50019788883429,11.4359612966661));
#13811=CARTESIAN_POINT('Ctrl Pts',(6.14547541273053,3.55186524189217,11.429889778572));
#13812=CARTESIAN_POINT('Ctrl Pts',(6.04072647420424,3.60167614566315,11.4240364149753));
#13813=CARTESIAN_POINT('Ctrl Pts',(5.9337232750384,3.64687262031137,11.4181830513785));
#13814=CARTESIAN_POINT('Ctrl Pts',(5.82491152198139,3.68725566712431,11.4123296877818));
#13815=CARTESIAN_POINT('Ctrl Pts',(5.71611610664293,3.72763265055867,11.4064772030479));
#13816=CARTESIAN_POINT('Ctrl Pts',(5.60551306457982,3.76319749948607,11.400624718314));
#13817=CARTESIAN_POINT('Ctrl Pts',(5.49356693383226,3.79379982286339,11.3947722335801));
#13818=CARTESIAN_POINT('Ctrl Pts',(5.38161053912773,3.82440495206284,11.3889192122519));
#13819=CARTESIAN_POINT('Ctrl Pts',(5.26831120948605,3.8500465422721,11.3830661909238));
#13820=CARTESIAN_POINT('Ctrl Pts',(5.15414676086497,3.87062461241163,11.3772131695956));
#13821=CARTESIAN_POINT('Ctrl Pts',(5.03994423619526,3.891209545735,11.3713581961718));
#13822=CARTESIAN_POINT('Ctrl Pts',(4.92487642518261,3.90672752767297,11.3655032227479));
#13823=CARTESIAN_POINT('Ctrl Pts',(4.80942869842444,3.91713013905202,11.3596482493241));
#13824=CARTESIAN_POINT('Ctrl Pts',(4.69385012649667,3.92754454045489,11.35378664004));
#13825=CARTESIAN_POINT('Ctrl Pts',(4.5778911911083,3.93283196250982,11.3479250307558));
#13826=CARTESIAN_POINT('Ctrl Pts',(4.4620398160126,3.93299605481526,11.3420634214716));
#13827=CARTESIAN_POINT('Ctrl Pts',(4.34611032148418,3.93316025776935,11.3361978596613));
#13828=CARTESIAN_POINT('Ctrl Pts',(4.23028894341342,3.92819426955622,11.330332297851));
#13829=CARTESIAN_POINT('Ctrl Pts',(4.1150592936417,3.91815369018068,11.3244667360406));
#13830=CARTESIAN_POINT('Ctrl Pts',(3.99966114985995,3.90809842901547,11.3185925973403));
#13831=CARTESIAN_POINT('Ctrl Pts',(3.88485686922435,3.89295382146551,11.31271845864));
#13832=CARTESIAN_POINT('Ctrl Pts',(3.771120751629,3.87282669801552,11.3068443199397));
#13833=CARTESIAN_POINT('Ctrl Pts',(3.74235874424487,3.86773687707272,11.3053588461584));
#13834=CARTESIAN_POINT('Ctrl Pts',(3.71366497212237,3.86232867299291,11.3038733723771));
#13835=CARTESIAN_POINT('Ctrl Pts',(3.68504694311492,3.85660431549219,11.3023878985958));
#13836=CARTESIAN_POINT('Ctrl Pts',(3.57188882785466,3.83396972015761,11.2965142092052));
#13837=CARTESIAN_POINT('Ctrl Pts',(3.45953928810432,3.80631288254159,11.2906405198146));
#13838=CARTESIAN_POINT('Ctrl Pts',(3.34847842460446,3.77370449948814,11.2847668304241));
#13839=CARTESIAN_POINT('Ctrl Pts',(3.23756095111315,3.74113821692065,11.2789007245183));
#13840=CARTESIAN_POINT('Ctrl Pts',(3.12792923790653,3.70363321764498,11.2730346186126));
#13841=CARTESIAN_POINT('Ctrl Pts',(3.02005406722172,3.66131135465759,11.2671685127068));
#13842=CARTESIAN_POINT('Ctrl Pts',(2.91228935933741,3.61903282871874,11.2613084136188));
#13843=CARTESIAN_POINT('Ctrl Pts',(2.80627799857622,3.57194740002713,11.2554483145307));
#13844=CARTESIAN_POINT('Ctrl Pts',(2.70247580056403,3.52022676595133,11.2495882154427));
#13845=CARTESIAN_POINT('Ctrl Pts',(2.59492865605821,3.46664016939171,11.2435166973486));
#13846=CARTESIAN_POINT('Ctrl Pts',(2.48975352039065,3.40807772474979,11.2374451792545));
#13847=CARTESIAN_POINT('Ctrl Pts',(2.38743525415579,3.3447851827912,11.2313736611604));
#13848=CARTESIAN_POINT('Ctrl Pts',(2.28879336499758,3.2837667924474,11.2255202975636));
#13849=CARTESIAN_POINT('Ctrl Pts',(2.19280696070861,3.21835260328323,11.2196669339669));
#13850=CARTESIAN_POINT('Ctrl Pts',(2.09988488333601,3.14880926708216,11.2138135703701));
#13851=CARTESIAN_POINT('Ctrl Pts',(2.00697675790056,3.07927637257896,11.2079610856362));
#13852=CARTESIAN_POINT('Ctrl Pts',(1.91713237521333,3.00561581126974,11.2021086009023));
#13853=CARTESIAN_POINT('Ctrl Pts',(1.83072994053781,2.92813640970017,11.1962561161684));
#13854=CARTESIAN_POINT('Ctrl Pts',(1.74431958391904,2.85064990430968,11.1904030948403));
#13855=CARTESIAN_POINT('Ctrl Pts',(1.66135211026155,2.76934413845836,11.1845500735121));
#13856=CARTESIAN_POINT('Ctrl Pts',(1.58217056302627,2.68456642395089,11.1786970521839));
#13857=CARTESIAN_POINT('Ctrl Pts',(1.50296260721615,2.59976043443874,11.1728420787601));
#13858=CARTESIAN_POINT('Ctrl Pts',(1.4275433704603,2.51148049548473,11.1669871053363));
#13859=CARTESIAN_POINT('Ctrl Pts',(1.35621666378742,2.42010821931617,11.1611321319125));
#13860=CARTESIAN_POINT('Ctrl Pts',(1.28480911745379,2.32863238440851,11.1552705226283));
#13861=CARTESIAN_POINT('Ctrl Pts',(1.21750361344906,2.23405754283284,11.1494089133442));
#13862=CARTESIAN_POINT('Ctrl Pts',(1.15456159309431,2.13679567922992,11.14354730406));
#13863=CARTESIAN_POINT('Ctrl Pts',(1.09157713047297,2.03946823123806,11.1376817422496));
#13864=CARTESIAN_POINT('Ctrl Pts',(1.03296221870713,1.93945050892894,11.1318161804393));
#13865=CARTESIAN_POINT('Ctrl Pts',(0.978932307255291,1.83717903641928,11.1259506186289));
#13866=CARTESIAN_POINT('Ctrl Pts',(0.924823390821317,1.73475801793329,11.1200764799286));
#13867=CARTESIAN_POINT('Ctrl Pts',(0.875313030951348,1.63007704422919,11.1142023412283));
#13868=CARTESIAN_POINT('Ctrl Pts',(0.830568579634417,1.52359258705176,11.108328202528));
#13869=CARTESIAN_POINT('Ctrl Pts',(0.819253438354853,1.49666440620301,11.1068427287467));
#13870=CARTESIAN_POINT('Ctrl Pts',(0.80824282790806,1.46962096545336,11.1053572549654));
#13871=CARTESIAN_POINT('Ctrl Pts',(0.797538944724832,1.44246978246123,11.1038717811841));
#13872=CARTESIAN_POINT('Ctrl Pts',(0.755214882272451,1.33511170082453,11.0979980917935));
#13873=CARTESIAN_POINT('Ctrl Pts',(0.717549385894021,1.22571046622653,11.0921244024029));
#13874=CARTESIAN_POINT('Ctrl Pts',(0.684743315654432,1.1147078365185,11.0862507130124));
#13875=CARTESIAN_POINT('Ctrl Pts',(0.651979601133517,1.00384852163365,11.0803846071066));
#13876=CARTESIAN_POINT('Ctrl Pts',(0.624062951896819,0.891392315905969,
11.0745185012009));
#13877=CARTESIAN_POINT('Ctrl Pts',(0.601146189443547,0.777800879011969,
11.0686523952951));
#13878=CARTESIAN_POINT('Ctrl Pts',(0.578252893463033,0.664325758302029,
11.0627922962071));
#13879=CARTESIAN_POINT('Ctrl Pts',(0.56034938173798,0.549718121237769,11.056932197119));
#13880=CARTESIAN_POINT('Ctrl Pts',(0.547538477608263,0.43445407204298,11.051072098031));
#13881=CARTESIAN_POINT('Ctrl Pts',(0.534265385283906,0.315031558912717,
11.0450005799369));
#13882=CARTESIAN_POINT('Ctrl Pts',(0.526459425701012,0.194904808852119,
11.0389290618428));
#13883=CARTESIAN_POINT('Ctrl Pts',(0.524176940102534,0.0746144778509115,
11.0328575437487));
#13884=CARTESIAN_POINT('Ctrl Pts',(0.521976466035727,-0.0413537254237361,
11.0270041801519));
#13885=CARTESIAN_POINT('Ctrl Pts',(0.524909379816371,-0.157473508273641,
11.0211508165552));
#13886=CARTESIAN_POINT('Ctrl Pts',(0.532973249020587,-0.273256763050374,
11.0152974529584));
#13887=CARTESIAN_POINT('Ctrl Pts',(0.541035907461977,-0.389022633361006,
11.0094449682245));
#13888=CARTESIAN_POINT('Ctrl Pts',(0.554227960794191,-0.504451664032298,
11.0035924834906));
#13889=CARTESIAN_POINT('Ctrl Pts',(0.572494928317955,-0.61905862840584,
10.9977399987567));
#13890=CARTESIAN_POINT('Ctrl Pts',(0.590763570677339,-0.733676100698993,
10.9918869774286));
#13891=CARTESIAN_POINT('Ctrl Pts',(0.614107987171045,-0.847470948843617,
10.9860339561004));
#13892=CARTESIAN_POINT('Ctrl Pts',(0.642422296087036,-0.95996662969496,
10.9801809347722));
#13893=CARTESIAN_POINT('Ctrl Pts',(0.670746048371866,-1.07249983002843,
10.9743259613484));
#13894=CARTESIAN_POINT('Ctrl Pts',(0.704042888267363,-1.18373260104292,
10.9684709879246));
#13895=CARTESIAN_POINT('Ctrl Pts',(0.742156842872519,-1.29320277232904,
10.9626160145008));
#13896=CARTESIAN_POINT('Ctrl Pts',(0.780313994749741,-1.4027970139936,10.9567544052167));
#13897=CARTESIAN_POINT('Ctrl Pts',(0.823299022409682,-1.51062427828903,
10.9508927959325));
#13898=CARTESIAN_POINT('Ctrl Pts',(0.870907461752496,-1.61624153322949,
10.9450311866484));
#13899=CARTESIAN_POINT('Ctrl Pts',(0.918548003815678,-1.7219300066608,10.939165624838));
#13900=CARTESIAN_POINT('Ctrl Pts',(0.9708179795764,-1.82540513551408,10.9333000630277));
#13901=CARTESIAN_POINT('Ctrl Pts',(1.02746737159447,-1.92624923204322,10.9274345012173));
#13902=CARTESIAN_POINT('Ctrl Pts',(1.08419959891766,-2.02724078737479,10.921560362517));
#13903=CARTESIAN_POINT('Ctrl Pts',(1.14532380559521,-2.12559328275801,10.9156862238167));
#13904=CARTESIAN_POINT('Ctrl Pts',(1.2105471379429,-2.22091863332889,10.9098120851164));
#13905=CARTESIAN_POINT('Ctrl Pts',(1.22704105391523,-2.24502485829095,10.908326611335));
#13906=CARTESIAN_POINT('Ctrl Pts',(1.2437969127476,-2.26893766709304,10.9068411375537));
#13907=CARTESIAN_POINT('Ctrl Pts',(1.26080958799867,-2.29265113866297,10.9053556637724));
#13908=CARTESIAN_POINT('Ctrl Pts',(1.32807914965896,-2.38641621760626,10.8994819743818));
#13909=CARTESIAN_POINT('Ctrl Pts',(1.39959104176202,-2.47737427957364,10.8936082849913));
#13910=CARTESIAN_POINT('Ctrl Pts',(1.47508293987044,-2.56511705914367,10.8877345956007));
#13911=CARTESIAN_POINT('Ctrl Pts',(1.55047737084619,-2.65274655454214,10.881868489695));
#13912=CARTESIAN_POINT('Ctrl Pts',(1.62984132191935,-2.7371687126603,10.8760023837892));
#13913=CARTESIAN_POINT('Ctrl Pts',(1.71286970282923,-2.81800484629168,10.8701362778835));
#13914=CARTESIAN_POINT('Ctrl Pts',(1.79581306373443,-2.89875820475167,10.8642761787955));
#13915=CARTESIAN_POINT('Ctrl Pts',(1.88241309652198,-2.97593255623304,10.8584160797075));
#13916=CARTESIAN_POINT('Ctrl Pts',(1.97232546858703,-3.04918339684846,10.8525559806195));
#13917=CARTESIAN_POINT('Ctrl Pts',(2.06548167391382,-3.12507696068184,10.8464844625253));
#13918=CARTESIAN_POINT('Ctrl Pts',(2.16219343971655,-3.19675822350879,10.8404129444312));
#13919=CARTESIAN_POINT('Ctrl Pts',(2.26203699164811,-3.26388674658653,10.8343414263371));
#13920=CARTESIAN_POINT('Ctrl Pts',(2.35829308496563,-3.3286032881822,10.8284880627404));
#13921=CARTESIAN_POINT('Ctrl Pts',(2.45745941016552,-3.38908837641634,10.8226346991436));
#13922=CARTESIAN_POINT('Ctrl Pts',(2.55912448792039,-3.44507944747522,10.8167813355469));
#13923=CARTESIAN_POINT('Ctrl Pts',(2.66077430100596,-3.50106211166319,10.810928850813));
#13924=CARTESIAN_POINT('Ctrl Pts',(2.76492175885539,-3.55255190110082,10.8050763660791));
#13925=CARTESIAN_POINT('Ctrl Pts',(2.87112958719468,-3.59933155036072,10.7992238813452));
#13926=CARTESIAN_POINT('Ctrl Pts',(2.97734715336553,-3.64611548868623,10.793370860017));
#13927=CARTESIAN_POINT('Ctrl Pts',(3.08562508744303,-3.68818826180115,10.7875178386889));
#13928=CARTESIAN_POINT('Ctrl Pts',(3.19550554699996,-3.72538050436778,10.7816648173607));
#13929=CARTESIAN_POINT('Ctrl Pts',(3.30542265381301,-3.76258515126585,10.7758098439369));
#13930=CARTESIAN_POINT('Ctrl Pts',(3.41694295775744,-3.79490589851757,10.7699548705131));
#13931=CARTESIAN_POINT('Ctrl Pts',(3.52959353901836,-3.82222326440095,10.7640998970892));
#13932=CARTESIAN_POINT('Ctrl Pts',(3.64237179524336,-3.84957159100969,10.758238287805));
#13933=CARTESIAN_POINT('Ctrl Pts',(3.75628248389902,-3.87190512047532,10.7523766785209));
#13934=CARTESIAN_POINT('Ctrl Pts',(3.87084247979791,-3.88915549373222,10.7465150692367));
#13935=CARTESIAN_POINT('Ctrl Pts',(3.98547972434332,-3.90641749904248,10.7406495074264));
#13936=CARTESIAN_POINT('Ctrl Pts',(4.10076673810925,-3.91858947974171,10.734783945616));
#13937=CARTESIAN_POINT('Ctrl Pts',(4.21621699797274,-3.92565509494703,10.7289183838057));
#13938=CARTESIAN_POINT('Ctrl Pts',(4.3318360744321,-3.93273104181473,10.7230442451054));
#13939=CARTESIAN_POINT('Ctrl Pts',(4.44761846188777,-3.93468571446805,10.717170106405));
#13940=CARTESIAN_POINT('Ctrl Pts',(4.56307929081561,-3.9315548156601,10.7112959677047));
#13941=CARTESIAN_POINT('Ctrl Pts',(4.59227744953982,-3.93076306246386,10.7098104939234));
#13942=CARTESIAN_POINT('Ctrl Pts',(4.62145508086281,-3.9296463438869,10.7083250201421));
#13943=CARTESIAN_POINT('Ctrl Pts',(4.65060443016853,-3.92820575784858,10.7068395463608));
#13944=CARTESIAN_POINT('Ctrl Pts',(4.76586343097591,-3.92250955840301,10.7009658569702));
#13945=CARTESIAN_POINT('Ctrl Pts',(4.88106348107307,-3.91172678479573,10.6950921675796));
#13946=CARTESIAN_POINT('Ctrl Pts',(4.99571930325014,-3.89585654574203,10.6892184781891));
#13947=CARTESIAN_POINT('Ctrl Pts',(5.11022709398941,-3.88000679665789,10.6833523722833));
#13948=CARTESIAN_POINT('Ctrl Pts',(5.22419164864235,-3.85908270064155,10.6774862663775));
#13949=CARTESIAN_POINT('Ctrl Pts',(5.33712936104568,-3.83313533749687,10.6716201604718));
#13950=CARTESIAN_POINT('Ctrl Pts',(5.44995142667033,-3.80721454412148,10.6657600613837));
#13951=CARTESIAN_POINT('Ctrl Pts',(5.56174834125169,-3.77628080694555,10.6598999622957));
#13952=CARTESIAN_POINT('Ctrl Pts',(5.67204394948978,-3.74043671252507,10.6540398632076));
#13953=CARTESIAN_POINT('Ctrl Pts',(5.78631877164823,-3.70329944495148,10.6479683451135));
#13954=CARTESIAN_POINT('Ctrl Pts',(5.89898146736717,-3.66089088356993,10.6418968270194));
#13955=CARTESIAN_POINT('Ctrl Pts',(6.00951623119543,-3.61338257420939,10.6358253089253));
#13956=CARTESIAN_POINT('Ctrl Pts',(6.11607939262224,-3.56758127637184,10.6299719453285));
#13957=CARTESIAN_POINT('Ctrl Pts',(6.22066449496693,-3.51704057673367,10.6241185817318));
#13958=CARTESIAN_POINT('Ctrl Pts',(6.32282783693948,-3.46196390626197,10.618265218135));
#13959=CARTESIAN_POINT('Ctrl Pts',(6.42497583942988,-3.40689550536707,10.6124127334011));
#13960=CARTESIAN_POINT('Ctrl Pts',(6.52470244099266,-3.34729268384366,10.6065602486672));
#13961=CARTESIAN_POINT('Ctrl Pts',(6.62158802124141,-3.28340510504094,10.6007077639333));
#13962=CARTESIAN_POINT('Ctrl Pts',(6.71848248459706,-3.21951166860502,10.5948547426052));
#13963=CARTESIAN_POINT('Ctrl Pts',(6.81253506389509,-3.1513329213804,10.589001721277));
#13964=CARTESIAN_POINT('Ctrl Pts',(6.90335523937891,-3.07916177739106,10.5831486999488));
#13965=CARTESIAN_POINT('Ctrl Pts',(6.99420570514549,-3.00696656293117,10.577293726525));
#13966=CARTESIAN_POINT('Ctrl Pts',(7.08182130012722,-2.9307765608921,10.5714387531012));
#13967=CARTESIAN_POINT('Ctrl Pts',(7.16584524856595,-2.85092439732749,10.5655837796773));
#13968=CARTESIAN_POINT('Ctrl Pts',(7.24996442735755,-2.7709817315923,10.5597221703932));
#13969=CARTESIAN_POINT('Ctrl Pts',(7.3304835351489,-2.68736890477215,10.553860561109));
#13970=CARTESIAN_POINT('Ctrl Pts',(7.4070832225216,-2.60045483265358,10.5479989518248));
#13971=CARTESIAN_POINT('Ctrl Pts',(7.48373456162614,-2.5134821537378,10.5421333900145));
#13972=CARTESIAN_POINT('Ctrl Pts',(7.55646095918195,-2.42320411789421,10.5362678282041));
#13973=CARTESIAN_POINT('Ctrl Pts',(7.62498493500465,-2.3300206957729,10.5304022663938));
#13974=CARTESIAN_POINT('Ctrl Pts',(7.6936091096864,-2.23670101663399,10.5245281276935));
#13975=CARTESIAN_POINT('Ctrl Pts',(7.75801836990249,-2.14046781452328,10.5186539889932));
#13976=CARTESIAN_POINT('Ctrl Pts',(7.81797986457587,-2.04174788390877,10.5127798502928));
#13977=CARTESIAN_POINT('Ctrl Pts',(7.83314314769978,-2.01678322507173,10.5112943765116));
#13978=CARTESIAN_POINT('Ctrl Pts',(7.84802223176479,-1.99165964874738,10.5098089027303));
#13979=CARTESIAN_POINT('Ctrl Pts',(7.86261383551002,-1.96638426639298,10.5083234289491));
#13980=CARTESIAN_POINT('Ctrl Pts',(7.92264529898111,-1.86239856207853,10.5022120263511));
#13981=CARTESIAN_POINT('Ctrl Pts',(7.97799354213095,-1.75551901299705,10.4961006237532));
#13982=CARTESIAN_POINT('Ctrl Pts',(8.02838127406931,-1.64618725094005,10.4899892211553));
#13983=CARTESIAN_POINT('Ctrl Pts',(8.07868495492499,-1.53703786369172,10.483888012904));
#13984=CARTESIAN_POINT('Ctrl Pts',(8.12404444964126,-1.4254447391088,10.4777868046527));
#13985=CARTESIAN_POINT('Ctrl Pts',(8.16422736076993,-1.31187565180693,10.4716855964014));
#13986=CARTESIAN_POINT('Ctrl Pts',(8.20432760106104,-1.19854021735164,10.4655969405506));
#13987=CARTESIAN_POINT('Ctrl Pts',(8.23927236440555,-1.08323726646985,10.4595082846999));
#13988=CARTESIAN_POINT('Ctrl Pts',(8.26887690552271,-0.96645526114898,10.4534196288492));
#13989=CARTESIAN_POINT('Ctrl Pts',(8.29844538206055,-0.849815520958192,
10.4473383902663));
#13990=CARTESIAN_POINT('Ctrl Pts',(8.32268649854621,-0.731700666397014,
10.4412571516834));
#13991=CARTESIAN_POINT('Ctrl Pts',(8.34146469134731,-0.612615951088222,
10.4351759131006));
#13992=CARTESIAN_POINT('Ctrl Pts',(8.36021580031284,-0.493702991969284,
10.4291034455037));
#13993=CARTESIAN_POINT('Ctrl Pts',(8.37351963251434,-0.373823320362487,
10.4230309779068));
#13994=CARTESIAN_POINT('Ctrl Pts',(8.38129141016021,-0.253493357861161,
10.41695851031));
#13995=CARTESIAN_POINT('Ctrl Pts',(8.38674991623802,-0.168979638917392,
10.4126935142183));
#13996=CARTESIAN_POINT('Ctrl Pts',(8.38948053515783,-0.0842440801685602,
10.4084285181267));
#13997=CARTESIAN_POINT('Ctrl Pts',(8.38946907025248,0.000531889783886232,
10.404163522035));
#13998=CARTESIAN_POINT('',(8.39098612953365,0.00160391675724327,12.904163522035));
#13999=CARTESIAN_POINT('Ctrl Pts',(8.39513361690685,0.00160560749195398,
12.904163522035));
#14000=CARTESIAN_POINT('Ctrl Pts',(8.39559657037226,0.0911727952049497,
12.8996146273196));
#14001=CARTESIAN_POINT('Ctrl Pts',(8.35221472178778,1.48320304232387,12.8288936934674));
#14002=CARTESIAN_POINT('Ctrl Pts',(6.70306870781759,4.07019284841877,12.6920007204769));
#14003=CARTESIAN_POINT('Ctrl Pts',(2.2541571275096,4.09432552951761,12.4934846030659));
#14004=CARTESIAN_POINT('Ctrl Pts',(-0.177919035112619,0.368952773014312,
12.2949684856539));
#14005=CARTESIAN_POINT('Ctrl Pts',(1.63408930668588,-3.69429991478975,12.0964523682425));
#14006=CARTESIAN_POINT('Ctrl Pts',(6.03077938153972,-4.37438301366497,11.8979362508306));
#14007=CARTESIAN_POINT('Ctrl Pts',(8.22530950611016,-1.90438093581909,11.7505066354283));
#14008=CARTESIAN_POINT('Ctrl Pts',(8.39241825399927,-0.301695760422687,
11.669249059163));
#14009=CARTESIAN_POINT('Ctrl Pts',(8.38967060075818,-0.00358974949148719,
11.654163522035));
#14010=CARTESIAN_POINT('',(8.38946824069671,0.0026092511641729,14.1541635219886));
#14011=CARTESIAN_POINT('Ctrl Pts',(8.38946824069672,0.0026092511641433,
14.1541635219886));
#14012=CARTESIAN_POINT('Ctrl Pts',(8.38938088713637,0.134279778690723,14.1475286566465));
#14013=CARTESIAN_POINT('Ctrl Pts',(8.38267733111356,0.265695130310272,14.1408937913045));
#14014=CARTESIAN_POINT('Ctrl Pts',(8.36945840043487,0.396237029246539,14.1342589259624));
#14015=CARTESIAN_POINT('Ctrl Pts',(8.35618100728446,0.527356267020553,14.1275947170496));
#14016=CARTESIAN_POINT('Ctrl Pts',(8.33633059839447,0.6575941279414,14.1209305081367));
#14017=CARTESIAN_POINT('Ctrl Pts',(8.31005900525452,0.786342094794398,14.1142662992239));
#14018=CARTESIAN_POINT('Ctrl Pts',(8.28363708409889,0.915826767117691,14.1075639572106));
#14019=CARTESIAN_POINT('Ctrl Pts',(8.2507203850698,1.04380426791905,14.1008616151973));
#14020=CARTESIAN_POINT('Ctrl Pts',(8.21151184783421,1.16967645468195,14.0941592731839));
#14021=CARTESIAN_POINT('Ctrl Pts',(8.18704777476732,1.24821410467266,14.0899773629089));
#14022=CARTESIAN_POINT('Ctrl Pts',(8.16013517678839,1.32593255787288,14.0857954526339));
#14023=CARTESIAN_POINT('Ctrl Pts',(8.13083256144065,1.40269105612251,14.0816135423589));
#14024=CARTESIAN_POINT('Ctrl Pts',(8.089675661946,1.51050197198552,14.0757398529683));
#14025=CARTESIAN_POINT('Ctrl Pts',(8.0437012121607,1.61667951064595,14.0698661635778));
#14026=CARTESIAN_POINT('Ctrl Pts',(7.99305884784686,1.72076204032031,14.0639924741872));
#14027=CARTESIAN_POINT('Ctrl Pts',(7.94248186758305,1.82471018967061,14.0581263682814));
#14028=CARTESIAN_POINT('Ctrl Pts',(7.88724913706096,1.92656834099077,14.0522602623757));
#14029=CARTESIAN_POINT('Ctrl Pts',(7.82755918302191,2.02589256725915,14.0463941564699));
#14030=CARTESIAN_POINT('Ctrl Pts',(7.7679303507354,2.12511508678516,14.0405340573819));
#14031=CARTESIAN_POINT('Ctrl Pts',(7.7038535849314,2.22180849033266,14.0346739582939));
#14032=CARTESIAN_POINT('Ctrl Pts',(7.63557406957853,2.31555190655232,14.0288138592059));
#14033=CARTESIAN_POINT('Ctrl Pts',(7.56483118508216,2.41267737136631,14.0227423411117));
#14034=CARTESIAN_POINT('Ctrl Pts',(7.48957677189747,2.50663556622635,14.0166708230176));
#14035=CARTESIAN_POINT('Ctrl Pts',(7.41013386930994,2.59698930827036,14.0105993049235));
#14036=CARTESIAN_POINT('Ctrl Pts',(7.33354541370155,2.68409656815383,14.0047459413268));
#14037=CARTESIAN_POINT('Ctrl Pts',(7.25306457641055,2.76785360237372,13.99889257773));
#14038=CARTESIAN_POINT('Ctrl Pts',(7.16902235077852,2.84790166533635,13.9930392141333));
#14039=CARTESIAN_POINT('Ctrl Pts',(7.08499274380386,2.9279377093517,13.9871867293994));
#14040=CARTESIAN_POINT('Ctrl Pts',(6.99740311081283,3.00426560454971,13.9813342446655));
#14041=CARTESIAN_POINT('Ctrl Pts',(6.90662093107597,3.07656383570151,13.9754817599316));
#14042=CARTESIAN_POINT('Ctrl Pts',(6.8158304278321,3.14886869563041,13.9696287386034));
#14043=CARTESIAN_POINT('Ctrl Pts',(6.72184711915271,3.2171428996569,13.9637757172752));
#14044=CARTESIAN_POINT('Ctrl Pts',(6.62507057891049,3.28110601057586,13.957922695947));
#14045=CARTESIAN_POINT('Ctrl Pts',(6.5282617618232,3.34509045442754,13.9520677225232));
#14046=CARTESIAN_POINT('Ctrl Pts',(6.4286582052149,3.40476071842588,13.9462127490994));
#14047=CARTESIAN_POINT('Ctrl Pts',(6.32668677345772,3.45988076053863,13.9403577756756));
#14048=CARTESIAN_POINT('Ctrl Pts',(6.22459977018035,3.51506327413923,13.9344961663914));
#14049=CARTESIAN_POINT('Ctrl Pts',(6.12013989893483,3.56568507604074,13.9286345571073));
#14050=CARTESIAN_POINT('Ctrl Pts',(6.01375691911479,3.61155695895883,13.9227729478231));
#14051=CARTESIAN_POINT('Ctrl Pts',(5.90730220447011,3.65745977362448,13.9169073860128));
#14052=CARTESIAN_POINT('Ctrl Pts',(5.79892218439194,3.69860614533675,13.9110418242024));
#14053=CARTESIAN_POINT('Ctrl Pts',(5.68908315875057,3.73485630212193,13.9051762623921));
#14054=CARTESIAN_POINT('Ctrl Pts',(5.57908352151408,3.7711594655272,13.8993021236917));
#14055=CARTESIAN_POINT('Ctrl Pts',(5.46762101708138,3.80255201393773,13.8934279849914));
#14056=CARTESIAN_POINT('Ctrl Pts',(5.35517360749481,3.82894492247999,13.8875538462911));
#14057=CARTESIAN_POINT('Ctrl Pts',(5.32673749332848,3.83561925818277,13.8860683725098));
#14058=CARTESIAN_POINT('Ctrl Pts',(5.29823842487211,3.84197412459091,13.8845828987285));
#14059=CARTESIAN_POINT('Ctrl Pts',(5.26968418053246,3.84800860743686,13.8830974249473));
#14060=CARTESIAN_POINT('Ctrl Pts',(5.15677827525878,3.87186946470474,13.8772237355567));
#14061=CARTESIAN_POINT('Ctrl Pts',(5.04263326983356,3.89079662734252,13.8713500461661));
#14062=CARTESIAN_POINT('Ctrl Pts',(4.92771819603679,3.90466558047488,13.8654763567756));
#14063=CARTESIAN_POINT('Ctrl Pts',(4.81295148839609,3.91851662748582,13.8596102508698));
#14064=CARTESIAN_POINT('Ctrl Pts',(4.69741709600489,3.92732240320996,13.8537441449641));
#14065=CARTESIAN_POINT('Ctrl Pts',(4.58159567745767,3.93100907416529,13.8478780390583));
#14066=CARTESIAN_POINT('Ctrl Pts',(4.46589285856744,3.93469197001655,13.8420179399703));
#14067=CARTESIAN_POINT('Ctrl Pts',(4.34990400861627,3.9332661746028,13.8361578408822));
#14068=CARTESIAN_POINT('Ctrl Pts',(4.23411570566302,3.92670955957549,13.8302977417942));
#14069=CARTESIAN_POINT('Ctrl Pts',(4.11415002489481,3.91991639683605,13.8242262237001));
#14070=CARTESIAN_POINT('Ctrl Pts',(3.99440008331198,3.90761515397094,13.818154705606));
#14071=CARTESIAN_POINT('Ctrl Pts',(3.87540837177331,3.88984028243916,13.8120831875119));
#14072=CARTESIAN_POINT('Ctrl Pts',(3.76069212752601,3.87270407624683,13.8062298239151));
#14073=CARTESIAN_POINT('Ctrl Pts',(3.64668100706311,3.85048088198604,13.8003764603183));
#14074=CARTESIAN_POINT('Ctrl Pts',(3.53385590176067,3.82325435656072,13.7945230967216));
#14075=CARTESIAN_POINT('Ctrl Pts',(3.42104773676812,3.79603191910658,13.7886706119877));
#14076=CARTESIAN_POINT('Ctrl Pts',(3.30942563436249,3.76380774111252,13.7828181272538));
#14077=CARTESIAN_POINT('Ctrl Pts',(3.19945898032121,3.72671632182976,13.7769656425199));
#14078=CARTESIAN_POINT('Ctrl Pts',(3.08948224381425,3.68962150176186,13.7711126211917));
#14079=CARTESIAN_POINT('Ctrl Pts',(2.98116164889807,3.64765868533161,13.7652595998635));
#14080=CARTESIAN_POINT('Ctrl Pts',(2.87494946195351,3.60101160992363,13.7594065785354));
#14081=CARTESIAN_POINT('Ctrl Pts',(2.76870185119335,3.55434897681511,13.7535516051115));
#14082=CARTESIAN_POINT('Ctrl Pts',(2.66456442474308,3.50299914422549,13.7476966316877));
#14083=CARTESIAN_POINT('Ctrl Pts',(2.56296693781071,3.44719284900569,13.7418416582639));
#14084=CARTESIAN_POINT('Ctrl Pts',(2.46125430317672,3.39132330451836,13.7359800489797));
#14085=CARTESIAN_POINT('Ctrl Pts',(2.36208771607841,3.33098741526799,13.7301184396956));
#14086=CARTESIAN_POINT('Ctrl Pts',(2.2658699877265,3.266460546534,13.7242568304114));
#14087=CARTESIAN_POINT('Ctrl Pts',(2.16958737905366,3.20189016685848,13.7183912686011));
#14088=CARTESIAN_POINT('Ctrl Pts',(2.07625792033225,3.13312342495535,13.7125257067907));
#14089=CARTESIAN_POINT('Ctrl Pts',(1.98625184864325,3.06047638454844,13.7066601449804));
#14090=CARTESIAN_POINT('Ctrl Pts',(1.89611416600202,2.9877231163506,13.70078600628));
#14091=CARTESIAN_POINT('Ctrl Pts',(1.80930987745507,2.91107849827482,13.6949118675797));
#14092=CARTESIAN_POINT('Ctrl Pts',(1.72617289907127,2.83089590434527,13.6890377288794));
#14093=CARTESIAN_POINT('Ctrl Pts',(1.70514891445961,2.81061903533139,13.6875522550981));
#14094=CARTESIAN_POINT('Ctrl Pts',(1.68435925428379,2.79011607799048,13.6860667813168));
#14095=CARTESIAN_POINT('Ctrl Pts',(1.66380890355829,2.76939307294563,13.6845813075356));
#14096=CARTESIAN_POINT('Ctrl Pts',(1.58255107285719,2.68745255241415,13.678707618145));
#14097=CARTESIAN_POINT('Ctrl Pts',(1.50476733649224,2.60179620351846,13.6728339287545));
#14098=CARTESIAN_POINT('Ctrl Pts',(1.43081659187915,2.51275065664571,13.6669602393639));
#14099=CARTESIAN_POINT('Ctrl Pts',(1.35696132462476,2.4238200759395,13.6610941334581));
#14100=CARTESIAN_POINT('Ctrl Pts',(1.28692946921923,2.33150931416306,13.6552280275524));
#14101=CARTESIAN_POINT('Ctrl Pts',(1.22104363811249,2.23618224667236,13.6493619216466));
#14102=CARTESIAN_POINT('Ctrl Pts',(1.15522527325745,2.14095279288434,13.6435018225586));
#14103=CARTESIAN_POINT('Ctrl Pts',(1.09354472160275,2.04271351482773,13.6376417234706));
#14104=CARTESIAN_POINT('Ctrl Pts',(1.03628435636688,1.94186129187543,13.6317816243825));
#14105=CARTESIAN_POINT('Ctrl Pts',(0.97695816778506,1.8373705507997,13.6257101062884));
#14106=CARTESIAN_POINT('Ctrl Pts',(0.922377416420168,1.73007511443088,13.6196385881943));
#14107=CARTESIAN_POINT('Ctrl Pts',(0.872807241895047,1.62044951855822,13.6135670701002));
#14108=CARTESIAN_POINT('Ctrl Pts',(0.825018163356123,1.51476285795587,13.6077137065035));
#14109=CARTESIAN_POINT('Ctrl Pts',(0.78188597511973,1.40691101378852,13.6018603429067));
#14110=CARTESIAN_POINT('Ctrl Pts',(0.743601075421737,1.29734343405639,13.59600697931));
#14111=CARTESIAN_POINT('Ctrl Pts',(0.705321924072611,1.18779230552768,13.5901544945761));
#14112=CARTESIAN_POINT('Ctrl Pts',(0.671888750357873,1.07652634357975,13.5843020098422));
#14113=CARTESIAN_POINT('Ctrl Pts',(0.643442991995572,0.964012890088044,
13.5784495251083));
#14114=CARTESIAN_POINT('Ctrl Pts',(0.614994625539152,0.851489120623304,
13.5725965037801));
#14115=CARTESIAN_POINT('Ctrl Pts',(0.591534684734126,0.73771803280579,13.5667434824519));
#14116=CARTESIAN_POINT('Ctrl Pts',(0.573153951520933,0.623179275408091,
13.5608904611238));
#14117=CARTESIAN_POINT('Ctrl Pts',(0.554767087978247,0.508602317122839,
13.5550354876999));
#14118=CARTESIAN_POINT('Ctrl Pts',(0.541462865925302,0.393257587853534,
13.5491805142761));
#14119=CARTESIAN_POINT('Ctrl Pts',(0.533280369761308,0.277631298915275,
13.5433255408523));
#14120=CARTESIAN_POINT('Ctrl Pts',(0.525088599788914,0.161873962430134,
13.5374639315682));
#14121=CARTESIAN_POINT('Ctrl Pts',(0.522030170953809,0.0458348416930943,
13.531602322284));
#14122=CARTESIAN_POINT('Ctrl Pts',(0.524092059439312,-0.0699982997375622,
13.5257407129999));
#14123=CARTESIAN_POINT('Ctrl Pts',(0.526155338271362,-0.18590954830616,
13.5198751511895));
#14124=CARTESIAN_POINT('Ctrl Pts',(0.533345783889082,-0.30161412967183,
13.5140095893792));
#14125=CARTESIAN_POINT('Ctrl Pts',(0.545598514508058,-0.41662958955932,
13.5081440275688));
#14126=CARTESIAN_POINT('Ctrl Pts',(0.557869161624378,-0.53181323025855,
13.5022698888685));
#14127=CARTESIAN_POINT('Ctrl Pts',(0.5752168052218,-0.646305331522023,13.4963957501682));
#14128=CARTESIAN_POINT('Ctrl Pts',(0.597525521411622,-0.759633733637311,
13.4905216114679));
#14129=CARTESIAN_POINT('Ctrl Pts',(0.603167031543545,-0.788292636432428,
13.4890361376866));
#14130=CARTESIAN_POINT('Ctrl Pts',(0.609125554976182,-0.81687719919773,
13.4875506639053));
#14131=CARTESIAN_POINT('Ctrl Pts',(0.615398718150294,-0.845379958307195,
13.486065190124));
#14132=CARTESIAN_POINT('Ctrl Pts',(0.640203337689973,-0.958082286609295,
13.4801915007334));
#14133=CARTESIAN_POINT('Ctrl Pts',(0.670013736544737,-1.06987969207632,
13.4743178113428));
#14134=CARTESIAN_POINT('Ctrl Pts',(0.704750006339644,-1.18029352095403,
13.4684441219523));
#14135=CARTESIAN_POINT('Ctrl Pts',(0.739441428346902,-1.29056479520569,
13.4625780160465));
#14136=CARTESIAN_POINT('Ctrl Pts',(0.779045950960212,-1.39945565478475,
13.4567119101408));
#14137=CARTESIAN_POINT('Ctrl Pts',(0.823432698140038,-1.50649774562664,
13.450845804235));
#14138=CARTESIAN_POINT('Ctrl Pts',(0.867773993856243,-1.61343022673123,
13.444985705147));
#14139=CARTESIAN_POINT('Ctrl Pts',(0.916887616414743,-1.71851732529578,
13.4391256060589));
#14140=CARTESIAN_POINT('Ctrl Pts',(0.970593142171489,-1.82130660880617,
13.4332655069709));
#14141=CARTESIAN_POINT('Ctrl Pts',(1.0262362407756,-1.92780429516568,13.4271939888768));
#14142=CARTESIAN_POINT('Ctrl Pts',(1.08680869349269,-2.03183480538726,13.4211224707827));
#14143=CARTESIAN_POINT('Ctrl Pts',(1.15205547888658,-2.13291809020055,13.4150509526886));
#14144=CARTESIAN_POINT('Ctrl Pts',(1.21495789513734,-2.23036937180675,13.4091975890918));
#14145=CARTESIAN_POINT('Ctrl Pts',(1.28220427665314,-2.32508119855183,13.4033442254951));
#14146=CARTESIAN_POINT('Ctrl Pts',(1.35352016544701,-2.41664992726846,13.3974908618983));
#14147=CARTESIAN_POINT('Ctrl Pts',(1.42482534640019,-2.50820490724864,13.3916383771644));
#14148=CARTESIAN_POINT('Ctrl Pts',(1.50019856589792,-2.59661740170161,13.3857858924305));
#14149=CARTESIAN_POINT('Ctrl Pts',(1.57932378762712,-2.68151520892743,13.3799334076966));
#14150=CARTESIAN_POINT('Ctrl Pts',(1.65845626407677,-2.7664208001423,13.3740803863684));
#14151=CARTESIAN_POINT('Ctrl Pts',(1.7413411449168,-2.84781076127939,13.3682273650402));
#14152=CARTESIAN_POINT('Ctrl Pts',(1.82762459127304,-2.92534878540021,13.3623743437121));
#14153=CARTESIAN_POINT('Ctrl Pts',(1.91393681482496,-3.00291266994949,13.3565193702882));
#14154=CARTESIAN_POINT('Ctrl Pts',(2.00364955065226,-3.07662178692314,13.3506643968644));
#14155=CARTESIAN_POINT('Ctrl Pts',(2.09637541959603,-3.14617971361553,13.3448094234406));
#14156=CARTESIAN_POINT('Ctrl Pts',(2.18920638140203,-3.21581647528342,13.3389478141564));
#14157=CARTESIAN_POINT('Ctrl Pts',(2.28505696177989,-3.28129240803428,13.3330862048723));
#14158=CARTESIAN_POINT('Ctrl Pts',(2.38351022884912,-3.34235403461939,13.3272245955881));
#14159=CARTESIAN_POINT('Ctrl Pts',(2.48202988367942,-3.40345683550777,13.3213590337778));
#14160=CARTESIAN_POINT('Ctrl Pts',(2.58315536031639,-3.46013920165589,13.3154934719674));
#14161=CARTESIAN_POINT('Ctrl Pts',(2.68644607561417,-3.51219411068511,13.3096279101571));
#14162=CARTESIAN_POINT('Ctrl Pts',(2.7898878272714,-3.5643251367586,13.3037537714568));
#14163=CARTESIAN_POINT('Ctrl Pts',(2.89550076099386,-3.61181503274344,13.2978796327564));
#14164=CARTESIAN_POINT('Ctrl Pts',(3.00282527382747,-3.65450524812213,13.2920054940561));
#14165=CARTESIAN_POINT('Ctrl Pts',(3.02996589103708,-3.66530090666834,13.2905200202748));
#14166=CARTESIAN_POINT('Ctrl Pts',(3.0572158956617,-3.67578987601307,13.2890345464936));
#14167=CARTESIAN_POINT('Ctrl Pts',(3.08456772922879,-3.68597010457415,13.2875490727123));
#14168=CARTESIAN_POINT('Ctrl Pts',(3.19271920026875,-3.72622359221341,13.2816753833217));
#14169=CARTESIAN_POINT('Ctrl Pts',(3.30282393812599,-3.7617801169372,13.2758016939311));
#14170=CARTESIAN_POINT('Ctrl Pts',(3.41443640720468,-3.79244734362739,13.2699280045406));
#14171=CARTESIAN_POINT('Ctrl Pts',(3.52590477410022,-3.82307497604686,13.2640618986348));
#14172=CARTESIAN_POINT('Ctrl Pts',(3.63887660628105,-3.84882575554979,13.2581957927291));
#14173=CARTESIAN_POINT('Ctrl Pts',(3.75288739300566,-3.86955575910631,13.2523296868233));
#14174=CARTESIAN_POINT('Ctrl Pts',(3.86678143413708,-3.89026453540327,13.2464695877353));
#14175=CARTESIAN_POINT('Ctrl Pts',(3.98171190960985,-3.90596268857882,13.2406094886472));
#14176=CARTESIAN_POINT('Ctrl Pts',(4.09720082745859,-3.91655656206789,13.2347493895592));
#14177=CARTESIAN_POINT('Ctrl Pts',(4.21685632199092,-3.92753263834395,13.2286778714651));
#14178=CARTESIAN_POINT('Ctrl Pts',(4.33711087880189,-3.93302906002751,13.222606353371));
#14179=CARTESIAN_POINT('Ctrl Pts',(4.45742285917651,-3.93299988435739,13.2165348352769));
#14180=CARTESIAN_POINT('Ctrl Pts',(4.57341193394532,-3.93297175699242,13.2106814716801));
#14181=CARTESIAN_POINT('Ctrl Pts',(4.68945392818294,-3.92780827699206,13.2048281080834));
#14182=CARTESIAN_POINT('Ctrl Pts',(4.80506087108329,-3.91752125475641,13.1989747444867));
#14183=CARTESIAN_POINT('Ctrl Pts',(4.92065045599021,-3.90723577708254,13.1931222597527));
#14184=CARTESIAN_POINT('Ctrl Pts',(5.03580470803506,-3.89182832340444,13.1872697750188));
#14185=CARTESIAN_POINT('Ctrl Pts',(5.15003953691746,-3.87136268743445,13.1814172902849));
#14186=CARTESIAN_POINT('Ctrl Pts',(5.26428483959988,-3.85089517504043,13.1755642689568));
#14187=CARTESIAN_POINT('Ctrl Pts',(5.37761014484924,-3.82536863128895,13.1697112476286));
#14188=CARTESIAN_POINT('Ctrl Pts',(5.48954103188702,-3.79489807457262,13.1638582263004));
#14189=CARTESIAN_POINT('Ctrl Pts',(5.6015092500373,-3.76441735533717,13.1580032528766));
#14190=CARTESIAN_POINT('Ctrl Pts',(5.71208172679141,-3.72898945278671,13.1521482794528));
#14191=CARTESIAN_POINT('Ctrl Pts',(5.8207993738973,-3.68877919110033,13.146293306029));
#14192=CARTESIAN_POINT('Ctrl Pts',(5.92964023849185,-3.64852335624717,13.1404316967448));
#14193=CARTESIAN_POINT('Ctrl Pts',(6.03662168984397,-3.6034744872829,13.1345700874607));
#14194=CARTESIAN_POINT('Ctrl Pts',(6.1413047062946,-3.55384552291111,13.1287084781765));
#14195=CARTESIAN_POINT('Ctrl Pts',(6.24605831127208,-3.50418309336414,13.1228429163662));
#14196=CARTESIAN_POINT('Ctrl Pts',(6.34851003103466,-3.44993461158913,13.1169773545558));
#14197=CARTESIAN_POINT('Ctrl Pts',(6.44824705873924,-3.39135807426041,13.1111117927455));
#14198=CARTESIAN_POINT('Ctrl Pts',(6.54812992644033,-3.33269588366734,13.1052376540452));
#14199=CARTESIAN_POINT('Ctrl Pts',(6.64528983455571,-3.26969323098426,13.0993635153448));
#14200=CARTESIAN_POINT('Ctrl Pts',(6.73934439670868,-3.20265037243659,13.0934893766445));
#14201=CARTESIAN_POINT('Ctrl Pts',(6.76312926002483,-3.18569632799282,13.0920039028632));
#14202=CARTESIAN_POINT('Ctrl Pts',(6.7867157099564,-3.1684841053128,13.090518429082));
#14203=CARTESIAN_POINT('Ctrl Pts',(6.81009792502291,-3.15101894365809,13.0890329553007));
#14204=CARTESIAN_POINT('Ctrl Pts',(6.90165114175847,-3.08263398843694,13.0832165729492));
#14205=CARTESIAN_POINT('Ctrl Pts',(6.9903885444588,-3.01013059775906,13.0774001905977));
#14206=CARTESIAN_POINT('Ctrl Pts',(7.07591125866037,-2.93377091982475,13.0715838082462));
#14207=CARTESIAN_POINT('Ctrl Pts',(7.1613231584205,-2.85751018350073,13.0657749623623));
#14208=CARTESIAN_POINT('Ctrl Pts',(7.24352833801147,-2.77740337089531,13.0599661164783));
#14209=CARTESIAN_POINT('Ctrl Pts',(7.3221579331218,-2.69375510159333,13.0541572705944));
#14210=CARTESIAN_POINT('Ctrl Pts',(7.40070768285688,-2.61019177394015,13.0483543233734));
#14211=CARTESIAN_POINT('Ctrl Pts',(7.47568878007658,-2.52309444557788,13.0425513761524));
#14212=CARTESIAN_POINT('Ctrl Pts',(7.54676702953445,-2.43280655728062,13.0367484289314));
#14213=CARTESIAN_POINT('Ctrl Pts',(7.61779426447069,-2.34258347071195,13.0309496466213));
#14214=CARTESIAN_POINT('Ctrl Pts',(7.68492396188114,-2.24917470849623,13.0251508643112));
#14215=CARTESIAN_POINT('Ctrl Pts',(7.74786078546853,-2.15295838644457,13.0193520820012));
#14216=CARTESIAN_POINT('Ctrl Pts',(7.81077427599178,-2.05677773542754,13.0135554495193));
#14217=CARTESIAN_POINT('Ctrl Pts',(7.86949775114576,-1.95779194581923,13.0077588170374));
#14218=CARTESIAN_POINT('Ctrl Pts',(7.92377838368981,-1.85640926908902,13.0019621845556));
#14219=CARTESIAN_POINT('Ctrl Pts',(7.97805265201111,-1.75503847913882,12.9961662317095));
#14220=CARTESIAN_POINT('Ctrl Pts',(8.02788491442897,-1.65127173294077,12.9903702788634));
#14221=CARTESIAN_POINT('Ctrl Pts',(8.07306802915816,-1.54554237424597,12.9845743260173));
#14222=CARTESIAN_POINT('Ctrl Pts',(8.11825730016423,-1.4397986097447,12.9787775834628));
#14223=CARTESIAN_POINT('Ctrl Pts',(8.15879599961505,-1.33209208974856,12.9729808409082));
#14224=CARTESIAN_POINT('Ctrl Pts',(8.19452523344622,-1.22287586847292,12.9671840983536));
#14225=CARTESIAN_POINT('Ctrl Pts',(8.23028873158198,-1.1135549089348,12.9613817967278));
#14226=CARTESIAN_POINT('Ctrl Pts',(8.261233424001,-1.00272175917822,12.9555794951021));
#14227=CARTESIAN_POINT('Ctrl Pts',(8.28725040532625,-0.890844340165236,
12.9497771934764));
#14228=CARTESIAN_POINT('Ctrl Pts',(8.31328093909956,-0.77890864333394,12.9439718693866));
#14229=CARTESIAN_POINT('Ctrl Pts',(8.33437857391976,-0.665928008763961,
12.9381665452968));
#14230=CARTESIAN_POINT('Ctrl Pts',(8.35048593506992,-0.552378436056247,
12.932361221207));
#14231=CARTESIAN_POINT('Ctrl Pts',(8.36661712325321,-0.438660893598316,
12.9265473095125));
#14232=CARTESIAN_POINT('Ctrl Pts',(8.37774325755507,-0.32437315207909,12.9207333978181));
#14233=CARTESIAN_POINT('Ctrl Pts',(8.38385899917048,-0.209994354059066,
12.9149194861236));
#14234=CARTESIAN_POINT('Ctrl Pts',(8.38763045292072,-0.139459270357369,
12.9113341647608));
#14235=CARTESIAN_POINT('Ctrl Pts',(8.38949751602963,-0.0688895527329186,
12.9077488433979));
#14236=CARTESIAN_POINT('Ctrl Pts',(8.38946877942379,0.00160329820526994,
12.904163522035));
#14237=CARTESIAN_POINT('',(8.38838636610598,-0.00299497982686102,15.4041639340473));
#14238=CARTESIAN_POINT('Ctrl Pts',(8.38946797146284,-0.00298763865733172,
15.404163522035));
#14239=CARTESIAN_POINT('Ctrl Pts',(8.38955615194013,0.113095247154287,15.3983099575575));
#14240=CARTESIAN_POINT('Ctrl Pts',(8.38450072803562,0.229234623628655,15.39245639308));
#14241=CARTESIAN_POINT('Ctrl Pts',(8.37431343004976,0.344941812805024,15.3866028286025));
#14242=CARTESIAN_POINT('Ctrl Pts',(8.36412752979414,0.460633126580709,15.380750067253));
#14243=CARTESIAN_POINT('Ctrl Pts',(8.34881119138193,0.575891960223374,15.3748973059036));
#14244=CARTESIAN_POINT('Ctrl Pts',(8.32842813354715,0.690233504465133,15.3690445445541));
#14245=CARTESIAN_POINT('Ctrl Pts',(8.30804296565823,0.804586885343549,15.3631911773267));
#14246=CARTESIAN_POINT('Ctrl Pts',(8.2825901076265,0.918022381936844,15.3573378100994));
#14247=CARTESIAN_POINT('Ctrl Pts',(8.25218451169293,1.03006483322276,15.351484442872));
#14248=CARTESIAN_POINT('Ctrl Pts',(8.22176844884118,1.14214585435522,15.3456290606631));
#14249=CARTESIAN_POINT('Ctrl Pts',(8.18639636531697,1.25283247866569,15.3397736784541));
#14250=CARTESIAN_POINT('Ctrl Pts',(8.1462330339211,1.36166484783254,15.3339182962452));
#14251=CARTESIAN_POINT('Ctrl Pts',(8.10602142242775,1.4706280437314,15.3280558753168));
#14252=CARTESIAN_POINT('Ctrl Pts',(8.06100720769499,1.57773214729757,15.3221934543884));
#14253=CARTESIAN_POINT('Ctrl Pts',(8.01140333883864,1.68253725122022,15.3163310334599));
#14254=CARTESIAN_POINT('Ctrl Pts',(7.96176576425408,1.78741356999826,15.3104646290284));
#14255=CARTESIAN_POINT('Ctrl Pts',(7.90753251760593,1.8899874145095,15.3045982245968));
#14256=CARTESIAN_POINT('Ctrl Pts',(7.84896164638746,1.98984506052513,15.2987318201653));
#14257=CARTESIAN_POINT('Ctrl Pts',(7.79029697220462,2.08986263148325,15.2928560205153));
#14258=CARTESIAN_POINT('Ctrl Pts',(7.72728102728111,2.18715497353262,15.2869802208654));
#14259=CARTESIAN_POINT('Ctrl Pts',(7.66021429275203,2.2813385938439,15.2811044212155));
#14260=CARTESIAN_POINT('Ctrl Pts',(7.62827708711094,2.32618887127316,15.2783063630866));
#14261=CARTESIAN_POINT('Ctrl Pts',(7.59542187401625,2.37033469463769,15.2755083049577));
#14262=CARTESIAN_POINT('Ctrl Pts',(7.56168410033237,2.41373752515241,15.2727102468289));
#14263=CARTESIAN_POINT('Ctrl Pts',(7.49086169628585,2.50484883641669,15.2668365574383));
#14264=CARTESIAN_POINT('Ctrl Pts',(7.41590794136691,2.59299221037409,15.2609628680477));
#14265=CARTESIAN_POINT('Ctrl Pts',(7.33710065212917,2.67776976170523,15.2550891786572));
#14266=CARTESIAN_POINT('Ctrl Pts',(7.25839511050558,2.76243785725297,15.2492230727514));
#14267=CARTESIAN_POINT('Ctrl Pts',(7.17584620747278,2.84374847230016,15.2433569668457));
#14268=CARTESIAN_POINT('Ctrl Pts',(7.08977335741909,2.92133492099204,15.2374908609399));
#14269=CARTESIAN_POINT('Ctrl Pts',(7.00378864486722,2.99884192214898,15.2316307618519));
#14270=CARTESIAN_POINT('Ctrl Pts',(6.91428746790389,3.07263206734264,15.2257706627638));
#14271=CARTESIAN_POINT('Ctrl Pts',(6.82162714094363,3.14237433651276,15.2199105636758));
#14272=CARTESIAN_POINT('Ctrl Pts',(6.72562384077868,3.21463274764695,15.2138390455817));
#14273=CARTESIAN_POINT('Ctrl Pts',(6.62622944448929,3.28254536113956,15.2077675274876));
#14274=CARTESIAN_POINT('Ctrl Pts',(6.52388049339166,3.34578827127266,15.2016960093935));
#14275=CARTESIAN_POINT('Ctrl Pts',(6.4252090219022,3.40675881310222,15.1958426457967));
#14276=CARTESIAN_POINT('Ctrl Pts',(6.32379204225246,3.46338921298687,15.1899892822));
#14277=CARTESIAN_POINT('Ctrl Pts',(6.22005081781549,3.51543291025725,15.1841359186032));
#14278=CARTESIAN_POINT('Ctrl Pts',(6.11632516977435,3.56746879334157,15.1782834338693));
#14279=CARTESIAN_POINT('Ctrl Pts',(6.01027634002654,3.61491915795506,15.1724309491354));
#14280=CARTESIAN_POINT('Ctrl Pts',(5.90234962745504,3.65758369942617,15.1665784644015));
#14281=CARTESIAN_POINT('Ctrl Pts',(5.79441301945312,3.70025215266289,15.1607254430733));
#14282=CARTESIAN_POINT('Ctrl Pts',(5.68459857059121,3.73813375858043,15.1548724217452));
#14283=CARTESIAN_POINT('Ctrl Pts',(5.57337029236903,3.77107686747101,15.149019400417));
#14284=CARTESIAN_POINT('Ctrl Pts',(5.46210491736823,3.80403096352455,15.1431644269932));
#14285=CARTESIAN_POINT('Ctrl Pts',(5.34942517129391,3.83204317013544,15.1373094535694));
#14286=CARTESIAN_POINT('Ctrl Pts',(5.23580821534284,3.85501226366258,15.1314544801456));
#14287=CARTESIAN_POINT('Ctrl Pts',(5.12206248916535,3.87800738970705,15.1255928708614));
#14288=CARTESIAN_POINT('Ctrl Pts',(5.00737783818905,3.89594791252093,15.1197312615773));
#14289=CARTESIAN_POINT('Ctrl Pts',(4.89223965728508,3.90878408546992,15.1138696522931));
#14290=CARTESIAN_POINT('Ctrl Pts',(4.77702383786034,3.92162891394458,15.1080040904828));
#14291=CARTESIAN_POINT('Ctrl Pts',(4.66135429075987,3.92936251147385,15.1021385286724));
#14292=CARTESIAN_POINT('Ctrl Pts',(4.54571780771183,3.93198724174961,15.0962729668621));
#14293=CARTESIAN_POINT('Ctrl Pts',(4.42991223576386,3.93461581002479,15.0903988281617));
#14294=CARTESIAN_POINT('Ctrl Pts',(4.31414023581944,3.9321206108403,15.0845246894614));
#14295=CARTESIAN_POINT('Ctrl Pts',(4.19888494768118,3.9245559495656,15.0786505507611));
#14296=CARTESIAN_POINT('Ctrl Pts',(4.16973876686725,3.92264297022323,15.0771650769798));
#14297=CARTESIAN_POINT('Ctrl Pts',(4.14062558366268,3.92040605411133,15.0756796031985));
#14298=CARTESIAN_POINT('Ctrl Pts',(4.11155310477521,3.91784659627563,15.0741941294172));
#14299=CARTESIAN_POINT('Ctrl Pts',(3.99659805612459,3.90772628279425,15.0683204400266));
#14300=CARTESIAN_POINT('Ctrl Pts',(3.88189734388171,3.89252541571307,15.062446750636));
#14301=CARTESIAN_POINT('Ctrl Pts',(3.76793592119876,3.87226174904628,15.0565730612455));
#14302=CARTESIAN_POINT('Ctrl Pts',(3.65412163341873,3.85202424467685,15.0507069553397));
#14303=CARTESIAN_POINT('Ctrl Pts',(3.54104514007597,3.82673701144322,15.044840849434));
#14304=CARTESIAN_POINT('Ctrl Pts',(3.42918772774957,3.796469671873,15.0389747435282));
#14305=CARTESIAN_POINT('Ctrl Pts',(3.31744485598842,3.76623332567293,15.0331146444402));
#14306=CARTESIAN_POINT('Ctrl Pts',(3.20691897865755,3.73102712386475,15.0272545453522));
#14307=CARTESIAN_POINT('Ctrl Pts',(3.09808195805375,3.6909718714319,15.0213944462641));
#14308=CARTESIAN_POINT('Ctrl Pts',(2.98531834604353,3.64947151687194,15.01532292817));
#14309=CARTESIAN_POINT('Ctrl Pts',(2.87436819643208,3.60276569939355,15.0092514100759));
#14310=CARTESIAN_POINT('Ctrl Pts',(2.76574034293541,3.55104565572003,15.0031798919818));
#14311=CARTESIAN_POINT('Ctrl Pts',(2.66101557502815,3.50118395454936,14.9973265283851));
#14312=CARTESIAN_POINT('Ctrl Pts',(2.55844949636893,3.44666234909959,14.9914731647883));
#14313=CARTESIAN_POINT('Ctrl Pts',(2.4584776647042,3.38770116740492,14.9856198011916));
#14314=CARTESIAN_POINT('Ctrl Pts',(2.35852084347372,3.32874883853335,14.9797673164577));
#14315=CARTESIAN_POINT('Ctrl Pts',(2.26115785049878,3.26535846866724,14.9739148317238));
#14316=CARTESIAN_POINT('Ctrl Pts',(2.16679840412643,3.19779565888478,14.9680623469899));
#14317=CARTESIAN_POINT('Ctrl Pts',(2.0724303062598,3.13022665449983,14.9622093256617));
#14318=CARTESIAN_POINT('Ctrl Pts',(1.98106663836847,3.05848469024496,14.9563563043336));
#14319=CARTESIAN_POINT('Ctrl Pts',(1.89308637793914,2.98287746787567,14.9505032830054));
#14320=CARTESIAN_POINT('Ctrl Pts',(1.80507677439373,2.90724502903746,14.9446483095816));
#14321=CARTESIAN_POINT('Ctrl Pts',(1.72045313531597,2.82774503781808,14.9387933361578));
#14322=CARTESIAN_POINT('Ctrl Pts',(1.63955919334883,2.74472358221698,14.932938362734));
#14323=CARTESIAN_POINT('Ctrl Pts',(1.5585735684889,2.66160803245965,14.9270767534498));
#14324=CARTESIAN_POINT('Ctrl Pts',(1.48132636632456,2.57496334834026,14.9212151441657));
#14325=CARTESIAN_POINT('Ctrl Pts',(1.40812252651924,2.48517044285445,14.9153535348815));
#14326=CARTESIAN_POINT('Ctrl Pts',(1.33486932482731,2.39531698935324,14.9094879730712));
#14327=CARTESIAN_POINT('Ctrl Pts',(1.26566516051922,2.30231141801716,14.9036224112609));
#14328=CARTESIAN_POINT('Ctrl Pts',(1.20077194179187,2.20656406513521,14.8977568494505));
#14329=CARTESIAN_POINT('Ctrl Pts',(1.13578383326246,2.11067670613952,14.8918827107502));
#14330=CARTESIAN_POINT('Ctrl Pts',(1.07511946643912,2.01203991488976,14.8860085720499));
#14331=CARTESIAN_POINT('Ctrl Pts',(1.01899512277585,1.91108911701067,14.8801344333495));
#14332=CARTESIAN_POINT('Ctrl Pts',(1.00480219249987,1.88556030826061,14.8786489595682));
#14333=CARTESIAN_POINT('Ctrl Pts',(0.99089935715119,1.85988361845691,14.8771634857869));
#14334=CARTESIAN_POINT('Ctrl Pts',(0.977289622341522,1.83406627987411,14.8756780120056));
#14335=CARTESIAN_POINT('Ctrl Pts',(0.923475575964183,1.73198233222459,14.869804322615));
#14336=CARTESIAN_POINT('Ctrl Pts',(0.874068636830534,1.62735788902668,14.8639306332245));
#14337=CARTESIAN_POINT('Ctrl Pts',(0.829316783819315,1.52061008483964,14.8580569438339));
#14338=CARTESIAN_POINT('Ctrl Pts',(0.784622709654518,1.41400010209616,14.8521908379281));
#14339=CARTESIAN_POINT('Ctrl Pts',(0.744571927662193,1.30527258776266,14.8463247320224));
#14340=CARTESIAN_POINT('Ctrl Pts',(0.709366843518082,1.19486971376267,14.8404586261166));
#14341=CARTESIAN_POINT('Ctrl Pts',(0.674197808931618,1.08457989089911,14.8345985270285));
#14342=CARTESIAN_POINT('Ctrl Pts',(0.643864727267642,0.972618512011817,
14.8287384279405));
#14343=CARTESIAN_POINT('Ctrl Pts',(0.618521886189556,0.859447576222089,
14.8228783288524));
#14344=CARTESIAN_POINT('Ctrl Pts',(0.592264733221715,0.742193691253597,
14.8168068107583));
#14345=CARTESIAN_POINT('Ctrl Pts',(0.571364866806784,0.62364174201213,14.8107352926642));
#14346=CARTESIAN_POINT('Ctrl Pts',(0.555937432822474,0.504322976708725,
14.8046637745701));
#14347=CARTESIAN_POINT('Ctrl Pts',(0.541064318870497,0.389291429999682,
14.7988104109734));
#14348=CARTESIAN_POINT('Ctrl Pts',(0.53127720502416,0.273547668375362,14.7929570473766));
#14349=CARTESIAN_POINT('Ctrl Pts',(0.526627067904312,0.157577136350896,
14.7871036837799));
#14350=CARTESIAN_POINT('Ctrl Pts',(0.521977628986904,0.0416240169115701,
14.7812511990459));
#14351=CARTESIAN_POINT('Ctrl Pts',(0.52246364971071,-0.0745553925237044,
14.775398714312));
#14352=CARTESIAN_POINT('Ctrl Pts',(0.528084055618252,-0.190472817542138,
14.7695462295781));
#14353=CARTESIAN_POINT('Ctrl Pts',(0.533704976841559,-0.306400870632207,
14.7636932082499));
#14354=CARTESIAN_POINT('Ctrl Pts',(0.544461199054441,-0.422066478872169,
14.7578401869217));
#14355=CARTESIAN_POINT('Ctrl Pts',(0.560299605357159,-0.53698437645785,
14.7519871655936));
#14356=CARTESIAN_POINT('Ctrl Pts',(0.57614329407421,-0.65194060138138,14.7461321921697));
#14357=CARTESIAN_POINT('Ctrl Pts',(0.597072480948472,-0.766148210722537,
14.7402772187459));
#14358=CARTESIAN_POINT('Ctrl Pts',(0.622982686253195,-0.879130745647937,
14.7344222453221));
#14359=CARTESIAN_POINT('Ctrl Pts',(0.64892225744763,-0.992241331764786,
14.7285606360379));
#14360=CARTESIAN_POINT('Ctrl Pts',(0.679854022439804,-1.10412366925764,
14.7226990267538));
#14361=CARTESIAN_POINT('Ctrl Pts',(0.71562320774221,-1.21431501837661,14.7168374174696));
#14362=CARTESIAN_POINT('Ctrl Pts',(0.751416512468981,-1.32458067033161,
14.7109718556592));
#14363=CARTESIAN_POINT('Ctrl Pts',(0.792053588223949,-1.43315267745741,
14.7051062938489));
#14364=CARTESIAN_POINT('Ctrl Pts',(0.837331609128034,-1.53958850903595,
14.6992407320385));
#14365=CARTESIAN_POINT('Ctrl Pts',(0.882675837603703,-1.64617997590503,
14.6933665933382));
#14366=CARTESIAN_POINT('Ctrl Pts',(0.932674377079799,-1.75062866206402,
14.6874924546379));
#14367=CARTESIAN_POINT('Ctrl Pts',(0.987078584220269,-1.85251677613741,
14.6816183159376));
#14368=CARTESIAN_POINT('Ctrl Pts',(1.00083652005029,-1.87828261684978,14.6801328421563));
#14369=CARTESIAN_POINT('Ctrl Pts',(1.0148759847093,-1.903884856244,14.6786473683751));
#14370=CARTESIAN_POINT('Ctrl Pts',(1.02919253023092,-1.92931704799615,14.6771618945939));
#14371=CARTESIAN_POINT('Ctrl Pts',(1.08580136614753,-2.02987809239909,14.6712882052033));
#14372=CARTESIAN_POINT('Ctrl Pts',(1.14693413516208,-2.12811303680113,14.6654145158127));
#14373=CARTESIAN_POINT('Ctrl Pts',(1.21237474753979,-2.22358736999259,14.6595408264222));
#14374=CARTESIAN_POINT('Ctrl Pts',(1.27773086993911,-2.31893843685057,14.6536747205164));
#14375=CARTESIAN_POINT('Ctrl Pts',(1.34738354359932,-2.41153564287397,14.6478086146106));
#14376=CARTESIAN_POINT('Ctrl Pts',(1.42107093402517,-2.50096919937989,14.6419425087049));
#14377=CARTESIAN_POINT('Ctrl Pts',(1.49468286950171,-2.59031117706298,14.6360824096168));
#14378=CARTESIAN_POINT('Ctrl Pts',(1.57232104269608,-2.67649563197526,14.6302223105288));
#14379=CARTESIAN_POINT('Ctrl Pts',(1.65368087293102,-2.75914246086472,14.6243622114408));
#14380=CARTESIAN_POINT('Ctrl Pts',(1.73797598022944,-2.84477099879301,14.6182906933467));
#14381=CARTESIAN_POINT('Ctrl Pts',(1.82626609711616,-2.92660145977944,14.6122191752526));
#14382=CARTESIAN_POINT('Ctrl Pts',(1.91816723322607,-3.00424909113149,14.6061476571585));
#14383=CARTESIAN_POINT('Ctrl Pts',(2.00676628807001,-3.07910678103463,14.6002942935617));
#14384=CARTESIAN_POINT('Ctrl Pts',(2.09872099172641,-3.15007676361758,14.594440929965));
#14385=CARTESIAN_POINT('Ctrl Pts',(2.19365105627081,-3.21685303873709,14.5885875663682));
#14386=CARTESIAN_POINT('Ctrl Pts',(2.28856686738551,-3.28361928762363,14.5827350816343));
#14387=CARTESIAN_POINT('Ctrl Pts',(2.38645681327443,-3.3461928434337,14.5768825969004));
#14388=CARTESIAN_POINT('Ctrl Pts',(2.48691001064333,-3.40430991083921,14.5710301121665));
#14389=CARTESIAN_POINT('Ctrl Pts',(2.58737241822185,-3.46243230679959,14.5651770908383));
#14390=CARTESIAN_POINT('Ctrl Pts',(2.69039818684172,-3.51609719519131,14.5593240695102));
#14391=CARTESIAN_POINT('Ctrl Pts',(2.79555074866315,-3.56508614335424,14.553471048182));
#14392=CARTESIAN_POINT('Ctrl Pts',(2.90073838089458,-3.61409143027743,14.5476160747582));
#14393=CARTESIAN_POINT('Ctrl Pts',(3.00805384249685,-3.65841750156485,14.5417611013343));
#14394=CARTESIAN_POINT('Ctrl Pts',(3.11704012191982,-3.69789385948559,14.5359061279105));
#14395=CARTESIAN_POINT('Ctrl Pts',(3.22614992329152,-3.73741495878741,14.5300445186264));
#14396=CARTESIAN_POINT('Ctrl Pts',(3.33693393344473,-3.77207523320529,14.5241829093422));
#14397=CARTESIAN_POINT('Ctrl Pts',(3.44891940435672,-3.80175388449577,14.5183213000581));
#14398=CARTESIAN_POINT('Ctrl Pts',(3.56098038789436,-3.83145254831884,14.5124557382477));
#14399=CARTESIAN_POINT('Ctrl Pts',(3.67424404273518,-3.85616281236668,14.5065901764374));
#14400=CARTESIAN_POINT('Ctrl Pts',(3.78822855300604,-3.87581521270592,14.500724614627));
#14401=CARTESIAN_POINT('Ctrl Pts',(3.90237973658759,-3.89549634967455,14.4948504759267));
#14402=CARTESIAN_POINT('Ctrl Pts',(4.01725347098413,-3.91010481078321,14.4889763372263));
#14403=CARTESIAN_POINT('Ctrl Pts',(4.13236389090702,-3.91962304430006,14.483102198526));
#14404=CARTESIAN_POINT('Ctrl Pts',(4.16147343691287,-3.92203005017006,14.4816167247448));
#14405=CARTESIAN_POINT('Ctrl Pts',(4.19059812690308,-3.92411179532528,14.4801312509635));
#14406=CARTESIAN_POINT('Ctrl Pts',(4.2197301326962,-3.92586852281323,14.4786457771823));
#14407=CARTESIAN_POINT('Ctrl Pts',(4.33492055578855,-3.93281477237915,14.4727720877917));
#14408=CARTESIAN_POINT('Ctrl Pts',(4.45060880595631,-3.9346985245286,14.4668983984011));
#14409=CARTESIAN_POINT('Ctrl Pts',(4.56631261571985,-3.93146580850201,14.4610247090106));
#14410=CARTESIAN_POINT('Ctrl Pts',(4.68186704099442,-3.92823726621553,14.4551586031049));
#14411=CARTESIAN_POINT('Ctrl Pts',(4.79743657670266,-3.91990540403825,14.4492924971991));
#14412=CARTESIAN_POINT('Ctrl Pts',(4.91253493122844,-3.90646809320872,14.4434263912934));
#14413=CARTESIAN_POINT('Ctrl Pts',(5.02751542650641,-3.89304454201418,14.4375662922054));
#14414=CARTESIAN_POINT('Ctrl Pts',(5.14202529238277,-3.87452598854531,14.4317061931173));
#14415=CARTESIAN_POINT('Ctrl Pts',(5.25558000903006,-3.85096231674724,14.4258460940292));
#14416=CARTESIAN_POINT('Ctrl Pts',(5.3732315207939,-3.8265485214281,14.4197745759351));
#14417=CARTESIAN_POINT('Ctrl Pts',(5.48985721139359,-3.79671871456854,14.413703057841));
#14418=CARTESIAN_POINT('Ctrl Pts',(5.60492560529334,-3.76158698819158,14.4076315397469));
#14419=CARTESIAN_POINT('Ctrl Pts',(5.71585949983983,-3.72771757281993,14.4017781761502));
#14420=CARTESIAN_POINT('Ctrl Pts',(5.82534565255436,-3.68892081630443,14.3959248125534));
#14421=CARTESIAN_POINT('Ctrl Pts',(5.93292077141457,-3.64535039198415,14.3900714489567));
#14422=CARTESIAN_POINT('Ctrl Pts',(6.04047973823267,-3.60178650961647,14.3842189642228));
#14423=CARTESIAN_POINT('Ctrl Pts',(6.14612785890583,-3.55345053966587,14.3783664794888));
#14424=CARTESIAN_POINT('Ctrl Pts',(6.24942072040807,-3.50054474463248,14.3725139947549));
#14425=CARTESIAN_POINT('Ctrl Pts',(6.35272305247842,-3.44763409884825,14.3666609734268));
#14426=CARTESIAN_POINT('Ctrl Pts',(6.45366932836057,-3.39015298341744,14.3608079520986));
#14427=CARTESIAN_POINT('Ctrl Pts',(6.55183932979794,-3.32834983529911,14.3549549307705));
#14428=CARTESIAN_POINT('Ctrl Pts',(6.65004207282762,-3.26652607463672,14.3490999573466));
#14429=CARTESIAN_POINT('Ctrl Pts',(6.7454663507795,-3.20037763495626,14.3432449839228));
#14430=CARTESIAN_POINT('Ctrl Pts',(6.83772114276442,-3.13019611820804,14.3373900104989));
#14431=CARTESIAN_POINT('Ctrl Pts',(6.93008049370588,-3.05993505972544,14.3315284012148));
#14432=CARTESIAN_POINT('Ctrl Pts',(7.01926285985733,-2.98563205106495,14.3256667919306));
#14433=CARTESIAN_POINT('Ctrl Pts',(7.10491045230746,-2.90761886022311,14.3198051826465));
#14434=CARTESIAN_POINT('Ctrl Pts',(7.19061579755809,-2.82955306451384,14.3139396208361));
#14435=CARTESIAN_POINT('Ctrl Pts',(7.27278133088469,-2.74777239570804,14.3080740590258));
#14436=CARTESIAN_POINT('Ctrl Pts',(7.35108748423156,-2.66264407040588,14.3022084972154));
#14437=CARTESIAN_POINT('Ctrl Pts',(7.42950814038058,-2.57739126661291,14.2963343585151));
#14438=CARTESIAN_POINT('Ctrl Pts',(7.50405788886716,-2.48878135187014,14.2904602198148));
#14439=CARTESIAN_POINT('Ctrl Pts',(7.57445858863925,-2.39721308763156,14.2845860811144));
#14440=CARTESIAN_POINT('Ctrl Pts',(7.59226177631162,-2.37405696846868,14.2831006073331));
#14441=CARTESIAN_POINT('Ctrl Pts',(7.6097998545509,-2.35071179676985,14.2816151335519));
#14442=CARTESIAN_POINT('Ctrl Pts',(7.62706878386022,-2.32718428237573,14.2801296597706));
#14443=CARTESIAN_POINT('Ctrl Pts',(7.69575812185698,-2.23360063515049,14.2742210009985));
#14444=CARTESIAN_POINT('Ctrl Pts',(7.76041482388324,-2.13681774927419,14.2683123422264));
#14445=CARTESIAN_POINT('Ctrl Pts',(7.82072869435389,-2.03721536015154,14.2624036834543));
#14446=CARTESIAN_POINT('Ctrl Pts',(7.88096338697472,-1.93774372541336,14.256502781354));
#14447=CARTESIAN_POINT('Ctrl Pts',(7.93686637664349,-1.83546029194052,14.2506018792537));
#14448=CARTESIAN_POINT('Ctrl Pts',(7.98816869929241,-1.73077641082834,14.2447009771534));
#14449=CARTESIAN_POINT('Ctrl Pts',(8.03941558209937,-1.62620565632571,14.2388064518614));
#14450=CARTESIAN_POINT('Ctrl Pts',(8.08607150902556,-1.51923997635001,14.2329119265695));
#14451=CARTESIAN_POINT('Ctrl Pts',(8.12791203700415,-1.41031762592057,14.2270174012775));
#14452=CARTESIAN_POINT('Ctrl Pts',(8.17100632961496,-1.29813138286778,14.220946244674));
#14453=CARTESIAN_POINT('Ctrl Pts',(8.20899184575389,-1.1838697237963,14.2148750880704));
#14454=CARTESIAN_POINT('Ctrl Pts',(8.24167531083385,-1.06803697901315,14.2088039314669));
#14455=CARTESIAN_POINT('Ctrl Pts',(8.27336048026638,-0.955742271725851,
14.2029182144793));
#14456=CARTESIAN_POINT('Ctrl Pts',(8.3000626598224,-0.841971478732594,14.1970324974917));
#14457=CARTESIAN_POINT('Ctrl Pts',(8.32165562211637,-0.727201620817306,
14.1911467805041));
#14458=CARTESIAN_POINT('Ctrl Pts',(8.34426906941924,-0.607007730854899,
14.1849829040926));
#14459=CARTESIAN_POINT('Ctrl Pts',(8.36127840500552,-0.485718479075838,
14.1788190276811));
#14460=CARTESIAN_POINT('Ctrl Pts',(8.37259849858251,-0.363895015438149,
14.1726551512696));
#14461=CARTESIAN_POINT('Ctrl Pts',(8.3839185921595,-0.24207155180046,14.166491274858));
#14462=CARTESIAN_POINT('Ctrl Pts',(8.38954939326522,-0.119714386616567,
14.1603273984465));
#14463=CARTESIAN_POINT('Ctrl Pts',(8.38946824069733,0.00260925024367313,
14.154163522035));
#14464=CARTESIAN_POINT('',(8.39173482151485,-0.000977378064454105,16.6541631314135));
#14465=CARTESIAN_POINT('Ctrl Pts',(8.39563349011517,-0.000965124593257569,
16.6541624592986));
#14466=CARTESIAN_POINT('Ctrl Pts',(8.39142528971798,1.24797165481331,16.5907106232987));
#14467=CARTESIAN_POINT('Ctrl Pts',(7.07426780414926,3.80700714954901,16.4610867481615));
#14468=CARTESIAN_POINT('Ctrl Pts',(2.71525479979042,4.31066727228104,16.2652908338871));
#14469=CARTESIAN_POINT('Ctrl Pts',(-0.109747265587407,0.873697681739816,
16.0667747164755));
#14470=CARTESIAN_POINT('Ctrl Pts',(1.246904763689,-3.36338762624652,15.8682585990637));
#14471=CARTESIAN_POINT('Ctrl Pts',(5.54281476546621,-4.52034652453288,15.6697424816522));
#14472=CARTESIAN_POINT('Ctrl Pts',(8.11523183285779,-2.19602354770684,15.5150446046431));
#14473=CARTESIAN_POINT('Ctrl Pts',(8.38879516314435,-0.445889532599667,
15.4265187667713));
#14474=CARTESIAN_POINT('Ctrl Pts',(8.38567196030232,-0.00301340328699777,
15.4041649680368));
#14475=CARTESIAN_POINT('',(8.38946746866507,0.00358900970105028,17.9041634947166));
#14476=CARTESIAN_POINT('Ctrl Pts',(8.38946746866507,0.00358900970105028,
17.9041634947166));
#14477=CARTESIAN_POINT('Ctrl Pts',(8.38933295163775,0.150998822502151,17.8967107583277));
#14478=CARTESIAN_POINT('Ctrl Pts',(8.3809074565855,0.298039767866117,17.8892580219388));
#14479=CARTESIAN_POINT('Ctrl Pts',(8.36433627259726,0.443918021640171,17.8818052855499));
#14480=CARTESIAN_POINT('Ctrl Pts',(8.34741428627491,0.592884433264276,17.8741947790631));
#14481=CARTESIAN_POINT('Ctrl Pts',(8.32199808271087,0.740638646204888,17.8665842725763));
#14482=CARTESIAN_POINT('Ctrl Pts',(8.28829050128427,0.886359857120285,17.8589737660894));
#14483=CARTESIAN_POINT('Ctrl Pts',(8.28009079873932,0.921807982836407,17.8571224351198));
#14484=CARTESIAN_POINT('Ctrl Pts',(8.27140067079434,0.957135906655535,17.8552711041501));
#14485=CARTESIAN_POINT('Ctrl Pts',(8.26222345997328,0.992332000327834,17.8534197731804));
#14486=CARTESIAN_POINT('Ctrl Pts',(8.23310706386843,1.10399810724074,17.8475460837898));
#14487=CARTESIAN_POINT('Ctrl Pts',(8.19902335211134,1.21456763442564,17.8416723943993));
#14488=CARTESIAN_POINT('Ctrl Pts',(8.16007056424081,1.32356535166693,17.8357987050087));
#14489=CARTESIAN_POINT('Ctrl Pts',(8.12116806807887,1.43242234261535,17.829932599103));
#14490=CARTESIAN_POINT('Ctrl Pts',(8.07740913522595,1.53971117384617,17.8240664931972));
#14491=CARTESIAN_POINT('Ctrl Pts',(8.02894253953352,1.64496886543686,17.8182003872914));
#14492=CARTESIAN_POINT('Ctrl Pts',(7.98052557301757,1.75011877449243,17.8123402882034));
#14493=CARTESIAN_POINT('Ctrl Pts',(7.92741070397869,1.85324130788132,17.8064801891154));
#14494=CARTESIAN_POINT('Ctrl Pts',(7.8697956055742,1.95389129912452,17.8006200900273));
#14495=CARTESIAN_POINT('Ctrl Pts',(7.81010188586044,2.05817251243223,17.7945485719332));
#14496=CARTESIAN_POINT('Ctrl Pts',(7.74557724197532,2.15979898249109,17.7884770538391));
#14497=CARTESIAN_POINT('Ctrl Pts',(7.67649495084179,2.25830081254833,17.782405535745));
#14498=CARTESIAN_POINT('Ctrl Pts',(7.60989484163788,2.35326339313092,17.7765521721482));
#14499=CARTESIAN_POINT('Ctrl Pts',(7.53905922600384,2.44532164376663,17.7706988085515));
#14500=CARTESIAN_POINT('Ctrl Pts',(7.46427786749433,2.53408276415567,17.7648454449547));
#14501=CARTESIAN_POINT('Ctrl Pts',(7.38950773715418,2.62283055736116,17.7589929602208));
#14502=CARTESIAN_POINT('Ctrl Pts',(7.310793308055,2.7082818887986,17.7531404754869));
#14503=CARTESIAN_POINT('Ctrl Pts',(7.2284646833785,2.79007697388514,17.747287990753));
#14504=CARTESIAN_POINT('Ctrl Pts',(7.14612851027254,2.87187955848272,17.7414349694248));
#14505=CARTESIAN_POINT('Ctrl Pts',(7.06017777595217,2.95002493912375,17.7355819480967));
#14506=CARTESIAN_POINT('Ctrl Pts',(6.97097897915068,3.02419065188116,17.7297289267685));
#14507=CARTESIAN_POINT('Ctrl Pts',(6.88175043282775,3.09838110033613,17.7238739533447));
#14508=CARTESIAN_POINT('Ctrl Pts',(6.78927198745366,3.1685889776424,17.7180189799208));
#14509=CARTESIAN_POINT('Ctrl Pts',(6.69394212490612,3.23453296329529,17.712164006497));
#14510=CARTESIAN_POINT('Ctrl Pts',(6.59850421820409,3.3005516879857,17.7063023972128));
#14511=CARTESIAN_POINT('Ctrl Pts',(6.50020878398385,3.36229664032851,17.7004407879287));
#14512=CARTESIAN_POINT('Ctrl Pts',(6.39948218503442,3.41953054900074,17.6945791786445));
#14513=CARTESIAN_POINT('Ctrl Pts',(6.29868766539961,3.4768030509179,17.6887136168342));
#14514=CARTESIAN_POINT('Ctrl Pts',(6.19545908369862,3.52955826466197,17.6828480550239));
#14515=CARTESIAN_POINT('Ctrl Pts',(6.09024465169915,3.57760624817609,17.6769824932135));
#14516=CARTESIAN_POINT('Ctrl Pts',(5.98487637039453,3.62572448962667,17.6711083545132));
#14517=CARTESIAN_POINT('Ctrl Pts',(5.87751682509897,3.66912160962375,17.6652342158128));
#14518=CARTESIAN_POINT('Ctrl Pts',(5.76863137102735,3.7076568329352,17.6593600771125));
#14519=CARTESIAN_POINT('Ctrl Pts',(5.74109601726098,3.71740176181844,17.6578746033312));
#14520=CARTESIAN_POINT('Ctrl Pts',(5.71346314002777,3.72683602521232,17.6563891295499));
#14521=CARTESIAN_POINT('Ctrl Pts',(5.68574037104254,3.73595786345046,17.6549036557687));
#14522=CARTESIAN_POINT('Ctrl Pts',(5.57612218988211,3.77202638593598,17.6490299663781));
#14523=CARTESIAN_POINT('Ctrl Pts',(5.46473264421296,3.80332636779926,17.6431562769875));
#14524=CARTESIAN_POINT('Ctrl Pts',(5.35202433030282,3.82968273367584,17.637282587597));
#14525=CARTESIAN_POINT('Ctrl Pts',(5.23946153341441,3.85600507100801,17.6314164816912));
#14526=CARTESIAN_POINT('Ctrl Pts',(5.12558375292259,3.87739639218158,17.6255503757855));
#14527=CARTESIAN_POINT('Ctrl Pts',(5.01086068620922,3.89373072721203,17.6196842698797));
#14528=CARTESIAN_POINT('Ctrl Pts',(4.89625509445457,3.91004833609151,17.6138241707917));
#14529=CARTESIAN_POINT('Ctrl Pts',(4.78080634474241,3.92131920098427,17.6079640717036));
#14530=CARTESIAN_POINT('Ctrl Pts',(4.664995674457,3.92746809921336,17.6021039726156));
#14531=CARTESIAN_POINT('Ctrl Pts',(4.54500681939418,3.93383883566267,17.5960324545215));
#14532=CARTESIAN_POINT('Ctrl Pts',(4.42462987597543,3.93471094705703,17.5899609364274));
#14533=CARTESIAN_POINT('Ctrl Pts',(4.30440784814854,3.93005933464042,17.5838894183333));
#14534=CARTESIAN_POINT('Ctrl Pts',(4.18850549386054,3.92557485837541,17.5780360547365));
#14535=CARTESIAN_POINT('Ctrl Pts',(4.07274756249806,3.91595678793296,17.5721826911398));
#14536=CARTESIAN_POINT('Ctrl Pts',(3.95762121081433,3.90123567312347,17.566329327543));
#14537=CARTESIAN_POINT('Ctrl Pts',(3.8425121449649,3.88651676863982,17.5604768428091));
#14538=CARTESIAN_POINT('Ctrl Pts',(3.72803487993564,3.86669639568011,17.5546243580753));
#14539=CARTESIAN_POINT('Ctrl Pts',(3.61467069760924,3.84185689989403,17.5487718733414));
#14540=CARTESIAN_POINT('Ctrl Pts',(3.50129612130937,3.81701512665969,17.5429188520132));
#14541=CARTESIAN_POINT('Ctrl Pts',(3.38903523418058,3.78715340422412,17.537065830685));
#14542=CARTESIAN_POINT('Ctrl Pts',(3.27835768764028,3.75240489358708,17.5312128093568));
#14543=CARTESIAN_POINT('Ctrl Pts',(3.16764322800079,3.71764479365066,17.525357835933));
#14544=CARTESIAN_POINT('Ctrl Pts',(3.05851355296416,3.67799478834095,17.5195028625092));
#14545=CARTESIAN_POINT('Ctrl Pts',(2.95142107917391,3.63363721858553,17.5136478890854));
#14546=CARTESIAN_POINT('Ctrl Pts',(2.84420722982018,3.58922937522232,17.5077862798012));
#14547=CARTESIAN_POINT('Ctrl Pts',(2.73903557206171,3.54010347642444,17.5019246705171));
#14548=CARTESIAN_POINT('Ctrl Pts',(2.63633662217621,3.48648917114839,17.4960630612329));
#14549=CARTESIAN_POINT('Ctrl Pts',(2.53356842163459,3.43283871335255,17.4901974994226));
#14550=CARTESIAN_POINT('Ctrl Pts',(2.43327660559645,3.37469402921931,17.4843319376123));
#14551=CARTESIAN_POINT('Ctrl Pts',(2.33586376372488,3.31232878521873,17.4784663758019));
#14552=CARTESIAN_POINT('Ctrl Pts',(2.2383084803864,3.24987234793533,17.4725922371016));
#14553=CARTESIAN_POINT('Ctrl Pts',(2.14364090930449,3.18318327105191,17.4667180984013));
#14554=CARTESIAN_POINT('Ctrl Pts',(2.05223161849938,3.11257628061503,17.4608439597009));
#14555=CARTESIAN_POINT('Ctrl Pts',(2.02911570112263,3.09472092540131,17.4593584859197));
#14556=CARTESIAN_POINT('Ctrl Pts',(2.00620796999553,3.07661520573659,17.4578730121384));
#14557=CARTESIAN_POINT('Ctrl Pts',(1.98351404100473,3.05826458067885,17.4563875383571));
#14558=CARTESIAN_POINT('Ctrl Pts',(1.89378031993646,2.98570465194078,17.4505138489665));
#14559=CARTESIAN_POINT('Ctrl Pts',(1.80709336742514,2.90907116048081,17.444640159576));
#14560=CARTESIAN_POINT('Ctrl Pts',(1.72384565741476,2.82864951647413,17.4387664701854));
#14561=CARTESIAN_POINT('Ctrl Pts',(1.64070542801886,2.74833170436522,17.4329003642796));
#14562=CARTESIAN_POINT('Ctrl Pts',(1.56099590507748,2.6642357504569,17.4270342583739));
#14563=CARTESIAN_POINT('Ctrl Pts',(1.48507756957515,2.57668805561826,17.4211681524681));
#14564=CARTESIAN_POINT('Ctrl Pts',(1.40923697348118,2.48923000850377,17.4153080533801));
#14565=CARTESIAN_POINT('Ctrl Pts',(1.33718011201403,2.39832756122633,17.409447954292));
#14566=CARTESIAN_POINT('Ctrl Pts',(1.2692310787425,2.30434432240768,17.403587855204));
#14567=CARTESIAN_POINT('Ctrl Pts',(1.1988305993671,2.20697038274255,17.3975163371099));
#14568=CARTESIAN_POINT('Ctrl Pts',(1.13284027138534,2.10628947244678,17.3914448190158));
#14569=CARTESIAN_POINT('Ctrl Pts',(1.0715755530835,2.00274427572439,17.3853733009217));
#14570=CARTESIAN_POINT('Ctrl Pts',(1.01251212507178,1.90291954067149,17.3795199373249));
#14571=CARTESIAN_POINT('Ctrl Pts',(0.957840789573258,1.80043319510697,17.3736665737282));
#14572=CARTESIAN_POINT('Ctrl Pts',(0.90779996765182,1.69571116201616,17.3678132101314));
#14573=CARTESIAN_POINT('Ctrl Pts',(0.857766659191405,1.59100485258623,17.3619607253975));
#14574=CARTESIAN_POINT('Ctrl Pts',(0.812362659957376,1.48406389576237,17.3561082406636));
#14575=CARTESIAN_POINT('Ctrl Pts',(0.771779681740187,1.37533735684723,17.3502557559297));
#14576=CARTESIAN_POINT('Ctrl Pts',(0.731192982608776,1.26660084916827,17.3444027346015));
#14577=CARTESIAN_POINT('Ctrl Pts',(0.695428327675673,1.15607882103234,17.3385497132734));
#14578=CARTESIAN_POINT('Ctrl Pts',(0.664628423208093,1.04423811205542,17.3326966919452));
#14579=CARTESIAN_POINT('Ctrl Pts',(0.63381824637756,0.932360102042171,17.3268417185214));
#14580=CARTESIAN_POINT('Ctrl Pts',(0.607976222210408,0.819162934756042,
17.3209867450975));
#14581=CARTESIAN_POINT('Ctrl Pts',(0.587194387559713,0.705125628203866,
17.3151317716737));
#14582=CARTESIAN_POINT('Ctrl Pts',(0.566388999368772,0.590959075012283,
17.3092701623895));
#14583=CARTESIAN_POINT('Ctrl Pts',(0.550655321670228,0.475950888719086,
17.3034085531054));
#14584=CARTESIAN_POINT('Ctrl Pts',(0.540033765612626,0.36058733041429,17.2975469438212));
#14585=CARTESIAN_POINT('Ctrl Pts',(0.529405047361767,0.245145981614885,
17.2916813820109));
#14586=CARTESIAN_POINT('Ctrl Pts',(0.523895334361594,0.129349195304322,
17.2858158202005));
#14587=CARTESIAN_POINT('Ctrl Pts',(0.523492910215201,0.013683627931959,
17.2799502583902));
#14588=CARTESIAN_POINT('Ctrl Pts',(0.523089897626005,-0.102151070868716,
17.2740761196899));
#14589=CARTESIAN_POINT('Ctrl Pts',(0.527809061586433,-0.217853756583575,
17.2682019809895));
#14590=CARTESIAN_POINT('Ctrl Pts',(0.53758682377809,-0.332942422014075,
17.2623278422892));
#14591=CARTESIAN_POINT('Ctrl Pts',(0.540059460213178,-0.362046466664684,
17.2608423685079));
#14592=CARTESIAN_POINT('Ctrl Pts',(0.542855339607083,-0.391111295726141,
17.2593568947267));
#14593=CARTESIAN_POINT('Ctrl Pts',(0.545972919096128,-0.420129230717572,
17.2578714209454));
#14594=CARTESIAN_POINT('Ctrl Pts',(0.55830009295806,-0.534868608177082,
17.2519977315548));
#14595=CARTESIAN_POINT('Ctrl Pts',(0.57570199575384,-0.64925607920481,17.2461240421643));
#14596=CARTESIAN_POINT('Ctrl Pts',(0.598151558931453,-0.762807121295276,
17.2402503527737));
#14597=CARTESIAN_POINT('Ctrl Pts',(0.620572137613951,-0.876211558322706,
17.2343842468679));
#14598=CARTESIAN_POINT('Ctrl Pts',(0.648027337096813,-0.988781312398336,
17.2285181409622));
#14599=CARTESIAN_POINT('Ctrl Pts',(0.680438300338676,-1.10003652350658,
17.2226520350564));
#14600=CARTESIAN_POINT('Ctrl Pts',(0.712816075167087,-1.21117781069601,
17.2167919359684));
#14601=CARTESIAN_POINT('Ctrl Pts',(0.750139405009676,-1.32100683807485,
17.2109318368804));
#14602=CARTESIAN_POINT('Ctrl Pts',(0.792278440894378,-1.42905415158187,
17.2050717377923));
#14603=CARTESIAN_POINT('Ctrl Pts',(0.835937757059272,-1.54099956566485,
17.1990002196982));
#14604=CARTESIAN_POINT('Ctrl Pts',(0.884766731611055,-1.65103183515588,
17.1929287016041));
#14605=CARTESIAN_POINT('Ctrl Pts',(0.938564386476564,-1.75864589466417,
17.18685718351));
#14606=CARTESIAN_POINT('Ctrl Pts',(0.990429048608736,-1.86239329501131,
17.1810038199133));
#14607=CARTESIAN_POINT('Ctrl Pts',(1.04691127806465,-1.96389286992691,17.1751504563165));
#14608=CARTESIAN_POINT('Ctrl Pts',(1.1077824187438,-2.06271337541874,17.1692970927198));
#14609=CARTESIAN_POINT('Ctrl Pts',(1.16864441982601,-2.16151904334421,17.1634446079859));
#14610=CARTESIAN_POINT('Ctrl Pts',(1.23389380521009,-2.2576460900056,17.157592123252));
#14611=CARTESIAN_POINT('Ctrl Pts',(1.30325715058331,-2.35068997590938,17.1517396385181));
#14612=CARTESIAN_POINT('Ctrl Pts',(1.372626855644,-2.44374239268825,17.1458866171899));
#14613=CARTESIAN_POINT('Ctrl Pts',(1.44611102357843,-2.53371075550955,17.1400335958617));
#14614=CARTESIAN_POINT('Ctrl Pts',(1.52339472781864,-2.62022206898113,17.1341805745336));
#14615=CARTESIAN_POINT('Ctrl Pts',(1.60070420766672,-2.70676223564645,17.1283256011097));
#14616=CARTESIAN_POINT('Ctrl Pts',(1.68181546853385,-2.78984275234677,17.1224706276859));
#14617=CARTESIAN_POINT('Ctrl Pts',(1.76637588188335,-2.86912659957476,17.1166156542621));
#14618=CARTESIAN_POINT('Ctrl Pts',(1.85103213360002,-2.94850030485997,17.110754044978));
#14619=CARTESIAN_POINT('Ctrl Pts',(1.93914503871145,-3.02406846932883,17.1048924356938));
#14620=CARTESIAN_POINT('Ctrl Pts',(2.03032789547589,-3.09553352841438,17.0990308264096));
#14621=CARTESIAN_POINT('Ctrl Pts',(2.12157223751029,-3.1670467769141,17.0931652645993));
#14622=CARTESIAN_POINT('Ctrl Pts',(2.2158903179078,-3.23445117118716,17.087299702789));
#14623=CARTESIAN_POINT('Ctrl Pts',(2.31286684386495,-3.29749273552403,17.0814341409786));
#14624=CARTESIAN_POINT('Ctrl Pts',(2.40998517328808,-3.36062648208991,17.0755600022783));
#14625=CARTESIAN_POINT('Ctrl Pts',(2.50976935170389,-3.41938445795698,17.069685863578));
#14626=CARTESIAN_POINT('Ctrl Pts',(2.61177987826993,-3.47355878779839,17.0638117248776));
#14627=CARTESIAN_POINT('Ctrl Pts',(2.63757667510419,-3.48725859141274,17.0623262510964));
#14628=CARTESIAN_POINT('Ctrl Pts',(2.6635157518535,-3.50066551228837,17.0608407773151));
#14629=CARTESIAN_POINT('Ctrl Pts',(2.68958981982905,-3.51377668432824,17.0593553035338));
#14630=CARTESIAN_POINT('Ctrl Pts',(2.79268889728607,-3.56561937120618,17.0534816141432));
#14631=CARTESIAN_POINT('Ctrl Pts',(2.89824332382782,-3.61300695171493,17.0476079247527));
#14632=CARTESIAN_POINT('Ctrl Pts',(3.00583127727128,-3.65569950751262,17.0417342353621));
#14633=CARTESIAN_POINT('Ctrl Pts',(3.11328032455943,-3.69833694320999,17.0358681294563));
#14634=CARTESIAN_POINT('Ctrl Pts',(3.22275729703346,-3.73629125797427,17.0300020235506));
#14635=CARTESIAN_POINT('Ctrl Pts',(3.33381621540456,-3.76936857931771,17.0241359176448));
#14636=CARTESIAN_POINT('Ctrl Pts',(3.44476141085816,-3.80241202990551,17.0182758185568));
#14637=CARTESIAN_POINT('Ctrl Pts',(3.55728493650575,-3.83058830328186,17.0124157194687));
#14638=CARTESIAN_POINT('Ctrl Pts',(3.67092191405302,-3.85375201704537,17.0065556203807));
#14639=CARTESIAN_POINT('Ctrl Pts',(3.78865865450265,-3.87775142475656,17.0004841022866));
#14640=CARTESIAN_POINT('Ctrl Pts',(3.90759028551902,-3.89636959407866,16.9944125841925));
#14641=CARTESIAN_POINT('Ctrl Pts',(4.02718344456594,-3.90950160771162,16.9883410660984));
#14642=CARTESIAN_POINT('Ctrl Pts',(4.14247952583186,-3.9221617775999,16.9824877025016));
#14643=CARTESIAN_POINT('Ctrl Pts',(4.25838996891244,-3.92972320188552,16.9766343389049));
#14644=CARTESIAN_POINT('Ctrl Pts',(4.3744284394501,-3.9321442406143,16.9707809753081));
#14645=CARTESIAN_POINT('Ctrl Pts',(4.49044948720186,-3.93456491583226,16.9649284905742));
#14646=CARTESIAN_POINT('Ctrl Pts',(4.60659811124423,-3.93184673152901,16.9590760058403));
#14647=CARTESIAN_POINT('Ctrl Pts',(4.7223861479458,-3.92400014359312,16.9532235211064));
#14648=CARTESIAN_POINT('Ctrl Pts',(4.83818480085579,-3.91615283623047,16.9473704997782));
#14649=CARTESIAN_POINT('Ctrl Pts',(4.95362238848057,-3.90317621844511,16.94151747845));
#14650=CARTESIAN_POINT('Ctrl Pts',(5.06821475517741,-3.88513272115375,16.9356644571219));
#14651=CARTESIAN_POINT('Ctrl Pts',(5.1828453406414,-3.8670832060076,16.929809483698));
#14652=CARTESIAN_POINT('Ctrl Pts',(5.29662973674041,-3.84396351528701,16.9239545102742));
#14653=CARTESIAN_POINT('Ctrl Pts',(5.40909358005421,-3.81588726403817,16.9180995368504));
#14654=CARTESIAN_POINT('Ctrl Pts',(5.52168488668901,-3.78777919196479,16.9122379275662));
#14655=CARTESIAN_POINT('Ctrl Pts',(5.63295225219454,-3.75470344704765,16.9063763182821));
#14656=CARTESIAN_POINT('Ctrl Pts',(5.74243599603799,-3.71682366521299,16.9005147089979));
#14657=CARTESIAN_POINT('Ctrl Pts',(5.85199356557387,-3.67891834076328,16.8946491471876));
#14658=CARTESIAN_POINT('Ctrl Pts',(5.95976473546107,-3.63620268089117,16.8887835853773));
#14659=CARTESIAN_POINT('Ctrl Pts',(6.06531095373924,-3.58888797675063,16.8829180235669));
#14660=CARTESIAN_POINT('Ctrl Pts',(6.17101150647557,-3.54150408690788,16.8770438848666));
#14661=CARTESIAN_POINT('Ctrl Pts',(6.27448024684995,-3.48950791632331,16.8711697461663));
#14662=CARTESIAN_POINT('Ctrl Pts',(6.37530423800722,-3.43315608981188,16.8652956074659));
#14663=CARTESIAN_POINT('Ctrl Pts',(6.40080097940688,-3.41890563283761,16.8638101336846));
#14664=CARTESIAN_POINT('Ctrl Pts',(6.42612874043806,-3.40437684241596,16.8623246599034));
#14665=CARTESIAN_POINT('Ctrl Pts',(6.4512811614294,-3.38957428955087,16.8608391861221));
#14666=CARTESIAN_POINT('Ctrl Pts',(6.55073596849879,-3.3310437393569,16.8549654967315));
#14667=CARTESIAN_POINT('Ctrl Pts',(6.64777818281768,-3.26803478452412,16.849091807341));
#14668=CARTESIAN_POINT('Ctrl Pts',(6.74197752530337,-3.20077182352804,16.8432181179504));
#14669=CARTESIAN_POINT('Ctrl Pts',(6.8360552475882,-3.13359570533373,16.8373520120446));
#14670=CARTESIAN_POINT('Ctrl Pts',(6.92729706413442,-3.06217674129316,16.8314859061389));
#14671=CARTESIAN_POINT('Ctrl Pts',(7.01529829275506,-2.98678459118286,16.8256198002331));
#14672=CARTESIAN_POINT('Ctrl Pts',(7.10320940923867,-2.91146964167383,16.8197597011451));
#14673=CARTESIAN_POINT('Ctrl Pts',(7.18788622632745,-2.83218986585923,16.8138996020571));
#14674=CARTESIAN_POINT('Ctrl Pts',(7.26895456310386,-2.74925709143524,16.808039502969));
#14675=CARTESIAN_POINT('Ctrl Pts',(7.35294766052476,-2.66333229170989,16.8019679848749));
#14676=CARTESIAN_POINT('Ctrl Pts',(7.43306662264047,-2.57348619555301,16.7958964667808));
#14677=CARTESIAN_POINT('Ctrl Pts',(7.50893414571678,-2.48011011502297,16.7898249486867));
#14678=CARTESIAN_POINT('Ctrl Pts',(7.58207568805712,-2.3900891116907,16.78397158509));
#14679=CARTESIAN_POINT('Ctrl Pts',(7.65126576583956,-2.29678777681912,16.7781182214932));
#14680=CARTESIAN_POINT('Ctrl Pts',(7.71620574220309,-2.20059220757009,16.7722648578965));
#14681=CARTESIAN_POINT('Ctrl Pts',(7.78113596804769,-2.10441108176208,16.7664123731626));
#14682=CARTESIAN_POINT('Ctrl Pts',(7.84181713023146,-2.00533692797378,16.7605598884287));
#14683=CARTESIAN_POINT('Ctrl Pts',(7.89799337677209,-1.903785622172,16.7547074036948));
#14684=CARTESIAN_POINT('Ctrl Pts',(7.95417477392029,-1.80222500547895,16.7488543823666));
#14685=CARTESIAN_POINT('Ctrl Pts',(8.00585023434433,-1.69818714681336,16.7430013610384));
#14686=CARTESIAN_POINT('Ctrl Pts',(8.0528097538547,-1.59211273035481,16.7371483397103));
#14687=CARTESIAN_POINT('Ctrl Pts',(8.09978493527166,-1.48600293602997,16.7312933662864));
#14688=CARTESIAN_POINT('Ctrl Pts',(8.14204088106384,-1.37785561086735,16.7254383928626));
#14689=CARTESIAN_POINT('Ctrl Pts',(8.17941590592433,-1.26813095796855,16.7195834194388));
#14690=CARTESIAN_POINT('Ctrl Pts',(8.21683329057491,-1.15828194626918,16.7137218101547));
#14691=CARTESIAN_POINT('Ctrl Pts',(8.24935857967433,-1.04685242999379,16.7078602008705));
#14692=CARTESIAN_POINT('Ctrl Pts',(8.27688008058664,-0.934317390893255,
16.7019985915864));
#14693=CARTESIAN_POINT('Ctrl Pts',(8.30442013944912,-0.82170646858944,16.696133029776));
#14694=CARTESIAN_POINT('Ctrl Pts',(8.32694961146846,-0.707988943345037,
16.6902674679657));
#14695=CARTESIAN_POINT('Ctrl Pts',(8.34440830307059,-0.59364787675788,16.6844019061553));
#14696=CARTESIAN_POINT('Ctrl Pts',(8.36189252356189,-0.479139615487285,
16.678527767455));
#14697=CARTESIAN_POINT('Ctrl Pts',(8.37429112164412,-0.364006402400336,
16.6726536287547));
#14698=CARTESIAN_POINT('Ctrl Pts',(8.38159588416645,-0.248734350329785,
16.6667794900543));
#14699=CARTESIAN_POINT('Ctrl Pts',(8.38344313935722,-0.219583930191288,
16.665294016273));
#14700=CARTESIAN_POINT('Ctrl Pts',(8.38496490290308,-0.190424618373388,
16.6638085424917));
#14701=CARTESIAN_POINT('Ctrl Pts',(8.38616156821618,-0.161264236942553,
16.6623230687105));
#14702=CARTESIAN_POINT('Ctrl Pts',(8.38835261922407,-0.107872630763612,
16.6596032198186));
#14703=CARTESIAN_POINT('Ctrl Pts',(8.38945560312462,-0.0544360677886508,
16.6568833709268));
#14704=CARTESIAN_POINT('Ctrl Pts',(8.38946898299941,-0.000984499569211592,
16.654163522035));
#14705=CARTESIAN_POINT('',(8.38330870139309,-0.00111159115176508,19.154163522035));
#14706=CARTESIAN_POINT('Ctrl Pts',(8.38330870139309,-0.00111159115176508,
19.154163522035));
#14707=CARTESIAN_POINT('Ctrl Pts',(8.38147360828864,0.724094734411765,19.1176145072401));
#14708=CARTESIAN_POINT('Ctrl Pts',(7.84121757765765,2.76483039537692,19.0148934533079));
#14709=CARTESIAN_POINT('Ctrl Pts',(4.55780727041761,4.64794687683432,18.8460003602387));
#14710=CARTESIAN_POINT('Ctrl Pts',(0.605699254871401,2.60485146316644,18.6474842428269));
#14711=CARTESIAN_POINT('Ctrl Pts',(0.180053019792298,-1.82371737090629,
18.4489681254154));
#14712=CARTESIAN_POINT('Ctrl Pts',(3.67066729059547,-4.58216052750365,18.2504520080036));
#14713=CARTESIAN_POINT('Ctrl Pts',(7.52217034079766,-3.26685715566783,18.0688504735435));
#14714=CARTESIAN_POINT('Ctrl Pts',(8.37983385625592,-0.97047922611876,17.9534209782207));
#14715=CARTESIAN_POINT('Ctrl Pts',(8.38858227448227,0.00358766171095831,
17.904163522035));
#14716=CARTESIAN_POINT('',(8.39024757142292,-0.00302155333681673,20.4041631666841));
#14717=CARTESIAN_POINT('Ctrl Pts',(8.39265998963715,-0.00300172473988639,
20.404162067119));
#14718=CARTESIAN_POINT('Ctrl Pts',(8.38321720628087,1.10505925672828,20.3479791054527));
#14719=CARTESIAN_POINT('Ctrl Pts',(7.31619850019849,3.53408620393106,20.2256241046493));
#14720=CARTESIAN_POINT('Ctrl Pts',(3.19725112513313,4.47527090540738,20.0370970647086));
#14721=CARTESIAN_POINT('Ctrl Pts',(0.013229802472921,1.36795617003671,19.838580947297));
#14722=CARTESIAN_POINT('Ctrl Pts',(0.898242515440645,-2.99210680286265,
19.6400648298852));
#14723=CARTESIAN_POINT('Ctrl Pts',(5.04181145526696,-4.6120552824946,19.4415487124736));
#14724=CARTESIAN_POINT('Ctrl Pts',(7.98514998524053,-2.48773831511406,19.2795816098569));
#14725=CARTESIAN_POINT('Ctrl Pts',(8.38479604675681,-0.588892267483202,
19.1837865463773));
#14726=CARTESIAN_POINT('Ctrl Pts',(8.38330870139309,-0.00111159115176508,
19.154163522035));
#14727=CARTESIAN_POINT('',(8.39034187497082,0.00295420694097821,21.6541639142457));
#14728=CARTESIAN_POINT('Ctrl Pts',(8.38946799139497,0.0029612832834954,
21.654163522035));
#14729=CARTESIAN_POINT('Ctrl Pts',(8.38932489603607,0.193011958324324,21.6445176826906));
#14730=CARTESIAN_POINT('Ctrl Pts',(8.37540471230823,0.382553267708013,21.6348718433462));
#14731=CARTESIAN_POINT('Ctrl Pts',(8.34793638037932,0.570062675618605,21.6252260040018));
#14732=CARTESIAN_POINT('Ctrl Pts',(8.33120994712477,0.684243747994348,21.6193523132224));
#14733=CARTESIAN_POINT('Ctrl Pts',(8.30942604979843,0.797878198448378,21.6134786224429));
#14734=CARTESIAN_POINT('Ctrl Pts',(8.28263035283746,0.91048290201921,21.6076049316635));
#14735=CARTESIAN_POINT('Ctrl Pts',(8.25586925156278,1.02294222265772,21.601738824354));
#14736=CARTESIAN_POINT('Ctrl Pts',(8.22410931350316,1.13437404209587,21.5958727170445));
#14737=CARTESIAN_POINT('Ctrl Pts',(8.18744777420902,1.24430188418961,21.5900066097351));
#14738=CARTESIAN_POINT('Ctrl Pts',(8.15082377577351,1.35411716184502,21.5841465092303));
#14739=CARTESIAN_POINT('Ctrl Pts',(8.10930828957067,1.46243113584916,21.5782864087255));
#14740=CARTESIAN_POINT('Ctrl Pts',(8.06304910562404,1.56877968749157,21.5724263082207));
#14741=CARTESIAN_POINT('Ctrl Pts',(8.01512101159534,1.67896501607009,21.5663547906528));
#14742=CARTESIAN_POINT('Ctrl Pts',(7.96210058167485,1.78703999080972,21.5602832730848));
#14743=CARTESIAN_POINT('Ctrl Pts',(7.90420805046819,1.89250764127977,21.5542117555169));
#14744=CARTESIAN_POINT('Ctrl Pts',(7.84839562560396,1.99418578861201,21.5483583904798));
#14745=CARTESIAN_POINT('Ctrl Pts',(7.78805540381289,2.09344035878736,21.5425050254427));
#14746=CARTESIAN_POINT('Ctrl Pts',(7.7234324412104,2.18984921120542,21.5366516604057));
#14747=CARTESIAN_POINT('Ctrl Pts',(7.65881918145674,2.28624358826544,21.5307991742252));
#14748=CARTESIAN_POINT('Ctrl Pts',(7.58992468945802,2.3797927540567,21.5249466880447));
#14749=CARTESIAN_POINT('Ctrl Pts',(7.5170377304785,2.47010297279157,21.5190942018642));
#14750=CARTESIAN_POINT('Ctrl Pts',(7.44414408868623,2.56042147183186,21.5132411790847));
#14751=CARTESIAN_POINT('Ctrl Pts',(7.36725751171053,2.64750011194895,21.5073881563052));
#14752=CARTESIAN_POINT('Ctrl Pts',(7.28670702447934,2.73097827271423,21.5015351335258));
#14753=CARTESIAN_POINT('Ctrl Pts',(7.20612967206777,2.8144842750969,21.4956801586474));
#14754=CARTESIAN_POINT('Ctrl Pts',(7.12188626625766,2.8943871131849,21.4898251837691));
#14755=CARTESIAN_POINT('Ctrl Pts',(7.03434212388975,2.97036356440778,21.4839702088908));
#14756=CARTESIAN_POINT('Ctrl Pts',(6.9466987615445,3.04642612512427,21.4781085981547));
#14757=CARTESIAN_POINT('Ctrl Pts',(6.85574750811192,3.11855314599317,21.4722469874187));
#14758=CARTESIAN_POINT('Ctrl Pts',(6.76188621259502,3.18646213936795,21.4663853766826));
#14759=CARTESIAN_POINT('Ctrl Pts',(6.66796162572878,3.25441692426735,21.4605198134201));
#14760=CARTESIAN_POINT('Ctrl Pts',(6.57112343373736,3.31814779158435,21.4546542501576));
#14761=CARTESIAN_POINT('Ctrl Pts',(6.47179638086606,3.37741690883146,21.4487886868951));
#14762=CARTESIAN_POINT('Ctrl Pts',(6.37232408770054,3.43677269193423,21.4429145467534));
#14763=CARTESIAN_POINT('Ctrl Pts',(6.27035603288893,3.4916535093278,21.4370404066117));
#14764=CARTESIAN_POINT('Ctrl Pts',(6.16633937963864,3.5418685249559,21.43116626647));
#14765=CARTESIAN_POINT('Ctrl Pts',(6.14003551731337,3.5545669613742,21.4296808065101));
#14766=CARTESIAN_POINT('Ctrl Pts',(6.11360073532189,3.56696727036229,21.4281953465501));
#14767=CARTESIAN_POINT('Ctrl Pts',(6.08704242687941,3.57906686804649,21.4267098865902));
#14768=CARTESIAN_POINT('Ctrl Pts',(5.98202764443305,3.62691014922707,21.4208361971999));
#14769=CARTESIAN_POINT('Ctrl Pts',(5.87473049369302,3.67020727738114,21.4149625078096));
#14770=CARTESIAN_POINT('Ctrl Pts',(5.76558170321074,3.70873471798612,21.4090888184194));
#14771=CARTESIAN_POINT('Ctrl Pts',(5.65657383400523,3.74721241606903,21.4032227125103));
#14772=CARTESIAN_POINT('Ctrl Pts',(5.54571946528469,3.78093253680742,21.3973566066013));
#14773=CARTESIAN_POINT('Ctrl Pts',(5.43347169575851,3.80971848566684,21.3914905006923));
#14774=CARTESIAN_POINT('Ctrl Pts',(5.32133886645076,3.83847495809868,21.3856304015974));
#14775=CARTESIAN_POINT('Ctrl Pts',(5.2078158722244,3.86230720652487,21.3797703025026));
#14776=CARTESIAN_POINT('Ctrl Pts',(5.09337283381983,3.88108781680694,21.3739102034077));
#14777=CARTESIAN_POINT('Ctrl Pts',(4.97480095183767,3.90054598863602,21.3678386853149));
#14778=CARTESIAN_POINT('Ctrl Pts',(4.85524181200714,3.91458098684631,21.361767167222));
#14779=CARTESIAN_POINT('Ctrl Pts',(4.73523241404701,3.92310846373235,21.3556956491291));
#14780=CARTESIAN_POINT('Ctrl Pts',(4.61953504933254,3.93132954158249,21.3498422855167));
#14781=CARTESIAN_POINT('Ctrl Pts',(4.50341967334397,3.93443203427796,21.3439889219043));
#14782=CARTESIAN_POINT('Ctrl Pts',(4.38737386119142,3.93239301788551,21.338135558292));
#14783=CARTESIAN_POINT('Ctrl Pts',(4.27134547286255,3.93035430764338,21.3322830735392));
#14784=CARTESIAN_POINT('Ctrl Pts',(4.15538704057191,3.92317563055062,21.3264305887864));
#14785=CARTESIAN_POINT('Ctrl Pts',(4.03998596579679,3.91088619033394,21.3205781040336));
#14786=CARTESIAN_POINT('Ctrl Pts',(3.92457431022854,3.89859562333378,21.3147250826833));
#14787=CARTESIAN_POINT('Ctrl Pts',(3.80972052460738,3.88119340544641,21.308872061333));
#14788=CARTESIAN_POINT('Ctrl Pts',(3.69590600846696,3.85876052306165,21.3030190399827));
#14789=CARTESIAN_POINT('Ctrl Pts',(3.58205353292439,3.83632015886496,21.2971640665335));
#14790=CARTESIAN_POINT('Ctrl Pts',(3.46924142122266,3.80884587373843,21.2913090930843));
#14791=CARTESIAN_POINT('Ctrl Pts',(3.35793932137559,3.77646942418624,21.2854541196351));
#14792=CARTESIAN_POINT('Ctrl Pts',(3.24651107480554,3.74405628006119,21.2795925103209));
#14793=CARTESIAN_POINT('Ctrl Pts',(3.13659665287681,3.70672999757413,21.2737309010066));
#14794=CARTESIAN_POINT('Ctrl Pts',(3.02864910972258,3.66467175305062,21.2678692916924));
#14795=CARTESIAN_POINT('Ctrl Pts',(2.92062877669618,3.62258514832407,21.2620037298492));
#14796=CARTESIAN_POINT('Ctrl Pts',(2.81457834037405,3.57576039443417,21.2561381680059));
#14797=CARTESIAN_POINT('Ctrl Pts',(2.71092791097229,3.52442547597468,21.2502726061627));
#14798=CARTESIAN_POINT('Ctrl Pts',(2.60712591915362,3.47301549324041,21.2443984674257));
#14799=CARTESIAN_POINT('Ctrl Pts',(2.50573129849915,3.4170823828248,21.2385243286886));
#14800=CARTESIAN_POINT('Ctrl Pts',(2.40714682128416,3.35689844536181,21.2326501899515));
#14801=CARTESIAN_POINT('Ctrl Pts',(2.38221641974906,3.34167891213201,21.2311647163605));
#14802=CARTESIAN_POINT('Ctrl Pts',(2.35746556750933,3.32618774336432,21.2296792427695));
#14803=CARTESIAN_POINT('Ctrl Pts',(2.33290044391734,3.31042975102834,21.2281937691785));
#14804=CARTESIAN_POINT('Ctrl Pts',(2.2357678544058,3.24812130811069,21.2223200801654));
#14805=CARTESIAN_POINT('Ctrl Pts',(2.14121813868295,3.18143046089737,21.2164463911523));
#14806=CARTESIAN_POINT('Ctrl Pts',(2.04967263659629,3.11059797367248,21.2105727021392));
#14807=CARTESIAN_POINT('Ctrl Pts',(1.95824532845483,3.03985693792168,21.204706596617));
#14808=CARTESIAN_POINT('Ctrl Pts',(1.86981484420736,2.96498514660278,21.1988404910948));
#14809=CARTESIAN_POINT('Ctrl Pts',(1.78477520674591,2.88626760843867,21.1929743855726));
#14810=CARTESIAN_POINT('Ctrl Pts',(1.69982264887592,2.80763067611049,21.1871142868736));
#14811=CARTESIAN_POINT('Ctrl Pts',(1.61825433271175,2.72515610892687,21.1812541881747));
#14812=CARTESIAN_POINT('Ctrl Pts',(1.54043218228572,2.63916988052344,21.1753940894757));
#14813=CARTESIAN_POINT('Ctrl Pts',(1.4598023789505,2.55008145714075,21.1693225712378));
#14814=CARTESIAN_POINT('Ctrl Pts',(1.38319450904063,2.45722347877443,21.163251053));
#14815=CARTESIAN_POINT('Ctrl Pts',(1.31097056336446,2.36100146482477,21.1571795347621));
#14816=CARTESIAN_POINT('Ctrl Pts',(1.24134168818897,2.26823679327836,21.1513261715658));
#14817=CARTESIAN_POINT('Ctrl Pts',(1.17578739168021,2.17234603005742,21.1454728083696));
#14818=CARTESIAN_POINT('Ctrl Pts',(1.1145912561187,2.07372646099095,21.1396194451733));
#14819=CARTESIAN_POINT('Ctrl Pts',(1.05340430898868,1.97512169938158,21.1337669608434));
#14820=CARTESIAN_POINT('Ctrl Pts',(0.996574439458465,1.87378929756515,21.1279144765135));
#14821=CARTESIAN_POINT('Ctrl Pts',(0.944341332402823,1.77015465437184,21.1220619921837));
#14822=CARTESIAN_POINT('Ctrl Pts',(0.89210343630009,1.66651050932781,21.1162089712626));
#14823=CARTESIAN_POINT('Ctrl Pts',(0.844463326450425,1.56056407224726,21.1103559503416));
#14824=CARTESIAN_POINT('Ctrl Pts',(0.80161392064252,1.45276377035986,21.1045029294206));
#14825=CARTESIAN_POINT('Ctrl Pts',(0.758750223749061,1.34492751503722,21.0986479564066));
#14826=CARTESIAN_POINT('Ctrl Pts',(0.720680560556225,1.23523654916782,21.0927929833926));
#14827=CARTESIAN_POINT('Ctrl Pts',(0.687548815718343,1.12415694805401,21.0869380103786));
#14828=CARTESIAN_POINT('Ctrl Pts',(0.654379520311777,1.01295145250839,21.0810764015063));
#14829=CARTESIAN_POINT('Ctrl Pts',(0.626159431681027,0.900354576560428,
21.0752147926339));
#14830=CARTESIAN_POINT('Ctrl Pts',(0.602981910917189,0.786845242503738,
21.0693531837616));
#14831=CARTESIAN_POINT('Ctrl Pts',(0.579788761386301,0.673259368296008,
21.0634876223647));
#14832=CARTESIAN_POINT('Ctrl Pts',(0.561645014854082,0.558760217870424,
21.0576220609678));
#14833=CARTESIAN_POINT('Ctrl Pts',(0.54859226094128,0.443832808778391,21.0517564995709));
#14834=CARTESIAN_POINT('Ctrl Pts',(0.535520420697833,0.328737347599823,
21.0458823612833));
#14835=CARTESIAN_POINT('Ctrl Pts',(0.527554458298878,0.213212788560315,
21.0400082229957));
#14836=CARTESIAN_POINT('Ctrl Pts',(0.524683904091009,0.0977452010752936,
21.034134084708));
#14837=CARTESIAN_POINT('Ctrl Pts',(0.523957985853879,0.0685452551822368,
21.032648607061));
#14838=CARTESIAN_POINT('Ctrl Pts',(0.523557662259861,0.0393489297663216,
21.0311631294139));
#14839=CARTESIAN_POINT('Ctrl Pts',(0.523482239653076,0.0101640260651543,
21.0296776517669));
#14840=CARTESIAN_POINT('Ctrl Pts',(0.523184013030639,-0.105235263722956,
21.0238039621628));
#14841=CARTESIAN_POINT('Ctrl Pts',(0.527968556727335,-0.220839887055731,
21.0179302725588));
#14842=CARTESIAN_POINT('Ctrl Pts',(0.53786196686908,-0.336165268047883,
21.0120565829547));
#14843=CARTESIAN_POINT('Ctrl Pts',(0.547742603693473,-0.451341753192286,
21.006190476833));
#14844=CARTESIAN_POINT('Ctrl Pts',(0.562718954643329,-0.566239305094551,
21.0003243707113));
#14845=CARTESIAN_POINT('Ctrl Pts',(0.582765128113554,-0.680372317202752,
20.9944582645896));
#14846=CARTESIAN_POINT('Ctrl Pts',(0.602790774565711,-0.794388458607166,
20.9885981652834));
#14847=CARTESIAN_POINT('Ctrl Pts',(0.627875846305067,-0.90764121293055,
20.9827380659773));
#14848=CARTESIAN_POINT('Ctrl Pts',(0.657942627492596,-1.01964973908694,
20.9768779666711));
#14849=CARTESIAN_POINT('Ctrl Pts',(0.689094147977195,-1.13569927146781,
20.9708064486579));
#14850=CARTESIAN_POINT('Ctrl Pts',(0.725593582909424,-1.25041265292102,
20.9647349306448));
#14851=CARTESIAN_POINT('Ctrl Pts',(0.767296409776802,-1.36326586395718,
20.9586634126316));
#14852=CARTESIAN_POINT('Ctrl Pts',(0.807500822808823,-1.47206417451096,
20.9528100488127));
#14853=CARTESIAN_POINT('Ctrl Pts',(0.852540983897707,-1.57913326801493,
20.9469566849938));
#14854=CARTESIAN_POINT('Ctrl Pts',(0.902236783211508,-1.68401947556852,
20.9411033211749));
#14855=CARTESIAN_POINT('Ctrl Pts',(0.95192512087805,-1.78888993483163,20.9352508362177));
#14856=CARTESIAN_POINT('Ctrl Pts',(1.00626752998871,-1.89157778658281,20.9293983512605));
#14857=CARTESIAN_POINT('Ctrl Pts',(1.06503647993748,-1.99165100893663,20.9235458663033));
#14858=CARTESIAN_POINT('Ctrl Pts',(1.12381081821856,-2.09173340667606,20.9176928447509));
#14859=CARTESIAN_POINT('Ctrl Pts',(1.18701229491361,-2.18920034218853,20.9118398231986));
#14860=CARTESIAN_POINT('Ctrl Pts',(1.25436867559231,-2.2836466084281,20.9059868016462));
#14861=CARTESIAN_POINT('Ctrl Pts',(1.32174752093128,-2.37812437433055,20.9001318279976));
#14862=CARTESIAN_POINT('Ctrl Pts',(1.39328378598043,-2.4695791315016,20.8942768543489));
#14863=CARTESIAN_POINT('Ctrl Pts',(1.46866382516935,-2.55763730863785,20.8884218807003));
#14864=CARTESIAN_POINT('Ctrl Pts',(1.544129297945,-2.64579528840083,20.8825602711915));
#14865=CARTESIAN_POINT('Ctrl Pts',(1.62344697120118,-2.73054869055349,20.8766986616827));
#14866=CARTESIAN_POINT('Ctrl Pts',(1.70626501463763,-2.81155943466489,20.8708370521739));
#14867=CARTESIAN_POINT('Ctrl Pts',(1.78913890288927,-2.89262480491627,20.8649714901387));
#14868=CARTESIAN_POINT('Ctrl Pts',(1.875517554177,-2.96994221701334,20.8591059281036));
#14869=CARTESIAN_POINT('Ctrl Pts',(1.96501595050223,-3.04321379020151,20.8532403660684));
#14870=CARTESIAN_POINT('Ctrl Pts',(2.05464521540632,-3.11659250437821,20.8473662271447));
#14871=CARTESIAN_POINT('Ctrl Pts',(2.14740299994959,-3.18591332641153,20.841492088221));
#14872=CARTESIAN_POINT('Ctrl Pts',(2.24287518041693,-3.2509215511383,20.8356179492974));
#14873=CARTESIAN_POINT('Ctrl Pts',(2.26701850066163,-3.26736104566367,20.83413247765));
#14874=CARTESIAN_POINT('Ctrl Pts',(2.29133528512573,-3.2835249799823,20.8326470060026));
#14875=CARTESIAN_POINT('Ctrl Pts',(2.31581860241582,-3.29940970789782,20.8311615343553));
#14876=CARTESIAN_POINT('Ctrl Pts',(2.41262785544023,-3.36221936011026,20.8252878449828));
#14877=CARTESIAN_POINT('Ctrl Pts',(2.51236506985887,-3.42086923424214,20.8194141556103));
#14878=CARTESIAN_POINT('Ctrl Pts',(2.61463719975846,-3.47507470831156,20.8135404662378));
#14879=CARTESIAN_POINT('Ctrl Pts',(2.71677728673431,-3.52921019802369,20.8076743603498));
#14880=CARTESIAN_POINT('Ctrl Pts',(2.82144541892948,-3.57891250723855,20.8018082544619));
#14881=CARTESIAN_POINT('Ctrl Pts',(2.92821950130668,-3.62394014093605,20.795942148574));
#14882=CARTESIAN_POINT('Ctrl Pts',(3.03488424838858,-3.6689216669123,20.7900820495035));
#14883=CARTESIAN_POINT('Ctrl Pts',(3.14365027784584,-3.709237879147,20.784221950433));
#14884=CARTESIAN_POINT('Ctrl Pts',(3.25407140468637,-3.74469341433325,20.7783618513625));
#14885=CARTESIAN_POINT('Ctrl Pts',(3.36847627434058,-3.78142810449233,20.7722903332617));
#14886=CARTESIAN_POINT('Ctrl Pts',(3.48465752136863,-3.8129445599251,20.7662188151609));
#14887=CARTESIAN_POINT('Ctrl Pts',(3.60209646100962,-3.83908014804578,20.7601472970601));
#14888=CARTESIAN_POINT('Ctrl Pts',(3.71531572524634,-3.8642766634985,20.7542939334801));
#14889=CARTESIAN_POINT('Ctrl Pts',(3.82970341985477,-3.88447223730536,20.7484405699001));
#14890=CARTESIAN_POINT('Ctrl Pts',(3.9447806840801,-3.89957227893647,20.74258720632));
#14891=CARTESIAN_POINT('Ctrl Pts',(4.05984066984796,-3.91467005334798,20.7367347216025));
#14892=CARTESIAN_POINT('Ctrl Pts',(4.17558960983971,-3.92467376310736,20.730882236885));
#14893=CARTESIAN_POINT('Ctrl Pts',(4.29154112620292,-3.92954040078583,20.7250297521675));
#14894=CARTESIAN_POINT('Ctrl Pts',(4.40750327377036,-3.93440748466991,20.7191767308554));
#14895=CARTESIAN_POINT('Ctrl Pts',(4.5236676218275,-3.93413654284151,20.7133237095432));
#14896=CARTESIAN_POINT('Ctrl Pts',(4.63954609087238,-3.92873666942567,20.7074706882311));
#14897=CARTESIAN_POINT('Ctrl Pts',(4.75546320763204,-3.92333499504741,20.701615714823));
#14898=CARTESIAN_POINT('Ctrl Pts',(4.87109384331342,-3.91280100685486,20.6957607414148));
#14899=CARTESIAN_POINT('Ctrl Pts',(4.98595405280371,-3.89719574711604,20.6899057680067));
#14900=CARTESIAN_POINT('Ctrl Pts',(5.10094444160083,-3.88157280081802,20.6840441587375));
#14901=CARTESIAN_POINT('Ctrl Pts',(5.21516225178086,-3.8608671666907,20.6781825494684));
#14902=CARTESIAN_POINT('Ctrl Pts',(5.32813266118402,-3.83519121386984,20.6723209401993));
#14903=CARTESIAN_POINT('Ctrl Pts',(5.44117924737086,-3.80949794756384,20.6664553784037));
#14904=CARTESIAN_POINT('Ctrl Pts',(5.55297636046322,-3.77882779797132,20.660589816608));
#14905=CARTESIAN_POINT('Ctrl Pts',(5.66306496703822,-3.7433428147382,20.6547242548124));
#14906=CARTESIAN_POINT('Ctrl Pts',(5.77331455016921,-3.70780594375239,20.6488501161261));
#14907=CARTESIAN_POINT('Ctrl Pts',(5.88185025514948,-3.66744033158329,20.6429759774399));
#14908=CARTESIAN_POINT('Ctrl Pts',(5.98823355085912,-3.6224558915374,20.6371018387536));
#14909=CARTESIAN_POINT('Ctrl Pts',(6.01513615250219,-3.61108005980913,20.6356163648169));
#14910=CARTESIAN_POINT('Ctrl Pts',(6.04190123492469,-3.59940908001501,20.6341308908803));
#14911=CARTESIAN_POINT('Ctrl Pts',(6.0685219765932,-3.58744680003981,20.6326454169436));
#14912=CARTESIAN_POINT('Ctrl Pts',(6.17378263635646,-3.54014693521476,20.6267717276009));
#14913=CARTESIAN_POINT('Ctrl Pts',(6.27713507773352,-3.48813162624027,20.6208980382581));
#14914=CARTESIAN_POINT('Ctrl Pts',(6.37812705671332,-3.43157685638819,20.6150243489154));
#14915=CARTESIAN_POINT('Ctrl Pts',(6.47898864554543,-3.3750951040655,20.6091582430583));
#14916=CARTESIAN_POINT('Ctrl Pts',(6.57749547543551,-3.31408574623456,20.6032921372012));
#14917=CARTESIAN_POINT('Ctrl Pts',(6.67321579448948,-3.24877255591069,20.5974260313441));
#14918=CARTESIAN_POINT('Ctrl Pts',(6.76883809714315,-3.18352624547055,20.5915659323054));
#14919=CARTESIAN_POINT('Ctrl Pts',(6.86167922527287,-3.11398510004121,20.5857058332668));
#14920=CARTESIAN_POINT('Ctrl Pts',(6.95133313243069,-3.04041814405701,20.5798457342281));
#14921=CARTESIAN_POINT('Ctrl Pts',(7.04422154908736,-2.96419705926262,20.5737742161158));
#14922=CARTESIAN_POINT('Ctrl Pts',(7.13368803324021,-2.88365441590578,20.5677026980034));
#14923=CARTESIAN_POINT('Ctrl Pts',(7.21931473949862,-2.79913790418828,20.5616311798911));
#14924=CARTESIAN_POINT('Ctrl Pts',(7.30186480880349,-2.71765813923469,20.5557778163453));
#14925=CARTESIAN_POINT('Ctrl Pts',(7.38084596487764,-2.63248547505956,20.5499244527995));
#14926=CARTESIAN_POINT('Ctrl Pts',(7.45591912758554,-2.54397102367926,20.5440710892537));
#14927=CARTESIAN_POINT('Ctrl Pts',(7.53098101830435,-2.45546986245346,20.5382186045712));
#14928=CARTESIAN_POINT('Ctrl Pts',(7.6021358152192,-2.36362822670152,20.5323661198888));
#14929=CARTESIAN_POINT('Ctrl Pts',(7.66908370878854,-2.26883150880627,20.5265136352063));
#14930=CARTESIAN_POINT('Ctrl Pts',(7.73603774057587,-2.17402609933181,20.52066061393));
#14931=CARTESIAN_POINT('Ctrl Pts',(7.79878386390566,-2.07626540659848,20.5148075926537));
#14932=CARTESIAN_POINT('Ctrl Pts',(7.8570651281001,-1.97596449764699,20.5089545713774));
#14933=CARTESIAN_POINT('Ctrl Pts',(7.91536583021796,-1.87563013641175,20.5030995980058));
#14934=CARTESIAN_POINT('Ctrl Pts',(7.96919850470418,-1.77275423134245,20.4972446246343));
#14935=CARTESIAN_POINT('Ctrl Pts',(8.01835209460449,-1.66777653690316,20.4913896512627));
#14936=CARTESIAN_POINT('Ctrl Pts',(8.06756139378336,-1.56267986373549,20.4855280420311));
#14937=CARTESIAN_POINT('Ctrl Pts',(8.11208084833505,-1.45547702102329,20.4796664327995));
#14938=CARTESIAN_POINT('Ctrl Pts',(8.15174747731444,-1.34662792192524,20.473804823568));
#14939=CARTESIAN_POINT('Ctrl Pts',(8.1914408537916,-1.2377054250843,20.4679392618104));
#14940=CARTESIAN_POINT('Ctrl Pts',(8.22627476499539,-1.12713485451428,20.4620737000529));
#14941=CARTESIAN_POINT('Ctrl Pts',(8.25613653612756,-1.01538978825197,20.4562081382954));
#14942=CARTESIAN_POINT('Ctrl Pts',(8.28604197249384,-0.903481323293121,
20.4503339996478));
#14943=CARTESIAN_POINT('Ctrl Pts',(8.31096067015872,-0.79039533705663,20.4444598610003));
#14944=CARTESIAN_POINT('Ctrl Pts',(8.33083128902692,-0.676614126679309,
20.4385857223527));
#14945=CARTESIAN_POINT('Ctrl Pts',(8.33585624585906,-0.647840706271703,
20.4371002480791));
#14946=CARTESIAN_POINT('Ctrl Pts',(8.34055863683056,-0.619022841748624,
20.4356147738054));
#14947=CARTESIAN_POINT('Ctrl Pts',(8.34493799733069,-0.590168351278482,
20.4341292995318));
#14948=CARTESIAN_POINT('Ctrl Pts',(8.37438559411386,-0.39614563935008,20.4241407070328));
#14949=CARTESIAN_POINT('Ctrl Pts',(8.38931639816492,-0.199865449716072,
20.4141521145339));
#14950=CARTESIAN_POINT('Ctrl Pts',(8.38946794062561,-0.00302796142341772,
20.404163522035));
#14951=CARTESIAN_POINT('',(8.38723842052662,0.00122266794094017,22.9041631982879));
#14952=CARTESIAN_POINT('Ctrl Pts',(8.38336796207569,0.00123261681410103,
22.9041626365075));
#14953=CARTESIAN_POINT('Ctrl Pts',(8.38497779636529,0.582186035453978,22.8748826604955));
#14954=CARTESIAN_POINT('Ctrl Pts',(7.99175245620736,2.47400439996808,22.7794306453466));
#14955=CARTESIAN_POINT('Ctrl Pts',(5.06563975414788,4.60896388279017,22.6178065910599));
#14956=CARTESIAN_POINT('Ctrl Pts',(0.913755812908484,3.01046009038452,22.4192904736486));
#14957=CARTESIAN_POINT('Ctrl Pts',(0.00621832850917159,-1.3449738921826,
22.2207743562367));
#14958=CARTESIAN_POINT('Ctrl Pts',(3.17413741150636,-4.46870214230704,22.0222582388252));
#14959=CARTESIAN_POINT('Ctrl Pts',(7.30539079965451,-3.54714769877334,21.8333884662538));
#14960=CARTESIAN_POINT('Ctrl Pts',(8.38348861036977,-1.11174890873364,21.7106907328197));
#14961=CARTESIAN_POINT('Ctrl Pts',(8.39284687402911,0.00293392250969736,
21.6541650385228));
#14962=CARTESIAN_POINT('',(8.38861467094264,-0.00383499285989103,24.1541639327802));
#14963=CARTESIAN_POINT('Ctrl Pts',(8.3894672436094,-0.00382769875130555,
24.154163522035));
#14964=CARTESIAN_POINT('Ctrl Pts',(8.38957872098432,0.110716401084503,24.1483738591514));
#14965=CARTESIAN_POINT('Ctrl Pts',(8.38468202707299,0.22538347931669,24.1425841962678));
#14966=CARTESIAN_POINT('Ctrl Pts',(8.37477179070765,0.339695558880501,24.1367945333842));
#14967=CARTESIAN_POINT('Ctrl Pts',(8.36486710287917,0.453943637469739,24.1310081120134));
#14968=CARTESIAN_POINT('Ctrl Pts',(8.34995448815683,0.567836691468084,24.1252216906425));
#14969=CARTESIAN_POINT('Ctrl Pts',(8.3300806409311,0.680898434525721,24.1194352692717));
#14970=CARTESIAN_POINT('Ctrl Pts',(8.31021213067698,0.793929815705951,24.1136504018007));
#14971=CARTESIAN_POINT('Ctrl Pts',(8.28538510867146,0.906129912621712,24.1078655343296));
#14972=CARTESIAN_POINT('Ctrl Pts',(8.25569783068645,1.01703003848253,24.1020806668586));
#14973=CARTESIAN_POINT('Ctrl Pts',(8.22601094500458,1.12792869885134,24.0962958758318));
#14974=CARTESIAN_POINT('Ctrl Pts',(8.19146404106767,1.23752701318639,24.090511084805));
#14975=CARTESIAN_POINT('Ctrl Pts',(8.15220573392728,1.34536975534977,24.0847262937782));
#14976=CARTESIAN_POINT('Ctrl Pts',(8.11293792104757,1.45323860982082,24.0789401020614));
#14977=CARTESIAN_POINT('Ctrl Pts',(8.06895658339419,1.55935064961409,24.0731539103447));
#14978=CARTESIAN_POINT('Ctrl Pts',(8.02045881068432,1.66326978763516,24.0673677186279));
#14979=CARTESIAN_POINT('Ctrl Pts',(7.9719085602857,1.76730137280327,24.0615752658821));
#14980=CARTESIAN_POINT('Ctrl Pts',(7.91883230006276,1.8691349359658,24.0557828131362));
#14981=CARTESIAN_POINT('Ctrl Pts',(7.86147349324196,1.96835823069616,24.0499903603903));
#14982=CARTESIAN_POINT('Ctrl Pts',(7.80407933131469,2.06764268517414,24.0441943372637));
#14983=CARTESIAN_POINT('Ctrl Pts',(7.74239759702477,2.16431331302349,24.038398314137));
#14984=CARTESIAN_POINT('Ctrl Pts',(7.67671450659402,2.25798772391674,24.0326022910103));
#14985=CARTESIAN_POINT('Ctrl Pts',(7.61093136673586,2.35180482101905,24.0267974392979));
#14986=CARTESIAN_POINT('Ctrl Pts',(7.54113496401743,2.44261625802189,24.0209925875855));
#14987=CARTESIAN_POINT('Ctrl Pts',(7.46765113422866,2.53007347604514,24.0151877358731));
#14988=CARTESIAN_POINT('Ctrl Pts',(7.43487130634739,2.5690865835821,24.012598294896));
#14989=CARTESIAN_POINT('Ctrl Pts',(7.40135820148236,2.6074327375437,24.0100088539189));
#14990=CARTESIAN_POINT('Ctrl Pts',(7.3671429492336,2.64508351089078,24.0074194129418));
#14991=CARTESIAN_POINT('Ctrl Pts',(7.28951033312009,2.73051114451976,24.0015441069273));
#14992=CARTESIAN_POINT('Ctrl Pts',(7.20798478842049,2.81265988752737,23.9956688009128));
#14993=CARTESIAN_POINT('Ctrl Pts',(7.12287415018794,2.89115429223226,23.9897934948984));
#14994=CARTESIAN_POINT('Ctrl Pts',(7.03787327883904,2.96954746298605,23.9839257662449));
#14995=CARTESIAN_POINT('Ctrl Pts',(6.94929680982533,3.04429539077778,23.9780580375915));
#14996=CARTESIAN_POINT('Ctrl Pts',(6.857491643667,3.11505694565336,23.972190308938));
#14997=CARTESIAN_POINT('Ctrl Pts',(6.76578039464117,3.18574611111335,23.9663285829996));
#14998=CARTESIAN_POINT('Ctrl Pts',(6.67084734352806,3.25245676483631,23.9604668570611));
#14999=CARTESIAN_POINT('Ctrl Pts',(6.57307442721387,3.3148862597581,23.9546051311227));
#15000=CARTESIAN_POINT('Ctrl Pts',(6.47181234780927,3.37954363840931,23.9485342213063));
#15001=CARTESIAN_POINT('Ctrl Pts',(6.36750425895161,3.43960828565306,23.94246331149));
#15002=CARTESIAN_POINT('Ctrl Pts',(6.26061003237402,3.49479105506607,23.9363924016736));
#15003=CARTESIAN_POINT('Ctrl Pts',(6.15751763618798,3.54801117844515,23.9305374115583));
#15004=CARTESIAN_POINT('Ctrl Pts',(6.05202032634843,3.5966905657536,23.9246824214429));
#15005=CARTESIAN_POINT('Ctrl Pts',(5.94455728337713,3.64061568652886,23.9188274313276));
#15006=CARTESIAN_POINT('Ctrl Pts',(5.83711042554598,3.68453419168804,23.9129733230395));
#15007=CARTESIAN_POINT('Ctrl Pts',(5.72769880536155,3.72369969793359,23.9071192147514));
#15008=CARTESIAN_POINT('Ctrl Pts',(5.61678201126526,3.7579466417688,23.9012651064632));
#15009=CARTESIAN_POINT('Ctrl Pts',(5.50585514034607,3.79219669694879,23.8954104663277));
#15010=CARTESIAN_POINT('Ctrl Pts',(5.39342321820423,3.82152717959801,23.8895558261921));
#15011=CARTESIAN_POINT('Ctrl Pts',(5.27996075302319,3.84582247479554,23.8837011860566));
#15012=CARTESIAN_POINT('Ctrl Pts',(5.16646058301809,3.87012584358667,23.8778446003598));
#15013=CARTESIAN_POINT('Ctrl Pts',(5.0519295925132,3.88939061130453,23.871988014663));
#15014=CARTESIAN_POINT('Ctrl Pts',(4.93685153040162,3.90355244956895,23.8661314289662));
#15015=CARTESIAN_POINT('Ctrl Pts',(4.82164342997129,3.91773029072397,23.860268225322));
#15016=CARTESIAN_POINT('Ctrl Pts',(4.70588743407938,3.92679364270126,23.8544050216778));
#15017=CARTESIAN_POINT('Ctrl Pts',(4.59007155145518,3.93073013403703,23.8485418180336));
#15018=CARTESIAN_POINT('Ctrl Pts',(4.47417776288739,3.93466927333493,23.8426746703845));
#15019=CARTESIAN_POINT('Ctrl Pts',(4.3582244192234,3.93347468899277,23.8368075227354));
#15020=CARTESIAN_POINT('Ctrl Pts',(4.24269692991518,3.92718607359502,23.8309403750863));
#15021=CARTESIAN_POINT('Ctrl Pts',(4.12700104370852,3.9208882916921,23.8250646752781));
#15022=CARTESIAN_POINT('Ctrl Pts',(4.01173266001832,3.90948170024186,23.8191889754699));
#15023=CARTESIAN_POINT('Ctrl Pts',(3.8973695681331,3.89305750105403,23.8133132756617));
#15024=CARTESIAN_POINT('Ctrl Pts',(3.86875799961211,3.88894846471443,23.8118432822845));
#15025=CARTESIAN_POINT('Ctrl Pts',(3.84020302981038,3.88452561834951,23.8103732889073));
#15026=CARTESIAN_POINT('Ctrl Pts',(3.81171199966483,3.87979088013116,23.80890329553));
#15027=CARTESIAN_POINT('Ctrl Pts',(3.6978466187317,3.86086833615514,23.8030284164887));
#15028=CARTESIAN_POINT('Ctrl Pts',(3.58462623467261,3.83689754454862,23.7971535374474));
#15029=CARTESIAN_POINT('Ctrl Pts',(3.47253316722319,3.80793370057226,23.7912786584061));
#15030=CARTESIAN_POINT('Ctrl Pts',(3.36058435047757,3.7790071296849,23.7854113396489));
#15031=CARTESIAN_POINT('Ctrl Pts',(3.24976036148445,3.74510038711803,23.7795440208917));
#15032=CARTESIAN_POINT('Ctrl Pts',(3.14053585228774,3.70632009831853,23.7736767021345));
#15033=CARTESIAN_POINT('Ctrl Pts',(3.03142276210058,3.66757936896773,23.7678153685802));
#15034=CARTESIAN_POINT('Ctrl Pts',(2.92390629310609,3.62397511950738,23.7619540350258));
#15035=CARTESIAN_POINT('Ctrl Pts',(2.8184477448103,3.5756642766864,23.7560927014715));
#15036=CARTESIAN_POINT('Ctrl Pts',(2.70921568447076,3.52562477791316,23.7500216379984));
#15037=CARTESIAN_POINT('Ctrl Pts',(2.60219201303895,3.47053566783608,23.7439505745254));
#15038=CARTESIAN_POINT('Ctrl Pts',(2.49786904705436,3.41062674713068,23.7378795110523));
#15039=CARTESIAN_POINT('Ctrl Pts',(2.39726494954109,3.35285343860099,23.7320248667189));
#15040=CARTESIAN_POINT('Ctrl Pts',(2.29917268481772,3.29059830715117,23.7261702223854));
#15041=CARTESIAN_POINT('Ctrl Pts',(2.2040096801521,3.22411468994603,23.7203155780519));
#15042=CARTESIAN_POINT('Ctrl Pts',(2.10886071749359,3.15764088289168,23.7144617976147));
#15043=CARTESIAN_POINT('Ctrl Pts',(2.01664049387269,3.08694006716538,23.7086080171774));
#15044=CARTESIAN_POINT('Ctrl Pts',(1.92773718261452,3.01230872563677,23.7027542367401));
#15045=CARTESIAN_POINT('Ctrl Pts',(1.83882551486383,2.93767036911357,23.6968999060751));
#15046=CARTESIAN_POINT('Ctrl Pts',(1.75323169556833,2.85910101785432,23.69104557541));
#15047=CARTESIAN_POINT('Ctrl Pts',(1.67131000399742,2.77693676113024,23.685191244745));
#15048=CARTESIAN_POINT('Ctrl Pts',(1.58936082382134,2.69474493440889,23.6793349496749));
#15049=CARTESIAN_POINT('Ctrl Pts',(1.51108651293609,2.60895609586038,23.6734786546048));
#15050=CARTESIAN_POINT('Ctrl Pts',(1.43680325412089,2.51994189251998,23.6676223595347));
#15051=CARTESIAN_POINT('Ctrl Pts',(1.36243567570538,2.43082664835063,23.661759416931));
#15052=CARTESIAN_POINT('Ctrl Pts',(1.29206845627402,2.33847904918574,23.6558964743273));
#15053=CARTESIAN_POINT('Ctrl Pts',(1.22597642064575,2.24330247814747,23.6500335317235));
#15054=CARTESIAN_POINT('Ctrl Pts',(1.1598397336403,2.14806160639685,23.6441666281515));
#15055=CARTESIAN_POINT('Ctrl Pts',(1.09798420146503,2.04998830545557,23.6382997245794));
#15056=CARTESIAN_POINT('Ctrl Pts',(1.04063948185516,1.9495119844011,23.6324328210074));
#15057=CARTESIAN_POINT('Ctrl Pts',(0.983210908885853,1.84888874001837,23.6265573384488));
#15058=CARTESIAN_POINT('Ctrl Pts',(0.930306500406061,1.74585582866359,23.6206818558903));
#15059=CARTESIAN_POINT('Ctrl Pts',(0.882108493602307,1.64086416591374,23.6148063733318));
#15060=CARTESIAN_POINT('Ctrl Pts',(0.870024583963843,1.61454129802779,23.6133333082606));
#15061=CARTESIAN_POINT('Ctrl Pts',(0.858236263459379,1.58809538796028,23.6118602431895));
#15062=CARTESIAN_POINT('Ctrl Pts',(0.846745912493526,1.56153368989778,23.6103871781184));
#15063=CARTESIAN_POINT('Ctrl Pts',(0.800938032747483,1.45564179205121,23.6045145996536));
#15064=CARTESIAN_POINT('Ctrl Pts',(0.759717063322716,1.34755549104644,23.5986420211887));
#15065=CARTESIAN_POINT('Ctrl Pts',(0.723298308983122,1.23770949688158,23.5927694427239));
#15066=CARTESIAN_POINT('Ctrl Pts',(0.686926674708178,1.12800562592879,23.5869044624398));
#15067=CARTESIAN_POINT('Ctrl Pts',(0.655345028307665,1.01654697822477,23.5810394821557));
#15068=CARTESIAN_POINT('Ctrl Pts',(0.628721323107011,0.903789748164359,
23.5751745018716));
#15069=CARTESIAN_POINT('Ctrl Pts',(0.602124945671036,0.791148257180299,
23.5693155416662));
#15070=CARTESIAN_POINT('Ctrl Pts',(0.580476481403955,0.677211234967463,
23.5634565814608));
#15071=CARTESIAN_POINT('Ctrl Pts',(0.563894391757136,0.562450968830149,
23.5575976212554));
#15072=CARTESIAN_POINT('Ctrl Pts',(0.54670952443267,0.443519037469597,23.5515256812325));
#15073=CARTESIAN_POINT('Ctrl Pts',(0.534966516338779,0.323703301238925,
23.5454537412096));
#15074=CARTESIAN_POINT('Ctrl Pts',(0.52873955281778,0.203542514833005,23.5393818011868));
#15075=CARTESIAN_POINT('Ctrl Pts',(0.522737940790728,0.0877303025979404,
23.5335296024151));
#15076=CARTESIAN_POINT('Ctrl Pts',(0.521860071897171,-0.0284019698800386,
23.5276774036435));
#15077=CARTESIAN_POINT('Ctrl Pts',(0.526119592198509,-0.144366539214522,
23.5218252048718));
#15078=CARTESIAN_POINT('Ctrl Pts',(0.530378467271945,-0.260313542351281,
23.5159738925854));
#15079=CARTESIAN_POINT('Ctrl Pts',(0.539773169020989,-0.376092479920382,
23.510122580299));
#15080=CARTESIAN_POINT('Ctrl Pts',(0.554265228645449,-0.491216752417696,
23.5042712680126));
#15081=CARTESIAN_POINT('Ctrl Pts',(0.568758601425841,-0.606351456566922,
23.4984194255265));
#15082=CARTESIAN_POINT('Ctrl Pts',(0.588350198618752,-0.720830967609783,
23.4925675830404));
#15083=CARTESIAN_POINT('Ctrl Pts',(0.612949892469742,-0.834175673072546,
23.4867157405544));
#15084=CARTESIAN_POINT('Ctrl Pts',(0.637557770711563,-0.947558088653727,
23.480861951143));
#15085=CARTESIAN_POINT('Ctrl Pts',(0.66717697113529,-1.05980454421068,23.4750081617316));
#15086=CARTESIAN_POINT('Ctrl Pts',(0.701666829446231,-1.17044814594567,
23.4691543723202));
#15087=CARTESIAN_POINT('Ctrl Pts',(0.736195775273815,-1.28121714058848,
23.4632939487821));
#15088=CARTESIAN_POINT('Ctrl Pts',(0.775606273355798,-1.39037926092924,
23.457433525244));
#15089=CARTESIAN_POINT('Ctrl Pts',(0.819708565962934,-1.49748514945619,
23.4515731017059));
#15090=CARTESIAN_POINT('Ctrl Pts',(0.863840584538135,-1.60466322983608,
23.4457087281064));
#15091=CARTESIAN_POINT('Ctrl Pts',(0.912670520868715,-1.70978194477564,
23.439844354507));
#15092=CARTESIAN_POINT('Ctrl Pts',(0.965962257586456,-1.81241577449947,
23.4339799809075));
#15093=CARTESIAN_POINT('Ctrl Pts',(1.01933198579058,-1.9151998069644,23.428107024904));
#15094=CARTESIAN_POINT('Ctrl Pts',(1.07717634040011,-2.01549133986442,23.4222340689005));
#15095=CARTESIAN_POINT('Ctrl Pts',(1.13921542089719,-2.11289303733621,23.416361112897));
#15096=CARTESIAN_POINT('Ctrl Pts',(1.15502567097137,-2.13771521687756,23.4148644288336));
#15097=CARTESIAN_POINT('Ctrl Pts',(1.17110814291829,-2.16234988164376,23.4133677447702));
#15098=CARTESIAN_POINT('Ctrl Pts',(1.18745779228822,-2.18679080604374,23.4118710607068));
#15099=CARTESIAN_POINT('Ctrl Pts',(1.25162480698497,-2.2827134230792,23.4059970663402));
#15100=CARTESIAN_POINT('Ctrl Pts',(1.32012417082163,-2.3759689987107,23.4001230719736));
#15101=CARTESIAN_POINT('Ctrl Pts',(1.39270701194138,-2.46614087790462,23.3942490776071));
#15102=CARTESIAN_POINT('Ctrl Pts',(1.46519617184847,-2.55619637406833,23.3883826646868));
#15103=CARTESIAN_POINT('Ctrl Pts',(1.54175807112617,-2.64317576999886,23.3825162517666));
#15104=CARTESIAN_POINT('Ctrl Pts',(1.62210012899226,-2.72669057667694,23.3766498388464));
#15105=CARTESIAN_POINT('Ctrl Pts',(1.70235994456939,-2.81011989327616,23.3707894310901));
#15106=CARTESIAN_POINT('Ctrl Pts',(1.78639193713453,-2.89009137905395,23.3649290233338));
#15107=CARTESIAN_POINT('Ctrl Pts',(1.87386318781676,-2.96624942819001,23.3590686155774));
#15108=CARTESIAN_POINT('Ctrl Pts',(1.96448371064007,-3.0451494344902,23.3529972125657));
#15109=CARTESIAN_POINT('Ctrl Pts',(2.05879552561944,-3.11995588402797,23.3469258095539));
#15110=CARTESIAN_POINT('Ctrl Pts',(2.15638626882769,-3.19031470879306,23.3408544065422));
#15111=CARTESIAN_POINT('Ctrl Pts',(2.25047727794221,-3.25815037234706,23.3350007321327));
#15112=CARTESIAN_POINT('Ctrl Pts',(2.34761571722282,-3.32185166556091,23.3291470577232));
#15113=CARTESIAN_POINT('Ctrl Pts',(2.44739888087793,-3.38114268105488,23.3232933833138));
#15114=CARTESIAN_POINT('Ctrl Pts',(2.54716706759119,-3.44042479727107,23.3174405875109));
#15115=CARTESIAN_POINT('Ctrl Pts',(2.64957883433474,-3.49529774103474,23.311587791708));
#15116=CARTESIAN_POINT('Ctrl Pts',(2.7542042123478,-3.54553003528332,23.3057349959051));
#15117=CARTESIAN_POINT('Ctrl Pts',(2.85883918116785,-3.59576693422963,23.2998816635876));
#15118=CARTESIAN_POINT('Ctrl Pts',(2.96568779222055,-3.64136215920086,23.2940283312702));
#15119=CARTESIAN_POINT('Ctrl Pts',(3.07429795205795,-3.68213143445575,23.2881749989528));
#15120=CARTESIAN_POINT('Ctrl Pts',(3.18294432583411,-3.72291430343004,23.2823197149559));
#15121=CARTESIAN_POINT('Ctrl Pts',(3.29335302978794,-3.75886787792341,23.276464430959));
#15122=CARTESIAN_POINT('Ctrl Pts',(3.40505526806061,-3.78985724545537,23.2706091469621));
#15123=CARTESIAN_POINT('Ctrl Pts',(3.51688405793957,-3.82088172199051,23.2647472292969));
#15124=CARTESIAN_POINT('Ctrl Pts',(3.63000890889168,-3.84693065562783,23.2588853116318));
#15125=CARTESIAN_POINT('Ctrl Pts',(3.7439491511572,-3.86791989493575,23.2530233939666));
#15126=CARTESIAN_POINT('Ctrl Pts',(3.85796620256293,-3.88892328346253,23.2471575246786));
#15127=CARTESIAN_POINT('Ctrl Pts',(3.97279933163732,-3.90486012927119,23.2412916553907));
#15128=CARTESIAN_POINT('Ctrl Pts',(4.08796276814762,-3.91569815981796,23.2354257861027));
#15129=CARTESIAN_POINT('Ctrl Pts',(4.20329452048084,-3.92655203056615,23.2295513436196));
#15130=CARTESIAN_POINT('Ctrl Pts',(4.31895713270896,-3.93229219308944,23.2236769011366));
#15131=CARTESIAN_POINT('Ctrl Pts',(4.43446478202045,-3.93293844468949,23.2178024586535));
#15132=CARTESIAN_POINT('Ctrl Pts',(4.46361489829682,-3.93310153613319,23.216319953534));
#15133=CARTESIAN_POINT('Ctrl Pts',(4.49275517300633,-3.93294046322736,23.2148374484145));
#15134=CARTESIAN_POINT('Ctrl Pts',(4.52187786675592,-3.93245606384164,23.2133549432951));
#15135=CARTESIAN_POINT('Ctrl Pts',(4.63726460974797,-3.93053682972457,23.2074811241122));
#15136=CARTESIAN_POINT('Ctrl Pts',(4.752758877098,-3.92353155340743,23.2016073049293));
#15137=CARTESIAN_POINT('Ctrl Pts',(4.867875659089,-3.91142348106862,23.1957334857464));
#15138=CARTESIAN_POINT('Ctrl Pts',(4.98284387373924,-3.89933103515785,23.1898672471932));
#15139=CARTESIAN_POINT('Ctrl Pts',(5.0974351647547,-3.88214893258858,23.18400100864));
#15140=CARTESIAN_POINT('Ctrl Pts',(5.21116449427817,-3.85991241756093,23.1781347700868));
#15141=CARTESIAN_POINT('Ctrl Pts',(5.3247774210237,-3.83769866176462,23.1722745356705));
#15142=CARTESIAN_POINT('Ctrl Pts',(5.4375297380568,-3.8104408623037,23.1664143012542));
#15143=CARTESIAN_POINT('Ctrl Pts',(5.54894217099982,-3.7782259861907,23.1605540668379));
#15144=CARTESIAN_POINT('Ctrl Pts',(5.66437049944754,-3.74484991493324,23.1544825984648));
#15145=CARTESIAN_POINT('Ctrl Pts',(5.77836007944622,-3.70615271434604,23.1484111300917));
#15146=CARTESIAN_POINT('Ctrl Pts',(5.89038980051059,-3.66228896217654,23.1423396617186));
#15147=CARTESIAN_POINT('Ctrl Pts',(5.99839769379383,-3.6199999033597,23.1364861569354));
#15148=CARTESIAN_POINT('Ctrl Pts',(6.10458360750112,-3.57290903297098,23.1306326521522));
#15149=CARTESIAN_POINT('Ctrl Pts',(6.20849740629629,-3.52120516808175,23.1247791473689));
#15150=CARTESIAN_POINT('Ctrl Pts',(6.31239563745666,-3.46950904910207,23.1189265195166));
#15151=CARTESIAN_POINT('Ctrl Pts',(6.41402206076365,-3.41320149374667,23.1130738916643));
#15152=CARTESIAN_POINT('Ctrl Pts',(6.51294909697806,-3.35251831428323,23.107221263812));
#15153=CARTESIAN_POINT('Ctrl Pts',(6.61188523344937,-3.29182955259937,23.1013680975789));
#15154=CARTESIAN_POINT('Ctrl Pts',(6.7081211370295,-3.22676458267386,23.0955149313458));
#15155=CARTESIAN_POINT('Ctrl Pts',(6.80125689887346,-3.15760339615587,23.0896617651127));
#15156=CARTESIAN_POINT('Ctrl Pts',(6.89442374865687,-3.08841912421144,23.0838066451416));
#15157=CARTESIAN_POINT('Ctrl Pts',(6.9844880675476,-3.0151361630527,23.0779515251705));
#15158=CARTESIAN_POINT('Ctrl Pts',(7.07108237348684,-2.93807529900495,23.0720964051994));
#15159=CARTESIAN_POINT('Ctrl Pts',(7.15777484577421,-2.86092707605381,23.0662346476585));
#15160=CARTESIAN_POINT('Ctrl Pts',(7.24098914483427,-2.77999267686708,23.0603728901177));
#15161=CARTESIAN_POINT('Ctrl Pts',(7.32039400746091,-2.69563038268273,23.0545111325768));
#15162=CARTESIAN_POINT('Ctrl Pts',(7.3998524279898,-2.61121118685083,23.0486454213305));
#15163=CARTESIAN_POINT('Ctrl Pts',(7.47549602687772,-2.52335980442883,23.0427797100843));
#15164=CARTESIAN_POINT('Ctrl Pts',(7.54703437145913,-2.43246692501389,23.036913998838));
#15165=CARTESIAN_POINT('Ctrl Pts',(7.61867732712394,-2.34144113222718,23.031039710116));
#15166=CARTESIAN_POINT('Ctrl Pts',(7.68620280773775,-2.24736530047097,23.0251654213941));
#15167=CARTESIAN_POINT('Ctrl Pts',(7.74936410791157,-2.15065838938292,23.0192911326722));
#15168=CARTESIAN_POINT('Ctrl Pts',(7.76532141490701,-2.12622599384061,23.0178070304093));
#15169=CARTESIAN_POINT('Ctrl Pts',(7.78100039336455,-2.10162577615285,23.0163229281464));
#15170=CARTESIAN_POINT('Ctrl Pts',(7.7963975407554,-2.07686471686776,23.0148388258835));
#15171=CARTESIAN_POINT('Ctrl Pts',(7.859037879908,-1.97612909928727,23.0088010406544));
#15172=CARTESIAN_POINT('Ctrl Pts',(7.91720903096368,-1.87240947858011,23.0027632554254));
#15173=CARTESIAN_POINT('Ctrl Pts',(7.97062389833732,-1.76612714633646,22.9967254701964));
#15174=CARTESIAN_POINT('Ctrl Pts',(8.02395744405096,-1.66000662401786,22.9906968772156));
#15175=CARTESIAN_POINT('Ctrl Pts',(8.07254894942104,-1.55133149453898,22.9846682842348));
#15176=CARTESIAN_POINT('Ctrl Pts',(8.11615516574377,-1.44055091743213,22.978639691254));
#15177=CARTESIAN_POINT('Ctrl Pts',(8.16104712140932,-1.32650394946593,22.9724333438191));
#15178=CARTESIAN_POINT('Ctrl Pts',(8.20065500283404,-1.21022577448384,22.9662269963841));
#15179=CARTESIAN_POINT('Ctrl Pts',(8.23476416089464,-1.0922341689436,22.9600206489492));
#15180=CARTESIAN_POINT('Ctrl Pts',(8.26780337610315,-0.977943747546674,
22.9540089834547));
#15181=CARTESIAN_POINT('Ctrl Pts',(8.29568352281609,-0.862046175210224,
22.9479973179601));
#15182=CARTESIAN_POINT('Ctrl Pts',(8.31825837322447,-0.745031984035302,
22.9419856524656));
#15183=CARTESIAN_POINT('Ctrl Pts',(8.34192982049566,-0.622333706692535,
22.9356819640605));
#15184=CARTESIAN_POINT('Ctrl Pts',(8.35976743530867,-0.498407995694312,
22.9293782756554));
#15185=CARTESIAN_POINT('Ctrl Pts',(8.37166192269059,-0.373837143477487,
22.9230745872503));
#15186=CARTESIAN_POINT('Ctrl Pts',(8.3835564100725,-0.249266291260661,22.9167708988452));
#15187=CARTESIAN_POINT('Ctrl Pts',(8.38950767782919,-0.12405077695408,22.9104672104401));
#15188=CARTESIAN_POINT('Ctrl Pts',(8.38946891794852,0.00121693452816299,
22.904163522035));
#15189=CARTESIAN_POINT('',(2.70777463088706,3.52286199445081,25.));
#15190=CARTESIAN_POINT('Ctrl Pts',(2.70777463088727,3.52286199445091,25.));
#15191=CARTESIAN_POINT('Ctrl Pts',(1.53601102873651,2.94121657640656,24.9338279608628));
#15192=CARTESIAN_POINT('Ctrl Pts',(-0.161182576319996,0.526756619563024,
24.8014838825885));
#15193=CARTESIAN_POINT('Ctrl Pts',(1.51353445936752,-3.60293174152366,24.6029677651766));
#15194=CARTESIAN_POINT('Ctrl Pts',(5.88727120760258,-4.42203261044561,24.4044516477652));
#15195=CARTESIAN_POINT('Ctrl Pts',(8.19434681762875,-1.99168802557944,24.254850422542));
#15196=CARTESIAN_POINT('Ctrl Pts',(8.39132408849758,-0.345158373668096,
24.1714212364563));
#15197=CARTESIAN_POINT('Ctrl Pts',(8.38828935556429,-0.00383777606628122,
24.1541640895078));
#15198=CARTESIAN_POINT('',(6.2051666064271,3.52286049294652,24.999933612301));
#15199=CARTESIAN_POINT('Origin',(4.45646910621825,5.55111512312578E-15,
25.));
#15200=CARTESIAN_POINT('',(8.38946742624093,-0.00363520271639387,23.9708364988139));
#15201=CARTESIAN_POINT('Ctrl Pts',(8.38946742624093,-0.00363520271639387,
23.9708364988139));
#15202=CARTESIAN_POINT('Ctrl Pts',(8.38933012983173,-0.152178926091542,
23.9783480087104));
#15203=CARTESIAN_POINT('Ctrl Pts',(8.38077390761021,-0.300347425473105,
23.9858595186069));
#15204=CARTESIAN_POINT('Ctrl Pts',(8.36394689447948,-0.447332465002422,
23.9933710285034));
#15205=CARTESIAN_POINT('Ctrl Pts',(8.34673858497178,-0.597648152853239,
24.0010527475444));
#15206=CARTESIAN_POINT('Ctrl Pts',(8.320880397383,-0.74672642332909,24.0087344665854));
#15207=CARTESIAN_POINT('Ctrl Pts',(8.28657873929154,-0.893727698261136,
24.0164161856264));
#15208=CARTESIAN_POINT('Ctrl Pts',(8.28057428401054,-0.919460057298328,
24.0177608593544));
#15209=CARTESIAN_POINT('Ctrl Pts',(8.27431122111926,-0.945128826938406,
24.0191055330824));
#15210=CARTESIAN_POINT('Ctrl Pts',(8.26779080650492,-0.970729569408433,
24.0204502068104));
#15211=CARTESIAN_POINT('Ctrl Pts',(8.23930241018745,-1.08258198074202,24.0263252316895));
#15212=CARTESIAN_POINT('Ctrl Pts',(8.20583861026129,-1.19336520554438,24.0322002565686));
#15213=CARTESIAN_POINT('Ctrl Pts',(8.16749505797018,-1.30260331084475,24.0380752814478));
#15214=CARTESIAN_POINT('Ctrl Pts',(8.12920103269124,-1.41170031714287,24.0439427177647));
#15215=CARTESIAN_POINT('Ctrl Pts',(8.08603992529645,-1.51925578683239,24.0498101540817));
#15216=CARTESIAN_POINT('Ctrl Pts',(8.03815798798727,-1.62480575891772,24.0556775903987));
#15217=CARTESIAN_POINT('Ctrl Pts',(7.99032512344514,-1.73024755599002,24.0615390133555));
#15218=CARTESIAN_POINT('Ctrl Pts',(7.9377812223183,-1.83368756997744,24.0674004363123));
#15219=CARTESIAN_POINT('Ctrl Pts',(7.88072153424563,-1.9346793814864,24.0732618592691));
#15220=CARTESIAN_POINT('Ctrl Pts',(7.82162147027464,-2.03928252115172,24.0793328786422));
#15221=CARTESIAN_POINT('Ctrl Pts',(7.75767676660413,-2.14125866643526,24.0854038980152));
#15222=CARTESIAN_POINT('Ctrl Pts',(7.68915788820171,-2.24013665628646,24.0914749173882));
#15223=CARTESIAN_POINT('Ctrl Pts',(7.6230808545844,-2.33549087707562,24.0973295805199));
#15224=CARTESIAN_POINT('Ctrl Pts',(7.55275036285019,-2.42796362735164,24.1031842436515));
#15225=CARTESIAN_POINT('Ctrl Pts',(7.47845403191733,-2.51716032640901,24.1090389067831));
#15226=CARTESIAN_POINT('Ctrl Pts',(7.40416899530404,-2.60634346603469,24.1148926799053));
#15227=CARTESIAN_POINT('Ctrl Pts',(7.32591958247458,-2.69225122749522,24.1207464530275));
#15228=CARTESIAN_POINT('Ctrl Pts',(7.24403394073769,-2.77452181345733,24.1266002261497));
#15229=CARTESIAN_POINT('Ctrl Pts',(7.16214096730267,-2.85679976558388,24.1324545233943));
#15230=CARTESIAN_POINT('Ctrl Pts',(7.07661140908675,-2.93543960214524,24.1383088206388));
#15231=CARTESIAN_POINT('Ctrl Pts',(6.98781002448427,-3.01011663486851,24.1441631178834));
#15232=CARTESIAN_POINT('Ctrl Pts',(6.89897923880363,-3.08481839226567,24.1500193534159));
#15233=CARTESIAN_POINT('Ctrl Pts',(6.80687478858566,-3.15555447124593,24.1558755889484));
#15234=CARTESIAN_POINT('Ctrl Pts',(6.71189365531805,-3.22204113929632,24.1617318244808));
#15235=CARTESIAN_POINT('Ctrl Pts',(6.61680532874655,-3.28860284251809,24.1675946692126));
#15236=CARTESIAN_POINT('Ctrl Pts',(6.5188341776721,-3.35090532574933,24.1734575139443));
#15237=CARTESIAN_POINT('Ctrl Pts',(6.41840532143876,-3.40870874194411,24.1793203586761));
#15238=CARTESIAN_POINT('Ctrl Pts',(6.31790900000042,-3.46655098880439,24.1851871418976));
#15239=CARTESIAN_POINT('Ctrl Pts',(6.21495205157806,-3.51988796087664,24.1910539251191));
#15240=CARTESIAN_POINT('Ctrl Pts',(6.10998172615481,-3.56852700924492,24.1969207083406));
#15241=CARTESIAN_POINT('Ctrl Pts',(6.00485847347324,-3.61723691798526,24.2027960386545));
#15242=CARTESIAN_POINT('Ctrl Pts',(5.89771637034563,-3.66123508732565,24.2086713689684));
#15243=CARTESIAN_POINT('Ctrl Pts',(5.78902010226335,-3.70037793244679,24.2145466992823));
#15244=CARTESIAN_POINT('Ctrl Pts',(5.7617650821707,-3.71019279591066,24.2160199075956));
#15245=CARTESIAN_POINT('Ctrl Pts',(5.73441240637848,-3.71970264008899,24.2174931159088));
#15246=CARTESIAN_POINT('Ctrl Pts',(5.7069695069686,-3.72890570378538,24.218966324222));
#15247=CARTESIAN_POINT('Ctrl Pts',(5.59752569619918,-3.76560803420041,24.2248415609982));
#15248=CARTESIAN_POINT('Ctrl Pts',(5.48628331429453,-3.79754882582684,24.2307167977744));
#15249=CARTESIAN_POINT('Ctrl Pts',(5.3736942655493,-3.82455056275768,24.2365920345506));
#15250=CARTESIAN_POINT('Ctrl Pts',(5.26125020068939,-3.85151752884025,24.2424597056295));
#15251=CARTESIAN_POINT('Ctrl Pts',(5.14746331553314,-3.87355799324999,24.2483273767085));
#15252=CARTESIAN_POINT('Ctrl Pts',(5.03280286735199,-3.89054345763897,24.2541950477874));
#15253=CARTESIAN_POINT('Ctrl Pts',(4.91825949136105,-3.90751157929513,24.260056727776));
#15254=CARTESIAN_POINT('Ctrl Pts',(4.80284473252738,-3.91943490723643,24.2659184077646));
#15255=CARTESIAN_POINT('Ctrl Pts',(4.68703965175696,-3.92623563015899,24.2717800877532));
#15256=CARTESIAN_POINT('Ctrl Pts',(4.56710053808121,-3.93327912664688,24.2778510191649));
#15257=CARTESIAN_POINT('Ctrl Pts',(4.44674315279411,-3.93482734251477,24.2839219505766));
#15258=CARTESIAN_POINT('Ctrl Pts',(4.3265100107905,-3.93085227826175,24.2899928819883));
#15259=CARTESIAN_POINT('Ctrl Pts',(4.21055385895036,-3.92701861687341,24.2958478553579));
#15260=CARTESIAN_POINT('Ctrl Pts',(4.09471370924887,-3.91804795116584,24.3017028287276));
#15261=CARTESIAN_POINT('Ctrl Pts',(3.97947710394769,-3.90396819015856,24.3075578020973));
#15262=CARTESIAN_POINT('Ctrl Pts',(3.86425764172276,-3.88989052371503,24.3134119044568));
#15263=CARTESIAN_POINT('Ctrl Pts',(3.74964195509695,-3.8707053233214,24.3192660068164));
#15264=CARTESIAN_POINT('Ctrl Pts',(3.63611199311522,-3.84649232509064,24.3251201091759));
#15265=CARTESIAN_POINT('Ctrl Pts',(3.52257150699411,-3.82227708233374,24.3309747542062));
#15266=CARTESIAN_POINT('Ctrl Pts',(3.41011734942133,-3.79303320133721,24.3368293992364));
#15267=CARTESIAN_POINT('Ctrl Pts',(3.29922011882796,-3.75889129680337,24.3426840442667));
#15268=CARTESIAN_POINT('Ctrl Pts',(3.18828583061333,-3.7247379833483,24.3485406456958));
#15269=CARTESIAN_POINT('Ctrl Pts',(3.07890989831364,-3.68568351315681,24.354397247125));
#15270=CARTESIAN_POINT('Ctrl Pts',(2.97154595985575,-3.64190777606969,24.3602538485541));
#15271=CARTESIAN_POINT('Ctrl Pts',(2.86406040794536,-3.59808245325947,24.3661170838822));
#15272=CARTESIAN_POINT('Ctrl Pts',(2.75859178123781,-3.54952534544128,24.3719803192103));
#15273=CARTESIAN_POINT('Ctrl Pts',(2.65557208355584,-3.49646377269458,24.3778435545384));
#15274=CARTESIAN_POINT('Ctrl Pts',(2.55248292375787,-3.4433664226237,24.3837107432147));
#15275=CARTESIAN_POINT('Ctrl Pts',(2.45184633842582,-3.38575876443387,24.389577931891));
#15276=CARTESIAN_POINT('Ctrl Pts',(2.35406665645412,-3.32391229415364,24.3954451205673));
#15277=CARTESIAN_POINT('Ctrl Pts',(2.25614422635233,-3.26197553448193,24.4013208747266));
#15278=CARTESIAN_POINT('Ctrl Pts',(2.16108736102153,-3.19578784755157,24.407196628886));
#15279=CARTESIAN_POINT('Ctrl Pts',(2.06926860346537,-3.12566197143203,24.4130723830453));
#15280=CARTESIAN_POINT('Ctrl Pts',(2.04629702175556,-3.10811760102093,24.4145424025748));
#15281=CARTESIAN_POINT('Ctrl Pts',(2.02352794312778,-3.09032691541717,24.4160124221043));
#15282=CARTESIAN_POINT('Ctrl Pts',(2.00096683935795,-3.07229517095019,24.4174824416337));
#15283=CARTESIAN_POINT('Ctrl Pts',(1.91094497346396,-3.00034606337101,24.4233480190582));
#15284=CARTESIAN_POINT('Ctrl Pts',(1.82393565654982,-2.92431514790276,24.4292135964826));
#15285=CARTESIAN_POINT('Ctrl Pts',(1.74033251279291,-2.84448431281591,24.4350791739071));
#15286=CARTESIAN_POINT('Ctrl Pts',(1.65683770803279,-2.7647569282956,24.4409371502923));
#15287=CARTESIAN_POINT('Ctrl Pts',(1.57674059598749,-2.68123969966455,24.4467951266775));
#15288=CARTESIAN_POINT('Ctrl Pts',(1.50040311551035,-2.59425574270928,24.4526531030628));
#15289=CARTESIAN_POINT('Ctrl Pts',(1.42414401815731,-2.50736110065214,24.4585050644933));
#15290=CARTESIAN_POINT('Ctrl Pts',(1.35163714593628,-2.41700711978729,24.4643570259237));
#15291=CARTESIAN_POINT('Ctrl Pts',(1.28320831761017,-2.32355438229501,24.4702089873542));
#15292=CARTESIAN_POINT('Ctrl Pts',(1.21217650993141,-2.22654677542837,24.4762835528414));
#15293=CARTESIAN_POINT('Ctrl Pts',(1.14553949184232,-2.1262002924728,24.4823581183285));
#15294=CARTESIAN_POINT('Ctrl Pts',(1.08361666321857,-2.02295709241472,24.4884326838156));
#15295=CARTESIAN_POINT('Ctrl Pts',(1.0240313716104,-1.92361124018631,24.4942779393375));
#15296=CARTESIAN_POINT('Ctrl Pts',(0.968811035467309,-1.82158379424227,
24.5001231948594));
#15297=CARTESIAN_POINT('Ctrl Pts',(0.918196132723883,-1.71729827491886,
24.5059684503812));
#15298=CARTESIAN_POINT('Ctrl Pts',(0.867588629715818,-1.61302800180167,
24.5118128513456));
#15299=CARTESIAN_POINT('Ctrl Pts',(0.821585402365603,-1.5065006843668,24.51765725231));
#15300=CARTESIAN_POINT('Ctrl Pts',(0.780380357407895,-1.39816326331008,
24.5235016532744));
#15301=CARTESIAN_POINT('Ctrl Pts',(0.739171299207984,-1.28981529052819,
24.5293466234652));
#15302=CARTESIAN_POINT('Ctrl Pts',(0.702761499724706,-1.17965725101988,
24.5351915936559));
#15303=CARTESIAN_POINT('Ctrl Pts',(0.67129596052861,-1.06815413548326,24.5410365638466));
#15304=CARTESIAN_POINT('Ctrl Pts',(0.639819691834387,-0.956612998272772,
24.5468835271256));
#15305=CARTESIAN_POINT('Ctrl Pts',(0.613291148174243,-0.843726271658716,
24.5527304904046));
#15306=CARTESIAN_POINT('Ctrl Pts',(0.591804726849639,-0.729971393165113,
24.5585774536836));
#15307=CARTESIAN_POINT('Ctrl Pts',(0.570293550341119,-0.616085454086971,
24.5644311534334));
#15308=CARTESIAN_POINT('Ctrl Pts',(0.553836167676953,-0.501329774199917,
24.5702848531833));
#15309=CARTESIAN_POINT('Ctrl Pts',(0.542475388479427,-0.386189302675539,
24.5761385529331));
#15310=CARTESIAN_POINT('Ctrl Pts',(0.531106843665713,-0.270970127332164,
24.5819962539566));
#15311=CARTESIAN_POINT('Ctrl Pts',(0.524841860939504,-0.155366049371791,
24.58785395498));
#15312=CARTESIAN_POINT('Ctrl Pts',(0.523671124009247,-0.0398626533586009,
24.5937116560034));
#15313=CARTESIAN_POINT('Ctrl Pts',(0.522498646528485,0.0758124631230528,
24.5995780657506));
#15314=CARTESIAN_POINT('Ctrl Pts',(0.52643551552501,0.191386186441255,24.6054444754977));
#15315=CARTESIAN_POINT('Ctrl Pts',(0.53542053161511,0.306377341855894,24.6113108852449));
#15316=CARTESIAN_POINT('Ctrl Pts',(0.537813751451311,0.337006014232916,
24.6128734431783));
#15317=CARTESIAN_POINT('Ctrl Pts',(0.540564835520931,0.367593410839932,
24.6144360011118));
#15318=CARTESIAN_POINT('Ctrl Pts',(0.543672019020073,0.398130574577568,
24.6159985590453));
#15319=CARTESIAN_POINT('Ctrl Pts',(0.555374373293993,0.513140424712632,
24.6218835048544));
#15320=CARTESIAN_POINT('Ctrl Pts',(0.572170952547528,0.627822293185062,
24.6277684506634));
#15321=CARTESIAN_POINT('Ctrl Pts',(0.594036604177521,0.741690074882627,
24.6336533964725));
#15322=CARTESIAN_POINT('Ctrl Pts',(0.615873974234077,0.85541057718122,24.6395307305474));
#15323=CARTESIAN_POINT('Ctrl Pts',(0.642767300034292,0.968318686419494,
24.6454080646223));
#15324=CARTESIAN_POINT('Ctrl Pts',(0.674639622070907,1.07993275384806,24.6512853986972));
#15325=CARTESIAN_POINT('Ctrl Pts',(0.706479146451478,1.19143196677092,24.6571566848042));
#15326=CARTESIAN_POINT('Ctrl Pts',(0.743287362771263,1.30163939346209,24.6630279709112));
#15327=CARTESIAN_POINT('Ctrl Pts',(0.784936274317255,1.4100835664148,24.6688992570182));
#15328=CARTESIAN_POINT('Ctrl Pts',(0.827975706773152,1.52214833554758,24.6749665661615));
#15329=CARTESIAN_POINT('Ctrl Pts',(0.876184643187749,1.63232961045123,24.6810338753048));
#15330=CARTESIAN_POINT('Ctrl Pts',(0.929365697162591,1.74012371451801,24.687101184448));
#15331=CARTESIAN_POINT('Ctrl Pts',(0.980768027523406,1.84431247600458,24.6929655629376));
#15332=CARTESIAN_POINT('Ctrl Pts',(1.03681499186309,1.94627080252259,24.6988299414272));
#15333=CARTESIAN_POINT('Ctrl Pts',(1.09727972431754,2.04556488445748,24.7046943199168));
#15334=CARTESIAN_POINT('Ctrl Pts',(1.15773454406417,2.14484268792421,24.7105577369886));
#15335=CARTESIAN_POINT('Ctrl Pts',(1.22260547769648,2.24145676411002,24.7164211540604));
#15336=CARTESIAN_POINT('Ctrl Pts',(1.29162073274145,2.33499973723795,24.7222845711322));
#15337=CARTESIAN_POINT('Ctrl Pts',(1.36064119517317,2.42854976843497,24.7281484306146));
#15338=CARTESIAN_POINT('Ctrl Pts',(1.43380635628817,2.5190279048759,24.734012290097));
#15339=CARTESIAN_POINT('Ctrl Pts',(1.51080271943892,2.60605804574618,24.7398761495794));
#15340=CARTESIAN_POINT('Ctrl Pts',(1.58782332448655,2.69311558759508,24.7457418552669));
#15341=CARTESIAN_POINT('Ctrl Pts',(1.66867725772992,2.77672266712549,24.7516075609543));
#15342=CARTESIAN_POINT('Ctrl Pts',(1.75301307349878,2.85653889858912,24.7574732666418));
#15343=CARTESIAN_POINT('Ctrl Pts',(1.83744127867344,2.93644256827968,24.7633453981765));
#15344=CARTESIAN_POINT('Ctrl Pts',(1.92535868085909,3.01254681782126,24.7692175297111));
#15345=CARTESIAN_POINT('Ctrl Pts',(2.01637948944588,3.08455047974898,24.7750896612457));
#15346=CARTESIAN_POINT('Ctrl Pts',(2.10745985758375,3.15660125734012,24.7809656352151));
#15347=CARTESIAN_POINT('Ctrl Pts',(2.20164734338103,3.22454586344089,24.7868416091845));
#15348=CARTESIAN_POINT('Ctrl Pts',(2.29852722361588,3.28812649259583,24.7927175831539));
#15349=CARTESIAN_POINT('Ctrl Pts',(2.3955445661498,3.351797335936,24.7986018945086));
#15350=CARTESIAN_POINT('Ctrl Pts',(2.49526157526195,3.41109163450781,24.8044862058633));
#15351=CARTESIAN_POINT('Ctrl Pts',(2.59723896199172,3.46579749419948,24.810370517218));
#15352=CARTESIAN_POINT('Ctrl Pts',(2.62117892165194,3.47864010682366,24.811751903631));
#15353=CARTESIAN_POINT('Ctrl Pts',(2.64524336845189,3.49123005542841,24.813133290044));
#15354=CARTESIAN_POINT('Ctrl Pts',(2.6694264723439,3.50356498793949,24.814514676457));
#15355=CARTESIAN_POINT('Ctrl Pts',(2.77135311732336,3.55555410780257,24.8203369266993));
#15356=CARTESIAN_POINT('Ctrl Pts',(2.87573214684329,3.60318416315759,24.8261591769416));
#15357=CARTESIAN_POINT('Ctrl Pts',(2.98215070061731,3.64621368530512,24.831981427184));
#15358=CARTESIAN_POINT('Ctrl Pts',(3.08843356897375,3.68918834409966,24.8377962539609));
#15359=CARTESIAN_POINT('Ctrl Pts',(3.19675040535977,3.72757397422257,24.8436110807378));
#15360=CARTESIAN_POINT('Ctrl Pts',(3.30666363734902,3.76117486747937,24.8494259075147));
#15361=CARTESIAN_POINT('Ctrl Pts',(3.41646738191227,3.79474229001342,24.8552349419915));
#15362=CARTESIAN_POINT('Ctrl Pts',(3.527863959767,3.82353433053595,24.8610439764684));
#15363=CARTESIAN_POINT('Ctrl Pts',(3.64039641461402,3.84740358709843,24.8668530109453));
#15364=CARTESIAN_POINT('Ctrl Pts',(3.75285104990077,3.87125633735566,24.8726580283009));
#15365=CARTESIAN_POINT('Ctrl Pts',(3.86643958958456,3.89019298622537,24.8784630456566));
#15366=CARTESIAN_POINT('Ctrl Pts',(3.98069124466208,3.90411634386747,24.8842680630123));
#15367=CARTESIAN_POINT('Ctrl Pts',(4.094902305717,3.91803475449069,24.8900710178245));
#15368=CARTESIAN_POINT('Ctrl Pts',(4.20977559646827,3.92694336304545,24.8958739726367));
#15369=CARTESIAN_POINT('Ctrl Pts',(4.32483218276851,3.93079644860742,24.9016769274489));
#15370=CARTESIAN_POINT('Ctrl Pts',(4.43987691797427,3.93464913729267,24.9074792845434));
#15371=CARTESIAN_POINT('Ctrl Pts',(4.55510449040278,3.93344732449005,24.9132816416378));
#15372=CARTESIAN_POINT('Ctrl Pts',(4.67003373631365,3.9271973656505,24.9190839987322));
#15373=CARTESIAN_POINT('Ctrl Pts',(4.78498014188058,3.92094647365297,24.9248872221549));
#15374=CARTESIAN_POINT('Ctrl Pts',(4.89962771203976,3.90964596129763,24.9306904455776));
#15375=CARTESIAN_POINT('Ctrl Pts',(5.01349899973073,3.89335417060065,24.9364936690003));
#15376=CARTESIAN_POINT('Ctrl Pts',(5.12748189437155,3.87704641207628,24.9423025802489));
#15377=CARTESIAN_POINT('Ctrl Pts',(5.2406865700215,3.85573766745363,24.9481114914976));
#15378=CARTESIAN_POINT('Ctrl Pts',(5.35264438188033,3.82953768427627,24.9539204027462));
#15379=CARTESIAN_POINT('Ctrl Pts',(5.46466153009208,3.80332381540909,24.959732392651));
#15380=CARTESIAN_POINT('Ctrl Pts',(5.5754300937844,3.77221366046194,24.9655443825558));
#15381=CARTESIAN_POINT('Ctrl Pts',(5.68449700357783,3.73636674903664,24.9713563724606));
#15382=CARTESIAN_POINT('Ctrl Pts',(5.79372777102106,3.70046598268257,24.9771770940606));
#15383=CARTESIAN_POINT('Ctrl Pts',(5.90125138639329,3.659814398766,24.9829978156605));
#15384=CARTESIAN_POINT('Ctrl Pts',(6.00663497107806,3.61461959152322,24.9888185372605));
#15385=CARTESIAN_POINT('Ctrl Pts',(6.07371407983929,3.58585204295718,24.992523562274));
#15386=CARTESIAN_POINT('Ctrl Pts',(6.13992659654999,3.55524469959169,24.9962285872875));
#15387=CARTESIAN_POINT('Ctrl Pts',(6.2051666064271,3.52286049294652,24.999933612301));
#15388=CARTESIAN_POINT('',(8.38711649681319,0.000995139969927731,22.720836447585));
#15389=CARTESIAN_POINT('Ctrl Pts',(8.38324944744337,0.000993557744290128,
22.7208364779651));
#15390=CARTESIAN_POINT('Ctrl Pts',(8.38162681228849,-0.716766452668138,
22.7570088194235));
#15391=CARTESIAN_POINT('Ctrl Pts',(7.84956874665837,-2.74980322918279,22.8593532000194));
#15392=CARTESIAN_POINT('Ctrl Pts',(4.5842072224326,-4.64729231912613,23.027869619752));
#15393=CARTESIAN_POINT('Ctrl Pts',(0.620554861050964,-2.6266912297477,23.2263857371638));
#15394=CARTESIAN_POINT('Ctrl Pts',(0.169765939565332,1.79941472931466,23.4249018545754));
#15395=CARTESIAN_POINT('Ctrl Pts',(3.6446464547419,4.57759142130336,23.6234179719871));
#15396=CARTESIAN_POINT('Ctrl Pts',(7.51158011891165,3.28158979616131,23.8053961797836));
#15397=CARTESIAN_POINT('Ctrl Pts',(8.37991817647902,0.977746425416355,23.9212023484429));
#15398=CARTESIAN_POINT('Ctrl Pts',(8.3887972543666,-0.00363417106214093,
23.9708364779651));
#15399=CARTESIAN_POINT('',(8.38946788667635,0.00309724314203014,21.4708364780002));
#15400=CARTESIAN_POINT('Ctrl Pts',(8.38946788667635,0.00309724314205896,
21.4708364780002));
#15401=CARTESIAN_POINT('Ctrl Pts',(8.38955759207542,-0.110814131887231,
21.4766158527956));
#15402=CARTESIAN_POINT('Ctrl Pts',(8.38469430172365,-0.224907558527928,
21.482395227591));
#15403=CARTESIAN_POINT('Ctrl Pts',(8.37485717235591,-0.338709260502223,
21.4881746023863));
#15404=CARTESIAN_POINT('Ctrl Pts',(8.36503009874381,-0.452394631577112,
21.4939480693626));
#15405=CARTESIAN_POINT('Ctrl Pts',(8.35023932928709,-0.565788448603539,
21.4997215363389));
#15406=CARTESIAN_POINT('Ctrl Pts',(8.33051606647788,-0.678416649046213,
21.5054950033152));
#15407=CARTESIAN_POINT('Ctrl Pts',(8.31080678309884,-0.790965021010322,
21.5112643781806));
#15408=CARTESIAN_POINT('Ctrl Pts',(8.28617202958311,-0.902748436502693,
21.517033753046));
#15409=CARTESIAN_POINT('Ctrl Pts',(8.25669478176716,-1.0132984826293,21.5228031279114));
#15410=CARTESIAN_POINT('Ctrl Pts',(8.22722829330747,-1.12380817738598,21.5285703969235));
#15411=CARTESIAN_POINT('Ctrl Pts',(8.19292293181746,-1.23308498557155,21.5343376659356));
#15412=CARTESIAN_POINT('Ctrl Pts',(8.15391250301967,-1.34067196862229,21.5401049349477));
#15413=CARTESIAN_POINT('Ctrl Pts',(8.11490622651922,-1.44824750003928,21.5458715900876));
#15414=CARTESIAN_POINT('Ctrl Pts',(8.07119602371571,-1.55413316295026,21.5516382452276));
#15415=CARTESIAN_POINT('Ctrl Pts',(8.02296488132278,-1.65788928646081,21.5574049003675));
#15416=CARTESIAN_POINT('Ctrl Pts',(7.97472640111752,-1.76166119526951,21.5631724328376));
#15417=CARTESIAN_POINT('Ctrl Pts',(7.92196579535307,-1.86330253458784,21.5689399653076));
#15418=CARTESIAN_POINT('Ctrl Pts',(7.86491290666649,-1.96239645820766,21.5747074977777));
#15419=CARTESIAN_POINT('Ctrl Pts',(7.80780235561602,-2.06159053433534,21.5804808593927));
#15420=CARTESIAN_POINT('Ctrl Pts',(7.7463910740646,-2.15823168457841,21.5862542210076));
#15421=CARTESIAN_POINT('Ctrl Pts',(7.68095329816581,-2.2519304376202,21.5920275826226));
#15422=CARTESIAN_POINT('Ctrl Pts',(7.61548004606714,-2.34567998816611,21.597804074187));
#15423=CARTESIAN_POINT('Ctrl Pts',(7.54597621438161,-2.43648362868273,21.6035805657515));
#15424=CARTESIAN_POINT('Ctrl Pts',(7.47275633226652,-2.52398501778002,21.6093570573159));
#15425=CARTESIAN_POINT('Ctrl Pts',(7.39942243936746,-2.61162265541639,21.6151425434637));
#15426=CARTESIAN_POINT('Ctrl Pts',(7.32236123103663,-2.6959474614805,21.6209280296114));
#15427=CARTESIAN_POINT('Ctrl Pts',(7.24192417901073,-2.77663988256573,21.6267135157592));
#15428=CARTESIAN_POINT('Ctrl Pts',(7.18842780549793,-2.83030609470683,21.630561276463));
#15429=CARTESIAN_POINT('Ctrl Pts',(7.13343895539129,-2.88236643337257,21.6344090371668));
#15430=CARTESIAN_POINT('Ctrl Pts',(7.07706859112929,-2.9327371753507,21.6382567978706));
#15431=CARTESIAN_POINT('Ctrl Pts',(6.99101801832057,-3.00962919577249,21.6441304872981));
#15432=CARTESIAN_POINT('Ctrl Pts',(6.90143708305444,-3.08285880543593,21.6500041767256));
#15433=CARTESIAN_POINT('Ctrl Pts',(6.80867061650115,-3.15208455708644,21.6558778661532));
#15434=CARTESIAN_POINT('Ctrl Pts',(6.71602392022475,-3.22122093174814,21.6617439720924));
#15435=CARTESIAN_POINT('Ctrl Pts',(6.62020019980454,-3.28636348372526,21.6676100780317));
#15436=CARTESIAN_POINT('Ctrl Pts',(6.52157959640588,-3.34720893631052,21.673476183971));
#15437=CARTESIAN_POINT('Ctrl Pts',(6.42305997930556,-3.40799208389239,21.6793362830892));
#15438=CARTESIAN_POINT('Ctrl Pts',(6.32174952542897,-3.46448666875841,21.6851963822073));
#15439=CARTESIAN_POINT('Ctrl Pts',(6.21805924531874,-3.51643131339486,21.6910564813255));
#15440=CARTESIAN_POINT('Ctrl Pts',(6.1106280572322,-3.570250001917,21.697127999407));
#15441=CARTESIAN_POINT('Ctrl Pts',(6.00064244543429,-3.61918397870955,21.7031995174885));
#15442=CARTESIAN_POINT('Ctrl Pts',(5.88859007690819,-3.66299311019146,21.7092710355701));
#15443=CARTESIAN_POINT('Ctrl Pts',(5.78056383891217,-3.70522814481066,21.7151243991883));
#15444=CARTESIAN_POINT('Ctrl Pts',(5.670617226365,-3.74270011227689,21.7209777628066));
#15445=CARTESIAN_POINT('Ctrl Pts',(5.5592089701512,-3.77524221640057,21.7268311264249));
#15446=CARTESIAN_POINT('Ctrl Pts',(5.44781744157284,-3.8077794344191,21.7326836111771));
#15447=CARTESIAN_POINT('Ctrl Pts',(5.33496510216676,-3.83538814509375,21.7385360959294));
#15448=CARTESIAN_POINT('Ctrl Pts',(5.2211260094527,-3.85795137609792,21.7443885806816));
#15449=CARTESIAN_POINT('Ctrl Pts',(5.10727647928484,-3.88051667583503,21.7502416020249));
#15450=CARTESIAN_POINT('Ctrl Pts',(4.99244042124382,-3.89803549596782,21.7560946233682));
#15451=CARTESIAN_POINT('Ctrl Pts',(4.87710155199393,-3.91044209080773,21.7619476447115));
#15452=CARTESIAN_POINT('Ctrl Pts',(4.76172421506629,-3.92285282347988,21.7678026181473));
#15453=CARTESIAN_POINT('Ctrl Pts',(4.64584414402544,-3.93014789633503,21.773657591583));
#15454=CARTESIAN_POINT('Ctrl Pts',(4.52994892396885,-3.93231353230936,21.7795125650188));
#15455=CARTESIAN_POINT('Ctrl Pts',(4.4139223516613,-3.93448162275213,21.7853741743101));
#15456=CARTESIAN_POINT('Ctrl Pts',(4.29788100937271,-3.93150866508802,21.7912357836015));
#15457=CARTESIAN_POINT('Ctrl Pts',(4.18231132576629,-3.92343300075554,21.7970973928928));
#15458=CARTESIAN_POINT('Ctrl Pts',(4.06666371272803,-3.91535189094711,21.8029629547076));
#15459=CARTESIAN_POINT('Ctrl Pts',(3.95148880111156,-3.90216126998636,21.8088285165223));
#15460=CARTESIAN_POINT('Ctrl Pts',(3.8372650238806,-3.88395099150547,21.8146940783371));
#15461=CARTESIAN_POINT('Ctrl Pts',(3.72287422355083,-3.86571408514363,21.8205682170378));
#15462=CARTESIAN_POINT('Ctrl Pts',(3.60943773643655,-3.84244295523982,21.8264423557385));
#15463=CARTESIAN_POINT('Ctrl Pts',(3.4974210636286,-3.81427789391451,21.8323164944392));
#15464=CARTESIAN_POINT('Ctrl Pts',(3.4690938789469,-3.80715541050437,21.8338019680535));
#15465=CARTESIAN_POINT('Ctrl Pts',(3.44085740010028,-3.79972020312893,21.8352874416679));
#15466=CARTESIAN_POINT('Ctrl Pts',(3.412718957351,-3.79197502981488,21.8367729152822));
#15467=CARTESIAN_POINT('Ctrl Pts',(3.30145712738501,-3.76134994640131,21.8426466060962));
#15468=CARTESIAN_POINT('Ctrl Pts',(3.19135900814053,-3.72577284172737,21.8485202969102));
#15469=CARTESIAN_POINT('Ctrl Pts',(3.08289845684532,-3.68534837853644,21.8543939877241));
#15470=CARTESIAN_POINT('Ctrl Pts',(2.97457793816869,-3.64497610707206,21.8602600950592));
#15471=CARTESIAN_POINT('Ctrl Pts',(2.86789116648166,-3.59976906594414,21.8661262023942));
#15472=CARTESIAN_POINT('Ctrl Pts',(2.76329906586566,-3.54988228177392,21.8719923097293));
#15473=CARTESIAN_POINT('Ctrl Pts',(2.65881406612829,-3.50004658098748,21.8778524102508));
#15474=CARTESIAN_POINT('Ctrl Pts',(2.5564198417327,-3.44554084563276,21.8837125107722));
#15475=CARTESIAN_POINT('Ctrl Pts',(2.45655884310556,-3.38656875605627,21.8895726112937));
#15476=CARTESIAN_POINT('Ctrl Pts',(2.3530951219056,-3.32546910836195,21.8956441288521));
#15477=CARTESIAN_POINT('Ctrl Pts',(2.25235128499276,-3.25957491100247,21.9017156464104));
#15478=CARTESIAN_POINT('Ctrl Pts',(2.15479348708341,-3.18916577560343,21.9077871639687));
#15479=CARTESIAN_POINT('Ctrl Pts',(2.06074098746527,-3.1212864740802,21.9136405290003));
#15480=CARTESIAN_POINT('Ctrl Pts',(1.96964987895512,-3.04921136114959,21.9194938940318));
#15481=CARTESIAN_POINT('Ctrl Pts',(1.88190900418916,-2.9732354903438,21.9253472590634));
#15482=CARTESIAN_POINT('Ctrl Pts',(1.79418130344622,-2.89727102708179,21.9311997452301));
#15483=CARTESIAN_POINT('Ctrl Pts',(1.70980314848196,-2.81740724088383,21.9370522313969));
#15484=CARTESIAN_POINT('Ctrl Pts',(1.62912982325913,-2.7339790743596,21.9429047175636));
#15485=CARTESIAN_POINT('Ctrl Pts',(1.54844910142523,-2.65054325864404,21.9487577403212));
#15486=CARTESIAN_POINT('Ctrl Pts',(1.47147417179507,-2.5635427099633,21.9546107630787));
#15487=CARTESIAN_POINT('Ctrl Pts',(1.39852250849697,-2.47334825802693,21.9604637858363));
#15488=CARTESIAN_POINT('Ctrl Pts',(1.32554651447847,-2.38312372458325,21.9663187606845));
#15489=CARTESIAN_POINT('Ctrl Pts',(1.256596714642,-2.28970349078143,21.9721737355327));
#15490=CARTESIAN_POINT('Ctrl Pts',(1.19194901058673,-2.19348980969093,21.9780287103809));
#15491=CARTESIAN_POINT('Ctrl Pts',(1.12722803684081,-2.09716708301633,21.9838903210749));
#15492=CARTESIAN_POINT('Ctrl Pts',(1.06681912134687,-1.99804493301132,21.9897519317689));
#15493=CARTESIAN_POINT('Ctrl Pts',(1.01095374320409,-1.89655289492104,21.995613542463));
#15494=CARTESIAN_POINT('Ctrl Pts',(0.955050694700068,-1.79499242013768,
22.0014791056764));
#15495=CARTESIAN_POINT('Ctrl Pts',(0.903697466682843,-1.69105924471863,
22.0073446688898));
#15496=CARTESIAN_POINT('Ctrl Pts',(0.857077917608687,-1.58520411031508,
22.0132102321033));
#15497=CARTESIAN_POINT('Ctrl Pts',(0.81039019950015,-1.47919419015233,22.019084372186));
#15498=CARTESIAN_POINT('Ctrl Pts',(0.768450123527769,-1.3712570858322,22.0249585122688));
#15499=CARTESIAN_POINT('Ctrl Pts',(0.731392153800996,-1.2618600154414,22.0308326523516));
#15500=CARTESIAN_POINT('Ctrl Pts',(0.722020886660144,-1.23419554330174,
22.0323181124657));
#15501=CARTESIAN_POINT('Ctrl Pts',(0.712961570755281,-1.20643776306536,
22.0338035725798));
#15502=CARTESIAN_POINT('Ctrl Pts',(0.704215862256281,-1.17859432935038,
22.0352890326939));
#15503=CARTESIAN_POINT('Ctrl Pts',(0.669634288741553,-1.06849807470993,
22.0411627189875));
#15504=CARTESIAN_POINT('Ctrl Pts',(0.63984478843726,-0.956695158277188,
22.0470364052811));
#15505=CARTESIAN_POINT('Ctrl Pts',(0.615016295092537,-0.84364050394368,
22.0529100915748));
#15506=CARTESIAN_POINT('Ctrl Pts',(0.590219857680636,-0.730731813859958,
22.058776194384));
#15507=CARTESIAN_POINT('Ctrl Pts',(0.570371777338458,-0.616574999635444,
22.0646422971931));
#15508=CARTESIAN_POINT('Ctrl Pts',(0.555591655487483,-0.501641420120213,
22.0705084000023));
#15509=CARTESIAN_POINT('Ctrl Pts',(0.54082666829106,-0.386825531111181,
22.0763684959977));
#15510=CARTESIAN_POINT('Ctrl Pts',(0.531119369574364,-0.271234866258815,
22.0822285919931));
#15511=CARTESIAN_POINT('Ctrl Pts',(0.526538461916261,-0.155351636541585,
22.0880886879886));
#15512=CARTESIAN_POINT('Ctrl Pts',(0.521792282148428,-0.0352875179510033,
22.0941602072434));
#15513=CARTESIAN_POINT('Ctrl Pts',(0.522549479060774,0.0850902335095483,
22.1002317264983));
#15514=CARTESIAN_POINT('Ctrl Pts',(0.528827799952726,0.205238323216817,
22.1063032457532));
#15515=CARTESIAN_POINT('Ctrl Pts',(0.53488053143222,0.321069313267738,22.1121566062861));
#15516=CARTESIAN_POINT('Ctrl Pts',(0.54606442746512,0.436686413749744,22.1180099668191));
#15517=CARTESIAN_POINT('Ctrl Pts',(0.562342347678128,0.551602926407942,
22.1238633273521));
#15518=CARTESIAN_POINT('Ctrl Pts',(0.578617823858808,0.666502185039311,
22.129715809038));
#15519=CARTESIAN_POINT('Ctrl Pts',(0.599985745507873,0.780700656050129,
22.1355682907239));
#15520=CARTESIAN_POINT('Ctrl Pts',(0.626357260670107,0.893718216549156,
22.1414207724098));
#15521=CARTESIAN_POINT('Ctrl Pts',(0.652731193832982,1.00674613961294,22.147273790709));
#15522=CARTESIAN_POINT('Ctrl Pts',(0.684109538631827,1.11859253455979,22.1531268090082));
#15523=CARTESIAN_POINT('Ctrl Pts',(0.720352789829755,1.22878959566545,22.1589798273073));
#15524=CARTESIAN_POINT('Ctrl Pts',(0.756608128995365,1.33902341005536,22.1648347977243));
#15525=CARTESIAN_POINT('Ctrl Pts',(0.79773147193756,1.44760640452048,22.1706897681413));
#15526=CARTESIAN_POINT('Ctrl Pts',(0.843534371264841,1.55408867217001,22.1765447385583));
#15527=CARTESIAN_POINT('Ctrl Pts',(0.889389182695605,1.6606916247233,22.1824063448833));
#15528=CARTESIAN_POINT('Ctrl Pts',(0.939933973069185,1.76518871854719,22.1882679512084));
#15529=CARTESIAN_POINT('Ctrl Pts',(0.994933287714969,1.86715258541418,22.1941295575334));
#15530=CARTESIAN_POINT('Ctrl Pts',(1.04996968904864,1.96918520772168,22.1999951164089));
#15531=CARTESIAN_POINT('Ctrl Pts',(1.10946638425299,2.06868084799046,22.2058606752844));
#15532=CARTESIAN_POINT('Ctrl Pts',(1.17314428316303,2.16524065782753,22.2117262341599));
#15533=CARTESIAN_POINT('Ctrl Pts',(1.23691529545404,2.26194166281259,22.2176003699832));
#15534=CARTESIAN_POINT('Ctrl Pts',(1.30487947188746,2.35569793653009,22.2234745058065));
#15535=CARTESIAN_POINT('Ctrl Pts',(1.37671709989604,2.44614320503816,22.2293486416299));
#15536=CARTESIAN_POINT('Ctrl Pts',(1.39488402735091,2.46901579531113,22.2308341444551));
#15537=CARTESIAN_POINT('Ctrl Pts',(1.41329848829932,2.49167682159717,22.2323196472803));
#15538=CARTESIAN_POINT('Ctrl Pts',(1.43195494784296,2.51412074208607,22.2338051501055));
#15539=CARTESIAN_POINT('Ctrl Pts',(1.50572274489267,2.60286419138592,22.2396788406988));
#15540=CARTESIAN_POINT('Ctrl Pts',(1.58352249613533,2.6885060166343,22.2455525312921));
#15541=CARTESIAN_POINT('Ctrl Pts',(1.66506350554639,2.77065764260722,22.2514262218855));
#15542=CARTESIAN_POINT('Ctrl Pts',(1.74649923756383,2.852703202821,22.2572923289715));
#15543=CARTESIAN_POINT('Ctrl Pts',(1.83166633342138,2.93126723454188,22.2631584360576));
#15544=CARTESIAN_POINT('Ctrl Pts',(1.9202335431614,3.00599370735964,22.2690245431437));
#15545=CARTESIAN_POINT('Ctrl Pts',(2.00871006087096,3.08064366093772,22.2748846433886));
#15546=CARTESIAN_POINT('Ctrl Pts',(2.10057945321058,3.15146360712732,22.2807447436334));
#15547=CARTESIAN_POINT('Ctrl Pts',(2.1954737583591,3.21813440318444,22.2866048438783));
#15548=CARTESIAN_POINT('Ctrl Pts',(2.29379160697434,3.28721051079219,22.2926763615299));
#15549=CARTESIAN_POINT('Ctrl Pts',(2.39535643328392,3.35183211386048,22.2987478791816));
#15550=CARTESIAN_POINT('Ctrl Pts',(2.49972132434884,3.41168977460571,22.3048193968332));
#15551=CARTESIAN_POINT('Ctrl Pts',(2.60033632757285,3.46939671673357,22.3106727615218));
#15552=CARTESIAN_POINT('Ctrl Pts',(2.70355325358029,3.52267594388975,22.3165261262104));
#15553=CARTESIAN_POINT('Ctrl Pts',(2.80894299142305,3.57129482135931,22.3223794908991));
#15554=CARTESIAN_POINT('Ctrl Pts',(2.91431690489155,3.61990639865594,22.3282319766991));
#15555=CARTESIAN_POINT('Ctrl Pts',(3.02186260643961,3.66385884462494,22.3340844624992));
#15556=CARTESIAN_POINT('Ctrl Pts',(3.13112847709521,3.70296654275944,22.3399369482993));
#15557=CARTESIAN_POINT('Ctrl Pts',(3.2404043654636,3.74207782636564,22.345789970667));
#15558=CARTESIAN_POINT('Ctrl Pts',(3.35140034744718,3.77634333992773,22.3516429930346));
#15559=CARTESIAN_POINT('Ctrl Pts',(3.46364769463818,3.80562670853411,22.3574960154022));
#15560=CARTESIAN_POINT('Ctrl Pts',(3.57593247794847,3.8349198435689,22.3633509898378));
#15561=CARTESIAN_POINT('Ctrl Pts',(3.68946905679595,3.85922742536008,22.3692059642733));
#15562=CARTESIAN_POINT('Ctrl Pts',(3.8037772112643,3.87846390859338,22.3750609387089));
#15563=CARTESIAN_POINT('Ctrl Pts',(3.91821491842669,3.89772219375533,22.3809225489589));
#15564=CARTESIAN_POINT('Ctrl Pts',(4.03342553896684,3.91189784029784,22.386784159209));
#15565=CARTESIAN_POINT('Ctrl Pts',(4.14892230926012,3.92095702191198,22.3926457694591));
#15566=CARTESIAN_POINT('Ctrl Pts',(4.2644969593582,3.93002231215836,22.3985113322098));
#15567=CARTESIAN_POINT('Ctrl Pts',(4.38035773153477,3.93396425365368,22.4043768949606));
#15568=CARTESIAN_POINT('Ctrl Pts',(4.49601817233813,3.93280114821091,22.4102424577113));
#15569=CARTESIAN_POINT('Ctrl Pts',(4.61184773617339,3.93163634203178,22.4161165973078));
#15570=CARTESIAN_POINT('Ctrl Pts',(4.72747597306673,3.92535161340455,22.4219907369042));
#15571=CARTESIAN_POINT('Ctrl Pts',(4.84242178029476,3.91401705839068,22.4278648765007));
#15572=CARTESIAN_POINT('Ctrl Pts',(4.87148949618726,3.91115075440921,22.4293503401729));
#15573=CARTESIAN_POINT('Ctrl Pts',(4.90051362575562,3.90796177220534,22.430835803845));
#15574=CARTESIAN_POINT('Ctrl Pts',(4.92948651226061,3.90445175838824,22.4323212675171));
#15575=CARTESIAN_POINT('Ctrl Pts',(5.04404871734446,3.89057275041667,22.4381949658048));
#15576=CARTESIAN_POINT('Ctrl Pts',(5.15819035855018,3.87162422586959,22.4440686640925));
#15577=CARTESIAN_POINT('Ctrl Pts',(5.27142732289849,3.84763980968403,22.4499423623801));
#15578=CARTESIAN_POINT('Ctrl Pts',(5.38451808878241,3.82368635940114,22.4558084772283));
#15579=CARTESIAN_POINT('Ctrl Pts',(5.49670610012062,3.79471003217636,22.4616745920764));
#15580=CARTESIAN_POINT('Ctrl Pts',(5.60751260704967,3.76079617357732,22.4675407069246));
#15581=CARTESIAN_POINT('Ctrl Pts',(5.71820565034903,3.72691704208592,22.4734008149894));
#15582=CARTESIAN_POINT('Ctrl Pts',(5.82751961035471,3.68811055608318,22.4792609230542));
#15583=CARTESIAN_POINT('Ctrl Pts',(5.93498683245613,3.64451290753654,22.4851210311189));
#15584=CARTESIAN_POINT('Ctrl Pts',(6.04633099472505,3.59934244942476,22.491192545861));
#15585=CARTESIAN_POINT('Ctrl Pts',(6.15569221744842,3.54902870825381,22.4972640606031));
#15586=CARTESIAN_POINT('Ctrl Pts',(6.26256820374707,3.49377947928967,22.5033355753452));
#15587=CARTESIAN_POINT('Ctrl Pts',(6.36560426585618,3.44051528792004,22.5091889479476));
#15588=CARTESIAN_POINT('Ctrl Pts',(6.46633020291411,3.38266436374306,22.5150423205501));
#15589=CARTESIAN_POINT('Ctrl Pts',(6.56431790427514,3.32046117949453,22.5208956931525));
#15590=CARTESIAN_POINT('Ctrl Pts',(6.66229089305707,3.25826733488,22.5267481868875));
#15591=CARTESIAN_POINT('Ctrl Pts',(6.7575261149343,3.19172275091743,22.5326006806224));
#15592=CARTESIAN_POINT('Ctrl Pts',(6.84962276725822,3.12110630300396,22.5384531743574));
#15593=CARTESIAN_POINT('Ctrl Pts',(6.94172786337115,3.05048338069242,22.5443062046723));
#15594=CARTESIAN_POINT('Ctrl Pts',(7.03069349002169,2.97578810369883,22.5501592349873));
#15595=CARTESIAN_POINT('Ctrl Pts',(7.11615094749728,2.89734041893089,22.5560122653022));
#15596=CARTESIAN_POINT('Ctrl Pts',(7.20163690629269,2.8188665707055,22.5618672476889));
#15597=CARTESIAN_POINT('Ctrl Pts',(7.28361206518037,2.73663810542358,22.5677222300757));
#15598=CARTESIAN_POINT('Ctrl Pts',(7.36174420731161,2.65101218159536,22.5735772124624));
#15599=CARTESIAN_POINT('Ctrl Pts',(7.43996490098065,2.56528921310634,22.5794388306289));
#15600=CARTESIAN_POINT('Ctrl Pts',(7.51433360593221,2.47616140600076,22.5853004487955));
#15601=CARTESIAN_POINT('Ctrl Pts',(7.58455801779941,2.3840194548793,22.591162066962));
#15602=CARTESIAN_POINT('Ctrl Pts',(7.65482978199884,2.29181537242536,22.5970276376186));
#15603=CARTESIAN_POINT('Ctrl Pts',(7.72095145358791,2.19659343743236,22.6028932082753));
#15604=CARTESIAN_POINT('Ctrl Pts',(7.78267470000588,2.0987723430272,22.6087587789319));
#15605=CARTESIAN_POINT('Ctrl Pts',(7.84448819954077,2.00080821242122,22.6146329263576));
#15606=CARTESIAN_POINT('Ctrl Pts',(7.90189023428523,1.90023769489433,22.6205070737834));
#15607=CARTESIAN_POINT('Ctrl Pts',(7.95467889546119,1.7975030654897,22.6263812212091));
#15608=CARTESIAN_POINT('Ctrl Pts',(7.96802749453962,1.77152469534649,22.6278666091157));
#15609=CARTESIAN_POINT('Ctrl Pts',(7.98108134602636,1.74540803842346,22.6293519970222));
#15610=CARTESIAN_POINT('Ctrl Pts',(7.99383768320666,1.71916042024444,22.6308373849288));
#15611=CARTESIAN_POINT('Ctrl Pts',(8.04811447871309,1.60747972504976,22.6371575452156));
#15612=CARTESIAN_POINT('Ctrl Pts',(8.09716102928467,1.49309802179009,22.6434777055024));
#15613=CARTESIAN_POINT('Ctrl Pts',(8.14072086865502,1.3765093355955,22.6497978657891));
#15614=CARTESIAN_POINT('Ctrl Pts',(8.18413881155106,1.26030043784261,22.6560974381106));
#15615=CARTESIAN_POINT('Ctrl Pts',(8.22210557102849,1.14189918600747,22.6623970104321));
#15616=CARTESIAN_POINT('Ctrl Pts',(8.25441234767607,1.02182001089472,22.6686965827536));
#15617=CARTESIAN_POINT('Ctrl Pts',(8.28665456255747,0.901980801647662,22.6749835660285));
#15618=CARTESIAN_POINT('Ctrl Pts',(8.31325924883263,0.780470651645069,22.6812705493034));
#15619=CARTESIAN_POINT('Ctrl Pts',(8.33406621362973,0.657821915562379,22.6875575325783));
#15620=CARTESIAN_POINT('Ctrl Pts',(8.3548100386261,0.535545363353235,22.6938254376804));
#15621=CARTESIAN_POINT('Ctrl Pts',(8.36979116524708,0.412137422350944,22.7000933427825));
#15622=CARTESIAN_POINT('Ctrl Pts',(8.37889986957347,0.288142164017332,22.7063612478845));
#15623=CARTESIAN_POINT('Ctrl Pts',(8.3859117894865,0.192690078860521,22.7111863082908));
#15624=CARTESIAN_POINT('Ctrl Pts',(8.38944469315269,0.0968903237123851,
22.7160113686972));
#15625=CARTESIAN_POINT('Ctrl Pts',(8.38946898007787,0.000996102502074969,
22.7208364291035));
#15626=CARTESIAN_POINT('',(8.39049475251801,-0.00287584216518763,20.2208360257257));
#15627=CARTESIAN_POINT('Ctrl Pts',(8.38946804882023,-0.00288400618541905,
20.2208364779651));
#15628=CARTESIAN_POINT('Ctrl Pts',(8.38933415447296,-0.185479428099694,
20.230105643973));
#15629=CARTESIAN_POINT('Ctrl Pts',(8.37648338631382,-0.367615513710913,
20.239374809981));
#15630=CARTESIAN_POINT('Ctrl Pts',(8.35111160572364,-0.547949633676686,
20.248643975989));
#15631=CARTESIAN_POINT('Ctrl Pts',(8.33503400411599,-0.66222384185733,20.2545176653732));
#15632=CARTESIAN_POINT('Ctrl Pts',(8.31389591767628,-0.77598016486602,20.2603913547574));
#15633=CARTESIAN_POINT('Ctrl Pts',(8.28774026569583,-0.888735226349951,
20.2662650441417));
#15634=CARTESIAN_POINT('Ctrl Pts',(8.26161838311929,-1.0013447104567,20.2721311500411));
#15635=CARTESIAN_POINT('Ctrl Pts',(8.23049191042047,-1.11295510505729,20.2779972559405));
#15636=CARTESIAN_POINT('Ctrl Pts',(8.19445537494036,-1.2230893895562,20.2838633618399));
#15637=CARTESIAN_POINT('Ctrl Pts',(8.15845574041331,-1.3331108979514,20.2897234609216));
#15638=CARTESIAN_POINT('Ctrl Pts',(8.11755617161554,-1.44165891245357,20.2955835600033));
#15639=CARTESIAN_POINT('Ctrl Pts',(8.0719018197416,-1.54826848252657,20.3014436590851));
#15640=CARTESIAN_POINT('Ctrl Pts',(8.02460036293674,-1.65872428283489,20.3075151771816));
#15641=CARTESIAN_POINT('Ctrl Pts',(7.97219466407808,-1.76709868861349,20.313586695278));
#15642=CARTESIAN_POINT('Ctrl Pts',(7.91490213138158,-1.87289348614907,20.3196582133745));
#15643=CARTESIAN_POINT('Ctrl Pts',(7.85966816525232,-1.97488699191162,20.3255115769651));
#15644=CARTESIAN_POINT('Ctrl Pts',(7.79989271092155,-2.07448267950373,20.3313649405556));
#15645=CARTESIAN_POINT('Ctrl Pts',(7.73581842257439,-2.17125702331955,20.3372183041461));
#15646=CARTESIAN_POINT('Ctrl Pts',(7.67175375476552,-2.26801683679405,20.3430707888738));
#15647=CARTESIAN_POINT('Ctrl Pts',(7.60339176436818,-2.36195580440928,20.3489232736015));
#15648=CARTESIAN_POINT('Ctrl Pts',(7.53101897535869,-2.45267855663323,20.3547757583292));
#15649=CARTESIAN_POINT('Ctrl Pts',(7.45863955073542,-2.54340962691641,20.3606287796513));
#15650=CARTESIAN_POINT('Ctrl Pts',(7.38224885413203,-2.63092357262074,20.3664818009733));
#15651=CARTESIAN_POINT('Ctrl Pts',(7.3021738566419,-2.71485791035484,20.3723348222953));
#15652=CARTESIAN_POINT('Ctrl Pts',(7.22207215259273,-2.79882024181253,20.3781897957131));
#15653=CARTESIAN_POINT('Ctrl Pts',(7.13828398930198,-2.87920029257801,20.3840447691308));
#15654=CARTESIAN_POINT('Ctrl Pts',(7.05117284161667,-2.95567277037048,20.3898997425486));
#15655=CARTESIAN_POINT('Ctrl Pts',(6.96396296463272,-3.03223191989552,20.3957613518268));
#15656=CARTESIAN_POINT('Ctrl Pts',(6.87342289684813,-3.10487438424982,20.401622961105));
#15657=CARTESIAN_POINT('Ctrl Pts',(6.77994887612719,-3.17331542063248,20.4074845703832));
#15658=CARTESIAN_POINT('Ctrl Pts',(6.68641182518651,-3.2418026073094,20.4133501321876));
#15659=CARTESIAN_POINT('Ctrl Pts',(6.58993722487058,-3.30608249626153,20.4192156939921));
#15660=CARTESIAN_POINT('Ctrl Pts',(6.49094846149591,-3.36591484636034,20.4250812557965));
#15661=CARTESIAN_POINT('Ctrl Pts',(6.39181495226808,-3.42583468603137,20.4309553944911));
#15662=CARTESIAN_POINT('Ctrl Pts',(6.29016030425197,-3.48129381060674,20.4368295331857));
#15663=CARTESIAN_POINT('Ctrl Pts',(6.18643058930618,-3.53209884729069,20.4427036718803));
#15664=CARTESIAN_POINT('Ctrl Pts',(6.16019903673279,-3.54494661219069,20.4441891457203));
#15665=CARTESIAN_POINT('Ctrl Pts',(6.13383487071145,-3.55749699255338,20.4456746195604));
#15666=CARTESIAN_POINT('Ctrl Pts',(6.1073454698712,-3.56974736247987,20.4471600934005));
#15667=CARTESIAN_POINT('Ctrl Pts',(6.00260413524884,-3.61818636279764,20.4530337827864));
#15668=CARTESIAN_POINT('Ctrl Pts',(5.89555464664127,-3.66209224752305,20.4589074721724));
#15669=CARTESIAN_POINT('Ctrl Pts',(5.7866264559468,-3.70123903915474,20.4647811615584));
#15670=CARTESIAN_POINT('Ctrl Pts',(5.67783890178138,-3.74033528860021,20.4706472674595));
#15671=CARTESIAN_POINT('Ctrl Pts',(5.56717785446262,-3.77468452577001,20.4765133733605));
#15672=CARTESIAN_POINT('Ctrl Pts',(5.45509540231072,-3.80410758532834,20.4823794792616));
#15673=CARTESIAN_POINT('Ctrl Pts',(5.34312772116331,-3.83350051604816,20.4882395783449));
#15674=CARTESIAN_POINT('Ctrl Pts',(5.22974192752406,-3.85797719849521,20.4940996774282));
#15675=CARTESIAN_POINT('Ctrl Pts',(5.11540741082015,-3.87740755024905,20.4999597765115));
#15676=CARTESIAN_POINT('Ctrl Pts',(4.99694796546249,-3.89753890478851,20.5060312946074));
#15677=CARTESIAN_POINT('Ctrl Pts',(4.87747047409657,-3.9122527809085,20.5121028127033));
#15678=CARTESIAN_POINT('Ctrl Pts',(4.75751144867638,-3.92146178204599,20.5181743307991));
#15679=CARTESIAN_POINT('Ctrl Pts',(4.64186264703803,-3.93033989640301,20.524027694391));
#15680=CARTESIAN_POINT('Ctrl Pts',(4.52576676687471,-3.93410188254948,20.5298810579829));
#15681=CARTESIAN_POINT('Ctrl Pts',(4.40971124521822,-3.93272204744178,20.5357344215748));
#15682=CARTESIAN_POINT('Ctrl Pts',(4.29367314890863,-3.93134241951168,20.5415869063038));
#15683=CARTESIAN_POINT('Ctrl Pts',(4.17767581206175,-3.92482251031784,20.5474393910328));
#15684=CARTESIAN_POINT('Ctrl Pts',(4.0622067941707,-3.91318875462185,20.5532918757618));
#15685=CARTESIAN_POINT('Ctrl Pts',(3.94672718932174,-3.90155393226672,20.559144897085));
#15686=CARTESIAN_POINT('Ctrl Pts',(3.83177641080876,-3.88480437275555,20.5649979184082));
#15687=CARTESIAN_POINT('Ctrl Pts',(3.7178363104098,-3.86301832676939,20.5708509397314));
#15688=CARTESIAN_POINT('Ctrl Pts',(3.60385820878753,-3.84122501471627,20.5767059131503));
#15689=CARTESIAN_POINT('Ctrl Pts',(3.49089186112378,-3.81439195359782,20.5825608865691));
#15690=CARTESIAN_POINT('Ctrl Pts',(3.37940765624663,-3.78264823014049,20.588415859988));
#15691=CARTESIAN_POINT('Ctrl Pts',(3.26779709834318,-3.75086852925005,20.5942774692671));
#15692=CARTESIAN_POINT('Ctrl Pts',(3.15767243361623,-3.71416717061233,20.6001390785463));
#15693=CARTESIAN_POINT('Ctrl Pts',(3.04948773799101,-3.67272275423307,20.6060006878255));
#15694=CARTESIAN_POINT('Ctrl Pts',(2.94123009263126,-3.63125039157957,20.6118662496308));
#15695=CARTESIAN_POINT('Ctrl Pts',(2.83491539910909,-3.58502876701982,20.6177318114361));
#15696=CARTESIAN_POINT('Ctrl Pts',(2.73097505567941,-3.53428341839687,20.6235973732414));
#15697=CARTESIAN_POINT('Ctrl Pts',(2.62688272597427,-3.48346386762795,20.6294715119368));
#15698=CARTESIAN_POINT('Ctrl Pts',(2.52517203685204,-3.42810758806947,20.6353456506321));
#15699=CARTESIAN_POINT('Ctrl Pts',(2.42624730078802,-3.36848458817249,20.6412197893274));
#15700=CARTESIAN_POINT('Ctrl Pts',(2.40123084918291,-3.35340690436134,20.6427052631557));
#15701=CARTESIAN_POINT('Ctrl Pts',(2.37639240112385,-3.33805656944734,20.644190736984));
#15702=CARTESIAN_POINT('Ctrl Pts',(2.35173816319912,-3.32243836022548,20.6456762108123));
#15703=CARTESIAN_POINT('Ctrl Pts',(2.25425321678615,-3.26068263718476,20.651549900236));
#15704=CARTESIAN_POINT('Ctrl Pts',(2.15932621079835,-3.19452990911246,20.6574235896598));
#15705=CARTESIAN_POINT('Ctrl Pts',(2.0673798458647,-3.12421854326219,20.6632972790835));
#15706=CARTESIAN_POINT('Ctrl Pts',(1.97555219232417,-3.05399795598916,20.6691633850225));
#15707=CARTESIAN_POINT('Ctrl Pts',(1.88669785204408,-2.97962965717206,20.6750294909615));
#15708=CARTESIAN_POINT('Ctrl Pts',(1.80121246044254,-2.90139641294738,20.6808955969005));
#15709=CARTESIAN_POINT('Ctrl Pts',(1.7158146047917,-2.82324327856697,20.6867556960218));
#15710=CARTESIAN_POINT('Ctrl Pts',(1.63377913892778,-2.74123334814802,20.6926157951432));
#15711=CARTESIAN_POINT('Ctrl Pts',(1.55546983260423,-2.65569053439796,20.6984758942645));
#15712=CARTESIAN_POINT('Ctrl Pts',(1.47433530578824,-2.56706153176774,20.7045474123461));
#15713=CARTESIAN_POINT('Ctrl Pts',(1.39720123616582,-2.4746401905453,20.7106189304278));
#15714=CARTESIAN_POINT('Ctrl Pts',(1.32443191198014,-2.37882996742285,20.7166904485094));
#15715=CARTESIAN_POINT('Ctrl Pts',(1.25427724722614,-2.28646228147308,20.7225438121394));
#15716=CARTESIAN_POINT('Ctrl Pts',(1.1881793396891,-2.19094541013953,20.7283971757693));
#15717=CARTESIAN_POINT('Ctrl Pts',(1.12642402368809,-2.0926750221467,20.7342505393993));
#15718=CARTESIAN_POINT('Ctrl Pts',(1.06467798004083,-1.99441938912332,20.7401030241663));
#15719=CARTESIAN_POINT('Ctrl Pts',(1.00727345122547,-1.89341141121052,20.7459555089334));
#15720=CARTESIAN_POINT('Ctrl Pts',(0.95445253454464,-1.79007511901691,20.7518079937004));
#15721=CARTESIAN_POINT('Ctrl Pts',(0.901626774896074,-1.68672935227494,
20.7576610150616));
#15722=CARTESIAN_POINT('Ctrl Pts',(0.853385650860985,-1.58105521477579,
20.7635140364227));
#15723=CARTESIAN_POINT('Ctrl Pts',(0.809924624211627,-1.47350003079302,
20.7693670577839));
#15724=CARTESIAN_POINT('Ctrl Pts',(0.766449102471797,-1.36590897508234,
20.7752220312406));
#15725=CARTESIAN_POINT('Ctrl Pts',(0.72775700292333,-1.25643600824745,20.7810770046973));
#15726=CARTESIAN_POINT('Ctrl Pts',(0.693994855236427,-1.14554638085883,
20.7869319781539));
#15727=CARTESIAN_POINT('Ctrl Pts',(0.660194442494234,-1.0345310743291,20.7927935874705));
#15728=CARTESIAN_POINT('Ctrl Pts',(0.631335254263033,-0.922096298012428,
20.7986551967871));
#15729=CARTESIAN_POINT('Ctrl Pts',(0.60751337043616,-0.808720436238716,
20.8045168061037));
#15730=CARTESIAN_POINT('Ctrl Pts',(0.583675423338946,-0.695268124292923,
20.8103823679463));
#15731=CARTESIAN_POINT('Ctrl Pts',(0.56488161102356,-0.580873869969791,
20.8162479297889));
#15732=CARTESIAN_POINT('Ctrl Pts',(0.551176277369566,-0.466022446823152,
20.8221134916315));
#15733=CARTESIAN_POINT('Ctrl Pts',(0.537450903157662,-0.351003082737979,
20.8279876303636));
#15734=CARTESIAN_POINT('Ctrl Pts',(0.52882888782412,-0.235525626099837,
20.8338617690956));
#15735=CARTESIAN_POINT('Ctrl Pts',(0.525302522788892,-0.120076198009198,
20.8397359078277));
#15736=CARTESIAN_POINT('Ctrl Pts',(0.524410762834271,-0.0908809287371239,
20.8412213812931));
#15737=CARTESIAN_POINT('Ctrl Pts',(0.523844610997288,-0.0616874304851447,
20.8427068547585));
#15738=CARTESIAN_POINT('Ctrl Pts',(0.523603417950699,-0.0325035082383315,
20.8441923282239));
#15739=CARTESIAN_POINT('Ctrl Pts',(0.522649719982162,0.0828922204297335,
20.8500660175624));
#15740=CARTESIAN_POINT('Ctrl Pts',(0.526777543537242,0.198522149960062,
20.8559397069009));
#15741=CARTESIAN_POINT('Ctrl Pts',(0.536015736779851,0.313901860553742,
20.8618133962393));
#15742=CARTESIAN_POINT('Ctrl Pts',(0.545242002647123,0.429132605101971,
20.8676795020931));
#15743=CARTESIAN_POINT('Ctrl Pts',(0.559565484335337,0.54411336510068,20.8735456079469));
#15744=CARTESIAN_POINT('Ctrl Pts',(0.578963048970497,0.658358394802545,
20.8794117138007));
#15745=CARTESIAN_POINT('Ctrl Pts',(0.598340750746892,0.772486439051222,
20.8852718128369));
#15746=CARTESIAN_POINT('Ctrl Pts',(0.622782131854229,0.885879846640568,
20.8911319118731));
#15747=CARTESIAN_POINT('Ctrl Pts',(0.652212208952136,0.998057342843189,
20.8969920109093));
#15748=CARTESIAN_POINT('Ctrl Pts',(0.682704056458585,1.11428194859214,20.9030635290228));
#15749=CARTESIAN_POINT('Ctrl Pts',(0.718551321817345,1.22920080160129,20.9091350471364));
#15750=CARTESIAN_POINT('Ctrl Pts',(0.759612461323276,1.34228906987127,20.91520656525));
#15751=CARTESIAN_POINT('Ctrl Pts',(0.799198240798473,1.45131398498159,20.9210599287956));
#15752=CARTESIAN_POINT('Ctrl Pts',(0.843629512017629,1.55863717857696,20.9269132923412));
#15753=CARTESIAN_POINT('Ctrl Pts',(0.8927287449547,1.66380396606726,20.9327666558868));
#15754=CARTESIAN_POINT('Ctrl Pts',(0.941820605809915,1.7689549631242,20.9386191405699));
#15755=CARTESIAN_POINT('Ctrl Pts',(0.99557886004476,1.87194982361109,20.944471625253));
#15756=CARTESIAN_POINT('Ctrl Pts',(1.05377843466681,1.97235524024878,20.950324109936));
#15757=CARTESIAN_POINT('Ctrl Pts',(1.11198334541237,2.07276986272188,20.9561771312138));
#15758=CARTESIAN_POINT('Ctrl Pts',(1.1746301788411,2.17059421192432,20.9620301524915));
#15759=CARTESIAN_POINT('Ctrl Pts',(1.24144900654662,2.26542154106194,20.9678831737693));
#15760=CARTESIAN_POINT('Ctrl Pts',(1.30829011962685,2.3602804969526,20.9737381471431));
#15761=CARTESIAN_POINT('Ctrl Pts',(1.37930575595772,2.45214010764749,20.9795931205169));
#15762=CARTESIAN_POINT('Ctrl Pts',(1.45418439696715,2.54062502636597,20.9854480938908));
#15763=CARTESIAN_POINT('Ctrl Pts',(1.52914790331058,2.62921023138879,20.9913097031258));
#15764=CARTESIAN_POINT('Ctrl Pts',(1.60798288596538,2.71441279485008,20.9971713123609));
#15765=CARTESIAN_POINT('Ctrl Pts',(1.69033944065475,2.79589264337699,21.003032921596));
#15766=CARTESIAN_POINT('Ctrl Pts',(1.77275152898083,2.87742743437113,21.0088984833577));
#15767=CARTESIAN_POINT('Ctrl Pts',(1.85868961223166,2.95523423535495,21.0147640451194));
#15768=CARTESIAN_POINT('Ctrl Pts',(1.94777037063086,3.02901298347535,21.0206296068811));
#15769=CARTESIAN_POINT('Ctrl Pts',(2.03698138696435,3.10289961423502,21.0265037455339));
#15770=CARTESIAN_POINT('Ctrl Pts',(2.12934392137204,3.17274618892872,21.0323778841867));
#15771=CARTESIAN_POINT('Ctrl Pts',(2.22444530359067,3.23829565427617,21.0382520228394));
#15772=CARTESIAN_POINT('Ctrl Pts',(2.24849489864431,3.2548720494958,21.0397374971048));
#15773=CARTESIAN_POINT('Ctrl Pts',(2.27271952094194,3.27117387327726,21.0412229713702));
#15774=CARTESIAN_POINT('Ctrl Pts',(2.29711225987554,3.28719744009283,21.0427084456356));
#15775=CARTESIAN_POINT('Ctrl Pts',(2.39356318796271,3.35055596226765,21.0485821350124));
#15776=CARTESIAN_POINT('Ctrl Pts',(2.49296565804658,3.40977140450462,21.0544558243892));
#15777=CARTESIAN_POINT('Ctrl Pts',(2.59492824722972,3.4645569168822,21.060329513766));
#15778=CARTESIAN_POINT('Ctrl Pts',(2.69675919312201,3.51927169601145,21.0661956196575));
#15779=CARTESIAN_POINT('Ctrl Pts',(2.80114332423419,3.56956772564308,21.072061725549));
#15780=CARTESIAN_POINT('Ctrl Pts',(2.90765992404886,3.61520111712029,21.0779278314404));
#15781=CARTESIAN_POINT('Ctrl Pts',(3.01406745221326,3.66078778058212,21.0837879305137));
#15782=CARTESIAN_POINT('Ctrl Pts',(3.12260272817269,3.70172114100203,21.089648029587));
#15783=CARTESIAN_POINT('Ctrl Pts',(3.23282068381178,3.73780330385939,21.0955081286603));
#15784=CARTESIAN_POINT('Ctrl Pts',(3.34701505223099,3.7751872289631,21.1015796467597));
#15785=CARTESIAN_POINT('Ctrl Pts',(3.46301540931486,3.80736309348091,21.1076511648592));
#15786=CARTESIAN_POINT('Ctrl Pts',(3.58030400243654,3.83416532128118,21.1137226829587));
#15787=CARTESIAN_POINT('Ctrl Pts',(3.69337832226668,3.86000452352401,21.1195760465395));
#15788=CARTESIAN_POINT('Ctrl Pts',(3.80764945932911,3.88084950156652,21.1254294101204));
#15789=CARTESIAN_POINT('Ctrl Pts',(3.92263909787558,3.89660294643846,21.1312827737013));
#15790=CARTESIAN_POINT('Ctrl Pts',(4.0376114711073,3.91235402598265,21.137135258419));
#15791=CARTESIAN_POINT('Ctrl Pts',(4.15330172210416,3.92301503636198,21.1429877431367));
#15792=CARTESIAN_POINT('Ctrl Pts',(4.26922372514543,3.92854020817745,21.1488402278543));
#15793=CARTESIAN_POINT('Ctrl Pts',(4.38515635667092,3.93406588657666,21.1546932491659));
#15794=CARTESIAN_POINT('Ctrl Pts',(4.50132036978176,3.93445477066204,21.1605462704775));
#15795=CARTESIAN_POINT('Ctrl Pts',(4.61722764119416,3.92971318208243,21.1663992917891));
#15796=CARTESIAN_POINT('Ctrl Pts',(4.73317356991329,3.92497001209173,21.172254265196));
#15797=CARTESIAN_POINT('Ctrl Pts',(4.84886217408903,3.91509298384522,21.1781092386028));
#15798=CARTESIAN_POINT('Ctrl Pts',(4.96380916969043,3.90014038978036,21.1839642120097));
#15799=CARTESIAN_POINT('Ctrl Pts',(5.07888644293921,3.88517084887172,21.1898258212765));
#15800=CARTESIAN_POINT('Ctrl Pts',(5.19322002006796,3.86511431382172,21.1956874305433));
#15801=CARTESIAN_POINT('Ctrl Pts',(5.30633444831095,3.84008045492665,21.2015490398101));
#15802=CARTESIAN_POINT('Ctrl Pts',(5.41952515043878,3.81502971551775,21.2074146016029));
#15803=CARTESIAN_POINT('Ctrl Pts',(5.5314946686843,3.7849950760068,21.2132801633956));
#15804=CARTESIAN_POINT('Ctrl Pts',(5.64178305657467,3.75013597608013,21.2191457251883));
#15805=CARTESIAN_POINT('Ctrl Pts',(5.75223271313403,3.71522590360091,21.2250198638708));
#15806=CARTESIAN_POINT('Ctrl Pts',(5.86099594678789,3.67547743287776,21.2308940025533));
#15807=CARTESIAN_POINT('Ctrl Pts',(5.96763304116629,3.6310979829402,21.2367681412357));
#15808=CARTESIAN_POINT('Ctrl Pts',(5.99459982438271,3.61987514333915,21.2382536151729));
#15809=CARTESIAN_POINT('Ctrl Pts',(6.02143076705886,3.60835637931336,21.2397390891101));
#15810=CARTESIAN_POINT('Ctrl Pts',(6.04811902591505,3.59654549993868,21.2412245630472));
#15811=CARTESIAN_POINT('Ctrl Pts',(6.15364665911984,3.54984428375247,21.2470982526581));
#15812=CARTESIAN_POINT('Ctrl Pts',(6.25729288846732,3.49841686028241,21.2529719422689));
#15813=CARTESIAN_POINT('Ctrl Pts',(6.35860447761976,3.44243664122715,21.2588456318798));
#15814=CARTESIAN_POINT('Ctrl Pts',(6.45978526401042,3.38652869788406,21.2647117380066));
#15815=CARTESIAN_POINT('Ctrl Pts',(6.55863704622935,3.32607984652786,21.2705778441334));
#15816=CARTESIAN_POINT('Ctrl Pts',(6.65472680827972,3.26131140422491,21.2764439502602));
#15817=CARTESIAN_POINT('Ctrl Pts',(6.75071817564942,3.19660928397399,21.2823040495697));
#15818=CARTESIAN_POINT('Ctrl Pts',(6.84395280796955,3.12759660044398,21.2881641488793));
#15819=CARTESIAN_POINT('Ctrl Pts',(6.93402313724634,3.05454006739746,21.2940242481889));
#15820=CARTESIAN_POINT('Ctrl Pts',(7.02734299371901,2.97884782520146,21.3000957662001));
#15821=CARTESIAN_POINT('Ctrl Pts',(7.11726551967245,2.89881465760119,21.3061672842113));
#15822=CARTESIAN_POINT('Ctrl Pts',(7.20337090161216,2.81478587577487,21.3122388022226));
#15823=CARTESIAN_POINT('Ctrl Pts',(7.28638245263658,2.73377631106523,21.3180921660407));
#15824=CARTESIAN_POINT('Ctrl Pts',(7.36584612356239,2.64905363478006,21.3239455298587));
#15825=CARTESIAN_POINT('Ctrl Pts',(7.44142084536629,2.56096702730768,21.3297988936768));
#15826=CARTESIAN_POINT('Ctrl Pts',(7.51698421987462,2.47289364574928,21.3356513786315));
#15827=CARTESIAN_POINT('Ctrl Pts',(7.58865953735275,2.38145765077103,21.3415038635863));
#15828=CARTESIAN_POINT('Ctrl Pts',(7.65614480402373,2.28704272563348,21.3473563485411));
#15829=CARTESIAN_POINT('Ctrl Pts',(7.72363625817945,2.19261914392633,21.3532093700894));
#15830=CARTESIAN_POINT('Ctrl Pts',(7.7869366575749,2.09521642523866,21.3590623916378));
#15831=CARTESIAN_POINT('Ctrl Pts',(7.84578669805172,1.99524817045103,21.3649154131861));
#15832=CARTESIAN_POINT('Ctrl Pts',(7.90465636614359,1.89524657433677,21.3707703868292));
#15833=CARTESIAN_POINT('Ctrl Pts',(7.95907251441327,1.79267809653119,21.3766253604723));
#15834=CARTESIAN_POINT('Ctrl Pts',(8.00882159145933,1.68798128561946,21.3824803341154));
#15835=CARTESIAN_POINT('Ctrl Pts',(8.05862705267118,1.58316581436881,21.3883419436163));
#15836=CARTESIAN_POINT('Ctrl Pts',(8.10375470767438,1.47621756879183,21.3942035531173));
#15837=CARTESIAN_POINT('Ctrl Pts',(8.14403896579817,1.36759552891844,21.4000651626182));
#15838=CARTESIAN_POINT('Ctrl Pts',(8.18435038788405,1.25890024443018,21.4059307246442));
#15839=CARTESIAN_POINT('Ctrl Pts',(8.21981178382042,1.14852931061809,21.4117962866702));
#15840=CARTESIAN_POINT('Ctrl Pts',(8.25030779065407,1.03695565791324,21.4176618486961));
#15841=CARTESIAN_POINT('Ctrl Pts',(8.2808483901102,0.925218857233,21.4235359876087));
#15842=CARTESIAN_POINT('Ctrl Pts',(8.30640901925999,0.812276229203628,21.4294101265213));
#15843=CARTESIAN_POINT('Ctrl Pts',(8.32692559949976,0.698609714801456,21.4352842654339));
#15844=CARTESIAN_POINT('Ctrl Pts',(8.33211390016254,0.669865350725404,21.4367697371089));
#15845=CARTESIAN_POINT('Ctrl Pts',(8.33697989374072,0.641074711219869,21.4382552087839));
#15846=CARTESIAN_POINT('Ctrl Pts',(8.34152307122561,0.61224561164665,21.4397406804589));
#15847=CARTESIAN_POINT('Ctrl Pts',(8.37110695828926,0.424518667507654,21.4494136519451));
#15848=CARTESIAN_POINT('Ctrl Pts',(8.38708943569742,0.234594111220408,21.4590866234314));
#15849=CARTESIAN_POINT('Ctrl Pts',(8.38922270894465,0.0440238599231025,
21.4687595949177));
#15850=CARTESIAN_POINT('Ctrl Pts',(8.3893753872624,0.0303847513748413,21.4694518892668));
#15851=CARTESIAN_POINT('Ctrl Pts',(8.38945714112686,0.0167423532144361,
21.470144183616));
#15852=CARTESIAN_POINT('Ctrl Pts',(8.38946788667581,0.00309724383391784,
21.4708364779651));
#15853=CARTESIAN_POINT('',(8.38721926685989,-0.00134106201782228,18.9708368356832));
#15854=CARTESIAN_POINT('Ctrl Pts',(8.38344183965918,-0.00135169739119494,
18.9708374363438));
#15855=CARTESIAN_POINT('Ctrl Pts',(8.38518238981383,-0.574802882154291,
18.9997407147355));
#15856=CARTESIAN_POINT('Ctrl Pts',(7.99895462546289,-2.45889274337807,19.0948160322645));
#15857=CARTESIAN_POINT('Ctrl Pts',(5.09181089789537,-4.60543441257073,19.2560633889306));
#15858=CARTESIAN_POINT('Ctrl Pts',(0.930911257582632,-3.03053249053979,
19.4545795063423));
#15859=CARTESIAN_POINT('Ctrl Pts',(-0.00134956819690293,1.31967343935667,
19.6530956237539));
#15860=CARTESIAN_POINT('Ctrl Pts',(3.14877515140037,4.46134753659125,19.8516117411657));
#15861=CARTESIAN_POINT('Ctrl Pts',(7.2934463239171,3.56148175989967,20.0408581667598));
#15862=CARTESIAN_POINT('Ctrl Pts',(8.38379978416848,1.11910507696889,20.1639325532169));
#15863=CARTESIAN_POINT('Ctrl Pts',(8.39304923023168,-0.00285552977342319,
20.2208349005368));
#15864=CARTESIAN_POINT('',(8.38946749588772,0.00355905287639204,17.7208364779273));
#15865=CARTESIAN_POINT('Ctrl Pts',(8.38946749588839,0.003559052130875,17.720836477965));
#15866=CARTESIAN_POINT('Ctrl Pts',(8.38957613282376,-0.116492263818579,
17.7269037316768));
#15867=CARTESIAN_POINT('Ctrl Pts',(8.38418299164283,-0.236671020316373,
17.7329709853887));
#15868=CARTESIAN_POINT('Ctrl Pts',(8.37328515500261,-0.356428169460906,
17.7390382391005));
#15869=CARTESIAN_POINT('Ctrl Pts',(8.36287449178463,-0.470831733108411,
17.7448342642326));
#15870=CARTESIAN_POINT('Ctrl Pts',(8.34744071078401,-0.584850100472209,
17.7506302893647));
#15871=CARTESIAN_POINT('Ctrl Pts',(8.32703452225374,-0.698005988649095,
17.7564263144967));
#15872=CARTESIAN_POINT('Ctrl Pts',(8.3066329990051,-0.811136007022526,17.7622210145362));
#15873=CARTESIAN_POINT('Ctrl Pts',(8.28126140237628,-0.923403522833055,
17.7680157145757));
#15874=CARTESIAN_POINT('Ctrl Pts',(8.25102193708545,-1.03433931268114,17.7738104146152));
#15875=CARTESIAN_POINT('Ctrl Pts',(8.2207817158513,-1.14527787576511,17.7796052595138));
#15876=CARTESIAN_POINT('Ctrl Pts',(8.18567349567977,-1.25488423951721,17.7854001044125));
#15877=CARTESIAN_POINT('Ctrl Pts',(8.14584972406252,-1.36270306988538,17.7911949493112));
#15878=CARTESIAN_POINT('Ctrl Pts',(8.1060148561022,-1.47055194247913,17.7969914088632));
#15879=CARTESIAN_POINT('Ctrl Pts',(8.06146197206998,-1.57661189612038,17.8027878684152));
#15880=CARTESIAN_POINT('Ctrl Pts',(8.01239183446375,-1.68044712822125,17.8085843279673));
#15881=CARTESIAN_POINT('Ctrl Pts',(7.96326770939825,-1.78439660088957,17.8143871648425));
#15882=CARTESIAN_POINT('Ctrl Pts',(7.90961659298189,-1.88611608537518,17.8201900017176));
#15883=CARTESIAN_POINT('Ctrl Pts',(7.85168541861316,-1.98519399355516,17.8259928385928));
#15884=CARTESIAN_POINT('Ctrl Pts',(7.79371681124774,-2.08433592223964,17.831799425048));
#15885=CARTESIAN_POINT('Ctrl Pts',(7.73146287032479,-2.18083252392463,17.8376060115032));
#15886=CARTESIAN_POINT('Ctrl Pts',(7.6652130495779,-2.27430237786288,17.8434125979584));
#15887=CARTESIAN_POINT('Ctrl Pts',(7.59886475324261,-2.36791116800896,17.8492278154863));
#15888=CARTESIAN_POINT('Ctrl Pts',(7.5285089834235,-2.45848390128237,17.8550430330141));
#15889=CARTESIAN_POINT('Ctrl Pts',(7.45447449914436,-2.54567332232279,17.860858250542));
#15890=CARTESIAN_POINT('Ctrl Pts',(7.43074226748708,-2.57362245384363,17.8627223560444));
#15891=CARTESIAN_POINT('Ctrl Pts',(7.40663229723318,-2.6012242220324,17.8645864615467));
#15892=CARTESIAN_POINT('Ctrl Pts',(7.38215616249663,-2.62846804217306,17.8664505670491));
#15893=CARTESIAN_POINT('Ctrl Pts',(7.3050332674982,-2.71431175494391,17.8723242564396));
#15894=CARTESIAN_POINT('Ctrl Pts',(7.22400056262058,-2.7969012245466,17.8781979458302));
#15895=CARTESIAN_POINT('Ctrl Pts',(7.13936345849576,-2.87585933148988,17.8840716352208));
#15896=CARTESIAN_POINT('Ctrl Pts',(7.05483562882367,-2.95471549609931,17.8899377411265));
#15897=CARTESIAN_POINT('Ctrl Pts',(6.9667129537625,-3.02994934254737,17.8958038470323));
#15898=CARTESIAN_POINT('Ctrl Pts',(6.87534011754019,-3.10121783023804,17.901669952938));
#15899=CARTESIAN_POINT('Ctrl Pts',(6.78406084593812,-3.17241333990525,17.9075300520261));
#15900=CARTESIAN_POINT('Ctrl Pts',(6.68953835692216,-3.23965131485814,17.9133901511141));
#15901=CARTESIAN_POINT('Ctrl Pts',(6.59215260222646,-3.30262698542814,17.9192502502022));
#15902=CARTESIAN_POINT('Ctrl Pts',(6.49125339167387,-3.36787467452176,17.9253217682963));
#15903=CARTESIAN_POINT('Ctrl Pts',(6.38728074481688,-3.42854639602921,17.9313932863904));
#15904=CARTESIAN_POINT('Ctrl Pts',(6.28069313369929,-3.48435011122029,17.9374648044845));
#15905=CARTESIAN_POINT('Ctrl Pts',(6.17793530063186,-3.53814875432732,17.9433181680812));
#15906=CARTESIAN_POINT('Ctrl Pts',(6.07274758221572,-3.58742298538944,17.949171531678));
#15907=CARTESIAN_POINT('Ctrl Pts',(5.96556771046482,-3.63195682830358,17.9550248952747));
#15908=CARTESIAN_POINT('Ctrl Pts',(5.85840393141092,-3.6764839846111,17.9608773800086));
#15909=CARTESIAN_POINT('Ctrl Pts',(5.74924897519467,-3.71627200952174,17.9667298647425));
#15910=CARTESIAN_POINT('Ctrl Pts',(5.6385612587536,-3.75115277520315,17.9725823494764));
#15911=CARTESIAN_POINT('Ctrl Pts',(5.52786339373526,-3.78603673898239,17.9784353708046));
#15912=CARTESIAN_POINT('Ctrl Pts',(5.41563288318893,-3.81601242493351,17.9842883921328));
#15913=CARTESIAN_POINT('Ctrl Pts',(5.302343348947,-3.84096156782231,17.9901414134609));
#15914=CARTESIAN_POINT('Ctrl Pts',(5.18901603045765,-3.86591903173206,17.9959963868848));
#15915=CARTESIAN_POINT('Ctrl Pts',(5.07462938919954,-3.88584653022755,18.0018513603086));
#15916=CARTESIAN_POINT('Ctrl Pts',(4.95966657710611,-3.90067703165643,18.0077063337324));
#15917=CARTESIAN_POINT('Ctrl Pts',(4.84457346943133,-3.9155243415538,18.0135679430165));
#15918=CARTESIAN_POINT('Ctrl Pts',(4.72890329752009,-3.92526307136828,18.0194295523007));
#15919=CARTESIAN_POINT('Ctrl Pts',(4.61314376508996,-3.92987812168105,18.0252911615848));
#15920=CARTESIAN_POINT('Ctrl Pts',(4.49730617515689,-3.93449628395615,18.0311567233952));
#15921=CARTESIAN_POINT('Ctrl Pts',(4.3813795168395,-3.93398388900967,18.0370222852055));
#15922=CARTESIAN_POINT('Ctrl Pts',(4.26584918109284,-3.92837791513815,18.0428878470159));
#15923=CARTESIAN_POINT('Ctrl Pts',(4.15014991165982,-3.92276374395788,18.0487619857162));
#15924=CARTESIAN_POINT('Ctrl Pts',(4.03484853116391,-3.91204116750257,18.0546361244165));
#15925=CARTESIAN_POINT('Ctrl Pts',(3.920423093794,-3.89629871449354,18.0605102631168));
#15926=CARTESIAN_POINT('Ctrl Pts',(3.89148676869231,-3.89231770512502,18.0619957368981));
#15927=CARTESIAN_POINT('Ctrl Pts',(3.8626063960005,-3.8880159260561,18.0634812106794));
#15928=CARTESIAN_POINT('Ctrl Pts',(3.83378956369566,-3.88339531690038,18.0649666844607));
#15929=CARTESIAN_POINT('Ctrl Pts',(3.71984536332599,-3.86512503618739,18.0708403738513));
#15930=CARTESIAN_POINT('Ctrl Pts',(3.6065161839055,-3.84180515537926,18.0767140632418));
#15931=CARTESIAN_POINT('Ctrl Pts',(3.49428448791038,-3.81348787336366,18.0825877526324));
#15932=CARTESIAN_POINT('Ctrl Pts',(3.38219769357849,-3.78520715161943,18.0884538585381));
#15933=CARTESIAN_POINT('Ctrl Pts',(3.27120596174663,-3.7519419599581,18.0943199644439));
#15934=CARTESIAN_POINT('Ctrl Pts',(3.16178440871784,-3.71379597367145,18.1001860703497));
#15935=CARTESIAN_POINT('Ctrl Pts',(3.0524749019655,-3.67568904838883,18.1060461694377));
#15936=CARTESIAN_POINT('Ctrl Pts',(2.94473276368286,-3.63271140485437,18.1119062685257));
#15937=CARTESIAN_POINT('Ctrl Pts',(2.83902006966279,-3.58501710095584,18.1177663676137));
#15938=CARTESIAN_POINT('Ctrl Pts',(2.7294935028116,-3.5356020953807,18.1238378857078));
#15939=CARTESIAN_POINT('Ctrl Pts',(2.62214601837952,-3.48112378161057,18.1299094038019));
#15940=CARTESIAN_POINT('Ctrl Pts',(2.51747156085872,-3.42180910032832,18.1359809218961));
#15941=CARTESIAN_POINT('Ctrl Pts',(2.41655814025049,-3.36462564294771,18.1418342854928));
#15942=CARTESIAN_POINT('Ctrl Pts',(2.31812935462938,-3.30294760703951,18.1476876490895));
#15943=CARTESIAN_POINT('Ctrl Pts',(2.22260398909766,-3.2370257395504,18.1535410126863));
#15944=CARTESIAN_POINT('Ctrl Pts',(2.12709296637793,-3.17111377000772,18.1593934974202));
#15945=CARTESIAN_POINT('Ctrl Pts',(2.03448483688213,-3.10095947046617,18.1652459821541));
#15946=CARTESIAN_POINT('Ctrl Pts',(1.94516939192894,-3.02685690857867,18.171098466888));
#15947=CARTESIAN_POINT('Ctrl Pts',(1.85584575794859,-2.95274755248114,18.1769514882162));
#15948=CARTESIAN_POINT('Ctrl Pts',(1.76981572662577,-2.87468947822612,18.1828045095444));
#15949=CARTESIAN_POINT('Ctrl Pts',(1.68743543206477,-2.79301656124772,18.1886575308726));
#15950=CARTESIAN_POINT('Ctrl Pts',(1.6050276620849,-2.71131640477453,18.1945125042964));
#15951=CARTESIAN_POINT('Ctrl Pts',(1.52627234256563,-2.62599929897492,18.2003674777202));
#15952=CARTESIAN_POINT('Ctrl Pts',(1.45148772198882,-2.53743490171365,18.206222451144));
#15953=CARTESIAN_POINT('Ctrl Pts',(1.37661834265025,-2.44877012808368,18.2120840604281));
#15954=CARTESIAN_POINT('Ctrl Pts',(1.30572891123235,-2.35685103299678,18.2179456697123));
#15955=CARTESIAN_POINT('Ctrl Pts',(1.23909650471908,-2.2620792521754,18.2238072789964));
#15956=CARTESIAN_POINT('Ctrl Pts',(1.17241916748489,-2.16724356604642,18.2296728408068));
#15957=CARTESIAN_POINT('Ctrl Pts',(1.11000479292623,-2.06955171118859,18.2355384026171));
#15958=CARTESIAN_POINT('Ctrl Pts',(1.05208544294362,-1.96943161171664,18.2414039644274));
#15959=CARTESIAN_POINT('Ctrl Pts',(0.99408140066554,-1.86916511210294,18.2472781031277));
#15960=CARTESIAN_POINT('Ctrl Pts',(0.940585690803906,-1.76646364659972,
18.2531522418281));
#15961=CARTESIAN_POINT('Ctrl Pts',(0.891783079702071,-1.66177692015513,
18.2590263805284));
#15962=CARTESIAN_POINT('Ctrl Pts',(0.879441696062798,-1.63530335606045,
18.2605118543097));
#15963=CARTESIAN_POINT('Ctrl Pts',(0.867400190053486,-1.60870291690944,
18.261997328091));
#15964=CARTESIAN_POINT('Ctrl Pts',(0.855661045316142,-1.58198303042175,
18.2634828018723));
#15965=CARTESIAN_POINT('Ctrl Pts',(0.809243470825123,-1.47633033176402,
18.2693564912629));
#15966=CARTESIAN_POINT('Ctrl Pts',(0.767402523625336,-1.3684570037977,18.2752301806535));
#15967=CARTESIAN_POINT('Ctrl Pts',(0.730355888078917,-1.25879676104101,
18.2811038700441));
#15968=CARTESIAN_POINT('Ctrl Pts',(0.693357083219335,-1.14927809995974,
18.2869699759499));
#15969=CARTESIAN_POINT('Ctrl Pts',(0.661140411341709,-1.03797749994103,
18.2928360818556));
#15970=CARTESIAN_POINT('Ctrl Pts',(0.633876318351498,-0.92535040830438,
18.2987021877614));
#15971=CARTESIAN_POINT('Ctrl Pts',(0.60664014344528,-0.812838645375174,
18.3045622868494));
#15972=CARTESIAN_POINT('Ctrl Pts',(0.584346556662297,-0.699003491780741,
18.3104223859375));
#15973=CARTESIAN_POINT('Ctrl Pts',(0.567116597632666,-0.584316749682063,
18.3162824850255));
#15974=CARTESIAN_POINT('Ctrl Pts',(0.54926502098909,-0.465492371570913,
18.3223540031196));
#15975=CARTESIAN_POINT('Ctrl Pts',(0.53684948325925,-0.345754225986596,
18.3284255212137));
#15976=CARTESIAN_POINT('Ctrl Pts',(0.529947056413576,-0.225640405064559,
18.3344970393078));
#15977=CARTESIAN_POINT('Ctrl Pts',(0.523292639280731,-0.109842369720487,
18.3403504029046));
#15978=CARTESIAN_POINT('Ctrl Pts',(0.52176199601243,0.00630436111424336,
18.3462037665014));
#15979=CARTESIAN_POINT('Ctrl Pts',(0.52537144936873,0.122311946727261,18.3520571300981));
#15980=CARTESIAN_POINT('Ctrl Pts',(0.528980360777749,0.238302114191518,
18.357909614832));
#15981=CARTESIAN_POINT('Ctrl Pts',(0.537727821401377,0.354152765141346,
18.3637620995659));
#15982=CARTESIAN_POINT('Ctrl Pts',(0.551578033464427,0.469376938001323,
18.3696145842999));
#15983=CARTESIAN_POINT('Ctrl Pts',(0.565429515405994,0.584611675371151,
18.375467605628));
#15984=CARTESIAN_POINT('Ctrl Pts',(0.584384629527829,0.699219410251753,
18.3813206269562));
#15985=CARTESIAN_POINT('Ctrl Pts',(0.60835588136781,0.812719883312295,18.3871736482844));
#15986=CARTESIAN_POINT('Ctrl Pts',(0.63233512808316,0.926258210972273,18.3930286217083));
#15987=CARTESIAN_POINT('Ctrl Pts',(0.661333753833645,1.03868813847936,18.3988835951321));
#15988=CARTESIAN_POINT('Ctrl Pts',(0.695213657743602,1.14954184409258,18.4047385685559));
#15989=CARTESIAN_POINT('Ctrl Pts',(0.729131960172976,1.26052118814265,18.4106001778401));
#15990=CARTESIAN_POINT('Ctrl Pts',(0.767942462081084,1.36992034933718,18.4164617871243));
#15991=CARTESIAN_POINT('Ctrl Pts',(0.811457871886902,1.47728876716716,18.4223233964084));
#15992=CARTESIAN_POINT('Ctrl Pts',(0.855002624453212,1.58472958431,18.4281889582188));
#15993=CARTESIAN_POINT('Ctrl Pts',(0.903258430626849,1.69013655669717,18.4340545200292));
#15994=CARTESIAN_POINT('Ctrl Pts',(0.95599150537962,1.79308269916004,18.4399200818395));
#15995=CARTESIAN_POINT('Ctrl Pts',(1.00880168882113,1.89617937413202,18.4457942205399));
#15996=CARTESIAN_POINT('Ctrl Pts',(1.06610200308904,1.99680768016434,18.4516683592402));
#15997=CARTESIAN_POINT('Ctrl Pts',(1.12761472117852,2.09456856731924,18.4575424979405));
#15998=CARTESIAN_POINT('Ctrl Pts',(1.14317028337947,2.11929069972031,18.4590279717217));
#15999=CARTESIAN_POINT('Ctrl Pts',(1.15899502620116,2.14382962277052,18.4605134455029));
#16000=CARTESIAN_POINT('Ctrl Pts',(1.17508405447843,2.1681792228085,18.461998919284));
#16001=CARTESIAN_POINT('Ctrl Pts',(1.23870143762904,2.26445960770712,18.4678726086746));
#16002=CARTESIAN_POINT('Ctrl Pts',(1.30666586619626,2.35809804104783,18.4737462980651));
#16003=CARTESIAN_POINT('Ctrl Pts',(1.37873089523012,2.44867648018753,18.4796199874557));
#16004=CARTESIAN_POINT('Ctrl Pts',(1.45070288154124,2.53913797405278,18.4854860933614));
#16005=CARTESIAN_POINT('Ctrl Pts',(1.52676468489713,2.62654701009299,18.4913521992672));
#16006=CARTESIAN_POINT('Ctrl Pts',(1.60662598968765,2.7105134589526,18.4972183051729));
#16007=CARTESIAN_POINT('Ctrl Pts',(1.68640551751977,2.79439392723859,18.5030784042609));
#16008=CARTESIAN_POINT('Ctrl Pts',(1.7699765249434,2.87483852260551,18.508938503349));
#16009=CARTESIAN_POINT('Ctrl Pts',(1.85700816963507,2.95148976606359,18.514798602437));
#16010=CARTESIAN_POINT('Ctrl Pts',(1.94717971751622,3.03090641151614,18.5208701205311));
#16011=CARTESIAN_POINT('Ctrl Pts',(2.04106603977298,3.10625047284982,18.5269416386253));
#16012=CARTESIAN_POINT('Ctrl Pts',(2.13825675480958,3.17716548101862,18.5330131567194));
#16013=CARTESIAN_POINT('Ctrl Pts',(2.23195532978195,3.24553245627,18.5388665203161));
#16014=CARTESIAN_POINT('Ctrl Pts',(2.32872456285561,3.30978291527765,18.5447198839129));
#16015=CARTESIAN_POINT('Ctrl Pts',(2.42816336637527,3.36963867880817,18.5505732475096));
#16016=CARTESIAN_POINT('Ctrl Pts',(2.52758723949308,3.42948545519714,18.5564257322435));
#16017=CARTESIAN_POINT('Ctrl Pts',(2.62967953219101,3.48493863512843,18.5622782169774));
#16018=CARTESIAN_POINT('Ctrl Pts',(2.73401164052156,3.53576431325191,18.5681307017113));
#16019=CARTESIAN_POINT('Ctrl Pts',(2.83835331470551,3.58659465140761,18.5739837230395));
#16020=CARTESIAN_POINT('Ctrl Pts',(2.94493484132314,3.63279646338019,18.5798367443676));
#16021=CARTESIAN_POINT('Ctrl Pts',(3.05330522310997,3.67418291830177,18.5856897656958));
#16022=CARTESIAN_POINT('Ctrl Pts',(3.16171174851262,3.71558317640557,18.5915447391196));
#16023=CARTESIAN_POINT('Ctrl Pts',(3.27190792968327,3.75216473665313,18.5973997125435));
#16024=CARTESIAN_POINT('Ctrl Pts',(3.3834257865437,3.78379003567876,18.6032546859673));
#16025=CARTESIAN_POINT('Ctrl Pts',(3.49507003457047,3.81545117791857,18.6091162952515));
#16026=CARTESIAN_POINT('Ctrl Pts',(3.60803855041088,3.84214473439123,18.6149779045356));
#16027=CARTESIAN_POINT('Ctrl Pts',(3.72185119198616,3.86378383454475,18.6208395138197));
#16028=CARTESIAN_POINT('Ctrl Pts',(3.83574057826135,3.8854375261024,18.6267050756301));
#16029=CARTESIAN_POINT('Ctrl Pts',(3.95047481579575,3.9020299157593,18.6325706374404));
#16030=CARTESIAN_POINT('Ctrl Pts',(4.0655683685142,3.91352598218824,18.6384361992507));
#16031=CARTESIAN_POINT('Ctrl Pts',(4.18083021623513,3.92503885868588,18.644310337951));
#16032=CARTESIAN_POINT('Ctrl Pts',(4.29645201679292,3.9314405167363,18.6501844766514));
#16033=CARTESIAN_POINT('Ctrl Pts',(4.41194788694267,3.9327480037544,18.6560586153517));
#16034=CARTESIAN_POINT('Ctrl Pts',(4.44115490702077,3.93307864587641,18.657544089133));
#16035=CARTESIAN_POINT('Ctrl Pts',(4.47035390021833,3.9330837738788,18.6590295629144));
#16036=CARTESIAN_POINT('Ctrl Pts',(4.49953707546216,3.93276418693331,18.6605150366957));
#16037=CARTESIAN_POINT('Ctrl Pts',(4.61492982689533,3.93150051303031,18.6663887260862));
#16038=CARTESIAN_POINT('Ctrl Pts',(4.7304591003676,3.92515175568444,18.6722624154768));
#16039=CARTESIAN_POINT('Ctrl Pts',(4.84564001121418,3.91369837962824,18.6781361048673));
#16040=CARTESIAN_POINT('Ctrl Pts',(4.96067221268433,3.9022597909565,18.684002210773));
#16041=CARTESIAN_POINT('Ctrl Pts',(5.0753565386091,3.88572973050952,18.6898683166788));
#16042=CARTESIAN_POINT('Ctrl Pts',(5.18920777737616,3.86414065993848,18.6957344225845));
#16043=CARTESIAN_POINT('Ctrl Pts',(5.30294243392468,3.84257369630075,18.7015945216725));
#16044=CARTESIAN_POINT('Ctrl Pts',(5.41584529664469,3.81595810322179,18.7074546207605));
#16045=CARTESIAN_POINT('Ctrl Pts',(5.52743662036568,3.78437809734187,18.7133147198485));
#16046=CARTESIAN_POINT('Ctrl Pts',(5.6430539044671,3.75165875689501,18.7193862379426));
#16047=CARTESIAN_POINT('Ctrl Pts',(5.7572627786953,3.71361007580449,18.7254577560367));
#16048=CARTESIAN_POINT('Ctrl Pts',(5.86954122754744,3.67038365568536,18.7315292741308));
#16049=CARTESIAN_POINT('Ctrl Pts',(5.97778542200087,3.6287103953871,18.7373826377275));
#16050=CARTESIAN_POINT('Ctrl Pts',(6.08423510851336,3.58222523438231,18.7432360013243));
#16051=CARTESIAN_POINT('Ctrl Pts',(6.18843909745943,3.53111440616699,18.749089364921));
#16052=CARTESIAN_POINT('Ctrl Pts',(6.2926274405271,3.48001125207059,18.7549418496548));
#16053=CARTESIAN_POINT('Ctrl Pts',(6.39457038564771,3.42428399363418,18.7607943343887));
#16054=CARTESIAN_POINT('Ctrl Pts',(6.49383903004364,3.36416598780318,18.7666468191226));
#16055=CARTESIAN_POINT('Ctrl Pts',(6.59311677604133,3.30404246995829,18.7724998404507));
#16056=CARTESIAN_POINT('Ctrl Pts',(6.68971938047393,3.23952761847101,18.7783528617788));
#16057=CARTESIAN_POINT('Ctrl Pts',(6.78324535799057,3.1708991270913,18.784205883107));
#16058=CARTESIAN_POINT('Ctrl Pts',(6.87680252822683,3.10224774678441,18.7900608565308));
#16059=CARTESIAN_POINT('Ctrl Pts',(6.96728069825453,3.0294802427534,18.7959158299545));
#16060=CARTESIAN_POINT('Ctrl Pts',(7.05431057604661,2.95291528792143,18.8017708033783));
#16061=CARTESIAN_POINT('Ctrl Pts',(7.14143909102679,2.87626355654737,18.8076324126624));
#16062=CARTESIAN_POINT('Ctrl Pts',(7.2251112028821,2.79580605704661,18.8134940219466));
#16063=CARTESIAN_POINT('Ctrl Pts',(7.30499362401849,2.71189916322325,18.8193556312307));
#16064=CARTESIAN_POINT('Ctrl Pts',(7.38492991045813,2.62793569036514,18.825221193041));
#16065=CARTESIAN_POINT('Ctrl Pts',(7.46107114709653,2.54051850246574,18.8310867548513));
#16066=CARTESIAN_POINT('Ctrl Pts',(7.53312469151333,2.4500366139045,18.8369523166616));
#16067=CARTESIAN_POINT('Ctrl Pts',(7.60528359588407,2.35942241863041,18.8428264553619));
#16068=CARTESIAN_POINT('Ctrl Pts',(7.67334263714126,2.26573491202981,18.8487005940622));
#16069=CARTESIAN_POINT('Ctrl Pts',(7.73705273843312,2.16939162717199,18.8545747327625));
#16070=CARTESIAN_POINT('Ctrl Pts',(7.75316398297845,2.14502798324159,18.8560602065441));
#16071=CARTESIAN_POINT('Ctrl Pts',(7.7689973440063,2.12049462006162,18.8575456803257));
#16072=CARTESIAN_POINT('Ctrl Pts',(7.78454926945208,2.09579851777062,18.8590311541073));
#16073=CARTESIAN_POINT('Ctrl Pts',(7.84764214276654,1.99560847643847,18.8650575981925));
#16074=CARTESIAN_POINT('Ctrl Pts',(7.90630062493316,1.89241860175928,18.8710840422777));
#16075=CARTESIAN_POINT('Ctrl Pts',(7.96023592199444,1.78664688751461,18.8771104863629));
#16076=CARTESIAN_POINT('Ctrl Pts',(8.01409026531018,1.68103393046431,18.8831278851058));
#16077=CARTESIAN_POINT('Ctrl Pts',(8.06323536030736,1.57284718606672,18.8891452838487));
#16078=CARTESIAN_POINT('Ctrl Pts',(8.10742607641088,1.46253280366693,18.8951626825916));
#16079=CARTESIAN_POINT('Ctrl Pts',(8.15373732803705,1.34692487576338,18.9014688322061));
#16080=CARTESIAN_POINT('Ctrl Pts',(8.19460665858368,1.22898037754779,18.9077749818206));
#16081=CARTESIAN_POINT('Ctrl Pts',(8.22980582173832,1.10924254845737,18.914081131435));
#16082=CARTESIAN_POINT('Ctrl Pts',(8.26330090637412,0.995301523727039,18.9200819847546));
#16083=CARTESIAN_POINT('Ctrl Pts',(8.29166179065473,0.879737151538623,18.9260828380741));
#16084=CARTESIAN_POINT('Ctrl Pts',(8.31474103369602,0.763037832375923,18.9320836913937));
#16085=CARTESIAN_POINT('Ctrl Pts',(8.33780142356753,0.646433843552852,18.9380796426848));
#16086=CARTESIAN_POINT('Ctrl Pts',(8.35558868569572,0.528697128874555,18.9440755939759));
#16087=CARTESIAN_POINT('Ctrl Pts',(8.36800575363701,0.410329204298241,18.9500715452669));
#16088=CARTESIAN_POINT('Ctrl Pts',(8.38041353140312,0.292049839981025,18.9560630105201));
#16089=CARTESIAN_POINT('Ctrl Pts',(8.38745907960768,0.173140588104466,18.9620544757732));
#16090=CARTESIAN_POINT('Ctrl Pts',(8.38909685992391,0.0541105422630869,
18.9680459410264));
#16091=CARTESIAN_POINT('Ctrl Pts',(8.38935112641114,0.0356310481993439,
18.968976120006));
#16092=CARTESIAN_POINT('Ctrl Pts',(8.389475152377,0.0171486531632183,18.9699062989855));
#16093=CARTESIAN_POINT('Ctrl Pts',(8.38946887973726,-0.00133472821663341,
18.9708364779651));
#16094=CARTESIAN_POINT('',(8.39185523779378,-0.000723473480808207,16.4708361660978));
#16095=CARTESIAN_POINT('Ctrl Pts',(8.38946903862512,-0.000729169072716852,
16.4708364779651));
#16096=CARTESIAN_POINT('Ctrl Pts',(8.38946175098302,-0.0400373309035612,
16.4728369003659));
#16097=CARTESIAN_POINT('Ctrl Pts',(8.38886518453448,-0.0793393664645754,
16.4748373227667));
#16098=CARTESIAN_POINT('Ctrl Pts',(8.38767979182206,-0.118623544857041,
16.4768377451675));
#16099=CARTESIAN_POINT('Ctrl Pts',(8.38419921262247,-0.23397071440906,16.4827114345581));
#16100=CARTESIAN_POINT('Ctrl Pts',(8.37563186558806,-0.349356676786783,
16.4885851239486));
#16101=CARTESIAN_POINT('Ctrl Pts',(8.36196753555699,-0.464296261488952,
16.4944588133392));
#16102=CARTESIAN_POINT('Ctrl Pts',(8.34832084745971,-0.579087448389105,
16.5003249192449));
#16103=CARTESIAN_POINT('Ctrl Pts',(8.32959031151523,-0.693432997207276,
16.5061910251507));
#16104=CARTESIAN_POINT('Ctrl Pts',(8.3058177061635,-0.80684840961582,16.5120571310564));
#16105=CARTESIAN_POINT('Ctrl Pts',(8.28206944365678,-0.920147686086943,
16.5179172301445));
#16106=CARTESIAN_POINT('Ctrl Pts',(8.25328946565947,-1.03251831869173,16.5237773292325));
#16107=CARTESIAN_POINT('Ctrl Pts',(8.21957119101511,-1.1434822689476,16.5296374283205));
#16108=CARTESIAN_POINT('Ctrl Pts',(8.18463643794527,-1.25844954537939,16.5357089464147));
#16109=CARTESIAN_POINT('Ctrl Pts',(8.14440038901463,-1.37190627480333,16.5417804645088));
#16110=CARTESIAN_POINT('Ctrl Pts',(8.09902464777767,-1.48333345093231,16.5478519826029));
#16111=CARTESIAN_POINT('Ctrl Pts',(8.05527929318676,-1.59075695957257,16.5537053461996));
#16112=CARTESIAN_POINT('Ctrl Pts',(8.00675740558003,-1.69629383642343,16.5595587097964));
#16113=CARTESIAN_POINT('Ctrl Pts',(7.95365385316226,-1.79949655341213,16.5654120733931));
#16114=CARTESIAN_POINT('Ctrl Pts',(7.90055827406422,-1.90268377486013,16.571264558127));
#16115=CARTESIAN_POINT('Ctrl Pts',(7.84288258698029,-2.00353716603874,16.5771170428609));
#16116=CARTESIAN_POINT('Ctrl Pts',(7.78086834664954,-2.10163238703154,16.5829695275948));
#16117=CARTESIAN_POINT('Ctrl Pts',(7.7188484204455,-2.19973660203915,16.588822548923));
#16118=CARTESIAN_POINT('Ctrl Pts',(7.6524893710108,-2.29508179491168,16.5946755702512));
#16119=CARTESIAN_POINT('Ctrl Pts',(7.58207655491009,-2.38727188997862,16.6005285915793));
#16120=CARTESIAN_POINT('Ctrl Pts',(7.51164025477536,-2.47949273222268,16.6063835650032));
#16121=CARTESIAN_POINT('Ctrl Pts',(7.43714775020153,-2.5685560560827,16.612238538427));
#16122=CARTESIAN_POINT('Ctrl Pts',(7.35892475080396,-2.65409876063656,16.6180935118508));
#16123=CARTESIAN_POINT('Ctrl Pts',(7.28061309568405,-2.73973841685837,16.623955121135));
#16124=CARTESIAN_POINT('Ctrl Pts',(7.19856278579147,-2.82184918457426,16.6298167304191));
#16125=CARTESIAN_POINT('Ctrl Pts',(7.11313653287923,-2.90010468502751,16.6356783397033));
#16126=CARTESIAN_POINT('Ctrl Pts',(7.02765267641722,-2.97841295373948,16.6415439015136));
#16127=CARTESIAN_POINT('Ctrl Pts',(6.93878865998304,-3.05286051407819,16.647409463324));
#16128=CARTESIAN_POINT('Ctrl Pts',(6.84693904892941,-3.12316225210835,16.6532750251343));
#16129=CARTESIAN_POINT('Ctrl Pts',(6.75495513121677,-3.19356678852219,16.6591491638346));
#16130=CARTESIAN_POINT('Ctrl Pts',(6.65997724365918,-3.25981316853829,16.665023302535));
#16131=CARTESIAN_POINT('Ctrl Pts',(6.56242762797238,-3.32166038370137,16.6708974412353));
#16132=CARTESIAN_POINT('Ctrl Pts',(6.53775892267483,-3.33730053475261,16.6723829150166));
#16133=CARTESIAN_POINT('Ctrl Pts',(6.51292586866964,-3.35265959262508,16.6738683887978));
#16134=CARTESIAN_POINT('Ctrl Pts',(6.48793551305559,-3.36773414002521,16.6753538625791));
#16135=CARTESIAN_POINT('Ctrl Pts',(6.38912152624024,-3.42734017969304,16.6812275519697));
#16136=CARTESIAN_POINT('Ctrl Pts',(6.28751735628548,-3.48269279839213,16.6871012413602));
#16137=CARTESIAN_POINT('Ctrl Pts',(6.18352515803437,-3.53352039669864,16.6929749307508));
#16138=CARTESIAN_POINT('Ctrl Pts',(6.07966722348089,-3.58428237180066,16.6988410366566));
#16139=CARTESIAN_POINT('Ctrl Pts',(5.97342775983422,-3.63053076501999,16.7047071425623));
#16140=CARTESIAN_POINT('Ctrl Pts',(5.8652365433307,-3.67203803195604,16.7105732484681));
#16141=CARTESIAN_POINT('Ctrl Pts',(5.75715611325451,-3.71350279597956,16.7164333475561));
#16142=CARTESIAN_POINT('Ctrl Pts',(5.64712828908232,-3.75023594331914,16.7222934466441));
#16143=CARTESIAN_POINT('Ctrl Pts',(5.5356054135459,-3.78205682535406,16.7281535457322));
#16144=CARTESIAN_POINT('Ctrl Pts',(5.42005904708462,-3.81502573221772,16.7342250638263));
#16145=CARTESIAN_POINT('Ctrl Pts',(5.30290812222079,-3.84272103666939,16.7402965819204));
#16146=CARTESIAN_POINT('Ctrl Pts',(5.18467637083413,-3.86499717719957,16.7463681000145));
#16147=CARTESIAN_POINT('Ctrl Pts',(5.0706927807632,-3.88647291819786,16.7522214636112));
#16148=CARTESIAN_POINT('Ctrl Pts',(4.95570513821216,-3.90291213998371,16.758074827208));
#16149=CARTESIAN_POINT('Ctrl Pts',(4.84019514443961,-3.91423598261409,16.7639281908047));
#16150=CARTESIAN_POINT('Ctrl Pts',(4.72470249410394,-3.92555812500761,16.7697806755387));
#16151=CARTESIAN_POINT('Ctrl Pts',(4.6086880595571,-3.93176637513343,16.7756331602726));
#16152=CARTESIAN_POINT('Ctrl Pts',(4.4926393660822,-3.9328336746297,16.7814856450065));
#16153=CARTESIAN_POINT('Ctrl Pts',(4.37658003250018,-3.93390107198301,16.7873386663346));
#16154=CARTESIAN_POINT('Ctrl Pts',(4.2604868468961,-3.92982657789509,16.7931916876628));
#16155=CARTESIAN_POINT('Ctrl Pts',(4.1448473292717,-3.92063526333841,16.799044708991));
#16156=CARTESIAN_POINT('Ctrl Pts',(4.02916924363496,-3.91144088330082,16.8048996824148));
#16157=CARTESIAN_POINT('Ctrl Pts',(3.91394553846898,-3.89712632209603,16.8107546558386));
#16158=CARTESIAN_POINT('Ctrl Pts',(3.79965790060827,-3.87776843560638,16.8166096292625));
#16159=CARTESIAN_POINT('Ctrl Pts',(3.68524073238977,-3.85838860943883,16.8224712385466));
#16160=CARTESIAN_POINT('Ctrl Pts',(3.57176215656407,-3.83395411830546,16.8283328478308));
#16161=CARTESIAN_POINT('Ctrl Pts',(3.45969306125265,-3.80459281871039,16.8341944571149));
#16162=CARTESIAN_POINT('Ctrl Pts',(3.34754839692717,-3.77521172057537,16.8400600189253));
#16163=CARTESIAN_POINT('Ctrl Pts',(3.23681549927388,-3.74089732076254,16.8459255807356));
#16164=CARTESIAN_POINT('Ctrl Pts',(3.12794784940035,-3.70182661265799,16.851791142546));
#16165=CARTESIAN_POINT('Ctrl Pts',(3.01892100832124,-3.66269877359551,16.8576652812463));
#16166=CARTESIAN_POINT('Ctrl Pts',(2.91176523916443,-3.61880090204656,16.8635394199466));
#16167=CARTESIAN_POINT('Ctrl Pts',(2.80691196447618,-3.57035715806244,16.8694135586469));
#16168=CARTESIAN_POINT('Ctrl Pts',(2.78039628305049,-3.5581065260591,16.8708990324282));
#16169=CARTESIAN_POINT('Ctrl Pts',(2.75402771143118,-3.54556540726136,16.8723845062095));
#16170=CARTESIAN_POINT('Ctrl Pts',(2.72781294149613,-3.5327378708543,16.8738699799907));
#16171=CARTESIAN_POINT('Ctrl Pts',(2.62415751654921,-3.48201670333726,16.8797436693813));
#16172=CARTESIAN_POINT('Ctrl Pts',(2.52256368980246,-3.42664510307157,16.8856173587718));
#16173=CARTESIAN_POINT('Ctrl Pts',(2.42347770034835,-3.36681376729678,16.8914910481624));
#16174=CARTESIAN_POINT('Ctrl Pts',(2.32451964021537,-3.30705967939739,16.8973571540682));
#16175=CARTESIAN_POINT('Ctrl Pts',(2.22806332878527,-3.24285751824533,16.9032232599739));
#16176=CARTESIAN_POINT('Ctrl Pts',(2.13453295918874,-3.1744450742008,16.9090893658797));
#16177=CARTESIAN_POINT('Ctrl Pts',(2.04109836349919,-3.10610268362746,16.9149494649677));
#16178=CARTESIAN_POINT('Ctrl Pts',(1.95058408157798,-3.03355882810684,16.9208095640558));
#16179=CARTESIAN_POINT('Ctrl Pts',(1.86338713317583,-2.95709568345064,16.9266696631438));
#16180=CARTESIAN_POINT('Ctrl Pts',(1.77304431780336,-2.87787392297555,16.9327411812379));
#16181=CARTESIAN_POINT('Ctrl Pts',(1.68626310554974,-2.7944449694587,16.938812699332));
#16182=CARTESIAN_POINT('Ctrl Pts',(1.60344973292686,-2.70717000862967,16.9448842174261));
#16183=CARTESIAN_POINT('Ctrl Pts',(1.52361191096514,-2.62303090689167,16.9507375810229));
#16184=CARTESIAN_POINT('Ctrl Pts',(1.44746200922122,-2.53531774700819,16.9565909446196));
#16185=CARTESIAN_POINT('Ctrl Pts',(1.37532742915778,-2.44439255560169,16.9624443082164));
#16186=CARTESIAN_POINT('Ctrl Pts',(1.30320367985882,-2.35348101630673,16.9682967929503));
#16187=CARTESIAN_POINT('Ctrl Pts',(1.23509431017858,-2.25935872800797,16.9741492776842));
#16188=CARTESIAN_POINT('Ctrl Pts',(1.1712863495637,-2.16242069343123,16.9800017624181));
#16189=CARTESIAN_POINT('Ctrl Pts',(1.10747253861552,-2.06547377093821,16.9858547837463));
#16190=CARTESIAN_POINT('Ctrl Pts',(1.04796114789175,-1.96571093407056,16.9917078050744));
#16191=CARTESIAN_POINT('Ctrl Pts',(0.992995399287234,-1.86355544092402,
16.9975608264026));
#16192=CARTESIAN_POINT('Ctrl Pts',(0.938011318544051,-1.76136587694766,
17.0034157998264));
#16193=CARTESIAN_POINT('Ctrl Pts',(0.887576090189599,-1.65678243353768,
17.0092707732503));
#16194=CARTESIAN_POINT('Ctrl Pts',(0.841886258637142,-1.55025154022579,
17.0151257466741));
#16195=CARTESIAN_POINT('Ctrl Pts',(0.796144643529277,-1.44359990782976,
17.0209873559582));
#16196=CARTESIAN_POINT('Ctrl Pts',(0.755159322920271,-1.33499680003379,
17.0268489652424));
#16197=CARTESIAN_POINT('Ctrl Pts',(0.719078130915673,-1.22490722004846,
17.0327105745265));
#16198=CARTESIAN_POINT('Ctrl Pts',(0.682972609098328,-1.11474340585084,
17.0385761363369));
#16199=CARTESIAN_POINT('Ctrl Pts',(0.651777911533777,-1.00309152050607,
17.0444416981472));
#16200=CARTESIAN_POINT('Ctrl Pts',(0.625591145712266,-0.890428577545389,
17.0503072599576));
#16201=CARTESIAN_POINT('Ctrl Pts',(0.599366088416401,-0.777600893729711,
17.0561813986579));
#16202=CARTESIAN_POINT('Ctrl Pts',(0.578163652735192,-0.663759606354293,
17.0620555373582));
#16203=CARTESIAN_POINT('Ctrl Pts',(0.562029353484096,-0.54938876246601,
17.0679296760586));
#16204=CARTESIAN_POINT('Ctrl Pts',(0.557949252597881,-0.520466243164526,
17.0694151498399));
#16205=CARTESIAN_POINT('Ctrl Pts',(0.554192999669724,-0.491509865733668,
17.0709006236212));
#16206=CARTESIAN_POINT('Ctrl Pts',(0.550760803062122,-0.46252745935487,
17.0723860974024));
#16207=CARTESIAN_POINT('Ctrl Pts',(0.537189606414729,-0.347928565046156,
17.078259786793));
#16208=CARTESIAN_POINT('Ctrl Pts',(0.528643816891126,-0.232541004059473,
17.0841334761836));
#16209=CARTESIAN_POINT('Ctrl Pts',(0.525205100560675,-0.116843133393246,
17.0900071655741));
#16210=CARTESIAN_POINT('Ctrl Pts',(0.52177082393606,-0.00129463954741409,
17.0958732714799));
#16211=CARTESIAN_POINT('Ctrl Pts',(0.523430519936596,0.114562958047589,
17.1017393773857));
#16212=CARTESIAN_POINT('Ctrl Pts',(0.530214330587271,0.23024429815942,17.1076054832914));
#16213=CARTESIAN_POINT('Ctrl Pts',(0.536991194702262,0.345807182052693,
17.1134655823795));
#16214=CARTESIAN_POINT('Ctrl Pts',(0.548881712651152,0.461193757478206,
17.1193256814675));
#16215=CARTESIAN_POINT('Ctrl Pts',(0.565863998068018,0.575917435432653,
17.1251857805555));
#16216=CARTESIAN_POINT('Ctrl Pts',(0.583458965599931,0.694780081961094,
17.1312572986496));
#16217=CARTESIAN_POINT('Ctrl Pts',(0.606520049384706,0.812930644802737,
17.1373288167438));
#16218=CARTESIAN_POINT('Ctrl Pts',(0.634963966896292,0.929831958009547,
17.1434003348379));
#16219=CARTESIAN_POINT('Ctrl Pts',(0.662385871719876,1.04253291360764,17.1492536984346));
#16220=CARTESIAN_POINT('Ctrl Pts',(0.694810342275373,1.15407241182042,17.1551070620314));
#16221=CARTESIAN_POINT('Ctrl Pts',(0.732110652197893,1.26397907655432,17.1609604256281));
#16222=CARTESIAN_POINT('Ctrl Pts',(0.769405361604394,1.37386923917234,17.166812910362));
#16223=CARTESIAN_POINT('Ctrl Pts',(0.811574321966307,1.48212666466751,17.1726653950959));
#16224=CARTESIAN_POINT('Ctrl Pts',(0.858441210786417,1.5882960252089,17.1785178798298));
#16225=CARTESIAN_POINT('Ctrl Pts',(0.905312396670987,1.69447512005519,17.184370901158));
#16226=CARTESIAN_POINT('Ctrl Pts',(0.956882200425629,1.79856539138962,17.1902239224862));
#16227=CARTESIAN_POINT('Ctrl Pts',(1.01292680785358,1.90013300570601,17.1960769438144));
#16228=CARTESIAN_POINT('Ctrl Pts',(1.06899010724043,2.00173449478324,17.2019319172382));
#16229=CARTESIAN_POINT('Ctrl Pts',(1.12953097844474,2.10081129231162,17.207786890662));
#16230=CARTESIAN_POINT('Ctrl Pts',(1.19428083182352,2.19695622678321,17.2136418640858));
#16231=CARTESIAN_POINT('Ctrl Pts',(1.25910407084427,2.29321012918863,17.21950347337));
#16232=CARTESIAN_POINT('Ctrl Pts',(1.32814558244219,2.38652519337785,17.2253650826541));
#16233=CARTESIAN_POINT('Ctrl Pts',(1.40109476304516,2.47652511052879,17.2312266919383));
#16234=CARTESIAN_POINT('Ctrl Pts',(1.47409313381637,2.56658571528485,17.2370922537486));
#16235=CARTESIAN_POINT('Ctrl Pts',(1.55100414698407,2.65332641340697,17.242957815559));
#16236=CARTESIAN_POINT('Ctrl Pts',(1.63147960722877,2.7364070111369,17.2488233773693));
#16237=CARTESIAN_POINT('Ctrl Pts',(1.71207274233427,2.81960909307758,17.2546975160696));
#16238=CARTESIAN_POINT('Ctrl Pts',(1.79624042741247,2.89914011079204,17.26057165477));
#16239=CARTESIAN_POINT('Ctrl Pts',(1.88360058794582,2.97469941131581,17.2664457934703));
#16240=CARTESIAN_POINT('Ctrl Pts',(1.90569254637927,2.99380712490334,17.2679312672516));
#16241=CARTESIAN_POINT('Ctrl Pts',(1.9279885171227,3.01266106132437,17.2694167410328));
#16242=CARTESIAN_POINT('Ctrl Pts',(1.95048203420881,3.03125680121655,17.2709022148141));
#16243=CARTESIAN_POINT('Ctrl Pts',(2.03942330959911,3.10478593481113,17.2767759042047));
#16244=CARTESIAN_POINT('Ctrl Pts',(2.13175162878624,3.17451972307133,17.2826495935952));
#16245=CARTESIAN_POINT('Ctrl Pts',(2.22710929658357,3.24013021947971,17.2885232829858));
#16246=CARTESIAN_POINT('Ctrl Pts',(2.32234384867323,3.30565600657334,17.2943893888916));
#16247=CARTESIAN_POINT('Ctrl Pts',(2.42059963407783,3.36706885657892,17.3002554947973));
#16248=CARTESIAN_POINT('Ctrl Pts',(2.52148514022352,3.42408032197601,17.3061216007031));
#16249=CARTESIAN_POINT('Ctrl Pts',(2.62226734089618,3.48103340835885,17.3119816997911));
#16250=CARTESIAN_POINT('Ctrl Pts',(2.72567354855922,3.53359387279992,17.3178417988791));
#16251=CARTESIAN_POINT('Ctrl Pts',(2.83128301384766,3.58151632205763,17.3237018979672));
#16252=CARTESIAN_POINT('Ctrl Pts',(2.94070262771,3.63116770395598,17.3297734160613));
#16253=CARTESIAN_POINT('Ctrl Pts',(3.05248710567141,3.67583983813406,17.3358449341554));
#16254=CARTESIAN_POINT('Ctrl Pts',(3.16613991472104,3.71531150478263,17.3419164522495));
#16255=CARTESIAN_POINT('Ctrl Pts',(3.27570908751243,3.75336492290354,17.3477698158462));
#16256=CARTESIAN_POINT('Ctrl Pts',(3.38701421701145,3.78658500868856,17.353623179443));
#16257=CARTESIAN_POINT('Ctrl Pts',(3.49959050262001,3.81482271383296,17.3594765430397));
#16258=CARTESIAN_POINT('Ctrl Pts',(3.61214988527817,3.84305617918098,17.3653290277736));
#16259=CARTESIAN_POINT('Ctrl Pts',(3.72597964392154,3.86630865087863,17.3711815125075));
#16260=CARTESIAN_POINT('Ctrl Pts',(3.84060157689801,3.88448145655621,17.3770339972414));
#16261=CARTESIAN_POINT('Ctrl Pts',(3.95523401916669,3.90265592843605,17.3828870185696));
#16262=CARTESIAN_POINT('Ctrl Pts',(4.07065837208287,3.91574974375606,17.3887400398978));
#16263=CARTESIAN_POINT('Ctrl Pts',(4.18638875014219,3.92371579007219,17.3945930612259));
#16264=CARTESIAN_POINT('Ctrl Pts',(4.3021577265176,3.93168449321862,17.4004480346498));
#16265=CARTESIAN_POINT('Ctrl Pts',(4.4182325190412,3.93452199832943,17.4063030080736));
#16266=CARTESIAN_POINT('Ctrl Pts',(4.5341253732997,3.93223327184222,17.4121579814974));
#16267=CARTESIAN_POINT('Ctrl Pts',(4.65014957722265,3.92994195137752,17.4180195907816));
#16268=CARTESIAN_POINT('Ctrl Pts',(4.76599101801497,3.92251281121624,17.4238812000657));
#16269=CARTESIAN_POINT('Ctrl Pts',(4.8811650992699,3.9100028533859,17.4297428093499));
#16270=CARTESIAN_POINT('Ctrl Pts',(4.99641684325361,3.89748445999913,17.4356083711602));
#16271=CARTESIAN_POINT('Ctrl Pts',(5.11099992429715,3.87987848954136,17.4414739329706));
#16272=CARTESIAN_POINT('Ctrl Pts',(5.22443971492151,3.85729311099999,17.4473394947809));
#16273=CARTESIAN_POINT('Ctrl Pts',(5.33804538234267,3.83467470709577,17.4532136334812));
#16274=CARTESIAN_POINT('Ctrl Pts',(5.45050402322474,3.8070624619667,17.4590877721816));
#16275=CARTESIAN_POINT('Ctrl Pts',(5.56135587029248,3.77461444899656,17.4649619108819));
#16276=CARTESIAN_POINT('Ctrl Pts',(5.58938849274594,3.76640887623419,17.4664473846632));
#16277=CARTESIAN_POINT('Ctrl Pts',(5.61731846126856,3.75789429531119,17.4679328584444));
#16278=CARTESIAN_POINT('Ctrl Pts',(5.64513855697309,3.74907374385224,17.4694183322257));
#16279=CARTESIAN_POINT('Ctrl Pts',(5.75514157624099,3.71419653485922,17.4752920216163));
#16280=CARTESIAN_POINT('Ctrl Pts',(5.86379148569802,3.6744156735816,17.4811657110068));
#16281=CARTESIAN_POINT('Ctrl Pts',(5.97061879934942,3.62985395116536,17.4870394003974));
#16282=CARTESIAN_POINT('Ctrl Pts',(6.07730818890302,3.58534976211912,17.4929055063032));
#16283=CARTESIAN_POINT('Ctrl Pts',(6.18217928446147,3.53607714469648,17.4987716122089));
#16284=CARTESIAN_POINT('Ctrl Pts',(6.28477745861988,3.48220871984125,17.5046377181147));
#16285=CARTESIAN_POINT('Ctrl Pts',(6.38727057355486,3.4283954555669,17.5104978172027));
#16286=CARTESIAN_POINT('Ctrl Pts',(6.48749503294883,3.36999593549452,17.5163579162907));
#16287=CARTESIAN_POINT('Ctrl Pts',(6.58501653870268,3.30723068860701,17.5222180153788));
#16288=CARTESIAN_POINT('Ctrl Pts',(6.68605639790208,3.24220101480216,17.5282895334729));
#16289=CARTESIAN_POINT('Ctrl Pts',(6.78419417148932,3.17248482959048,17.534361051567));
#16290=CARTESIAN_POINT('Ctrl Pts',(6.87897479145501,3.09837944819475,17.5404325696611));
#16291=CARTESIAN_POINT('Ctrl Pts',(6.97034986799851,3.02693673237615,17.5462859332579));
#16292=CARTESIAN_POINT('Ctrl Pts',(7.05860453609393,2.95141508308455,17.5521392968546));
#16293=CARTESIAN_POINT('Ctrl Pts',(7.14336157645623,2.87212427540636,17.5579926604514));
#16294=CARTESIAN_POINT('Ctrl Pts',(7.22810589083405,2.79284537297619,17.5638451451853));
#16295=CARTESIAN_POINT('Ctrl Pts',(7.30935332006476,2.70979871960462,17.5696976299192));
#16296=CARTESIAN_POINT('Ctrl Pts',(7.38676171131797,2.62333266066238,17.5755501146531));
#16297=CARTESIAN_POINT('Ctrl Pts',(7.4641771998814,2.53685867394338,17.5814031359812));
#16298=CARTESIAN_POINT('Ctrl Pts',(7.53775267516254,2.44696496624974,17.5872561573094));
#16299=CARTESIAN_POINT('Ctrl Pts',(7.60718514505177,2.35403429087964,17.5931091786376));
#16300=CARTESIAN_POINT('Ctrl Pts',(7.6766407720106,2.26107262133462,17.5989641520614));
#16301=CARTESIAN_POINT('Ctrl Pts',(7.74195039883708,2.16507230082249,17.6048191254852));
#16302=CARTESIAN_POINT('Ctrl Pts',(7.80285378256125,2.06644588555732,17.610674098909));
#16303=CARTESIAN_POINT('Ctrl Pts',(7.86382619244812,1.96770768991853,17.6165357081932));
#16304=CARTESIAN_POINT('Ctrl Pts',(7.92038217449507,1.86633781064922,17.6223973174773));
#16305=CARTESIAN_POINT('Ctrl Pts',(7.972306923632,1.762774359254,17.6282589267615));
#16306=CARTESIAN_POINT('Ctrl Pts',(8.02426668600853,1.65914107426309,17.6341244885718));
#16307=CARTESIAN_POINT('Ctrl Pts',(8.07158882890953,1.55331164806977,17.6399900503822));
#16308=CARTESIAN_POINT('Ctrl Pts',(8.11410694751338,1.44574355330601,17.6458556121925));
#16309=CARTESIAN_POINT('Ctrl Pts',(8.15668723803494,1.33801816760475,17.6517297508928));
#16310=CARTESIAN_POINT('Ctrl Pts',(8.19444935059135,1.2285494284808,17.6576038895932));
#16311=CARTESIAN_POINT('Ctrl Pts',(8.22727687127466,1.11780937506817,17.6634780282935));
#16312=CARTESIAN_POINT('Ctrl Pts',(8.23557841534231,1.08980502340459,17.6649635020748));
#16313=CARTESIAN_POINT('Ctrl Pts',(8.24356464775546,1.06171941638178,17.6664489758561));
#16314=CARTESIAN_POINT('Ctrl Pts',(8.25123420762655,1.03356026681257,17.6679344496374));
#16315=CARTESIAN_POINT('Ctrl Pts',(8.28989601302147,0.891611631032941,17.6754226366021));
#16316=CARTESIAN_POINT('Ctrl Pts',(8.32061081407376,0.747412562252989,17.6829108235669));
#16317=CARTESIAN_POINT('Ctrl Pts',(8.34316333708667,0.601744925806739,17.6903990105316));
#16318=CARTESIAN_POINT('Ctrl Pts',(8.36531050155811,0.458695516182177,17.6977526049923));
#16319=CARTESIAN_POINT('Ctrl Pts',(8.37958618475085,0.314229690772142,17.7051061994529));
#16320=CARTESIAN_POINT('Ctrl Pts',(8.38583177918674,0.169109385552526,17.7124597939135));
#16321=CARTESIAN_POINT('Ctrl Pts',(8.38820328930776,0.114005859999161,17.7152520219181));
#16322=CARTESIAN_POINT('Ctrl Pts',(8.38941749976572,0.0588082088045671,
17.7180442499227));
#16323=CARTESIAN_POINT('Ctrl Pts',(8.38946749588772,0.00355905287639466,
17.7208364779273));
#16324=CARTESIAN_POINT('',(8.38850524290982,-0.00312121602759044,15.2208368624451));
#16325=CARTESIAN_POINT('Ctrl Pts',(8.38601483107283,-0.00313894636463737,
15.2208378571301));
#16326=CARTESIAN_POINT('Ctrl Pts',(8.38918468738173,-0.431668147948809,
15.2424722516526));
#16327=CARTESIAN_POINT('Ctrl Pts',(8.12699578129889,-2.16714071178393,15.3302786853124));
#16328=CARTESIAN_POINT('Ctrl Pts',(5.59178989108131,-4.50829591265121,15.4842571581091));
#16329=CARTESIAN_POINT('Ctrl Pts',(1.28358086881555,-3.3980090573042,15.6827732755208));
#16330=CARTESIAN_POINT('Ctrl Pts',(-0.118957460370758,0.824109855735944,
15.8812893929325));
#16331=CARTESIAN_POINT('Ctrl Pts',(2.66859282628323,4.29152463912485,16.0798055103441));
#16332=CARTESIAN_POINT('Ctrl Pts',(7.04885138217592,3.83350581901215,16.2763209308836));
#16333=CARTESIAN_POINT('Ctrl Pts',(8.39253775623418,1.26226890306036,16.4066643122856));
#16334=CARTESIAN_POINT('Ctrl Pts',(8.3957692530271,-0.000714131161949812,
16.4708356545507));
#16335=CARTESIAN_POINT('',(8.38779848858743,0.00244925732166319,13.97083596737));
#16336=CARTESIAN_POINT('Ctrl Pts',(8.3894683492347,0.00244017049050211,
13.970836477965));
#16337=CARTESIAN_POINT('Ctrl Pts',(8.38954098951505,-0.114639422405106,
13.9767346357567));
#16338=CARTESIAN_POINT('Ctrl Pts',(8.38438136405865,-0.231739061658239,
13.9826327935484));
#16339=CARTESIAN_POINT('Ctrl Pts',(8.37401070864951,-0.348363019306455,
13.9885309513401));
#16340=CARTESIAN_POINT('Ctrl Pts',(8.36363894134007,-0.464999480910128,
13.9944297415087));
#16341=CARTESIAN_POINT('Ctrl Pts',(8.34805506770137,-0.581159756869867,
14.0003285316773));
#16342=CARTESIAN_POINT('Ctrl Pts',(8.32733222229877,-0.696353169424395,
14.0062273218459));
#16343=CARTESIAN_POINT('Ctrl Pts',(8.3066024391392,-0.811585147334493,14.0121280868579));
#16344=CARTESIAN_POINT('Ctrl Pts',(8.28073033206417,-0.925849220138849,
14.0180288518698));
#16345=CARTESIAN_POINT('Ctrl Pts',(8.24984005631773,-1.03866541048662,14.0239296168817));
#16346=CARTESIAN_POINT('Ctrl Pts',(8.21891015066804,-1.15162633553168,14.0298379521319));
#16347=CARTESIAN_POINT('Ctrl Pts',(8.18294932296882,-1.26313527712322,14.0357462873821));
#16348=CARTESIAN_POINT('Ctrl Pts',(8.14213163441006,-1.37272747779112,14.0416546226322));
#16349=CARTESIAN_POINT('Ctrl Pts',(8.10128765710371,-1.48239026162536,14.0475667631624));
#16350=CARTESIAN_POINT('Ctrl Pts',(8.0555807437954,-1.59013347291978,14.0534789036926));
#16351=CARTESIAN_POINT('Ctrl Pts',(8.00523238555656,-1.69551413654383,14.0593910442228));
#16352=CARTESIAN_POINT('Ctrl Pts',(7.95479113524709,-1.80108922613115,14.0653140925758));
#16353=CARTESIAN_POINT('Ctrl Pts',(7.89969151625316,-1.90429269979155,14.0712371409289));
#16354=CARTESIAN_POINT('Ctrl Pts',(7.8402004918376,-2.00470718808871,14.077160189282));
#16355=CARTESIAN_POINT('Ctrl Pts',(7.78166363993183,-2.10351113521166,14.0829882382639));
#16356=CARTESIAN_POINT('Ctrl Pts',(7.71887548050658,-2.19961464379018,14.0888162872457));
#16357=CARTESIAN_POINT('Ctrl Pts',(7.65212862443776,-2.29265113866306,14.0946443362276));
#16358=CARTESIAN_POINT('Ctrl Pts',(7.58485906277745,-2.38641621760638,14.1005180256182));
#16359=CARTESIAN_POINT('Ctrl Pts',(7.51334717067436,-2.47737427957379,14.1063917150087));
#16360=CARTESIAN_POINT('Ctrl Pts',(7.43785527256591,-2.56511705914385,14.1122654043993));
#16361=CARTESIAN_POINT('Ctrl Pts',(7.36246084159014,-2.65274655454233,14.118131510305));
#16362=CARTESIAN_POINT('Ctrl Pts',(7.28309689051695,-2.73716871266051,14.1239976162108));
#16363=CARTESIAN_POINT('Ctrl Pts',(7.20006850960705,-2.8180048462919,14.1298637221165));
#16364=CARTESIAN_POINT('Ctrl Pts',(7.11712514870153,-2.89875820475219,14.1357238212046));
#16365=CARTESIAN_POINT('Ctrl Pts',(7.03052511591363,-2.97593255623383,14.1415839202926));
#16366=CARTESIAN_POINT('Ctrl Pts',(6.9406127438482,-3.04918339684949,14.1474440193806));
#16367=CARTESIAN_POINT('Ctrl Pts',(6.84745653852143,-3.12507696068279,14.1535155374747));
#16368=CARTESIAN_POINT('Ctrl Pts',(6.75074477271872,-3.19675822350967,14.1595870555688));
#16369=CARTESIAN_POINT('Ctrl Pts',(6.6509012207872,-3.26388674658733,14.1656585736629));
#16370=CARTESIAN_POINT('Ctrl Pts',(6.5546451274696,-3.328603288183,14.1715119372597));
#16371=CARTESIAN_POINT('Ctrl Pts',(6.45547880226965,-3.38908837641713,14.1773653008564));
#16372=CARTESIAN_POINT('Ctrl Pts',(6.35381372451471,-3.44507944747599,14.1832186644532));
#16373=CARTESIAN_POINT('Ctrl Pts',(6.25216391142903,-3.50106211166396,14.1890711491871));
#16374=CARTESIAN_POINT('Ctrl Pts',(6.1480164535795,-3.55255190110159,14.194923633921));
#16375=CARTESIAN_POINT('Ctrl Pts',(6.04180862524011,-3.59933155036147,14.2007761186549));
#16376=CARTESIAN_POINT('Ctrl Pts',(5.93559105906875,-3.64611548868715,14.2066291399831));
#16377=CARTESIAN_POINT('Ctrl Pts',(5.82731312499075,-3.68818826180218,14.2124821613113));
#16378=CARTESIAN_POINT('Ctrl Pts',(5.71743266543329,-3.72538050436888,14.2183351826394));
#16379=CARTESIAN_POINT('Ctrl Pts',(5.60751555862045,-3.76258515126677,14.2241901560633));
#16380=CARTESIAN_POINT('Ctrl Pts',(5.49599525467625,-3.79490589851833,14.2300451294871));
#16381=CARTESIAN_POINT('Ctrl Pts',(5.38334467341555,-3.82222326440158,14.2359001029109));
#16382=CARTESIAN_POINT('Ctrl Pts',(5.27056641719066,-3.84957159101021,14.2417617121951));
#16383=CARTESIAN_POINT('Ctrl Pts',(5.15665572853512,-3.87190512047574,14.2476233214792));
#16384=CARTESIAN_POINT('Ctrl Pts',(5.04209573263636,-3.88915549373256,14.2534849307634));
#16385=CARTESIAN_POINT('Ctrl Pts',(4.92745848809112,-3.90641749904273,14.2593504925737));
#16386=CARTESIAN_POINT('Ctrl Pts',(4.81217147432536,-3.91858947974188,14.2652160543841));
#16387=CARTESIAN_POINT('Ctrl Pts',(4.69672121446205,-3.92565509494713,14.2710816161944));
#16388=CARTESIAN_POINT('Ctrl Pts',(4.58110213800274,-3.93273104181478,14.2769557548947));
#16389=CARTESIAN_POINT('Ctrl Pts',(4.46531975054712,-3.93468571446805,14.2828298935951));
#16390=CARTESIAN_POINT('Ctrl Pts',(4.34985892161933,-3.93155481566005,14.2887040322954));
#16391=CARTESIAN_POINT('Ctrl Pts',(4.32066076289567,-3.93076306246382,14.2901895060767));
#16392=CARTESIAN_POINT('Ctrl Pts',(4.29148313157325,-3.92964634388687,14.2916749798579));
#16393=CARTESIAN_POINT('Ctrl Pts',(4.26233378226808,-3.92820575784858,14.2931604536392));
#16394=CARTESIAN_POINT('Ctrl Pts',(4.14707478146079,-3.92250955840302,14.2990341430298));
#16395=CARTESIAN_POINT('Ctrl Pts',(4.03187473136373,-3.91172678479576,14.3049078324204));
#16396=CARTESIAN_POINT('Ctrl Pts',(3.91721890918676,-3.89585654574209,14.3107815218109));
#16397=CARTESIAN_POINT('Ctrl Pts',(3.8027111184477,-3.88000679665798,14.3166476277167));
#16398=CARTESIAN_POINT('Ctrl Pts',(3.68874656379495,-3.85908270064171,14.3225137336224));
#16399=CARTESIAN_POINT('Ctrl Pts',(3.57580885139183,-3.8331353374971,14.3283798395282));
#16400=CARTESIAN_POINT('Ctrl Pts',(3.46298678576733,-3.80721454412178,14.3342399386162));
#16401=CARTESIAN_POINT('Ctrl Pts',(3.35118987118612,-3.77628080694593,14.3401000377043));
#16402=CARTESIAN_POINT('Ctrl Pts',(3.24089426294817,-3.74043671252554,14.3459601367923));
#16403=CARTESIAN_POINT('Ctrl Pts',(3.12661944078964,-3.70329944495197,14.3520316548864));
#16404=CARTESIAN_POINT('Ctrl Pts',(3.01395674507062,-3.66089088357044,14.3581031729805));
#16405=CARTESIAN_POINT('Ctrl Pts',(2.90342198124228,-3.61338257420991,14.3641746910746));
#16406=CARTESIAN_POINT('Ctrl Pts',(2.79685881981555,-3.56758127637244,14.3700280546714));
#16407=CARTESIAN_POINT('Ctrl Pts',(2.69227371747094,-3.51704057673436,14.3758814182681));
#16408=CARTESIAN_POINT('Ctrl Pts',(2.59011037549847,-3.46196390626275,14.3817347818649));
#16409=CARTESIAN_POINT('Ctrl Pts',(2.48796237300794,-3.40689550536784,14.3875872665988));
#16410=CARTESIAN_POINT('Ctrl Pts',(2.38823577144503,-3.3472926838444,14.3934397513327));
#16411=CARTESIAN_POINT('Ctrl Pts',(2.29135019119615,-3.28340510504164,14.3992922360666));
#16412=CARTESIAN_POINT('Ctrl Pts',(2.19445572784055,-3.21951166860579,14.4051452573948));
#16413=CARTESIAN_POINT('Ctrl Pts',(2.10040314854254,-3.15133292138124,14.4109982787229));
#16414=CARTESIAN_POINT('Ctrl Pts',(2.00958297305876,-3.07916177739198,14.4168513000511));
#16415=CARTESIAN_POINT('Ctrl Pts',(1.91873250729247,-3.00696656293238,14.4227062734749));
#16416=CARTESIAN_POINT('Ctrl Pts',(1.83111691231099,-2.93077656089362,14.4285612468987));
#16417=CARTESIAN_POINT('Ctrl Pts',(1.7470929638725,-2.85092439732934,14.4344162203226));
#16418=CARTESIAN_POINT('Ctrl Pts',(1.66297378508079,-2.77098173159415,14.4402778296067));
#16419=CARTESIAN_POINT('Ctrl Pts',(1.58245467728933,-2.687368904774,14.4461394388909));
#16420=CARTESIAN_POINT('Ctrl Pts',(1.50585498991652,-2.60045483265542,14.452001048175));
#16421=CARTESIAN_POINT('Ctrl Pts',(1.42920365081196,-2.51348215373971,14.4578666099854));
#16422=CARTESIAN_POINT('Ctrl Pts',(1.35647725325612,-2.42320411789621,14.4637321717957));
#16423=CARTESIAN_POINT('Ctrl Pts',(1.28795327743338,-2.33002069577498,14.4695977336061));
#16424=CARTESIAN_POINT('Ctrl Pts',(1.21932910275137,-2.23670101663586,14.4754718723064));
#16425=CARTESIAN_POINT('Ctrl Pts',(1.15491984253505,-2.1404678145249,14.4813460110067));
#16426=CARTESIAN_POINT('Ctrl Pts',(1.09495834786145,-2.04174788391013,14.4872201497071));
#16427=CARTESIAN_POINT('Ctrl Pts',(1.07979506473727,-2.01678322507266,14.4887056234884));
#16428=CARTESIAN_POINT('Ctrl Pts',(1.06491598067201,-1.99165964874789,14.4901910972696));
#16429=CARTESIAN_POINT('Ctrl Pts',(1.05032437692652,-1.96638426639306,14.4916765710509));
#16430=CARTESIAN_POINT('Ctrl Pts',(0.99262793745291,-1.86644325965767,14.4975502604415));
#16431=CARTESIAN_POINT('Ctrl Pts',(0.939237743903457,-1.76379430943517,
14.503423949832));
#16432=CARTESIAN_POINT('Ctrl Pts',(0.89041761862265,-1.65884471479919,14.5092976392226));
#16433=CARTESIAN_POINT('Ctrl Pts',(0.841660524710002,-1.5540306199494,14.5151637451284));
#16434=CARTESIAN_POINT('Ctrl Pts',(0.797461937793022,-1.44692215891174,
14.5210298510341));
#16435=CARTESIAN_POINT('Ctrl Pts',(0.75804110261241,-1.33795340058767,14.5268959569399));
#16436=CARTESIAN_POINT('Ctrl Pts',(0.718660633864798,-1.22909622488385,
14.5327560560279));
#16437=CARTESIAN_POINT('Ctrl Pts',(0.684048325261163,-1.11838292713387,
14.538616155116));
#16438=CARTESIAN_POINT('Ctrl Pts',(0.6543761008303,-1.00626923752046,14.544476254204));
#16439=CARTESIAN_POINT('Ctrl Pts',(0.62363337023519,-0.890110741758223,
14.5505477722981));
#16440=CARTESIAN_POINT('Ctrl Pts',(0.59819409826764,-0.772449309985185,
14.5566192903922));
#16441=CARTESIAN_POINT('Ctrl Pts',(0.578193756662317,-0.65381137419503,
14.5626908084863));
#16442=CARTESIAN_POINT('Ctrl Pts',(0.558912043314759,-0.53943619425096,
14.5685441720831));
#16443=CARTESIAN_POINT('Ctrl Pts',(0.544685211133058,-0.424153918083215,
14.5743975356798));
#16444=CARTESIAN_POINT('Ctrl Pts',(0.535582850168585,-0.308447673229725,
14.5802508992765));
#16445=CARTESIAN_POINT('Ctrl Pts',(0.52648185589297,-0.192758801279415,
14.5861033840104));
#16446=CARTESIAN_POINT('Ctrl Pts',(0.522503835326865,-0.0766464989801795,
14.5919558687443));
#16447=CARTESIAN_POINT('Ctrl Pts',(0.523666474601265,0.0394012784882832,
14.5978083534783));
#16448=CARTESIAN_POINT('Ctrl Pts',(0.524829220474074,0.155459695979616,
14.6036613748064));
#16449=CARTESIAN_POINT('Ctrl Pts',(0.53113355900714,0.271453163732685,14.6095143961346));
#16450=CARTESIAN_POINT('Ctrl Pts',(0.542545056721865,0.386894733453194,
14.6153674174627));
#16451=CARTESIAN_POINT('Ctrl Pts',(0.553960360391488,0.502374805166933,
14.6212223908866));
#16452=CARTESIAN_POINT('Ctrl Pts',(0.570486169631157,0.617302201916618,
14.6270773643104));
#16453=CARTESIAN_POINT('Ctrl Pts',(0.5920363876896,0.731196802485668,14.6329323377342));
#16454=CARTESIAN_POINT('Ctrl Pts',(0.613611030152174,0.845220487955169,
14.6387939470184));
#16455=CARTESIAN_POINT('Ctrl Pts',(0.640221370504495,0.958208634743751,
14.6446555563025));
#16456=CARTESIAN_POINT('Ctrl Pts',(0.671730528273218,1.0696928982725,14.6505171655867));
#16457=CARTESIAN_POINT('Ctrl Pts',(0.703260932898381,1.18125233645872,14.656382727397));
#16458=CARTESIAN_POINT('Ctrl Pts',(0.73969660303148,1.29130548088959,14.6622482892074));
#16459=CARTESIAN_POINT('Ctrl Pts',(0.780851864843685,1.39940233489516,14.6681138510177));
#16460=CARTESIAN_POINT('Ctrl Pts',(0.822067305742706,1.50765725301394,14.673987989718));
#16461=CARTESIAN_POINT('Ctrl Pts',(0.868015948077903,1.61394979394547,14.6798621284184));
#16462=CARTESIAN_POINT('Ctrl Pts',(0.918465383892158,1.71785292176214,14.6857362671187));
#16463=CARTESIAN_POINT('Ctrl Pts',(0.931223222616284,1.74412832655552,14.6872217409));
#16464=CARTESIAN_POINT('Ctrl Pts',(0.9442686679649,1.77025106733085,14.6887072146812));
#16465=CARTESIAN_POINT('Ctrl Pts',(0.957597522927404,1.79621453163029,14.6901926884625));
#16466=CARTESIAN_POINT('Ctrl Pts',(1.01030094655475,1.89887627276679,14.6960663778531));
#16467=CARTESIAN_POINT('Ctrl Pts',(1.06761433321634,1.99938744358087,14.7019400672437));
#16468=CARTESIAN_POINT('Ctrl Pts',(1.1293384469066,2.09730555138455,14.7078137566342));
#16469=CARTESIAN_POINT('Ctrl Pts',(1.19098286896731,2.19509723771196,14.71367986254));
#16470=CARTESIAN_POINT('Ctrl Pts',(1.25702647493838,2.29030217257155,14.7195459684457));
#16471=CARTESIAN_POINT('Ctrl Pts',(1.32722336797488,2.38250081000735,14.7254120743515));
#16472=CARTESIAN_POINT('Ctrl Pts',(1.39734838028703,2.47460503721279,14.7312721734395));
#16473=CARTESIAN_POINT('Ctrl Pts',(1.47161797148397,2.56370876344736,14.7371322725275));
#16474=CARTESIAN_POINT('Ctrl Pts',(1.54974238956812,2.64942046393402,14.7429923716155));
#16475=CARTESIAN_POINT('Ctrl Pts',(1.63068535842668,2.73822444703484,14.7490638897097));
#16476=CARTESIAN_POINT('Ctrl Pts',(1.71576631157221,2.82338664813948,14.7551354078038));
#16477=CARTESIAN_POINT('Ctrl Pts',(1.80461632458522,2.90450784549555,14.7612069258979));
#16478=CARTESIAN_POINT('Ctrl Pts',(1.89027388562354,2.98271429340019,14.7670602894946));
#16479=CARTESIAN_POINT('Ctrl Pts',(1.97943398589382,3.05716483048471,14.7729136530914));
#16480=CARTESIAN_POINT('Ctrl Pts',(2.07172837496346,3.12753907164953,14.7787670166882));
#16481=CARTESIAN_POINT('Ctrl Pts',(2.1640089063411,3.1979027463588,14.7846195014221));
#16482=CARTESIAN_POINT('Ctrl Pts',(2.25942246233626,3.26419109167836,14.790471986156));
#16483=CARTESIAN_POINT('Ctrl Pts',(2.35756859820218,3.32612472066967,14.7963244708899));
#16484=CARTESIAN_POINT('Ctrl Pts',(2.45572373275119,3.38806402814333,14.8021774922181));
#16485=CARTESIAN_POINT('Ctrl Pts',(2.55661159580834,3.44564760508657,14.8080305135462));
#16486=CARTESIAN_POINT('Ctrl Pts',(2.65980433418451,3.49864040691994,14.8138835348744));
#16487=CARTESIAN_POINT('Ctrl Pts',(2.76303148933148,3.55165088287598,14.8197385082983));
#16488=CARTESIAN_POINT('Ctrl Pts',(2.86856468104479,3.60006735054383,14.8255934817221));
#16489=CARTESIAN_POINT('Ctrl Pts',(2.97595378583079,3.64370187942126,14.8314484551459));
#16490=CARTESIAN_POINT('Ctrl Pts',(3.08346460237365,3.68738586243261,14.8373100644301));
#16491=CARTESIAN_POINT('Ctrl Pts',(3.19283514735745,3.72627693362311,14.8431716737142));
#16492=CARTESIAN_POINT('Ctrl Pts',(3.30359766295086,3.76023622067798,14.8490332829984));
#16493=CARTESIAN_POINT('Ctrl Pts',(3.41443486652191,3.79421840672948,14.8548988448087));
#16494=CARTESIAN_POINT('Ctrl Pts',(3.52666551071602,3.82326208351088,14.8607644066191));
#16495=CARTESIAN_POINT('Ctrl Pts',(3.63981080425168,3.84727932672286,14.8666299684294));
#16496=CARTESIAN_POINT('Ctrl Pts',(3.75312154395694,3.87133168903498,14.8725041071297));
#16497=CARTESIAN_POINT('Ctrl Pts',(3.86734919622866,3.89034288170052,14.8783782458301));
#16498=CARTESIAN_POINT('Ctrl Pts',(3.98200892886182,3.90427669871167,14.8842523845304));
#16499=CARTESIAN_POINT('Ctrl Pts',(4.01100450341064,3.90780033356254,14.8857378583117));
#16500=CARTESIAN_POINT('Ctrl Pts',(4.04002770747369,3.91099952969375,14.887223332093));
#16501=CARTESIAN_POINT('Ctrl Pts',(4.06907070931136,3.91387422920998,14.8887088058742));
#16502=CARTESIAN_POINT('Ctrl Pts',(4.18390920320717,3.92524103504815,14.8945824952648));
#16503=CARTESIAN_POINT('Ctrl Pts',(4.29943966079135,3.93156820814744,14.9004561846554));
#16504=CARTESIAN_POINT('Ctrl Pts',(4.41518224425229,3.93278328859207,14.906329874046));
#16505=CARTESIAN_POINT('Ctrl Pts',(4.53077539316417,3.93399680025369,14.9121959799517));
#16506=CARTESIAN_POINT('Ctrl Pts',(4.64657971395735,3.93011134058083,14.9180620858574));
#16507=CARTESIAN_POINT('Ctrl Pts',(4.7621093558544,3.92110609876886,14.9239281917632));
#16508=CARTESIAN_POINT('Ctrl Pts',(4.87752069687014,3.91211007820977,14.9297882908512));
#16509=CARTESIAN_POINT('Ctrl Pts',(4.99265750900708,3.89800473537631,14.9356483899392));
#16510=CARTESIAN_POINT('Ctrl Pts',(5.10703371360898,3.87882130184036,14.9415084890273));
#16511=CARTESIAN_POINT('Ctrl Pts',(5.22553635073912,3.85894577378684,14.9475800071214));
#16512=CARTESIAN_POINT('Ctrl Pts',(5.34322201051843,3.83361882040822,14.9536515252155));
#16513=CARTESIAN_POINT('Ctrl Pts',(5.45955522633896,3.80293402988025,14.9597230433096));
#16514=CARTESIAN_POINT('Ctrl Pts',(5.57170849674366,3.77335176839867,14.9655764069064));
#16515=CARTESIAN_POINT('Ctrl Pts',(5.68260440564314,3.73879018073727,14.9714297705031));
#16516=CARTESIAN_POINT('Ctrl Pts',(5.79177409886216,3.69938502681463,14.9772831340998));
#16517=CARTESIAN_POINT('Ctrl Pts',(5.90092740061891,3.65998578944331,14.9831356188337));
#16518=CARTESIAN_POINT('Ctrl Pts',(6.00835461355294,3.61574457207778,14.9889881035676));
#16519=CARTESIAN_POINT('Ctrl Pts',(6.11360388172153,3.56684641326449,14.9948405883015));
#16520=CARTESIAN_POINT('Ctrl Pts',(6.21886279983567,3.51794377114619,15.0006936096297));
#16521=CARTESIAN_POINT('Ctrl Pts',(6.32194300152003,3.46438351287028,15.0065466309579));
#16522=CARTESIAN_POINT('Ctrl Pts',(6.42241503368695,3.40639774692699,15.0123996522861));
#16523=CARTESIAN_POINT('Ctrl Pts',(6.52292057521672,3.34839264161104,15.0182546257099));
#16524=CARTESIAN_POINT('Ctrl Pts',(6.62081585988714,3.28595930008577,15.0241095991338));
#16525=CARTESIAN_POINT('Ctrl Pts',(6.7156989519954,3.21937408574241,15.0299645725576));
#16526=CARTESIAN_POINT('Ctrl Pts',(6.81068958190116,3.15271340561123,15.0358261818417));
#16527=CARTESIAN_POINT('Ctrl Pts',(6.90266086686863,3.08189169799395,15.0416877911259));
#16528=CARTESIAN_POINT('Ctrl Pts',(6.99124253543272,3.00722673946418,15.0475494004101));
#16529=CARTESIAN_POINT('Ctrl Pts',(7.07988393526634,2.93251143380462,15.0534149622204));
#16530=CARTESIAN_POINT('Ctrl Pts',(7.16513086442159,2.85394799620938,15.0592805240307));
#16531=CARTESIAN_POINT('Ctrl Pts',(7.24664988211231,2.77189109415057,15.0651460858411));
#16532=CARTESIAN_POINT('Ctrl Pts',(7.32828810060065,2.68971420477527,15.0710202245414));
#16533=CARTESIAN_POINT('Ctrl Pts',(7.40618725169891,2.60403396056314,15.0768943632417));
#16534=CARTESIAN_POINT('Ctrl Pts',(7.48005407906505,2.51523814219947,15.082768501942));
#16535=CARTESIAN_POINT('Ctrl Pts',(7.49873379382105,2.49278312933778,15.0842539757233));
#16536=CARTESIAN_POINT('Ctrl Pts',(7.51715585839743,2.47012901786282,15.0857394495046));
#16537=CARTESIAN_POINT('Ctrl Pts',(7.53531597848376,2.44728235746121,15.0872249232859));
#16538=CARTESIAN_POINT('Ctrl Pts',(7.60699321998688,2.35710753552386,15.093088026749));
#16539=CARTESIAN_POINT('Ctrl Pts',(7.67483038428635,2.26362391034172,15.098951130212));
#16540=CARTESIAN_POINT('Ctrl Pts',(7.73850576221524,2.16719274377987,15.1048142336751));
#16541=CARTESIAN_POINT('Ctrl Pts',(7.80210141413587,2.07088231575513,15.1106699961242));
#16542=CARTESIAN_POINT('Ctrl Pts',(7.86154541167449,1.97163202414246,15.1165257585734));
#16543=CARTESIAN_POINT('Ctrl Pts',(7.91655588661019,1.86983648273238,15.1223815210225));
#16544=CARTESIAN_POINT('Ctrl Pts',(7.97151088479885,1.76814359968883,15.1282313780754));
#16545=CARTESIAN_POINT('Ctrl Pts',(8.0220410543321,1.66391093219982,15.1340812351284));
#16546=CARTESIAN_POINT('Ctrl Pts',(8.06790791255176,1.55756179591964,15.1399310921813));
#16547=CARTESIAN_POINT('Ctrl Pts',(8.11373968553886,1.45129400997222,15.1457764744652));
#16548=CARTESIAN_POINT('Ctrl Pts',(8.15491507826354,1.34291335396013,15.1516218567491));
#16549=CARTESIAN_POINT('Ctrl Pts',(8.19124197953134,1.23286681550144,15.157467239033));
#16550=CARTESIAN_POINT('Ctrl Pts',(8.22755295518617,1.12286852114066,15.1633100587175));
#16551=CARTESIAN_POINT('Ctrl Pts',(8.25901953475836,1.01120618864942,15.169152878402));
#16552=CARTESIAN_POINT('Ctrl Pts',(8.28549833137557,0.89834525261235,15.1749956980865));
#16553=CARTESIAN_POINT('Ctrl Pts',(8.31197003508108,0.785514548789573,15.1808369526468));
#16554=CARTESIAN_POINT('Ctrl Pts',(8.33345652218681,0.671486283928796,15.1866782072072));
#16555=CARTESIAN_POINT('Ctrl Pts',(8.34986493302147,0.556738660262869,15.1925194617675));
#16556=CARTESIAN_POINT('Ctrl Pts',(8.36627724229281,0.441963773972303,15.1983621041381));
#16557=CARTESIAN_POINT('Ctrl Pts',(8.37760900470372,0.326469597483212,15.2042047465087));
#16558=CARTESIAN_POINT('Ctrl Pts',(8.38381896595424,0.210741735856192,15.2100473888793));
#16559=CARTESIAN_POINT('Ctrl Pts',(8.38764142737385,0.139506945751002,15.2136437519079));
#16560=CARTESIAN_POINT('Ctrl Pts',(8.38952433087012,0.0681837294481043,
15.2172401149364));
#16561=CARTESIAN_POINT('Ctrl Pts',(8.38946787315746,-0.00311436263953271,
15.220836477965));
#16562=CARTESIAN_POINT('',(8.39488259067608,0.00183385008468958,12.720836477965));
#16563=CARTESIAN_POINT('Ctrl Pts',(8.39488259067608,0.00183385008468958,
12.720836477965));
#16564=CARTESIAN_POINT('Ctrl Pts',(8.38794844153403,-1.19755615080374,12.7817401958959));
#16565=CARTESIAN_POINT('Ctrl Pts',(7.16216767756852,-3.71234879616597,12.908815952964));
#16566=CARTESIAN_POINT('Ctrl Pts',(2.88215862231082,-4.37438359324252,13.1020637491693));
#16567=CARTESIAN_POINT('Ctrl Pts',(-0.0728084404743118,-1.04848949713193,
13.3005798665811));
#16568=CARTESIAN_POINT('Ctrl Pts',(1.12005071800708,3.23759133606708,13.4990959839926));
#16569=CARTESIAN_POINT('Ctrl Pts',(5.36833837100506,4.55874760921314,13.6976121014044));
#16570=CARTESIAN_POINT('Ctrl Pts',(8.07197562134217,2.29834034645692,13.8548584366129));
#16571=CARTESIAN_POINT('Ctrl Pts',(8.38739215187287,0.496171455525351,13.9459327326844));
#16572=CARTESIAN_POINT('Ctrl Pts',(8.38460083020223,0.00246665792446467,
13.9708349896186));
#16573=CARTESIAN_POINT('',(8.3894674945056,-0.00356057987879016,11.470836477965));
#16574=CARTESIAN_POINT('Ctrl Pts',(8.39010368535713,-0.00356115582826364,
11.470836477965));
#16575=CARTESIAN_POINT('Ctrl Pts',(8.39272718587054,-0.287370610773653,
11.485202588602));
#16576=CARTESIAN_POINT('Ctrl Pts',(8.23517039613131,-1.87555148934049,11.5657407383767));
#16577=CARTESIAN_POINT('Ctrl Pts',(6.07814237389157,-4.35704729530058,11.7124509272874));
#16578=CARTESIAN_POINT('Ctrl Pts',(1.67433257548842,-3.72470155112426,11.9109670446996));
#16579=CARTESIAN_POINT('Ctrl Pts',(-0.181649509920632,0.318655022234989,
12.1094831621109));
#16580=CARTESIAN_POINT('Ctrl Pts',(2.20986920695914,4.07019338769287,12.3079992795228));
#16581=CARTESIAN_POINT('Ctrl Pts',(6.65878137671893,4.09432607198936,12.5065153969342));
#16582=CARTESIAN_POINT('Ctrl Pts',(8.34470937675079,1.5118780642868,12.6441277964151));
#16583=CARTESIAN_POINT('Ctrl Pts',(8.39548241161008,0.105584031371379,12.7155681567587));
#16584=CARTESIAN_POINT('Ctrl Pts',(8.39488259067608,0.00183385008468958,
12.720836477965));
#16585=CARTESIAN_POINT('',(8.38701749039333,0.000299844226979141,10.2208363971417));
#16586=CARTESIAN_POINT('Ctrl Pts',(8.38946909489633,0.000298426274701803,
10.220836477965));
#16587=CARTESIAN_POINT('Ctrl Pts',(8.38947828962052,-0.120880079792136,
10.2269326063233));
#16588=CARTESIAN_POINT('Ctrl Pts',(8.38388277070175,-0.241964705586662,
10.2330287346816));
#16589=CARTESIAN_POINT('Ctrl Pts',(8.37273441684076,-0.362429326648316,
10.2391248630399));
#16590=CARTESIAN_POINT('Ctrl Pts',(8.36157285084987,-0.483036712663702,
10.2452282160379));
#16591=CARTESIAN_POINT('Ctrl Pts',(8.34484535990885,-0.603022269854458,
10.2513315690359));
#16592=CARTESIAN_POINT('Ctrl Pts',(8.3226552564171,-0.721868168026954,10.2574349220339));
#16593=CARTESIAN_POINT('Ctrl Pts',(8.30041592491439,-0.840977721895287,
10.2635518151187));
#16594=CARTESIAN_POINT('Ctrl Pts',(8.27268982620504,-0.958942208026926,
10.2696687082035));
#16595=CARTESIAN_POINT('Ctrl Pts',(8.23963100122632,-1.07525581893749,10.2757856012883));
#16596=CARTESIAN_POINT('Ctrl Pts',(8.20653266957785,-1.19170842944702,10.2819098043146));
#16597=CARTESIAN_POINT('Ctrl Pts',(8.16808901353143,-1.30650588770032,10.2880340073409));
#16598=CARTESIAN_POINT('Ctrl Pts',(8.12450272777354,-1.41916114347173,10.2941582103672));
#16599=CARTESIAN_POINT('Ctrl Pts',(8.08082011201351,-1.53206537849982,10.3002959484878));
#16600=CARTESIAN_POINT('Ctrl Pts',(8.03197229300387,-1.64281761691874,10.3064336866084));
#16601=CARTESIAN_POINT('Ctrl Pts',(7.97820906556213,-1.7509530715472,10.3125714247291));
#16602=CARTESIAN_POINT('Ctrl Pts',(7.94823223058556,-1.81124630230657,10.3159936516214));
#16603=CARTESIAN_POINT('Ctrl Pts',(7.91672806648528,-1.87072649483671,10.3194158785138));
#16604=CARTESIAN_POINT('Ctrl Pts',(7.88374568220558,-1.92931704799615,10.3228381054062));
#16605=CARTESIAN_POINT('Ctrl Pts',(7.82713684628902,-2.029878092399,10.3287117947967));
#16606=CARTESIAN_POINT('Ctrl Pts',(7.76600407727453,-2.12811303680096,10.3345854841873));
#16607=CARTESIAN_POINT('Ctrl Pts',(7.70056346489689,-2.22358736999233,10.3404591735779));
#16608=CARTESIAN_POINT('Ctrl Pts',(7.6352073424978,-2.31893843684999,10.3463252794836));
#16609=CARTESIAN_POINT('Ctrl Pts',(7.56555466883785,-2.41153564287309,10.3521913853894));
#16610=CARTESIAN_POINT('Ctrl Pts',(7.49186727841229,-2.50096919937873,10.3580574912951));
#16611=CARTESIAN_POINT('Ctrl Pts',(7.41825534293565,-2.59031117706201,10.3639175903832));
#16612=CARTESIAN_POINT('Ctrl Pts',(7.34061716974116,-2.67649563197447,10.3697776894712));
#16613=CARTESIAN_POINT('Ctrl Pts',(7.25925733950609,-2.7591424608641,10.3756377885592));
#16614=CARTESIAN_POINT('Ctrl Pts',(7.17496223220766,-2.84477099879243,10.3817093066534));
#16615=CARTESIAN_POINT('Ctrl Pts',(7.08667211532095,-2.9266014597789,10.3877808247475));
#16616=CARTESIAN_POINT('Ctrl Pts',(6.99477097921102,-3.00424909113099,10.3938523428416));
#16617=CARTESIAN_POINT('Ctrl Pts',(6.90617192436707,-3.07910678103417,10.3997057064383));
#16618=CARTESIAN_POINT('Ctrl Pts',(6.81421722071067,-3.15007676361715,10.4055590700351));
#16619=CARTESIAN_POINT('Ctrl Pts',(6.71928715616625,-3.2168530387367,10.4114124336318));
#16620=CARTESIAN_POINT('Ctrl Pts',(6.62437134505164,-3.28361928762319,10.4172649183657));
#16621=CARTESIAN_POINT('Ctrl Pts',(6.52648139916281,-3.34619284343324,10.4231174030996));
#16622=CARTESIAN_POINT('Ctrl Pts',(6.42602820179401,-3.40430991083872,10.4289698878335));
#16623=CARTESIAN_POINT('Ctrl Pts',(6.32556579421566,-3.46243230679904,10.4348229091617));
#16624=CARTESIAN_POINT('Ctrl Pts',(6.22254002559596,-3.51609719519072,10.4406759304899));
#16625=CARTESIAN_POINT('Ctrl Pts',(6.11738746377471,-3.56508614335361,10.446528951818));
#16626=CARTESIAN_POINT('Ctrl Pts',(6.01219983154318,-3.61409143027689,10.4523839252419));
#16627=CARTESIAN_POINT('Ctrl Pts',(5.90488436994082,-3.65841750156439,10.4582388986657));
#16628=CARTESIAN_POINT('Ctrl Pts',(5.79589809051774,-3.69789385948521,10.4640938720895));
#16629=CARTESIAN_POINT('Ctrl Pts',(5.68678828914592,-3.7374149587871,10.4699554813737));
#16630=CARTESIAN_POINT('Ctrl Pts',(5.57600427899261,-3.77207523320505,10.4758170906578));
#16631=CARTESIAN_POINT('Ctrl Pts',(5.4640188080805,-3.80175388449559,10.481678699942));
#16632=CARTESIAN_POINT('Ctrl Pts',(5.35195782454314,-3.8314525483186,10.4875442617523));
#16633=CARTESIAN_POINT('Ctrl Pts',(5.23869416970259,-3.85616281236641,10.4934098235627));
#16634=CARTESIAN_POINT('Ctrl Pts',(5.12470965943203,-3.87581521270565,10.499275385373));
#16635=CARTESIAN_POINT('Ctrl Pts',(5.01055847585061,-3.8954963496743,10.5051495240733));
#16636=CARTESIAN_POINT('Ctrl Pts',(4.8956847414542,-3.910104810783,10.5110236627737));
#16637=CARTESIAN_POINT('Ctrl Pts',(4.78057432153144,-3.91962304429989,10.516897801474));
#16638=CARTESIAN_POINT('Ctrl Pts',(4.75146477552493,-3.92203005016997,10.5183832752553));
#16639=CARTESIAN_POINT('Ctrl Pts',(4.72234008553406,-3.92411179532524,10.5198687490365));
#16640=CARTESIAN_POINT('Ctrl Pts',(4.69320807974027,-3.92586852281323,10.5213542228178));
#16641=CARTESIAN_POINT('Ctrl Pts',(4.57801765664793,-3.93281477237915,10.5272279122084));
#16642=CARTESIAN_POINT('Ctrl Pts',(4.46232940648016,-3.9346985245286,10.5331016015989));
#16643=CARTESIAN_POINT('Ctrl Pts',(4.34662559671664,-3.93146580850201,10.5389752909895));
#16644=CARTESIAN_POINT('Ctrl Pts',(4.23107117144161,-3.92823726621551,10.5448413968952));
#16645=CARTESIAN_POINT('Ctrl Pts',(4.11550163573292,-3.91990540403819,10.550707502801));
#16646=CARTESIAN_POINT('Ctrl Pts',(4.00040328120669,-3.90646809320856,10.5565736087067));
#16647=CARTESIAN_POINT('Ctrl Pts',(3.88542278592874,-3.89304454201398,10.5624337077948));
#16648=CARTESIAN_POINT('Ctrl Pts',(3.77091292005242,-3.87452598854507,10.5682938068828));
#16649=CARTESIAN_POINT('Ctrl Pts',(3.65735820340515,-3.85096231674697,10.5741539059709));
#16650=CARTESIAN_POINT('Ctrl Pts',(3.53970669164138,-3.82654852142781,10.580225424065));
#16651=CARTESIAN_POINT('Ctrl Pts',(3.42308100104176,-3.79671871456822,10.5862969421591));
#16652=CARTESIAN_POINT('Ctrl Pts',(3.30801260714209,-3.76158698819125,10.5923684602532));
#16653=CARTESIAN_POINT('Ctrl Pts',(3.19707871259567,-3.72771757281959,10.5982218238499));
#16654=CARTESIAN_POINT('Ctrl Pts',(3.0875925598812,-3.68892081630408,10.6040751874467));
#16655=CARTESIAN_POINT('Ctrl Pts',(2.98001744102106,-3.6453503919838,10.6099285510434));
#16656=CARTESIAN_POINT('Ctrl Pts',(2.87245847420294,-3.60178650961608,10.6157810357773));
#16657=CARTESIAN_POINT('Ctrl Pts',(2.76681035352976,-3.55345053966544,10.6216335205112));
#16658=CARTESIAN_POINT('Ctrl Pts',(2.66351749202751,-3.50054474463201,10.6274860052451));
#16659=CARTESIAN_POINT('Ctrl Pts',(2.56021515995673,-3.44763409884752,10.6333390265733));
#16660=CARTESIAN_POINT('Ctrl Pts',(2.45926888407418,-3.39015298341643,10.6391920479015));
#16661=CARTESIAN_POINT('Ctrl Pts',(2.36109888263643,-3.32834983529776,10.6450450692297));
#16662=CARTESIAN_POINT('Ctrl Pts',(2.26289613960697,-3.26652607463542,10.6509000426535));
#16663=CARTESIAN_POINT('Ctrl Pts',(2.16747186165528,-3.20037763495503,10.6567550160773));
#16664=CARTESIAN_POINT('Ctrl Pts',(2.07521706967055,-3.13019611820688,10.6626099895012));
#16665=CARTESIAN_POINT('Ctrl Pts',(1.9828577187291,-3.05993505972421,10.6684715987853));
#16666=CARTESIAN_POINT('Ctrl Pts',(1.89367535257766,-2.98563205106366,10.6743332080695));
#16667=CARTESIAN_POINT('Ctrl Pts',(1.80802776012755,-2.90761886022175,10.6801948173537));
#16668=CARTESIAN_POINT('Ctrl Pts',(1.72232241487705,-2.82955306451251,10.686060379164));
#16669=CARTESIAN_POINT('Ctrl Pts',(1.64015688155057,-2.74777239570676,10.6919259409743));
#16670=CARTESIAN_POINT('Ctrl Pts',(1.56185072820382,-2.66264407040466,10.6977915027846));
#16671=CARTESIAN_POINT('Ctrl Pts',(1.48343007205496,-2.57739126661179,10.703665641485));
#16672=CARTESIAN_POINT('Ctrl Pts',(1.40888032356853,-2.48878135186914,10.7095397801853));
#16673=CARTESIAN_POINT('Ctrl Pts',(1.33847962379658,-2.39721308763069,10.7154139188856));
#16674=CARTESIAN_POINT('Ctrl Pts',(1.32067643612444,-2.37405696846808,10.7168993926669));
#16675=CARTESIAN_POINT('Ctrl Pts',(1.30313835788537,-2.35071179676952,10.7183848664482));
#16676=CARTESIAN_POINT('Ctrl Pts',(1.28586942857625,-2.32718428237569,10.7198703402294));
#16677=CARTESIAN_POINT('Ctrl Pts',(1.21758661662196,-2.23415449388392,10.72574402962));
#16678=CARTESIAN_POINT('Ctrl Pts',(1.15328798418074,-2.1379619493952,10.7316177190106));
#16679=CARTESIAN_POINT('Ctrl Pts',(1.09328032509298,-2.03898264399506,10.7374914084011));
#16680=CARTESIAN_POINT('Ctrl Pts',(1.03335014153048,-1.94013113017675,10.7433575143069));
#16681=CARTESIAN_POINT('Ctrl Pts',(0.977700126209272,-1.83850036069192,
10.7492236202126));
#16682=CARTESIAN_POINT('Ctrl Pts',(0.926595691254537,-1.73449781617977,
10.7550897261184));
#16683=CARTESIAN_POINT('Ctrl Pts',(0.875543586590257,-1.63060176894848,
10.7609498252064));
#16684=CARTESIAN_POINT('Ctrl Pts',(0.829027984993367,-1.52433914610499,
10.7668099242945));
#16685=CARTESIAN_POINT('Ctrl Pts',(0.787269631400051,-1.41614413602353,
10.7726700233825));
#16686=CARTESIAN_POINT('Ctrl Pts',(0.744004731675103,-1.30404569681056,
10.7787415414766));
#16687=CARTESIAN_POINT('Ctrl Pts',(0.705847056357807,-1.18987319180386,
10.7848130595707));
#16688=CARTESIAN_POINT('Ctrl Pts',(0.672988850968731,-1.07413507443758,
10.7908845776648));
#16689=CARTESIAN_POINT('Ctrl Pts',(0.641311267158917,-0.962555520123894,
10.7967379412616));
#16690=CARTESIAN_POINT('Ctrl Pts',(0.614559001394734,-0.849521356134258,
10.8025913048583));
#16691=CARTESIAN_POINT('Ctrl Pts',(0.592854075775143,-0.735505198169326,
10.8084446684551));
#16692=CARTESIAN_POINT('Ctrl Pts',(0.571152409077104,-0.621506159346891,
10.814297153189));
#16693=CARTESIAN_POINT('Ctrl Pts',(0.55449665289178,-0.506525825468772,
10.8201496379229));
#16694=CARTESIAN_POINT('Ctrl Pts',(0.542957764981321,-0.391047288713175,
10.8260021226568));
#16695=CARTESIAN_POINT('Ctrl Pts',(0.531417819109705,-0.2755581641256,10.831855143985));
#16696=CARTESIAN_POINT('Ctrl Pts',(0.524995715215706,-0.159571156976264,
10.8377081653132));
#16697=CARTESIAN_POINT('Ctrl Pts',(0.523710494086693,-0.0435740600020554,
10.8435611866414));
#16698=CARTESIAN_POINT('Ctrl Pts',(0.522424844311616,0.0724617242438926,
10.8494161600652));
#16699=CARTESIAN_POINT('Ctrl Pts',(0.526279488596708,0.188507192109541,
10.8552711334891));
#16700=CARTESIAN_POINT('Ctrl Pts',(0.535241367677898,0.304075685482606,
10.8611261069129));
#16701=CARTESIAN_POINT('Ctrl Pts',(0.544213403897897,0.419775160898442,
10.8669877161971));
#16702=CARTESIAN_POINT('Ctrl Pts',(0.558304196241379,0.534996170699235,
10.8728493254812));
#16703=CARTESIAN_POINT('Ctrl Pts',(0.577428918229164,0.649258207468796,
10.8787109347654));
#16704=CARTESIAN_POINT('Ctrl Pts',(0.596566536157391,0.763597291968611,
10.8845764965757));
#16705=CARTESIAN_POINT('Ctrl Pts',(0.620744756811182,0.876975712768846,
10.890442058386));
#16706=CARTESIAN_POINT('Ctrl Pts',(0.649828246082207,0.988925862713038,
10.8963076201964));
#16707=CARTESIAN_POINT('Ctrl Pts',(0.678954262547775,1.10103971123416,10.9021817588967));
#16708=CARTESIAN_POINT('Ctrl Pts',(0.712999741548429,1.21172072744612,10.908055897597));
#16709=CARTESIAN_POINT('Ctrl Pts',(0.751780383614942,1.32051901486342,10.9139300362974));
#16710=CARTESIAN_POINT('Ctrl Pts',(0.761587374894654,1.3480323256054,10.9154155100786));
#16711=CARTESIAN_POINT('Ctrl Pts',(0.771696946848984,1.37542534998821,10.9169009838599));
#16712=CARTESIAN_POINT('Ctrl Pts',(0.782105650995835,1.40269105612248,10.9183864576411));
#16713=CARTESIAN_POINT('Ctrl Pts',(0.823262550490445,1.51050197198537,10.9242601470317));
#16714=CARTESIAN_POINT('Ctrl Pts',(0.869237000275695,1.6166795106457,10.9301338364222));
#16715=CARTESIAN_POINT('Ctrl Pts',(0.919879364589478,1.72076204031997,10.9360075258128));
#16716=CARTESIAN_POINT('Ctrl Pts',(0.970456344853387,1.8247101896705,10.9418736317186));
#16717=CARTESIAN_POINT('Ctrl Pts',(1.02568907537559,1.92656834099087,10.9477397376243));
#16718=CARTESIAN_POINT('Ctrl Pts',(1.08537902941477,2.02589256725946,10.9536058435301));
#16719=CARTESIAN_POINT('Ctrl Pts',(1.14500786170141,2.12511508678566,10.9594659426181));
#16720=CARTESIAN_POINT('Ctrl Pts',(1.20908462750555,2.22180849033333,10.9653260417062));
#16721=CARTESIAN_POINT('Ctrl Pts',(1.27736414285858,2.31555190655315,10.9711861407942));
#16722=CARTESIAN_POINT('Ctrl Pts',(1.34810702735494,2.41267737136708,10.9772576588883));
#16723=CARTESIAN_POINT('Ctrl Pts',(1.42336144053963,2.50663556622707,10.9833291769824));
#16724=CARTESIAN_POINT('Ctrl Pts',(1.50280434312715,2.59698930827102,10.9894006950765));
#16725=CARTESIAN_POINT('Ctrl Pts',(1.57939279873556,2.68409656815448,10.9952540586733));
#16726=CARTESIAN_POINT('Ctrl Pts',(1.65987363602657,2.76785360237434,11.00110742227));
#16727=CARTESIAN_POINT('Ctrl Pts',(1.74391586165861,2.84790166533695,11.0069607858668));
#16728=CARTESIAN_POINT('Ctrl Pts',(1.82794546863324,2.92793770935223,11.0128132706007));
#16729=CARTESIAN_POINT('Ctrl Pts',(1.91553510162423,3.00426560455017,11.0186657553346));
#16730=CARTESIAN_POINT('Ctrl Pts',(2.00631728136105,3.07656383570192,11.0245182400685));
#16731=CARTESIAN_POINT('Ctrl Pts',(2.09710778460494,3.14886869563082,11.0303712613967));
#16732=CARTESIAN_POINT('Ctrl Pts',(2.19109109328435,3.2171428996573,11.0362242827248));
#16733=CARTESIAN_POINT('Ctrl Pts',(2.28786763352659,3.28110601057625,11.042077304053));
#16734=CARTESIAN_POINT('Ctrl Pts',(2.38467645061428,3.34509045442816,11.0479322774768));
#16735=CARTESIAN_POINT('Ctrl Pts',(2.484280007223,3.40476071842671,11.0537872509007));
#16736=CARTESIAN_POINT('Ctrl Pts',(2.58625143898061,3.45988076053962,11.0596422243245));
#16737=CARTESIAN_POINT('Ctrl Pts',(2.68833844225797,3.51506327414014,11.0655038336087));
#16738=CARTESIAN_POINT('Ctrl Pts',(2.79279831350346,3.56568507604157,11.0713654428928));
#16739=CARTESIAN_POINT('Ctrl Pts',(2.89918129332347,3.61155695895959,11.077227052177));
#16740=CARTESIAN_POINT('Ctrl Pts',(3.00563600796784,3.65745977362504,11.0830926139873));
#16741=CARTESIAN_POINT('Ctrl Pts',(3.11401602804567,3.69860614533714,11.0889581757977));
#16742=CARTESIAN_POINT('Ctrl Pts',(3.22385505368668,3.73485630212218,11.094823737608));
#16743=CARTESIAN_POINT('Ctrl Pts',(3.33385469092331,3.77115946552747,11.1006978763083));
#16744=CARTESIAN_POINT('Ctrl Pts',(3.44531719535615,3.80255201393801,11.1065720150087));
#16745=CARTESIAN_POINT('Ctrl Pts',(3.55776460494286,3.82894492248026,11.112446153709));
#16746=CARTESIAN_POINT('Ctrl Pts',(3.58620071910883,3.83561925818295,11.1139316274902));
#16747=CARTESIAN_POINT('Ctrl Pts',(3.61469978756485,3.841974124591,11.1154171012715));
#16748=CARTESIAN_POINT('Ctrl Pts',(3.64325403190415,3.84800860743688,11.1169025750527));
#16749=CARTESIAN_POINT('Ctrl Pts',(3.75615993717776,3.87186946470475,11.1227762644433));
#16750=CARTESIAN_POINT('Ctrl Pts',(3.87030494260292,3.89079662734251,11.1286499538339));
#16751=CARTESIAN_POINT('Ctrl Pts',(3.98522001639962,3.90466558047487,11.1345236432244));
#16752=CARTESIAN_POINT('Ctrl Pts',(4.09998672404016,3.91851662748579,11.1403897491302));
#16753=CARTESIAN_POINT('Ctrl Pts',(4.21552111643121,3.92732240320993,11.1462558550359));
#16754=CARTESIAN_POINT('Ctrl Pts',(4.33134253497827,3.93100907416528,11.1521219609417));
#16755=CARTESIAN_POINT('Ctrl Pts',(4.4470453538682,3.93469197001653,11.1579820600297));
#16756=CARTESIAN_POINT('Ctrl Pts',(4.56303420381904,3.93326617460282,11.1638421591177));
#16757=CARTESIAN_POINT('Ctrl Pts',(4.67882250677198,3.92670955957558,11.1697022582058));
#16758=CARTESIAN_POINT('Ctrl Pts',(4.79878818754027,3.91991639683617,11.1757737762999));
#16759=CARTESIAN_POINT('Ctrl Pts',(4.91853812912318,3.9076151539711,11.181845294394));
#16760=CARTESIAN_POINT('Ctrl Pts',(5.03752984066193,3.88984028243934,11.1879168124881));
#16761=CARTESIAN_POINT('Ctrl Pts',(5.15224608490948,3.87270407624702,11.1937701760849));
#16762=CARTESIAN_POINT('Ctrl Pts',(5.26625720537262,3.85048088198621,11.1996235396816));
#16763=CARTESIAN_POINT('Ctrl Pts',(5.37908231067531,3.82325435656085,11.2054769032784));
#16764=CARTESIAN_POINT('Ctrl Pts',(5.49189047566793,3.7960319191067,11.2113293880123));
#16765=CARTESIAN_POINT('Ctrl Pts',(5.60351257807364,3.76380774111264,11.2171818727462));
#16766=CARTESIAN_POINT('Ctrl Pts',(5.71347923211499,3.72671632182986,11.2230343574801));
#16767=CARTESIAN_POINT('Ctrl Pts',(5.82345596862205,3.68962150176194,11.2288873788083));
#16768=CARTESIAN_POINT('Ctrl Pts',(5.93177656353831,3.64765868533166,11.2347404001365));
#16769=CARTESIAN_POINT('Ctrl Pts',(6.03798875048295,3.60101160992364,11.2405934214646));
#16770=CARTESIAN_POINT('Ctrl Pts',(6.14423636124303,3.55434897681516,11.2464483948885));
#16771=CARTESIAN_POINT('Ctrl Pts',(6.24837378769322,3.50299914422559,11.2523033683123));
#16772=CARTESIAN_POINT('Ctrl Pts',(6.34997127462551,3.44719284900584,11.2581583417361));
#16773=CARTESIAN_POINT('Ctrl Pts',(6.45168390925957,3.39132330451849,11.2640199510203));
#16774=CARTESIAN_POINT('Ctrl Pts',(6.55085049635795,3.33098741526809,11.2698815603044));
#16775=CARTESIAN_POINT('Ctrl Pts',(6.64706822470992,3.26646054653405,11.2757431695886));
#16776=CARTESIAN_POINT('Ctrl Pts',(6.74335083338242,3.20189016685876,11.2816087313989));
#16777=CARTESIAN_POINT('Ctrl Pts',(6.83668029210354,3.13312342495588,11.2874742932092));
#16778=CARTESIAN_POINT('Ctrl Pts',(6.92668636379225,3.06047638454924,11.2933398550196));
#16779=CARTESIAN_POINT('Ctrl Pts',(7.01682404643358,2.98772311635138,11.2992139937199));
#16780=CARTESIAN_POINT('Ctrl Pts',(7.10362833498062,2.91107849827556,11.3050881324202));
#16781=CARTESIAN_POINT('Ctrl Pts',(7.1867653133645,2.83089590434597,11.3109622711206));
#16782=CARTESIAN_POINT('Ctrl Pts',(7.20778929797644,2.81061903533184,11.3124477449019));
#16783=CARTESIAN_POINT('Ctrl Pts',(7.22857895815252,2.79011607799067,11.3139332186831));
#16784=CARTESIAN_POINT('Ctrl Pts',(7.24912930887828,2.76939307294556,11.3154186924644));
#16785=CARTESIAN_POINT('Ctrl Pts',(7.32927828383865,2.68857072423587,11.3212122286667));
#16786=CARTESIAN_POINT('Ctrl Pts',(7.40606706242935,2.6041132158985,11.3270057648691));
#16787=CARTESIAN_POINT('Ctrl Pts',(7.47914097595604,2.51633538462103,11.3327993010714));
#16788=CARTESIAN_POINT('Ctrl Pts',(7.55209911577413,2.42869662301384,11.3385836583597));
#16789=CARTESIAN_POINT('Ctrl Pts',(7.62135383077772,2.33774832840261,11.3443680156479));
#16790=CARTESIAN_POINT('Ctrl Pts',(7.68658655478061,2.24384274593675,11.3501523729362));
#16791=CARTESIAN_POINT('Ctrl Pts',(7.7517602556785,2.15002213001398,11.3559314964904));
#16792=CARTESIAN_POINT('Ctrl Pts',(7.81291895401834,2.05324988897331,11.3617106200447));
#16793=CARTESIAN_POINT('Ctrl Pts',(7.86978389785402,1.95391175164092,11.3674897435989));
#16794=CARTESIAN_POINT('Ctrl Pts',(7.9266120402158,1.85463790329963,11.3732651270586));
#16795=CARTESIAN_POINT('Ctrl Pts',(7.97915173944889,1.75280182648967,11.3790405105184));
#16796=CARTESIAN_POINT('Ctrl Pts',(8.02716768780263,1.6488179521922,11.3848158939781));
#16797=CARTESIAN_POINT('Ctrl Pts',(8.07516492791672,1.54487459266761,11.3905890272009));
#16798=CARTESIAN_POINT('Ctrl Pts',(8.11864174333495,1.43878548517782,11.3963621604238));
#16799=CARTESIAN_POINT('Ctrl Pts',(8.15740931008386,1.33098858275012,11.4021352936466));
#16800=CARTESIAN_POINT('Ctrl Pts',(8.19618594375124,1.22316646889425,11.4079097770839));
#16801=CARTESIAN_POINT('Ctrl Pts',(8.23025097372873,1.11363615900231,11.4136842605211));
#16802=CARTESIAN_POINT('Ctrl Pts',(8.25946432045127,1.00285412723924,11.4194587439584));
#16803=CARTESIAN_POINT('Ctrl Pts',(8.28867979540815,0.892064024845738,11.4252336480751));
#16804=CARTESIAN_POINT('Ctrl Pts',(8.31304278359162,0.780022433108546,11.4310085521918));
#16805=CARTESIAN_POINT('Ctrl Pts',(8.33246391806155,0.667198035491587,11.4367834563085));
#16806=CARTESIAN_POINT('Ctrl Pts',(8.35190402178076,0.55426343864161,11.4425640009606));
#16807=CARTESIAN_POINT('Ctrl Pts',(8.36639256469885,0.440544929944047,11.4483445456126));
#16808=CARTESIAN_POINT('Ctrl Pts',(8.37589186159069,0.326518398668027,11.4541250902647));
#16809=CARTESIAN_POINT('Ctrl Pts',(8.38504592594477,0.216635928706429,11.4596955528315));
#16810=CARTESIAN_POINT('Ctrl Pts',(8.38956710420808,0.106467789835327,11.4652660153982));
#16811=CARTESIAN_POINT('Ctrl Pts',(8.3894674945056,-0.00356057987879016,
11.470836477965));
#16812=CARTESIAN_POINT('',(8.38956893211207,0.00341085378143758,8.97083652763293));
#16813=CARTESIAN_POINT('Ctrl Pts',(8.39119799873609,0.00339649975582836,
8.97083732632742));
#16814=CARTESIAN_POINT('Ctrl Pts',(8.38152382860528,-1.0554250693434,9.02447201786367));
#16815=CARTESIAN_POINT('Ctrl Pts',(7.39472429574437,-3.43645618331368,9.14427874853716));
#16816=CARTESIAN_POINT('Ctrl Pts',(3.37012330303654,-4.52034712344961,9.33025751834786));
#16817=CARTESIAN_POINT('Ctrl Pts',(0.0690675541444807,-1.53765826549021,
9.52877363575949));
#16818=CARTESIAN_POINT('Ctrl Pts',(0.785910689414721,2.85318878264351,9.72728975317118));
#16819=CARTESIAN_POINT('Ctrl Pts',(4.86418140136913,4.63113981703775,9.9258058705828));
#16820=CARTESIAN_POINT('Ctrl Pts',(7.93452534716083,2.58985569568638,10.0903213748425));
#16821=CARTESIAN_POINT('Ctrl Pts',(8.38346869164466,0.638758348126131,10.1886648399649));
#16822=CARTESIAN_POINT('Ctrl Pts',(8.38303806571692,0.000302145835691118,
10.22083626595));
#16823=CARTESIAN_POINT('',(8.38946839700585,-0.00236191959998835,7.72083647791993));
#16824=CARTESIAN_POINT('Ctrl Pts',(8.38946839700532,-0.00236192048784542,
7.72083647796504));
#16825=CARTESIAN_POINT('Ctrl Pts',(8.38938451678962,-0.142036744660387,
7.7279338449949));
#16826=CARTESIAN_POINT('Ctrl Pts',(8.38186061236754,-0.281485965734069,
7.73503121202475));
#16827=CARTESIAN_POINT('Ctrl Pts',(8.36696529334037,-0.420129230717581,
7.7421285790546));
#16828=CARTESIAN_POINT('Ctrl Pts',(8.35463811947842,-0.53486860817727,7.74800226844517));
#16829=CARTESIAN_POINT('Ctrl Pts',(8.33723621668261,-0.64925607920517,7.75387595783574));
#16830=CARTESIAN_POINT('Ctrl Pts',(8.31478665350495,-0.762807121295797,
7.75974964722631));
#16831=CARTESIAN_POINT('Ctrl Pts',(8.29236607482239,-0.87621155832346,7.76561575313208));
#16832=CARTESIAN_POINT('Ctrl Pts',(8.26491087533944,-0.988781312399312,
7.77148185903784));
#16833=CARTESIAN_POINT('Ctrl Pts',(8.23249991209748,-1.10003652350777,7.7773479649436));
#16834=CARTESIAN_POINT('Ctrl Pts',(8.20012213726901,-1.21117781069729,7.78320806403164));
#16835=CARTESIAN_POINT('Ctrl Pts',(8.16279880742635,-1.3210068380762,7.78906816311968));
#16836=CARTESIAN_POINT('Ctrl Pts',(8.12065977154157,-1.42905415158329,7.79492826220772));
#16837=CARTESIAN_POINT('Ctrl Pts',(8.07700045537665,-1.54099956566621,7.80099978030183));
#16838=CARTESIAN_POINT('Ctrl Pts',(8.02817148082484,-1.65103183515718,7.80707129839594));
#16839=CARTESIAN_POINT('Ctrl Pts',(7.97437382595932,-1.75864589466542,7.81314281649004));
#16840=CARTESIAN_POINT('Ctrl Pts',(7.92250916382703,-1.86239329501268,7.8189961800868));
#16841=CARTESIAN_POINT('Ctrl Pts',(7.86602693437099,-1.96389286992841,7.82484954368356));
#16842=CARTESIAN_POINT('Ctrl Pts',(7.80515579369172,-2.06271337542034,7.83070290728031));
#16843=CARTESIAN_POINT('Ctrl Pts',(7.74429379260934,-2.16151904334598,7.83655539201423));
#16844=CARTESIAN_POINT('Ctrl Pts',(7.67904440722507,-2.25764609000753,7.84240787674815));
#16845=CARTESIAN_POINT('Ctrl Pts',(7.60968106185165,-2.35068997591145,7.84826036148206));
#16846=CARTESIAN_POINT('Ctrl Pts',(7.54031135679081,-2.44374239269039,7.85411338281024));
#16847=CARTESIAN_POINT('Ctrl Pts',(7.46682718885623,-2.53371075551174,7.85996640413843));
#16848=CARTESIAN_POINT('Ctrl Pts',(7.38954348461585,-2.62022206898338,7.86581942546661));
#16849=CARTESIAN_POINT('Ctrl Pts',(7.31223400476758,-2.70676223564879,7.87167439889044));
#16850=CARTESIAN_POINT('Ctrl Pts',(7.23112274390024,-2.78984275234918,7.87752937231428));
#16851=CARTESIAN_POINT('Ctrl Pts',(7.14656233055052,-2.86912659957723,7.88338434573811));
#16852=CARTESIAN_POINT('Ctrl Pts',(7.06190607883368,-2.94850030486245,7.88924595502227));
#16853=CARTESIAN_POINT('Ctrl Pts',(6.97379317372207,-3.02406846933132,7.89510756430643));
#16854=CARTESIAN_POINT('Ctrl Pts',(6.88261031695746,-3.09553352841685,7.9009691735906));
#16855=CARTESIAN_POINT('Ctrl Pts',(6.79136597492294,-3.16704677691652,7.90683473540094));
#16856=CARTESIAN_POINT('Ctrl Pts',(6.69704789452532,-3.23445117118951,7.91270029721129));
#16857=CARTESIAN_POINT('Ctrl Pts',(6.60007136856806,-3.2974927355263,7.91856585902163));
#16858=CARTESIAN_POINT('Ctrl Pts',(6.5029530391447,-3.36062648209218,7.92443999772197));
#16859=CARTESIAN_POINT('Ctrl Pts',(6.40316886072867,-3.41938445795923,7.93031413642231));
#16860=CARTESIAN_POINT('Ctrl Pts',(6.3011583341624,-3.4735587878006,7.93618827512266));
#16861=CARTESIAN_POINT('Ctrl Pts',(6.27536153732952,-3.48725859141418,7.93767374890386));
#16862=CARTESIAN_POINT('Ctrl Pts',(6.2494224605816,-3.50066551228908,7.93915922268506));
#16863=CARTESIAN_POINT('Ctrl Pts',(6.22334839260746,-3.51377668432824,7.94064469646626));
#16864=CARTESIAN_POINT('Ctrl Pts',(6.12024931515043,-3.56561937120619,7.94651838585683));
#16865=CARTESIAN_POINT('Ctrl Pts',(6.01469488860868,-3.61300695171493,7.9523920752474));
#16866=CARTESIAN_POINT('Ctrl Pts',(5.9071069351652,-3.65569950751263,7.95826576463797));
#16867=CARTESIAN_POINT('Ctrl Pts',(5.79965788787712,-3.69833694320997,7.96413187054372));
#16868=CARTESIAN_POINT('Ctrl Pts',(5.69018091540317,-3.73629125797423,7.96999797644947));
#16869=CARTESIAN_POINT('Ctrl Pts',(5.57912199703213,-3.76936857931766,7.97586408235522));
#16870=CARTESIAN_POINT('Ctrl Pts',(5.46817680157858,-3.80241202990545,7.98172418144326));
#16871=CARTESIAN_POINT('Ctrl Pts',(5.35565327593104,-3.83058830328179,7.9875842805313));
#16872=CARTESIAN_POINT('Ctrl Pts',(5.24201629838382,-3.85375201704531,7.99344437961934));
#16873=CARTESIAN_POINT('Ctrl Pts',(5.12427955793418,-3.87775142475651,7.99951589771344));
#16874=CARTESIAN_POINT('Ctrl Pts',(5.00534792691778,-3.89636959407862,8.00558741580755));
#16875=CARTESIAN_POINT('Ctrl Pts',(4.88575476787085,-3.90950160771159,8.01165893390166));
#16876=CARTESIAN_POINT('Ctrl Pts',(4.77045868660498,-3.92216177759987,8.01751229749841));
#16877=CARTESIAN_POINT('Ctrl Pts',(4.65454824352446,-3.9297232018855,8.02336566109515));
#16878=CARTESIAN_POINT('Ctrl Pts',(4.53850977298686,-3.93214424061429,8.0292190246919));
#16879=CARTESIAN_POINT('Ctrl Pts',(4.42248872523512,-3.93456491583226,8.0350715094258));
#16880=CARTESIAN_POINT('Ctrl Pts',(4.30634010119277,-3.93184673152903,8.0409239941597));
#16881=CARTESIAN_POINT('Ctrl Pts',(4.19055206449122,-3.92400014359316,8.0467764788936));
#16882=CARTESIAN_POINT('Ctrl Pts',(4.07475341158138,-3.91615283623053,8.05262950022177));
#16883=CARTESIAN_POINT('Ctrl Pts',(3.95931582395675,-3.90317621844521,8.05848252154994));
#16884=CARTESIAN_POINT('Ctrl Pts',(3.84472345726007,-3.8851327211539,8.06433554287811));
#16885=CARTESIAN_POINT('Ctrl Pts',(3.73009287179602,-3.86708320600778,8.07019051630193));
#16886=CARTESIAN_POINT('Ctrl Pts',(3.61630847569694,-3.8439635152872,8.07604548972575));
#16887=CARTESIAN_POINT('Ctrl Pts',(3.50384463238308,-3.81588726403837,8.08190046314957));
#16888=CARTESIAN_POINT('Ctrl Pts',(3.39125332574829,-3.78777919196502,8.08776207243372));
#16889=CARTESIAN_POINT('Ctrl Pts',(3.27998596024276,-3.75470344704791,8.09362368171788));
#16890=CARTESIAN_POINT('Ctrl Pts',(3.17050221639931,-3.71682366521327,8.09948529100203));
#16891=CARTESIAN_POINT('Ctrl Pts',(3.0609446468634,-3.67891834076357,8.10535085281237));
#16892=CARTESIAN_POINT('Ctrl Pts',(2.95317347697617,-3.63620268089148,8.1112164146227));
#16893=CARTESIAN_POINT('Ctrl Pts',(2.84762725869796,-3.58888797675095,8.11708197643304));
#16894=CARTESIAN_POINT('Ctrl Pts',(2.7419267059617,-3.54150408690825,8.12295611513337));
#16895=CARTESIAN_POINT('Ctrl Pts',(2.63845796558737,-3.48950791632374,8.1288302538337));
#16896=CARTESIAN_POINT('Ctrl Pts',(2.53763397443016,-3.43315608981237,8.13470439253403));
#16897=CARTESIAN_POINT('Ctrl Pts',(2.51213723303021,-3.41890563283795,8.13618986631532));
#16898=CARTESIAN_POINT('Ctrl Pts',(2.48680947199874,-3.40437684241615,8.13767534009662));
#16899=CARTESIAN_POINT('Ctrl Pts',(2.46165705100713,-3.38957428955088,8.13916081387791));
#16900=CARTESIAN_POINT('Ctrl Pts',(2.36220224393779,-3.33104373935695,8.14503450326848));
#16901=CARTESIAN_POINT('Ctrl Pts',(2.26516002961895,-3.26803478452421,8.15090819265904));
#16902=CARTESIAN_POINT('Ctrl Pts',(2.1709606871333,-3.20077182352816,8.15678188204961));
#16903=CARTESIAN_POINT('Ctrl Pts',(2.0768829648484,-3.13359570533381,8.16264798795536));
#16904=CARTESIAN_POINT('Ctrl Pts',(1.98564114830211,-3.06217674129319,8.16851409386112));
#16905=CARTESIAN_POINT('Ctrl Pts',(1.89763991968141,-2.98678459118283,8.17438019976687));
#16906=CARTESIAN_POINT('Ctrl Pts',(1.80972880319777,-2.91146964167377,8.1802402988549));
#16907=CARTESIAN_POINT('Ctrl Pts',(1.72505198610896,-2.83218986585914,8.18610039794294));
#16908=CARTESIAN_POINT('Ctrl Pts',(1.64398364933252,-2.74925709143511,8.19196049703097));
#16909=CARTESIAN_POINT('Ctrl Pts',(1.55999055191163,-2.66333229170977,8.19803201512508));
#16910=CARTESIAN_POINT('Ctrl Pts',(1.47987158979592,-2.57348619555289,8.20410353321919));
#16911=CARTESIAN_POINT('Ctrl Pts',(1.40400406671963,-2.48011011502285,8.2101750513133));
#16912=CARTESIAN_POINT('Ctrl Pts',(1.33086252437931,-2.3900891116906,8.21602841491005));
#16913=CARTESIAN_POINT('Ctrl Pts',(1.26167244659689,-2.29678777681905,8.22188177850679));
#16914=CARTESIAN_POINT('Ctrl Pts',(1.19673247023338,-2.20059220757005,8.22773514210354));
#16915=CARTESIAN_POINT('Ctrl Pts',(1.13180224438879,-2.10441108176206,8.23358762683744));
#16916=CARTESIAN_POINT('Ctrl Pts',(1.07112108220504,-2.00533692797377,8.23944011157134));
#16917=CARTESIAN_POINT('Ctrl Pts',(1.01494483566442,-1.90378562217202,8.24529259630524));
#16918=CARTESIAN_POINT('Ctrl Pts',(0.958763438516236,-1.802225005479,8.25114561763342));
#16919=CARTESIAN_POINT('Ctrl Pts',(0.907087978092209,-1.69818714681344,
8.25699863896159));
#16920=CARTESIAN_POINT('Ctrl Pts',(0.86012845858185,-1.59211273035492,8.26285166028976));
#16921=CARTESIAN_POINT('Ctrl Pts',(0.813153277164838,-1.48600293602997,
8.26870663371358));
#16922=CARTESIAN_POINT('Ctrl Pts',(0.770897331372616,-1.37785561086723,
8.27456160713741));
#16923=CARTESIAN_POINT('Ctrl Pts',(0.733522306512086,-1.26813095796831,
8.28041658056123));
#16924=CARTESIAN_POINT('Ctrl Pts',(0.69610492186153,-1.15828194626896,8.28627818984538));
#16925=CARTESIAN_POINT('Ctrl Pts',(0.663579632762124,-1.0468524299936,8.29213979912953));
#16926=CARTESIAN_POINT('Ctrl Pts',(0.636058131849826,-0.934317390893103,
8.29800140841368));
#16927=CARTESIAN_POINT('Ctrl Pts',(0.608518072987343,-0.821706468589274,
8.30386697022402));
#16928=CARTESIAN_POINT('Ctrl Pts',(0.585988600968007,-0.707988943344857,
8.30973253203436));
#16929=CARTESIAN_POINT('Ctrl Pts',(0.568529909365876,-0.593647876757686,
8.3155980938447));
#16930=CARTESIAN_POINT('Ctrl Pts',(0.551045688874598,-0.479139615487187,
8.32147223254503));
#16931=CARTESIAN_POINT('Ctrl Pts',(0.538647090792383,-0.364006402400335,
8.32734637124536));
#16932=CARTESIAN_POINT('Ctrl Pts',(0.531342328270057,-0.248734350329883,
8.33322050994569));
#16933=CARTESIAN_POINT('Ctrl Pts',(0.529495073079284,-0.219583930191329,
8.33470598372699));
#16934=CARTESIAN_POINT('Ctrl Pts',(0.527973309533415,-0.190424618373375,
8.33619145750828));
#16935=CARTESIAN_POINT('Ctrl Pts',(0.52677664422032,-0.161264236942484,
8.33767693128958));
#16936=CARTESIAN_POINT('Ctrl Pts',(0.522044928021695,-0.0459616141750869,
8.34355062068014));
#16937=CARTESIAN_POINT('Ctrl Pts',(0.522384339860266,0.0697414737208014,
8.34942431007071));
#16938=CARTESIAN_POINT('Ctrl Pts',(0.527839574319278,0.185361811307665,
8.35529799946128));
#16939=CARTESIAN_POINT('Ctrl Pts',(0.533287765558104,0.300832872176622,
8.36116410536703));
#16940=CARTESIAN_POINT('Ctrl Pts',(0.54383862492926,0.416220986286492,8.36703021127279));
#16941=CARTESIAN_POINT('Ctrl Pts',(0.559484937268936,0.531039910890344,
8.37289631717854));
#16942=CARTESIAN_POINT('Ctrl Pts',(0.575115227984102,0.645741262378132,
8.37875641626658));
#16943=CARTESIAN_POINT('Ctrl Pts',(0.595830537820032,0.759874176753978,
8.38461651535462));
#16944=CARTESIAN_POINT('Ctrl Pts',(0.621571682550897,0.872955182096708,
8.39047661444265));
#16945=CARTESIAN_POINT('Ctrl Pts',(0.648241509058696,0.990115892133119,
8.39654813253676));
#16946=CARTESIAN_POINT('Ctrl Pts',(0.680306637325,1.10614690796246,8.40261965063087));
#16947=CARTESIAN_POINT('Ctrl Pts',(0.717642784699322,1.22051904430748,8.40869116872498));
#16948=CARTESIAN_POINT('Ctrl Pts',(0.753637414460184,1.3307816983897,8.41454453232173));
#16949=CARTESIAN_POINT('Ctrl Pts',(0.7945306590742,1.43950220472268,8.42039789591848));
#16950=CARTESIAN_POINT('Ctrl Pts',(0.840159971949192,1.54622030946504,8.42625125951523));
#16951=CARTESIAN_POINT('Ctrl Pts',(0.88578243373641,1.65292239084311,8.43210374424913));
#16952=CARTESIAN_POINT('Ctrl Pts',(0.936139387461083,1.75762228866743,8.43795622898303));
#16953=CARTESIAN_POINT('Ctrl Pts',(0.991020069077824,1.85987955819255,8.44380871371694));
#16954=CARTESIAN_POINT('Ctrl Pts',(1.0459057825162,1.9621462033363,8.44966173504511));
#16955=CARTESIAN_POINT('Ctrl Pts',(1.10531585297771,2.06196941092612,8.45551475637329));
#16956=CARTESIAN_POINT('Ctrl Pts',(1.16899381535657,2.1589338137085,8.46136777770146));
#16957=CARTESIAN_POINT('Ctrl Pts',(1.23269301556566,2.25593055599182,8.46722275112528));
#16958=CARTESIAN_POINT('Ctrl Pts',(1.30066271144355,2.35006625239295,8.47307772454911));
#16959=CARTESIAN_POINT('Ctrl Pts',(1.37260384185533,2.44095555700136,8.47893269797293));
#16960=CARTESIAN_POINT('Ctrl Pts',(1.44462650829791,2.53194787296222,8.48479430725709));
#16961=CARTESIAN_POINT('Ctrl Pts',(1.52062933666531,2.61968612920501,8.49065591654124));
#16962=CARTESIAN_POINT('Ctrl Pts',(1.60027374570524,2.70381897740657,8.4965175258254));
#16963=CARTESIAN_POINT('Ctrl Pts',(1.67997185955514,2.78800855700561,8.50238308763574));
#16964=CARTESIAN_POINT('Ctrl Pts',(1.76331614732318,2.86858760114024,8.50824864944608));
#16965=CARTESIAN_POINT('Ctrl Pts',(1.84993332006699,2.94524365639124,8.51411421125643));
#16966=CARTESIAN_POINT('Ctrl Pts',(1.93667714836154,3.02201180159609,8.51998834995676));
#16967=CARTESIAN_POINT('Ctrl Pts',(2.02670309284885,3.09484525070625,8.5258624886571));
#16968=CARTESIAN_POINT('Ctrl Pts',(2.11960712152811,3.16347357575657,8.53173662735743));
#16969=CARTESIAN_POINT('Ctrl Pts',(2.14310103371124,3.18082855879583,8.53322210113869));
#16970=CARTESIAN_POINT('Ctrl Pts',(2.16677886975879,3.19791484891566,8.53470757491996));
#16971=CARTESIAN_POINT('Ctrl Pts',(2.19063384345448,3.21472853628673,8.53619304870123));
#16972=CARTESIAN_POINT('Ctrl Pts',(2.28495843381453,3.28121128298559,8.54206673809179));
#16973=CARTESIAN_POINT('Ctrl Pts',(2.38236864490508,3.3436498169556,8.54794042748236));
#16974=CARTESIAN_POINT('Ctrl Pts',(2.48248265636078,3.40174462530319,8.55381411687292));
#16975=CARTESIAN_POINT('Ctrl Pts',(2.58246741122243,3.45976442779545,8.55968022277868));
#16976=CARTESIAN_POINT('Ctrl Pts',(2.68514867019757,3.51345145198743,8.56554632868444));
#16977=CARTESIAN_POINT('Ctrl Pts',(2.7901139282814,3.56254816402011,8.57141243459019));
#16978=CARTESIAN_POINT('Ctrl Pts',(2.89497170327807,3.6115946016451,8.57727253367823));
#16979=CARTESIAN_POINT('Ctrl Pts',(3.00210845333796,3.65605990263494,8.58313263276627));
#16980=CARTESIAN_POINT('Ctrl Pts',(3.11108582888008,3.69573170523224,8.5889927318543));
#16981=CARTESIAN_POINT('Ctrl Pts',(3.2239948595146,3.7368347759614,8.59506424994841));
#16982=CARTESIAN_POINT('Ctrl Pts',(3.33887944364003,3.77279171431066,8.60113576804251));
#16983=CARTESIAN_POINT('Ctrl Pts',(3.45522752790838,3.80342007959462,8.60720728613662));
#16984=CARTESIAN_POINT('Ctrl Pts',(3.56739513252589,3.83294794323635,8.61306064973337));
#16985=CARTESIAN_POINT('Ctrl Pts',(3.68092244399082,3.85752344941429,8.61891401333012));
#16986=CARTESIAN_POINT('Ctrl Pts',(3.79533458933496,3.87703367932051,8.62476737692687));
#16987=CARTESIAN_POINT('Ctrl Pts',(3.90972955608043,3.89654097983135,8.63061986166077));
#16988=CARTESIAN_POINT('Ctrl Pts',(4.02500868538324,3.91098444686735,8.63647234639467));
#16989=CARTESIAN_POINT('Ctrl Pts',(4.14068761087392,3.92030241782418,8.64232483112857));
#16990=CARTESIAN_POINT('Ctrl Pts',(4.25637714256894,3.92962124311384,8.64817785245674));
#16991=CARTESIAN_POINT('Ctrl Pts',(4.37246613148667,3.93381360495587,8.65403087378492));
#16992=CARTESIAN_POINT('Ctrl Pts',(4.48846650909144,3.9328698384525,8.65988389511309));
#16993=CARTESIAN_POINT('Ctrl Pts',(4.60450557506257,3.93192575718477,8.66573886853692));
#16994=CARTESIAN_POINT('Ctrl Pts',(4.72045555804647,3.92584214471091,8.67159384196076));
#16995=CARTESIAN_POINT('Ctrl Pts',(4.83583052496501,3.91466140476625,8.67744881538459));
#16996=CARTESIAN_POINT('Ctrl Pts',(4.95133625458897,3.903467992889,8.68331042466874));
#16997=CARTESIAN_POINT('Ctrl Pts',(5.06626525593137,3.88716596299063,8.68917203395289));
#16998=CARTESIAN_POINT('Ctrl Pts',(5.18013874012203,3.86584935828669,8.69503364323705));
#16999=CARTESIAN_POINT('Ctrl Pts',(5.29408901003933,3.84451837963965,8.70089920504739));
#17000=CARTESIAN_POINT('Ctrl Pts',(5.40698194423309,3.81816618682185,8.70676476685773));
#17001=CARTESIAN_POINT('Ctrl Pts',(5.51835262215726,3.78693707349053,8.71263032866807));
#17002=CARTESIAN_POINT('Ctrl Pts',(5.62988615132805,3.75566229553606,8.7185044673684));
#17003=CARTESIAN_POINT('Ctrl Pts',(5.73989259089843,3.71949649341352,8.72437860606873));
#17004=CARTESIAN_POINT('Ctrl Pts',(5.84792566853679,3.67863257681175,8.73025274476906));
#17005=CARTESIAN_POINT('Ctrl Pts',(5.87524547021817,3.66829875941166,8.73173821855034));
#17006=CARTESIAN_POINT('Ctrl Pts',(5.90243919400706,3.65766472835785,8.73322369233161));
#17007=CARTESIAN_POINT('Ctrl Pts',(5.92949987557082,3.64673406660543,8.73470916611288));
#17008=CARTESIAN_POINT('Ctrl Pts',(6.0365001068818,3.6035133024449,8.74058285550345));
#17009=CARTESIAN_POINT('Ctrl Pts',(6.14177469884634,3.55550726078617,8.74645654489402));
#17010=CARTESIAN_POINT('Ctrl Pts',(6.24486497997806,3.50287441949021,8.75233023428459));
#17011=CARTESIAN_POINT('Ctrl Pts',(6.34782216187183,3.45030953213706,8.75819634019034));
#17012=CARTESIAN_POINT('Ctrl Pts',(6.44860027668607,3.39312991089164,8.76406244609609));
#17013=CARTESIAN_POINT('Ctrl Pts',(6.5467592938117,3.33154257539215,8.76992855200183));
#17014=CARTESIAN_POINT('Ctrl Pts',(6.64481779735428,3.27001830453962,8.77578865108987));
#17015=CARTESIAN_POINT('Ctrl Pts',(6.74026218989035,3.20409551531674,8.7816487501779));
#17016=CARTESIAN_POINT('Ctrl Pts',(6.83267638869174,3.13402743298778,8.78750884926594));
#17017=CARTESIAN_POINT('Ctrl Pts',(6.92842468095541,3.06143145409922,8.79358036736005));
#17018=CARTESIAN_POINT('Ctrl Pts',(7.02091960413443,2.98438563480163,8.79965188545415));
#17019=CARTESIAN_POINT('Ctrl Pts',(7.10973026289912,2.90322135471075,8.80572340354826));
#17020=CARTESIAN_POINT('Ctrl Pts',(7.19534988371865,2.82497337206843,8.81157676714501));
#17021=CARTESIAN_POINT('Ctrl Pts',(7.27754510971338,2.74289809700929,8.81743013074176));
#17022=CARTESIAN_POINT('Ctrl Pts',(7.35596362117029,2.65733335465519,8.82328349433851));
#17023=CARTESIAN_POINT('Ctrl Pts',(7.43437035835158,2.57178145955925,8.82913597907241));
#17024=CARTESIAN_POINT('Ctrl Pts',(7.50900122945863,2.4827414434393,8.83498846380631));
#17025=CARTESIAN_POINT('Ctrl Pts',(7.57954183930544,2.39058689527223,8.84084094854022));
#17026=CARTESIAN_POINT('Ctrl Pts',(7.65008891677911,2.29842389777034,8.84669396986839));
#17027=CARTESIAN_POINT('Ctrl Pts',(7.716544736349,2.20314612863679,8.85254699119657));
#17028=CARTESIAN_POINT('Ctrl Pts',(7.77863658993046,2.10515847625905,8.85840001252475));
#17029=CARTESIAN_POINT('Ctrl Pts',(7.84074915234425,2.00713814310682,8.86425498594858));
#17030=CARTESIAN_POINT('Ctrl Pts',(7.89849463361993,1.90640647833885,8.8701099593724));
#17031=CARTESIAN_POINT('Ctrl Pts',(7.95164523700569,1.80339480280214,8.87596493279623));
#17032=CARTESIAN_POINT('Ctrl Pts',(8.00485607977335,1.70026637676274,8.88182654208039));
#17033=CARTESIAN_POINT('Ctrl Pts',(8.0534614608428,1.59485314960669,8.88768815136454));
#17034=CARTESIAN_POINT('Ctrl Pts',(8.09728084946573,1.48760843310034,8.89354976064869));
#17035=CARTESIAN_POINT('Ctrl Pts',(8.14112978582425,1.38029140069397,8.89941532245903));
#17036=CARTESIAN_POINT('Ctrl Pts',(8.18018616476053,1.27114080783443,8.90528088426938));
#17037=CARTESIAN_POINT('Ctrl Pts',(8.21431919951715,1.16062555386887,8.91114644607972));
#17038=CARTESIAN_POINT('Ctrl Pts',(8.24850214514226,1.04994869949638,8.91702058478005));
#17039=CARTESIAN_POINT('Ctrl Pts',(8.27774727498152,0.937903599778417,8.92289472348039));
#17040=CARTESIAN_POINT('Ctrl Pts',(8.30197476408481,0.824969839034305,8.92876886218072));
#17041=CARTESIAN_POINT('Ctrl Pts',(8.30810150056227,0.796410734599732,8.930254335962));
#17042=CARTESIAN_POINT('Ctrl Pts',(8.31390761712603,0.767794825730547,8.93173980974327));
#17043=CARTESIAN_POINT('Ctrl Pts',(8.31939234913042,0.73912990696419,8.93322528352454));
#17044=CARTESIAN_POINT('Ctrl Pts',(8.35134129734664,0.572154746727596,8.94187827238096));
#17045=CARTESIAN_POINT('Ctrl Pts',(8.37247152198213,0.403048461862582,8.95053126123738));
#17046=CARTESIAN_POINT('Ctrl Pts',(8.38256404026409,0.232954005888667,8.9591842500938));
#17047=CARTESIAN_POINT('Ctrl Pts',(8.38709427926657,0.156603533486162,8.96306832605088));
#17048=CARTESIAN_POINT('Ctrl Pts',(8.3894011415604,0.0800542813425082,8.96695240200797));
#17049=CARTESIAN_POINT('Ctrl Pts',(8.38946762642983,0.00341174640567755,
8.97083647796505));
#17050=CARTESIAN_POINT('',(8.38749085931107,-0.00196533283241418,6.47083650547062));
#17051=CARTESIAN_POINT('Ctrl Pts',(8.38946861452844,-0.00196662954943281,
6.47083652098856));
#17052=CARTESIAN_POINT('Ctrl Pts',(8.38940224472119,-0.134697483397542,
6.47751946712156));
#17053=CARTESIAN_POINT('Ctrl Pts',(8.3826120138021,-0.267199067172086,6.48420241325457));
#17054=CARTESIAN_POINT('Ctrl Pts',(8.36919582435493,-0.398821550545337,
6.49088535938758));
#17055=CARTESIAN_POINT('Ctrl Pts',(8.35619499781929,-0.526369024532905,
6.49736140266085));
#17056=CARTESIAN_POINT('Ctrl Pts',(8.33697255677429,-0.653090823469789,
6.50383744593412));
#17057=CARTESIAN_POINT('Ctrl Pts',(8.31166870378154,-0.778411885153282,
6.51031348920739));
#17058=CARTESIAN_POINT('Ctrl Pts',(8.28515220303635,-0.909738763572521,
6.51709988677027));
#17059=CARTESIAN_POINT('Ctrl Pts',(8.25195718178392,-1.03952699090368,6.52388628433315));
#17060=CARTESIAN_POINT('Ctrl Pts',(8.21230166279796,-1.1671378697206,6.53067268189603));
#17061=CARTESIAN_POINT('Ctrl Pts',(8.17264614381199,-1.29474874853751,6.53745907945891));
#17062=CARTESIAN_POINT('Ctrl Pts',(8.12653032448532,-1.42018201414962,6.54424547702179));
#17063=CARTESIAN_POINT('Ctrl Pts',(8.07422738824537,-1.5428266308384,6.55103187458467));
#17064=CARTESIAN_POINT('Ctrl Pts',(8.02895871678309,-1.64897667247336,6.55690556397521));
#17065=CARTESIAN_POINT('Ctrl Pts',(7.9789388073681,-1.75330944973437,6.56277925336574));
#17066=CARTESIAN_POINT('Ctrl Pts',(7.92433492144924,-1.85536942077644,6.56865294275628));
#17067=CARTESIAN_POINT('Ctrl Pts',(7.86980153427699,-1.95729762280764,6.57451904866199));
#17068=CARTESIAN_POINT('Ctrl Pts',(7.8106961333658,-2.05695849323454,6.58038515456771));
#17069=CARTESIAN_POINT('Ctrl Pts',(7.74723415481786,-2.15391606032251,6.58625126047342));
#17070=CARTESIAN_POINT('Ctrl Pts',(7.68383716052746,-2.25077434409698,6.59211135956142));
#17071=CARTESIAN_POINT('Ctrl Pts',(7.61609268697309,-2.34493448698235,6.59797145864942));
#17072=CARTESIAN_POINT('Ctrl Pts',(7.54426190722241,-2.43598534849183,6.60383155773742));
#17073=CARTESIAN_POINT('Ctrl Pts',(7.46983963680992,-2.53032111736513,6.60990307583154));
#17074=CARTESIAN_POINT('Ctrl Pts',(7.39103085717528,-2.62131861918634,6.61597459392566));
#17075=CARTESIAN_POINT('Ctrl Pts',(7.30817516591715,-2.70855340524727,6.62204611201978));
#17076=CARTESIAN_POINT('Ctrl Pts',(7.22829654586318,-2.79265377572805,6.6278994756165));
#17077=CARTESIAN_POINT('Ctrl Pts',(7.14465713571739,-2.87325684652984,6.63375283921322));
#17078=CARTESIAN_POINT('Ctrl Pts',(7.05760146765486,-2.95001685389883,6.63960620280993));
#17079=CARTESIAN_POINT('Ctrl Pts',(6.97055887070799,-3.02676533601099,6.6454586875438));
#17080=CARTESIAN_POINT('Ctrl Pts',(6.88010134556457,-3.09967162886433,6.65131117227766));
#17081=CARTESIAN_POINT('Ctrl Pts',(6.78660845297658,-3.16842857339228,6.65716365701153));
#17082=CARTESIAN_POINT('Ctrl Pts',(6.69310698834552,-3.23719182200896,6.66301667833968));
#17083=CARTESIAN_POINT('Ctrl Pts',(6.59656993587893,-3.30180472123734,6.66886969966782));
#17084=CARTESIAN_POINT('Ctrl Pts',(6.49740734899187,-3.36200239279869,6.67472272099596));
#17085=CARTESIAN_POINT('Ctrl Pts',(6.39821168946716,-3.42222014144598,6.68057769441975));
#17086=CARTESIAN_POINT('Ctrl Pts',(6.2963891072718,-3.47801952002286,6.68643266784353));
#17087=CARTESIAN_POINT('Ctrl Pts',(6.19237522048142,-3.52918106116189,6.69228764126732));
#17088=CARTESIAN_POINT('Ctrl Pts',(6.08824344731042,-3.58040058733635,6.69814925055144));
#17089=CARTESIAN_POINT('Ctrl Pts',(5.98191578343647,-3.62697160217744,6.70401085983556));
#17090=CARTESIAN_POINT('Ctrl Pts',(5.87384892563323,-3.66872231812591,6.70987246911968));
#17091=CARTESIAN_POINT('Ctrl Pts',(5.7657091975541,-3.71050118688877,6.71573803092999));
#17092=CARTESIAN_POINT('Ctrl Pts',(5.6558283309636,-3.74745315320136,6.72160359274029));
#17093=CARTESIAN_POINT('Ctrl Pts',(5.54467765156527,-3.7794564638098,6.7274691545506));
#17094=CARTESIAN_POINT('Ctrl Pts',(5.43336444261215,-3.81150657110769,6.7333432932509));
#17095=CARTESIAN_POINT('Ctrl Pts',(5.32077811532862,-3.83859348489971,6.7392174319512));
#17096=CARTESIAN_POINT('Ctrl Pts',(5.20739969924563,-3.86064660963103,6.7450915706515));
#17097=CARTESIAN_POINT('Ctrl Pts',(5.17872814872826,-3.86622348485688,6.74657704443311));
#17098=CARTESIAN_POINT('Ctrl Pts',(5.15000596460422,-3.8714787079246,6.74806251821472));
#17099=CARTESIAN_POINT('Ctrl Pts',(5.12124095466385,-3.87641166409274,6.74954799199633));
#17100=CARTESIAN_POINT('Ctrl Pts',(5.00750166434592,-3.89591699139477,6.75542168138689));
#17101=CARTESIAN_POINT('Ctrl Pts',(4.89271374425863,-3.91044465986001,6.76129537077745));
#17102=CARTESIAN_POINT('Ctrl Pts',(4.77735066381133,-3.91988826702964,6.76716906016801));
#17103=CARTESIAN_POINT('Ctrl Pts',(4.66213652793885,-3.92931968161522,6.77303516607376));
#17104=CARTESIAN_POINT('Ctrl Pts',(4.54634911647336,-3.93368005515109,6.7789012719795));
#17105=CARTESIAN_POINT('Ctrl Pts',(4.43047156984463,-3.93291407586061,6.78476737788524));
#17106=CARTESIAN_POINT('Ctrl Pts',(4.31471268034736,-3.93214888092316,6.79062747697327));
#17107=CARTESIAN_POINT('Ctrl Pts',(4.19886424995417,-3.92626777720655,6.79648757606131));
#17108=CARTESIAN_POINT('Ctrl Pts',(4.08341334764641,-3.91526734732079,6.80234767514934));
#17109=CARTESIAN_POINT('Ctrl Pts',(3.96379724016887,-3.90387004702073,6.80841919324345));
#17110=CARTESIAN_POINT('Ctrl Pts',(3.84460833632183,-3.88697702228025,6.81449071133756));
#17111=CARTESIAN_POINT('Ctrl Pts',(3.72638740277365,-3.86464354194477,6.82056222943167));
#17112=CARTESIAN_POINT('Ctrl Pts',(3.61241424184788,-3.84311252140626,6.82641559302841));
#17113=CARTESIAN_POINT('Ctrl Pts',(3.49934112920872,-3.81652536002302,6.83226895662515));
#17114=CARTESIAN_POINT('Ctrl Pts',(3.38764538702075,-3.78498412906591,6.8381223202219));
#17115=CARTESIAN_POINT('Ctrl Pts',(3.27596641557261,-3.75344763391849,6.84397480495579));
#17116=CARTESIAN_POINT('Ctrl Pts',(3.16566480085435,-3.71695866046953,6.84982728968969));
#17117=CARTESIAN_POINT('Ctrl Pts',(3.05720441453362,-3.67566964274603,6.85567977442358));
#17118=CARTESIAN_POINT('Ctrl Pts',(2.94873408385168,-3.63437683937396,6.86153279575175));
#17119=CARTESIAN_POINT('Ctrl Pts',(2.84210570329225,-3.58828326384537,6.86738581707992));
#17120=CARTESIAN_POINT('Ctrl Pts',(2.73776414600782,-3.53758989422856,6.87323883840809));
#17121=CARTESIAN_POINT('Ctrl Pts',(2.633387788799,-3.486879617394,6.8790938118319));
#17122=CARTESIAN_POINT('Ctrl Pts',(2.53130014286779,-3.43156667638692,6.88494878525572));
#17123=CARTESIAN_POINT('Ctrl Pts',(2.43192178106723,-3.37189814914743,6.89080375867953));
#17124=CARTESIAN_POINT('Ctrl Pts',(2.33243078665827,-3.31216199529646,6.89666536796368));
#17125=CARTESIAN_POINT('Ctrl Pts',(2.23565555956539,-3.2480606150503,6.90252697724783));
#17126=CARTESIAN_POINT('Ctrl Pts',(2.14198803388732,-3.17988464662193,6.90838858653197));
#17127=CARTESIAN_POINT('Ctrl Pts',(2.04825734750881,-3.11166270663737,6.91425414834231));
#17128=CARTESIAN_POINT('Ctrl Pts',(1.95763885738999,-3.0393609645716,6.92011971015264));
#17129=CARTESIAN_POINT('Ctrl Pts',(1.87049038389219,-2.96330947551498,6.92598527196297));
#17130=CARTESIAN_POINT('Ctrl Pts',(1.78321447795156,-2.8871467805285,6.93185941066329));
#17131=CARTESIAN_POINT('Ctrl Pts',(1.69941901290558,-2.80722367981402,6.93773354936362));
#17132=CARTESIAN_POINT('Ctrl Pts',(1.61942408143677,-2.72390611573943,6.94360768806394));
#17133=CARTESIAN_POINT('Ctrl Pts',(1.5991946691944,-2.70283646395339,6.94509316184529));
#17134=CARTESIAN_POINT('Ctrl Pts',(1.57920809482474,-2.68154989365626,6.94657863562664));
#17135=CARTESIAN_POINT('Ctrl Pts',(1.55946910757725,-2.66005263253832,6.94806410940799));
#17136=CARTESIAN_POINT('Ctrl Pts',(1.48141947692606,-2.57505063779408,6.95393779879857));
#17137=CARTESIAN_POINT('Ctrl Pts',(1.40698413988467,-2.48646903502784,6.95981148818915));
#17138=CARTESIAN_POINT('Ctrl Pts',(1.33650917954418,-2.39464800251476,6.96568517757973));
#17139=CARTESIAN_POINT('Ctrl Pts',(1.26612520899834,-2.30294551958089,6.9715512834855));
#17140=CARTESIAN_POINT('Ctrl Pts',(1.1996916958887,-2.20801224908382,6.97741738939126));
#17141=CARTESIAN_POINT('Ctrl Pts',(1.13751703415736,-2.11022419267781,6.98328349529703));
#17142=CARTESIAN_POINT('Ctrl Pts',(1.07540603848755,-2.01253626999577,6.98914359438508));
#17143=CARTESIAN_POINT('Ctrl Pts',(1.01754544013918,-1.9119997225896,6.99500369347313));
#17144=CARTESIAN_POINT('Ctrl Pts',(0.964202155499195,-1.80902198574683,
7.00086379256118));
#17145=CARTESIAN_POINT('Ctrl Pts',(0.908934366845095,-1.70232904708896,
7.00693531065528));
#17146=CARTESIAN_POINT('Ctrl Pts',(0.858516269715577,-1.59301580650514,
7.01300682874938));
#17147=CARTESIAN_POINT('Ctrl Pts',(0.813194576020285,-1.48156663623706,
7.01907834684348));
#17148=CARTESIAN_POINT('Ctrl Pts',(0.769501326999528,-1.37412192372434,
7.02493171044025));
#17149=CARTESIAN_POINT('Ctrl Pts',(0.730544717543736,-1.2646925468088,7.03078507403701));
#17150=CARTESIAN_POINT('Ctrl Pts',(0.696497737248281,-1.15373493685772,
7.03663843763377));
#17151=CARTESIAN_POINT('Ctrl Pts',(0.662455868992337,-1.04279398681836,
7.04249092236769));
#17152=CARTESIAN_POINT('Ctrl Pts',(0.633322285299647,-0.930325654857197,
7.04834340710161));
#17153=CARTESIAN_POINT('Ctrl Pts',(0.60922036390406,-0.816802371912494,
7.05419589183553));
#17154=CARTESIAN_POINT('Ctrl Pts',(0.585116232685891,-0.703268680406987,
7.06004891316371));
#17155=CARTESIAN_POINT('Ctrl Pts',(0.566044766663728,-0.588680249797354,
7.0659019344919));
#17156=CARTESIAN_POINT('Ctrl Pts',(0.552078252356837,-0.473519862606984,
7.07175495582009));
#17157=CARTESIAN_POINT('Ctrl Pts',(0.538107079947701,-0.358321067203494,
7.07760992924392));
#17158=CARTESIAN_POINT('Ctrl Pts',(0.529244294512347,-0.242550345822682,
7.08346490266776));
#17159=CARTESIAN_POINT('Ctrl Pts',(0.525510271062557,-0.126695052434562,
7.08931987609159));
#17160=CARTESIAN_POINT('Ctrl Pts',(0.521772015576805,-0.0107084519524598,
7.09518148537576));
#17161=CARTESIAN_POINT('Ctrl Pts',(0.523174137377517,0.105362498689283,
7.10104309465992));
#17162=CARTESIAN_POINT('Ctrl Pts',(0.529684882096246,0.221030896452396,
7.10690470394409));
#17163=CARTESIAN_POINT('Ctrl Pts',(0.536200017057955,0.336777290265595,
7.11277026575444));
#17164=CARTESIAN_POINT('Ctrl Pts',(0.547830592916088,0.452120180650977,
7.1186358275648));
#17165=CARTESIAN_POINT('Ctrl Pts',(0.564493239609307,0.566579962347384,
7.12450138937515));
#17166=CARTESIAN_POINT('Ctrl Pts',(0.581180251178772,0.681207112317725,
7.1303755280755));
#17167=CARTESIAN_POINT('Ctrl Pts',(0.602913941301662,0.794948172202939,
7.13624966677584));
#17168=CARTESIAN_POINT('Ctrl Pts',(0.629560331022235,0.907335784771954,
7.14212380547619));
#17169=CARTESIAN_POINT('Ctrl Pts',(0.636298767976385,0.935756777246556,
7.14360927925734));
#17170=CARTESIAN_POINT('Ctrl Pts',(0.64335112797796,0.964091304739122,7.14509475303849));
#17171=CARTESIAN_POINT('Ctrl Pts',(0.650714752463244,0.992332000327921,
7.14658022681964));
#17172=CARTESIAN_POINT('Ctrl Pts',(0.679831148568076,1.10399810724073,7.1524539162102));
#17173=CARTESIAN_POINT('Ctrl Pts',(0.713914860325132,1.21456763442555,7.15832760560076));
#17174=CARTESIAN_POINT('Ctrl Pts',(0.752867648195629,1.32356535166675,7.16420129499132));
#17175=CARTESIAN_POINT('Ctrl Pts',(0.791770144357513,1.43242234261505,7.17006740089707));
#17176=CARTESIAN_POINT('Ctrl Pts',(0.835529077210374,1.53971117384574,7.17593350680282));
#17177=CARTESIAN_POINT('Ctrl Pts',(0.883995672902733,1.64496886543632,7.18179961270856));
#17178=CARTESIAN_POINT('Ctrl Pts',(0.932412639418556,1.75011877449166,7.1876597117966));
#17179=CARTESIAN_POINT('Ctrl Pts',(0.985527508457297,1.85324130788033,7.19351981088463));
#17180=CARTESIAN_POINT('Ctrl Pts',(1.04314260686162,1.95389129912333,7.19937990997266));
#17181=CARTESIAN_POINT('Ctrl Pts',(1.10283632657537,2.0581725124311,7.20545142806677));
#17182=CARTESIAN_POINT('Ctrl Pts',(1.16736097046048,2.15979898249002,7.21152294616088));
#17183=CARTESIAN_POINT('Ctrl Pts',(1.236443261594,2.25830081254732,7.21759446425499));
#17184=CARTESIAN_POINT('Ctrl Pts',(1.30304337079782,2.35326339312984,7.22344782785173));
#17185=CARTESIAN_POINT('Ctrl Pts',(1.37387898643177,2.4453216437655,7.22930119144848));
#17186=CARTESIAN_POINT('Ctrl Pts',(1.44866034494117,2.53408276415449,7.23515455504522));
#17187=CARTESIAN_POINT('Ctrl Pts',(1.52343047528123,2.62283055735992,7.24100703977912));
#17188=CARTESIAN_POINT('Ctrl Pts',(1.6021449043803,2.70828188879732,7.24685952451301));
#17189=CARTESIAN_POINT('Ctrl Pts',(1.68447352905669,2.79007697388383,7.25271200924691));
#17190=CARTESIAN_POINT('Ctrl Pts',(1.76680970216264,2.87187955848148,7.25856503057508));
#17191=CARTESIAN_POINT('Ctrl Pts',(1.852760436483,2.95002493912258,7.26441805190325));
#17192=CARTESIAN_POINT('Ctrl Pts',(1.94195923328449,3.02419065188005,7.27027107323143));
#17193=CARTESIAN_POINT('Ctrl Pts',(2.03118777960722,3.09838110033492,7.27612604665524));
#17194=CARTESIAN_POINT('Ctrl Pts',(2.12366622498109,3.1685889776411,7.28198102007905));
#17195=CARTESIAN_POINT('Ctrl Pts',(2.21899608752842,3.23453296329393,7.28783599350286));
#17196=CARTESIAN_POINT('Ctrl Pts',(2.31443399423034,3.30055168798435,7.29369760278701));
#17197=CARTESIAN_POINT('Ctrl Pts',(2.41272942845047,3.36229664032718,7.29955921207116));
#17198=CARTESIAN_POINT('Ctrl Pts',(2.51345602739979,3.41953054899944,7.30542082135531));
#17199=CARTESIAN_POINT('Ctrl Pts',(2.61425054703449,3.47680305091663,7.31128638316564));
#17200=CARTESIAN_POINT('Ctrl Pts',(2.71747912873537,3.52955826466073,7.31715194497597));
#17201=CARTESIAN_POINT('Ctrl Pts',(2.82269356073474,3.5776062481749,7.32301750678631));
#17202=CARTESIAN_POINT('Ctrl Pts',(2.92806184203923,3.62572448962551,7.32889164548664));
#17203=CARTESIAN_POINT('Ctrl Pts',(3.03542138733468,3.66912160962264,7.33476578418696));
#17204=CARTESIAN_POINT('Ctrl Pts',(3.14430684140617,3.70765683293414,7.34063992288729));
#17205=CARTESIAN_POINT('Ctrl Pts',(3.1718421951735,3.71740176181774,7.34212539666862));
#17206=CARTESIAN_POINT('Ctrl Pts',(3.19947507240767,3.72683602521197,7.34361087044995));
#17207=CARTESIAN_POINT('Ctrl Pts',(3.22719784139387,3.73595786345043,7.34509634423129));
#17208=CARTESIAN_POINT('Ctrl Pts',(3.33681602255434,3.77202638593596,7.35097003362186));
#17209=CARTESIAN_POINT('Ctrl Pts',(3.44820556822354,3.80332636779926,7.35684372301242));
#17210=CARTESIAN_POINT('Ctrl Pts',(3.56091388213373,3.82968273367585,7.36271741240299));
#17211=CARTESIAN_POINT('Ctrl Pts',(3.67347667902218,3.85600507100802,7.36858351830874));
#17212=CARTESIAN_POINT('Ctrl Pts',(3.78735445951403,3.8773963921816,7.3744496242145));
#17213=CARTESIAN_POINT('Ctrl Pts',(3.90207752622745,3.89373072721205,7.38031573012025));
#17214=CARTESIAN_POINT('Ctrl Pts',(4.01668311798205,3.91004833609152,7.38617582920829));
#17215=CARTESIAN_POINT('Ctrl Pts',(4.13213186769417,3.92131920098428,7.39203592829633));
#17216=CARTESIAN_POINT('Ctrl Pts',(4.24794253797954,3.92746809921336,7.39789602738437));
#17217=CARTESIAN_POINT('Ctrl Pts',(4.36793139304236,3.93383883566267,7.40396754547847));
#17218=CARTESIAN_POINT('Ctrl Pts',(4.48830833646111,3.93471094705703,7.41003906357258));
#17219=CARTESIAN_POINT('Ctrl Pts',(4.608530364288,3.93005933464041,7.41611058166669));
#17220=CARTESIAN_POINT('Ctrl Pts',(4.724432718576,3.9255748583754,7.42196394526344));
#17221=CARTESIAN_POINT('Ctrl Pts',(4.84019064993848,3.91595678793296,7.42781730886019));
#17222=CARTESIAN_POINT('Ctrl Pts',(4.95531700162222,3.90123567312346,7.43367067245694));
#17223=CARTESIAN_POINT('Ctrl Pts',(5.07042606747164,3.88651676863981,7.43952315719084));
#17224=CARTESIAN_POINT('Ctrl Pts',(5.18490333250089,3.8666963956801,7.44537564192474));
#17225=CARTESIAN_POINT('Ctrl Pts',(5.29826751482728,3.84185689989402,7.45122812665864));
#17226=CARTESIAN_POINT('Ctrl Pts',(5.41164209112713,3.81701512665969,7.45708114798682));
#17227=CARTESIAN_POINT('Ctrl Pts',(5.52390297825591,3.78715340422412,7.46293416931499));
#17228=CARTESIAN_POINT('Ctrl Pts',(5.63458052479618,3.75240489358708,7.46878719064317));
#17229=CARTESIAN_POINT('Ctrl Pts',(5.74529498443553,3.71764479365072,7.47464216406698));
#17230=CARTESIAN_POINT('Ctrl Pts',(5.85442465947203,3.67799478834106,7.4804971374908));
#17231=CARTESIAN_POINT('Ctrl Pts',(5.96151713326215,3.63363721858571,7.48635211091462));
#17232=CARTESIAN_POINT('Ctrl Pts',(6.06873098261585,3.58922937522253,7.49221372019877));
#17233=CARTESIAN_POINT('Ctrl Pts',(6.17390264037431,3.54010347642467,7.49807532948292));
#17234=CARTESIAN_POINT('Ctrl Pts',(6.2766015902598,3.48648917114864,7.50393693876707));
#17235=CARTESIAN_POINT('Ctrl Pts',(6.37936979080141,3.43283871335283,7.50980250057741));
#17236=CARTESIAN_POINT('Ctrl Pts',(6.47966160683954,3.37469402921962,7.51566806238775));
#17237=CARTESIAN_POINT('Ctrl Pts',(6.57707444871111,3.31232878521906,7.52153362419809));
#17238=CARTESIAN_POINT('Ctrl Pts',(6.67462973204956,3.24987234793569,7.52740776289841));
#17239=CARTESIAN_POINT('Ctrl Pts',(6.76929730313146,3.1831832710523,7.53328190159875));
#17240=CARTESIAN_POINT('Ctrl Pts',(6.86070659393655,3.11257628061546,7.53915604029908));
#17241=CARTESIAN_POINT('Ctrl Pts',(6.88382251131349,3.0947209254016,7.54064151408037));
#17242=CARTESIAN_POINT('Ctrl Pts',(6.90673024244077,3.07661520573675,7.54212698786166));
#17243=CARTESIAN_POINT('Ctrl Pts',(6.92942417143176,3.05826458067886,7.54361246164295));
#17244=CARTESIAN_POINT('Ctrl Pts',(7.01799445038805,2.98664542733415,7.54940999574309));
#17245=CARTESIAN_POINT('Ctrl Pts',(7.10361700632803,2.91104090485563,7.55520752984322));
#17246=CARTESIAN_POINT('Ctrl Pts',(7.18590465504607,2.83172572555942,7.56100506394336));
#17247=CARTESIAN_POINT('Ctrl Pts',(7.26808555473045,2.752513439211,7.56679507709506));
#17248=CARTESIAN_POINT('Ctrl Pts',(7.34693984312148,2.66960035561418,7.57258509024676));
#17249=CARTESIAN_POINT('Ctrl Pts',(7.42211184837868,2.5833025618133,7.57837510339846));
#17250=CARTESIAN_POINT('Ctrl Pts',(7.49917778727706,2.49483052383362,7.58431099400353));
#17251=CARTESIAN_POINT('Ctrl Pts',(7.57237304629976,2.40280120236074,7.59024688460859));
#17252=CARTESIAN_POINT('Ctrl Pts',(7.64135273563583,2.30759729308818,7.59618277521365));
#17253=CARTESIAN_POINT('Ctrl Pts',(7.70851969504273,2.21489526483849,7.60196267545894));
#17254=CARTESIAN_POINT('Ctrl Pts',(7.77168962164127,2.11918379008929,7.60774257570424));
#17255=CARTESIAN_POINT('Ctrl Pts',(7.83058414359826,2.02085049286832,7.61352247594953));
#17256=CARTESIAN_POINT('Ctrl Pts',(7.88945761009809,1.92255235091234,7.61930030981517));
#17257=CARTESIAN_POINT('Ctrl Pts',(7.94405849151773,1.82163461327772,7.62507814368081));
#17258=CARTESIAN_POINT('Ctrl Pts',(7.99415212720601,1.71851326530083,7.63085597754645));
#17259=CARTESIAN_POINT('Ctrl Pts',(8.04424071635473,1.6154023059882,7.6366332293408));
#17260=CARTESIAN_POINT('Ctrl Pts',(8.0898227776142,1.51008856014189,7.64241048113515));
#17261=CARTESIAN_POINT('Ctrl Pts',(8.13071034258294,1.40301116780918,7.6481877329295));
#17262=CARTESIAN_POINT('Ctrl Pts',(8.17355698758577,1.2908032869873,7.65424179501204));
#17263=CARTESIAN_POINT('Ctrl Pts',(8.21124789224062,1.1766590224032,7.66029585709457));
#17264=CARTESIAN_POINT('Ctrl Pts',(8.24362463857504,1.0611041295459,7.66634991917711));
#17265=CARTESIAN_POINT('Ctrl Pts',(8.27455419731127,0.950714351370795,7.67213337458799));
#17266=CARTESIAN_POINT('Ctrl Pts',(8.30063436669227,0.839037768841426,7.67791682999887));
#17267=CARTESIAN_POINT('Ctrl Pts',(8.32177926695921,0.726544122041247,7.68370028540975));
#17268=CARTESIAN_POINT('Ctrl Pts',(8.34293597481183,0.613987657334305,7.68948697037691));
#17269=CARTESIAN_POINT('Ctrl Pts',(8.35915186896831,0.500613639988626,7.69527365534406));
#17270=CARTESIAN_POINT('Ctrl Pts',(8.370392900461,0.386897315654267,7.70106034031121));
#17271=CARTESIAN_POINT('Ctrl Pts',(8.38164815637142,0.273037094516247,7.70685434775802));
#17272=CARTESIAN_POINT('Ctrl Pts',(8.38791597036706,0.158834124771027,7.71264835520482));
#17273=CARTESIAN_POINT('Ctrl Pts',(8.38921435632238,0.0447637999217728,
7.71844236265162));
#17274=CARTESIAN_POINT('Ctrl Pts',(8.38939318969279,0.0290523078391149,
7.71924040107439));
#17275=CARTESIAN_POINT('Ctrl Pts',(8.38947782861755,0.0133433237550547,
7.72003843949716));
#17276=CARTESIAN_POINT('Ctrl Pts',(8.38946839700585,-0.00236191960000097,
7.72083647791993));
#17277=CARTESIAN_POINT('',(8.38897355277412,0.00337481364521056,5.22083644943854));
#17278=CARTESIAN_POINT('Ctrl Pts',(8.38695162751728,0.00337251368749724,
5.22083647796503));
#17279=CARTESIAN_POINT('Ctrl Pts',(8.37945749364734,-0.914486619189309,
5.2672027086816));
#17280=CARTESIAN_POINT('Ctrl Pts',(7.6012952590149,-3.15372830043783,5.37974097853539));
#17281=CARTESIAN_POINT('Ctrl Pts',(3.87112667961493,-4.61205589356117,5.55845128752638));
#17282=CARTESIAN_POINT('Ctrl Pts',(0.263602650510944,-2.00837153064666,
5.75696740493805));
#17283=CARTESIAN_POINT('Ctrl Pts',(0.495825964855193,2.43454127651753,5.95548352234969));
#17284=CARTESIAN_POINT('Ctrl Pts',(4.35513092859251,4.64794749265716,6.15399963976136));
#17285=CARTESIAN_POINT('Ctrl Pts',(7.77505612682836,2.87997114683924,6.32578395829981));
#17286=CARTESIAN_POINT('Ctrl Pts',(8.38045329723552,0.780274519420981,6.43139623770103));
#17287=CARTESIAN_POINT('Ctrl Pts',(8.38398528402403,-0.00196303439876837,
6.47083647796504));
#17288=CARTESIAN_POINT('Ctrl Pts',(7.19731080507723,-2.82068711164422,4.12982512801404));
#17289=CARTESIAN_POINT('Ctrl Pts',(7.11420835835676,-2.90143717084377,4.13568811753562));
#17290=CARTESIAN_POINT('Ctrl Pts',(7.02761824116375,-2.97843011948875,4.1415511070572));
#17291=CARTESIAN_POINT('Ctrl Pts',(6.93792639155195,-3.05136997774185,4.14741409657878));
#17292=CARTESIAN_POINT('Ctrl Pts',(6.84810427325219,-3.12441577404479,4.1532856015224));
#17293=CARTESIAN_POINT('Ctrl Pts',(6.75517176325591,-3.19339648709836,4.15915710646601));
#17294=CARTESIAN_POINT('Ctrl Pts',(6.65954368229696,-3.25805945498783,4.16502861140963));
#17295=CARTESIAN_POINT('Ctrl Pts',(6.63886022591221,-3.27204544804174,4.16629856282135));
#17296=CARTESIAN_POINT('Ctrl Pts',(6.61805075562464,-3.28582962195859,4.16756851423307));
#17297=CARTESIAN_POINT('Ctrl Pts',(6.59711961001077,-3.29940970790425,4.1688384656448));
#17298=CARTESIAN_POINT('Ctrl Pts',(6.50031035698119,-3.36221936011964,4.1747121550176));
#17299=CARTESIAN_POINT('Ctrl Pts',(6.40057314255717,-3.42086923425397,4.1805858443904));
#17300=CARTESIAN_POINT('Ctrl Pts',(6.29830101265205,-3.47507470832534,4.1864595337632));
#17301=CARTESIAN_POINT('Ctrl Pts',(6.19616092567059,-3.52921019803947,4.19232563965145));
#17302=CARTESIAN_POINT('Ctrl Pts',(6.09149279346964,-3.57891250725582,4.19819174553969));
#17303=CARTESIAN_POINT('Ctrl Pts',(5.98471871108655,-3.6239401409543,4.20405785142794));
#17304=CARTESIAN_POINT('Ctrl Pts',(5.878053963999,-3.66892166693144,4.20991795049874));
#17305=CARTESIAN_POINT('Ctrl Pts',(5.76928793453597,-3.70923787916653,4.21577804956954));
#17306=CARTESIAN_POINT('Ctrl Pts',(5.65886680768961,-3.74469341435269,4.22163814864034));
#17307=CARTESIAN_POINT('Ctrl Pts',(5.54446193803734,-3.7814281045091,4.22770966674101));
#17308=CARTESIAN_POINT('Ctrl Pts',(5.42828069101142,-3.81294455993941,4.23378118484168));
#17309=CARTESIAN_POINT('Ctrl Pts',(5.31084175137267,-3.83908014805784,4.23985270294235));
#17310=CARTESIAN_POINT('Ctrl Pts',(5.19762248713018,-3.86427666351018,4.24570606652268));
#17311=CARTESIAN_POINT('Ctrl Pts',(5.08323479251593,-3.88447223731615,4.251559430103));
#17312=CARTESIAN_POINT('Ctrl Pts',(4.96815752828476,-3.89957227894587,4.25741279368332));
#17313=CARTESIAN_POINT('Ctrl Pts',(4.85309754251115,-3.91467005335599,4.26326527840112));
#17314=CARTESIAN_POINT('Ctrl Pts',(4.73734860251363,-3.92467376311349,4.26911776311893));
#17315=CARTESIAN_POINT('Ctrl Pts',(4.62139708614469,-3.92954040078956,4.27497024783673));
#17316=CARTESIAN_POINT('Ctrl Pts',(4.50543493857151,-3.93440748467126,4.28082326914916));
#17317=CARTESIAN_POINT('Ctrl Pts',(4.38927059050865,-3.93413654283997,4.28667629046159));
#17318=CARTESIAN_POINT('Ctrl Pts',(4.27339212145814,-3.92873666942074,4.29252931177402));
#17319=CARTESIAN_POINT('Ctrl Pts',(4.15747500469308,-3.92333499503909,4.29838428518246));
#17320=CARTESIAN_POINT('Ctrl Pts',(4.04184436900636,-3.91280100684266,4.3042392585909));
#17321=CARTESIAN_POINT('Ctrl Pts',(3.92698415951086,-3.89719574709948,4.31009423199933));
#17322=CARTESIAN_POINT('Ctrl Pts',(3.81199377070867,-3.8815728007971,4.31595584126872));
#17323=CARTESIAN_POINT('Ctrl Pts',(3.69777596052368,-3.86086716666494,4.32181745053811));
#17324=CARTESIAN_POINT('Ctrl Pts',(3.58480555111573,-3.83519121383876,4.3276790598075));
#17325=CARTESIAN_POINT('Ctrl Pts',(3.47175896492413,-3.80949794752744,4.33354462160343));
#17326=CARTESIAN_POINT('Ctrl Pts',(3.35996185182716,-3.77882779792911,4.33941018339935));
#17327=CARTESIAN_POINT('Ctrl Pts',(3.24987324524777,-3.74334281468969,4.34527574519528));
#17328=CARTESIAN_POINT('Ctrl Pts',(3.13962366211244,-3.70780594369759,4.35114988388182));
#17329=CARTESIAN_POINT('Ctrl Pts',(3.03108795712803,-3.6674403315217,4.35702402256836));
#17330=CARTESIAN_POINT('Ctrl Pts',(2.92470466141453,-3.62245589146854,4.36289816125491));
#17331=CARTESIAN_POINT('Ctrl Pts',(2.89780205982261,-3.61108005976048,4.36438363518876));
#17332=CARTESIAN_POINT('Ctrl Pts',(2.87103697745075,-3.59940907998768,4.36586910912261));
#17333=CARTESIAN_POINT('Ctrl Pts',(2.84441623583233,-3.58744680003488,4.36735458305646));
#17334=CARTESIAN_POINT('Ctrl Pts',(2.73915557606051,-3.5401469352056,4.37322827239962));
#17335=CARTESIAN_POINT('Ctrl Pts',(2.63580313467552,-3.48813162622624,4.37910196174278));
#17336=CARTESIAN_POINT('Ctrl Pts',(2.53481115568846,-3.43157685636875,4.38497565108594));
#17337=CARTESIAN_POINT('Ctrl Pts',(2.43394956684899,-3.3750951040406,4.39084175694348));
#17338=CARTESIAN_POINT('Ctrl Pts',(2.33544273695223,-3.31408574620366,4.39670786280102));
#17339=CARTESIAN_POINT('Ctrl Pts',(2.23972241789224,-3.24877255587332,4.40257396865856));
#17340=CARTESIAN_POINT('Ctrl Pts',(2.14410011523251,-3.18352624542667,4.40843406769764));
#17341=CARTESIAN_POINT('Ctrl Pts',(2.05125898709741,-3.11398509999038,4.41429416673671));
#17342=CARTESIAN_POINT('Ctrl Pts',(1.96160507993493,-3.04041814399884,4.42015426577579));
#17343=CARTESIAN_POINT('Ctrl Pts',(1.86871666328278,-2.96419705920454,4.42622578388797));
#17344=CARTESIAN_POINT('Ctrl Pts',(1.77925017913452,-2.88365441584827,4.43229730200015));
#17345=CARTESIAN_POINT('Ctrl Pts',(1.69362347288065,-2.79913790413179,4.43836882011233));
#17346=CARTESIAN_POINT('Ctrl Pts',(1.61107340357164,-2.71765813917078,4.44422218365858));
#17347=CARTESIAN_POINT('Ctrl Pts',(1.53209224749404,-2.6324854749879,4.45007554720482));
#17348=CARTESIAN_POINT('Ctrl Pts',(1.45701908478339,-2.5439710235996,4.45592891075106));
#17349=CARTESIAN_POINT('Ctrl Pts',(1.38195719406189,-2.45546986236586,4.46178139543397));
#17350=CARTESIAN_POINT('Ctrl Pts',(1.31080239714504,-2.36362822660573,4.46763388011688));
#17351=CARTESIAN_POINT('Ctrl Pts',(1.24385450357439,-2.2688315087021,4.47348636479978));
#17352=CARTESIAN_POINT('Ctrl Pts',(1.17690047178557,-2.17402609921901,4.47933938607654));
#17353=CARTESIAN_POINT('Ctrl Pts',(1.11415434845501,-2.07626540647684,4.48519240735329));
#17354=CARTESIAN_POINT('Ctrl Pts',(1.05587308426051,-1.97596449751639,4.49104542863004));
#17355=CARTESIAN_POINT('Ctrl Pts',(0.997572382142501,-1.87563013627202,
4.49690040200206));
#17356=CARTESIAN_POINT('Ctrl Pts',(0.943739707656872,-1.77275423119346,
4.50275537537409));
#17357=CARTESIAN_POINT('Ctrl Pts',(0.894586117757878,-1.66777653674484,
4.5086103487461));
#17358=CARTESIAN_POINT('Ctrl Pts',(0.845376818580375,-1.56267986356792,
4.51447195797815));
#17359=CARTESIAN_POINT('Ctrl Pts',(0.800857364030778,-1.4554770208464,4.52033356721019));
#17360=CARTESIAN_POINT('Ctrl Pts',(0.761190735054206,-1.34662792173904,
4.52619517644224));
#17361=CARTESIAN_POINT('Ctrl Pts',(0.721497358579749,-1.23770542488845,
4.53206073820023));
#17362=CARTESIAN_POINT('Ctrl Pts',(0.686663447379408,-1.12713485430877,
4.53792629995823));
#17363=CARTESIAN_POINT('Ctrl Pts',(0.656801676251452,-1.01538978803684,
4.54379186171623));
#17364=CARTESIAN_POINT('Ctrl Pts',(0.626896239889432,-0.903481323068519,
4.54966600036426));
#17365=CARTESIAN_POINT('Ctrl Pts',(0.601977542229545,-0.790395336822605,
4.55554013901229));
#17366=CARTESIAN_POINT('Ctrl Pts',(0.582106923367081,-0.676614126435978,
4.56141427766032));
#17367=CARTESIAN_POINT('Ctrl Pts',(0.577081966551582,-0.647840706112964,
4.56289975192959));
#17368=CARTESIAN_POINT('Ctrl Pts',(0.572379575594817,-0.619022841674758,
4.56438522619885));
#17369=CARTESIAN_POINT('Ctrl Pts',(0.568000215107508,-0.590168351289692,
4.56587070046812));
#17370=CARTESIAN_POINT('Ctrl Pts',(0.550683857697303,-0.476075284540527,
4.57174438989032));
#17371=CARTESIAN_POINT('Ctrl Pts',(0.538364388507258,-0.361029421583703,
4.57761807931251));
#17372=CARTESIAN_POINT('Ctrl Pts',(0.531139093181675,-0.245506188830913,
4.58349176873471));
#17373=CARTESIAN_POINT('Ctrl Pts',(0.523923126390626,-0.130132107416246,
4.58935787467247));
#17374=CARTESIAN_POINT('Ctrl Pts',(0.521788279408659,-0.0142822904555608,
4.59522398061024));
#17375=CARTESIAN_POINT('Ctrl Pts',(0.524780570811782,0.101559148053415,
4.601090086548));
#17376=CARTESIAN_POINT('Ctrl Pts',(0.527769798146824,0.217281966412697,
4.6069501856684));
#17377=CARTESIAN_POINT('Ctrl Pts',(0.535875710330134,0.33299601283302,4.6128102847888));
#17378=CARTESIAN_POINT('Ctrl Pts',(0.549092365648309,0.448214242581623,
4.6186703839092));
#17379=CARTESIAN_POINT('Ctrl Pts',(0.562785847635657,0.567589282309495,
4.62474190199131));
#17380=CARTESIAN_POINT('Ctrl Pts',(0.58196583128496,0.686431603246408,4.63081342007342));
#17381=CARTESIAN_POINT('Ctrl Pts',(0.606566667743219,0.804201600485852,
4.63688493815552));
#17382=CARTESIAN_POINT('Ctrl Pts',(0.630283576667667,0.917740028469782,
4.64273830178528));
#17383=CARTESIAN_POINT('Ctrl Pts',(0.659038399718432,1.03028142638004,4.64859166541504));
#17384=CARTESIAN_POINT('Ctrl Pts',(0.692719913269095,1.14135052134503,4.6544450290448));
#17385=CARTESIAN_POINT('Ctrl Pts',(0.726396369654919,1.25240293966273,4.6602975138119));
#17386=CARTESIAN_POINT('Ctrl Pts',(0.764997925825997,1.36198309932832,4.666149998579));
#17387=CARTESIAN_POINT('Ctrl Pts',(0.808363263132728,1.46963014314666,4.6720024833461));
#17388=CARTESIAN_POINT('Ctrl Pts',(0.851732576459734,1.57728705675629,4.67785550470761));
#17389=CARTESIAN_POINT('Ctrl Pts',(0.899866384803132,1.68301011894143,4.68370852606913));
#17390=CARTESIAN_POINT('Ctrl Pts',(0.952555199468043,1.78635840023286,4.68956154743065));
#17391=CARTESIAN_POINT('Ctrl Pts',(1.00526158687103,1.88974115017363,4.69541652088792));
#17392=CARTESIAN_POINT('Ctrl Pts',(1.06252581387436,1.99074717642117,4.70127149434519));
#17393=CARTESIAN_POINT('Ctrl Pts',(1.12409276732383,2.08896073107578,4.70712646780246));
#17394=CARTESIAN_POINT('Ctrl Pts',(1.18572949900678,2.18728559817907,4.71298807712008));
#17395=CARTESIAN_POINT('Ctrl Pts',(1.25167847095215,2.28281132647617,4.71884968643769));
#17396=CARTESIAN_POINT('Ctrl Pts',(1.32164156803488,2.37515163849536,4.72471129575531));
#17397=CARTESIAN_POINT('Ctrl Pts',(1.3916518417479,2.46755421626525,4.73057685759914));
#17398=CARTESIAN_POINT('Ctrl Pts',(1.4656813671716,2.55676678356299,4.73644241944298));
#17399=CARTESIAN_POINT('Ctrl Pts',(1.54339327503609,2.64243792770661,4.74230798128681));
#17400=CARTESIAN_POINT('Ctrl Pts',(1.6212188167669,2.72823434407179,4.74818212002045));
#17401=CARTESIAN_POINT('Ctrl Pts',(1.70273719741743,2.81047871013839,4.7540562587541));
#17402=CARTESIAN_POINT('Ctrl Pts',(1.78757639195902,2.88885802347121,4.75993039748774));
#17403=CARTESIAN_POINT('Ctrl Pts',(1.80903083454441,2.90867886791542,4.76141587095175));
#17404=CARTESIAN_POINT('Ctrl Pts',(1.83069748965618,2.92825275158177,4.76290134441576));
#17405=CARTESIAN_POINT('Ctrl Pts',(1.85257003950644,2.94757504575836,4.76438681787977));
#17406=CARTESIAN_POINT('Ctrl Pts',(1.93905597614796,3.02397705290271,4.77026050726535));
#17407=CARTESIAN_POINT('Ctrl Pts',(2.02905141551935,3.09669665561652,4.77613419665092));
#17408=CARTESIAN_POINT('Ctrl Pts',(2.12220959255693,3.1653943708299,4.7820078860365));
#17409=CARTESIAN_POINT('Ctrl Pts',(2.21524749363605,3.23400339083902,4.78787399193727));
#17410=CARTESIAN_POINT('Ctrl Pts',(2.31143968238032,3.29860060683084,4.79374009783804));
#17411=CARTESIAN_POINT('Ctrl Pts',(2.41040430111351,3.35888490623179,4.7996062037388));
#17412=CARTESIAN_POINT('Ctrl Pts',(2.50926758133778,3.41910747527808,4.80546630282185));
#17413=CARTESIAN_POINT('Ctrl Pts',(2.61089729393848,3.47502569860976,4.8113264019049));
#17414=CARTESIAN_POINT('Ctrl Pts',(2.7148809503522,3.52638053751252,4.81718650098795));
#17415=CARTESIAN_POINT('Ctrl Pts',(2.82261609998951,3.57958814190542,4.82325801908393));
#17416=CARTESIAN_POINT('Ctrl Pts',(2.93287788661398,3.62789660396052,4.82932953717991));
#17417=CARTESIAN_POINT('Ctrl Pts',(3.04517728711491,3.67106856396499,4.83540105527589));
#17418=CARTESIAN_POINT('Ctrl Pts',(3.1534416802838,3.71268932089643,4.8412544188677));
#17419=CARTESIAN_POINT('Ctrl Pts',(3.2635993624148,3.74953617963213,4.84710778245952));
#17420=CARTESIAN_POINT('Ctrl Pts',(3.37519066260441,3.78144495231334,4.85296114605134));
#17421=CARTESIAN_POINT('Ctrl Pts',(3.48676520773655,3.81334893399992,4.85881363078035));
#17422=CARTESIAN_POINT('Ctrl Pts',(3.59977254580557,3.84031619033397,4.86466611550936));
#17423=CARTESIAN_POINT('Ctrl Pts',(3.71373796252527,3.86223244357308,4.87051860023837));
#17424=CARTESIAN_POINT('Ctrl Pts',(3.82771382834356,3.88415070623837,4.87637162156165));
#17425=CARTESIAN_POINT('Ctrl Pts',(3.94264754170268,3.90101696716596,4.88222464288493));
#17426=CARTESIAN_POINT('Ctrl Pts',(4.05805502030093,3.91276822929019,4.88807766420822));
#17427=CARTESIAN_POINT('Ctrl Pts',(4.17350098952296,3.92452341068737,4.89393263762719));
#17428=CARTESIAN_POINT('Ctrl Pts',(4.28942062738185,3.93116015924477,4.89978761104616));
#17429=CARTESIAN_POINT('Ctrl Pts',(4.40532627839294,3.93266746765628,4.90564258446514));
#17430=CARTESIAN_POINT('Ctrl Pts',(4.52136329357403,3.93417648440828,4.91150419374455));
#17431=CARTESIAN_POINT('Ctrl Pts',(4.637385876926,3.93054445212009,4.91736580302396));
#17432=CARTESIAN_POINT('Ctrl Pts',(4.75290782541861,3.92181247457841,4.92322741230336));
#17433=CARTESIAN_POINT('Ctrl Pts',(4.86850767121012,3.91307460900011,4.92909297410899));
#17434=CARTESIAN_POINT('Ctrl Pts',(4.98360580076896,3.8992299997122,4.93495853591461));
#17435=CARTESIAN_POINT('Ctrl Pts',(5.09772429923083,3.88037121644752,4.94082409772024));
#17436=CARTESIAN_POINT('Ctrl Pts',(5.21200966692894,3.86148485701594,4.94669823641595));
#17437=CARTESIAN_POINT('Ctrl Pts',(5.32531214201382,3.83756977586982,4.95257237511167));
#17438=CARTESIAN_POINT('Ctrl Pts',(5.43716702778179,3.80876890696206,4.95844651380739));
#17439=CARTESIAN_POINT('Ctrl Pts',(5.46545330325994,3.80148563715814,4.9599319876354));
#17440=CARTESIAN_POINT('Ctrl Pts',(5.49364709804283,3.79389016356313,4.96141746146341));
#17441=CARTESIAN_POINT('Ctrl Pts',(5.52174109764923,3.78598528579717,4.96290293529143));
#17442=CARTESIAN_POINT('Ctrl Pts',(5.63282715258497,3.75472872930564,4.96877662467622));
#17443=CARTESIAN_POINT('Ctrl Pts',(5.74272138899312,3.71852684366733,4.97465031406101));
#17444=CARTESIAN_POINT('Ctrl Pts',(5.85095055194696,3.67748698128469,4.9805240034458));
#17445=CARTESIAN_POINT('Ctrl Pts',(5.95903998088213,3.63650010522052,4.9863901093457));
#17446=CARTESIAN_POINT('Ctrl Pts',(6.06546822876711,3.59068781936645,4.9922562152456));
#17447=CARTESIAN_POINT('Ctrl Pts',(6.16977525966529,3.5402077657336,4.9981223211455));
#17448=CARTESIAN_POINT('Ctrl Pts',(6.27397548149021,3.48977940303377,5.00398242022755));
#17449=CARTESIAN_POINT('Ctrl Pts',(6.37605843714023,3.43469295874976,5.00984251930961));
#17450=CARTESIAN_POINT('Ctrl Pts',(6.47558284037743,3.37515462290689,5.01570261839166));
#17451=CARTESIAN_POINT('Ctrl Pts',(6.57869785717465,3.31346827965012,5.02177413648797));
#17452=CARTESIAN_POINT('Ctrl Pts',(6.67906580016466,3.24700291184717,5.02784565458427));
#17453=CARTESIAN_POINT('Ctrl Pts',(6.7762221100382,3.17604077449713,5.03391717268058));
#17454=CARTESIAN_POINT('Ctrl Pts',(6.86988751591982,3.10762836355058,5.03977053627116));
#17455=CARTESIAN_POINT('Ctrl Pts',(6.96056774764238,3.03503703141585,5.04562389986173));
#17456=CARTESIAN_POINT('Ctrl Pts',(7.04787564489083,2.95856403535989,5.05147726345231));
#17457=CARTESIAN_POINT('Ctrl Pts',(7.13517043315111,2.882102521468,5.05732974817995));
#17458=CARTESIAN_POINT('Ctrl Pts',(7.21909358303961,2.80176077466077,5.0631822329076));
#17459=CARTESIAN_POINT('Ctrl Pts',(7.29929171894275,2.71787575002653,5.06903471763525));
#17460=CARTESIAN_POINT('Ctrl Pts',(7.3794972079375,2.63398303426251,5.07488773895712));
#17461=CARTESIAN_POINT('Ctrl Pts',(7.45597671849276,2.54654669350122,5.08074076027899));
#17462=CARTESIAN_POINT('Ctrl Pts',(7.52841488805971,2.45593935459052,5.08659378160086));
#17463=CARTESIAN_POINT('Ctrl Pts',(7.60087721715508,2.36530179638255,5.09244875501837));
#17464=CARTESIAN_POINT('Ctrl Pts',(7.66929526724543,2.2714914595771,5.09830372843588));
#17465=CARTESIAN_POINT('Ctrl Pts',(7.73339542612834,2.1749121577389,5.10415870185339));
#17466=CARTESIAN_POINT('Ctrl Pts',(7.79756823430694,2.0782233956688,5.11002031113113));
#17467=CARTESIAN_POINT('Ctrl Pts',(7.8574131550048,1.97875974919543,5.11588192040887));
#17468=CARTESIAN_POINT('Ctrl Pts',(7.91270115276907,1.87695206129382,5.12174352968661));
#17469=CARTESIAN_POINT('Ctrl Pts',(7.96802643163604,1.77507572372099,5.12760909149051));
#17470=CARTESIAN_POINT('Ctrl Pts',(8.01878848855072,1.67085256789871,5.13347465329441));
#17471=CARTESIAN_POINT('Ctrl Pts',(8.06480602839219,1.56473437237006,5.13934021509831));
#17472=CARTESIAN_POINT('Ctrl Pts',(8.1108908571634,1.45846100601245,5.14521435379218));
#17473=CARTESIAN_POINT('Ctrl Pts',(8.15221717618438,1.35028745415923,5.15108849248606));
#17474=CARTESIAN_POINT('Ctrl Pts',(8.18865317747412,1.24068169095217,5.15696263117993));
#17475=CARTESIAN_POINT('Ctrl Pts',(8.19786724775897,1.21296418161894,5.15844810502098));
#17476=CARTESIAN_POINT('Ctrl Pts',(8.20676883607817,1.18515513589334,5.15993357886203));
#17477=CARTESIAN_POINT('Ctrl Pts',(8.21535632972457,1.15726221789226,5.16141905270308));
#17478=CARTESIAN_POINT('Ctrl Pts',(8.25675564365641,1.02279368535541,5.16858035033138));
#17479=CARTESIAN_POINT('Ctrl Pts',(8.29096263526288,0.886013494682714,5.17574164795968));
#17480=CARTESIAN_POINT('Ctrl Pts',(8.31775870655057,0.747617296727038,5.18290294558798));
#17481=CARTESIAN_POINT('Ctrl Pts',(8.34421505075933,0.610975719273807,5.18997345055125));
#17482=CARTESIAN_POINT('Ctrl Pts',(8.36344717827975,0.472758846995365,5.19704395551452));
#17483=CARTESIAN_POINT('Ctrl Pts',(8.37529061117875,0.333657027888083,5.20411446047779));
#17484=CARTESIAN_POINT('Ctrl Pts',(8.3846273168625,0.22399686802106,5.20968845447433));
#17485=CARTESIAN_POINT('Ctrl Pts',(8.38937290030595,0.113787124790175,5.21526244847088));
#17486=CARTESIAN_POINT('Ctrl Pts',(8.38946765781205,0.00337537569402483,
5.22083644246742));
#17487=CARTESIAN_POINT('Origin',(4.45646910621825,0.,0.));
#17488=CARTESIAN_POINT('Ctrl Pts',(6.97215211287823,3.02321484681493,3.97983001953316));
#17489=CARTESIAN_POINT('Ctrl Pts',(6.88323273247801,3.09720660246909,3.97396457891235));
#17490=CARTESIAN_POINT('Ctrl Pts',(6.79116193806773,3.16717580965372,3.96809913829154));
#17491=CARTESIAN_POINT('Ctrl Pts',(6.69635098528666,3.23286531854035,3.96223369767072));
#17492=CARTESIAN_POINT('Ctrl Pts',(6.66972216368927,3.25131502463075,3.96058631656864));
#17493=CARTESIAN_POINT('Ctrl Pts',(6.64287733814909,3.26942741083934,3.95893893546656));
#17494=CARTESIAN_POINT('Ctrl Pts',(6.61582595255236,3.28719744009848,3.95729155436448));
#17495=CARTESIAN_POINT('Ctrl Pts',(6.51937502447031,3.35055596226958,3.95141786498793));
#17496=CARTESIAN_POINT('Ctrl Pts',(6.41997255439171,3.40977140450338,3.94554417561138));
#17497=CARTESIAN_POINT('Ctrl Pts',(6.31800996521393,3.46455691687835,3.93967048623484));
#17498=CARTESIAN_POINT('Ctrl Pts',(6.21617901932698,3.51927169600501,3.93380438034361));
#17499=CARTESIAN_POINT('Ctrl Pts',(6.11179488822022,3.56956772563459,3.92793827445239));
#17500=CARTESIAN_POINT('Ctrl Pts',(6.005278288411,3.61520111711028,3.92207216856116));
#17501=CARTESIAN_POINT('Ctrl Pts',(5.89887076025228,3.66078778057049,3.91621206948815));
#17502=CARTESIAN_POINT('Ctrl Pts',(5.79033548429857,3.70172114098933,3.91035197041514));
#17503=CARTESIAN_POINT('Ctrl Pts',(5.68011752866518,3.73780330384614,3.90449187134213));
#17504=CARTESIAN_POINT('Ctrl Pts',(5.56592316024469,3.77518722895164,3.89842035324257));
#17505=CARTESIAN_POINT('Ctrl Pts',(5.4499228031593,3.80736309347115,3.89234883514302));
#17506=CARTESIAN_POINT('Ctrl Pts',(5.33263421003588,3.83416532127297,3.88627731704346));
#17507=CARTESIAN_POINT('Ctrl Pts',(5.21955989021131,3.86000452351564,3.88042395346285));
#17508=CARTESIAN_POINT('Ctrl Pts',(5.10528875315441,3.88084950155849,3.87457058988224));
#17509=CARTESIAN_POINT('Ctrl Pts',(4.9902991146134,3.89660294643127,3.86871722630163));
#17510=CARTESIAN_POINT('Ctrl Pts',(4.87532674138706,3.9123540259763,3.86286474158424));
#17511=CARTESIAN_POINT('Ctrl Pts',(4.7596364903955,3.92301503635694,3.85701225686685));
#17512=CARTESIAN_POINT('Ctrl Pts',(4.64371448735941,3.92854020817419,3.85115977214946));
#17513=CARTESIAN_POINT('Ctrl Pts',(4.52778185583898,3.93406588657518,3.84530675083815));
#17514=CARTESIAN_POINT('Ctrl Pts',(4.41161784273307,3.93445477066279,3.83945372952684));
#17515=CARTESIAN_POINT('Ctrl Pts',(4.29571057132544,3.92971318208583,3.83360070821553));
#17516=CARTESIAN_POINT('Ctrl Pts',(4.1797646426111,3.92497001209778,3.82774573480892));
#17517=CARTESIAN_POINT('Ctrl Pts',(4.06407603843998,3.91509298385434,3.8218907614023));
#17518=CARTESIAN_POINT('Ctrl Pts',(3.94912904284302,3.90014038979296,3.81603578799569));
#17519=CARTESIAN_POINT('Ctrl Pts',(3.83405176959896,3.88517084888785,3.81017417872917));
#17520=CARTESIAN_POINT('Ctrl Pts',(3.71971819247475,3.86511431384181,3.80431256946265));
#17521=CARTESIAN_POINT('Ctrl Pts',(3.60660376423607,3.84008045495111,3.79845096019613));
#17522=CARTESIAN_POINT('Ctrl Pts',(3.4934130621126,3.81502971554659,3.79258539840369));
#17523=CARTESIAN_POINT('Ctrl Pts',(3.38144354387121,3.78499507604044,3.78671983661125));
#17524=CARTESIAN_POINT('Ctrl Pts',(3.27115515598469,3.75013597611896,3.78085427481881));
#17525=CARTESIAN_POINT('Ctrl Pts',(3.16070549942915,3.71522590364493,3.77498013613662));
#17526=CARTESIAN_POINT('Ctrl Pts',(3.05194226577884,3.67547743292736,3.76910599745443));
#17527=CARTESIAN_POINT('Ctrl Pts',(2.9453051714037,3.63109798299575,3.76323185877225));
#17528=CARTESIAN_POINT('Ctrl Pts',(2.91833838813867,3.61987514337564,3.76174638483244));
#17529=CARTESIAN_POINT('Ctrl Pts',(2.89150744541438,3.60835637932971,3.76026091089263));
#17530=CARTESIAN_POINT('Ctrl Pts',(2.86481918651057,3.59654549993387,3.75877543695282));
#17531=CARTESIAN_POINT('Ctrl Pts',(2.7592915532681,3.54984428373059,3.75290174733985));
#17532=CARTESIAN_POINT('Ctrl Pts',(2.65564532388516,3.49841686024048,3.74702805772688));
#17533=CARTESIAN_POINT('Ctrl Pts',(2.55433373469968,3.44243664116246,3.74115436811391));
#17534=CARTESIAN_POINT('Ctrl Pts',(2.45315294827605,3.38652869779667,3.73528826198502));
#17535=CARTESIAN_POINT('Ctrl Pts',(2.35430116602657,3.32607984641507,3.72942215585613));
#17536=CARTESIAN_POINT('Ctrl Pts',(2.25821140394823,3.26131140408433,3.72355604972724));
#17537=CARTESIAN_POINT('Ctrl Pts',(2.16222003655062,3.19660928380567,3.7176959504156));
#17538=CARTESIAN_POINT('Ctrl Pts',(2.06898540420516,3.12759660024554,3.71183585110395));
#17539=CARTESIAN_POINT('Ctrl Pts',(1.97891507490576,3.05454006716678,3.7059757517923));
#17540=CARTESIAN_POINT('Ctrl Pts',(1.88559521845507,2.9788478249742,3.69990423378184));
#17541=CARTESIAN_POINT('Ctrl Pts',(1.79567269252324,2.89881465737932,3.69383271577137));
#17542=CARTESIAN_POINT('Ctrl Pts',(1.70956731060431,2.81478587556015,3.68776119776091));
#17543=CARTESIAN_POINT('Ctrl Pts',(1.62655575955935,2.73377631081778,3.68190783394074));
#17544=CARTESIAN_POINT('Ctrl Pts',(1.54709208861569,2.64905363449789,3.67605447012057));
#17545=CARTESIAN_POINT('Ctrl Pts',(1.47151736679682,2.56096702698902,3.67020110630041));
#17546=CARTESIAN_POINT('Ctrl Pts',(1.39595399227351,2.47289364539414,3.66434862134354));
#17547=CARTESIAN_POINT('Ctrl Pts',(1.32427867478326,2.38145765037765,3.65849613638667));
#17548=CARTESIAN_POINT('Ctrl Pts',(1.25679340810317,2.28704272520033,3.6526436514298));
#17549=CARTESIAN_POINT('Ctrl Pts',(1.18930195393846,2.19261914345359,3.64679062987935));
#17550=CARTESIAN_POINT('Ctrl Pts',(1.12600155453702,2.09521642472481,3.64093760832891));
#17551=CARTESIAN_POINT('Ctrl Pts',(1.06715151405735,1.99524816989482,3.63508458677846));
#17552=CARTESIAN_POINT('Ctrl Pts',(1.0082818459628,1.89524657373847,3.6292296131333));
#17553=CARTESIAN_POINT('Ctrl Pts',(0.953865697693562,1.79267809588955,3.62337463948814));
#17554=CARTESIAN_POINT('Ctrl Pts',(0.90411662065121,1.68798128493348,3.61751966584299));
#17555=CARTESIAN_POINT('Ctrl Pts',(0.854311159443263,1.58316581363882,3.61165805633998));
#17556=CARTESIAN_POINT('Ctrl Pts',(0.809183504447205,1.47621756801684,3.60579644683696));
#17557=CARTESIAN_POINT('Ctrl Pts',(0.768899246333945,1.36759552809771,3.59993483733395));
#17558=CARTESIAN_POINT('Ctrl Pts',(0.728587824258648,1.25890024356375,3.59406927530593));
#17559=CARTESIAN_POINT('Ctrl Pts',(0.693126428336241,1.14852930970523,3.5882037132779));
#17560=CARTESIAN_POINT('Ctrl Pts',(0.662630421520099,1.03695565695347,3.58233815124987));
#17561=CARTESIAN_POINT('Ctrl Pts',(0.632089822081742,0.925218856227082,
3.57646401233526));
#17562=CARTESIAN_POINT('Ctrl Pts',(0.606529192953198,0.812276228151098,
3.57058987342065));
#17563=CARTESIAN_POINT('Ctrl Pts',(0.58601261273831,0.698609713702123,3.56471573450604));
#17564=CARTESIAN_POINT('Ctrl Pts',(0.580824312153497,0.669865350011271,
3.56323026285108));
#17565=CARTESIAN_POINT('Ctrl Pts',(0.575958318644603,0.641074710892202,
3.56174479119612));
#17566=CARTESIAN_POINT('Ctrl Pts',(0.571415141220305,0.612245611706398,
3.56025931954116));
#17567=CARTESIAN_POINT('Ctrl Pts',(0.553451007686799,0.498252751851379,
3.55438563056146));
#17568=CARTESIAN_POINT('Ctrl Pts',(0.54047826906871,0.383278728455498,3.54851194158175));
#17569=CARTESIAN_POINT('Ctrl Pts',(0.532596909919817,0.267798407605622,
3.54263825260205));
#17570=CARTESIAN_POINT('Ctrl Pts',(0.524725726346264,0.152467182702637,
3.53677214710681));
#17571=CARTESIAN_POINT('Ctrl Pts',(0.521932877680621,0.0366313687176008,
3.53090604161158));
#17572=CARTESIAN_POINT('Ctrl Pts',(0.524267131582289,-0.0792251896119151,
3.52503993611635));
#17573=CARTESIAN_POINT('Ctrl Pts',(0.526598995237857,-0.194963112309522,
3.51917983743802));
#17574=CARTESIAN_POINT('Ctrl Pts',(0.53404751032907,-0.310721326493507,
3.51331973875968));
#17575=CARTESIAN_POINT('Ctrl Pts',(0.546609501711141,-0.426012761597005,
3.50745964008135));
#17576=CARTESIAN_POINT('Ctrl Pts',(0.559624702323609,-0.545463660036011,
3.50138812183336));
#17577=CARTESIAN_POINT('Ctrl Pts',(0.578129342378842,-0.664413012117803,
3.49531660358536));
#17578=CARTESIAN_POINT('Ctrl Pts',(0.602060839081441,-0.782320848646783,
3.48924508533737));
#17579=CARTESIAN_POINT('Ctrl Pts',(0.625132455800145,-0.89599215163021,
3.48339172214579));
#17580=CARTESIAN_POINT('Ctrl Pts',(0.65324756792712,-1.00869505654769,3.47753835895422));
#17581=CARTESIAN_POINT('Ctrl Pts',(0.686297653232049,-1.11995366649157,
3.47168499576264));
#17582=CARTESIAN_POINT('Ctrl Pts',(0.719342776190778,-1.23119557137296,
3.46583251143157));
#17583=CARTESIAN_POINT('Ctrl Pts',(0.757321281390588,-1.34099321653664,
3.4599800271005));
#17584=CARTESIAN_POINT('Ctrl Pts',(0.800074470503964,-1.44888483597551,
3.45412754276943));
#17585=CARTESIAN_POINT('Ctrl Pts',(0.842831579531272,-1.55678634767906,
3.44827452184131));
#17586=CARTESIAN_POINT('Ctrl Pts',(0.890364090523692,-1.66278110214558,
3.44242150091319));
#17587=CARTESIAN_POINT('Ctrl Pts',(0.942465022694893,-1.76642698716397,
3.43656847998508));
#17588=CARTESIAN_POINT('Ctrl Pts',(0.994583331562293,-1.8701074401446,3.43071350695817));
#17589=CARTESIAN_POINT('Ctrl Pts',(1.05127290588136,-1.97143709699979,3.42485853393127));
#17590=CARTESIAN_POINT('Ctrl Pts',(1.11228099811018,-2.06999876753311,3.41900356090437));
#17591=CARTESIAN_POINT('Ctrl Pts',(1.17335823525027,-2.16867214518124,3.41314195201039));
#17592=CARTESIAN_POINT('Ctrl Pts',(1.23876354184247,-2.26457092343504,3.40728034311642));
#17593=CARTESIAN_POINT('Ctrl Pts',(1.30820100167465,-2.35730713779801,3.40141873422244));
#17594=CARTESIAN_POINT('Ctrl Pts',(1.37768528373957,-2.45010588492963,3.39555317279886));
#17595=CARTESIAN_POINT('Ctrl Pts',(1.45120687163467,-2.53973750316626,3.38968761137527));
#17596=CARTESIAN_POINT('Ctrl Pts',(1.52843089759619,-2.62584867211522,3.38382204995169));
#17597=CARTESIAN_POINT('Ctrl Pts',(1.6057678441364,-2.71208575683858,3.37794791163015));
#17598=CARTESIAN_POINT('Ctrl Pts',(1.68681774542571,-2.79479182468583,3.37207377330861));
#17599=CARTESIAN_POINT('Ctrl Pts',(1.77121036033838,-2.87365176520671,3.36619963498708));
#17600=CARTESIAN_POINT('Ctrl Pts',(1.79255193144471,-2.89359420957591,3.36471415736789));
#17601=CARTESIAN_POINT('Ctrl Pts',(1.81410711560377,-2.91329090116227,3.3632286797487));
#17602=CARTESIAN_POINT('Ctrl Pts',(1.83586962136719,-2.93273717540429,3.36174320212951));
#17603=CARTESIAN_POINT('Ctrl Pts',(1.92192019416297,-3.00962919581136,3.35586951270257));
#17604=CARTESIAN_POINT('Ctrl Pts',(2.01150112941559,-3.08285880546186,3.34999582327562));
#17605=CARTESIAN_POINT('Ctrl Pts',(2.10426759595503,-3.15208455710113,3.34412213384868));
#17606=CARTESIAN_POINT('Ctrl Pts',(2.19691429221737,-3.22122093175143,3.33825602790999));
#17607=CARTESIAN_POINT('Ctrl Pts',(2.29273801262315,-3.28636348371889,3.33238992197131));
#17608=CARTESIAN_POINT('Ctrl Pts',(2.39135861600727,-3.34720893629611,3.32652381603263));
#17609=CARTESIAN_POINT('Ctrl Pts',(2.48987823309264,-3.40799208386971,3.32066371691511));
#17610=CARTESIAN_POINT('Ctrl Pts',(2.59118868695411,-3.46448666872914,3.31480361779758));
#17611=CARTESIAN_POINT('Ctrl Pts',(2.69487896704929,-3.51643131336056,3.30894351868005));
#17612=CARTESIAN_POINT('Ctrl Pts',(2.80231015513581,-3.57025000188531,3.3028720005983));
#17613=CARTESIAN_POINT('Ctrl Pts',(2.9122957669345,-3.61918397868074,3.29680048251654));
#17614=CARTESIAN_POINT('Ctrl Pts',(3.02434813546215,-3.66299311016559,3.29072896443478));
#17615=CARTESIAN_POINT('Ctrl Pts',(3.13237437344265,-3.70522814478098,3.2848756008172));
#17616=CARTESIAN_POINT('Ctrl Pts',(3.24232098597441,-3.74270011224495,3.27902223719963));
#17617=CARTESIAN_POINT('Ctrl Pts',(3.3537292421731,-3.7752422163678,3.27316887358205));
#17618=CARTESIAN_POINT('Ctrl Pts',(3.46512077073589,-3.80777943438538,3.26731638883054));
#17619=CARTESIAN_POINT('Ctrl Pts',(3.57797311012667,-3.83538814506056,3.26146390407902));
#17620=CARTESIAN_POINT('Ctrl Pts',(3.69181220282584,-3.85795137606662,3.25561141932751));
#17621=CARTESIAN_POINT('Ctrl Pts',(3.80566173297885,-3.88051667580563,3.24975839798493));
#17622=CARTESIAN_POINT('Ctrl Pts',(3.92049779100541,-3.89803549594168,3.24390537664236));
#17623=CARTESIAN_POINT('Ctrl Pts',(4.0358366602414,-3.91044209078609,3.23805235529978));
#17624=CARTESIAN_POINT('Ctrl Pts',(4.15121399715382,-3.92285282346262,3.2321973818648));
#17625=CARTESIAN_POINT('Ctrl Pts',(4.26709406817998,-3.93014789632348,3.22634240842981));
#17626=CARTESIAN_POINT('Ctrl Pts',(4.38298928822251,-3.93231353230478,3.22048743499483));
#17627=CARTESIAN_POINT('Ctrl Pts',(4.49901586051564,-3.93448162275452,3.2146258257043));
#17628=CARTESIAN_POINT('Ctrl Pts',(4.61505720279046,-3.93150866509864,3.20876421641378));
#17629=CARTESIAN_POINT('Ctrl Pts',(4.73062688638383,-3.92343300077555,3.20290260712326));
#17630=CARTESIAN_POINT('Ctrl Pts',(4.84627449940883,-3.91535189097653,3.19703704530932));
#17631=CARTESIAN_POINT('Ctrl Pts',(4.96144941101277,-3.90216127002637,3.19117148349538));
#17632=CARTESIAN_POINT('Ctrl Pts',(5.07567318823202,-3.88395099155711,3.18530592168144));
#17633=CARTESIAN_POINT('Ctrl Pts',(5.19006398855021,-3.8657140852069,3.17943178298154));
#17634=CARTESIAN_POINT('Ctrl Pts',(5.30350047565371,-3.84244295531576,3.17355764428164));
#17635=CARTESIAN_POINT('Ctrl Pts',(5.41551714845178,-3.81427789400406,3.16768350558174));
#17636=CARTESIAN_POINT('Ctrl Pts',(5.4438443332678,-3.80715541056296,3.16619803196044));
#17637=CARTESIAN_POINT('Ctrl Pts',(5.47208081224791,-3.79972020315359,3.16471255833915));
#17638=CARTESIAN_POINT('Ctrl Pts',(5.50021925512976,-3.7919750298027,3.16322708471785));
#17639=CARTESIAN_POINT('Ctrl Pts',(5.61148308992333,-3.76134939455417,3.15735328806591));
#17640=CARTESIAN_POINT('Ctrl Pts',(5.72158317202569,-3.72577155942982,3.15147949141397));
#17641=CARTESIAN_POINT('Ctrl Pts',(5.83004561867318,-3.68534619329475,3.14560569476203));
#17642=CARTESIAN_POINT('Ctrl Pts',(5.93835150618608,-3.64497917878768,3.13974037658857));
#17643=CARTESIAN_POINT('Ctrl Pts',(6.0450240781394,-3.59977869882972,3.13387505841512));
#17644=CARTESIAN_POINT('Ctrl Pts',(6.14960259571522,-3.5498997150263,3.12800974024167));
#17645=CARTESIAN_POINT('Ctrl Pts',(6.22734497102816,-3.51282029595477,3.12364953532253));
#17646=CARTESIAN_POINT('Ctrl Pts',(6.30393031702241,-3.47315647915035,3.11928933040339));
#17647=CARTESIAN_POINT('Ctrl Pts',(6.37917532067789,-3.43098962587739,3.11492912548425));
#17648=CARTESIAN_POINT('Ctrl Pts',(6.37998521093114,-3.43053564256519,2.93155396442585));
#17649=CARTESIAN_POINT('Ctrl Pts',(6.27882394601473,-3.48725719934643,2.93741792315029));
#17650=CARTESIAN_POINT('Ctrl Pts',(6.17524123718123,-3.53945011573742,2.94328188187473));
#17651=CARTESIAN_POINT('Ctrl Pts',(6.06968549222072,-3.58692373656496,2.94914584059916));
#17652=CARTESIAN_POINT('Ctrl Pts',(5.963964485873,-3.63447168358324,2.95501898012142));
#17653=CARTESIAN_POINT('Ctrl Pts',(5.85626465769322,-3.67728542650477,2.96089211964368));
#17654=CARTESIAN_POINT('Ctrl Pts',(5.74705199721677,-3.71522338513607,2.96676525916594));
#17655=CARTESIAN_POINT('Ctrl Pts',(5.67901496281762,-3.73885788122078,2.97042409316892));
#17656=CARTESIAN_POINT('Ctrl Pts',(5.61039108120681,-3.76060107992407,2.97408292717189));
#17657=CARTESIAN_POINT('Ctrl Pts',(5.54129499694641,-3.78042878345907,2.97774176117487));
#17658=CARTESIAN_POINT('Ctrl Pts',(5.43037195465575,-3.81225908500628,2.9836154514598));
#17659=CARTESIAN_POINT('Ctrl Pts',(5.31786206639191,-3.83925630756806,2.98948914174473));
#17660=CARTESIAN_POINT('Ctrl Pts',(5.20422432099473,-3.86126289428402,2.99536283202965));
#17661=CARTESIAN_POINT('Ctrl Pts',(5.0907332918741,-3.88324106857019,3.00122893886627));
#17662=CARTESIAN_POINT('Ctrl Pts',(4.97611770335411,-3.90024134288557,3.00709504570289));
#17663=CARTESIAN_POINT('Ctrl Pts',(4.86085174606983,-3.91215588653963,3.0129611525395));
#17664=CARTESIAN_POINT('Ctrl Pts',(4.74570381894656,-3.92405822992624,3.01882125259363));
#17665=CARTESIAN_POINT('Ctrl Pts',(4.62990725623192,-3.93088515895652,3.02468135264775));
#17666=CARTESIAN_POINT('Ctrl Pts',(4.51394583026764,-3.93257999615933,3.03054145270187));
#17667=CARTESIAN_POINT('Ctrl Pts',(4.39380080731622,-3.93433597883148,3.03661297044707));
#17668=CARTESIAN_POINT('Ctrl Pts',(4.27347924425192,-3.93058248633172,3.04268448819226));
#17669=CARTESIAN_POINT('Ctrl Pts',(4.15352470819547,-3.92131530123588,3.04875600593745));
#17670=CARTESIAN_POINT('Ctrl Pts',(4.03788020712725,-3.91238109139314,3.05460937058253));
#17671=CARTESIAN_POINT('Ctrl Pts',(3.92257725922248,-3.89832262491659,3.06046273522761));
#17672=CARTESIAN_POINT('Ctrl Pts',(3.80810148792087,-3.87918914614167,3.06631609987269));
#17673=CARTESIAN_POINT('Ctrl Pts',(3.69364290420577,-3.86005854009972,3.07216858568367));
#17674=CARTESIAN_POINT('Ctrl Pts',(3.5800116575329,-3.83585450493382,3.07802107149465));
#17675=CARTESIAN_POINT('Ctrl Pts',(3.4676855107552,-3.80667781685595,3.08387355730563));
#17676=CARTESIAN_POINT('Ctrl Pts',(3.35534906464776,-3.77749845352979,3.08972657973861));
#17677=CARTESIAN_POINT('Ctrl Pts',(3.24431835621806,-3.74334563478088,3.09557960217159));
#17678=CARTESIAN_POINT('Ctrl Pts',(3.13505757406079,-3.70437046779628,3.10143262460457));
#17679=CARTESIAN_POINT('Ctrl Pts',(3.02576035083068,-3.66538230166533,3.10728759915991));
#17680=CARTESIAN_POINT('Ctrl Pts',(2.91823461660142,-3.62156872786435,3.11314257371526));
#17681=CARTESIAN_POINT('Ctrl Pts',(2.81292544837541,-3.57312933501777,3.11899754827061));
#17682=CARTESIAN_POINT('Ctrl Pts',(2.7074969251424,-3.52463504206924,3.12485915872044));
#17683=CARTESIAN_POINT('Ctrl Pts',(2.60429035767502,-3.4715046385104,3.13072076917027));
#17684=CARTESIAN_POINT('Ctrl Pts',(2.50372712116051,-3.41398414463113,3.13658237962011));
#17685=CARTESIAN_POINT('Ctrl Pts',(2.40309607376402,-3.35642486405846,3.1424479426175));
#17686=CARTESIAN_POINT('Ctrl Pts',(2.30511225485916,-3.29446981882981,3.14831350561488));
#17687=CARTESIAN_POINT('Ctrl Pts',(2.21016744244267,-3.22840794127989,3.15417906861227));
#17688=CARTESIAN_POINT('Ctrl Pts',(2.11508379709062,-3.16224946483051,3.16005320852196));
#17689=CARTESIAN_POINT('Ctrl Pts',(2.02304835400144,-3.09197242093831,3.16592734843165));
#17690=CARTESIAN_POINT('Ctrl Pts',(1.93441931562576,-3.01790554089627,3.17180148834134));
#17691=CARTESIAN_POINT('Ctrl Pts',(1.91200663972036,-2.99917537064811,3.1732869517564));
#17692=CARTESIAN_POINT('Ctrl Pts',(1.88981161247733,-2.98020302289591,3.17477241517146));
#17693=CARTESIAN_POINT('Ctrl Pts',(1.86783963578063,-2.9609941683127,3.17625787858652));
#17694=CARTESIAN_POINT('Ctrl Pts',(1.78096001147519,-2.88504023423732,3.18213156511009));
#17695=CARTESIAN_POINT('Ctrl Pts',(1.69728140969937,-2.80513280674074,3.18800525163367));
#17696=CARTESIAN_POINT('Ctrl Pts',(1.61718504894668,-2.72157216368103,3.19387893815724));
#17697=CARTESIAN_POINT('Ctrl Pts',(1.53719210076511,-2.63811940593424,3.19974504115243));
#17698=CARTESIAN_POINT('Ctrl Pts',(1.46077247920051,-2.55102310807291,3.20561114414763));
#17699=CARTESIAN_POINT('Ctrl Pts',(1.38827385857003,-2.46062327923412,3.21147724714282));
#17700=CARTESIAN_POINT('Ctrl Pts',(1.31584947613255,-2.37031601932813,3.21733734328046));
#17701=CARTESIAN_POINT('Ctrl Pts',(1.24733836523732,-2.27671227749517,3.22319743941811));
#17702=CARTESIAN_POINT('Ctrl Pts',(1.18305041014706,-2.18018784516647,3.22905753555575));
#17703=CARTESIAN_POINT('Ctrl Pts',(1.11644304679787,-2.08018096320598,3.23512905474085));
#17704=CARTESIAN_POINT('Ctrl Pts',(1.05436963498423,-1.97703898989284,3.24120057392596));
#17705=CARTESIAN_POINT('Ctrl Pts',(0.997128392570591,-1.87121640301161,
3.24727209311106));
#17706=CARTESIAN_POINT('Ctrl Pts',(0.94194391223764,-1.76919617741396,3.25312545367651));
#17707=CARTESIAN_POINT('Ctrl Pts',(0.891250537100192,-1.66468505426169,
3.25897881424196));
#17708=CARTESIAN_POINT('Ctrl Pts',(0.845270148035759,-1.55811780184352,
3.2648321748074));
#17709=CARTESIAN_POINT('Ctrl Pts',(0.799296662970429,-1.45156655059955,
3.2706846564852));
#17710=CARTESIAN_POINT('Ctrl Pts',(0.758034920515486,-1.34296016320006,
3.276537138163));
#17711=CARTESIAN_POINT('Ctrl Pts',(0.721659237634693,-1.23275473859599,
3.2823896198408));
#17712=CARTESIAN_POINT('Ctrl Pts',(0.685280219724785,-1.12253921003591,
3.28824263809126));
#17713=CARTESIAN_POINT('Ctrl Pts',(0.653788281410874,-1.01072474518332,
3.29409565634172));
#17714=CARTESIAN_POINT('Ctrl Pts',(0.627308087424881,-0.897783321382907,
3.29994867459217));
#17715=CARTESIAN_POINT('Ctrl Pts',(0.600819061861613,-0.784804229772644,
3.30580364491983));
#17716=CARTESIAN_POINT('Ctrl Pts',(0.57934519858409,-0.670697833855755,
3.31165861524749));
#17717=CARTESIAN_POINT('Ctrl Pts',(0.562960062424372,-0.55594633364676,
3.31751358557514));
#17718=CARTESIAN_POINT('Ctrl Pts',(0.546556355840786,-0.441064777515275,
3.32337519175127));
#17719=CARTESIAN_POINT('Ctrl Pts',(0.535252946213132,-0.325537067002251,
3.3292367979274));
#17720=CARTESIAN_POINT('Ctrl Pts',(0.529071532504052,-0.209850656381681,
3.33509840410352));
#17721=CARTESIAN_POINT('Ctrl Pts',(0.522885950631409,-0.0940862377351004,
3.34096396279512));
#17722=CARTESIAN_POINT('Ctrl Pts',(0.521829245699624,0.0218366819985692,
3.34682952148671));
#17723=CARTESIAN_POINT('Ctrl Pts',(0.525871012423307,0.137432256241249,
3.3526950801783));
#17724=CARTESIAN_POINT('Ctrl Pts',(0.52991868921005,0.253196859816847,3.3585692157681));
#17725=CARTESIAN_POINT('Ctrl Pts',(0.539079683852553,0.368632752348954,
3.36444335135789));
#17726=CARTESIAN_POINT('Ctrl Pts',(0.553271946061515,0.483260725638233,
3.37031748694768));
#17727=CARTESIAN_POINT('Ctrl Pts',(0.556861010019064,0.512248854620215,
3.37180298996452));
#17728=CARTESIAN_POINT('Ctrl Pts',(0.560771584283068,0.541185375824925,
3.37328849298135));
#17729=CARTESIAN_POINT('Ctrl Pts',(0.56500183200524,0.570062675264016,3.37477399599818));
#17730=CARTESIAN_POINT('Ctrl Pts',(0.581728265213222,0.684243747394415,
3.380647686766));
#17731=CARTESIAN_POINT('Ctrl Pts',(0.603512162472252,0.797878197613152,
3.38652137753381));
#17732=CARTESIAN_POINT('Ctrl Pts',(0.630307859347065,0.91048290096033,3.39239506830163));
#17733=CARTESIAN_POINT('Ctrl Pts',(0.657068960535059,1.02294222137272,3.39826117559934));
#17734=CARTESIAN_POINT('Ctrl Pts',(0.68882889848895,1.13437404059641,3.40412728289704));
#17735=CARTESIAN_POINT('Ctrl Pts',(0.725490437660223,1.24430188248872,3.40999339019475));
#17736=CARTESIAN_POINT('Ctrl Pts',(0.762114435972227,1.3541171599406,3.41585349068769));
#17737=CARTESIAN_POINT('Ctrl Pts',(0.803629922034241,1.46243113375427,3.42171359118062));
#17738=CARTESIAN_POINT('Ctrl Pts',(0.849889105824581,1.56877968522046,3.42757369167355));
#17739=CARTESIAN_POINT('Ctrl Pts',(0.89781719982298,1.678965013919,3.4336452092459));
#17740=CARTESIAN_POINT('Ctrl Pts',(0.950837629724561,1.78703998878236,3.43971672681824));
#17741=CARTESIAN_POINT('Ctrl Pts',(1.00873016092378,1.89250763937686,3.44578824439059));
#17742=CARTESIAN_POINT('Ctrl Pts',(1.0645425856255,1.99418578654608,3.45164160941561));
#17743=CARTESIAN_POINT('Ctrl Pts',(1.12488280723949,2.09344035657259,3.45749497444064));
#17744=CARTESIAN_POINT('Ctrl Pts',(1.18950576965194,2.18984920885697,3.46334833946566));
#17745=CARTESIAN_POINT('Ctrl Pts',(1.25411902921493,2.28624358578236,3.46920082563404));
#17746=CARTESIAN_POINT('Ctrl Pts',(1.32301352100993,2.3797927514542,3.47505331180243));
#17747=CARTESIAN_POINT('Ctrl Pts',(1.39590047977422,2.47010297008576,3.48090579797081));
#17748=CARTESIAN_POINT('Ctrl Pts',(1.46879412135073,2.5604214690221,3.48675882073815));
#17749=CARTESIAN_POINT('Ctrl Pts',(1.5456806980991,2.64750010905138,3.49261184350549));
#17750=CARTESIAN_POINT('Ctrl Pts',(1.6262311850929,2.73097826974585,3.49846486627283));
#17751=CARTESIAN_POINT('Ctrl Pts',(1.70680853726662,2.81448427205731,3.50431984113898));
#17752=CARTESIAN_POINT('Ctrl Pts',(1.79105194282877,2.89438711009113,3.51017481600513));
#17753=CARTESIAN_POINT('Ctrl Pts',(1.87859608494008,2.97036356127767,3.51602979087128));
#17754=CARTESIAN_POINT('Ctrl Pts',(1.96623944702887,3.04642612195816,3.52189140159519));
#17755=CARTESIAN_POINT('Ctrl Pts',(2.05719070019636,3.11855314280891,3.52775301231909));
#17756=CARTESIAN_POINT('Ctrl Pts',(2.15105199544097,3.18646213618416,3.533614623043));
#17757=CARTESIAN_POINT('Ctrl Pts',(2.24497658203479,3.25441692108407,3.53948018629335));
#17758=CARTESIAN_POINT('Ctrl Pts',(2.34181477374659,3.31814778842023,3.54534574954369));
#17759=CARTESIAN_POINT('Ctrl Pts',(2.4411418263325,3.37741690570594,3.55121131279404));
#17760=CARTESIAN_POINT('Ctrl Pts',(2.54061411921397,3.43677268884842,3.55708545292368));
#17761=CARTESIAN_POINT('Ctrl Pts',(2.64258217373584,3.49165350630103,3.56295959305331));
#17762=CARTESIAN_POINT('Ctrl Pts',(2.74659882669214,3.5418685220083,3.56883373318295));
#17763=CARTESIAN_POINT('Ctrl Pts',(2.77290269104623,3.55456695946195,3.57031919325857));
#17764=CARTESIAN_POINT('Ctrl Pts',(2.79933747508719,3.56696726943899,3.5718046533342));
#17765=CARTESIAN_POINT('Ctrl Pts',(2.82589578559808,3.57906686806516,3.57329011340983));
#17766=CARTESIAN_POINT('Ctrl Pts',(2.93091056805809,3.62691014925051,3.57916380280099));
#17767=CARTESIAN_POINT('Ctrl Pts',(3.03820771881232,3.6702072774082,3.58503749219215));
#17768=CARTESIAN_POINT('Ctrl Pts',(3.14735650930925,3.70873471801559,3.59091118158331));
#17769=CARTESIAN_POINT('Ctrl Pts',(3.25636437852917,3.74721241610082,3.59677728749319));
#17770=CARTESIAN_POINT('Ctrl Pts',(3.36721874726458,3.78093253684036,3.60264339340306));
#17771=CARTESIAN_POINT('Ctrl Pts',(3.47946651680597,3.80971848569966,3.60850949931294));
#17772=CARTESIAN_POINT('Ctrl Pts',(3.59159934612842,3.83847495813125,3.61436959840861));
#17773=CARTESIAN_POINT('Ctrl Pts',(3.70512234036981,3.86230720655599,3.62022969750427));
#17774=CARTESIAN_POINT('Ctrl Pts',(3.81956537878968,3.88108781683533,3.62608979659993));
#17775=CARTESIAN_POINT('Ctrl Pts',(3.93813726076493,3.90054598865784,3.6321613146925));
#17776=CARTESIAN_POINT('Ctrl Pts',(4.05769640058846,3.91458098686229,3.63823283278506));
#17777=CARTESIAN_POINT('Ctrl Pts',(4.17770579854166,3.92310846374316,3.64430435087763));
#17778=CARTESIAN_POINT('Ctrl Pts',(4.29340316327078,3.93132954158983,3.65015771449077));
#17779=CARTESIAN_POINT('Ctrl Pts',(4.40951853927424,3.93443203428057,3.65601107810392));
#17780=CARTESIAN_POINT('Ctrl Pts',(4.5255643514418,3.93239301788205,3.66186444171707));
#17781=CARTESIAN_POINT('Ctrl Pts',(4.64159273978531,3.93035430763386,3.6677169264706));
#17782=CARTESIAN_POINT('Ctrl Pts',(4.75755117209072,3.92317563053372,3.67356941122413));
#17783=CARTESIAN_POINT('Ctrl Pts',(4.87295224688062,3.91088619030828,3.67942189597767));
#17784=CARTESIAN_POINT('Ctrl Pts',(4.98836390246322,3.8985956232994,3.6852749173287));
#17785=CARTESIAN_POINT('Ctrl Pts',(5.10321768809874,3.88119340540197,3.69112793867973));
#17786=CARTESIAN_POINT('Ctrl Pts',(5.2170322042534,3.85876052300569,3.69698096003076));
#17787=CARTESIAN_POINT('Ctrl Pts',(5.33088467980967,3.8363201587976,3.70283593348066));
#17788=CARTESIAN_POINT('Ctrl Pts',(5.443696791525,3.80884587365829,3.70869090693055));
#17789=CARTESIAN_POINT('Ctrl Pts',(5.55499889138541,3.77646942409185,3.71454588038045));
#17790=CARTESIAN_POINT('Ctrl Pts',(5.66642713796823,3.7440562799527,3.72040748969536));
#17791=CARTESIAN_POINT('Ctrl Pts',(5.77634155990948,3.70672999745012,3.72626909901028));
#17792=CARTESIAN_POINT('Ctrl Pts',(5.88428910307584,3.66467175290961,3.73213070832519));
#17793=CARTESIAN_POINT('Ctrl Pts',(5.99230943611389,3.62258514816623,3.73799627016906));
#17794=CARTESIAN_POINT('Ctrl Pts',(6.0983598724473,3.57576039425805,3.74386183201292));
#17795=CARTESIAN_POINT('Ctrl Pts',(6.20201030185977,3.52442547577877,3.74972739385679));
#17796=CARTESIAN_POINT('Ctrl Pts',(6.30581229368861,3.47301549302495,3.75560153259447));
#17797=CARTESIAN_POINT('Ctrl Pts',(6.40720691435273,3.41708238258832,3.76147567133214));
#17798=CARTESIAN_POINT('Ctrl Pts',(6.50579139157662,3.35689844510279,3.76734981006982));
#17799=CARTESIAN_POINT('Ctrl Pts',(6.5307217929916,3.341678911942,3.76883528365371));
#17800=CARTESIAN_POINT('Ctrl Pts',(6.55547264511292,3.32618774324588,3.7703207572376));
#17801=CARTESIAN_POINT('Ctrl Pts',(6.58003776858831,3.31042975098398,3.77180623082149));
#17802=CARTESIAN_POINT('Ctrl Pts',(6.59622194482155,3.30004795403904,3.77278490150863));
#17803=CARTESIAN_POINT('Ctrl Pts',(6.61233446581222,3.28954459824748,3.77376357219578));
#17804=CARTESIAN_POINT('Ctrl Pts',(6.62837333988161,3.27892070654281,3.77474224288293));
#17805=CARTESIAN_POINT('Origin',(4.45646910621825,0.,0.));
#17806=CARTESIAN_POINT('Ctrl Pts',(6.37692902980906,3.42691262734843,2.69315322924027));
#17807=CARTESIAN_POINT('Ctrl Pts',(5.65097596260216,3.82742863485321,2.6513283969878));
#17808=CARTESIAN_POINT('Ctrl Pts',(3.45307807194487,4.29849211691197,2.54333152559812));
#17809=CARTESIAN_POINT('Ctrl Pts',(0.275078285875853,2.03215589035587,2.36916261507124));
#17810=CARTESIAN_POINT('Ctrl Pts',(0.482062492976864,-2.41200736048335,
2.17064649765957));
#17811=CARTESIAN_POINT('Ctrl Pts',(3.73790413319295,-4.3039644467813,2.00262135099753));
#17812=CARTESIAN_POINT('Ctrl Pts',(5.75771551529821,-3.77032809480342,1.90076824347269));
#17813=CARTESIAN_POINT('Ctrl Pts',(6.37611478183885,-3.42549916664848,1.86508717508508));
#17814=CARTESIAN_POINT('Ctrl Pts',(6.37607929534711,-3.42544344211231,1.6817486560154));
#17815=CARTESIAN_POINT('Ctrl Pts',(5.77024621859546,-3.76371820199713,1.71671412291191));
#17816=CARTESIAN_POINT('Ctrl Pts',(3.77067693841887,-4.30358028239296,1.81785162894564));
#17817=CARTESIAN_POINT('Ctrl Pts',(0.508467943610061,-2.45499576926686,
1.98516117411659));
#17818=CARTESIAN_POINT('Ctrl Pts',(0.253275128055896,1.9866819812542,2.18367729152824));
#17819=CARTESIAN_POINT('Ctrl Pts',(3.41948173903076,4.29681960175239,2.35856292813192));
#17820=CARTESIAN_POINT('Ctrl Pts',(5.63863432548647,3.83414340656477,2.46727652559838));
#17821=CARTESIAN_POINT('Ctrl Pts',(6.3770723437125,3.42716806216871,2.50981808392762));
#17822=CARTESIAN_POINT('Origin',(4.45646910621825,0.,0.));
#17823=CARTESIAN_POINT('Ctrl Pts',(6.37730370004212,3.42771650614551,1.44343144191858));
#17824=CARTESIAN_POINT('Ctrl Pts',(5.99388198929395,3.64655365578385,1.42114830395004));
#17825=CARTESIAN_POINT('Ctrl Pts',(4.33567752240144,4.26502542083611,1.33269312684427));
#17826=CARTESIAN_POINT('Ctrl Pts',(1.04993737828694,3.16381092564229,1.17806591060129));
#17827=CARTESIAN_POINT('Ctrl Pts',(-0.0487366697561428,-1.1475464932117,
0.979549793189644));
#17828=CARTESIAN_POINT('Ctrl Pts',(2.81174385334673,-4.22821688899241,0.791955857486359));
#17829=CARTESIAN_POINT('Ctrl Pts',(5.42295440143473,-3.95757168087368,0.670533960920302));
#17830=CARTESIAN_POINT('Ctrl Pts',(6.37917532067772,-3.43420595741613,0.615284103491462));
#17831=CARTESIAN_POINT('Ctrl Pts',(6.38006015424921,-3.4304936204481,0.431770922268101));
#17832=CARTESIAN_POINT('Ctrl Pts',(6.27895466275247,-3.48718680803797,0.437639464367201));
#17833=CARTESIAN_POINT('Ctrl Pts',(6.17523350067364,-3.53946657277982,0.443508006466302));
#17834=CARTESIAN_POINT('Ctrl Pts',(6.06931927524152,-3.58708841991407,0.449376548565403));
#17835=CARTESIAN_POINT('Ctrl Pts',(5.95939934748487,-3.63651133714051,0.455467040384969));
#17836=CARTESIAN_POINT('Ctrl Pts',(5.8471175673446,-3.68091679339533,0.461557532204536));
#17837=CARTESIAN_POINT('Ctrl Pts',(5.73297491792037,-3.72008358947628,0.467648024024102));
#17838=CARTESIAN_POINT('Ctrl Pts',(5.62312163480198,-3.75777853663603,0.473509641268489));
#17839=CARTESIAN_POINT('Ctrl Pts',(5.51154524410124,-3.79062130430239,0.479371258512876));
#17840=CARTESIAN_POINT('Ctrl Pts',(5.39871211440115,-3.8184639730565,0.485232875757263));
#17841=CARTESIAN_POINT('Ctrl Pts',(5.28589743439592,-3.84630208916952,0.491093534550441));
#17842=CARTESIAN_POINT('Ctrl Pts',(5.17182682369662,-3.86914163356721,0.49695419334362));
#17843=CARTESIAN_POINT('Ctrl Pts',(5.05697990829913,-3.88688509948315,0.502814852136798));
#17844=CARTESIAN_POINT('Ctrl Pts',(4.94212422200554,-3.90462992047333,0.508675958510386));
#17845=CARTESIAN_POINT('Ctrl Pts',(4.82649252014119,-3.91727782647895,0.514537064883973));
#17846=CARTESIAN_POINT('Ctrl Pts',(4.71057198396183,-3.92478288922106,0.52039817125756));
#17847=CARTESIAN_POINT('Ctrl Pts',(4.59461478773703,-3.93229032545065,0.526261131214931));
#17848=CARTESIAN_POINT('Ctrl Pts',(4.47836898628299,-3.93465165759226,0.532124091172302));
#17849=CARTESIAN_POINT('Ctrl Pts',(4.3623235183463,-3.93187304071282,0.537987051129672));
#17850=CARTESIAN_POINT('Ctrl Pts',(4.24614968162425,-3.92909135014441,0.543856496657412));
#17851=CARTESIAN_POINT('Ctrl Pts',(4.13017703269396,-3.92115837136354,0.549725942185151));
#17852=CARTESIAN_POINT('Ctrl Pts',(4.01489124968035,-3.90813229006074,0.555595387712891));
#17853=CARTESIAN_POINT('Ctrl Pts',(3.8995298288338,-3.89509766247811,0.561468684124309));
#17854=CARTESIAN_POINT('Ctrl Pts',(3.78485657719902,-3.87696334197444,0.567341980535728));
#17855=CARTESIAN_POINT('Ctrl Pts',(3.67134713414353,-3.85383866929656,0.573215276947146));
#17856=CARTESIAN_POINT('Ctrl Pts',(3.55767425096559,-3.83068069983533,0.579097030208134));
#17857=CARTESIAN_POINT('Ctrl Pts',(3.44516891911741,-3.80251813613975,0.584978783469122));
#17858=CARTESIAN_POINT('Ctrl Pts',(3.33429186531407,-3.76951021221547,0.59086053673011));
#17859=CARTESIAN_POINT('Ctrl Pts',(3.30483516258775,-3.76074099830421,0.592423141898406));
#17860=CARTESIAN_POINT('Ctrl Pts',(3.27549327419337,-3.75163005928345,0.593985747066702));
#17861=CARTESIAN_POINT('Ctrl Pts',(3.24627458536827,-3.74218094454353,0.595548352234998));
#17862=CARTESIAN_POINT('Ctrl Pts',(3.13625460306234,-3.7066012700853,0.601432182067205));
#17863=CARTESIAN_POINT('Ctrl Pts',(3.02762898411309,-3.66610869725488,0.607316011899411));
#17864=CARTESIAN_POINT('Ctrl Pts',(2.9208675596608,-3.62083096681002,0.613199841731618));
#17865=CARTESIAN_POINT('Ctrl Pts',(2.81424037276223,-3.57561016677616,0.619076273471047));
#17866=CARTESIAN_POINT('Ctrl Pts',(2.7094730940747,-3.52561633477818,0.624952705210476));
#17867=CARTESIAN_POINT('Ctrl Pts',(2.60702018232466,-3.47102689098037,0.630829136949905));
#17868=CARTESIAN_POINT('Ctrl Pts',(2.50466900473832,-3.41649165365962,0.636699733483107));
#17869=CARTESIAN_POINT('Ctrl Pts',(2.40462798357623,-3.35737007477141,0.64257033001631));
#17870=CARTESIAN_POINT('Ctrl Pts',(2.30733077539245,-3.29388728328328,0.648440926549512));
#17871=CARTESIAN_POINT('Ctrl Pts',(2.20676771144991,-3.22827364298628,0.65450857417856));
#17872=CARTESIAN_POINT('Ctrl Pts',(2.10913631219929,-3.15800103645049,0.660576221807607));
#17873=CARTESIAN_POINT('Ctrl Pts',(2.0148871533803,-3.08336935309022,0.666643869436655));
#17874=CARTESIAN_POINT('Ctrl Pts',(1.92379782053678,-3.01123979425424,0.672508091265106));
#17875=CARTESIAN_POINT('Ctrl Pts',(1.83586791850928,-2.93503904215122,0.678372313093558));
#17876=CARTESIAN_POINT('Ctrl Pts',(1.75147329799903,-2.85508085306116,0.68423653492201));
#17877=CARTESIAN_POINT('Ctrl Pts',(1.66708967288883,-2.77513308136821,0.690099992727061));
#17878=CARTESIAN_POINT('Ctrl Pts',(1.58624071202294,-2.69142912907891,0.695963450532113));
#17879=CARTESIAN_POINT('Ctrl Pts',(1.50926687912181,-2.60432103101707,0.701826908337165));
#17880=CARTESIAN_POINT('Ctrl Pts',(1.43228464761449,-2.5172034286005,0.707691005903433));
#17881=CARTESIAN_POINT('Ctrl Pts',(1.35917865723167,-2.42668125024711,0.713555103469702));
#17882=CARTESIAN_POINT('Ctrl Pts',(1.29024994083508,-2.33314062944356,0.719419201035971));
#17883=CARTESIAN_POINT('Ctrl Pts',(1.22129720254228,-2.23956740940994,0.725285342260536));
#17884=CARTESIAN_POINT('Ctrl Pts',(1.15652487732791,-2.14297398598627,0.731151483485101));
#17885=CARTESIAN_POINT('Ctrl Pts',(1.09619102868573,-2.04377597638643,0.737017624709665));
#17886=CARTESIAN_POINT('Ctrl Pts',(1.03578811269634,-1.94446440957907,0.742890481216312));
#17887=CARTESIAN_POINT('Ctrl Pts',(0.979834028691006,-1.84254265710323,
0.748763337722959));
#17888=CARTESIAN_POINT('Ctrl Pts',(0.92854122569731,-1.73845157247564,0.754636194229606));
#17889=CARTESIAN_POINT('Ctrl Pts',(0.877213378961228,-1.63428937180561,
0.760513063128995));
#17890=CARTESIAN_POINT('Ctrl Pts',(0.830553320027273,-1.52795526336591,
0.766389932028385));
#17891=CARTESIAN_POINT('Ctrl Pts',(0.788724972113124,-1.41990914031055,
0.772266800927774));
#17892=CARTESIAN_POINT('Ctrl Pts',(0.746835572580654,-1.31170531581597,
0.778152247559129));
#17893=CARTESIAN_POINT('Ctrl Pts',(0.7097920897946,-1.20178487800983,0.784037694190484));
#17894=CARTESIAN_POINT('Ctrl Pts',(0.677708366468663,-1.09062196554404,
0.78992314082184));
#17895=CARTESIAN_POINT('Ctrl Pts',(0.670183066830447,-1.06454848845837,
0.791303583763444));
#17896=CARTESIAN_POINT('Ctrl Pts',(0.662930403658656,-1.03840669499931,
0.792684026705048));
#17897=CARTESIAN_POINT('Ctrl Pts',(0.655951435417046,-1.01220276324844,
0.794064469646653));
#17898=CARTESIAN_POINT('Ctrl Pts',(0.626295337403964,-0.900853013338637,
0.799930458681192));
#17899=CARTESIAN_POINT('Ctrl Pts',(0.601486334207142,-0.788008674215623,
0.805796447715731));
#17900=CARTESIAN_POINT('Ctrl Pts',(0.581673949443585,-0.674130175140967,
0.81166243675027));
#17901=CARTESIAN_POINT('Ctrl Pts',(0.561887502550487,-0.560400762902271,
0.817520746181091));
#17902=CARTESIAN_POINT('Ctrl Pts',(0.547084736594483,-0.445640287361216,
0.823379055611912));
#17903=CARTESIAN_POINT('Ctrl Pts',(0.537365211052586,-0.330323566972319,
0.829237365042733));
#17904=CARTESIAN_POINT('Ctrl Pts',(0.527655794716167,-0.21512678663773,
0.835089581289938));
#17905=CARTESIAN_POINT('Ctrl Pts',(0.523019137769456,-0.0993753225297563,
0.840941797537144));
#17906=CARTESIAN_POINT('Ctrl Pts',(0.523503496516046,0.0164472763632276,
0.846794013784349));
#17907=CARTESIAN_POINT('Ctrl Pts',(0.524006247659929,0.136667969167399,
0.852868454337431));
#17908=CARTESIAN_POINT('Ctrl Pts',(0.530026726470097,0.256964858772304,
0.858942894890512));
#17909=CARTESIAN_POINT('Ctrl Pts',(0.541559615467651,0.376792620987839,
0.865017335443594));
#17910=CARTESIAN_POINT('Ctrl Pts',(0.552657486269063,0.492100504708243,
0.870862649350912));
#17911=CARTESIAN_POINT('Ctrl Pts',(0.568859397830202,0.606973561036211,
0.87670796325823));
#17912=CARTESIAN_POINT('Ctrl Pts',(0.590107572941103,0.720928216950054,
0.882553277165548));
#17913=CARTESIAN_POINT('Ctrl Pts',(0.611352377896869,0.834864798612026,
0.888397663952556));
#17914=CARTESIAN_POINT('Ctrl Pts',(0.637641779113809,0.947882862223743,
0.894242050739565));
#17915=CARTESIAN_POINT('Ctrl Pts',(0.668866615925173,1.05950760994232,0.900086437526574));
#17916=CARTESIAN_POINT('Ctrl Pts',(0.700094106349606,1.17114184398394,0.905931320993237));
#17917=CARTESIAN_POINT('Ctrl Pts',(0.736257754424545,1.28138212767146,0.911776204459899));
#17918=CARTESIAN_POINT('Ctrl Pts',(0.777198322519407,1.38976814621004,0.917621087926562));
#17919=CARTESIAN_POINT('Ctrl Pts',(0.818152342803302,1.49818977806026,0.923467891896064));
#17920=CARTESIAN_POINT('Ctrl Pts',(0.863886257564295,1.60475554589305,0.929314695865567));
#17921=CARTESIAN_POINT('Ctrl Pts',(0.914192707903539,1.70902513672051,0.935161499835069));
#17922=CARTESIAN_POINT('Ctrl Pts',(0.964556201126772,1.81341295966598,0.941014933542075));
#17923=CARTESIAN_POINT('Ctrl Pts',(1.01950239820608,1.91549903551455,0.946868367249082));
#17924=CARTESIAN_POINT('Ctrl Pts',(1.0787779588869,2.01486761680251,0.952721800956089));
#17925=CARTESIAN_POINT('Ctrl Pts',(1.13809340619642,2.11430306338302,0.958579173448898));
#17926=CARTESIAN_POINT('Ctrl Pts',(1.20174379031527,2.2110170292401,0.964436545941708));
#17927=CARTESIAN_POINT('Ctrl Pts',(1.26943343021391,2.30462417757766,0.970293918434517));
#17928=CARTESIAN_POINT('Ctrl Pts',(1.33722268194242,2.39836907785702,0.976159910615556));
#17929=CARTESIAN_POINT('Ctrl Pts',(1.40906279582494,2.48899771280837,0.982025902796595));
#17930=CARTESIAN_POINT('Ctrl Pts',(1.48461894191781,2.57615907912292,0.987891894977633));
#17931=CARTESIAN_POINT('Ctrl Pts',(1.50474963722611,2.59938179492657,0.989454792337859));
#17932=CARTESIAN_POINT('Ctrl Pts',(1.52514392806353,2.62235859143156,0.991017689698084));
#17933=CARTESIAN_POINT('Ctrl Pts',(1.54579507190206,2.64508330038158,0.99258058705831));
#17934=CARTESIAN_POINT('Ctrl Pts',(1.62342757052777,2.73051081713931,0.998455885207339));
#17935=CARTESIAN_POINT('Ctrl Pts',(1.70495298987006,2.81265945630749,1.00433118335637));
#17936=CARTESIAN_POINT('Ctrl Pts',(1.79006349645624,2.89115377042275,1.0102064815054));
#17937=CARTESIAN_POINT('Ctrl Pts',(1.87506423519424,2.96954684965761,1.01607420222526));
#17938=CARTESIAN_POINT('Ctrl Pts',(1.96364056522896,3.04429469924159,1.02194192294512));
#17939=CARTESIAN_POINT('Ctrl Pts',(2.05544558753515,3.11505618933762,1.02780964366498));
#17940=CARTESIAN_POINT('Ctrl Pts',(2.14715669181916,3.18574528928516,1.03367136161167));
#17941=CARTESIAN_POINT('Ctrl Pts',(2.24208959325428,3.25245589098474,1.03953307955836));
#17942=CARTESIAN_POINT('Ctrl Pts',(2.33986235636494,3.31488534741028,1.04539479750505));
#17943=CARTESIAN_POINT('Ctrl Pts',(2.44112446476054,3.3795428060165,1.05146571029525));
#17944=CARTESIAN_POINT('Ctrl Pts',(2.54543259012771,3.43960753068541,1.05753662308546));
#17945=CARTESIAN_POINT('Ctrl Pts',(2.65232685961407,3.49479037340125,1.06360753587566));
#17946=CARTESIAN_POINT('Ctrl Pts',(2.75541910430907,3.54801046790737,1.06946251790507));
#17947=CARTESIAN_POINT('Ctrl Pts',(2.86091625959808,3.59668983951194,1.07531749993449));
#17948=CARTESIAN_POINT('Ctrl Pts',(2.96837914617397,3.64061495778054,1.0811724819639));
#17949=CARTESIAN_POINT('Ctrl Pts',(3.07582584722618,3.68453346026704,1.08702658214514));
#17950=CARTESIAN_POINT('Ctrl Pts',(3.18523730877148,3.7236989770682,1.09288068232638));
#17951=CARTESIAN_POINT('Ctrl Pts',(3.29615394353355,3.75794594469425,1.09873478250762));
#17952=CARTESIAN_POINT('Ctrl Pts',(3.40708065488555,3.79219602359978,1.10458941452402));
#17953=CARTESIAN_POINT('Ctrl Pts',(3.51951241675792,3.82152654323087,1.11044404654043));
#17954=CARTESIAN_POINT('Ctrl Pts',(3.63297472209708,3.84582188866319,1.11629867855683));
#17955=CARTESIAN_POINT('Ctrl Pts',(3.74647473218941,3.87012530770198,1.12215525613088));
#17956=CARTESIAN_POINT('Ctrl Pts',(3.86100556320786,3.88939013893042,1.12801183370492));
#17957=CARTESIAN_POINT('Ctrl Pts',(3.97608346737002,3.90355205396167,1.13386841127897));
#17958=CARTESIAN_POINT('Ctrl Pts',(4.09129141055242,3.91772997207856,1.13973160683598));
#17959=CARTESIAN_POINT('Ctrl Pts',(4.20704725074402,3.92679341422568,1.14559480239299));
#17960=CARTESIAN_POINT('Ctrl Pts',(4.32286298031701,3.93073000893239,1.15145799795));
#17961=CARTESIAN_POINT('Ctrl Pts',(4.43875661605547,3.93466925168182,1.15732513752295));
#17962=CARTESIAN_POINT('Ctrl Pts',(4.55470980954187,3.93347478398154,1.1631922770959));
#17963=CARTESIAN_POINT('Ctrl Pts',(4.67023715244117,3.92718629840934,1.16905941666885));
#17964=CARTESIAN_POINT('Ctrl Pts',(4.78593289379385,3.92088864642494,1.17493510847892));
#17965=CARTESIAN_POINT('Ctrl Pts',(4.90120113639546,3.90948219795967,1.18081080028899));
#17966=CARTESIAN_POINT('Ctrl Pts',(5.01556409209311,3.89305815481475,1.18668649209905));
#17967=CARTESIAN_POINT('Ctrl Pts',(5.04417717223732,3.88894893553188,1.18815656288936));
#17968=CARTESIAN_POINT('Ctrl Pts',(5.0727336478532,3.88452587313218,1.18962663367966));
#17969=CARTESIAN_POINT('Ctrl Pts',(5.10122617683407,3.87979088610339,1.19109670446997));
#17970=CARTESIAN_POINT('Ctrl Pts',(5.21506675973802,3.86087246423347,1.19697030438069));
#17971=CARTESIAN_POINT('Ctrl Pts',(5.32826262852322,3.83690799495832,1.20284390429142));
#17972=CARTESIAN_POINT('Ctrl Pts',(5.44033177785518,3.80795263144901,1.20871750420215));
#17973=CARTESIAN_POINT('Ctrl Pts',(5.55227467966402,3.77902988657691,1.21458448741733));
#17974=CARTESIAN_POINT('Ctrl Pts',(5.6630929884551,3.74512752236364,1.22045147063252));
#17975=CARTESIAN_POINT('Ctrl Pts',(5.77231213114212,3.70635213299535,1.22631845384771));
#17976=CARTESIAN_POINT('Ctrl Pts',(5.88141493970294,3.66761804500455,1.2321791878803));
#17977=CARTESIAN_POINT('Ctrl Pts',(5.98892158433081,3.62402139587162,1.23803992191289));
#17978=CARTESIAN_POINT('Ctrl Pts',(6.09437090185581,3.57571904766681,1.24390065594547));
#17979=CARTESIAN_POINT('Ctrl Pts',(6.19115331118495,3.53138668264788,1.2492796946479));
#17980=CARTESIAN_POINT('Ctrl Pts',(6.28620258476723,3.48309099504578,1.25465873335032));
#17981=CARTESIAN_POINT('Ctrl Pts',(6.37917532067788,3.4309896258774,1.26003777205275));
#17982=CARTESIAN_POINT('Ctrl Pts',(2.17296269996979,-3.20554048108048,-0.411765747138983));
#17983=CARTESIAN_POINT('Ctrl Pts',(1.10598262521586,-2.44554835076675,-0.345549597099719));
#17984=CARTESIAN_POINT('Ctrl Pts',(-0.190085171851759,0.209786400507346,
-0.213161407923235));
#17985=CARTESIAN_POINT('Ctrl Pts',(2.11904905146237,4.02596493684606,-0.0146011796095345));
#17986=CARTESIAN_POINT('Ctrl Pts',(6.57036830017086,4.14281137096193,0.183914937802122));
#17987=CARTESIAN_POINT('Ctrl Pts',(9.08469850437939,0.471525498888313,0.382431055213778));
#17988=CARTESIAN_POINT('Ctrl Pts',(7.36116941620609,-3.63455711911314,0.580947172625436));
#17989=CARTESIAN_POINT('Ctrl Pts',(2.97726580402431,-4.41062931823268,0.77946329003709));
#17990=CARTESIAN_POINT('Ctrl Pts',(-0.0518523842630756,-1.14834011450979,
0.977979407448747));
#17991=CARTESIAN_POINT('Ctrl Pts',(1.04758148582589,3.16599895701937,1.1764955248604));
#17992=CARTESIAN_POINT('Ctrl Pts',(5.26885307852876,4.58075644304919,1.37501164227206));
#17993=CARTESIAN_POINT('Ctrl Pts',(8.74613631193873,1.80065901519612,1.57352775968371));
#17994=CARTESIAN_POINT('Ctrl Pts',(8.2950356860829,-2.62850749839492,1.77204387709537));
#17995=CARTESIAN_POINT('Ctrl Pts',(4.32864266632258,-4.6505056552148,1.97055999450703));
#17996=CARTESIAN_POINT('Ctrl Pts',(0.479313869061077,-2.41367545883394,
2.16907611191868));
#17997=CARTESIAN_POINT('Ctrl Pts',(0.272186515624751,2.03356129066451,2.36759222933034));
#17998=CARTESIAN_POINT('Ctrl Pts',(3.89694643539194,4.61849687019083,2.56610834674199));
#17999=CARTESIAN_POINT('Ctrl Pts',(8.03410612006349,2.97390317522259,2.76462446415365));
#18000=CARTESIAN_POINT('Ctrl Pts',(8.89493411795877,-1.39413568050936,2.9631405815653));
#18001=CARTESIAN_POINT('Ctrl Pts',(5.69110016326603,-4.48545097223521,3.16165669897696));
#18002=CARTESIAN_POINT('Ctrl Pts',(1.35661463604595,-3.46907591290164,3.36017281638862));
#18003=CARTESIAN_POINT('Ctrl Pts',(-0.139083166427389,0.724213049156903,
3.55868893380027));
#18004=CARTESIAN_POINT('Ctrl Pts',(2.57373840321099,4.25428138787658,3.75720505121192));
#18005=CARTESIAN_POINT('Ctrl Pts',(7.01072892820446,3.88835980295648,3.95572116862359));
#18006=CARTESIAN_POINT('Ctrl Pts',(9.10857690015422,-0.0384477492421469,
4.15423728603523));
#18007=CARTESIAN_POINT('Ctrl Pts',(6.94611304441007,-3.93004557143118,4.3527534034469));
#18008=CARTESIAN_POINT('Ctrl Pts',(2.50368062941278,-4.22258242327136,4.55126952085854));
#18009=CARTESIAN_POINT('Ctrl Pts',(-0.15042524517621,-0.648158610486061,
4.74978563827021));
#18010=CARTESIAN_POINT('Ctrl Pts',(1.41437509517098,3.51983652671062,4.94830175568186));
#18011=CARTESIAN_POINT('Ctrl Pts',(5.76506726388787,4.46443232806813,5.14681787309352));
#18012=CARTESIAN_POINT('Ctrl Pts',(8.91737013208296,1.32058592540232,5.34533399050517));
#18013=CARTESIAN_POINT('Ctrl Pts',(7.98446469607637,-3.03262794728552,5.54385010791683));
#18014=CARTESIAN_POINT('Ctrl Pts',(3.82068800849579,-4.60861883268182,5.74236622532849));
#18015=CARTESIAN_POINT('Ctrl Pts',(0.239147556357015,-1.9641242562649,5.94088234274014));
#18016=CARTESIAN_POINT('Ctrl Pts',(0.519749957626067,2.47907795239849,6.13939846015179));
#18017=CARTESIAN_POINT('Ctrl Pts',(4.40552487083362,4.65198772933701,6.33791457756345));
#18018=CARTESIAN_POINT('Ctrl Pts',(8.33795354574623,2.56469563392857,6.53643069497511));
#18019=CARTESIAN_POINT('Ctrl Pts',(8.71579260460107,-1.87129593734266,6.73494681238676));
#18020=CARTESIAN_POINT('Ctrl Pts',(5.19302422456139,-4.59359028502123,6.93346292979842));
#18021=CARTESIAN_POINT('Ctrl Pts',(0.995732677906764,-3.10916202902842,
7.13197904721008));
#18022=CARTESIAN_POINT('Ctrl Pts',(-0.0322822778871914,1.22257767061497,
7.33049516462173));
#18023=CARTESIAN_POINT('Ctrl Pts',(3.05041589877745,4.43470399540276,7.52901128203338));
#18024=CARTESIAN_POINT('Ctrl Pts',(7.42075085684839,3.58561275821527,7.72752739944505));
#18025=CARTESIAN_POINT('Ctrl Pts',(9.07645297431008,-0.547114437358846,
7.9260435168567));
#18026=CARTESIAN_POINT('Ctrl Pts',(6.5012617467849,-4.17880463841992,8.12455963426836));
#18027=CARTESIAN_POINT('Ctrl Pts',(2.05348831510913,-3.98362504090881,8.32307575168001));
#18028=CARTESIAN_POINT('Ctrl Pts',(-0.193681017610346,-0.140317407516647,
8.52159186909167));
#18029=CARTESIAN_POINT('Ctrl Pts',(1.81766867783776,3.83149023855917,8.72010798650331));
#18030=CARTESIAN_POINT('Ctrl Pts',(6.24558161029013,4.2944920068349,8.91862410391498));
#18031=CARTESIAN_POINT('Ctrl Pts',(9.03505934404192,0.824679685151172,9.11714022132663));
#18032=CARTESIAN_POINT('Ctrl Pts',(7.6315512320161,-3.40035860512303,9.31565633873829));
#18033=CARTESIAN_POINT('Ctrl Pts',(3.32036330565075,-4.51141316650472,9.51417245614994));
#18034=CARTESIAN_POINT('Ctrl Pts',(0.0495994604212725,-1.49100136617927,
9.71268857356161));
#18035=CARTESIAN_POINT('Ctrl Pts',(0.814563009263402,2.89484112343983,9.91120469097325));
#18036=CARTESIAN_POINT('Ctrl Pts',(4.91471488529713,4.62964317792977,10.1097208083849));
#18037=CARTESIAN_POINT('Ctrl Pts',(8.59521399360942,2.1247060752228,10.3082369257966));
#18038=CARTESIAN_POINT('Ctrl Pts',(8.48552926132444,-2.32599643497811,10.5067530432082));
#18039=CARTESIAN_POINT('Ctrl Pts',(4.68610787984395,-4.64659565516981,10.7052691606199));
#18040=CARTESIAN_POINT('Ctrl Pts',(0.676387677669684,-2.71193096197848,
10.9037852780315));
#18041=CARTESIAN_POINT('Ctrl Pts',(0.128394142987057,1.70626851979591,11.1023013954432));
#18042=CARTESIAN_POINT('Ctrl Pts',(3.54396933091606,4.56189974780998,11.3008175128549));
#18043=CARTESIAN_POINT('Ctrl Pts',(7.79519445548059,3.23982996331418,11.4993336302665));
#18044=CARTESIAN_POINT('Ctrl Pts',(8.98887841448097,-1.04921447348414,11.6978497476782));
#18045=CARTESIAN_POINT('Ctrl Pts',(6.03186814454124,-4.3774082536412,11.8963658650898));
#18046=CARTESIAN_POINT('Ctrl Pts',(1.63213740257258,-3.69685482224785,12.0948819825015));
#18047=CARTESIAN_POINT('Ctrl Pts',(-0.181124089683036,0.369207933724872,
12.2933980999131));
#18048=CARTESIAN_POINT('Ctrl Pts',(2.2526340504912,4.09715708707193,12.4919142173248));
#18049=CARTESIAN_POINT('Ctrl Pts',(6.70462241331237,4.07300771627025,12.6904303347364));
#18050=CARTESIAN_POINT('Ctrl Pts',(9.09779474190718,0.318875355730261,12.8889464521481));
#18051=CARTESIAN_POINT('Ctrl Pts',(7.24052934071316,-3.72727698993507,13.0874625695597));
#18052=CARTESIAN_POINT('Ctrl Pts',(2.83367453520978,-4.36005996854408,13.2859786869714));
#18053=CARTESIAN_POINT('Ctrl Pts',(-0.0870558709899348,-0.999982965095223,
13.4844948043831));
#18054=CARTESIAN_POINT('Ctrl Pts',(1.1530874699283,3.2758594160949,13.6830109217947));
#18055=CARTESIAN_POINT('Ctrl Pts',(5.41840487637927,4.55173205747878,13.8815270392064));
#18056=CARTESIAN_POINT('Ctrl Pts',(8.80279980247531,1.65921506374814,14.080043156618));
#18057=CARTESIAN_POINT('Ctrl Pts',(8.20690775291552,-2.75277952374592,14.2785592740297));
#18058=CARTESIAN_POINT('Ctrl Pts',(4.17643533161801,-4.64383098681233,14.4770753914414));
#18059=CARTESIAN_POINT('Ctrl Pts',(0.402412514292184,-2.28215036718792,
14.675591508853));
#18060=CARTESIAN_POINT('Ctrl Pts',(0.341017607518878,2.16948014760412,14.8741076262646));
#18061=CARTESIAN_POINT('Ctrl Pts',(4.04847489906614,4.63434201110855,15.0726237436763));
#18062=CARTESIAN_POINT('Ctrl Pts',(8.12956552465056,2.85516161537223,15.271139861088));
#18063=CARTESIAN_POINT('Ctrl Pts',(8.84690431993714,-1.53872147678918,15.4696559784996));
#18064=CARTESIAN_POINT('Ctrl Pts',(5.54356606143321,-4.52347271009317,15.6681720959113));
#18065=CARTESIAN_POINT('Ctrl Pts',(1.24468509012015,-3.36571368106855,15.8666882133229));
#18066=CARTESIAN_POINT('Ctrl Pts',(-0.112905173860372,0.874301914415817,
16.0652043307346));
#18067=CARTESIAN_POINT('Ctrl Pts',(2.71405060913991,4.31364844766405,16.2637204481462));
#18068=CARTESIAN_POINT('Ctrl Pts',(7.1366801074503,3.80263778683562,16.4622365655579));
#18069=CARTESIAN_POINT('Ctrl Pts',(9.10482335385156,-0.190756225336315,
16.6607526829696));
#18070=CARTESIAN_POINT('Ctrl Pts',(6.81609220134375,-4.00945931491334,16.8592688003812));
#18071=CARTESIAN_POINT('Ctrl Pts',(2.36646310311057,-4.15637583189606,17.0577849177929));
#18072=CARTESIAN_POINT('Ctrl Pts',(-0.16917825360623,-0.496962424679848,
17.2563010352045));
#18073=CARTESIAN_POINT('Ctrl Pts',(1.53126025266144,3.61755971783011,17.4548171526162));
#18074=CARTESIAN_POINT('Ctrl Pts',(5.91054938364417,4.41918948403437,17.6533332700278));
#18075=CARTESIAN_POINT('Ctrl Pts',(8.95821945609951,1.17380958265607,17.8518493874395));
#18076=CARTESIAN_POINT('Ctrl Pts',(7.88327219050615,-3.14652280629029,18.0503655048511));
#18077=CARTESIAN_POINT('Ctrl Pts',(3.67012384502666,-4.58532946245115,18.2488816222628));
#18078=CARTESIAN_POINT('Ctrl Pts',(0.177095531876928,-1.82497861910485,
18.4473977396744));
#18079=CARTESIAN_POINT('Ctrl Pts',(0.603036135785551,2.60665292882547,18.6459138570862));
#18080=CARTESIAN_POINT('Ctrl Pts',(4.55787735396168,4.65116130836808,18.8444299744978));
#18081=CARTESIAN_POINT('Ctrl Pts',(8.41985082781949,2.43622463611074,19.0429460919094));
#18082=CARTESIAN_POINT('Ctrl Pts',(8.65223471259592,-2.00976021586402,19.2414622093211));
#18083=CARTESIAN_POINT('Ctrl Pts',(5.04221626688697,-4.61524489208584,19.4399783267328));
#18084=CARTESIAN_POINT('Ctrl Pts',(0.895781713701428,-2.99417608693739,
19.6384944441444));
#18085=CARTESIAN_POINT('Ctrl Pts',(0.0101569427980723,1.36890222246852,
19.8370105615561));
#18086=CARTESIAN_POINT('Ctrl Pts',(3.1963802739596,4.47836591752857,20.0355266789677));
#18087=CARTESIAN_POINT('Ctrl Pts',(7.53656898706393,3.48662728959027,20.2340427963793));
#18088=CARTESIAN_POINT('Ctrl Pts',(9.05606082131957,-0.698098281184544,
20.432558913791));
#18089=CARTESIAN_POINT('Ctrl Pts',(6.36333405195284,-4.24351873734398,20.6310750312027));
#18090=CARTESIAN_POINT('Ctrl Pts',(1.9243366462227,-3.90280543100934,20.8295911486144));
#18091=CARTESIAN_POINT('Ctrl Pts',(-0.195782035254683,0.0120228054752082,
21.028107266026));
#18092=CARTESIAN_POINT('Ctrl Pts',(1.94454241477252,3.91584087042925,21.2266233834376));
#18093=CARTESIAN_POINT('Ctrl Pts',(6.38524148680512,4.23360619038166,21.4251395008493));
#18094=CARTESIAN_POINT('Ctrl Pts',(9.05960761710739,0.674315805600993,21.623655618261));
#18095=CARTESIAN_POINT('Ctrl Pts',(7.5185068390623,-3.50250076674849,21.8221717356726));
#18096=CARTESIAN_POINT('Ctrl Pts',(3.17325057532877,-4.47179261159471,22.0206878530843));
#18097=CARTESIAN_POINT('Ctrl Pts',(0.0031406198327811,-1.34590405051051,
22.2192039704959));
#18098=CARTESIAN_POINT('Ctrl Pts',(0.911305739869395,3.01254206724522,22.4177200879076));
#18099=CARTESIAN_POINT('Ctrl Pts',(5.06606104496655,4.6121513544261,22.6162362053192));
#18100=CARTESIAN_POINT('Ctrl Pts',(8.66256938155685,1.98805571626367,22.8147523227309));
#18101=CARTESIAN_POINT('Ctrl Pts',(8.4072000996685,-2.45669335535235,23.0132684401425));
#18102=CARTESIAN_POINT('Ctrl Pts',(4.53384760969594,-4.65159218721967,23.2117845575542));
#18103=CARTESIAN_POINT('Ctrl Pts',(0.589592923617338,-2.58676106216746,
23.4103006749659));
#18104=CARTESIAN_POINT('Ctrl Pts',(0.186627431348294,1.84718698340797,23.6088167923775));
#18105=CARTESIAN_POINT('Ctrl Pts',(3.69375302108596,4.58911293885384,23.8073329097892));
#18106=CARTESIAN_POINT('Ctrl Pts',(7.89964467060016,3.12919021086655,24.0058490272008));
#18107=CARTESIAN_POINT('Ctrl Pts',(8.95179466357075,-1.19786968887199,24.2043651446125));
#18108=CARTESIAN_POINT('Ctrl Pts',(5.88826072308503,-4.42509080397621,24.4028812620241));
#18109=CARTESIAN_POINT('Ctrl Pts',(1.51149918181804,-3.60542346049212,24.6013973794358));
#18110=CARTESIAN_POINT('Ctrl Pts',(-0.164376056275096,0.527120914407128,
24.7999134968474));
#18111=CARTESIAN_POINT('Ctrl Pts',(1.53399129555416,2.94325066577138,24.9322575751219));
#18112=CARTESIAN_POINT('Ctrl Pts',(2.70656526709436,3.52529833870864,24.9984296142591));
#18113=CARTESIAN_POINT('Ctrl Pts',(2.31196529717974,-3.01041142380583,-0.273445981108207));
#18114=CARTESIAN_POINT('Ctrl Pts',(1.30993489857133,-2.29668186568531,-0.207229831068943));
#18115=CARTESIAN_POINT('Ctrl Pts',(0.0927619053280601,0.197016191301887,
-0.0748416418924601));
#18116=CARTESIAN_POINT('Ctrl Pts',(2.26133350378215,3.78089464452436,0.123718586421241));
#18117=CARTESIAN_POINT('Ctrl Pts',(6.44169010710979,3.89062835157607,0.322234703832897));
#18118=CARTESIAN_POINT('Ctrl Pts',(8.80296690727615,0.442822593209179,0.520750821244553));
#18119=CARTESIAN_POINT('Ctrl Pts',(7.18435323294509,-3.41331277406459,0.719266938656211));
#18120=CARTESIAN_POINT('Ctrl Pts',(3.06730851213489,-4.14214356803415,0.917783056067867));
#18121=CARTESIAN_POINT('Ctrl Pts',(0.222580126422941,-1.07843785456408,
1.11629917347952));
#18122=CARTESIAN_POINT('Ctrl Pts',(1.25508877879203,2.97327688863128,1.31481529089117));
#18123=CARTESIAN_POINT('Ctrl Pts',(5.21940128729496,4.30191464036023,1.51333140830283));
#18124=CARTESIAN_POINT('Ctrl Pts',(8.48501382017349,1.69104851481962,1.71184752571448));
#18125=CARTESIAN_POINT('Ctrl Pts',(8.06137278822348,-2.46850384433775,1.91036364312614));
#18126=CARTESIAN_POINT('Ctrl Pts',(4.33642377308406,-4.36741804808325,2.1088797605378));
#18127=CARTESIAN_POINT('Ctrl Pts',(0.721412996069988,-2.26674915432179,
2.30739587794946));
#18128=CARTESIAN_POINT('Ctrl Pts',(0.526893989166935,1.90977346146706,2.50591199536111));
#18129=CARTESIAN_POINT('Ctrl Pts',(3.93100594327419,4.33735771577206,2.70442811277276));
#18130=CARTESIAN_POINT('Ctrl Pts',(7.81632664047099,2.79287444498747,2.90294423018442));
#18131=CARTESIAN_POINT('Ctrl Pts',(8.62475394129306,-1.30927124574203,3.10146034759608));
#18132=CARTESIAN_POINT('Ctrl Pts',(5.61594516345689,-4.21241064570382,3.29997646500774));
#18133=CARTESIAN_POINT('Ctrl Pts',(1.54531032840212,-3.25790481196126,3.49849258241939));
#18134=CARTESIAN_POINT('Ctrl Pts',(0.140659294449413,0.680128436785933,
3.69700869983105));
#18135=CARTESIAN_POINT('Ctrl Pts',(2.68834480713824,3.99531291703776,3.8955248172427));
#18136=CARTESIAN_POINT('Ctrl Pts',(6.85524491106594,3.65166587031902,4.09404093465435));
#18137=CARTESIAN_POINT('Ctrl Pts',(8.82539176693615,-0.0361073410931478,
4.29255705206602));
#18138=CARTESIAN_POINT('Ctrl Pts',(6.79456235351217,-3.69081412452673,4.49107316947766));
#18139=CARTESIAN_POINT('Ctrl Pts',(2.62255162068078,-3.96554354562172,4.68958928688933));
#18140=CARTESIAN_POINT('Ctrl Pts',(0.130007635661538,-0.608703617053558,
4.88810540430098));
#18141=CARTESIAN_POINT('Ctrl Pts',(1.59955476768487,3.30557550356288,5.08662152171263));
#18142=CARTESIAN_POINT('Ctrl Pts',(5.68540970649173,4.19267145760527,5.28513763912429));
#18143=CARTESIAN_POINT('Ctrl Pts',(8.64582422058695,1.24019864338394,5.48365375653594));
#18144=CARTESIAN_POINT('Ctrl Pts',(7.76970701088062,-2.84802449713069,5.68216987394761));
#18145=CARTESIAN_POINT('Ctrl Pts',(3.85938955257665,-4.32808097846753,5.88068599135924));
#18146=CARTESIAN_POINT('Ctrl Pts',(0.495866191827503,-1.844563228489,6.07920210877092));
#18147=CARTESIAN_POINT('Ctrl Pts',(0.759387641428115,2.32817043879295,6.27771822618256));
#18148=CARTESIAN_POINT('Ctrl Pts',(4.40862597053364,4.36880990474354,6.47623434359423));
#18149=CARTESIAN_POINT('Ctrl Pts',(8.10167813322798,2.40857636349708,6.67475046100588));
#18150=CARTESIAN_POINT('Ctrl Pts',(8.45651720821394,-1.75738559545474,6.87326657841754));
#18151=CARTESIAN_POINT('Ctrl Pts',(5.14818832037566,-4.31396725511023,7.0717826958292));
#18152=CARTESIAN_POINT('Ctrl Pts',(1.20639613410644,-2.9198997628929,7.27029881324085));
#18153=CARTESIAN_POINT('Ctrl Pts',(0.240958952754043,1.14815638979818,7.4688149306525));
#18154=CARTESIAN_POINT('Ctrl Pts',(3.13600578243834,4.16475276096279,7.66733104806417));
#18155=CARTESIAN_POINT('Ctrl Pts',(7.24030780616454,3.36734777563528,7.86584716547581));
#18156=CARTESIAN_POINT('Ctrl Pts',(8.79522330270695,-0.513810248872322,
8.06436328288747));
#18157=CARTESIAN_POINT('Ctrl Pts',(6.37679023796107,-3.92443062116999,8.26287940029913));
#18158=CARTESIAN_POINT('Ctrl Pts',(2.1997636091463,-3.74113208118609,8.46139551771078));
#18159=CARTESIAN_POINT('Ctrl Pts',(0.089384947459713,-0.131775945129999,
8.65991163512245));
#18160=CARTESIAN_POINT('Ctrl Pts',(1.97829888761515,3.5982580948319,8.8584277525341));
#18161=CARTESIAN_POINT('Ctrl Pts',(6.13667397417128,4.03307581767334,9.05694386994575));
#18162=CARTESIAN_POINT('Ctrl Pts',(8.75634940354159,0.774479423926291,9.2554599873574));
#18163=CARTESIAN_POINT('Ctrl Pts',(7.43827624901926,-3.19337049409171,9.45397610476906));
#18164=CARTESIAN_POINT('Ctrl Pts',(3.38952083310589,-4.23679245796831,9.65249222218073));
#18165=CARTESIAN_POINT('Ctrl Pts',(0.317856350200649,-1.40024048117564,
9.85100833959237));
#18166=CARTESIAN_POINT('Ctrl Pts',(1.03625470449417,2.71862509287945,10.049524457004));
#18167=CARTESIAN_POINT('Ctrl Pts',(4.88682034851015,4.34782552060827,10.2480405744157));
#18168=CARTESIAN_POINT('Ctrl Pts',(8.34327851098385,1.99537004097493,10.4465566918273));
#18169=CARTESIAN_POINT('Ctrl Pts',(8.24027055552775,-2.18440736622039,10.645072809239));
#18170=CARTESIAN_POINT('Ctrl Pts',(4.67212920832948,-4.36374605926514,10.8435889266506));
#18171=CARTESIAN_POINT('Ctrl Pts',(0.906490441907856,-2.54684911848653,
11.0421050440623));
#18172=CARTESIAN_POINT('Ctrl Pts',(0.391854608507251,1.60240379879482,11.2406211614739));
#18173=CARTESIAN_POINT('Ctrl Pts',(3.59951541494433,4.28420579809219,11.4391372788856));
#18174=CARTESIAN_POINT('Ctrl Pts',(7.59195811086242,3.04261362173219,11.6376533962972));
#18175=CARTESIAN_POINT('Ctrl Pts',(8.71297961965247,-0.98534623276214,11.8361695137089));
#18176=CARTESIAN_POINT('Ctrl Pts',(5.93596976765481,-4.11094475056566,12.0346856311206));
#18177=CARTESIAN_POINT('Ctrl Pts',(1.80406135300024,-3.47181826426207,12.2332017485322));
#18178=CARTESIAN_POINT('Ctrl Pts',(0.101177504597399,0.346733347466743,
12.4317178659439));
#18179=CARTESIAN_POINT('Ctrl Pts',(2.38678685852808,3.84775315515312,12.6302339833555));
#18180=CARTESIAN_POINT('Ctrl Pts',(6.56777184536255,3.82507381537617,12.8287501007672));
#18181=CARTESIAN_POINT('Ctrl Pts',(8.81526594492522,0.29946463609684,13.0272662181788));
#18182=CARTESIAN_POINT('Ctrl Pts',(7.07105681270762,-3.5003885604986,13.2257823355905));
#18183=CARTESIAN_POINT('Ctrl Pts',(2.93245799361878,-4.09465249784007,13.4242984530022));
#18184=CARTESIAN_POINT('Ctrl Pts',(0.189519561683291,-0.939111566208993,
13.6228145704138));
#18185=CARTESIAN_POINT('Ctrl Pts',(1.35417235664619,3.07644987396012,13.8213306878255));
#18186=CARTESIAN_POINT('Ctrl Pts',(5.3598495029257,4.27465703983832,14.0198468052371));
#18187=CARTESIAN_POINT('Ctrl Pts',(8.53822806601778,1.55821460123144,14.2183629226488));
#18188=CARTESIAN_POINT('Ctrl Pts',(7.97860941701375,-2.58521112879858,14.4168790400604));
#18189=CARTESIAN_POINT('Ctrl Pts',(4.19348166959603,-4.36114968300486,14.6153951574721));
#18190=CARTESIAN_POINT('Ctrl Pts',(0.649192814085452,-2.14323031537866,
14.8139112748837));
#18191=CARTESIAN_POINT('Ctrl Pts',(0.59153516483578,2.03741860650786,15.0124273922954));
#18192=CARTESIAN_POINT('Ctrl Pts',(4.07331050026509,4.35223832436584,15.2109435097071));
#18193=CARTESIAN_POINT('Ctrl Pts',(7.9059751985768,2.68136097312093,15.4094596271187));
#18194=CARTESIAN_POINT('Ctrl Pts',(8.57964783407003,-1.44505575241412,15.6079757445304));
#18195=CARTESIAN_POINT('Ctrl Pts',(5.47739182177246,-4.24811790776339,15.806491861942));
#18196=CARTESIAN_POINT('Ctrl Pts',(1.44019420657955,-3.16083449095397,16.0050079793537));
#18197=CARTESIAN_POINT('Ctrl Pts',(0.165243768843413,0.821081027223728,
16.2035240967653));
#18198=CARTESIAN_POINT('Ctrl Pts',(2.82011586731386,4.05106615928717,16.402040214177));
#18199=CARTESIAN_POINT('Ctrl Pts',(6.97352913523386,3.57116196212476,16.6005563315886));
#18200=CARTESIAN_POINT('Ctrl Pts',(8.82186670813997,-0.17914442924803,16.7990724490003));
#18201=CARTESIAN_POINT('Ctrl Pts',(6.67245619587356,-3.76539376000376,16.997588566412));
#18202=CARTESIAN_POINT('Ctrl Pts',(2.49368685944485,-3.90336711073225,17.1961046838236));
#18203=CARTESIAN_POINT('Ctrl Pts',(0.112396168534027,-0.466711111367439,
17.3946208012353));
#18204=CARTESIAN_POINT('Ctrl Pts',(1.70932484092508,3.39735004600064,17.5931369186469));
#18205=CARTESIAN_POINT('Ctrl Pts',(5.82203597524696,4.15018265569229,17.7916530360586));
#18206=CARTESIAN_POINT('Ctrl Pts',(8.68418694674809,1.10235693414467,17.9901691534703));
#18207=CARTESIAN_POINT('Ctrl Pts',(7.67467433961344,-2.9549862986379,18.1886852708819));
#18208=CARTESIAN_POINT('Ctrl Pts',(3.71799059648846,-4.30620928893205,18.3872013882936));
#18209=CARTESIAN_POINT('Ctrl Pts',(0.437591425226463,-1.7138877251997,18.5857175057052));
#18210=CARTESIAN_POINT('Ctrl Pts',(0.837603987051035,2.44797961565228,18.7842336231169));
#18211=CARTESIAN_POINT('Ctrl Pts',(4.55170438690705,4.36803379003202,18.9827497405285));
#18212=CARTESIAN_POINT('Ctrl Pts',(8.17859012825258,2.28792570825151,19.1812658579402));
#18213=CARTESIAN_POINT('Ctrl Pts',(8.39682823991214,-1.88742121606535,19.3797819753518));
#18214=CARTESIAN_POINT('Ctrl Pts',(5.0065604104293,-4.33430369349561,19.5782980927635));
#18215=CARTESIAN_POINT('Ctrl Pts',(1.11252942855707,-2.81191329518458,19.7768142101752));
#18216=CARTESIAN_POINT('Ctrl Pts',(0.280814794700937,1.28557380975688,19.9753303275868));
#18217=CARTESIAN_POINT('Ctrl Pts',(3.27308495055695,4.20575687553525,20.1738464449984));
#18218=CARTESIAN_POINT('Ctrl Pts',(7.34907580467911,3.27438779359847,20.3723625624101));
#18219=CARTESIAN_POINT('Ctrl Pts',(8.77607246974106,-0.65560333835151,20.5708786798217));
#18220=CARTESIAN_POINT('Ctrl Pts',(6.24725853788356,-3.98520541525919,20.7693947972334));
#18221=CARTESIAN_POINT('Ctrl Pts',(2.07847371693811,-3.66523215780504,20.9679109146451));
#18222=CARTESIAN_POINT('Ctrl Pts',(0.0874118238771355,0.0112909480203034,
21.1664270320568));
#18223=CARTESIAN_POINT('Ctrl Pts',(2.09744951113826,3.6774740982752,21.3649431494684));
#18224=CARTESIAN_POINT('Ctrl Pts',(6.26783241381338,3.97589626917586,21.56345926688));
#18225=CARTESIAN_POINT('Ctrl Pts',(8.77940336342984,0.633268559987037,21.7619753842917));
#18226=CARTESIAN_POINT('Ctrl Pts',(7.33211314362288,-3.28929501353682,21.9604915017033));
#18227=CARTESIAN_POINT('Ctrl Pts',(3.25136321302202,-4.1995837027451,22.159007619115));
#18228=CARTESIAN_POINT('Ctrl Pts',(0.274225572405194,-1.26397559254583,
22.3575237365266));
#18229=CARTESIAN_POINT('Ctrl Pts',(1.12710846943813,2.82916129353447,22.5560398539383));
#18230=CARTESIAN_POINT('Ctrl Pts',(5.0289536987851,4.33139846700858,22.75455597135));
#18231=CARTESIAN_POINT('Ctrl Pts',(8.40653381239982,1.86703792222437,22.9530720887616));
#18232=CARTESIAN_POINT('Ctrl Pts',(8.1667094807393,-2.30714844669435,23.1515882061733));
#18233=CARTESIAN_POINT('Ctrl Pts',(4.52913739170739,-4.36843844023836,23.3501043235849));
#18234=CARTESIAN_POINT('Ctrl Pts',(0.824979095953012,-2.42929861537115,
23.5486204409966));
#18235=CARTESIAN_POINT('Ctrl Pts',(0.44654309475883,1.73474421227166,23.7471365584082));
#18236=CARTESIAN_POINT('Ctrl Pts',(3.74018140704413,4.30976245591016,23.9456526758199));
#18237=CARTESIAN_POINT('Ctrl Pts',(7.69005018696339,2.93870878051704,24.1441687932315));
#18238=CARTESIAN_POINT('Ctrl Pts',(8.67815324699032,-1.12495244308866,24.3426849106432));
#18239=CARTESIAN_POINT('Ctrl Pts',(5.80110407974766,-4.15572474791461,24.5412010280549));
#18240=CARTESIAN_POINT('Ctrl Pts',(1.69076667459873,-3.38595255220879,24.7397171454665));
#18241=CARTESIAN_POINT('Ctrl Pts',(0.116906044416222,0.495033780363739,
24.9382332628782));
#18242=CARTESIAN_POINT('Ctrl Pts',(1.71188963858453,2.76408782845127,25.0705773411526));
#18243=CARTESIAN_POINT('Ctrl Pts',(2.81308617627174,3.31070484176046,25.1367493802898));
#18244=CARTESIAN_POINT('Ctrl Pts',(2.45096789438968,-2.81528236653118,-0.135126215077433));
#18245=CARTESIAN_POINT('Ctrl Pts',(1.5138871719268,-2.14781538060387,-0.0689100650381678));
#18246=CARTESIAN_POINT('Ctrl Pts',(0.375608982507884,0.184245982096433,
0.0634781241383155));
#18247=CARTESIAN_POINT('Ctrl Pts',(2.40361795610193,3.53582435220265,0.262038352452016));
#18248=CARTESIAN_POINT('Ctrl Pts',(6.31301191404873,3.63844533219021,0.460554469863673));
#18249=CARTESIAN_POINT('Ctrl Pts',(8.52123531017291,0.41411968753004,0.659070587275328));
#18250=CARTESIAN_POINT('Ctrl Pts',(7.00753704968407,-3.19206842901602,0.857586704686986));
#18251=CARTESIAN_POINT('Ctrl Pts',(3.15735122024546,-3.87365781783563,1.05610282209864));
#18252=CARTESIAN_POINT('Ctrl Pts',(0.497012637108953,-1.00853559461836,
1.25461893951029));
#18253=CARTESIAN_POINT('Ctrl Pts',(1.46259607175817,2.78055482024318,1.45313505692195));
#18254=CARTESIAN_POINT('Ctrl Pts',(5.16994949606116,4.02307283767128,1.6516511743336));
#18255=CARTESIAN_POINT('Ctrl Pts',(8.22389132840824,1.58143801444312,1.85016729174526));
#18256=CARTESIAN_POINT('Ctrl Pts',(7.82770989036406,-2.30850019028058,2.04868340915692));
#18257=CARTESIAN_POINT('Ctrl Pts',(4.34420487984554,-4.08433044095169,2.24719952656857));
#18258=CARTESIAN_POINT('Ctrl Pts',(0.963512123078899,-2.11982284980964,
2.44571564398023));
#18259=CARTESIAN_POINT('Ctrl Pts',(0.781601462709117,1.78598563226962,2.64423176139188));
#18260=CARTESIAN_POINT('Ctrl Pts',(3.96506545115642,4.05621856135326,2.84274787880354));
#18261=CARTESIAN_POINT('Ctrl Pts',(7.59854716087849,2.61184571475234,3.0412639962152));
#18262=CARTESIAN_POINT('Ctrl Pts',(8.35457376462735,-1.22440681097471,3.23978011362686));
#18263=CARTESIAN_POINT('Ctrl Pts',(5.54079016364776,-3.93937031917242,3.43829623103851));
#18264=CARTESIAN_POINT('Ctrl Pts',(1.7340060207583,-3.04673371102089,3.63681234845017));
#18265=CARTESIAN_POINT('Ctrl Pts',(0.420401755326215,0.636043824414959,
3.83532846586182));
#18266=CARTESIAN_POINT('Ctrl Pts',(2.8029512110655,3.73634444619894,4.03384458327349));
#18267=CARTESIAN_POINT('Ctrl Pts',(6.6997608939274,3.41497193768155,4.23236070068513));
#18268=CARTESIAN_POINT('Ctrl Pts',(8.54220663371807,-0.0337669329441494,
4.4308768180968));
#18269=CARTESIAN_POINT('Ctrl Pts',(6.64301166261426,-3.45158267762228,4.62939293550844));
#18270=CARTESIAN_POINT('Ctrl Pts',(2.74142261194879,-3.70850466797209,4.82790905292011));
#18271=CARTESIAN_POINT('Ctrl Pts',(0.410440516499291,-0.569248623621048,
5.02642517033176));
#18272=CARTESIAN_POINT('Ctrl Pts',(1.78473444019877,3.09131448041513,5.22494128774342));
#18273=CARTESIAN_POINT('Ctrl Pts',(5.60575214909559,3.92091058714242,5.42345740515506));
#18274=CARTESIAN_POINT('Ctrl Pts',(8.37427830909092,1.15981136136555,5.62197352256674));
#18275=CARTESIAN_POINT('Ctrl Pts',(7.55494932568486,-2.66342104697584,5.82048963997839));
#18276=CARTESIAN_POINT('Ctrl Pts',(3.89809109665752,-4.04754312425325,6.01900575739004));
#18277=CARTESIAN_POINT('Ctrl Pts',(0.752584827297987,-1.72500220071308,
6.21752187480171));
#18278=CARTESIAN_POINT('Ctrl Pts',(0.999025325230166,2.17726292518741,6.41603799221334));
#18279=CARTESIAN_POINT('Ctrl Pts',(4.41172707023364,4.08563208015006,6.61455410962502));
#18280=CARTESIAN_POINT('Ctrl Pts',(7.86540272070975,2.25245709306557,6.81307022703666));
#18281=CARTESIAN_POINT('Ctrl Pts',(8.1972418118268,-1.64347525356681,7.01158634444832));
#18282=CARTESIAN_POINT('Ctrl Pts',(5.10335241618994,-4.03434422519923,7.21010246185998));
#18283=CARTESIAN_POINT('Ctrl Pts',(1.4170595903061,-2.73063749675737,7.40861857927163));
#18284=CARTESIAN_POINT('Ctrl Pts',(0.514200183395272,1.07373510898141,7.60713469668328));
#18285=CARTESIAN_POINT('Ctrl Pts',(3.22159566609925,3.89480152652282,7.80565081409495));
#18286=CARTESIAN_POINT('Ctrl Pts',(7.05986475548066,3.14908279305528,8.0041669315066));
#18287=CARTESIAN_POINT('Ctrl Pts',(8.51399363110384,-0.480506060385796,
8.20268304891826));
#18288=CARTESIAN_POINT('Ctrl Pts',(6.25231872913724,-3.67005660392007,8.40119916632992));
#18289=CARTESIAN_POINT('Ctrl Pts',(2.34603890318347,-3.49863912146337,8.59971528374156));
#18290=CARTESIAN_POINT('Ctrl Pts',(0.372450912529775,-0.123234482743352,
8.79823140115322));
#18291=CARTESIAN_POINT('Ctrl Pts',(2.13892909739252,3.36502595110463,8.99674751856487));
#18292=CARTESIAN_POINT('Ctrl Pts',(6.02776633805246,3.77165962851178,9.19526363597655));
#18293=CARTESIAN_POINT('Ctrl Pts',(8.47763946304124,0.72427916270141,9.39377975338818));
#18294=CARTESIAN_POINT('Ctrl Pts',(7.24500126602242,-2.98638238306039,9.59229587079984));
#18295=CARTESIAN_POINT('Ctrl Pts',(3.45867836056103,-3.9621717494319,9.79081198821151));
#18296=CARTESIAN_POINT('Ctrl Pts',(0.586113239980029,-1.30947959617202,
9.98932810562315));
#18297=CARTESIAN_POINT('Ctrl Pts',(1.25794639972494,2.54240906231909,10.1878442230349));
#18298=CARTESIAN_POINT('Ctrl Pts',(4.85892581172318,4.06600786328675,10.3863603404465));
#18299=CARTESIAN_POINT('Ctrl Pts',(8.09134302835829,1.86603400672705,10.5848764578582));
#18300=CARTESIAN_POINT('Ctrl Pts',(7.99501184973105,-2.04281829746266,10.7833925752698));
#18301=CARTESIAN_POINT('Ctrl Pts',(4.658150536815,-4.08089646336047,10.9819086926815));
#18302=CARTESIAN_POINT('Ctrl Pts',(1.13659320614603,-2.38176727499459,11.1804248100931));
#18303=CARTESIAN_POINT('Ctrl Pts',(0.655315074027438,1.49853907779376,11.3789409275048));
#18304=CARTESIAN_POINT('Ctrl Pts',(3.6550614989726,4.00651184837438,11.5774570449165));
#18305=CARTESIAN_POINT('Ctrl Pts',(7.38872176624422,2.84539728015019,11.7759731623281));
#18306=CARTESIAN_POINT('Ctrl Pts',(8.43708082482397,-0.921477992040132,
11.9744892797398));
#18307=CARTESIAN_POINT('Ctrl Pts',(5.84007139076835,-3.84448124749012,12.1730053971514));
#18308=CARTESIAN_POINT('Ctrl Pts',(1.97598530342792,-3.24678170627628,12.3715215145631));
#18309=CARTESIAN_POINT('Ctrl Pts',(0.383479098877827,0.324258761208613,
12.5700376319747));
#18310=CARTESIAN_POINT('Ctrl Pts',(2.52093966656498,3.59834922323431,12.7685537493864));
#18311=CARTESIAN_POINT('Ctrl Pts',(6.43092127741269,3.5771399144821,12.967069866798));
#18312=CARTESIAN_POINT('Ctrl Pts',(8.53273714794332,0.280053916463419,13.1655859842097));
#18313=CARTESIAN_POINT('Ctrl Pts',(6.90158428470204,-3.27350013106212,13.3641021016213));
#18314=CARTESIAN_POINT('Ctrl Pts',(3.0312414520278,-3.82924502713605,13.562618219033));
#18315=CARTESIAN_POINT('Ctrl Pts',(0.466094994356506,-0.878240167322765,
13.7611343364446));
#18316=CARTESIAN_POINT('Ctrl Pts',(1.55525724336407,2.87704033182534,13.9596504538563));
#18317=CARTESIAN_POINT('Ctrl Pts',(5.30129412947213,3.99758202219787,14.1581665712679));
#18318=CARTESIAN_POINT('Ctrl Pts',(8.27365632956023,1.45721413871475,14.3566826886797));
#18319=CARTESIAN_POINT('Ctrl Pts',(7.75031108111198,-2.41764273385123,14.5551988060912));
#18320=CARTESIAN_POINT('Ctrl Pts',(4.21052800757405,-4.07846837919741,14.753714923503));
#18321=CARTESIAN_POINT('Ctrl Pts',(0.895973113878727,-2.00431026356939,
14.9522310409146));
#18322=CARTESIAN_POINT('Ctrl Pts',(0.842052722152676,1.9053570654116,15.1507471583263));
#18323=CARTESIAN_POINT('Ctrl Pts',(4.09814610146403,4.07013463762311,15.3492632757379));
#18324=CARTESIAN_POINT('Ctrl Pts',(7.682384872503,2.50756033086961,15.5477793931496));
#18325=CARTESIAN_POINT('Ctrl Pts',(8.31239134820293,-1.35139002803904,15.7462955105612));
#18326=CARTESIAN_POINT('Ctrl Pts',(5.41121758211169,-3.97276310543362,15.9448116279729));
#18327=CARTESIAN_POINT('Ctrl Pts',(1.63570332303896,-2.95595530083938,16.1433277453845));
#18328=CARTESIAN_POINT('Ctrl Pts',(0.443392711547191,0.767860140031627,
16.3418438627962));
#18329=CARTESIAN_POINT('Ctrl Pts',(2.92618112548781,3.7884838709103,16.5403599802078));
#18330=CARTESIAN_POINT('Ctrl Pts',(6.8103781630174,3.33968613741389,16.7388760976195));
#18331=CARTESIAN_POINT('Ctrl Pts',(8.5389100624284,-0.167532633159739,16.9373922150311));
#18332=CARTESIAN_POINT('Ctrl Pts',(6.52882019040339,-3.5213282050942,17.1359083324428));
#18333=CARTESIAN_POINT('Ctrl Pts',(2.62091061577914,-3.65035838956845,17.3344244498544));
#18334=CARTESIAN_POINT('Ctrl Pts',(0.393970590674286,-0.43645979805503,
17.5329405672661));
#18335=CARTESIAN_POINT('Ctrl Pts',(1.88738942918871,3.17714037417117,17.7314566846778));
#18336=CARTESIAN_POINT('Ctrl Pts',(5.73352256684974,3.8811758273502,17.9299728020894));
#18337=CARTESIAN_POINT('Ctrl Pts',(8.41015443739666,1.03090428563328,18.1284889195011));
#18338=CARTESIAN_POINT('Ctrl Pts',(7.46607648872073,-2.76344979098553,18.3270050369127));
#18339=CARTESIAN_POINT('Ctrl Pts',(3.76585734795025,-4.02708911541293,18.5255211543244));
#18340=CARTESIAN_POINT('Ctrl Pts',(0.698087318576006,-1.60279683129456,
18.724037271736));
#18341=CARTESIAN_POINT('Ctrl Pts',(1.07217183831651,2.28930630247911,18.9225533891477));
#18342=CARTESIAN_POINT('Ctrl Pts',(4.54553141985243,4.08490627169594,19.1210695065593));
#18343=CARTESIAN_POINT('Ctrl Pts',(7.93732942868568,2.13962678039228,19.319585623971));
#18344=CARTESIAN_POINT('Ctrl Pts',(8.14142176722837,-1.76508221626667,19.5181017413827));
#18345=CARTESIAN_POINT('Ctrl Pts',(4.97090455397163,-4.05336249490537,19.7166178587943));
#18346=CARTESIAN_POINT('Ctrl Pts',(1.3292771434127,-2.62965050343175,19.915133976206));
#18347=CARTESIAN_POINT('Ctrl Pts',(0.551472646603815,1.20224539704524,20.1136500936177));
#18348=CARTESIAN_POINT('Ctrl Pts',(3.3497896271543,3.93314783354192,20.3121662110293));
#18349=CARTESIAN_POINT('Ctrl Pts',(7.16158262229433,3.06214829760668,20.510682328441));
#18350=CARTESIAN_POINT('Ctrl Pts',(8.49608411816253,-0.613108395518473,
20.7091984458526));
#18351=CARTESIAN_POINT('Ctrl Pts',(6.13118302381429,-3.72689209317441,20.9077145632643));
#18352=CARTESIAN_POINT('Ctrl Pts',(2.23261078765349,-3.42765888460072,21.1062306806759));
#18353=CARTESIAN_POINT('Ctrl Pts',(0.370605683008962,0.0105590905653954,
21.3047467980876));
#18354=CARTESIAN_POINT('Ctrl Pts',(2.250356607504,3.43910732612115,21.5032629154992));
#18355=CARTESIAN_POINT('Ctrl Pts',(6.15042334082164,3.71818634797007,21.7017790329109));
#18356=CARTESIAN_POINT('Ctrl Pts',(8.49919910975228,0.592221314373082,21.9002951503225));
#18357=CARTESIAN_POINT('Ctrl Pts',(7.14571944818345,-3.07608926032515,22.0988112677342));
#18358=CARTESIAN_POINT('Ctrl Pts',(3.32947585071529,-3.92737479389549,22.2973273851459));
#18359=CARTESIAN_POINT('Ctrl Pts',(0.545310524977601,-1.18204713458114,
22.4958435025575));
#18360=CARTESIAN_POINT('Ctrl Pts',(1.34291119900688,2.64578051982372,22.6943596199692));
#18361=CARTESIAN_POINT('Ctrl Pts',(4.99184635260365,4.05064557959106,22.8928757373808));
#18362=CARTESIAN_POINT('Ctrl Pts',(8.15049824324278,1.74602012818506,23.0913918547925));
#18363=CARTESIAN_POINT('Ctrl Pts',(7.92621886181009,-2.15760353803636,23.2899079722041));
#18364=CARTESIAN_POINT('Ctrl Pts',(4.52442717371885,-4.08528469325705,23.4884240896158));
#18365=CARTESIAN_POINT('Ctrl Pts',(1.06036526828869,-2.27183616857484,23.6869402070274));
#18366=CARTESIAN_POINT('Ctrl Pts',(0.706458758169362,1.62230144113535,23.8854563244391));
#18367=CARTESIAN_POINT('Ctrl Pts',(3.78660979300229,4.03041197296648,24.0839724418507));
#18368=CARTESIAN_POINT('Ctrl Pts',(7.48045570332662,2.74822735016753,24.2824885592624));
#18369=CARTESIAN_POINT('Ctrl Pts',(8.40451183040988,-1.05203519730533,24.481004676674));
#18370=CARTESIAN_POINT('Ctrl Pts',(5.71394743641032,-3.88635869185298,24.6795207940858));
#18371=CARTESIAN_POINT('Ctrl Pts',(1.87003416737941,-3.16648164392546,24.8780369114974));
#18372=CARTESIAN_POINT('Ctrl Pts',(0.398188145107553,0.462946646320358,
25.076553028909));
#18373=CARTESIAN_POINT('Ctrl Pts',(1.88978798161488,2.58492499113116,25.2088971071835));
#18374=CARTESIAN_POINT('Ctrl Pts',(2.91960708544911,3.09611134481228,25.2750691463207));
#18375=CARTESIAN_POINT('Ctrl Pts',(2.58997049159961,-2.62015330925654,0.00319355095334283));
#18376=CARTESIAN_POINT('Ctrl Pts',(1.71783944528228,-1.99894889552244,0.0694097009926075));
#18377=CARTESIAN_POINT('Ctrl Pts',(0.65845605968771,0.171475772890977,0.20179789016909));
#18378=CARTESIAN_POINT('Ctrl Pts',(2.5459024084217,3.29075405988094,0.400358118482792));
#18379=CARTESIAN_POINT('Ctrl Pts',(6.18433372098768,3.38626231280436,0.598874235894448));
#18380=CARTESIAN_POINT('Ctrl Pts',(8.23950371306965,0.385416781850904,0.797390353306103));
#18381=CARTESIAN_POINT('Ctrl Pts',(6.83072086642306,-2.97082408396747,0.995906470717762));
#18382=CARTESIAN_POINT('Ctrl Pts',(3.24739392835603,-3.60517206763711,1.19442258812942));
#18383=CARTESIAN_POINT('Ctrl Pts',(0.771445147794971,-0.938633334672633,
1.39293870554108));
#18384=CARTESIAN_POINT('Ctrl Pts',(1.6701033647243,2.58783275185508,1.59145482295273));
#18385=CARTESIAN_POINT('Ctrl Pts',(5.12049770482736,3.74423103498232,1.78997094036439));
#18386=CARTESIAN_POINT('Ctrl Pts',(7.96276883664299,1.47182751406662,1.98848705777604));
#18387=CARTESIAN_POINT('Ctrl Pts',(7.59404699250464,-2.14849653622342,2.1870031751877));
#18388=CARTESIAN_POINT('Ctrl Pts',(4.35198598660702,-3.80124283382013,2.38551929259936));
#18389=CARTESIAN_POINT('Ctrl Pts',(1.20561125008781,-1.97289654529749,2.58403541001101));
#18390=CARTESIAN_POINT('Ctrl Pts',(1.0363089362513,1.66219780307218,2.78255152742267));
#18391=CARTESIAN_POINT('Ctrl Pts',(3.99912495903867,3.77507940693446,2.98106764483432));
#18392=CARTESIAN_POINT('Ctrl Pts',(7.38076768128599,2.43081698451723,3.17958376224598));
#18393=CARTESIAN_POINT('Ctrl Pts',(8.08439358796167,-1.13954237620741,3.37809987965763));
#18394=CARTESIAN_POINT('Ctrl Pts',(5.4656351638386,-3.66632999264102,3.5766159970693));
#18395=CARTESIAN_POINT('Ctrl Pts',(1.92270171311447,-2.83556261008053,3.77513211448094));
#18396=CARTESIAN_POINT('Ctrl Pts',(0.700144216203009,0.591959212043988,
3.97364823189261));
#18397=CARTESIAN_POINT('Ctrl Pts',(2.91755761499276,3.47737597536012,4.17216434930425));
#18398=CARTESIAN_POINT('Ctrl Pts',(6.54427687678886,3.1782780050441,4.37068046671592));
#18399=CARTESIAN_POINT('Ctrl Pts',(8.2590215005,-0.0314265247951463,4.56919658412757));
#18400=CARTESIAN_POINT('Ctrl Pts',(6.49146097171637,-3.21235123071783,4.76771270153922));
#18401=CARTESIAN_POINT('Ctrl Pts',(2.86029360321679,-3.45146579032245,4.96622881895089));
#18402=CARTESIAN_POINT('Ctrl Pts',(0.690873397337037,-0.529793630188544,
5.16474493636253));
#18403=CARTESIAN_POINT('Ctrl Pts',(1.96991411271267,2.8770534572674,5.36326105377419));
#18404=CARTESIAN_POINT('Ctrl Pts',(5.52609459169944,3.64914971667956,5.56177717118585));
#18405=CARTESIAN_POINT('Ctrl Pts',(8.1027323975949,1.07942407934716,5.7602932885975));
#18406=CARTESIAN_POINT('Ctrl Pts',(7.34019164048911,-2.47881759682101,5.95880940600916));
#18407=CARTESIAN_POINT('Ctrl Pts',(3.93679264073839,-3.76700527003896,6.15732552342081));
#18408=CARTESIAN_POINT('Ctrl Pts',(1.00930346276847,-1.60544117293717,6.35584164083248));
#18409=CARTESIAN_POINT('Ctrl Pts',(1.23866300903221,2.02635541158186,6.55435775824412));
#18410=CARTESIAN_POINT('Ctrl Pts',(4.41482816993367,3.80245425555658,6.75287387565579));
#18411=CARTESIAN_POINT('Ctrl Pts',(7.6291273081915,2.09633782263408,6.95138999306744));
#18412=CARTESIAN_POINT('Ctrl Pts',(7.93796641543966,-1.5295649116789,7.14990611047909));
#18413=CARTESIAN_POINT('Ctrl Pts',(5.05851651200422,-3.75472119528823,7.34842222789076));
#18414=CARTESIAN_POINT('Ctrl Pts',(1.62772304650576,-2.54137523062185,7.5469383453024));
#18415=CARTESIAN_POINT('Ctrl Pts',(0.787441414036509,0.999313828164636,
7.74545446271406));
#18416=CARTESIAN_POINT('Ctrl Pts',(3.30718554976015,3.62485029208286,7.94397058012572));
#18417=CARTESIAN_POINT('Ctrl Pts',(6.8794217047968,2.93081781047529,8.14248669753737));
#18418=CARTESIAN_POINT('Ctrl Pts',(8.23276395950072,-0.447201871899268,
8.34100281494903));
#18419=CARTESIAN_POINT('Ctrl Pts',(6.12784722031342,-3.41568258667014,8.53951893236069));
#18420=CARTESIAN_POINT('Ctrl Pts',(2.49231419722064,-3.25614616174064,8.73803504977233));
#18421=CARTESIAN_POINT('Ctrl Pts',(0.655516877599837,-0.114693020356707,
8.93655116718401));
#18422=CARTESIAN_POINT('Ctrl Pts',(2.29955930716991,3.13179380737736,9.13506728459565));
#18423=CARTESIAN_POINT('Ctrl Pts',(5.9188587019336,3.51024343935022,9.33358340200731));
#18424=CARTESIAN_POINT('Ctrl Pts',(8.19892952254092,0.674078901476532,9.53209951941897));
#18425=CARTESIAN_POINT('Ctrl Pts',(7.05172628302556,-2.77939427202906,9.73061563683061));
#18426=CARTESIAN_POINT('Ctrl Pts',(3.52783588801619,-3.68755104089551,9.92913175424228));
#18427=CARTESIAN_POINT('Ctrl Pts',(0.854370129759403,-1.21871871116838,
10.1276478716539));
#18428=CARTESIAN_POINT('Ctrl Pts',(1.47963809495571,2.36619303175871,10.3261639890656));
#18429=CARTESIAN_POINT('Ctrl Pts',(4.83103127493619,3.78419020596524,10.5246801064772));
#18430=CARTESIAN_POINT('Ctrl Pts',(7.83940754573271,1.73669797247918,10.7231962238889));
#18431=CARTESIAN_POINT('Ctrl Pts',(7.74975314393437,-1.90122922870495,10.9217123413006));
#18432=CARTESIAN_POINT('Ctrl Pts',(4.64417186530054,-3.79804686745578,11.1202284587122));
#18433=CARTESIAN_POINT('Ctrl Pts',(1.36669597038421,-2.21668543150265,11.3187445761239));
#18434=CARTESIAN_POINT('Ctrl Pts',(0.91877553954763,1.39467435679268,11.5172606935355));
#18435=CARTESIAN_POINT('Ctrl Pts',(3.71060758300086,3.72881789865659,11.7157768109472));
#18436=CARTESIAN_POINT('Ctrl Pts',(7.18548542162604,2.64818093856821,11.9142929283589));
#18437=CARTESIAN_POINT('Ctrl Pts',(8.16118202999545,-0.857609751318129,
12.1128090457705));
#18438=CARTESIAN_POINT('Ctrl Pts',(5.74417301388192,-3.57801774441457,12.3113251631822));
#18439=CARTESIAN_POINT('Ctrl Pts',(2.14790925385559,-3.02174514829049,12.5098412805938));
#18440=CARTESIAN_POINT('Ctrl Pts',(0.665780693158256,0.301784174950485,
12.7083573980055));
#18441=CARTESIAN_POINT('Ctrl Pts',(2.65509247460188,3.34894529131551,12.9068735154171));
#18442=CARTESIAN_POINT('Ctrl Pts',(6.29407070946287,3.32920601358802,13.1053896328288));
#18443=CARTESIAN_POINT('Ctrl Pts',(8.25020835096136,0.260643196829997,13.3039057502404));
#18444=CARTESIAN_POINT('Ctrl Pts',(6.7321117566965,-3.04661170162563,13.5024218676521));
#18445=CARTESIAN_POINT('Ctrl Pts',(3.1300249104368,-3.56383755643203,13.7009379850637));
#18446=CARTESIAN_POINT('Ctrl Pts',(0.742670427029733,-0.817368768436538,
13.8994541024754));
#18447=CARTESIAN_POINT('Ctrl Pts',(1.75634213008195,2.67763078969056,14.0979702198871));
#18448=CARTESIAN_POINT('Ctrl Pts',(5.24273875601857,3.7205070045574,14.2964863372987));
#18449=CARTESIAN_POINT('Ctrl Pts',(8.0090845931027,1.35621367619806,14.4950024547104));
#18450=CARTESIAN_POINT('Ctrl Pts',(7.52201274521021,-2.25007433890389,14.693518572122));
#18451=CARTESIAN_POINT('Ctrl Pts',(4.22757434555207,-3.79578707538995,14.8920346895337));
#18452=CARTESIAN_POINT('Ctrl Pts',(1.14275341367199,-1.86539021176013,15.0905508069453));
#18453=CARTESIAN_POINT('Ctrl Pts',(1.09257027946957,1.77329552431533,15.289066924357));
#18454=CARTESIAN_POINT('Ctrl Pts',(4.12298170266298,3.78803095088039,15.4875830417686));
#18455=CARTESIAN_POINT('Ctrl Pts',(7.45879454642923,2.3337596886183,15.6860991591803));
#18456=CARTESIAN_POINT('Ctrl Pts',(8.04513486233581,-1.25772430366396,15.8846152765919));
#18457=CARTESIAN_POINT('Ctrl Pts',(5.34504334245093,-3.69740830310385,16.0831313940036));
#18458=CARTESIAN_POINT('Ctrl Pts',(1.83121243949837,-2.75107611072479,16.2816475114153));
#18459=CARTESIAN_POINT('Ctrl Pts',(0.721541654250978,0.714639252839528,
16.4801636288269));
#18460=CARTESIAN_POINT('Ctrl Pts',(3.03224638366176,3.52590158253341,16.6786797462386));
#18461=CARTESIAN_POINT('Ctrl Pts',(6.64722719080097,3.10821031270302,16.8771958636502));
#18462=CARTESIAN_POINT('Ctrl Pts',(8.25595341671681,-0.155920837071448,
17.0757119810619));
#18463=CARTESIAN_POINT('Ctrl Pts',(6.38518418493321,-3.27726265018464,17.2742280984735));
#18464=CARTESIAN_POINT('Ctrl Pts',(2.74813437211341,-3.39734966840464,17.4727442158852));
#18465=CARTESIAN_POINT('Ctrl Pts',(0.675545012814546,-0.406208484742623,
17.6712603332969));
#18466=CARTESIAN_POINT('Ctrl Pts',(2.06545401745235,2.9569307023417,17.8697764507085));
#18467=CARTESIAN_POINT('Ctrl Pts',(5.64500915845253,3.61216899900811,18.0682925681202));
#18468=CARTESIAN_POINT('Ctrl Pts',(8.13612192804524,0.959451637121888,18.2668086855318));
#18469=CARTESIAN_POINT('Ctrl Pts',(7.25747863782803,-2.57191328333314,18.4653248029435));
#18470=CARTESIAN_POINT('Ctrl Pts',(3.81372409941205,-3.74796894189382,18.6638409203551));
#18471=CARTESIAN_POINT('Ctrl Pts',(0.958583211925542,-1.49170593738941,
18.8623570377668));
#18472=CARTESIAN_POINT('Ctrl Pts',(1.306739689582,2.13063298930591,19.0608731551785));
#18473=CARTESIAN_POINT('Ctrl Pts',(4.53935845279781,3.80177875335989,19.2593892725901));
#18474=CARTESIAN_POINT('Ctrl Pts',(7.69606872911877,1.99132785253305,19.4579053900018));
#18475=CARTESIAN_POINT('Ctrl Pts',(7.88601529454458,-1.64274321646801,19.6564215074134));
#18476=CARTESIAN_POINT('Ctrl Pts',(4.93524869751396,-3.77242129631514,19.8549376248251));
#18477=CARTESIAN_POINT('Ctrl Pts',(1.54602485826833,-2.44738771167893,20.0534537422367));
#18478=CARTESIAN_POINT('Ctrl Pts',(0.822130498506685,1.11891698433359,20.2519698596484));
#18479=CARTESIAN_POINT('Ctrl Pts',(3.42649430375165,3.66053879154859,20.45048597706));
#18480=CARTESIAN_POINT('Ctrl Pts',(6.97408943990954,2.84990880161489,20.6490020944717));
#18481=CARTESIAN_POINT('Ctrl Pts',(8.21609576658401,-0.570613452685432,
20.8475182118833));
#18482=CARTESIAN_POINT('Ctrl Pts',(6.015107509745,-3.46857877108964,21.046034329295));
#18483=CARTESIAN_POINT('Ctrl Pts',(2.38674785836889,-3.19008561139642,21.2445504467067));
#18484=CARTESIAN_POINT('Ctrl Pts',(0.653799542140776,0.00982723311048271,
21.4430665641183));
#18485=CARTESIAN_POINT('Ctrl Pts',(2.40326370386975,3.2007405539671,21.64158268153));
#18486=CARTESIAN_POINT('Ctrl Pts',(6.03301426782987,3.46047642676426,21.8400987989417));
#18487=CARTESIAN_POINT('Ctrl Pts',(8.21899485607472,0.551174068759129,22.0386149163533));
#18488=CARTESIAN_POINT('Ctrl Pts',(6.95932575274402,-2.86288350711349,22.2371310337649));
#18489=CARTESIAN_POINT('Ctrl Pts',(3.40758848840856,-3.65516588504588,22.4356471511766));
#18490=CARTESIAN_POINT('Ctrl Pts',(0.816395477550012,-1.10011867661645,
22.6341632685882));
#18491=CARTESIAN_POINT('Ctrl Pts',(1.55871392857562,2.46239974611297,22.8326793859999));
#18492=CARTESIAN_POINT('Ctrl Pts',(4.95473900642221,3.76989269217354,23.0311955034116));
#18493=CARTESIAN_POINT('Ctrl Pts',(7.89446267408575,1.62500233414576,23.2297116208232));
#18494=CARTESIAN_POINT('Ctrl Pts',(7.68572824288089,-2.00805862937836,23.4282277382349));
#18495=CARTESIAN_POINT('Ctrl Pts',(4.5197169557303,-3.80213094627573,23.6267438556465));
#18496=CARTESIAN_POINT('Ctrl Pts',(1.29575144062437,-2.11437372177854,23.8252599730582));
#18497=CARTESIAN_POINT('Ctrl Pts',(0.966374421579891,1.50985866999905,24.0237760904698));
#18498=CARTESIAN_POINT('Ctrl Pts',(3.83303817896047,3.7510614900228,24.2222922078815));
#18499=CARTESIAN_POINT('Ctrl Pts',(7.27086121968984,2.55774591981802,24.4208083252931));
#18500=CARTESIAN_POINT('Ctrl Pts',(8.13087041382945,-0.979117951521988,
24.6193244427048));
#18501=CARTESIAN_POINT('Ctrl Pts',(5.62679079307294,-3.61699263579137,24.8178405601165));
#18502=CARTESIAN_POINT('Ctrl Pts',(2.04930166016011,-2.94701073564213,25.0163566775281));
#18503=CARTESIAN_POINT('Ctrl Pts',(0.679470245798868,0.430859512276974,
25.2148727949398));
#18504=CARTESIAN_POINT('Ctrl Pts',(2.06768632464525,2.40576215381105,25.3472168732142));
#18505=CARTESIAN_POINT('Ctrl Pts',(3.02612799462649,2.8815178478641,25.4133889123514));
#18506=CARTESIAN_POINT('Ctrl Pts',(7.67921910621823,-4.71466720739905E-12,
7.06143953130409));
#18507=CARTESIAN_POINT('Ctrl Pts',(7.67921910621831,0.0545498630660913,
7.05794747266055));
#18508=CARTESIAN_POINT('Ctrl Pts',(7.67783410610462,0.109093485856064,7.05449675160843));
#18509=CARTESIAN_POINT('Ctrl Pts',(7.67397229027254,0.185079155343071,7.04974406424712));
#18510=CARTESIAN_POINT('Ctrl Pts',(7.67266413224706,0.206568690253113,7.04840602391199));
#18511=CARTESIAN_POINT('Ctrl Pts',(7.67020844577946,0.241185816649767,7.04626001003213));
#18512=CARTESIAN_POINT('Ctrl Pts',(7.66919559031489,0.254322015162662,7.04544784665494));
#18513=CARTESIAN_POINT('Ctrl Pts',(7.66692191112318,0.281624966894758,7.04376421665415));
#18514=CARTESIAN_POINT('Ctrl Pts',(7.66564780386039,0.295790350290824,7.04289318545173));
#18515=CARTESIAN_POINT('Ctrl Pts',(7.66241913326567,0.329205624482212,7.04084409294529));
#18516=CARTESIAN_POINT('Ctrl Pts',(7.66038489069605,0.348447399679791,7.03966855651076));
#18517=CARTESIAN_POINT('Ctrl Pts',(7.6530305271936,0.412489953607678,7.03576978018177));
#18518=CARTESIAN_POINT('Ctrl Pts',(7.64694286227679,0.457198418187983,7.0330706032779));
#18519=CARTESIAN_POINT('Ctrl Pts',(7.63014773790944,0.563754898121742,7.02668095458917));
#18520=CARTESIAN_POINT('Ctrl Pts',(7.61856835416684,0.625447582698257,7.02301702342752));
#18521=CARTESIAN_POINT('Ctrl Pts',(7.53208656273389,1.02195459713622,6.99959512792977));
#18522=CARTESIAN_POINT('Ctrl Pts',(7.4059461969243,1.34325170704917,6.98144958759926));
#18523=CARTESIAN_POINT('Ctrl Pts',(7.21453106278311,1.66743364901107,6.95901953622476));
#18524=CARTESIAN_POINT('Ctrl Pts',(7.19704299798727,1.69602337056475,6.95700035940156));
#18525=CARTESIAN_POINT('Ctrl Pts',(7.1724331160615,1.73488124331287,6.95419170118274));
#18526=CARTESIAN_POINT('Ctrl Pts',(7.16569204497459,1.74538949448345,6.9534255965834));
#18527=CARTESIAN_POINT('Ctrl Pts',(7.15484438255907,1.76208500746242,6.9521974547987));
#18528=CARTESIAN_POINT('Ctrl Pts',(7.15077708781622,1.76829782648793,6.95173799300674));
#18529=CARTESIAN_POINT('Ctrl Pts',(7.14224598542037,1.78123137515562,6.95077628348628));
#18530=CARTESIAN_POINT('Ctrl Pts',(7.13777838645317,1.78794943866016,6.95027376979013));
#18531=CARTESIAN_POINT('Ctrl Pts',(7.12681494783224,1.80430198963618,6.94904344895844));
#18532=CARTESIAN_POINT('Ctrl Pts',(7.12029216956595,1.81391820683403,6.94831386601263));
#18533=CARTESIAN_POINT('Ctrl Pts',(7.09664511410958,1.84837729442617,6.94567809970447));
#18534=CARTESIAN_POINT('Ctrl Pts',(7.0792247380929,1.87301380605635,6.94375348487185));
#18535=CARTESIAN_POINT('Ctrl Pts',(7.03482017917462,1.93397801363059,6.93889682132624));
#18536=CARTESIAN_POINT('Ctrl Pts',(7.00741244238302,1.96998804594177,6.93594259379422));
#18537=CARTESIAN_POINT('Ctrl Pts',(6.88300525647569,2.12649139742149,6.92276058556181));
#18538=CARTESIAN_POINT('Ctrl Pts',(6.77816524591359,2.24048354031629,6.91224862792232));
#18539=CARTESIAN_POINT('Ctrl Pts',(6.50860736048722,2.49425508036803,6.88722768406429));
#18540=CARTESIAN_POINT('Ctrl Pts',(6.33721225166477,2.6259120767463,6.87286630142336));
#18541=CARTESIAN_POINT('Ctrl Pts',(6.12199490454193,2.75926665925321,6.85679631632119));
#18542=CARTESIAN_POINT('Ctrl Pts',(6.08971857443983,2.77849330529497,6.85443207935948));
#18543=CARTESIAN_POINT('Ctrl Pts',(6.03940100920803,2.80728704713101,6.85081504063938));
#18544=CARTESIAN_POINT('Ctrl Pts',(6.02159350464018,2.81725391519632,6.84954795653557));
#18545=CARTESIAN_POINT('Ctrl Pts',(5.99117344482579,2.83390257713619,6.84740504987146));
#18546=CARTESIAN_POINT('Ctrl Pts',(5.97860916200309,2.84067085116231,6.84652616077616));
#18547=CARTESIAN_POINT('Ctrl Pts',(5.95307214613288,2.8542093497338,6.84475212417148));
#18548=CARTESIAN_POINT('Ctrl Pts',(5.94009742753306,2.86097512860345,6.84385714923083));
#18549=CARTESIAN_POINT('Ctrl Pts',(5.9079452940464,2.87746359089304,6.84165475441424));
#18550=CARTESIAN_POINT('Ctrl Pts',(5.88871563032272,2.88708326332889,6.84035096422927));
#18551=CARTESIAN_POINT('Ctrl Pts',(5.81610436206522,2.92250314298512,6.83547655693551));
#18552=CARTESIAN_POINT('Ctrl Pts',(5.76210853617939,2.94702205490176,6.83195016001737));
#18553=CARTESIAN_POINT('Ctrl Pts',(5.62381835365986,3.00527057658443,6.82313671059623));
#18554=CARTESIAN_POINT('Ctrl Pts',(5.53871763960454,3.03695495190129,6.81791355744433));
#18555=CARTESIAN_POINT('Ctrl Pts',(5.32004022474157,3.10801025218747,6.80484974487328));
#18556=CARTESIAN_POINT('Ctrl Pts',(5.18504351812508,3.14239769296895,6.79711620624979));
#18557=CARTESIAN_POINT('Ctrl Pts',(4.88632415695871,3.19819886884139,6.78009289464508));
#18558=CARTESIAN_POINT('Ctrl Pts',(4.72233958322252,3.21598370194662,6.77080282897045));
#18559=CARTESIAN_POINT('Ctrl Pts',(4.53071098778791,3.22200820053171,6.75931067882571));
#18560=CARTESIAN_POINT('Ctrl Pts',(4.50367614109252,3.22251766300787,6.75767450568788));
#18561=CARTESIAN_POINT('Ctrl Pts',(4.4663052108205,3.22275155838395,6.75538832135935));
#18562=CARTESIAN_POINT('Ctrl Pts',(4.4559712302031,3.22276652914662,6.7547535498709));
#18563=CARTESIAN_POINT('Ctrl Pts',(4.4382326663515,3.22270690991921,6.75365923699334));
#18564=CARTESIAN_POINT('Ctrl Pts',(4.43082800828194,3.22265650147056,6.7532010259754));
#18565=CARTESIAN_POINT('Ctrl Pts',(4.41533765113833,3.22249765812268,6.75223939045816));
#18566=CARTESIAN_POINT('Ctrl Pts',(4.40725213376453,3.22238430944009,6.75173568443449));
#18567=CARTESIAN_POINT('Ctrl Pts',(4.38745473400983,3.22203224781219,6.75049818339108));
#18568=CARTESIAN_POINT('Ctrl Pts',(4.37574362641558,3.2217601053569,6.74976256505833));
#18569=CARTESIAN_POINT('Ctrl Pts',(4.33324338548577,3.22054061551258,6.74708061424375));
#18570=CARTESIAN_POINT('Ctrl Pts',(4.30246783862567,3.2192157246286,6.74511501416291));
#18571=CARTESIAN_POINT('Ctrl Pts',(4.22526128858735,3.21478238617426,6.74013260070047));
#18572=CARTESIAN_POINT('Ctrl Pts',(4.1788707185064,3.21110908295534,6.73709220825989));
#18573=CARTESIAN_POINT('Ctrl Pts',(3.80599027407461,3.17344339261597,6.71235907738362));
#18574=CARTESIAN_POINT('Ctrl Pts',(3.486332456222,3.0907556932948,6.68959230843498));
#18575=CARTESIAN_POINT('Ctrl Pts',(3.11979746471539,2.93332655536681,6.66383483414238));
#18576=CARTESIAN_POINT('Ctrl Pts',(3.05589615559065,2.90335881580813,6.65934585249315));
#18577=CARTESIAN_POINT('Ctrl Pts',(2.97190778834495,2.86055188500096,6.65344450995049));
#18578=CARTESIAN_POINT('Ctrl Pts',(2.95090853225848,2.8495555442316,6.65196884671701));
#18579=CARTESIAN_POINT('Ctrl Pts',(2.91673344162846,2.83117637183442,6.64956651451181));
#18580=CARTESIAN_POINT('Ctrl Pts',(2.90348508964356,2.82393098745104,6.64863502870482));
#18581=CARTESIAN_POINT('Ctrl Pts',(2.87791383845791,2.80971195893903,6.64683655592072));
#18582=CARTESIAN_POINT('Ctrl Pts',(2.86558503518017,2.80274970487728,6.64596918919227));
#18583=CARTESIAN_POINT('Ctrl Pts',(2.83685329473996,2.78627380744042,6.64394699982994));
#18584=CARTESIAN_POINT('Ctrl Pts',(2.82048753523173,2.77669613569922,6.64279451309375));
#18585=CARTESIAN_POINT('Ctrl Pts',(2.76740056055959,2.74499595198367,6.6390531587996));
#18586=CARTESIAN_POINT('Ctrl Pts',(2.73103512065816,2.72228454611836,6.63648571237267));
#18587=CARTESIAN_POINT('Ctrl Pts',(2.64597800151533,2.66677422141495,6.63046069388591));
#18588=CARTESIAN_POINT('Ctrl Pts',(2.59770739603153,2.63335684437312,6.62702565189595));
#18589=CARTESIAN_POINT('Ctrl Pts',(2.32466469171216,2.4330806882104,6.60742857800775));
#18590=CARTESIAN_POINT('Ctrl Pts',(2.12150553136897,2.23883961320361,6.59229460778197));
#18591=CARTESIAN_POINT('Ctrl Pts',(1.88712318114709,1.94766412125108,6.57087024492528));
#18592=CARTESIAN_POINT('Ctrl Pts',(1.83147651957991,1.87198945180368,6.56538487669216));
#18593=CARTESIAN_POINT('Ctrl Pts',(1.77035223314986,1.78077155976628,6.55873008886696));
#18594=CARTESIAN_POINT('Ctrl Pts',(1.76158506924278,1.76747594259092,6.5577590752292));
#18595=CARTESIAN_POINT('Ctrl Pts',(1.74750260969583,1.74577118725325,6.55617130538348));
#18596=CARTESIAN_POINT('Ctrl Pts',(1.74212695631936,1.73740127911217,6.5555583957658));
#18597=CARTESIAN_POINT('Ctrl Pts',(1.73259000765924,1.72239992766327,6.55445851383493));
#18598=CARTESIAN_POINT('Ctrl Pts',(1.72841402400765,1.71577805109736,6.55397252102732));
#18599=CARTESIAN_POINT('Ctrl Pts',(1.71933975850382,1.70127206672224,6.55290678858469));
#18600=CARTESIAN_POINT('Ctrl Pts',(1.71445146408054,1.69338210580463,6.55232643795355));
#18601=CARTESIAN_POINT('Ctrl Pts',(1.70059138453959,1.67079384729648,6.55066323723582));
#18602=CARTESIAN_POINT('Ctrl Pts',(1.69170338883237,1.6560448648964,6.54957519841967));
#18603=CARTESIAN_POINT('Ctrl Pts',(1.63028708352406,1.55225642267066,6.54190821677805));
#18604=CARTESIAN_POINT('Ctrl Pts',(1.581956513041,1.46081408225307,6.53510124996775));
#18605=CARTESIAN_POINT('Ctrl Pts',(1.44766852525336,1.17417306079102,6.51394136699242));
#18606=CARTESIAN_POINT('Ctrl Pts',(1.37659953460437,0.972612949668182,6.49934281088194));
#18607=CARTESIAN_POINT('Ctrl Pts',(1.29312558635291,0.631252147921198,6.47602193979214));
#18608=CARTESIAN_POINT('Ctrl Pts',(1.26896214407291,0.495004713421878,6.46705093425879));
#18609=CARTESIAN_POINT('Ctrl Pts',(1.25070726795639,0.33150916594133,6.45670309542836));
#18610=CARTESIAN_POINT('Ctrl Pts',(1.24811213979421,0.305373430999844,6.45506114259031));
#18611=CARTESIAN_POINT('Ctrl Pts',(1.24434977985552,0.262109829862578,6.45236273293054));
#18612=CARTESIAN_POINT('Ctrl Pts',(1.24299942787276,0.244999539383633,6.45130059021131));
#18613=CARTESIAN_POINT('Ctrl Pts',(1.24079978475586,0.213969230666835,6.44938325016281));
#18614=CARTESIAN_POINT('Ctrl Pts',(1.23990404209925,0.200053029587059,6.44852661909977));
#18615=CARTESIAN_POINT('Ctrl Pts',(1.23817025693055,0.170083702153091,6.44668860698538));
#18616=CARTESIAN_POINT('Ctrl Pts',(1.23736193587382,0.154029184025547,6.4457081776259));
#18617=CARTESIAN_POINT('Ctrl Pts',(1.23546770296442,0.109823313951739,6.44301969980809));
#18618=CARTESIAN_POINT('Ctrl Pts',(1.23463072691646,0.0816623168428676,
6.44131944048409));
#18619=CARTESIAN_POINT('Ctrl Pts',(1.23185162351298,-0.0857441899358567,
6.43128008385597));
#18620=CARTESIAN_POINT('Ctrl Pts',(1.23856693518712,-0.224994120066761,
6.42321786095159));
#18621=CARTESIAN_POINT('Ctrl Pts',(1.27574499601554,-0.552610559315221,
6.40449739916481));
#18622=CARTESIAN_POINT('Ctrl Pts',(1.31394717235191,-0.739552479198644,
6.39402076261361));
#18623=CARTESIAN_POINT('Ctrl Pts',(1.40408609072948,-1.04144522622785,6.37617311039338));
#18624=CARTESIAN_POINT('Ctrl Pts',(1.44663602769604,-1.15868369210127,6.36898760959665));
#18625=CARTESIAN_POINT('Ctrl Pts',(1.50246463102475,-1.28850868785228,6.36043218465812));
#18626=CARTESIAN_POINT('Ctrl Pts',(1.50918863123946,-1.30381549804905,6.3594137090073));
#18627=CARTESIAN_POINT('Ctrl Pts',(1.52015522525942,-1.32826197499614,6.35777033058758));
#18628=CARTESIAN_POINT('Ctrl Pts',(1.52432221555184,-1.33743548888224,6.35714983988396));
#18629=CARTESIAN_POINT('Ctrl Pts',(1.53181375854405,-1.35372461890982,6.35604098927605));
#18630=CARTESIAN_POINT('Ctrl Pts',(1.53512139198103,-1.3608478156862,6.3555536647527));
#18631=CARTESIAN_POINT('Ctrl Pts',(1.54230522728327,-1.37617176337293,6.35449998020553));
#18632=CARTESIAN_POINT('Ctrl Pts',(1.54618995698475,-1.38436812459012,6.35393312129449));
#18633=CARTESIAN_POINT('Ctrl Pts',(1.55712532754275,-1.40719112675114,6.35234576693081));
#18634=CARTESIAN_POINT('Ctrl Pts',(1.56425187325645,-1.42178080794705,6.3513207800823));
#18635=CARTESIAN_POINT('Ctrl Pts',(1.60765590912273,-1.5089620726903,6.34513690373842));
#18636=CARTESIAN_POINT('Ctrl Pts',(1.64655157937313,-1.58021020495437,6.33983699319324));
#18637=CARTESIAN_POINT('Ctrl Pts',(1.77114349345315,-1.78926284956254,6.32369506924111));
#18638=CARTESIAN_POINT('Ctrl Pts',(1.86459801223715,-1.92214392848086,6.31264122068349));
#18639=CARTESIAN_POINT('Ctrl Pts',(2.10164730026644,-2.21029724533973,6.28748151720168));
#18640=CARTESIAN_POINT('Ctrl Pts',(2.25132255145439,-2.35965197640766,6.27353937786568));
#18641=CARTESIAN_POINT('Ctrl Pts',(2.43575032279125,-2.51068998829175,6.25852989158309));
#18642=CARTESIAN_POINT('Ctrl Pts',(2.45717403514613,-2.52778320121041,6.25681518979986));
#18643=CARTESIAN_POINT('Ctrl Pts',(2.49263972149303,-2.55534700863238,6.25402276402041));
#18644=CARTESIAN_POINT('Ctrl Pts',(2.50655328009757,-2.56597982791365,6.25293864562728));
#18645=CARTESIAN_POINT('Ctrl Pts',(2.53172271028672,-2.58489150091124,6.25099757115393));
#18646=CARTESIAN_POINT('Ctrl Pts',(2.54294698154918,-2.59321149316611,6.25013901723904));
#18647=CARTESIAN_POINT('Ctrl Pts',(2.56700222314939,-2.61080121868161,6.24831382898448));
#18648=CARTESIAN_POINT('Ctrl Pts',(2.57984813343294,-2.62004996978445,6.24734802131185));
#18649=CARTESIAN_POINT('Ctrl Pts',(2.61482102242391,-2.64484045058727,6.24474213980746));
#18650=CARTESIAN_POINT('Ctrl Pts',(2.63707660440195,-2.66019917779934,6.24310906360733));
#18651=CARTESIAN_POINT('Ctrl Pts',(2.75799428501011,-2.74141789366567,6.23436648895444));
#18652=CARTESIAN_POINT('Ctrl Pts',(2.86004805611365,-2.80207657323799,6.2274535142884));
#18653=CARTESIAN_POINT('Ctrl Pts',(3.10274555887014,-2.92875656313907,6.21180223373956));
#18654=CARTESIAN_POINT('Ctrl Pts',(3.24527478284619,-2.99051716569644,6.20318165744625));
#18655=CARTESIAN_POINT('Ctrl Pts',(3.55137655637161,-3.09766789410364,6.18502229334651));
#18656=CARTESIAN_POINT('Ctrl Pts',(3.71518931338,-3.14089623823361,6.17549649820751));
#18657=CARTESIAN_POINT('Ctrl Pts',(3.90811462294718,-3.17587000544165,6.16374261435684));
#18658=CARTESIAN_POINT('Ctrl Pts',(3.93467356102573,-3.18034152761911,6.16211279383551));
#18659=CARTESIAN_POINT('Ctrl Pts',(3.9714816246255,-3.18606515979188,6.15983395863119));
#18660=CARTESIAN_POINT('Ctrl Pts',(3.98168622306138,-3.18760180494331,6.15920005256082));
#18661=CARTESIAN_POINT('Ctrl Pts',(3.99922168109147,-3.19015628634111,6.15810683660689));
#18662=CARTESIAN_POINT('Ctrl Pts',(4.00654906450147,-3.19119794004161,6.15764885108599));
#18663=CARTESIAN_POINT('Ctrl Pts',(4.02189312839014,-3.19332534020925,6.1566872203085));
#18664=CARTESIAN_POINT('Ctrl Pts',(4.02991036223953,-3.19440614853321,6.15618329067231));
#18665=CARTESIAN_POINT('Ctrl Pts',(4.04956404157137,-3.19698036744667,6.15494445306365));
#18666=CARTESIAN_POINT('Ctrl Pts',(4.06120467115549,-3.19844043525146,6.15420771293067));
#18667=CARTESIAN_POINT('Ctrl Pts',(4.10355507725739,-3.20351766479161,6.15151710531463));
#18668=CARTESIAN_POINT('Ctrl Pts',(4.13430744436685,-3.20675621774022,6.14954381136009));
#18669=CARTESIAN_POINT('Ctrl Pts',(4.21168338884739,-3.21378054377743,6.14453768907915));
#18670=CARTESIAN_POINT('Ctrl Pts',(4.25835073874192,-3.21699457562839,6.14148101275596));
#18671=CARTESIAN_POINT('Ctrl Pts',(4.63899007278846,-3.23489622157584,6.11632907114974));
#18672=CARTESIAN_POINT('Ctrl Pts',(4.97335016979985,-3.19855892402255,6.09313818176793));
#18673=CARTESIAN_POINT('Ctrl Pts',(5.35944158697716,-3.09435751119089,6.06738422899522));
#18674=CARTESIAN_POINT('Ctrl Pts',(5.42214657120999,-3.07536595252416,6.06322431739818));
#18675=CARTESIAN_POINT('Ctrl Pts',(5.50607932307142,-3.04712442341133,6.05768399963668));
#18676=CARTESIAN_POINT('Ctrl Pts',(5.5278466031188,-3.03953930103551,6.05624968716785));
#18677=CARTESIAN_POINT('Ctrl Pts',(5.56360313648351,-3.02664757856896,6.05389730155039));
#18678=CARTESIAN_POINT('Ctrl Pts',(5.57763986775712,-3.02147604017148,6.05297479163161));
#18679=CARTESIAN_POINT('Ctrl Pts',(5.6049523350546,-3.01119679654915,6.05118146066393));
#18680=CARTESIAN_POINT('Ctrl Pts',(5.61823124665056,-3.00609857019894,6.05031034840215));
#18681=CARTESIAN_POINT('Ctrl Pts',(5.64850016095526,-2.99424677950658,6.04832623648522));
#18682=CARTESIAN_POINT('Ctrl Pts',(5.66546741554319,-2.98743617863443,6.04721517666254));
#18683=CARTESIAN_POINT('Ctrl Pts',(5.72111869065572,-2.96454615671034,6.04357396356449));
#18684=CARTESIAN_POINT('Ctrl Pts',(5.75954817542988,-2.94785645329155,6.04106438575535));
#18685=CARTESIAN_POINT('Ctrl Pts',(5.84987264037354,-2.90651742284235,6.03516910679155));
#18686=CARTESIAN_POINT('Ctrl Pts',(5.90145610767507,-2.88122023594089,6.03180506668112));
#18687=CARTESIAN_POINT('Ctrl Pts',(6.09515758979043,-2.77971514464306,6.0191377611272));
#18688=CARTESIAN_POINT('Ctrl Pts',(6.23216579202492,-2.69425727127677,6.01011764512194));
#18689=CARTESIAN_POINT('Ctrl Pts',(6.5241172185557,-2.48017341526836,5.98987538747658));
#18690=CARTESIAN_POINT('Ctrl Pts',(6.67455803008167,-2.34659092720768,5.97870083864261));
#18691=CARTESIAN_POINT('Ctrl Pts',(6.82946475245728,-2.18075583845231,5.96508718217023));
#18692=CARTESIAN_POINT('Ctrl Pts',(6.84711913849459,-2.16138767641669,5.96350047187086));
#18693=CARTESIAN_POINT('Ctrl Pts',(6.87132121489615,-2.13417692134579,5.96127214354097));
#18694=CARTESIAN_POINT('Ctrl Pts',(6.87807130262276,-2.12651466823914,5.96064476501514));
#18695=CARTESIAN_POINT('Ctrl Pts',(6.88963211702837,-2.11326517144869,5.95955980615747));
#18696=CARTESIAN_POINT('Ctrl Pts',(6.89446034277903,-2.107693205832,5.95910350506069));
#18697=CARTESIAN_POINT('Ctrl Pts',(6.90456386884837,-2.0959521660517,5.95814181889217));
#18698=CARTESIAN_POINT('Ctrl Pts',(6.90983502322842,-2.08977968254442,5.95763612757738));
#18699=CARTESIAN_POINT('Ctrl Pts',(6.92275618613006,-2.07453283187,5.95638686010046));
#18700=CARTESIAN_POINT('Ctrl Pts',(6.93037944362659,-2.0654360467395,5.95564138266314));
#18701=CARTESIAN_POINT('Ctrl Pts',(6.95827833931186,-2.03176843041808,5.95288255568935));
#18702=CARTESIAN_POINT('Ctrl Pts',(6.97823884415019,-2.00694035881856,5.95084850390347));
#18703=CARTESIAN_POINT('Ctrl Pts',(7.12604202740783,-1.81740725256396,5.93534996911446));
#18704=CARTESIAN_POINT('Ctrl Pts',(7.23798981984625,-1.64095086079407,5.92111854117941));
#18705=CARTESIAN_POINT('Ctrl Pts',(7.3803369854828,-1.35960586758362,5.89982885787792));
#18706=CARTESIAN_POINT('Ctrl Pts',(7.42380131093422,-1.26193249485502,5.89266166909107));
#18707=CARTESIAN_POINT('Ctrl Pts',(7.5054964708819,-1.05065314499286,5.87772243499036));
#18708=CARTESIAN_POINT('Ctrl Pts',(7.54241008394384,-0.936703797256036,
5.86999377157115));
#18709=CARTESIAN_POINT('Ctrl Pts',(7.57999296240963,-0.794034710956098,
5.86072126571752));
#18710=CARTESIAN_POINT('Ctrl Pts',(7.58673492621508,-0.767025668870155,
5.85898303790319));
#18711=CARTESIAN_POINT('Ctrl Pts',(7.59683758733288,-0.724199320161467,
5.85625322076193));
#18712=CARTESIAN_POINT('Ctrl Pts',(7.60043052570603,-0.708438748581375,
5.85525422157419));
#18713=CARTESIAN_POINT('Ctrl Pts',(7.60690043584985,-0.679039225560604,
5.85340090817654));
#18714=CARTESIAN_POINT('Ctrl Pts',(7.60980778331766,-0.665407416356418,
5.85254564053503));
#18715=CARTESIAN_POINT('Ctrl Pts',(7.61532821032295,-0.638674543218368,
5.85087618797657));
#18716=CARTESIAN_POINT('Ctrl Pts',(7.61794844533969,-0.625575262008021,
5.85006179090648));
#18717=CARTESIAN_POINT('Ctrl Pts',(7.62365658001599,-0.596086570610306,
5.84823643786342));
#18718=CARTESIAN_POINT('Ctrl Pts',(7.62669887465297,-0.57968864502427,5.84722693839758));
#18719=CARTESIAN_POINT('Ctrl Pts',(7.63404904468938,-0.538281766951424,
5.84469127655215));
#18720=CARTESIAN_POINT('Ctrl Pts',(7.63818912353459,-0.513243910511666,
5.84317035789014));
#18721=CARTESIAN_POINT('Ctrl Pts',(7.66678699860404,-0.326623731942253,
5.8319200181707));
#18722=CARTESIAN_POINT('Ctrl Pts',(7.67921910621361,-0.163436536696629,
5.82257685402867));
#18723=CARTESIAN_POINT('Ctrl Pts',(7.67921910621823,-9.10799213826863E-11,
5.81337971654115));
#18724=CARTESIAN_POINT('',(2.58258872576669,-2.62522787511044,25.0015778214036));
#18725=CARTESIAN_POINT('Ctrl Pts',(2.62314711761431,-2.65048072028474,25.));
#18726=CARTESIAN_POINT('Ctrl Pts',(2.61007479697457,-2.64143867267145,25.0005259404679));
#18727=CARTESIAN_POINT('Ctrl Pts',(2.59706937140007,-2.63229991316527,25.0010518809357));
#18728=CARTESIAN_POINT('Ctrl Pts',(2.58413226446108,-2.62306544209225,25.0015778214036));
#18729=CARTESIAN_POINT('Ctrl Pts',(2.58086696126463,-2.62738283509833,25.));
#18730=CARTESIAN_POINT('Ctrl Pts',(2.51895112061205,-2.59291341350604,25.));
#18731=CARTESIAN_POINT('Ctrl Pts',(2.45838415266209,-2.55633419485211,25.));
#18732=CARTESIAN_POINT('Ctrl Pts',(2.39928606905601,-2.51767449708445,25.));
#18733=CARTESIAN_POINT('Ctrl Pts',(2.31388248279346,-2.46180674923679,25.));
#18734=CARTESIAN_POINT('Ctrl Pts',(2.23154518283394,-2.40159687600469,25.));
#18735=CARTESIAN_POINT('Ctrl Pts',(2.15235473238406,-2.3374492656266,25.));
#18736=CARTESIAN_POINT('Ctrl Pts',(2.0706327165835,-2.27125098036485,24.9999999999999));
#18737=CARTESIAN_POINT('Ctrl Pts',(1.99226142380909,-2.20085884507454,24.9999999999999));
#18738=CARTESIAN_POINT('Ctrl Pts',(1.91734952117858,-2.12666429431228,24.9999999999999));
#18739=CARTESIAN_POINT('Ctrl Pts',(1.84247962307714,-2.05251134584625,24.9999999999999));
#18740=CARTESIAN_POINT('Ctrl Pts',(1.77106477073175,-1.97455960018966,24.9999999999999));
#18741=CARTESIAN_POINT('Ctrl Pts',(1.70324071360077,-1.8931555210592,24.9999999999999));
#18742=CARTESIAN_POINT('Ctrl Pts',(1.68150575299838,-1.86706869394182,24.9999999999999));
#18743=CARTESIAN_POINT('Ctrl Pts',(1.66013978843617,-1.84062702848735,24.9999999999999));
#18744=CARTESIAN_POINT('Ctrl Pts',(1.63914800286785,-1.81384113209172,24.9999999999999));
#18745=CARTESIAN_POINT('Ctrl Pts',(1.62919321696348,-1.80113864601651,24.9999999999999));
#18746=CARTESIAN_POINT('Ctrl Pts',(1.6193222495985,-1.78835819280448,24.9999999999999));
#18747=CARTESIAN_POINT('Ctrl Pts',(1.60954519814125,-1.77551370299918,24.9999999999999));
#18748=CARTESIAN_POINT('Ctrl Pts',(1.54334451395581,-1.6885433094361,24.9999999999999));
#18749=CARTESIAN_POINT('Ctrl Pts',(1.48133988628096,-1.59850518093636,24.9999999999999));
#18750=CARTESIAN_POINT('Ctrl Pts',(1.42362862152261,-1.50583407628298,24.9999999999999));
#18751=CARTESIAN_POINT('Ctrl Pts',(1.36499217356469,-1.41167733880783,24.9999999999999));
#18752=CARTESIAN_POINT('Ctrl Pts',(1.31078728724555,-1.31480192020701,24.9999999999999));
#18753=CARTESIAN_POINT('Ctrl Pts',(1.26114495505595,-1.21561705804934,24.9999999999999));
#18754=CARTESIAN_POINT('Ctrl Pts',(1.2111258651229,-1.11567943784823,24.9999999999999));
#18755=CARTESIAN_POINT('Ctrl Pts',(1.16573827734856,-1.01339645096499,25.));
#18756=CARTESIAN_POINT('Ctrl Pts',(1.12515384086073,-0.909149914337555,
25.));
#18757=CARTESIAN_POINT('Ctrl Pts',(1.08984118530872,-0.818444649980424,
25.));
#18758=CARTESIAN_POINT('Ctrl Pts',(1.05816525700407,-0.726251929697037,
24.9999999999999));
#18759=CARTESIAN_POINT('Ctrl Pts',(1.03026717068748,-0.632807598513387,
24.9999999999999));
#18760=CARTESIAN_POINT('Ctrl Pts',(1.0257979958373,-0.617838146842787,25.));
#18761=CARTESIAN_POINT('Ctrl Pts',(1.02142649755212,-0.602838610619727,
24.9999999999999));
#18762=CARTESIAN_POINT('Ctrl Pts',(1.01715621625056,-0.587820957022462,
24.9999999999999));
#18763=CARTESIAN_POINT('Ctrl Pts',(0.985703770959921,-0.477209525408138,
24.9999999999999));
#18764=CARTESIAN_POINT('Ctrl Pts',(0.959689578443777,-0.365453494535015,
24.9999999999999));
#18765=CARTESIAN_POINT('Ctrl Pts',(0.93924671117129,-0.252983170698471,
25.));
#18766=CARTESIAN_POINT('Ctrl Pts',(0.918870509582298,-0.140879620803699,
25.));
#18767=CARTESIAN_POINT('Ctrl Pts',(0.904028866916014,-0.0280655825087988,
25.));
#18768=CARTESIAN_POINT('Ctrl Pts',(0.894895231890315,0.0850624586136153,
25.));
#18769=CARTESIAN_POINT('Ctrl Pts',(0.886340822666338,0.191016282665257,
25.));
#18770=CARTESIAN_POINT('Ctrl Pts',(0.882793434187598,0.297246370144321,
25.));
#18771=CARTESIAN_POINT('Ctrl Pts',(0.884434707218777,0.403440761847383,
25.));
#18772=CARTESIAN_POINT('Ctrl Pts',(0.885637860676345,0.481287742286474,
25.));
#18773=CARTESIAN_POINT('Ctrl Pts',(0.889630094231931,0.559115847805151,
25.));
#18774=CARTESIAN_POINT('Ctrl Pts',(0.896336380065494,0.636828108152072,
25.));
#18775=CARTESIAN_POINT('Ctrl Pts',(0.898266237245346,0.659191241384986,
25.));
#18776=CARTESIAN_POINT('Ctrl Pts',(0.900420926006865,0.681544782497862,
25.));
#18777=CARTESIAN_POINT('Ctrl Pts',(0.902798848013211,0.703886417160758,
25.));
#18778=CARTESIAN_POINT('Ctrl Pts',(0.90514245462499,0.725905643432187,25.));
#18779=CARTESIAN_POINT('Ctrl Pts',(0.907703616726005,0.747918192377519,
25.));
#18780=CARTESIAN_POINT('Ctrl Pts',(0.910476780326299,0.769891749104374,
25.));
#18781=CARTESIAN_POINT('Ctrl Pts',(0.924563913848233,0.881513157783874,
25.));
#18782=CARTESIAN_POINT('Ctrl Pts',(0.944128901058905,0.992259489847555,
25.));
#18783=CARTESIAN_POINT('Ctrl Pts',(0.968856780713456,1.10183615184693,25.));
#18784=CARTESIAN_POINT('Ctrl Pts',(0.994044372209712,1.21344993509565,25.));
#18785=CARTESIAN_POINT('Ctrl Pts',(1.0245887260487,1.32385079384828,25.));
#18786=CARTESIAN_POINT('Ctrl Pts',(1.06021172903275,1.43273620380258,25.));
#18787=CARTESIAN_POINT('Ctrl Pts',(1.09656535472959,1.54385483799233,25.));
#18788=CARTESIAN_POINT('Ctrl Pts',(1.13820822442275,1.65339597590095,25.));
#18789=CARTESIAN_POINT('Ctrl Pts',(1.18489932594814,1.76103650943336,25.));
#18790=CARTESIAN_POINT('Ctrl Pts',(1.22344065551518,1.84988875626652,25.));
#18791=CARTESIAN_POINT('Ctrl Pts',(1.26542279926213,1.93744616388805,25.));
#18792=CARTESIAN_POINT('Ctrl Pts',(1.31073612832854,2.02352051946335,25.));
#18793=CARTESIAN_POINT('Ctrl Pts',(1.32070254197158,2.04245209322752,25.));
#18794=CARTESIAN_POINT('Ctrl Pts',(1.33083018884825,2.0613118898127,25.));
#18795=CARTESIAN_POINT('Ctrl Pts',(1.34111804451498,2.08009784379795,25.));
#18796=CARTESIAN_POINT('Ctrl Pts',(1.35034361641663,2.09694403360137,25.));
#18797=CARTESIAN_POINT('Ctrl Pts',(1.35969385765356,2.11372318424346,25.));
#18798=CARTESIAN_POINT('Ctrl Pts',(1.36916492541488,2.13042919793156,25.));
#18799=CARTESIAN_POINT('Ctrl Pts',(1.42850674181193,2.2351022107311,25.));
#18800=CARTESIAN_POINT('Ctrl Pts',(1.49262023288704,2.33696417549315,25.));
#18801=CARTESIAN_POINT('Ctrl Pts',(1.56123071821778,2.43568204796968,25.));
#18802=CARTESIAN_POINT('Ctrl Pts',(1.63034991151195,2.53513185766571,25.));
#18803=CARTESIAN_POINT('Ctrl Pts',(1.70403334168491,2.63139161134848,25.));
#18804=CARTESIAN_POINT('Ctrl Pts',(1.78205063137054,2.72410643348489,25.));
#18805=CARTESIAN_POINT('Ctrl Pts',(1.81727298375025,2.76596425947796,25.));
#18806=CARTESIAN_POINT('Ctrl Pts',(1.85337933069364,2.80709927385776,25.));
#18807=CARTESIAN_POINT('Ctrl Pts',(1.89035154083729,2.84747716338277,25.));
#18808=CARTESIAN_POINT('Ctrl Pts',(1.90419446776442,2.8625952256245,25.));
#18809=CARTESIAN_POINT('Ctrl Pts',(1.91816074658184,2.87760919409566,25.));
#18810=CARTESIAN_POINT('Ctrl Pts',(1.93224291148647,2.89251028361586,25.));
#18811=CARTESIAN_POINT('Ctrl Pts',(2.01699807592679,2.98219424209656,25.));
#18812=CARTESIAN_POINT('Ctrl Pts',(2.10584503538453,3.06768542877611,25.));
#18813=CARTESIAN_POINT('Ctrl Pts',(2.19852420314815,3.14863093007319,25.));
#18814=CARTESIAN_POINT('Ctrl Pts',(2.29008964672514,3.22860371047983,25.));
#18815=CARTESIAN_POINT('Ctrl Pts',(2.38539622530628,3.30414016034279,25.));
#18816=CARTESIAN_POINT('Ctrl Pts',(2.48423691550681,3.37487470703325,25.));
#18817=CARTESIAN_POINT('Ctrl Pts',(2.55686352024641,3.42684935384624,25.));
#18818=CARTESIAN_POINT('Ctrl Pts',(2.63139913748095,3.47623095136753,25.));
#18819=CARTESIAN_POINT('Ctrl Pts',(2.70777463088727,3.52286199445091,25.));
#18820=CARTESIAN_POINT('Ctrl Pts',(2.17296269996979,-3.20554048108048,-0.411765747138983));
#18821=CARTESIAN_POINT('Ctrl Pts',(1.10598262521586,-2.44554835076675,-0.345549597099719));
#18822=CARTESIAN_POINT('Ctrl Pts',(-0.190085171851759,0.209786400507346,
-0.213161407923235));
#18823=CARTESIAN_POINT('Ctrl Pts',(2.11904905146237,4.02596493684606,-0.0146011796095345));
#18824=CARTESIAN_POINT('Ctrl Pts',(6.57036830017086,4.14281137096193,0.183914937802122));
#18825=CARTESIAN_POINT('Ctrl Pts',(9.08469850437939,0.471525498888313,0.382431055213778));
#18826=CARTESIAN_POINT('Ctrl Pts',(7.36116941620609,-3.63455711911314,0.580947172625436));
#18827=CARTESIAN_POINT('Ctrl Pts',(2.97726580402431,-4.41062931823268,0.77946329003709));
#18828=CARTESIAN_POINT('Ctrl Pts',(-0.0518523842630756,-1.14834011450979,
0.977979407448747));
#18829=CARTESIAN_POINT('Ctrl Pts',(1.04758148582589,3.16599895701937,1.1764955248604));
#18830=CARTESIAN_POINT('Ctrl Pts',(5.26885307852876,4.58075644304919,1.37501164227206));
#18831=CARTESIAN_POINT('Ctrl Pts',(8.74613631193873,1.80065901519612,1.57352775968371));
#18832=CARTESIAN_POINT('Ctrl Pts',(8.2950356860829,-2.62850749839492,1.77204387709537));
#18833=CARTESIAN_POINT('Ctrl Pts',(4.32864266632258,-4.6505056552148,1.97055999450703));
#18834=CARTESIAN_POINT('Ctrl Pts',(0.479313869061077,-2.41367545883394,
2.16907611191868));
#18835=CARTESIAN_POINT('Ctrl Pts',(0.272186515624751,2.03356129066451,2.36759222933034));
#18836=CARTESIAN_POINT('Ctrl Pts',(3.89694643539194,4.61849687019083,2.56610834674199));
#18837=CARTESIAN_POINT('Ctrl Pts',(8.03410612006349,2.97390317522259,2.76462446415365));
#18838=CARTESIAN_POINT('Ctrl Pts',(8.89493411795877,-1.39413568050936,2.9631405815653));
#18839=CARTESIAN_POINT('Ctrl Pts',(5.69110016326603,-4.48545097223521,3.16165669897696));
#18840=CARTESIAN_POINT('Ctrl Pts',(1.35661463604595,-3.46907591290164,3.36017281638862));
#18841=CARTESIAN_POINT('Ctrl Pts',(-0.139083166427389,0.724213049156903,
3.55868893380027));
#18842=CARTESIAN_POINT('Ctrl Pts',(2.57373840321099,4.25428138787658,3.75720505121192));
#18843=CARTESIAN_POINT('Ctrl Pts',(7.01072892820446,3.88835980295648,3.95572116862359));
#18844=CARTESIAN_POINT('Ctrl Pts',(9.10857690015422,-0.0384477492421469,
4.15423728603523));
#18845=CARTESIAN_POINT('Ctrl Pts',(6.94611304441007,-3.93004557143118,4.3527534034469));
#18846=CARTESIAN_POINT('Ctrl Pts',(2.50368062941278,-4.22258242327136,4.55126952085854));
#18847=CARTESIAN_POINT('Ctrl Pts',(-0.15042524517621,-0.648158610486061,
4.74978563827021));
#18848=CARTESIAN_POINT('Ctrl Pts',(1.41437509517098,3.51983652671062,4.94830175568186));
#18849=CARTESIAN_POINT('Ctrl Pts',(5.76506726388787,4.46443232806813,5.14681787309352));
#18850=CARTESIAN_POINT('Ctrl Pts',(8.91737013208296,1.32058592540232,5.34533399050517));
#18851=CARTESIAN_POINT('Ctrl Pts',(7.98446469607637,-3.03262794728552,5.54385010791683));
#18852=CARTESIAN_POINT('Ctrl Pts',(3.82068800849579,-4.60861883268182,5.74236622532849));
#18853=CARTESIAN_POINT('Ctrl Pts',(0.239147556357015,-1.9641242562649,5.94088234274014));
#18854=CARTESIAN_POINT('Ctrl Pts',(0.519749957626067,2.47907795239849,6.13939846015179));
#18855=CARTESIAN_POINT('Ctrl Pts',(4.40552487083362,4.65198772933701,6.33791457756345));
#18856=CARTESIAN_POINT('Ctrl Pts',(8.33795354574623,2.56469563392857,6.53643069497511));
#18857=CARTESIAN_POINT('Ctrl Pts',(8.71579260460107,-1.87129593734266,6.73494681238676));
#18858=CARTESIAN_POINT('Ctrl Pts',(5.19302422456139,-4.59359028502123,6.93346292979842));
#18859=CARTESIAN_POINT('Ctrl Pts',(0.995732677906764,-3.10916202902842,
7.13197904721008));
#18860=CARTESIAN_POINT('Ctrl Pts',(-0.0322822778871914,1.22257767061497,
7.33049516462173));
#18861=CARTESIAN_POINT('Ctrl Pts',(3.05041589877745,4.43470399540276,7.52901128203338));
#18862=CARTESIAN_POINT('Ctrl Pts',(7.42075085684839,3.58561275821527,7.72752739944505));
#18863=CARTESIAN_POINT('Ctrl Pts',(9.07645297431008,-0.547114437358846,
7.9260435168567));
#18864=CARTESIAN_POINT('Ctrl Pts',(6.5012617467849,-4.17880463841992,8.12455963426836));
#18865=CARTESIAN_POINT('Ctrl Pts',(2.05348831510913,-3.98362504090881,8.32307575168001));
#18866=CARTESIAN_POINT('Ctrl Pts',(-0.193681017610346,-0.140317407516647,
8.52159186909167));
#18867=CARTESIAN_POINT('Ctrl Pts',(1.81766867783776,3.83149023855917,8.72010798650331));
#18868=CARTESIAN_POINT('Ctrl Pts',(6.24558161029013,4.2944920068349,8.91862410391498));
#18869=CARTESIAN_POINT('Ctrl Pts',(9.03505934404192,0.824679685151172,9.11714022132663));
#18870=CARTESIAN_POINT('Ctrl Pts',(7.6315512320161,-3.40035860512303,9.31565633873829));
#18871=CARTESIAN_POINT('Ctrl Pts',(3.32036330565075,-4.51141316650472,9.51417245614994));
#18872=CARTESIAN_POINT('Ctrl Pts',(0.0495994604212725,-1.49100136617927,
9.71268857356161));
#18873=CARTESIAN_POINT('Ctrl Pts',(0.814563009263402,2.89484112343983,9.91120469097325));
#18874=CARTESIAN_POINT('Ctrl Pts',(4.91471488529713,4.62964317792977,10.1097208083849));
#18875=CARTESIAN_POINT('Ctrl Pts',(8.59521399360942,2.1247060752228,10.3082369257966));
#18876=CARTESIAN_POINT('Ctrl Pts',(8.48552926132444,-2.32599643497811,10.5067530432082));
#18877=CARTESIAN_POINT('Ctrl Pts',(4.68610787984395,-4.64659565516981,10.7052691606199));
#18878=CARTESIAN_POINT('Ctrl Pts',(0.676387677669684,-2.71193096197848,
10.9037852780315));
#18879=CARTESIAN_POINT('Ctrl Pts',(0.128394142987057,1.70626851979591,11.1023013954432));
#18880=CARTESIAN_POINT('Ctrl Pts',(3.54396933091606,4.56189974780998,11.3008175128549));
#18881=CARTESIAN_POINT('Ctrl Pts',(7.79519445548059,3.23982996331418,11.4993336302665));
#18882=CARTESIAN_POINT('Ctrl Pts',(8.98887841448097,-1.04921447348414,11.6978497476782));
#18883=CARTESIAN_POINT('Ctrl Pts',(6.03186814454124,-4.3774082536412,11.8963658650898));
#18884=CARTESIAN_POINT('Ctrl Pts',(1.63213740257258,-3.69685482224785,12.0948819825015));
#18885=CARTESIAN_POINT('Ctrl Pts',(-0.181124089683036,0.369207933724872,
12.2933980999131));
#18886=CARTESIAN_POINT('Ctrl Pts',(2.2526340504912,4.09715708707193,12.4919142173248));
#18887=CARTESIAN_POINT('Ctrl Pts',(6.70462241331237,4.07300771627025,12.6904303347364));
#18888=CARTESIAN_POINT('Ctrl Pts',(9.09779474190718,0.318875355730261,12.8889464521481));
#18889=CARTESIAN_POINT('Ctrl Pts',(7.24052934071316,-3.72727698993507,13.0874625695597));
#18890=CARTESIAN_POINT('Ctrl Pts',(2.83367453520978,-4.36005996854408,13.2859786869714));
#18891=CARTESIAN_POINT('Ctrl Pts',(-0.0870558709899348,-0.999982965095223,
13.4844948043831));
#18892=CARTESIAN_POINT('Ctrl Pts',(1.1530874699283,3.2758594160949,13.6830109217947));
#18893=CARTESIAN_POINT('Ctrl Pts',(5.41840487637927,4.55173205747878,13.8815270392064));
#18894=CARTESIAN_POINT('Ctrl Pts',(8.80279980247531,1.65921506374814,14.080043156618));
#18895=CARTESIAN_POINT('Ctrl Pts',(8.20690775291552,-2.75277952374592,14.2785592740297));
#18896=CARTESIAN_POINT('Ctrl Pts',(4.17643533161801,-4.64383098681233,14.4770753914414));
#18897=CARTESIAN_POINT('Ctrl Pts',(0.402412514292184,-2.28215036718792,
14.675591508853));
#18898=CARTESIAN_POINT('Ctrl Pts',(0.341017607518878,2.16948014760412,14.8741076262646));
#18899=CARTESIAN_POINT('Ctrl Pts',(4.04847489906614,4.63434201110855,15.0726237436763));
#18900=CARTESIAN_POINT('Ctrl Pts',(8.12956552465056,2.85516161537223,15.271139861088));
#18901=CARTESIAN_POINT('Ctrl Pts',(8.84690431993714,-1.53872147678918,15.4696559784996));
#18902=CARTESIAN_POINT('Ctrl Pts',(5.54356606143321,-4.52347271009317,15.6681720959113));
#18903=CARTESIAN_POINT('Ctrl Pts',(1.24468509012015,-3.36571368106855,15.8666882133229));
#18904=CARTESIAN_POINT('Ctrl Pts',(-0.112905173860372,0.874301914415817,
16.0652043307346));
#18905=CARTESIAN_POINT('Ctrl Pts',(2.71405060913991,4.31364844766405,16.2637204481462));
#18906=CARTESIAN_POINT('Ctrl Pts',(7.1366801074503,3.80263778683562,16.4622365655579));
#18907=CARTESIAN_POINT('Ctrl Pts',(9.10482335385156,-0.190756225336315,
16.6607526829696));
#18908=CARTESIAN_POINT('Ctrl Pts',(6.81609220134375,-4.00945931491334,16.8592688003812));
#18909=CARTESIAN_POINT('Ctrl Pts',(2.36646310311057,-4.15637583189606,17.0577849177929));
#18910=CARTESIAN_POINT('Ctrl Pts',(-0.16917825360623,-0.496962424679848,
17.2563010352045));
#18911=CARTESIAN_POINT('Ctrl Pts',(1.53126025266144,3.61755971783011,17.4548171526162));
#18912=CARTESIAN_POINT('Ctrl Pts',(5.91054938364417,4.41918948403437,17.6533332700278));
#18913=CARTESIAN_POINT('Ctrl Pts',(8.95821945609951,1.17380958265607,17.8518493874395));
#18914=CARTESIAN_POINT('Ctrl Pts',(7.88327219050615,-3.14652280629029,18.0503655048511));
#18915=CARTESIAN_POINT('Ctrl Pts',(3.67012384502666,-4.58532946245115,18.2488816222628));
#18916=CARTESIAN_POINT('Ctrl Pts',(0.177095531876928,-1.82497861910485,
18.4473977396744));
#18917=CARTESIAN_POINT('Ctrl Pts',(0.603036135785551,2.60665292882547,18.6459138570862));
#18918=CARTESIAN_POINT('Ctrl Pts',(4.55787735396168,4.65116130836808,18.8444299744978));
#18919=CARTESIAN_POINT('Ctrl Pts',(8.41985082781949,2.43622463611074,19.0429460919094));
#18920=CARTESIAN_POINT('Ctrl Pts',(8.65223471259592,-2.00976021586402,19.2414622093211));
#18921=CARTESIAN_POINT('Ctrl Pts',(5.04221626688697,-4.61524489208584,19.4399783267328));
#18922=CARTESIAN_POINT('Ctrl Pts',(0.895781713701428,-2.99417608693739,
19.6384944441444));
#18923=CARTESIAN_POINT('Ctrl Pts',(0.0101569427980723,1.36890222246852,
19.8370105615561));
#18924=CARTESIAN_POINT('Ctrl Pts',(3.1963802739596,4.47836591752857,20.0355266789677));
#18925=CARTESIAN_POINT('Ctrl Pts',(7.53656898706393,3.48662728959027,20.2340427963793));
#18926=CARTESIAN_POINT('Ctrl Pts',(9.05606082131957,-0.698098281184544,
20.432558913791));
#18927=CARTESIAN_POINT('Ctrl Pts',(6.36333405195284,-4.24351873734398,20.6310750312027));
#18928=CARTESIAN_POINT('Ctrl Pts',(1.9243366462227,-3.90280543100934,20.8295911486144));
#18929=CARTESIAN_POINT('Ctrl Pts',(-0.195782035254683,0.0120228054752082,
21.028107266026));
#18930=CARTESIAN_POINT('Ctrl Pts',(1.94454241477252,3.91584087042925,21.2266233834376));
#18931=CARTESIAN_POINT('Ctrl Pts',(6.38524148680512,4.23360619038166,21.4251395008493));
#18932=CARTESIAN_POINT('Ctrl Pts',(9.05960761710739,0.674315805600993,21.623655618261));
#18933=CARTESIAN_POINT('Ctrl Pts',(7.5185068390623,-3.50250076674849,21.8221717356726));
#18934=CARTESIAN_POINT('Ctrl Pts',(3.17325057532877,-4.47179261159471,22.0206878530843));
#18935=CARTESIAN_POINT('Ctrl Pts',(0.0031406198327811,-1.34590405051051,
22.2192039704959));
#18936=CARTESIAN_POINT('Ctrl Pts',(0.911305739869395,3.01254206724522,22.4177200879076));
#18937=CARTESIAN_POINT('Ctrl Pts',(5.06606104496655,4.6121513544261,22.6162362053192));
#18938=CARTESIAN_POINT('Ctrl Pts',(8.66256938155685,1.98805571626367,22.8147523227309));
#18939=CARTESIAN_POINT('Ctrl Pts',(8.4072000996685,-2.45669335535235,23.0132684401425));
#18940=CARTESIAN_POINT('Ctrl Pts',(4.53384760969594,-4.65159218721967,23.2117845575542));
#18941=CARTESIAN_POINT('Ctrl Pts',(0.589592923617338,-2.58676106216746,
23.4103006749659));
#18942=CARTESIAN_POINT('Ctrl Pts',(0.186627431348294,1.84718698340797,23.6088167923775));
#18943=CARTESIAN_POINT('Ctrl Pts',(3.69375302108596,4.58911293885384,23.8073329097892));
#18944=CARTESIAN_POINT('Ctrl Pts',(7.89964467060016,3.12919021086655,24.0058490272008));
#18945=CARTESIAN_POINT('Ctrl Pts',(8.95179466357075,-1.19786968887199,24.2043651446125));
#18946=CARTESIAN_POINT('Ctrl Pts',(5.88826072308503,-4.42509080397621,24.4028812620241));
#18947=CARTESIAN_POINT('Ctrl Pts',(1.51149918181804,-3.60542346049212,24.6013973794358));
#18948=CARTESIAN_POINT('Ctrl Pts',(-0.164376056275096,0.527120914407128,
24.7999134968474));
#18949=CARTESIAN_POINT('Ctrl Pts',(1.53399129555416,2.94325066577138,24.9322575751219));
#18950=CARTESIAN_POINT('Ctrl Pts',(2.70656526709436,3.52529833870864,24.9984296142591));
#18951=CARTESIAN_POINT('Ctrl Pts',(2.31196529717974,-3.01041142380583,-0.273445981108207));
#18952=CARTESIAN_POINT('Ctrl Pts',(1.30993489857133,-2.29668186568531,-0.207229831068943));
#18953=CARTESIAN_POINT('Ctrl Pts',(0.0927619053280601,0.197016191301887,
-0.0748416418924601));
#18954=CARTESIAN_POINT('Ctrl Pts',(2.26133350378215,3.78089464452436,0.123718586421241));
#18955=CARTESIAN_POINT('Ctrl Pts',(6.44169010710979,3.89062835157607,0.322234703832897));
#18956=CARTESIAN_POINT('Ctrl Pts',(8.80296690727615,0.442822593209179,0.520750821244553));
#18957=CARTESIAN_POINT('Ctrl Pts',(7.18435323294509,-3.41331277406459,0.719266938656211));
#18958=CARTESIAN_POINT('Ctrl Pts',(3.06730851213489,-4.14214356803415,0.917783056067867));
#18959=CARTESIAN_POINT('Ctrl Pts',(0.222580126422941,-1.07843785456408,
1.11629917347952));
#18960=CARTESIAN_POINT('Ctrl Pts',(1.25508877879203,2.97327688863128,1.31481529089117));
#18961=CARTESIAN_POINT('Ctrl Pts',(5.21940128729496,4.30191464036023,1.51333140830283));
#18962=CARTESIAN_POINT('Ctrl Pts',(8.48501382017349,1.69104851481962,1.71184752571448));
#18963=CARTESIAN_POINT('Ctrl Pts',(8.06137278822348,-2.46850384433775,1.91036364312614));
#18964=CARTESIAN_POINT('Ctrl Pts',(4.33642377308406,-4.36741804808325,2.1088797605378));
#18965=CARTESIAN_POINT('Ctrl Pts',(0.721412996069988,-2.26674915432179,
2.30739587794946));
#18966=CARTESIAN_POINT('Ctrl Pts',(0.526893989166935,1.90977346146706,2.50591199536111));
#18967=CARTESIAN_POINT('Ctrl Pts',(3.93100594327419,4.33735771577206,2.70442811277276));
#18968=CARTESIAN_POINT('Ctrl Pts',(7.81632664047099,2.79287444498747,2.90294423018442));
#18969=CARTESIAN_POINT('Ctrl Pts',(8.62475394129306,-1.30927124574203,3.10146034759608));
#18970=CARTESIAN_POINT('Ctrl Pts',(5.61594516345689,-4.21241064570382,3.29997646500774));
#18971=CARTESIAN_POINT('Ctrl Pts',(1.54531032840212,-3.25790481196126,3.49849258241939));
#18972=CARTESIAN_POINT('Ctrl Pts',(0.140659294449413,0.680128436785933,
3.69700869983105));
#18973=CARTESIAN_POINT('Ctrl Pts',(2.68834480713824,3.99531291703776,3.8955248172427));
#18974=CARTESIAN_POINT('Ctrl Pts',(6.85524491106594,3.65166587031902,4.09404093465435));
#18975=CARTESIAN_POINT('Ctrl Pts',(8.82539176693615,-0.0361073410931478,
4.29255705206602));
#18976=CARTESIAN_POINT('Ctrl Pts',(6.79456235351217,-3.69081412452673,4.49107316947766));
#18977=CARTESIAN_POINT('Ctrl Pts',(2.62255162068078,-3.96554354562172,4.68958928688933));
#18978=CARTESIAN_POINT('Ctrl Pts',(0.130007635661538,-0.608703617053558,
4.88810540430098));
#18979=CARTESIAN_POINT('Ctrl Pts',(1.59955476768487,3.30557550356288,5.08662152171263));
#18980=CARTESIAN_POINT('Ctrl Pts',(5.68540970649173,4.19267145760527,5.28513763912429));
#18981=CARTESIAN_POINT('Ctrl Pts',(8.64582422058695,1.24019864338394,5.48365375653594));
#18982=CARTESIAN_POINT('Ctrl Pts',(7.76970701088062,-2.84802449713069,5.68216987394761));
#18983=CARTESIAN_POINT('Ctrl Pts',(3.85938955257665,-4.32808097846753,5.88068599135924));
#18984=CARTESIAN_POINT('Ctrl Pts',(0.495866191827503,-1.844563228489,6.07920210877092));
#18985=CARTESIAN_POINT('Ctrl Pts',(0.759387641428115,2.32817043879295,6.27771822618256));
#18986=CARTESIAN_POINT('Ctrl Pts',(4.40862597053364,4.36880990474354,6.47623434359423));
#18987=CARTESIAN_POINT('Ctrl Pts',(8.10167813322798,2.40857636349708,6.67475046100588));
#18988=CARTESIAN_POINT('Ctrl Pts',(8.45651720821394,-1.75738559545474,6.87326657841754));
#18989=CARTESIAN_POINT('Ctrl Pts',(5.14818832037566,-4.31396725511023,7.0717826958292));
#18990=CARTESIAN_POINT('Ctrl Pts',(1.20639613410644,-2.9198997628929,7.27029881324085));
#18991=CARTESIAN_POINT('Ctrl Pts',(0.240958952754043,1.14815638979818,7.4688149306525));
#18992=CARTESIAN_POINT('Ctrl Pts',(3.13600578243834,4.16475276096279,7.66733104806417));
#18993=CARTESIAN_POINT('Ctrl Pts',(7.24030780616454,3.36734777563528,7.86584716547581));
#18994=CARTESIAN_POINT('Ctrl Pts',(8.79522330270695,-0.513810248872322,
8.06436328288747));
#18995=CARTESIAN_POINT('Ctrl Pts',(6.37679023796107,-3.92443062116999,8.26287940029913));
#18996=CARTESIAN_POINT('Ctrl Pts',(2.1997636091463,-3.74113208118609,8.46139551771078));
#18997=CARTESIAN_POINT('Ctrl Pts',(0.089384947459713,-0.131775945129999,
8.65991163512245));
#18998=CARTESIAN_POINT('Ctrl Pts',(1.97829888761515,3.5982580948319,8.8584277525341));
#18999=CARTESIAN_POINT('Ctrl Pts',(6.13667397417128,4.03307581767334,9.05694386994575));
#19000=CARTESIAN_POINT('Ctrl Pts',(8.75634940354159,0.774479423926291,9.2554599873574));
#19001=CARTESIAN_POINT('Ctrl Pts',(7.43827624901926,-3.19337049409171,9.45397610476906));
#19002=CARTESIAN_POINT('Ctrl Pts',(3.38952083310589,-4.23679245796831,9.65249222218073));
#19003=CARTESIAN_POINT('Ctrl Pts',(0.317856350200649,-1.40024048117564,
9.85100833959237));
#19004=CARTESIAN_POINT('Ctrl Pts',(1.03625470449417,2.71862509287945,10.049524457004));
#19005=CARTESIAN_POINT('Ctrl Pts',(4.88682034851015,4.34782552060827,10.2480405744157));
#19006=CARTESIAN_POINT('Ctrl Pts',(8.34327851098385,1.99537004097493,10.4465566918273));
#19007=CARTESIAN_POINT('Ctrl Pts',(8.24027055552775,-2.18440736622039,10.645072809239));
#19008=CARTESIAN_POINT('Ctrl Pts',(4.67212920832948,-4.36374605926514,10.8435889266506));
#19009=CARTESIAN_POINT('Ctrl Pts',(0.906490441907856,-2.54684911848653,
11.0421050440623));
#19010=CARTESIAN_POINT('Ctrl Pts',(0.391854608507251,1.60240379879482,11.2406211614739));
#19011=CARTESIAN_POINT('Ctrl Pts',(3.59951541494433,4.28420579809219,11.4391372788856));
#19012=CARTESIAN_POINT('Ctrl Pts',(7.59195811086242,3.04261362173219,11.6376533962972));
#19013=CARTESIAN_POINT('Ctrl Pts',(8.71297961965247,-0.98534623276214,11.8361695137089));
#19014=CARTESIAN_POINT('Ctrl Pts',(5.93596976765481,-4.11094475056566,12.0346856311206));
#19015=CARTESIAN_POINT('Ctrl Pts',(1.80406135300024,-3.47181826426207,12.2332017485322));
#19016=CARTESIAN_POINT('Ctrl Pts',(0.101177504597399,0.346733347466743,
12.4317178659439));
#19017=CARTESIAN_POINT('Ctrl Pts',(2.38678685852808,3.84775315515312,12.6302339833555));
#19018=CARTESIAN_POINT('Ctrl Pts',(6.56777184536255,3.82507381537617,12.8287501007672));
#19019=CARTESIAN_POINT('Ctrl Pts',(8.81526594492522,0.29946463609684,13.0272662181788));
#19020=CARTESIAN_POINT('Ctrl Pts',(7.07105681270762,-3.5003885604986,13.2257823355905));
#19021=CARTESIAN_POINT('Ctrl Pts',(2.93245799361878,-4.09465249784007,13.4242984530022));
#19022=CARTESIAN_POINT('Ctrl Pts',(0.189519561683291,-0.939111566208993,
13.6228145704138));
#19023=CARTESIAN_POINT('Ctrl Pts',(1.35417235664619,3.07644987396012,13.8213306878255));
#19024=CARTESIAN_POINT('Ctrl Pts',(5.3598495029257,4.27465703983832,14.0198468052371));
#19025=CARTESIAN_POINT('Ctrl Pts',(8.53822806601778,1.55821460123144,14.2183629226488));
#19026=CARTESIAN_POINT('Ctrl Pts',(7.97860941701375,-2.58521112879858,14.4168790400604));
#19027=CARTESIAN_POINT('Ctrl Pts',(4.19348166959603,-4.36114968300486,14.6153951574721));
#19028=CARTESIAN_POINT('Ctrl Pts',(0.649192814085452,-2.14323031537866,
14.8139112748837));
#19029=CARTESIAN_POINT('Ctrl Pts',(0.59153516483578,2.03741860650786,15.0124273922954));
#19030=CARTESIAN_POINT('Ctrl Pts',(4.07331050026509,4.35223832436584,15.2109435097071));
#19031=CARTESIAN_POINT('Ctrl Pts',(7.9059751985768,2.68136097312093,15.4094596271187));
#19032=CARTESIAN_POINT('Ctrl Pts',(8.57964783407003,-1.44505575241412,15.6079757445304));
#19033=CARTESIAN_POINT('Ctrl Pts',(5.47739182177246,-4.24811790776339,15.806491861942));
#19034=CARTESIAN_POINT('Ctrl Pts',(1.44019420657955,-3.16083449095397,16.0050079793537));
#19035=CARTESIAN_POINT('Ctrl Pts',(0.165243768843413,0.821081027223728,
16.2035240967653));
#19036=CARTESIAN_POINT('Ctrl Pts',(2.82011586731386,4.05106615928717,16.402040214177));
#19037=CARTESIAN_POINT('Ctrl Pts',(6.97352913523386,3.57116196212476,16.6005563315886));
#19038=CARTESIAN_POINT('Ctrl Pts',(8.82186670813997,-0.17914442924803,16.7990724490003));
#19039=CARTESIAN_POINT('Ctrl Pts',(6.67245619587356,-3.76539376000376,16.997588566412));
#19040=CARTESIAN_POINT('Ctrl Pts',(2.49368685944485,-3.90336711073225,17.1961046838236));
#19041=CARTESIAN_POINT('Ctrl Pts',(0.112396168534027,-0.466711111367439,
17.3946208012353));
#19042=CARTESIAN_POINT('Ctrl Pts',(1.70932484092508,3.39735004600064,17.5931369186469));
#19043=CARTESIAN_POINT('Ctrl Pts',(5.82203597524696,4.15018265569229,17.7916530360586));
#19044=CARTESIAN_POINT('Ctrl Pts',(8.68418694674809,1.10235693414467,17.9901691534703));
#19045=CARTESIAN_POINT('Ctrl Pts',(7.67467433961344,-2.9549862986379,18.1886852708819));
#19046=CARTESIAN_POINT('Ctrl Pts',(3.71799059648846,-4.30620928893205,18.3872013882936));
#19047=CARTESIAN_POINT('Ctrl Pts',(0.437591425226463,-1.7138877251997,18.5857175057052));
#19048=CARTESIAN_POINT('Ctrl Pts',(0.837603987051035,2.44797961565228,18.7842336231169));
#19049=CARTESIAN_POINT('Ctrl Pts',(4.55170438690705,4.36803379003202,18.9827497405285));
#19050=CARTESIAN_POINT('Ctrl Pts',(8.17859012825258,2.28792570825151,19.1812658579402));
#19051=CARTESIAN_POINT('Ctrl Pts',(8.39682823991214,-1.88742121606535,19.3797819753518));
#19052=CARTESIAN_POINT('Ctrl Pts',(5.0065604104293,-4.33430369349561,19.5782980927635));
#19053=CARTESIAN_POINT('Ctrl Pts',(1.11252942855707,-2.81191329518458,19.7768142101752));
#19054=CARTESIAN_POINT('Ctrl Pts',(0.280814794700937,1.28557380975688,19.9753303275868));
#19055=CARTESIAN_POINT('Ctrl Pts',(3.27308495055695,4.20575687553525,20.1738464449984));
#19056=CARTESIAN_POINT('Ctrl Pts',(7.34907580467911,3.27438779359847,20.3723625624101));
#19057=CARTESIAN_POINT('Ctrl Pts',(8.77607246974106,-0.65560333835151,20.5708786798217));
#19058=CARTESIAN_POINT('Ctrl Pts',(6.24725853788356,-3.98520541525919,20.7693947972334));
#19059=CARTESIAN_POINT('Ctrl Pts',(2.07847371693811,-3.66523215780504,20.9679109146451));
#19060=CARTESIAN_POINT('Ctrl Pts',(0.0874118238771355,0.0112909480203034,
21.1664270320568));
#19061=CARTESIAN_POINT('Ctrl Pts',(2.09744951113826,3.6774740982752,21.3649431494684));
#19062=CARTESIAN_POINT('Ctrl Pts',(6.26783241381338,3.97589626917586,21.56345926688));
#19063=CARTESIAN_POINT('Ctrl Pts',(8.77940336342984,0.633268559987037,21.7619753842917));
#19064=CARTESIAN_POINT('Ctrl Pts',(7.33211314362288,-3.28929501353682,21.9604915017033));
#19065=CARTESIAN_POINT('Ctrl Pts',(3.25136321302202,-4.1995837027451,22.159007619115));
#19066=CARTESIAN_POINT('Ctrl Pts',(0.274225572405194,-1.26397559254583,
22.3575237365266));
#19067=CARTESIAN_POINT('Ctrl Pts',(1.12710846943813,2.82916129353447,22.5560398539383));
#19068=CARTESIAN_POINT('Ctrl Pts',(5.0289536987851,4.33139846700858,22.75455597135));
#19069=CARTESIAN_POINT('Ctrl Pts',(8.40653381239982,1.86703792222437,22.9530720887616));
#19070=CARTESIAN_POINT('Ctrl Pts',(8.1667094807393,-2.30714844669435,23.1515882061733));
#19071=CARTESIAN_POINT('Ctrl Pts',(4.52913739170739,-4.36843844023836,23.3501043235849));
#19072=CARTESIAN_POINT('Ctrl Pts',(0.824979095953012,-2.42929861537115,
23.5486204409966));
#19073=CARTESIAN_POINT('Ctrl Pts',(0.44654309475883,1.73474421227166,23.7471365584082));
#19074=CARTESIAN_POINT('Ctrl Pts',(3.74018140704413,4.30976245591016,23.9456526758199));
#19075=CARTESIAN_POINT('Ctrl Pts',(7.69005018696339,2.93870878051704,24.1441687932315));
#19076=CARTESIAN_POINT('Ctrl Pts',(8.67815324699032,-1.12495244308866,24.3426849106432));
#19077=CARTESIAN_POINT('Ctrl Pts',(5.80110407974766,-4.15572474791461,24.5412010280549));
#19078=CARTESIAN_POINT('Ctrl Pts',(1.69076667459873,-3.38595255220879,24.7397171454665));
#19079=CARTESIAN_POINT('Ctrl Pts',(0.116906044416222,0.495033780363739,
24.9382332628782));
#19080=CARTESIAN_POINT('Ctrl Pts',(1.71188963858453,2.76408782845127,25.0705773411526));
#19081=CARTESIAN_POINT('Ctrl Pts',(2.81308617627174,3.31070484176046,25.1367493802898));
#19082=CARTESIAN_POINT('Ctrl Pts',(2.45096789438968,-2.81528236653118,-0.135126215077433));
#19083=CARTESIAN_POINT('Ctrl Pts',(1.5138871719268,-2.14781538060387,-0.0689100650381678));
#19084=CARTESIAN_POINT('Ctrl Pts',(0.375608982507884,0.184245982096433,
0.0634781241383155));
#19085=CARTESIAN_POINT('Ctrl Pts',(2.40361795610193,3.53582435220265,0.262038352452016));
#19086=CARTESIAN_POINT('Ctrl Pts',(6.31301191404873,3.63844533219021,0.460554469863673));
#19087=CARTESIAN_POINT('Ctrl Pts',(8.52123531017291,0.41411968753004,0.659070587275328));
#19088=CARTESIAN_POINT('Ctrl Pts',(7.00753704968407,-3.19206842901602,0.857586704686986));
#19089=CARTESIAN_POINT('Ctrl Pts',(3.15735122024546,-3.87365781783563,1.05610282209864));
#19090=CARTESIAN_POINT('Ctrl Pts',(0.497012637108953,-1.00853559461836,
1.25461893951029));
#19091=CARTESIAN_POINT('Ctrl Pts',(1.46259607175817,2.78055482024318,1.45313505692195));
#19092=CARTESIAN_POINT('Ctrl Pts',(5.16994949606116,4.02307283767128,1.6516511743336));
#19093=CARTESIAN_POINT('Ctrl Pts',(8.22389132840824,1.58143801444312,1.85016729174526));
#19094=CARTESIAN_POINT('Ctrl Pts',(7.82770989036406,-2.30850019028058,2.04868340915692));
#19095=CARTESIAN_POINT('Ctrl Pts',(4.34420487984554,-4.08433044095169,2.24719952656857));
#19096=CARTESIAN_POINT('Ctrl Pts',(0.963512123078899,-2.11982284980964,
2.44571564398023));
#19097=CARTESIAN_POINT('Ctrl Pts',(0.781601462709117,1.78598563226962,2.64423176139188));
#19098=CARTESIAN_POINT('Ctrl Pts',(3.96506545115642,4.05621856135326,2.84274787880354));
#19099=CARTESIAN_POINT('Ctrl Pts',(7.59854716087849,2.61184571475234,3.0412639962152));
#19100=CARTESIAN_POINT('Ctrl Pts',(8.35457376462735,-1.22440681097471,3.23978011362686));
#19101=CARTESIAN_POINT('Ctrl Pts',(5.54079016364776,-3.93937031917242,3.43829623103851));
#19102=CARTESIAN_POINT('Ctrl Pts',(1.7340060207583,-3.04673371102089,3.63681234845017));
#19103=CARTESIAN_POINT('Ctrl Pts',(0.420401755326215,0.636043824414959,
3.83532846586182));
#19104=CARTESIAN_POINT('Ctrl Pts',(2.8029512110655,3.73634444619894,4.03384458327349));
#19105=CARTESIAN_POINT('Ctrl Pts',(6.6997608939274,3.41497193768155,4.23236070068513));
#19106=CARTESIAN_POINT('Ctrl Pts',(8.54220663371807,-0.0337669329441494,
4.4308768180968));
#19107=CARTESIAN_POINT('Ctrl Pts',(6.64301166261426,-3.45158267762228,4.62939293550844));
#19108=CARTESIAN_POINT('Ctrl Pts',(2.74142261194879,-3.70850466797209,4.82790905292011));
#19109=CARTESIAN_POINT('Ctrl Pts',(0.410440516499291,-0.569248623621048,
5.02642517033176));
#19110=CARTESIAN_POINT('Ctrl Pts',(1.78473444019877,3.09131448041513,5.22494128774342));
#19111=CARTESIAN_POINT('Ctrl Pts',(5.60575214909559,3.92091058714242,5.42345740515506));
#19112=CARTESIAN_POINT('Ctrl Pts',(8.37427830909092,1.15981136136555,5.62197352256674));
#19113=CARTESIAN_POINT('Ctrl Pts',(7.55494932568486,-2.66342104697584,5.82048963997839));
#19114=CARTESIAN_POINT('Ctrl Pts',(3.89809109665752,-4.04754312425325,6.01900575739004));
#19115=CARTESIAN_POINT('Ctrl Pts',(0.752584827297987,-1.72500220071308,
6.21752187480171));
#19116=CARTESIAN_POINT('Ctrl Pts',(0.999025325230166,2.17726292518741,6.41603799221334));
#19117=CARTESIAN_POINT('Ctrl Pts',(4.41172707023364,4.08563208015006,6.61455410962502));
#19118=CARTESIAN_POINT('Ctrl Pts',(7.86540272070975,2.25245709306557,6.81307022703666));
#19119=CARTESIAN_POINT('Ctrl Pts',(8.1972418118268,-1.64347525356681,7.01158634444832));
#19120=CARTESIAN_POINT('Ctrl Pts',(5.10335241618994,-4.03434422519923,7.21010246185998));
#19121=CARTESIAN_POINT('Ctrl Pts',(1.4170595903061,-2.73063749675737,7.40861857927163));
#19122=CARTESIAN_POINT('Ctrl Pts',(0.514200183395272,1.07373510898141,7.60713469668328));
#19123=CARTESIAN_POINT('Ctrl Pts',(3.22159566609925,3.89480152652282,7.80565081409495));
#19124=CARTESIAN_POINT('Ctrl Pts',(7.05986475548066,3.14908279305528,8.0041669315066));
#19125=CARTESIAN_POINT('Ctrl Pts',(8.51399363110384,-0.480506060385796,
8.20268304891826));
#19126=CARTESIAN_POINT('Ctrl Pts',(6.25231872913724,-3.67005660392007,8.40119916632992));
#19127=CARTESIAN_POINT('Ctrl Pts',(2.34603890318347,-3.49863912146337,8.59971528374156));
#19128=CARTESIAN_POINT('Ctrl Pts',(0.372450912529775,-0.123234482743352,
8.79823140115322));
#19129=CARTESIAN_POINT('Ctrl Pts',(2.13892909739252,3.36502595110463,8.99674751856487));
#19130=CARTESIAN_POINT('Ctrl Pts',(6.02776633805246,3.77165962851178,9.19526363597655));
#19131=CARTESIAN_POINT('Ctrl Pts',(8.47763946304124,0.72427916270141,9.39377975338818));
#19132=CARTESIAN_POINT('Ctrl Pts',(7.24500126602242,-2.98638238306039,9.59229587079984));
#19133=CARTESIAN_POINT('Ctrl Pts',(3.45867836056103,-3.9621717494319,9.79081198821151));
#19134=CARTESIAN_POINT('Ctrl Pts',(0.586113239980029,-1.30947959617202,
9.98932810562315));
#19135=CARTESIAN_POINT('Ctrl Pts',(1.25794639972494,2.54240906231909,10.1878442230349));
#19136=CARTESIAN_POINT('Ctrl Pts',(4.85892581172318,4.06600786328675,10.3863603404465));
#19137=CARTESIAN_POINT('Ctrl Pts',(8.09134302835829,1.86603400672705,10.5848764578582));
#19138=CARTESIAN_POINT('Ctrl Pts',(7.99501184973105,-2.04281829746266,10.7833925752698));
#19139=CARTESIAN_POINT('Ctrl Pts',(4.658150536815,-4.08089646336047,10.9819086926815));
#19140=CARTESIAN_POINT('Ctrl Pts',(1.13659320614603,-2.38176727499459,11.1804248100931));
#19141=CARTESIAN_POINT('Ctrl Pts',(0.655315074027438,1.49853907779376,11.3789409275048));
#19142=CARTESIAN_POINT('Ctrl Pts',(3.6550614989726,4.00651184837438,11.5774570449165));
#19143=CARTESIAN_POINT('Ctrl Pts',(7.38872176624422,2.84539728015019,11.7759731623281));
#19144=CARTESIAN_POINT('Ctrl Pts',(8.43708082482397,-0.921477992040132,
11.9744892797398));
#19145=CARTESIAN_POINT('Ctrl Pts',(5.84007139076835,-3.84448124749012,12.1730053971514));
#19146=CARTESIAN_POINT('Ctrl Pts',(1.97598530342792,-3.24678170627628,12.3715215145631));
#19147=CARTESIAN_POINT('Ctrl Pts',(0.383479098877827,0.324258761208613,
12.5700376319747));
#19148=CARTESIAN_POINT('Ctrl Pts',(2.52093966656498,3.59834922323431,12.7685537493864));
#19149=CARTESIAN_POINT('Ctrl Pts',(6.43092127741269,3.5771399144821,12.967069866798));
#19150=CARTESIAN_POINT('Ctrl Pts',(8.53273714794332,0.280053916463419,13.1655859842097));
#19151=CARTESIAN_POINT('Ctrl Pts',(6.90158428470204,-3.27350013106212,13.3641021016213));
#19152=CARTESIAN_POINT('Ctrl Pts',(3.0312414520278,-3.82924502713605,13.562618219033));
#19153=CARTESIAN_POINT('Ctrl Pts',(0.466094994356506,-0.878240167322765,
13.7611343364446));
#19154=CARTESIAN_POINT('Ctrl Pts',(1.55525724336407,2.87704033182534,13.9596504538563));
#19155=CARTESIAN_POINT('Ctrl Pts',(5.30129412947213,3.99758202219787,14.1581665712679));
#19156=CARTESIAN_POINT('Ctrl Pts',(8.27365632956023,1.45721413871475,14.3566826886797));
#19157=CARTESIAN_POINT('Ctrl Pts',(7.75031108111198,-2.41764273385123,14.5551988060912));
#19158=CARTESIAN_POINT('Ctrl Pts',(4.21052800757405,-4.07846837919741,14.753714923503));
#19159=CARTESIAN_POINT('Ctrl Pts',(0.895973113878727,-2.00431026356939,
14.9522310409146));
#19160=CARTESIAN_POINT('Ctrl Pts',(0.842052722152676,1.9053570654116,15.1507471583263));
#19161=CARTESIAN_POINT('Ctrl Pts',(4.09814610146403,4.07013463762311,15.3492632757379));
#19162=CARTESIAN_POINT('Ctrl Pts',(7.682384872503,2.50756033086961,15.5477793931496));
#19163=CARTESIAN_POINT('Ctrl Pts',(8.31239134820293,-1.35139002803904,15.7462955105612));
#19164=CARTESIAN_POINT('Ctrl Pts',(5.41121758211169,-3.97276310543362,15.9448116279729));
#19165=CARTESIAN_POINT('Ctrl Pts',(1.63570332303896,-2.95595530083938,16.1433277453845));
#19166=CARTESIAN_POINT('Ctrl Pts',(0.443392711547191,0.767860140031627,
16.3418438627962));
#19167=CARTESIAN_POINT('Ctrl Pts',(2.92618112548781,3.7884838709103,16.5403599802078));
#19168=CARTESIAN_POINT('Ctrl Pts',(6.8103781630174,3.33968613741389,16.7388760976195));
#19169=CARTESIAN_POINT('Ctrl Pts',(8.5389100624284,-0.167532633159739,16.9373922150311));
#19170=CARTESIAN_POINT('Ctrl Pts',(6.52882019040339,-3.5213282050942,17.1359083324428));
#19171=CARTESIAN_POINT('Ctrl Pts',(2.62091061577914,-3.65035838956845,17.3344244498544));
#19172=CARTESIAN_POINT('Ctrl Pts',(0.393970590674286,-0.43645979805503,
17.5329405672661));
#19173=CARTESIAN_POINT('Ctrl Pts',(1.88738942918871,3.17714037417117,17.7314566846778));
#19174=CARTESIAN_POINT('Ctrl Pts',(5.73352256684974,3.8811758273502,17.9299728020894));
#19175=CARTESIAN_POINT('Ctrl Pts',(8.41015443739666,1.03090428563328,18.1284889195011));
#19176=CARTESIAN_POINT('Ctrl Pts',(7.46607648872073,-2.76344979098553,18.3270050369127));
#19177=CARTESIAN_POINT('Ctrl Pts',(3.76585734795025,-4.02708911541293,18.5255211543244));
#19178=CARTESIAN_POINT('Ctrl Pts',(0.698087318576006,-1.60279683129456,
18.724037271736));
#19179=CARTESIAN_POINT('Ctrl Pts',(1.07217183831651,2.28930630247911,18.9225533891477));
#19180=CARTESIAN_POINT('Ctrl Pts',(4.54553141985243,4.08490627169594,19.1210695065593));
#19181=CARTESIAN_POINT('Ctrl Pts',(7.93732942868568,2.13962678039228,19.319585623971));
#19182=CARTESIAN_POINT('Ctrl Pts',(8.14142176722837,-1.76508221626667,19.5181017413827));
#19183=CARTESIAN_POINT('Ctrl Pts',(4.97090455397163,-4.05336249490537,19.7166178587943));
#19184=CARTESIAN_POINT('Ctrl Pts',(1.3292771434127,-2.62965050343175,19.915133976206));
#19185=CARTESIAN_POINT('Ctrl Pts',(0.551472646603815,1.20224539704524,20.1136500936177));
#19186=CARTESIAN_POINT('Ctrl Pts',(3.3497896271543,3.93314783354192,20.3121662110293));
#19187=CARTESIAN_POINT('Ctrl Pts',(7.16158262229433,3.06214829760668,20.510682328441));
#19188=CARTESIAN_POINT('Ctrl Pts',(8.49608411816253,-0.613108395518473,
20.7091984458526));
#19189=CARTESIAN_POINT('Ctrl Pts',(6.13118302381429,-3.72689209317441,20.9077145632643));
#19190=CARTESIAN_POINT('Ctrl Pts',(2.23261078765349,-3.42765888460072,21.1062306806759));
#19191=CARTESIAN_POINT('Ctrl Pts',(0.370605683008962,0.0105590905653954,
21.3047467980876));
#19192=CARTESIAN_POINT('Ctrl Pts',(2.250356607504,3.43910732612115,21.5032629154992));
#19193=CARTESIAN_POINT('Ctrl Pts',(6.15042334082164,3.71818634797007,21.7017790329109));
#19194=CARTESIAN_POINT('Ctrl Pts',(8.49919910975228,0.592221314373082,21.9002951503225));
#19195=CARTESIAN_POINT('Ctrl Pts',(7.14571944818345,-3.07608926032515,22.0988112677342));
#19196=CARTESIAN_POINT('Ctrl Pts',(3.32947585071529,-3.92737479389549,22.2973273851459));
#19197=CARTESIAN_POINT('Ctrl Pts',(0.545310524977601,-1.18204713458114,
22.4958435025575));
#19198=CARTESIAN_POINT('Ctrl Pts',(1.34291119900688,2.64578051982372,22.6943596199692));
#19199=CARTESIAN_POINT('Ctrl Pts',(4.99184635260365,4.05064557959106,22.8928757373808));
#19200=CARTESIAN_POINT('Ctrl Pts',(8.15049824324278,1.74602012818506,23.0913918547925));
#19201=CARTESIAN_POINT('Ctrl Pts',(7.92621886181009,-2.15760353803636,23.2899079722041));
#19202=CARTESIAN_POINT('Ctrl Pts',(4.52442717371885,-4.08528469325705,23.4884240896158));
#19203=CARTESIAN_POINT('Ctrl Pts',(1.06036526828869,-2.27183616857484,23.6869402070274));
#19204=CARTESIAN_POINT('Ctrl Pts',(0.706458758169362,1.62230144113535,23.8854563244391));
#19205=CARTESIAN_POINT('Ctrl Pts',(3.78660979300229,4.03041197296648,24.0839724418507));
#19206=CARTESIAN_POINT('Ctrl Pts',(7.48045570332662,2.74822735016753,24.2824885592624));
#19207=CARTESIAN_POINT('Ctrl Pts',(8.40451183040988,-1.05203519730533,24.481004676674));
#19208=CARTESIAN_POINT('Ctrl Pts',(5.71394743641032,-3.88635869185298,24.6795207940858));
#19209=CARTESIAN_POINT('Ctrl Pts',(1.87003416737941,-3.16648164392546,24.8780369114974));
#19210=CARTESIAN_POINT('Ctrl Pts',(0.398188145107553,0.462946646320358,
25.076553028909));
#19211=CARTESIAN_POINT('Ctrl Pts',(1.88978798161488,2.58492499113116,25.2088971071835));
#19212=CARTESIAN_POINT('Ctrl Pts',(2.91960708544911,3.09611134481228,25.2750691463207));
#19213=CARTESIAN_POINT('Ctrl Pts',(2.58997049159961,-2.62015330925654,0.00319355095334283));
#19214=CARTESIAN_POINT('Ctrl Pts',(1.71783944528228,-1.99894889552244,0.0694097009926075));
#19215=CARTESIAN_POINT('Ctrl Pts',(0.65845605968771,0.171475772890977,0.20179789016909));
#19216=CARTESIAN_POINT('Ctrl Pts',(2.5459024084217,3.29075405988094,0.400358118482792));
#19217=CARTESIAN_POINT('Ctrl Pts',(6.18433372098768,3.38626231280436,0.598874235894448));
#19218=CARTESIAN_POINT('Ctrl Pts',(8.23950371306965,0.385416781850904,0.797390353306103));
#19219=CARTESIAN_POINT('Ctrl Pts',(6.83072086642306,-2.97082408396747,0.995906470717762));
#19220=CARTESIAN_POINT('Ctrl Pts',(3.24739392835603,-3.60517206763711,1.19442258812942));
#19221=CARTESIAN_POINT('Ctrl Pts',(0.771445147794971,-0.938633334672633,
1.39293870554108));
#19222=CARTESIAN_POINT('Ctrl Pts',(1.6701033647243,2.58783275185508,1.59145482295273));
#19223=CARTESIAN_POINT('Ctrl Pts',(5.12049770482736,3.74423103498232,1.78997094036439));
#19224=CARTESIAN_POINT('Ctrl Pts',(7.96276883664299,1.47182751406662,1.98848705777604));
#19225=CARTESIAN_POINT('Ctrl Pts',(7.59404699250464,-2.14849653622342,2.1870031751877));
#19226=CARTESIAN_POINT('Ctrl Pts',(4.35198598660702,-3.80124283382013,2.38551929259936));
#19227=CARTESIAN_POINT('Ctrl Pts',(1.20561125008781,-1.97289654529749,2.58403541001101));
#19228=CARTESIAN_POINT('Ctrl Pts',(1.0363089362513,1.66219780307218,2.78255152742267));
#19229=CARTESIAN_POINT('Ctrl Pts',(3.99912495903867,3.77507940693446,2.98106764483432));
#19230=CARTESIAN_POINT('Ctrl Pts',(7.38076768128599,2.43081698451723,3.17958376224598));
#19231=CARTESIAN_POINT('Ctrl Pts',(8.08439358796167,-1.13954237620741,3.37809987965763));
#19232=CARTESIAN_POINT('Ctrl Pts',(5.4656351638386,-3.66632999264102,3.5766159970693));
#19233=CARTESIAN_POINT('Ctrl Pts',(1.92270171311447,-2.83556261008053,3.77513211448094));
#19234=CARTESIAN_POINT('Ctrl Pts',(0.700144216203009,0.591959212043988,
3.97364823189261));
#19235=CARTESIAN_POINT('Ctrl Pts',(2.91755761499276,3.47737597536012,4.17216434930425));
#19236=CARTESIAN_POINT('Ctrl Pts',(6.54427687678886,3.1782780050441,4.37068046671592));
#19237=CARTESIAN_POINT('Ctrl Pts',(8.2590215005,-0.0314265247951463,4.56919658412757));
#19238=CARTESIAN_POINT('Ctrl Pts',(6.49146097171637,-3.21235123071783,4.76771270153922));
#19239=CARTESIAN_POINT('Ctrl Pts',(2.86029360321679,-3.45146579032245,4.96622881895089));
#19240=CARTESIAN_POINT('Ctrl Pts',(0.690873397337037,-0.529793630188544,
5.16474493636253));
#19241=CARTESIAN_POINT('Ctrl Pts',(1.96991411271267,2.8770534572674,5.36326105377419));
#19242=CARTESIAN_POINT('Ctrl Pts',(5.52609459169944,3.64914971667956,5.56177717118585));
#19243=CARTESIAN_POINT('Ctrl Pts',(8.1027323975949,1.07942407934716,5.7602932885975));
#19244=CARTESIAN_POINT('Ctrl Pts',(7.34019164048911,-2.47881759682101,5.95880940600916));
#19245=CARTESIAN_POINT('Ctrl Pts',(3.93679264073839,-3.76700527003896,6.15732552342081));
#19246=CARTESIAN_POINT('Ctrl Pts',(1.00930346276847,-1.60544117293717,6.35584164083248));
#19247=CARTESIAN_POINT('Ctrl Pts',(1.23866300903221,2.02635541158186,6.55435775824412));
#19248=CARTESIAN_POINT('Ctrl Pts',(4.41482816993367,3.80245425555658,6.75287387565579));
#19249=CARTESIAN_POINT('Ctrl Pts',(7.6291273081915,2.09633782263408,6.95138999306744));
#19250=CARTESIAN_POINT('Ctrl Pts',(7.93796641543966,-1.5295649116789,7.14990611047909));
#19251=CARTESIAN_POINT('Ctrl Pts',(5.05851651200422,-3.75472119528823,7.34842222789076));
#19252=CARTESIAN_POINT('Ctrl Pts',(1.62772304650576,-2.54137523062185,7.5469383453024));
#19253=CARTESIAN_POINT('Ctrl Pts',(0.787441414036509,0.999313828164636,
7.74545446271406));
#19254=CARTESIAN_POINT('Ctrl Pts',(3.30718554976015,3.62485029208286,7.94397058012572));
#19255=CARTESIAN_POINT('Ctrl Pts',(6.8794217047968,2.93081781047529,8.14248669753737));
#19256=CARTESIAN_POINT('Ctrl Pts',(8.23276395950072,-0.447201871899268,
8.34100281494903));
#19257=CARTESIAN_POINT('Ctrl Pts',(6.12784722031342,-3.41568258667014,8.53951893236069));
#19258=CARTESIAN_POINT('Ctrl Pts',(2.49231419722064,-3.25614616174064,8.73803504977233));
#19259=CARTESIAN_POINT('Ctrl Pts',(0.655516877599837,-0.114693020356707,
8.93655116718401));
#19260=CARTESIAN_POINT('Ctrl Pts',(2.29955930716991,3.13179380737736,9.13506728459565));
#19261=CARTESIAN_POINT('Ctrl Pts',(5.9188587019336,3.51024343935022,9.33358340200731));
#19262=CARTESIAN_POINT('Ctrl Pts',(8.19892952254092,0.674078901476532,9.53209951941897));
#19263=CARTESIAN_POINT('Ctrl Pts',(7.05172628302556,-2.77939427202906,9.73061563683061));
#19264=CARTESIAN_POINT('Ctrl Pts',(3.52783588801619,-3.68755104089551,9.92913175424228));
#19265=CARTESIAN_POINT('Ctrl Pts',(0.854370129759403,-1.21871871116838,
10.1276478716539));
#19266=CARTESIAN_POINT('Ctrl Pts',(1.47963809495571,2.36619303175871,10.3261639890656));
#19267=CARTESIAN_POINT('Ctrl Pts',(4.83103127493619,3.78419020596524,10.5246801064772));
#19268=CARTESIAN_POINT('Ctrl Pts',(7.83940754573271,1.73669797247918,10.7231962238889));
#19269=CARTESIAN_POINT('Ctrl Pts',(7.74975314393437,-1.90122922870495,10.9217123413006));
#19270=CARTESIAN_POINT('Ctrl Pts',(4.64417186530054,-3.79804686745578,11.1202284587122));
#19271=CARTESIAN_POINT('Ctrl Pts',(1.36669597038421,-2.21668543150265,11.3187445761239));
#19272=CARTESIAN_POINT('Ctrl Pts',(0.91877553954763,1.39467435679268,11.5172606935355));
#19273=CARTESIAN_POINT('Ctrl Pts',(3.71060758300086,3.72881789865659,11.7157768109472));
#19274=CARTESIAN_POINT('Ctrl Pts',(7.18548542162604,2.64818093856821,11.9142929283589));
#19275=CARTESIAN_POINT('Ctrl Pts',(8.16118202999545,-0.857609751318129,
12.1128090457705));
#19276=CARTESIAN_POINT('Ctrl Pts',(5.74417301388192,-3.57801774441457,12.3113251631822));
#19277=CARTESIAN_POINT('Ctrl Pts',(2.14790925385559,-3.02174514829049,12.5098412805938));
#19278=CARTESIAN_POINT('Ctrl Pts',(0.665780693158256,0.301784174950485,
12.7083573980055));
#19279=CARTESIAN_POINT('Ctrl Pts',(2.65509247460188,3.34894529131551,12.9068735154171));
#19280=CARTESIAN_POINT('Ctrl Pts',(6.29407070946287,3.32920601358802,13.1053896328288));
#19281=CARTESIAN_POINT('Ctrl Pts',(8.25020835096136,0.260643196829997,13.3039057502404));
#19282=CARTESIAN_POINT('Ctrl Pts',(6.7321117566965,-3.04661170162563,13.5024218676521));
#19283=CARTESIAN_POINT('Ctrl Pts',(3.1300249104368,-3.56383755643203,13.7009379850637));
#19284=CARTESIAN_POINT('Ctrl Pts',(0.742670427029733,-0.817368768436538,
13.8994541024754));
#19285=CARTESIAN_POINT('Ctrl Pts',(1.75634213008195,2.67763078969056,14.0979702198871));
#19286=CARTESIAN_POINT('Ctrl Pts',(5.24273875601857,3.7205070045574,14.2964863372987));
#19287=CARTESIAN_POINT('Ctrl Pts',(8.0090845931027,1.35621367619806,14.4950024547104));
#19288=CARTESIAN_POINT('Ctrl Pts',(7.52201274521021,-2.25007433890389,14.693518572122));
#19289=CARTESIAN_POINT('Ctrl Pts',(4.22757434555207,-3.79578707538995,14.8920346895337));
#19290=CARTESIAN_POINT('Ctrl Pts',(1.14275341367199,-1.86539021176013,15.0905508069453));
#19291=CARTESIAN_POINT('Ctrl Pts',(1.09257027946957,1.77329552431533,15.289066924357));
#19292=CARTESIAN_POINT('Ctrl Pts',(4.12298170266298,3.78803095088039,15.4875830417686));
#19293=CARTESIAN_POINT('Ctrl Pts',(7.45879454642923,2.3337596886183,15.6860991591803));
#19294=CARTESIAN_POINT('Ctrl Pts',(8.04513486233581,-1.25772430366396,15.8846152765919));
#19295=CARTESIAN_POINT('Ctrl Pts',(5.34504334245093,-3.69740830310385,16.0831313940036));
#19296=CARTESIAN_POINT('Ctrl Pts',(1.83121243949837,-2.75107611072479,16.2816475114153));
#19297=CARTESIAN_POINT('Ctrl Pts',(0.721541654250978,0.714639252839528,
16.4801636288269));
#19298=CARTESIAN_POINT('Ctrl Pts',(3.03224638366176,3.52590158253341,16.6786797462386));
#19299=CARTESIAN_POINT('Ctrl Pts',(6.64722719080097,3.10821031270302,16.8771958636502));
#19300=CARTESIAN_POINT('Ctrl Pts',(8.25595341671681,-0.155920837071448,
17.0757119810619));
#19301=CARTESIAN_POINT('Ctrl Pts',(6.38518418493321,-3.27726265018464,17.2742280984735));
#19302=CARTESIAN_POINT('Ctrl Pts',(2.74813437211341,-3.39734966840464,17.4727442158852));
#19303=CARTESIAN_POINT('Ctrl Pts',(0.675545012814546,-0.406208484742623,
17.6712603332969));
#19304=CARTESIAN_POINT('Ctrl Pts',(2.06545401745235,2.9569307023417,17.8697764507085));
#19305=CARTESIAN_POINT('Ctrl Pts',(5.64500915845253,3.61216899900811,18.0682925681202));
#19306=CARTESIAN_POINT('Ctrl Pts',(8.13612192804524,0.959451637121888,18.2668086855318));
#19307=CARTESIAN_POINT('Ctrl Pts',(7.25747863782803,-2.57191328333314,18.4653248029435));
#19308=CARTESIAN_POINT('Ctrl Pts',(3.81372409941205,-3.74796894189382,18.6638409203551));
#19309=CARTESIAN_POINT('Ctrl Pts',(0.958583211925542,-1.49170593738941,
18.8623570377668));
#19310=CARTESIAN_POINT('Ctrl Pts',(1.306739689582,2.13063298930591,19.0608731551785));
#19311=CARTESIAN_POINT('Ctrl Pts',(4.53935845279781,3.80177875335989,19.2593892725901));
#19312=CARTESIAN_POINT('Ctrl Pts',(7.69606872911877,1.99132785253305,19.4579053900018));
#19313=CARTESIAN_POINT('Ctrl Pts',(7.88601529454458,-1.64274321646801,19.6564215074134));
#19314=CARTESIAN_POINT('Ctrl Pts',(4.93524869751396,-3.77242129631514,19.8549376248251));
#19315=CARTESIAN_POINT('Ctrl Pts',(1.54602485826833,-2.44738771167893,20.0534537422367));
#19316=CARTESIAN_POINT('Ctrl Pts',(0.822130498506685,1.11891698433359,20.2519698596484));
#19317=CARTESIAN_POINT('Ctrl Pts',(3.42649430375165,3.66053879154859,20.45048597706));
#19318=CARTESIAN_POINT('Ctrl Pts',(6.97408943990954,2.84990880161489,20.6490020944717));
#19319=CARTESIAN_POINT('Ctrl Pts',(8.21609576658401,-0.570613452685432,
20.8475182118833));
#19320=CARTESIAN_POINT('Ctrl Pts',(6.015107509745,-3.46857877108964,21.046034329295));
#19321=CARTESIAN_POINT('Ctrl Pts',(2.38674785836889,-3.19008561139642,21.2445504467067));
#19322=CARTESIAN_POINT('Ctrl Pts',(0.653799542140776,0.00982723311048271,
21.4430665641183));
#19323=CARTESIAN_POINT('Ctrl Pts',(2.40326370386975,3.2007405539671,21.64158268153));
#19324=CARTESIAN_POINT('Ctrl Pts',(6.03301426782987,3.46047642676426,21.8400987989417));
#19325=CARTESIAN_POINT('Ctrl Pts',(8.21899485607472,0.551174068759129,22.0386149163533));
#19326=CARTESIAN_POINT('Ctrl Pts',(6.95932575274402,-2.86288350711349,22.2371310337649));
#19327=CARTESIAN_POINT('Ctrl Pts',(3.40758848840856,-3.65516588504588,22.4356471511766));
#19328=CARTESIAN_POINT('Ctrl Pts',(0.816395477550012,-1.10011867661645,
22.6341632685882));
#19329=CARTESIAN_POINT('Ctrl Pts',(1.55871392857562,2.46239974611297,22.8326793859999));
#19330=CARTESIAN_POINT('Ctrl Pts',(4.95473900642221,3.76989269217354,23.0311955034116));
#19331=CARTESIAN_POINT('Ctrl Pts',(7.89446267408575,1.62500233414576,23.2297116208232));
#19332=CARTESIAN_POINT('Ctrl Pts',(7.68572824288089,-2.00805862937836,23.4282277382349));
#19333=CARTESIAN_POINT('Ctrl Pts',(4.5197169557303,-3.80213094627573,23.6267438556465));
#19334=CARTESIAN_POINT('Ctrl Pts',(1.29575144062437,-2.11437372177854,23.8252599730582));
#19335=CARTESIAN_POINT('Ctrl Pts',(0.966374421579891,1.50985866999905,24.0237760904698));
#19336=CARTESIAN_POINT('Ctrl Pts',(3.83303817896047,3.7510614900228,24.2222922078815));
#19337=CARTESIAN_POINT('Ctrl Pts',(7.27086121968984,2.55774591981802,24.4208083252931));
#19338=CARTESIAN_POINT('Ctrl Pts',(8.13087041382945,-0.979117951521988,
24.6193244427048));
#19339=CARTESIAN_POINT('Ctrl Pts',(5.62679079307294,-3.61699263579137,24.8178405601165));
#19340=CARTESIAN_POINT('Ctrl Pts',(2.04930166016011,-2.94701073564213,25.0163566775281));
#19341=CARTESIAN_POINT('Ctrl Pts',(0.679470245798868,0.430859512276974,
25.2148727949398));
#19342=CARTESIAN_POINT('Ctrl Pts',(2.06768632464525,2.40576215381105,25.3472168732142));
#19343=CARTESIAN_POINT('Ctrl Pts',(3.02612799462649,2.8815178478641,25.4133889123514));
#19344=CARTESIAN_POINT('Ctrl Pts',(6.63714354025255,2.37292574162131,4.40103865535666));
#19345=CARTESIAN_POINT('Ctrl Pts',(6.55488268407852,2.44852193194201,4.39474007739806));
#19346=CARTESIAN_POINT('Ctrl Pts',(6.46865122448045,2.51987705892792,4.38835546741982));
#19347=CARTESIAN_POINT('Ctrl Pts',(6.34696491642476,2.61030910125518,4.37937007910812));
#19348=CARTESIAN_POINT('Ctrl Pts',(6.31472595028534,2.63335701953105,4.3769914840871));
#19349=CARTESIAN_POINT('Ctrl Pts',(6.27107086748787,2.66336558124252,4.37376126446673));
#19350=CARTESIAN_POINT('Ctrl Pts',(6.26002316332987,2.67085913519949,4.37294301546732));
#19351=CARTESIAN_POINT('Ctrl Pts',(6.24261690245388,2.68250839866624,4.37165205802598));
#19352=CARTESIAN_POINT('Ctrl Pts',(6.23628951948158,2.6867107311069,4.37118241763664));
#19353=CARTESIAN_POINT('Ctrl Pts',(6.22330577753974,2.69526789232314,4.37021785074703));
#19354=CARTESIAN_POINT('Ctrl Pts',(6.21664813926369,2.69962045492134,4.36972277181799));
#19355=CARTESIAN_POINT('Ctrl Pts',(6.20075835437278,2.70992495110662,4.36854012389255));
#19356=CARTESIAN_POINT('Ctrl Pts',(6.19151180693461,2.71585438495665,4.36785109474993));
#19357=CARTESIAN_POINT('Ctrl Pts',(6.160121426178,2.73575802401162,4.36550966700096));
#19358=CARTESIAN_POINT('Ctrl Pts',(6.13783830938031,2.7495091732844,4.36384371533823));
#19359=CARTESIAN_POINT('Ctrl Pts',(6.08327588902524,2.78226893632639,4.35975985053256));
#19360=CARTESIAN_POINT('Ctrl Pts',(6.05082845238185,2.80098889165221,4.35732739463932));
#19361=CARTESIAN_POINT('Ctrl Pts',(5.92055058942352,2.87315321216537,4.34756715150589));
#19362=CARTESIAN_POINT('Ctrl Pts',(5.82030654684858,2.92206918328703,4.34007319236212));
#19363=CARTESIAN_POINT('Ctrl Pts',(5.46097046585614,3.0748899487689,4.31368798604764));
#19364=CARTESIAN_POINT('Ctrl Pts',(5.19105024728478,3.15030519228401,4.29483732674159));
#19365=CARTESIAN_POINT('Ctrl Pts',(4.87794294707159,3.19528722530131,4.2748209914205));
#19366=CARTESIAN_POINT('Ctrl Pts',(4.84104104073695,3.19993832188371,4.27248750713435));
#19367=CARTESIAN_POINT('Ctrl Pts',(4.78625005656266,3.20588259564447,4.26905934501755));
#19368=CARTESIAN_POINT('Ctrl Pts',(4.768418409425,3.20766680708476,4.26794935779944));
#19369=CARTESIAN_POINT('Ctrl Pts',(4.7366175001221,3.21058107167193,4.26597970089389));
#19370=CARTESIAN_POINT('Ctrl Pts',(4.722654121626,3.21176890323759,4.26511824015335));
#19371=CARTESIAN_POINT('Ctrl Pts',(4.6931501173022,3.21408500617995,4.26330498964153));
#19372=CARTESIAN_POINT('Ctrl Pts',(4.67760812520572,3.21519173232151,4.2623538961011));
#19373=CARTESIAN_POINT('Ctrl Pts',(4.63620557221076,3.2178383225922,4.25983077171111));
#19374=CARTESIAN_POINT('Ctrl Pts',(4.61033310461793,3.21917918065689,4.25826498224459));
#19375=CARTESIAN_POINT('Ctrl Pts',(4.48230818218853,3.22426715039714,4.25056729856685));
#19376=CARTESIAN_POINT('Ctrl Pts',(4.38002823204493,3.22346492852175,4.24457846371601));
#19377=CARTESIAN_POINT('Ctrl Pts',(4.05824805926166,3.2056131389574,4.22603670586311));
#19378=CARTESIAN_POINT('Ctrl Pts',(3.84037747209945,3.17095675489344,4.21395968460233));
#19379=CARTESIAN_POINT('Ctrl Pts',(3.49629258695045,3.07939594756862,4.19385642585561));
#19380=CARTESIAN_POINT('Ctrl Pts',(3.36721050871641,3.03613653969115,4.18605151726928));
#19381=CARTESIAN_POINT('Ctrl Pts',(3.22562740500828,2.9784948021723,4.17679911218933));
#19382=CARTESIAN_POINT('Ctrl Pts',(3.21004177644008,2.97200630279114,4.1757708375915));
#19383=CARTESIAN_POINT('Ctrl Pts',(3.18519325751506,2.96143170810658,4.1741146693485));
#19384=CARTESIAN_POINT('Ctrl Pts',(3.17589716340947,2.9574238008972,4.17349129744577));
#19385=CARTESIAN_POINT('Ctrl Pts',(3.15941805788424,2.95022675503432,4.17237925543451));
#19386=CARTESIAN_POINT('Ctrl Pts',(3.15222762705379,2.94705505388434,4.17189164343547));
#19387=CARTESIAN_POINT('Ctrl Pts',(3.1367918728316,2.9401787814991,4.17083965940718));
#19388=CARTESIAN_POINT('Ctrl Pts',(3.12855065247452,2.93646587635556,4.17027480545196));
#19389=CARTESIAN_POINT('Ctrl Pts',(3.10568063995503,2.92604631954392,4.16869861759416));
#19390=CARTESIAN_POINT('Ctrl Pts',(3.09108653173385,2.91926479528544,4.16768289114376));
#19391=CARTESIAN_POINT('Ctrl Pts',(3.00560381272456,2.87876185249217,4.16167762961063));
#19392=CARTESIAN_POINT('Ctrl Pts',(2.93592123784515,2.84257135568898,4.15655612283921));
#19393=CARTESIAN_POINT('Ctrl Pts',(2.68541284117065,2.70061929695741,4.13747898122937));
#19394=CARTESIAN_POINT('Ctrl Pts',(2.51369121042546,2.5798451953233,4.12312153948582));
#19395=CARTESIAN_POINT('Ctrl Pts',(2.22834397850403,2.33440408802079,4.09794487026822));
#19396=CARTESIAN_POINT('Ctrl Pts',(2.11042164841072,2.21586561164759,4.08702846526219));
#19397=CARTESIAN_POINT('Ctrl Pts',(1.98455041380825,2.06796451924443,4.07480193663515));
#19398=CARTESIAN_POINT('Ctrl Pts',(1.96716265469409,2.04700091311345,4.07309812618114));
#19399=CARTESIAN_POINT('Ctrl Pts',(1.93906762667253,2.01224058369367,4.07031975593556));
#19400=CARTESIAN_POINT('Ctrl Pts',(1.9282033194139,1.99857311759262,4.06923891004568));
#19401=CARTESIAN_POINT('Ctrl Pts',(1.90884863049959,1.97381421231537,4.06730140466714));
#19402=CARTESIAN_POINT('Ctrl Pts',(1.90031833680597,1.96275466801485,4.06644317176497));
#19403=CARTESIAN_POINT('Ctrl Pts',(1.88225380033723,1.93901643977188,4.06461624372245));
#19404=CARTESIAN_POINT('Ctrl Pts',(1.87274070080213,1.92632207479819,4.06364839295676));
#19405=CARTESIAN_POINT('Ctrl Pts',(1.8471730468032,1.89167420662591,4.06103099857694));
#19406=CARTESIAN_POINT('Ctrl Pts',(1.83130181161244,1.86958657831453,4.05938856069004));
#19407=CARTESIAN_POINT('Ctrl Pts',(1.7462413396612,1.74799070773689,4.05048324001675));
#19408=CARTESIAN_POINT('Ctrl Pts',(1.68242372657146,1.64483526708385,4.04342609480348));
#19409=CARTESIAN_POINT('Ctrl Pts',(1.54710730965076,1.39573022678048,4.02723439550252));
#19410=CARTESIAN_POINT('Ctrl Pts',(1.48053060468139,1.24749381197568,4.01823512076678));
#19411=CARTESIAN_POINT('Ctrl Pts',(1.39684237616308,1.01580908814963,4.00442603493253));
#19412=CARTESIAN_POINT('Ctrl Pts',(1.37138949904329,0.9356636824112,3.99969011159615));
#19413=CARTESIAN_POINT('Ctrl Pts',(1.32517093714158,0.767614272247132,3.98968340997938));
#19414=CARTESIAN_POINT('Ctrl Pts',(1.30490904509874,0.679651377057018,3.9844032805968));
#19415=CARTESIAN_POINT('Ctrl Pts',(1.28547292042375,0.575455991472863,3.97797809526813));
#19416=CARTESIAN_POINT('Ctrl Pts',(1.28269421267998,0.559927951396196,3.97701614546647));
#19417=CARTESIAN_POINT('Ctrl Pts',(1.27835703829167,0.534620704294659,3.97544028404424));
#19418=CARTESIAN_POINT('Ctrl Pts',(1.27672941411996,0.524853406381223,3.9748301245578));
#19419=CARTESIAN_POINT('Ctrl Pts',(1.27389602883365,0.507353346849962,3.97373314985021));
#19420=CARTESIAN_POINT('Ctrl Pts',(1.27267339156884,0.499623514805698,3.97324729181695));
#19421=CARTESIAN_POINT('Ctrl Pts',(1.27005674941131,0.482680715699323,3.97217941298946));
#19422=CARTESIAN_POINT('Ctrl Pts',(1.26867455853299,0.47346625807546,3.97159676239257));
#19423=CARTESIAN_POINT('Ctrl Pts',(1.26482731482698,0.447037631196479,3.96992049698131));
#19424=CARTESIAN_POINT('Ctrl Pts',(1.26246165270143,0.429809636743399,3.96882156870142));
#19425=CARTESIAN_POINT('Ctrl Pts',(1.24637826765028,0.305207683919472,3.96083271876518));
#19426=CARTESIAN_POINT('Ctrl Pts',(1.23794002750252,0.197232275798578,3.95369310244792));
#19427=CARTESIAN_POINT('Ctrl Pts',(1.22865345360236,-0.138725282627019,
3.93119484354953));
#19428=CARTESIAN_POINT('Ctrl Pts',(1.24653243089846,-0.366552032762402,
3.91558625067927));
#19429=CARTESIAN_POINT('Ctrl Pts',(1.31030989068635,-0.70868233097507,3.8926303279593));
#19430=CARTESIAN_POINT('Ctrl Pts',(1.3389117627164,-0.825463839051558,3.88487144671705));
#19431=CARTESIAN_POINT('Ctrl Pts',(1.38210312469079,-0.967040775300621,
3.87556839034563));
#19432=CARTESIAN_POINT('Ctrl Pts',(1.39057972650078,-0.993587660551746,
3.87382828416188));
#19433=CARTESIAN_POINT('Ctrl Pts',(1.4045180813754,-1.035361778117,3.87109618430907));
#19434=CARTESIAN_POINT('Ctrl Pts',(1.40975182770082,-1.05066308093795,3.87009676015599));
#19435=CARTESIAN_POINT('Ctrl Pts',(1.41971047807015,-1.07907777978,3.86824304451542));
#19436=CARTESIAN_POINT('Ctrl Pts',(1.42440568862094,-1.09220110866687,3.86738779626718));
#19437=CARTESIAN_POINT('Ctrl Pts',(1.4350298487967,-1.12129956485655,3.86549323885396));
#19438=CARTESIAN_POINT('Ctrl Pts',(1.44100068371131,-1.13725903411091,3.86445534932941));
#19439=CARTESIAN_POINT('Ctrl Pts',(1.45881585788157,-1.1837503947489,3.86143489130146));
#19440=CARTESIAN_POINT('Ctrl Pts',(1.47099954344172,-1.21415056836899,3.85946368227856));
#19441=CARTESIAN_POINT('Ctrl Pts',(1.49968350643886,-1.28267763377836,3.85502544082345));
#19442=CARTESIAN_POINT('Ctrl Pts',(1.51646197687699,-1.32068213309878,3.85256776540599));
#19443=CARTESIAN_POINT('Ctrl Pts',(1.5746066649179,-1.44578050557826,3.84447705397044));
#19444=CARTESIAN_POINT('Ctrl Pts',(1.61914674970129,-1.53134459804915,3.83894350740677));
#19445=CARTESIAN_POINT('Ctrl Pts',(1.778715517037,-1.80694666613101,3.82089462923562));
#19446=CARTESIAN_POINT('Ctrl Pts',(1.90952483699347,-1.98707954159423,3.80876126785247));
#19447=CARTESIAN_POINT('Ctrl Pts',(2.1168215912362,-2.21810207501499,3.79092449909815));
#19448=CARTESIAN_POINT('Ctrl Pts',(2.1785168759092,-2.2814157953018,3.78574902387989));
#19449=CARTESIAN_POINT('Ctrl Pts',(2.2541382939114,-2.35289247870969,3.77944059449199));
#19450=CARTESIAN_POINT('Ctrl Pts',(2.26562585417085,-2.3635925718365,3.77848318624358));
#19451=CARTESIAN_POINT('Ctrl Pts',(2.28446891407095,-2.38088855824728,3.77691329431993));
#19452=CARTESIAN_POINT('Ctrl Pts',(2.29177752751084,-2.3875354498998,3.77630451584164));
#19453=CARTESIAN_POINT('Ctrl Pts',(2.30492952173099,-2.39938663164652,3.77520899355371));
#19454=CARTESIAN_POINT('Ctrl Pts',(2.31076142675809,-2.40460336515258,3.77472319571049));
#19455=CARTESIAN_POINT('Ctrl Pts',(2.32359342226826,-2.41599793931169,3.77365420546329));
#19456=CARTESIAN_POINT('Ctrl Pts',(2.33060128390207,-2.42216653490683,3.7730703736257));
#19457=CARTESIAN_POINT('Ctrl Pts',(2.35080461701518,-2.43979508856389,3.77138738132441));
#19458=CARTESIAN_POINT('Ctrl Pts',(2.36406640284601,-2.45117806583521,3.77028284263082));
#19459=CARTESIAN_POINT('Ctrl Pts',(2.4621748538238,-2.53401106487337,3.76211735666286));
#19460=CARTESIAN_POINT('Ctrl Pts',(2.55055938668049,-2.60113908931772,3.75479440108431));
#19461=CARTESIAN_POINT('Ctrl Pts',(2.83233467554104,-2.79306617366292,3.7319551653276));
#19462=CARTESIAN_POINT('Ctrl Pts',(3.03579394575537,-2.90184944463289,3.71620264191942));
#19463=CARTESIAN_POINT('Ctrl Pts',(3.35635752644414,-3.03137811991607,3.6934343253737));
#19464=CARTESIAN_POINT('Ctrl Pts',(3.46587483272944,-3.06891300888237,3.68597227780328));
#19465=CARTESIAN_POINT('Ctrl Pts',(3.60371155635547,-3.10800295327964,3.67696974816441));
#19466=CARTESIAN_POINT('Ctrl Pts',(3.63033389859338,-3.11518514555741,3.67524826398053));
#19467=CARTESIAN_POINT('Ctrl Pts',(3.67264699455988,-3.12601980402549,3.67253880236369));
#19468=CARTESIAN_POINT('Ctrl Pts',(3.68827811827691,-3.12989768826049,3.67154359781388));
#19469=CARTESIAN_POINT('Ctrl Pts',(3.71613899817122,-3.13658832904476,3.6697796907865));
#19470=CARTESIAN_POINT('Ctrl Pts',(3.72835725498703,-3.13944710959247,3.66900952383088));
#19471=CARTESIAN_POINT('Ctrl Pts',(3.75669072457087,-3.14590215974455,3.66723123430979));
#19472=CARTESIAN_POINT('Ctrl Pts',(3.77281759004304,-3.14944611040867,3.66622480512684));
#19473=CARTESIAN_POINT('Ctrl Pts',(3.81852870812302,-3.15912367826299,3.66338786105483));
#19474=CARTESIAN_POINT('Ctrl Pts',(3.84817345768673,-3.16496553910517,3.66156665347908));
#19475=CARTESIAN_POINT('Ctrl Pts',(4.07958447297222,-3.20719631283937,3.64748521629961));
#19476=CARTESIAN_POINT('Ctrl Pts',(4.28433346042802,-3.22467592339774,3.63586481153996));
#19477=CARTESIAN_POINT('Ctrl Pts',(4.70776648503966,-3.22035175015661,3.61214653455955));
#19478=CARTESIAN_POINT('Ctrl Pts',(4.92533534426433,-3.19592825335681,3.6001191850577));
#19479=CARTESIAN_POINT('Ctrl Pts',(5.17531399632524,-3.14177983364646,3.58493232121331));
#19480=CARTESIAN_POINT('Ctrl Pts',(5.2117521295321,-3.13321971460517,3.58268278148958));
#19481=CARTESIAN_POINT('Ctrl Pts',(5.26068429100659,-3.12082134716424,3.57960328381719));
#19482=CARTESIAN_POINT('Ctrl Pts',(5.27331763260748,-3.11753851874338,3.57880290543457));
#19483=CARTESIAN_POINT('Ctrl Pts',(5.29321360210141,-3.112239229039,3.57753351194048));
#19484=CARTESIAN_POINT('Ctrl Pts',(5.30048985622825,-3.11027383697552,3.5770673923595));
#19485=CARTESIAN_POINT('Ctrl Pts',(5.31546292406649,-3.1061730448663,3.57610420237694));
#19486=CARTESIAN_POINT('Ctrl Pts',(5.32315871646269,-3.10403454841218,3.5756069425064));
#19487=CARTESIAN_POINT('Ctrl Pts',(5.34160834478264,-3.09883383139897,3.57440964479764));
#19488=CARTESIAN_POINT('Ctrl Pts',(5.35235429594077,-3.09574422464262,3.5737080495546));
#19489=CARTESIAN_POINT('Ctrl Pts',(5.38935421379915,-3.08489746764332,3.57127826306103));
#19490=CARTESIAN_POINT('Ctrl Pts',(5.41552446774038,-3.07686199033169,3.56953513563952));
#19491=CARTESIAN_POINT('Ctrl Pts',(5.47941747965404,-3.05634957809481,3.56522440861166));
#19492=CARTESIAN_POINT('Ctrl Pts',(5.51701730178626,-3.04350675278819,3.56264019759241));
#19493=CARTESIAN_POINT('Ctrl Pts',(5.66996691858379,-2.9880860358259,3.55195876841439));
#19494=CARTESIAN_POINT('Ctrl Pts',(5.78306712207926,-2.9396205982028,3.54366556446107));
#19495=CARTESIAN_POINT('Ctrl Pts',(6.06374047260983,-2.79984457493999,3.52245827590234));
#19496=CARTESIAN_POINT('Ctrl Pts',(6.22639116872241,-2.69995239561272,3.50958365281332));
#19497=CARTESIAN_POINT('Ctrl Pts',(6.37918776290017,-2.58636241268449,3.49716578845861));
#19498=CARTESIAN_POINT('Ctrl Pts',(2.17296269996979,-3.20554048108048,-0.411765747138983));
#19499=CARTESIAN_POINT('Ctrl Pts',(1.10598262521586,-2.44554835076675,-0.345549597099719));
#19500=CARTESIAN_POINT('Ctrl Pts',(-0.190085171851759,0.209786400507346,
-0.213161407923235));
#19501=CARTESIAN_POINT('Ctrl Pts',(2.11904905146237,4.02596493684606,-0.0146011796095345));
#19502=CARTESIAN_POINT('Ctrl Pts',(6.57036830017086,4.14281137096193,0.183914937802122));
#19503=CARTESIAN_POINT('Ctrl Pts',(9.08469850437939,0.471525498888313,0.382431055213778));
#19504=CARTESIAN_POINT('Ctrl Pts',(7.36116941620609,-3.63455711911314,0.580947172625436));
#19505=CARTESIAN_POINT('Ctrl Pts',(2.97726580402431,-4.41062931823268,0.77946329003709));
#19506=CARTESIAN_POINT('Ctrl Pts',(-0.0518523842630756,-1.14834011450979,
0.977979407448747));
#19507=CARTESIAN_POINT('Ctrl Pts',(1.04758148582589,3.16599895701937,1.1764955248604));
#19508=CARTESIAN_POINT('Ctrl Pts',(5.26885307852876,4.58075644304919,1.37501164227206));
#19509=CARTESIAN_POINT('Ctrl Pts',(8.74613631193873,1.80065901519612,1.57352775968371));
#19510=CARTESIAN_POINT('Ctrl Pts',(8.2950356860829,-2.62850749839492,1.77204387709537));
#19511=CARTESIAN_POINT('Ctrl Pts',(4.32864266632258,-4.6505056552148,1.97055999450703));
#19512=CARTESIAN_POINT('Ctrl Pts',(0.479313869061077,-2.41367545883394,
2.16907611191868));
#19513=CARTESIAN_POINT('Ctrl Pts',(0.272186515624751,2.03356129066451,2.36759222933034));
#19514=CARTESIAN_POINT('Ctrl Pts',(3.89694643539194,4.61849687019083,2.56610834674199));
#19515=CARTESIAN_POINT('Ctrl Pts',(8.03410612006349,2.97390317522259,2.76462446415365));
#19516=CARTESIAN_POINT('Ctrl Pts',(8.89493411795877,-1.39413568050936,2.9631405815653));
#19517=CARTESIAN_POINT('Ctrl Pts',(5.69110016326603,-4.48545097223521,3.16165669897696));
#19518=CARTESIAN_POINT('Ctrl Pts',(1.35661463604595,-3.46907591290164,3.36017281638862));
#19519=CARTESIAN_POINT('Ctrl Pts',(-0.139083166427389,0.724213049156903,
3.55868893380027));
#19520=CARTESIAN_POINT('Ctrl Pts',(2.57373840321099,4.25428138787658,3.75720505121192));
#19521=CARTESIAN_POINT('Ctrl Pts',(7.01072892820446,3.88835980295648,3.95572116862359));
#19522=CARTESIAN_POINT('Ctrl Pts',(9.10857690015422,-0.0384477492421469,
4.15423728603523));
#19523=CARTESIAN_POINT('Ctrl Pts',(6.94611304441007,-3.93004557143118,4.3527534034469));
#19524=CARTESIAN_POINT('Ctrl Pts',(2.50368062941278,-4.22258242327136,4.55126952085854));
#19525=CARTESIAN_POINT('Ctrl Pts',(-0.15042524517621,-0.648158610486061,
4.74978563827021));
#19526=CARTESIAN_POINT('Ctrl Pts',(1.41437509517098,3.51983652671062,4.94830175568186));
#19527=CARTESIAN_POINT('Ctrl Pts',(5.76506726388787,4.46443232806813,5.14681787309352));
#19528=CARTESIAN_POINT('Ctrl Pts',(8.91737013208296,1.32058592540232,5.34533399050517));
#19529=CARTESIAN_POINT('Ctrl Pts',(7.98446469607637,-3.03262794728552,5.54385010791683));
#19530=CARTESIAN_POINT('Ctrl Pts',(3.82068800849579,-4.60861883268182,5.74236622532849));
#19531=CARTESIAN_POINT('Ctrl Pts',(0.239147556357015,-1.9641242562649,5.94088234274014));
#19532=CARTESIAN_POINT('Ctrl Pts',(0.519749957626067,2.47907795239849,6.13939846015179));
#19533=CARTESIAN_POINT('Ctrl Pts',(4.40552487083362,4.65198772933701,6.33791457756345));
#19534=CARTESIAN_POINT('Ctrl Pts',(8.33795354574623,2.56469563392857,6.53643069497511));
#19535=CARTESIAN_POINT('Ctrl Pts',(8.71579260460107,-1.87129593734266,6.73494681238676));
#19536=CARTESIAN_POINT('Ctrl Pts',(5.19302422456139,-4.59359028502123,6.93346292979842));
#19537=CARTESIAN_POINT('Ctrl Pts',(0.995732677906764,-3.10916202902842,
7.13197904721008));
#19538=CARTESIAN_POINT('Ctrl Pts',(-0.0322822778871914,1.22257767061497,
7.33049516462173));
#19539=CARTESIAN_POINT('Ctrl Pts',(3.05041589877745,4.43470399540276,7.52901128203338));
#19540=CARTESIAN_POINT('Ctrl Pts',(7.42075085684839,3.58561275821527,7.72752739944505));
#19541=CARTESIAN_POINT('Ctrl Pts',(9.07645297431008,-0.547114437358846,
7.9260435168567));
#19542=CARTESIAN_POINT('Ctrl Pts',(6.5012617467849,-4.17880463841992,8.12455963426836));
#19543=CARTESIAN_POINT('Ctrl Pts',(2.05348831510913,-3.98362504090881,8.32307575168001));
#19544=CARTESIAN_POINT('Ctrl Pts',(-0.193681017610346,-0.140317407516647,
8.52159186909167));
#19545=CARTESIAN_POINT('Ctrl Pts',(1.81766867783776,3.83149023855917,8.72010798650331));
#19546=CARTESIAN_POINT('Ctrl Pts',(6.24558161029013,4.2944920068349,8.91862410391498));
#19547=CARTESIAN_POINT('Ctrl Pts',(9.03505934404192,0.824679685151172,9.11714022132663));
#19548=CARTESIAN_POINT('Ctrl Pts',(7.6315512320161,-3.40035860512303,9.31565633873829));
#19549=CARTESIAN_POINT('Ctrl Pts',(3.32036330565075,-4.51141316650472,9.51417245614994));
#19550=CARTESIAN_POINT('Ctrl Pts',(0.0495994604212725,-1.49100136617927,
9.71268857356161));
#19551=CARTESIAN_POINT('Ctrl Pts',(0.814563009263402,2.89484112343983,9.91120469097325));
#19552=CARTESIAN_POINT('Ctrl Pts',(4.91471488529713,4.62964317792977,10.1097208083849));
#19553=CARTESIAN_POINT('Ctrl Pts',(8.59521399360942,2.1247060752228,10.3082369257966));
#19554=CARTESIAN_POINT('Ctrl Pts',(8.48552926132444,-2.32599643497811,10.5067530432082));
#19555=CARTESIAN_POINT('Ctrl Pts',(4.68610787984395,-4.64659565516981,10.7052691606199));
#19556=CARTESIAN_POINT('Ctrl Pts',(0.676387677669684,-2.71193096197848,
10.9037852780315));
#19557=CARTESIAN_POINT('Ctrl Pts',(0.128394142987057,1.70626851979591,11.1023013954432));
#19558=CARTESIAN_POINT('Ctrl Pts',(3.54396933091606,4.56189974780998,11.3008175128549));
#19559=CARTESIAN_POINT('Ctrl Pts',(7.79519445548059,3.23982996331418,11.4993336302665));
#19560=CARTESIAN_POINT('Ctrl Pts',(8.98887841448097,-1.04921447348414,11.6978497476782));
#19561=CARTESIAN_POINT('Ctrl Pts',(6.03186814454124,-4.3774082536412,11.8963658650898));
#19562=CARTESIAN_POINT('Ctrl Pts',(1.63213740257258,-3.69685482224785,12.0948819825015));
#19563=CARTESIAN_POINT('Ctrl Pts',(-0.181124089683036,0.369207933724872,
12.2933980999131));
#19564=CARTESIAN_POINT('Ctrl Pts',(2.2526340504912,4.09715708707193,12.4919142173248));
#19565=CARTESIAN_POINT('Ctrl Pts',(6.70462241331237,4.07300771627025,12.6904303347364));
#19566=CARTESIAN_POINT('Ctrl Pts',(9.09779474190718,0.318875355730261,12.8889464521481));
#19567=CARTESIAN_POINT('Ctrl Pts',(7.24052934071316,-3.72727698993507,13.0874625695597));
#19568=CARTESIAN_POINT('Ctrl Pts',(2.83367453520978,-4.36005996854408,13.2859786869714));
#19569=CARTESIAN_POINT('Ctrl Pts',(-0.0870558709899348,-0.999982965095223,
13.4844948043831));
#19570=CARTESIAN_POINT('Ctrl Pts',(1.1530874699283,3.2758594160949,13.6830109217947));
#19571=CARTESIAN_POINT('Ctrl Pts',(5.41840487637927,4.55173205747878,13.8815270392064));
#19572=CARTESIAN_POINT('Ctrl Pts',(8.80279980247531,1.65921506374814,14.080043156618));
#19573=CARTESIAN_POINT('Ctrl Pts',(8.20690775291552,-2.75277952374592,14.2785592740297));
#19574=CARTESIAN_POINT('Ctrl Pts',(4.17643533161801,-4.64383098681233,14.4770753914414));
#19575=CARTESIAN_POINT('Ctrl Pts',(0.402412514292184,-2.28215036718792,
14.675591508853));
#19576=CARTESIAN_POINT('Ctrl Pts',(0.341017607518878,2.16948014760412,14.8741076262646));
#19577=CARTESIAN_POINT('Ctrl Pts',(4.04847489906614,4.63434201110855,15.0726237436763));
#19578=CARTESIAN_POINT('Ctrl Pts',(8.12956552465056,2.85516161537223,15.271139861088));
#19579=CARTESIAN_POINT('Ctrl Pts',(8.84690431993714,-1.53872147678918,15.4696559784996));
#19580=CARTESIAN_POINT('Ctrl Pts',(5.54356606143321,-4.52347271009317,15.6681720959113));
#19581=CARTESIAN_POINT('Ctrl Pts',(1.24468509012015,-3.36571368106855,15.8666882133229));
#19582=CARTESIAN_POINT('Ctrl Pts',(-0.112905173860372,0.874301914415817,
16.0652043307346));
#19583=CARTESIAN_POINT('Ctrl Pts',(2.71405060913991,4.31364844766405,16.2637204481462));
#19584=CARTESIAN_POINT('Ctrl Pts',(7.1366801074503,3.80263778683562,16.4622365655579));
#19585=CARTESIAN_POINT('Ctrl Pts',(9.10482335385156,-0.190756225336315,
16.6607526829696));
#19586=CARTESIAN_POINT('Ctrl Pts',(6.81609220134375,-4.00945931491334,16.8592688003812));
#19587=CARTESIAN_POINT('Ctrl Pts',(2.36646310311057,-4.15637583189606,17.0577849177929));
#19588=CARTESIAN_POINT('Ctrl Pts',(-0.16917825360623,-0.496962424679848,
17.2563010352045));
#19589=CARTESIAN_POINT('Ctrl Pts',(1.53126025266144,3.61755971783011,17.4548171526162));
#19590=CARTESIAN_POINT('Ctrl Pts',(5.91054938364417,4.41918948403437,17.6533332700278));
#19591=CARTESIAN_POINT('Ctrl Pts',(8.95821945609951,1.17380958265607,17.8518493874395));
#19592=CARTESIAN_POINT('Ctrl Pts',(7.88327219050615,-3.14652280629029,18.0503655048511));
#19593=CARTESIAN_POINT('Ctrl Pts',(3.67012384502666,-4.58532946245115,18.2488816222628));
#19594=CARTESIAN_POINT('Ctrl Pts',(0.177095531876928,-1.82497861910485,
18.4473977396744));
#19595=CARTESIAN_POINT('Ctrl Pts',(0.603036135785551,2.60665292882547,18.6459138570862));
#19596=CARTESIAN_POINT('Ctrl Pts',(4.55787735396168,4.65116130836808,18.8444299744978));
#19597=CARTESIAN_POINT('Ctrl Pts',(8.41985082781949,2.43622463611074,19.0429460919094));
#19598=CARTESIAN_POINT('Ctrl Pts',(8.65223471259592,-2.00976021586402,19.2414622093211));
#19599=CARTESIAN_POINT('Ctrl Pts',(5.04221626688697,-4.61524489208584,19.4399783267328));
#19600=CARTESIAN_POINT('Ctrl Pts',(0.895781713701428,-2.99417608693739,
19.6384944441444));
#19601=CARTESIAN_POINT('Ctrl Pts',(0.0101569427980723,1.36890222246852,
19.8370105615561));
#19602=CARTESIAN_POINT('Ctrl Pts',(3.1963802739596,4.47836591752857,20.0355266789677));
#19603=CARTESIAN_POINT('Ctrl Pts',(7.53656898706393,3.48662728959027,20.2340427963793));
#19604=CARTESIAN_POINT('Ctrl Pts',(9.05606082131957,-0.698098281184544,
20.432558913791));
#19605=CARTESIAN_POINT('Ctrl Pts',(6.36333405195284,-4.24351873734398,20.6310750312027));
#19606=CARTESIAN_POINT('Ctrl Pts',(1.9243366462227,-3.90280543100934,20.8295911486144));
#19607=CARTESIAN_POINT('Ctrl Pts',(-0.195782035254683,0.0120228054752082,
21.028107266026));
#19608=CARTESIAN_POINT('Ctrl Pts',(1.94454241477252,3.91584087042925,21.2266233834376));
#19609=CARTESIAN_POINT('Ctrl Pts',(6.38524148680512,4.23360619038166,21.4251395008493));
#19610=CARTESIAN_POINT('Ctrl Pts',(9.05960761710739,0.674315805600993,21.623655618261));
#19611=CARTESIAN_POINT('Ctrl Pts',(7.5185068390623,-3.50250076674849,21.8221717356726));
#19612=CARTESIAN_POINT('Ctrl Pts',(3.17325057532877,-4.47179261159471,22.0206878530843));
#19613=CARTESIAN_POINT('Ctrl Pts',(0.0031406198327811,-1.34590405051051,
22.2192039704959));
#19614=CARTESIAN_POINT('Ctrl Pts',(0.911305739869395,3.01254206724522,22.4177200879076));
#19615=CARTESIAN_POINT('Ctrl Pts',(5.06606104496655,4.6121513544261,22.6162362053192));
#19616=CARTESIAN_POINT('Ctrl Pts',(8.66256938155685,1.98805571626367,22.8147523227309));
#19617=CARTESIAN_POINT('Ctrl Pts',(8.4072000996685,-2.45669335535235,23.0132684401425));
#19618=CARTESIAN_POINT('Ctrl Pts',(4.53384760969594,-4.65159218721967,23.2117845575542));
#19619=CARTESIAN_POINT('Ctrl Pts',(0.589592923617338,-2.58676106216746,
23.4103006749659));
#19620=CARTESIAN_POINT('Ctrl Pts',(0.186627431348294,1.84718698340797,23.6088167923775));
#19621=CARTESIAN_POINT('Ctrl Pts',(3.69375302108596,4.58911293885384,23.8073329097892));
#19622=CARTESIAN_POINT('Ctrl Pts',(7.89964467060016,3.12919021086655,24.0058490272008));
#19623=CARTESIAN_POINT('Ctrl Pts',(8.95179466357075,-1.19786968887199,24.2043651446125));
#19624=CARTESIAN_POINT('Ctrl Pts',(5.88826072308503,-4.42509080397621,24.4028812620241));
#19625=CARTESIAN_POINT('Ctrl Pts',(1.51149918181804,-3.60542346049212,24.6013973794358));
#19626=CARTESIAN_POINT('Ctrl Pts',(-0.164376056275096,0.527120914407128,
24.7999134968474));
#19627=CARTESIAN_POINT('Ctrl Pts',(1.53399129555416,2.94325066577138,24.9322575751219));
#19628=CARTESIAN_POINT('Ctrl Pts',(2.70656526709436,3.52529833870864,24.9984296142591));
#19629=CARTESIAN_POINT('Ctrl Pts',(2.31196529717974,-3.01041142380583,-0.273445981108207));
#19630=CARTESIAN_POINT('Ctrl Pts',(1.30993489857133,-2.29668186568531,-0.207229831068943));
#19631=CARTESIAN_POINT('Ctrl Pts',(0.0927619053280601,0.197016191301887,
-0.0748416418924601));
#19632=CARTESIAN_POINT('Ctrl Pts',(2.26133350378215,3.78089464452436,0.123718586421241));
#19633=CARTESIAN_POINT('Ctrl Pts',(6.44169010710979,3.89062835157607,0.322234703832897));
#19634=CARTESIAN_POINT('Ctrl Pts',(8.80296690727615,0.442822593209179,0.520750821244553));
#19635=CARTESIAN_POINT('Ctrl Pts',(7.18435323294509,-3.41331277406459,0.719266938656211));
#19636=CARTESIAN_POINT('Ctrl Pts',(3.06730851213489,-4.14214356803415,0.917783056067867));
#19637=CARTESIAN_POINT('Ctrl Pts',(0.222580126422941,-1.07843785456408,
1.11629917347952));
#19638=CARTESIAN_POINT('Ctrl Pts',(1.25508877879203,2.97327688863128,1.31481529089117));
#19639=CARTESIAN_POINT('Ctrl Pts',(5.21940128729496,4.30191464036023,1.51333140830283));
#19640=CARTESIAN_POINT('Ctrl Pts',(8.48501382017349,1.69104851481962,1.71184752571448));
#19641=CARTESIAN_POINT('Ctrl Pts',(8.06137278822348,-2.46850384433775,1.91036364312614));
#19642=CARTESIAN_POINT('Ctrl Pts',(4.33642377308406,-4.36741804808325,2.1088797605378));
#19643=CARTESIAN_POINT('Ctrl Pts',(0.721412996069988,-2.26674915432179,
2.30739587794946));
#19644=CARTESIAN_POINT('Ctrl Pts',(0.526893989166935,1.90977346146706,2.50591199536111));
#19645=CARTESIAN_POINT('Ctrl Pts',(3.93100594327419,4.33735771577206,2.70442811277276));
#19646=CARTESIAN_POINT('Ctrl Pts',(7.81632664047099,2.79287444498747,2.90294423018442));
#19647=CARTESIAN_POINT('Ctrl Pts',(8.62475394129306,-1.30927124574203,3.10146034759608));
#19648=CARTESIAN_POINT('Ctrl Pts',(5.61594516345689,-4.21241064570382,3.29997646500774));
#19649=CARTESIAN_POINT('Ctrl Pts',(1.54531032840212,-3.25790481196126,3.49849258241939));
#19650=CARTESIAN_POINT('Ctrl Pts',(0.140659294449413,0.680128436785933,
3.69700869983105));
#19651=CARTESIAN_POINT('Ctrl Pts',(2.68834480713824,3.99531291703776,3.8955248172427));
#19652=CARTESIAN_POINT('Ctrl Pts',(6.85524491106594,3.65166587031902,4.09404093465435));
#19653=CARTESIAN_POINT('Ctrl Pts',(8.82539176693615,-0.0361073410931478,
4.29255705206602));
#19654=CARTESIAN_POINT('Ctrl Pts',(6.79456235351217,-3.69081412452673,4.49107316947766));
#19655=CARTESIAN_POINT('Ctrl Pts',(2.62255162068078,-3.96554354562172,4.68958928688933));
#19656=CARTESIAN_POINT('Ctrl Pts',(0.130007635661538,-0.608703617053558,
4.88810540430098));
#19657=CARTESIAN_POINT('Ctrl Pts',(1.59955476768487,3.30557550356288,5.08662152171263));
#19658=CARTESIAN_POINT('Ctrl Pts',(5.68540970649173,4.19267145760527,5.28513763912429));
#19659=CARTESIAN_POINT('Ctrl Pts',(8.64582422058695,1.24019864338394,5.48365375653594));
#19660=CARTESIAN_POINT('Ctrl Pts',(7.76970701088062,-2.84802449713069,5.68216987394761));
#19661=CARTESIAN_POINT('Ctrl Pts',(3.85938955257665,-4.32808097846753,5.88068599135924));
#19662=CARTESIAN_POINT('Ctrl Pts',(0.495866191827503,-1.844563228489,6.07920210877092));
#19663=CARTESIAN_POINT('Ctrl Pts',(0.759387641428115,2.32817043879295,6.27771822618256));
#19664=CARTESIAN_POINT('Ctrl Pts',(4.40862597053364,4.36880990474354,6.47623434359423));
#19665=CARTESIAN_POINT('Ctrl Pts',(8.10167813322798,2.40857636349708,6.67475046100588));
#19666=CARTESIAN_POINT('Ctrl Pts',(8.45651720821394,-1.75738559545474,6.87326657841754));
#19667=CARTESIAN_POINT('Ctrl Pts',(5.14818832037566,-4.31396725511023,7.0717826958292));
#19668=CARTESIAN_POINT('Ctrl Pts',(1.20639613410644,-2.9198997628929,7.27029881324085));
#19669=CARTESIAN_POINT('Ctrl Pts',(0.240958952754043,1.14815638979818,7.4688149306525));
#19670=CARTESIAN_POINT('Ctrl Pts',(3.13600578243834,4.16475276096279,7.66733104806417));
#19671=CARTESIAN_POINT('Ctrl Pts',(7.24030780616454,3.36734777563528,7.86584716547581));
#19672=CARTESIAN_POINT('Ctrl Pts',(8.79522330270695,-0.513810248872322,
8.06436328288747));
#19673=CARTESIAN_POINT('Ctrl Pts',(6.37679023796107,-3.92443062116999,8.26287940029913));
#19674=CARTESIAN_POINT('Ctrl Pts',(2.1997636091463,-3.74113208118609,8.46139551771078));
#19675=CARTESIAN_POINT('Ctrl Pts',(0.089384947459713,-0.131775945129999,
8.65991163512245));
#19676=CARTESIAN_POINT('Ctrl Pts',(1.97829888761515,3.5982580948319,8.8584277525341));
#19677=CARTESIAN_POINT('Ctrl Pts',(6.13667397417128,4.03307581767334,9.05694386994575));
#19678=CARTESIAN_POINT('Ctrl Pts',(8.75634940354159,0.774479423926291,9.2554599873574));
#19679=CARTESIAN_POINT('Ctrl Pts',(7.43827624901926,-3.19337049409171,9.45397610476906));
#19680=CARTESIAN_POINT('Ctrl Pts',(3.38952083310589,-4.23679245796831,9.65249222218073));
#19681=CARTESIAN_POINT('Ctrl Pts',(0.317856350200649,-1.40024048117564,
9.85100833959237));
#19682=CARTESIAN_POINT('Ctrl Pts',(1.03625470449417,2.71862509287945,10.049524457004));
#19683=CARTESIAN_POINT('Ctrl Pts',(4.88682034851015,4.34782552060827,10.2480405744157));
#19684=CARTESIAN_POINT('Ctrl Pts',(8.34327851098385,1.99537004097493,10.4465566918273));
#19685=CARTESIAN_POINT('Ctrl Pts',(8.24027055552775,-2.18440736622039,10.645072809239));
#19686=CARTESIAN_POINT('Ctrl Pts',(4.67212920832948,-4.36374605926514,10.8435889266506));
#19687=CARTESIAN_POINT('Ctrl Pts',(0.906490441907856,-2.54684911848653,
11.0421050440623));
#19688=CARTESIAN_POINT('Ctrl Pts',(0.391854608507251,1.60240379879482,11.2406211614739));
#19689=CARTESIAN_POINT('Ctrl Pts',(3.59951541494433,4.28420579809219,11.4391372788856));
#19690=CARTESIAN_POINT('Ctrl Pts',(7.59195811086242,3.04261362173219,11.6376533962972));
#19691=CARTESIAN_POINT('Ctrl Pts',(8.71297961965247,-0.98534623276214,11.8361695137089));
#19692=CARTESIAN_POINT('Ctrl Pts',(5.93596976765481,-4.11094475056566,12.0346856311206));
#19693=CARTESIAN_POINT('Ctrl Pts',(1.80406135300024,-3.47181826426207,12.2332017485322));
#19694=CARTESIAN_POINT('Ctrl Pts',(0.101177504597399,0.346733347466743,
12.4317178659439));
#19695=CARTESIAN_POINT('Ctrl Pts',(2.38678685852808,3.84775315515312,12.6302339833555));
#19696=CARTESIAN_POINT('Ctrl Pts',(6.56777184536255,3.82507381537617,12.8287501007672));
#19697=CARTESIAN_POINT('Ctrl Pts',(8.81526594492522,0.29946463609684,13.0272662181788));
#19698=CARTESIAN_POINT('Ctrl Pts',(7.07105681270762,-3.5003885604986,13.2257823355905));
#19699=CARTESIAN_POINT('Ctrl Pts',(2.93245799361878,-4.09465249784007,13.4242984530022));
#19700=CARTESIAN_POINT('Ctrl Pts',(0.189519561683291,-0.939111566208993,
13.6228145704138));
#19701=CARTESIAN_POINT('Ctrl Pts',(1.35417235664619,3.07644987396012,13.8213306878255));
#19702=CARTESIAN_POINT('Ctrl Pts',(5.3598495029257,4.27465703983832,14.0198468052371));
#19703=CARTESIAN_POINT('Ctrl Pts',(8.53822806601778,1.55821460123144,14.2183629226488));
#19704=CARTESIAN_POINT('Ctrl Pts',(7.97860941701375,-2.58521112879858,14.4168790400604));
#19705=CARTESIAN_POINT('Ctrl Pts',(4.19348166959603,-4.36114968300486,14.6153951574721));
#19706=CARTESIAN_POINT('Ctrl Pts',(0.649192814085452,-2.14323031537866,
14.8139112748837));
#19707=CARTESIAN_POINT('Ctrl Pts',(0.59153516483578,2.03741860650786,15.0124273922954));
#19708=CARTESIAN_POINT('Ctrl Pts',(4.07331050026509,4.35223832436584,15.2109435097071));
#19709=CARTESIAN_POINT('Ctrl Pts',(7.9059751985768,2.68136097312093,15.4094596271187));
#19710=CARTESIAN_POINT('Ctrl Pts',(8.57964783407003,-1.44505575241412,15.6079757445304));
#19711=CARTESIAN_POINT('Ctrl Pts',(5.47739182177246,-4.24811790776339,15.806491861942));
#19712=CARTESIAN_POINT('Ctrl Pts',(1.44019420657955,-3.16083449095397,16.0050079793537));
#19713=CARTESIAN_POINT('Ctrl Pts',(0.165243768843413,0.821081027223728,
16.2035240967653));
#19714=CARTESIAN_POINT('Ctrl Pts',(2.82011586731386,4.05106615928717,16.402040214177));
#19715=CARTESIAN_POINT('Ctrl Pts',(6.97352913523386,3.57116196212476,16.6005563315886));
#19716=CARTESIAN_POINT('Ctrl Pts',(8.82186670813997,-0.17914442924803,16.7990724490003));
#19717=CARTESIAN_POINT('Ctrl Pts',(6.67245619587356,-3.76539376000376,16.997588566412));
#19718=CARTESIAN_POINT('Ctrl Pts',(2.49368685944485,-3.90336711073225,17.1961046838236));
#19719=CARTESIAN_POINT('Ctrl Pts',(0.112396168534027,-0.466711111367439,
17.3946208012353));
#19720=CARTESIAN_POINT('Ctrl Pts',(1.70932484092508,3.39735004600064,17.5931369186469));
#19721=CARTESIAN_POINT('Ctrl Pts',(5.82203597524696,4.15018265569229,17.7916530360586));
#19722=CARTESIAN_POINT('Ctrl Pts',(8.68418694674809,1.10235693414467,17.9901691534703));
#19723=CARTESIAN_POINT('Ctrl Pts',(7.67467433961344,-2.9549862986379,18.1886852708819));
#19724=CARTESIAN_POINT('Ctrl Pts',(3.71799059648846,-4.30620928893205,18.3872013882936));
#19725=CARTESIAN_POINT('Ctrl Pts',(0.437591425226463,-1.7138877251997,18.5857175057052));
#19726=CARTESIAN_POINT('Ctrl Pts',(0.837603987051035,2.44797961565228,18.7842336231169));
#19727=CARTESIAN_POINT('Ctrl Pts',(4.55170438690705,4.36803379003202,18.9827497405285));
#19728=CARTESIAN_POINT('Ctrl Pts',(8.17859012825258,2.28792570825151,19.1812658579402));
#19729=CARTESIAN_POINT('Ctrl Pts',(8.39682823991214,-1.88742121606535,19.3797819753518));
#19730=CARTESIAN_POINT('Ctrl Pts',(5.0065604104293,-4.33430369349561,19.5782980927635));
#19731=CARTESIAN_POINT('Ctrl Pts',(1.11252942855707,-2.81191329518458,19.7768142101752));
#19732=CARTESIAN_POINT('Ctrl Pts',(0.280814794700937,1.28557380975688,19.9753303275868));
#19733=CARTESIAN_POINT('Ctrl Pts',(3.27308495055695,4.20575687553525,20.1738464449984));
#19734=CARTESIAN_POINT('Ctrl Pts',(7.34907580467911,3.27438779359847,20.3723625624101));
#19735=CARTESIAN_POINT('Ctrl Pts',(8.77607246974106,-0.65560333835151,20.5708786798217));
#19736=CARTESIAN_POINT('Ctrl Pts',(6.24725853788356,-3.98520541525919,20.7693947972334));
#19737=CARTESIAN_POINT('Ctrl Pts',(2.07847371693811,-3.66523215780504,20.9679109146451));
#19738=CARTESIAN_POINT('Ctrl Pts',(0.0874118238771355,0.0112909480203034,
21.1664270320568));
#19739=CARTESIAN_POINT('Ctrl Pts',(2.09744951113826,3.6774740982752,21.3649431494684));
#19740=CARTESIAN_POINT('Ctrl Pts',(6.26783241381338,3.97589626917586,21.56345926688));
#19741=CARTESIAN_POINT('Ctrl Pts',(8.77940336342984,0.633268559987037,21.7619753842917));
#19742=CARTESIAN_POINT('Ctrl Pts',(7.33211314362288,-3.28929501353682,21.9604915017033));
#19743=CARTESIAN_POINT('Ctrl Pts',(3.25136321302202,-4.1995837027451,22.159007619115));
#19744=CARTESIAN_POINT('Ctrl Pts',(0.274225572405194,-1.26397559254583,
22.3575237365266));
#19745=CARTESIAN_POINT('Ctrl Pts',(1.12710846943813,2.82916129353447,22.5560398539383));
#19746=CARTESIAN_POINT('Ctrl Pts',(5.0289536987851,4.33139846700858,22.75455597135));
#19747=CARTESIAN_POINT('Ctrl Pts',(8.40653381239982,1.86703792222437,22.9530720887616));
#19748=CARTESIAN_POINT('Ctrl Pts',(8.1667094807393,-2.30714844669435,23.1515882061733));
#19749=CARTESIAN_POINT('Ctrl Pts',(4.52913739170739,-4.36843844023836,23.3501043235849));
#19750=CARTESIAN_POINT('Ctrl Pts',(0.824979095953012,-2.42929861537115,
23.5486204409966));
#19751=CARTESIAN_POINT('Ctrl Pts',(0.44654309475883,1.73474421227166,23.7471365584082));
#19752=CARTESIAN_POINT('Ctrl Pts',(3.74018140704413,4.30976245591016,23.9456526758199));
#19753=CARTESIAN_POINT('Ctrl Pts',(7.69005018696339,2.93870878051704,24.1441687932315));
#19754=CARTESIAN_POINT('Ctrl Pts',(8.67815324699032,-1.12495244308866,24.3426849106432));
#19755=CARTESIAN_POINT('Ctrl Pts',(5.80110407974766,-4.15572474791461,24.5412010280549));
#19756=CARTESIAN_POINT('Ctrl Pts',(1.69076667459873,-3.38595255220879,24.7397171454665));
#19757=CARTESIAN_POINT('Ctrl Pts',(0.116906044416222,0.495033780363739,
24.9382332628782));
#19758=CARTESIAN_POINT('Ctrl Pts',(1.71188963858453,2.76408782845127,25.0705773411526));
#19759=CARTESIAN_POINT('Ctrl Pts',(2.81308617627174,3.31070484176046,25.1367493802898));
#19760=CARTESIAN_POINT('Ctrl Pts',(2.45096789438968,-2.81528236653118,-0.135126215077433));
#19761=CARTESIAN_POINT('Ctrl Pts',(1.5138871719268,-2.14781538060387,-0.0689100650381678));
#19762=CARTESIAN_POINT('Ctrl Pts',(0.375608982507884,0.184245982096433,
0.0634781241383155));
#19763=CARTESIAN_POINT('Ctrl Pts',(2.40361795610193,3.53582435220265,0.262038352452016));
#19764=CARTESIAN_POINT('Ctrl Pts',(6.31301191404873,3.63844533219021,0.460554469863673));
#19765=CARTESIAN_POINT('Ctrl Pts',(8.52123531017291,0.41411968753004,0.659070587275328));
#19766=CARTESIAN_POINT('Ctrl Pts',(7.00753704968407,-3.19206842901602,0.857586704686986));
#19767=CARTESIAN_POINT('Ctrl Pts',(3.15735122024546,-3.87365781783563,1.05610282209864));
#19768=CARTESIAN_POINT('Ctrl Pts',(0.497012637108953,-1.00853559461836,
1.25461893951029));
#19769=CARTESIAN_POINT('Ctrl Pts',(1.46259607175817,2.78055482024318,1.45313505692195));
#19770=CARTESIAN_POINT('Ctrl Pts',(5.16994949606116,4.02307283767128,1.6516511743336));
#19771=CARTESIAN_POINT('Ctrl Pts',(8.22389132840824,1.58143801444312,1.85016729174526));
#19772=CARTESIAN_POINT('Ctrl Pts',(7.82770989036406,-2.30850019028058,2.04868340915692));
#19773=CARTESIAN_POINT('Ctrl Pts',(4.34420487984554,-4.08433044095169,2.24719952656857));
#19774=CARTESIAN_POINT('Ctrl Pts',(0.963512123078899,-2.11982284980964,
2.44571564398023));
#19775=CARTESIAN_POINT('Ctrl Pts',(0.781601462709117,1.78598563226962,2.64423176139188));
#19776=CARTESIAN_POINT('Ctrl Pts',(3.96506545115642,4.05621856135326,2.84274787880354));
#19777=CARTESIAN_POINT('Ctrl Pts',(7.59854716087849,2.61184571475234,3.0412639962152));
#19778=CARTESIAN_POINT('Ctrl Pts',(8.35457376462735,-1.22440681097471,3.23978011362686));
#19779=CARTESIAN_POINT('Ctrl Pts',(5.54079016364776,-3.93937031917242,3.43829623103851));
#19780=CARTESIAN_POINT('Ctrl Pts',(1.7340060207583,-3.04673371102089,3.63681234845017));
#19781=CARTESIAN_POINT('Ctrl Pts',(0.420401755326215,0.636043824414959,
3.83532846586182));
#19782=CARTESIAN_POINT('Ctrl Pts',(2.8029512110655,3.73634444619894,4.03384458327349));
#19783=CARTESIAN_POINT('Ctrl Pts',(6.6997608939274,3.41497193768155,4.23236070068513));
#19784=CARTESIAN_POINT('Ctrl Pts',(8.54220663371807,-0.0337669329441494,
4.4308768180968));
#19785=CARTESIAN_POINT('Ctrl Pts',(6.64301166261426,-3.45158267762228,4.62939293550844));
#19786=CARTESIAN_POINT('Ctrl Pts',(2.74142261194879,-3.70850466797209,4.82790905292011));
#19787=CARTESIAN_POINT('Ctrl Pts',(0.410440516499291,-0.569248623621048,
5.02642517033176));
#19788=CARTESIAN_POINT('Ctrl Pts',(1.78473444019877,3.09131448041513,5.22494128774342));
#19789=CARTESIAN_POINT('Ctrl Pts',(5.60575214909559,3.92091058714242,5.42345740515506));
#19790=CARTESIAN_POINT('Ctrl Pts',(8.37427830909092,1.15981136136555,5.62197352256674));
#19791=CARTESIAN_POINT('Ctrl Pts',(7.55494932568486,-2.66342104697584,5.82048963997839));
#19792=CARTESIAN_POINT('Ctrl Pts',(3.89809109665752,-4.04754312425325,6.01900575739004));
#19793=CARTESIAN_POINT('Ctrl Pts',(0.752584827297987,-1.72500220071308,
6.21752187480171));
#19794=CARTESIAN_POINT('Ctrl Pts',(0.999025325230166,2.17726292518741,6.41603799221334));
#19795=CARTESIAN_POINT('Ctrl Pts',(4.41172707023364,4.08563208015006,6.61455410962502));
#19796=CARTESIAN_POINT('Ctrl Pts',(7.86540272070975,2.25245709306557,6.81307022703666));
#19797=CARTESIAN_POINT('Ctrl Pts',(8.1972418118268,-1.64347525356681,7.01158634444832));
#19798=CARTESIAN_POINT('Ctrl Pts',(5.10335241618994,-4.03434422519923,7.21010246185998));
#19799=CARTESIAN_POINT('Ctrl Pts',(1.4170595903061,-2.73063749675737,7.40861857927163));
#19800=CARTESIAN_POINT('Ctrl Pts',(0.514200183395272,1.07373510898141,7.60713469668328));
#19801=CARTESIAN_POINT('Ctrl Pts',(3.22159566609925,3.89480152652282,7.80565081409495));
#19802=CARTESIAN_POINT('Ctrl Pts',(7.05986475548066,3.14908279305528,8.0041669315066));
#19803=CARTESIAN_POINT('Ctrl Pts',(8.51399363110384,-0.480506060385796,
8.20268304891826));
#19804=CARTESIAN_POINT('Ctrl Pts',(6.25231872913724,-3.67005660392007,8.40119916632992));
#19805=CARTESIAN_POINT('Ctrl Pts',(2.34603890318347,-3.49863912146337,8.59971528374156));
#19806=CARTESIAN_POINT('Ctrl Pts',(0.372450912529775,-0.123234482743352,
8.79823140115322));
#19807=CARTESIAN_POINT('Ctrl Pts',(2.13892909739252,3.36502595110463,8.99674751856487));
#19808=CARTESIAN_POINT('Ctrl Pts',(6.02776633805246,3.77165962851178,9.19526363597655));
#19809=CARTESIAN_POINT('Ctrl Pts',(8.47763946304124,0.72427916270141,9.39377975338818));
#19810=CARTESIAN_POINT('Ctrl Pts',(7.24500126602242,-2.98638238306039,9.59229587079984));
#19811=CARTESIAN_POINT('Ctrl Pts',(3.45867836056103,-3.9621717494319,9.79081198821151));
#19812=CARTESIAN_POINT('Ctrl Pts',(0.586113239980029,-1.30947959617202,
9.98932810562315));
#19813=CARTESIAN_POINT('Ctrl Pts',(1.25794639972494,2.54240906231909,10.1878442230349));
#19814=CARTESIAN_POINT('Ctrl Pts',(4.85892581172318,4.06600786328675,10.3863603404465));
#19815=CARTESIAN_POINT('Ctrl Pts',(8.09134302835829,1.86603400672705,10.5848764578582));
#19816=CARTESIAN_POINT('Ctrl Pts',(7.99501184973105,-2.04281829746266,10.7833925752698));
#19817=CARTESIAN_POINT('Ctrl Pts',(4.658150536815,-4.08089646336047,10.9819086926815));
#19818=CARTESIAN_POINT('Ctrl Pts',(1.13659320614603,-2.38176727499459,11.1804248100931));
#19819=CARTESIAN_POINT('Ctrl Pts',(0.655315074027438,1.49853907779376,11.3789409275048));
#19820=CARTESIAN_POINT('Ctrl Pts',(3.6550614989726,4.00651184837438,11.5774570449165));
#19821=CARTESIAN_POINT('Ctrl Pts',(7.38872176624422,2.84539728015019,11.7759731623281));
#19822=CARTESIAN_POINT('Ctrl Pts',(8.43708082482397,-0.921477992040132,
11.9744892797398));
#19823=CARTESIAN_POINT('Ctrl Pts',(5.84007139076835,-3.84448124749012,12.1730053971514));
#19824=CARTESIAN_POINT('Ctrl Pts',(1.97598530342792,-3.24678170627628,12.3715215145631));
#19825=CARTESIAN_POINT('Ctrl Pts',(0.383479098877827,0.324258761208613,
12.5700376319747));
#19826=CARTESIAN_POINT('Ctrl Pts',(2.52093966656498,3.59834922323431,12.7685537493864));
#19827=CARTESIAN_POINT('Ctrl Pts',(6.43092127741269,3.5771399144821,12.967069866798));
#19828=CARTESIAN_POINT('Ctrl Pts',(8.53273714794332,0.280053916463419,13.1655859842097));
#19829=CARTESIAN_POINT('Ctrl Pts',(6.90158428470204,-3.27350013106212,13.3641021016213));
#19830=CARTESIAN_POINT('Ctrl Pts',(3.0312414520278,-3.82924502713605,13.562618219033));
#19831=CARTESIAN_POINT('Ctrl Pts',(0.466094994356506,-0.878240167322765,
13.7611343364446));
#19832=CARTESIAN_POINT('Ctrl Pts',(1.55525724336407,2.87704033182534,13.9596504538563));
#19833=CARTESIAN_POINT('Ctrl Pts',(5.30129412947213,3.99758202219787,14.1581665712679));
#19834=CARTESIAN_POINT('Ctrl Pts',(8.27365632956023,1.45721413871475,14.3566826886797));
#19835=CARTESIAN_POINT('Ctrl Pts',(7.75031108111198,-2.41764273385123,14.5551988060912));
#19836=CARTESIAN_POINT('Ctrl Pts',(4.21052800757405,-4.07846837919741,14.753714923503));
#19837=CARTESIAN_POINT('Ctrl Pts',(0.895973113878727,-2.00431026356939,
14.9522310409146));
#19838=CARTESIAN_POINT('Ctrl Pts',(0.842052722152676,1.9053570654116,15.1507471583263));
#19839=CARTESIAN_POINT('Ctrl Pts',(4.09814610146403,4.07013463762311,15.3492632757379));
#19840=CARTESIAN_POINT('Ctrl Pts',(7.682384872503,2.50756033086961,15.5477793931496));
#19841=CARTESIAN_POINT('Ctrl Pts',(8.31239134820293,-1.35139002803904,15.7462955105612));
#19842=CARTESIAN_POINT('Ctrl Pts',(5.41121758211169,-3.97276310543362,15.9448116279729));
#19843=CARTESIAN_POINT('Ctrl Pts',(1.63570332303896,-2.95595530083938,16.1433277453845));
#19844=CARTESIAN_POINT('Ctrl Pts',(0.443392711547191,0.767860140031627,
16.3418438627962));
#19845=CARTESIAN_POINT('Ctrl Pts',(2.92618112548781,3.7884838709103,16.5403599802078));
#19846=CARTESIAN_POINT('Ctrl Pts',(6.8103781630174,3.33968613741389,16.7388760976195));
#19847=CARTESIAN_POINT('Ctrl Pts',(8.5389100624284,-0.167532633159739,16.9373922150311));
#19848=CARTESIAN_POINT('Ctrl Pts',(6.52882019040339,-3.5213282050942,17.1359083324428));
#19849=CARTESIAN_POINT('Ctrl Pts',(2.62091061577914,-3.65035838956845,17.3344244498544));
#19850=CARTESIAN_POINT('Ctrl Pts',(0.393970590674286,-0.43645979805503,
17.5329405672661));
#19851=CARTESIAN_POINT('Ctrl Pts',(1.88738942918871,3.17714037417117,17.7314566846778));
#19852=CARTESIAN_POINT('Ctrl Pts',(5.73352256684974,3.8811758273502,17.9299728020894));
#19853=CARTESIAN_POINT('Ctrl Pts',(8.41015443739666,1.03090428563328,18.1284889195011));
#19854=CARTESIAN_POINT('Ctrl Pts',(7.46607648872073,-2.76344979098553,18.3270050369127));
#19855=CARTESIAN_POINT('Ctrl Pts',(3.76585734795025,-4.02708911541293,18.5255211543244));
#19856=CARTESIAN_POINT('Ctrl Pts',(0.698087318576006,-1.60279683129456,
18.724037271736));
#19857=CARTESIAN_POINT('Ctrl Pts',(1.07217183831651,2.28930630247911,18.9225533891477));
#19858=CARTESIAN_POINT('Ctrl Pts',(4.54553141985243,4.08490627169594,19.1210695065593));
#19859=CARTESIAN_POINT('Ctrl Pts',(7.93732942868568,2.13962678039228,19.319585623971));
#19860=CARTESIAN_POINT('Ctrl Pts',(8.14142176722837,-1.76508221626667,19.5181017413827));
#19861=CARTESIAN_POINT('Ctrl Pts',(4.97090455397163,-4.05336249490537,19.7166178587943));
#19862=CARTESIAN_POINT('Ctrl Pts',(1.3292771434127,-2.62965050343175,19.915133976206));
#19863=CARTESIAN_POINT('Ctrl Pts',(0.551472646603815,1.20224539704524,20.1136500936177));
#19864=CARTESIAN_POINT('Ctrl Pts',(3.3497896271543,3.93314783354192,20.3121662110293));
#19865=CARTESIAN_POINT('Ctrl Pts',(7.16158262229433,3.06214829760668,20.510682328441));
#19866=CARTESIAN_POINT('Ctrl Pts',(8.49608411816253,-0.613108395518473,
20.7091984458526));
#19867=CARTESIAN_POINT('Ctrl Pts',(6.13118302381429,-3.72689209317441,20.9077145632643));
#19868=CARTESIAN_POINT('Ctrl Pts',(2.23261078765349,-3.42765888460072,21.1062306806759));
#19869=CARTESIAN_POINT('Ctrl Pts',(0.370605683008962,0.0105590905653954,
21.3047467980876));
#19870=CARTESIAN_POINT('Ctrl Pts',(2.250356607504,3.43910732612115,21.5032629154992));
#19871=CARTESIAN_POINT('Ctrl Pts',(6.15042334082164,3.71818634797007,21.7017790329109));
#19872=CARTESIAN_POINT('Ctrl Pts',(8.49919910975228,0.592221314373082,21.9002951503225));
#19873=CARTESIAN_POINT('Ctrl Pts',(7.14571944818345,-3.07608926032515,22.0988112677342));
#19874=CARTESIAN_POINT('Ctrl Pts',(3.32947585071529,-3.92737479389549,22.2973273851459));
#19875=CARTESIAN_POINT('Ctrl Pts',(0.545310524977601,-1.18204713458114,
22.4958435025575));
#19876=CARTESIAN_POINT('Ctrl Pts',(1.34291119900688,2.64578051982372,22.6943596199692));
#19877=CARTESIAN_POINT('Ctrl Pts',(4.99184635260365,4.05064557959106,22.8928757373808));
#19878=CARTESIAN_POINT('Ctrl Pts',(8.15049824324278,1.74602012818506,23.0913918547925));
#19879=CARTESIAN_POINT('Ctrl Pts',(7.92621886181009,-2.15760353803636,23.2899079722041));
#19880=CARTESIAN_POINT('Ctrl Pts',(4.52442717371885,-4.08528469325705,23.4884240896158));
#19881=CARTESIAN_POINT('Ctrl Pts',(1.06036526828869,-2.27183616857484,23.6869402070274));
#19882=CARTESIAN_POINT('Ctrl Pts',(0.706458758169362,1.62230144113535,23.8854563244391));
#19883=CARTESIAN_POINT('Ctrl Pts',(3.78660979300229,4.03041197296648,24.0839724418507));
#19884=CARTESIAN_POINT('Ctrl Pts',(7.48045570332662,2.74822735016753,24.2824885592624));
#19885=CARTESIAN_POINT('Ctrl Pts',(8.40451183040988,-1.05203519730533,24.481004676674));
#19886=CARTESIAN_POINT('Ctrl Pts',(5.71394743641032,-3.88635869185298,24.6795207940858));
#19887=CARTESIAN_POINT('Ctrl Pts',(1.87003416737941,-3.16648164392546,24.8780369114974));
#19888=CARTESIAN_POINT('Ctrl Pts',(0.398188145107553,0.462946646320358,
25.076553028909));
#19889=CARTESIAN_POINT('Ctrl Pts',(1.88978798161488,2.58492499113116,25.2088971071835));
#19890=CARTESIAN_POINT('Ctrl Pts',(2.91960708544911,3.09611134481228,25.2750691463207));
#19891=CARTESIAN_POINT('Ctrl Pts',(2.58997049159961,-2.62015330925654,0.00319355095334283));
#19892=CARTESIAN_POINT('Ctrl Pts',(1.71783944528228,-1.99894889552244,0.0694097009926075));
#19893=CARTESIAN_POINT('Ctrl Pts',(0.65845605968771,0.171475772890977,0.20179789016909));
#19894=CARTESIAN_POINT('Ctrl Pts',(2.5459024084217,3.29075405988094,0.400358118482792));
#19895=CARTESIAN_POINT('Ctrl Pts',(6.18433372098768,3.38626231280436,0.598874235894448));
#19896=CARTESIAN_POINT('Ctrl Pts',(8.23950371306965,0.385416781850904,0.797390353306103));
#19897=CARTESIAN_POINT('Ctrl Pts',(6.83072086642306,-2.97082408396747,0.995906470717762));
#19898=CARTESIAN_POINT('Ctrl Pts',(3.24739392835603,-3.60517206763711,1.19442258812942));
#19899=CARTESIAN_POINT('Ctrl Pts',(0.771445147794971,-0.938633334672633,
1.39293870554108));
#19900=CARTESIAN_POINT('Ctrl Pts',(1.6701033647243,2.58783275185508,1.59145482295273));
#19901=CARTESIAN_POINT('Ctrl Pts',(5.12049770482736,3.74423103498232,1.78997094036439));
#19902=CARTESIAN_POINT('Ctrl Pts',(7.96276883664299,1.47182751406662,1.98848705777604));
#19903=CARTESIAN_POINT('Ctrl Pts',(7.59404699250464,-2.14849653622342,2.1870031751877));
#19904=CARTESIAN_POINT('Ctrl Pts',(4.35198598660702,-3.80124283382013,2.38551929259936));
#19905=CARTESIAN_POINT('Ctrl Pts',(1.20561125008781,-1.97289654529749,2.58403541001101));
#19906=CARTESIAN_POINT('Ctrl Pts',(1.0363089362513,1.66219780307218,2.78255152742267));
#19907=CARTESIAN_POINT('Ctrl Pts',(3.99912495903867,3.77507940693446,2.98106764483432));
#19908=CARTESIAN_POINT('Ctrl Pts',(7.38076768128599,2.43081698451723,3.17958376224598));
#19909=CARTESIAN_POINT('Ctrl Pts',(8.08439358796167,-1.13954237620741,3.37809987965763));
#19910=CARTESIAN_POINT('Ctrl Pts',(5.4656351638386,-3.66632999264102,3.5766159970693));
#19911=CARTESIAN_POINT('Ctrl Pts',(1.92270171311447,-2.83556261008053,3.77513211448094));
#19912=CARTESIAN_POINT('Ctrl Pts',(0.700144216203009,0.591959212043988,
3.97364823189261));
#19913=CARTESIAN_POINT('Ctrl Pts',(2.91755761499276,3.47737597536012,4.17216434930425));
#19914=CARTESIAN_POINT('Ctrl Pts',(6.54427687678886,3.1782780050441,4.37068046671592));
#19915=CARTESIAN_POINT('Ctrl Pts',(8.2590215005,-0.0314265247951463,4.56919658412757));
#19916=CARTESIAN_POINT('Ctrl Pts',(6.49146097171637,-3.21235123071783,4.76771270153922));
#19917=CARTESIAN_POINT('Ctrl Pts',(2.86029360321679,-3.45146579032245,4.96622881895089));
#19918=CARTESIAN_POINT('Ctrl Pts',(0.690873397337037,-0.529793630188544,
5.16474493636253));
#19919=CARTESIAN_POINT('Ctrl Pts',(1.96991411271267,2.8770534572674,5.36326105377419));
#19920=CARTESIAN_POINT('Ctrl Pts',(5.52609459169944,3.64914971667956,5.56177717118585));
#19921=CARTESIAN_POINT('Ctrl Pts',(8.1027323975949,1.07942407934716,5.7602932885975));
#19922=CARTESIAN_POINT('Ctrl Pts',(7.34019164048911,-2.47881759682101,5.95880940600916));
#19923=CARTESIAN_POINT('Ctrl Pts',(3.93679264073839,-3.76700527003896,6.15732552342081));
#19924=CARTESIAN_POINT('Ctrl Pts',(1.00930346276847,-1.60544117293717,6.35584164083248));
#19925=CARTESIAN_POINT('Ctrl Pts',(1.23866300903221,2.02635541158186,6.55435775824412));
#19926=CARTESIAN_POINT('Ctrl Pts',(4.41482816993367,3.80245425555658,6.75287387565579));
#19927=CARTESIAN_POINT('Ctrl Pts',(7.6291273081915,2.09633782263408,6.95138999306744));
#19928=CARTESIAN_POINT('Ctrl Pts',(7.93796641543966,-1.5295649116789,7.14990611047909));
#19929=CARTESIAN_POINT('Ctrl Pts',(5.05851651200422,-3.75472119528823,7.34842222789076));
#19930=CARTESIAN_POINT('Ctrl Pts',(1.62772304650576,-2.54137523062185,7.5469383453024));
#19931=CARTESIAN_POINT('Ctrl Pts',(0.787441414036509,0.999313828164636,
7.74545446271406));
#19932=CARTESIAN_POINT('Ctrl Pts',(3.30718554976015,3.62485029208286,7.94397058012572));
#19933=CARTESIAN_POINT('Ctrl Pts',(6.8794217047968,2.93081781047529,8.14248669753737));
#19934=CARTESIAN_POINT('Ctrl Pts',(8.23276395950072,-0.447201871899268,
8.34100281494903));
#19935=CARTESIAN_POINT('Ctrl Pts',(6.12784722031342,-3.41568258667014,8.53951893236069));
#19936=CARTESIAN_POINT('Ctrl Pts',(2.49231419722064,-3.25614616174064,8.73803504977233));
#19937=CARTESIAN_POINT('Ctrl Pts',(0.655516877599837,-0.114693020356707,
8.93655116718401));
#19938=CARTESIAN_POINT('Ctrl Pts',(2.29955930716991,3.13179380737736,9.13506728459565));
#19939=CARTESIAN_POINT('Ctrl Pts',(5.9188587019336,3.51024343935022,9.33358340200731));
#19940=CARTESIAN_POINT('Ctrl Pts',(8.19892952254092,0.674078901476532,9.53209951941897));
#19941=CARTESIAN_POINT('Ctrl Pts',(7.05172628302556,-2.77939427202906,9.73061563683061));
#19942=CARTESIAN_POINT('Ctrl Pts',(3.52783588801619,-3.68755104089551,9.92913175424228));
#19943=CARTESIAN_POINT('Ctrl Pts',(0.854370129759403,-1.21871871116838,
10.1276478716539));
#19944=CARTESIAN_POINT('Ctrl Pts',(1.47963809495571,2.36619303175871,10.3261639890656));
#19945=CARTESIAN_POINT('Ctrl Pts',(4.83103127493619,3.78419020596524,10.5246801064772));
#19946=CARTESIAN_POINT('Ctrl Pts',(7.83940754573271,1.73669797247918,10.7231962238889));
#19947=CARTESIAN_POINT('Ctrl Pts',(7.74975314393437,-1.90122922870495,10.9217123413006));
#19948=CARTESIAN_POINT('Ctrl Pts',(4.64417186530054,-3.79804686745578,11.1202284587122));
#19949=CARTESIAN_POINT('Ctrl Pts',(1.36669597038421,-2.21668543150265,11.3187445761239));
#19950=CARTESIAN_POINT('Ctrl Pts',(0.91877553954763,1.39467435679268,11.5172606935355));
#19951=CARTESIAN_POINT('Ctrl Pts',(3.71060758300086,3.72881789865659,11.7157768109472));
#19952=CARTESIAN_POINT('Ctrl Pts',(7.18548542162604,2.64818093856821,11.9142929283589));
#19953=CARTESIAN_POINT('Ctrl Pts',(8.16118202999545,-0.857609751318129,
12.1128090457705));
#19954=CARTESIAN_POINT('Ctrl Pts',(5.74417301388192,-3.57801774441457,12.3113251631822));
#19955=CARTESIAN_POINT('Ctrl Pts',(2.14790925385559,-3.02174514829049,12.5098412805938));
#19956=CARTESIAN_POINT('Ctrl Pts',(0.665780693158256,0.301784174950485,
12.7083573980055));
#19957=CARTESIAN_POINT('Ctrl Pts',(2.65509247460188,3.34894529131551,12.9068735154171));
#19958=CARTESIAN_POINT('Ctrl Pts',(6.29407070946287,3.32920601358802,13.1053896328288));
#19959=CARTESIAN_POINT('Ctrl Pts',(8.25020835096136,0.260643196829997,13.3039057502404));
#19960=CARTESIAN_POINT('Ctrl Pts',(6.7321117566965,-3.04661170162563,13.5024218676521));
#19961=CARTESIAN_POINT('Ctrl Pts',(3.1300249104368,-3.56383755643203,13.7009379850637));
#19962=CARTESIAN_POINT('Ctrl Pts',(0.742670427029733,-0.817368768436538,
13.8994541024754));
#19963=CARTESIAN_POINT('Ctrl Pts',(1.75634213008195,2.67763078969056,14.0979702198871));
#19964=CARTESIAN_POINT('Ctrl Pts',(5.24273875601857,3.7205070045574,14.2964863372987));
#19965=CARTESIAN_POINT('Ctrl Pts',(8.0090845931027,1.35621367619806,14.4950024547104));
#19966=CARTESIAN_POINT('Ctrl Pts',(7.52201274521021,-2.25007433890389,14.693518572122));
#19967=CARTESIAN_POINT('Ctrl Pts',(4.22757434555207,-3.79578707538995,14.8920346895337));
#19968=CARTESIAN_POINT('Ctrl Pts',(1.14275341367199,-1.86539021176013,15.0905508069453));
#19969=CARTESIAN_POINT('Ctrl Pts',(1.09257027946957,1.77329552431533,15.289066924357));
#19970=CARTESIAN_POINT('Ctrl Pts',(4.12298170266298,3.78803095088039,15.4875830417686));
#19971=CARTESIAN_POINT('Ctrl Pts',(7.45879454642923,2.3337596886183,15.6860991591803));
#19972=CARTESIAN_POINT('Ctrl Pts',(8.04513486233581,-1.25772430366396,15.8846152765919));
#19973=CARTESIAN_POINT('Ctrl Pts',(5.34504334245093,-3.69740830310385,16.0831313940036));
#19974=CARTESIAN_POINT('Ctrl Pts',(1.83121243949837,-2.75107611072479,16.2816475114153));
#19975=CARTESIAN_POINT('Ctrl Pts',(0.721541654250978,0.714639252839528,
16.4801636288269));
#19976=CARTESIAN_POINT('Ctrl Pts',(3.03224638366176,3.52590158253341,16.6786797462386));
#19977=CARTESIAN_POINT('Ctrl Pts',(6.64722719080097,3.10821031270302,16.8771958636502));
#19978=CARTESIAN_POINT('Ctrl Pts',(8.25595341671681,-0.155920837071448,
17.0757119810619));
#19979=CARTESIAN_POINT('Ctrl Pts',(6.38518418493321,-3.27726265018464,17.2742280984735));
#19980=CARTESIAN_POINT('Ctrl Pts',(2.74813437211341,-3.39734966840464,17.4727442158852));
#19981=CARTESIAN_POINT('Ctrl Pts',(0.675545012814546,-0.406208484742623,
17.6712603332969));
#19982=CARTESIAN_POINT('Ctrl Pts',(2.06545401745235,2.9569307023417,17.8697764507085));
#19983=CARTESIAN_POINT('Ctrl Pts',(5.64500915845253,3.61216899900811,18.0682925681202));
#19984=CARTESIAN_POINT('Ctrl Pts',(8.13612192804524,0.959451637121888,18.2668086855318));
#19985=CARTESIAN_POINT('Ctrl Pts',(7.25747863782803,-2.57191328333314,18.4653248029435));
#19986=CARTESIAN_POINT('Ctrl Pts',(3.81372409941205,-3.74796894189382,18.6638409203551));
#19987=CARTESIAN_POINT('Ctrl Pts',(0.958583211925542,-1.49170593738941,
18.8623570377668));
#19988=CARTESIAN_POINT('Ctrl Pts',(1.306739689582,2.13063298930591,19.0608731551785));
#19989=CARTESIAN_POINT('Ctrl Pts',(4.53935845279781,3.80177875335989,19.2593892725901));
#19990=CARTESIAN_POINT('Ctrl Pts',(7.69606872911877,1.99132785253305,19.4579053900018));
#19991=CARTESIAN_POINT('Ctrl Pts',(7.88601529454458,-1.64274321646801,19.6564215074134));
#19992=CARTESIAN_POINT('Ctrl Pts',(4.93524869751396,-3.77242129631514,19.8549376248251));
#19993=CARTESIAN_POINT('Ctrl Pts',(1.54602485826833,-2.44738771167893,20.0534537422367));
#19994=CARTESIAN_POINT('Ctrl Pts',(0.822130498506685,1.11891698433359,20.2519698596484));
#19995=CARTESIAN_POINT('Ctrl Pts',(3.42649430375165,3.66053879154859,20.45048597706));
#19996=CARTESIAN_POINT('Ctrl Pts',(6.97408943990954,2.84990880161489,20.6490020944717));
#19997=CARTESIAN_POINT('Ctrl Pts',(8.21609576658401,-0.570613452685432,
20.8475182118833));
#19998=CARTESIAN_POINT('Ctrl Pts',(6.015107509745,-3.46857877108964,21.046034329295));
#19999=CARTESIAN_POINT('Ctrl Pts',(2.38674785836889,-3.19008561139642,21.2445504467067));
#20000=CARTESIAN_POINT('Ctrl Pts',(0.653799542140776,0.00982723311048271,
21.4430665641183));
#20001=CARTESIAN_POINT('Ctrl Pts',(2.40326370386975,3.2007405539671,21.64158268153));
#20002=CARTESIAN_POINT('Ctrl Pts',(6.03301426782987,3.46047642676426,21.8400987989417));
#20003=CARTESIAN_POINT('Ctrl Pts',(8.21899485607472,0.551174068759129,22.0386149163533));
#20004=CARTESIAN_POINT('Ctrl Pts',(6.95932575274402,-2.86288350711349,22.2371310337649));
#20005=CARTESIAN_POINT('Ctrl Pts',(3.40758848840856,-3.65516588504588,22.4356471511766));
#20006=CARTESIAN_POINT('Ctrl Pts',(0.816395477550012,-1.10011867661645,
22.6341632685882));
#20007=CARTESIAN_POINT('Ctrl Pts',(1.55871392857562,2.46239974611297,22.8326793859999));
#20008=CARTESIAN_POINT('Ctrl Pts',(4.95473900642221,3.76989269217354,23.0311955034116));
#20009=CARTESIAN_POINT('Ctrl Pts',(7.89446267408575,1.62500233414576,23.2297116208232));
#20010=CARTESIAN_POINT('Ctrl Pts',(7.68572824288089,-2.00805862937836,23.4282277382349));
#20011=CARTESIAN_POINT('Ctrl Pts',(4.5197169557303,-3.80213094627573,23.6267438556465));
#20012=CARTESIAN_POINT('Ctrl Pts',(1.29575144062437,-2.11437372177854,23.8252599730582));
#20013=CARTESIAN_POINT('Ctrl Pts',(0.966374421579891,1.50985866999905,24.0237760904698));
#20014=CARTESIAN_POINT('Ctrl Pts',(3.83303817896047,3.7510614900228,24.2222922078815));
#20015=CARTESIAN_POINT('Ctrl Pts',(7.27086121968984,2.55774591981802,24.4208083252931));
#20016=CARTESIAN_POINT('Ctrl Pts',(8.13087041382945,-0.979117951521988,
24.6193244427048));
#20017=CARTESIAN_POINT('Ctrl Pts',(5.62679079307294,-3.61699263579137,24.8178405601165));
#20018=CARTESIAN_POINT('Ctrl Pts',(2.04930166016011,-2.94701073564213,25.0163566775281));
#20019=CARTESIAN_POINT('Ctrl Pts',(0.679470245798868,0.430859512276974,
25.2148727949398));
#20020=CARTESIAN_POINT('Ctrl Pts',(2.06768632464525,2.40576215381105,25.3472168732142));
#20021=CARTESIAN_POINT('Ctrl Pts',(3.02612799462649,2.8815178478641,25.4133889123514));
#20022=CARTESIAN_POINT('Ctrl Pts',(6.37918160141763,2.58636699315934,3.1286030352177));
#20023=CARTESIAN_POINT('Ctrl Pts',(6.30741621831574,2.63971758075101,3.12256282893198));
#20024=CARTESIAN_POINT('Ctrl Pts',(6.23342241705917,2.69008701405223,3.11654829135272));
#20025=CARTESIAN_POINT('Ctrl Pts',(6.07812215225983,2.78658711682447,3.10441138359402));
#20026=CARTESIAN_POINT('Ctrl Pts',(5.99675027082823,2.83237759333759,3.09830425807943));
#20027=CARTESIAN_POINT('Ctrl Pts',(5.87725019107504,2.89294836706277,3.08970510167227));
#20028=CARTESIAN_POINT('Ctrl Pts',(5.84065556149054,2.91063519540686,3.08711917555247));
#20029=CARTESIAN_POINT('Ctrl Pts',(5.77476040826474,2.94095952209419,3.08254573546535));
#20030=CARTESIAN_POINT('Ctrl Pts',(5.74558885575873,2.95386276872368,3.08054945346403));
#20031=CARTESIAN_POINT('Ctrl Pts',(5.70078278328311,2.97289129927177,3.07752534154838));
#20032=CARTESIAN_POINT('Ctrl Pts',(5.68528464289493,2.97933072989385,3.07648689840741));
#20033=CARTESIAN_POINT('Ctrl Pts',(5.66962384056547,2.98569475463646,3.07544503925855));
#20034=CARTESIAN_POINT('Ctrl Pts',(5.66951100782513,2.9857405986252,3.07543753327549));
#20035=CARTESIAN_POINT('Ctrl Pts',(5.66927747768848,2.98583546659269,3.07542199893488));
#20036=CARTESIAN_POINT('Ctrl Pts',(5.66915677994456,2.98588448963843,3.07541397061041));
#20037=CARTESIAN_POINT('Ctrl Pts',(5.66890694243952,2.98598594692363,3.07539735335573));
#20038=CARTESIAN_POINT('Ctrl Pts',(5.66877780222149,2.98603838011524,3.07538876445963));
#20039=CARTESIAN_POINT('Ctrl Pts',(5.66851045644071,2.98614690698533,3.07537098480326));
#20040=CARTESIAN_POINT('Ctrl Pts',(5.66837225039046,2.98620299944473,3.07536179408465));
#20041=CARTESIAN_POINT('Ctrl Pts',(5.66808609964525,2.98631911376347,3.07534276623617));
#20042=CARTESIAN_POINT('Ctrl Pts',(5.66793815437648,2.98637913422672,3.0753329291533));
#20043=CARTESIAN_POINT('Ctrl Pts',(5.66763179751311,2.9865033947639,3.07531256045323));
#20044=CARTESIAN_POINT('Ctrl Pts',(5.66747338527249,2.98656763322601,3.07530202889102));
#20045=CARTESIAN_POINT('Ctrl Pts',(5.66714530760974,2.98670064308427,3.07528021922124));
#20046=CARTESIAN_POINT('Ctrl Pts',(5.66697564141815,2.98676941263535,3.07526894117525));
#20047=CARTESIAN_POINT('Ctrl Pts',(5.66662420452476,2.9869118231053,3.07524558229451));
#20048=CARTESIAN_POINT('Ctrl Pts',(5.66644243297915,2.98698546188136,3.07523350153351));
#20049=CARTESIAN_POINT('Ctrl Pts',(5.66606586392061,2.9871379764623,3.0752084763802));
#20050=CARTESIAN_POINT('Ctrl Pts',(5.66587106538793,2.98721684981588,3.07519553206976));
#20051=CARTESIAN_POINT('Ctrl Pts',(5.66546744449525,2.9873802287776,3.07516871396948));
#20052=CARTESIAN_POINT('Ctrl Pts',(5.66525862099383,2.98746473154354,3.07515484027637));
#20053=CARTESIAN_POINT('Ctrl Pts',(5.66482586918937,2.98763979659986,3.07512609212352));
#20054=CARTESIAN_POINT('Ctrl Pts',(5.66460193955519,2.9877303556142,3.07511121777453));
#20055=CARTESIAN_POINT('Ctrl Pts',(5.6641378041319,2.98791799514358,3.07508039111529));
#20056=CARTESIAN_POINT('Ctrl Pts',(5.66389759679584,2.98801507187713,3.07506443893236));
#20057=CARTESIAN_POINT('Ctrl Pts',(5.66339963639431,2.98821624637538,3.0750313729991));
#20058=CARTESIAN_POINT('Ctrl Pts',(5.6631418815587,2.9883203397603,3.07501425939714));
#20059=CARTESIAN_POINT('Ctrl Pts',(5.66260745005453,2.98853608762625,3.07497878007606));
#20060=CARTESIAN_POINT('Ctrl Pts',(5.6623307713298,2.9886477370428,3.07496041452798));
#20061=CARTESIAN_POINT('Ctrl Pts',(5.6617570005945,2.98887918069369,3.07492233325841));
#20062=CARTESIAN_POINT('Ctrl Pts',(5.66145990620808,2.98899896906207,3.07490261773515));
#20063=CARTESIAN_POINT('Ctrl Pts',(5.66092414283189,2.98921489583492,3.07486706870618));
#20064=CARTESIAN_POINT('Ctrl Pts',(5.66068548022041,2.98931104993951,3.07485123467112));
#20065=CARTESIAN_POINT('Ctrl Pts',(5.66011191373954,2.98954205268078,3.07481318565032));
#20066=CARTESIAN_POINT('Ctrl Pts',(5.65977699866029,2.98967687364897,3.07479097159834));
#20067=CARTESIAN_POINT('Ctrl Pts',(5.65897213208931,2.99000071770139,3.07473759506564));
#20068=CARTESIAN_POINT('Ctrl Pts',(5.65850215856685,2.99018968631521,3.07470643442356));
#20069=CARTESIAN_POINT('Ctrl Pts',(5.65678508330488,2.99087962376996,3.07459261171173));
#20070=CARTESIAN_POINT('Ctrl Pts',(5.65553771149205,2.99137992381229,3.07450997221269));
#20071=CARTESIAN_POINT('Ctrl Pts',(5.64115186888314,2.9971394016061,3.07355744020205));
#20072=CARTESIAN_POINT('Ctrl Pts',(5.62797904602356,3.00231282711055,3.0726904470855));
#20073=CARTESIAN_POINT('Ctrl Pts',(5.59742155520105,3.0140820795246,3.07069108338549));
#20074=CARTESIAN_POINT('Ctrl Pts',(5.58001292423118,3.0206146037519,3.06956084978733));
#20075=CARTESIAN_POINT('Ctrl Pts',(5.52316140676146,3.04138842854456,3.06589760916342));
#20076=CARTESIAN_POINT('Ctrl Pts',(5.48349593535826,3.05501099402468,3.06338507493675));
#20077=CARTESIAN_POINT('Ctrl Pts',(5.24854294857735,3.13060885443019,3.04873495747833));
#20078=CARTESIAN_POINT('Ctrl Pts',(5.04796525040568,3.17462406827909,3.03720476709825));
#20079=CARTESIAN_POINT('Ctrl Pts',(4.63887649500039,3.22424682531855,3.01415537300919));
#20080=CARTESIAN_POINT('Ctrl Pts',(4.43130577231929,3.22930105445226,3.00267951248));
#20081=CARTESIAN_POINT('Ctrl Pts',(4.19223620995792,3.2120646007964,2.98837875207932));
#20082=CARTESIAN_POINT('Ctrl Pts',(4.1597945784986,3.20923075863535,2.9864143575472));
#20083=CARTESIAN_POINT('Ctrl Pts',(4.11549503930727,3.20468368787138,2.98369260973874));
#20084=CARTESIAN_POINT('Ctrl Pts',(4.10359429724189,3.20339510712159,2.98295753886961));
#20085=CARTESIAN_POINT('Ctrl Pts',(4.08361598010529,3.20111923058502,2.98171658371324));
#20086=CARTESIAN_POINT('Ctrl Pts',(4.07553432314849,3.20016756918412,2.98121267470738));
#20087=CARTESIAN_POINT('Ctrl Pts',(4.06015685945751,3.19829770925481,2.9802500622131));
#20088=CARTESIAN_POINT('Ctrl Pts',(4.05286044277384,3.19738513135089,2.97979169207905));
#20089=CARTESIAN_POINT('Ctrl Pts',(4.03551478953637,3.19515535594678,2.97869825952451));
#20090=CARTESIAN_POINT('Ctrl Pts',(4.02546858800257,3.19381571669535,2.97806196649877));
#20091=CARTESIAN_POINT('Ctrl Pts',(3.98991932947084,3.1889045193157,2.97580015828257));
#20092=CARTESIAN_POINT('Ctrl Pts',(3.96445370251704,3.18507479869402,2.97416124471114));
#20093=CARTESIAN_POINT('Ctrl Pts',(3.73354710376588,3.1475141030085,2.95914719429602));
#20094=CARTESIAN_POINT('Ctrl Pts',(3.53179628582646,3.09425724726375,2.94495688384999));
#20095=CARTESIAN_POINT('Ctrl Pts',(3.12245455097615,2.94256399556581,2.91545991982143));
#20096=CARTESIAN_POINT('Ctrl Pts',(2.91730732113421,2.84065043100939,2.90028322806361));
#20097=CARTESIAN_POINT('Ctrl Pts',(2.69790851115881,2.70084919901108,2.88388698218973));
#20098=CARTESIAN_POINT('Ctrl Pts',(2.67143566419799,2.68342644549244,2.88190427482752));
#20099=CARTESIAN_POINT('Ctrl Pts',(2.63131027830807,2.65616184759386,2.87889144865722));
#20100=CARTESIAN_POINT('Ctrl Pts',(2.61747125921,2.64659922231818,2.87785092388267));
#20101=CARTESIAN_POINT('Ctrl Pts',(2.59241816647276,2.62899639125184,2.87596441246112));
#20102=CARTESIAN_POINT('Ctrl Pts',(2.5811797214581,2.62099173290751,2.87511710091933));
#20103=CARTESIAN_POINT('Ctrl Pts',(2.55677377061703,2.60337108892213,2.87327455540356));
#20104=CARTESIAN_POINT('Ctrl Pts',(2.54362708372376,2.5937268181082,2.87228044056938));
#20105=CARTESIAN_POINT('Ctrl Pts',(2.50774061716639,2.56697962664781,2.86956197260998));
#20106=CARTESIAN_POINT('Ctrl Pts',(2.48515292268647,2.54967443228986,2.86784552822854));
#20107=CARTESIAN_POINT('Ctrl Pts',(2.36017613199945,2.45127171250288,2.85831254494002));
#20108=CARTESIAN_POINT('Ctrl Pts',(2.2625556945755,2.3643026245916,2.85073616686963));
#20109=CARTESIAN_POINT('Ctrl Pts',(2.01559144488247,2.11577774383062,2.83080029611922));
#20110=CARTESIAN_POINT('Ctrl Pts',(1.87706289127506,1.94449379476505,2.81878285706658));
#20111=CARTESIAN_POINT('Ctrl Pts',(1.69966627522793,1.67247945703279,2.80024810077018));
#20112=CARTESIAN_POINT('Ctrl Pts',(1.64663236578805,1.58175922024594,2.79413722795883));
#20113=CARTESIAN_POINT('Ctrl Pts',(1.59014539348432,1.47329715792194,2.78672200435909));
#20114=CARTESIAN_POINT('Ctrl Pts',(1.58228742048877,1.45790800427642,2.78566739911584));
#20115=CARTESIAN_POINT('Ctrl Pts',(1.57039380379087,1.43414549275553,2.78403401280563));
#20116=CARTESIAN_POINT('Ctrl Pts',(1.56626986278352,1.4258163534841,2.78346055499314));
#20117=CARTESIAN_POINT('Ctrl Pts',(1.55873910949178,1.41043954299495,2.78239994589603));
#20118=CARTESIAN_POINT('Ctrl Pts',(1.55532189262773,1.40339719231727,2.78191344691955));
#20119=CARTESIAN_POINT('Ctrl Pts',(1.54762732448303,1.38739168360427,2.78080606040031));
#20120=CARTESIAN_POINT('Ctrl Pts',(1.54336575165569,1.37842121079492,2.78018423162992));
#20121=CARTESIAN_POINT('Ctrl Pts',(1.53240116583824,1.35506316324844,2.77856227815285));
#20122=CARTESIAN_POINT('Ctrl Pts',(1.5257629514458,1.34064570526993,2.77755841617804));
#20123=CARTESIAN_POINT('Ctrl Pts',(1.48113244221961,1.24179759375036,2.77066013185173));
#20124=CARTESIAN_POINT('Ctrl Pts',(1.44669071043467,1.15582015859053,2.76458329457475));
#20125=CARTESIAN_POINT('Ctrl Pts',(1.38869762157164,0.990796268431566,2.75292599013063));
#20126=CARTESIAN_POINT('Ctrl Pts',(1.36438349275767,0.912088182955032,2.74736875828496));
#20127=CARTESIAN_POINT('Ctrl Pts',(1.30882384929709,0.704317436087036,2.73282385412915));
#20128=CARTESIAN_POINT('Ctrl Pts',(1.28248865597636,0.574094932078838,2.72383562217646));
#20129=CARTESIAN_POINT('Ctrl Pts',(1.2508203206929,0.345697770631459,2.70849869969516));
#20130=CARTESIAN_POINT('Ctrl Pts',(1.24180200072098,0.248212341007797,2.7020832132299));
#20131=CARTESIAN_POINT('Ctrl Pts',(1.23527469584318,0.108554355449584,2.69309941890341));
#20132=CARTESIAN_POINT('Ctrl Pts',(1.23413448035723,0.0666130458958216,
2.69042765331163));
#20133=CARTESIAN_POINT('Ctrl Pts',(1.23356090963365,-0.00834375021116602,
2.68569865564482));
#20134=CARTESIAN_POINT('Ctrl Pts',(1.23381536220876,-0.0413501889883888,
2.68363217820089));
#20135=CARTESIAN_POINT('Ctrl Pts',(1.23497111062394,-0.0914349446359473,
2.68051956925222));
#20136=CARTESIAN_POINT('Ctrl Pts',(1.23550133759388,-0.108518828846837,
2.67946193803549));
#20137=CARTESIAN_POINT('Ctrl Pts',(1.2367107390131,-0.139527593404653,2.67754941078168));
#20138=CARTESIAN_POINT('Ctrl Pts',(1.23734440303871,-0.153453731036658,
2.67669311465616));
#20139=CARTESIAN_POINT('Ctrl Pts',(1.23890609070547,-0.183482838240074,
2.6748521559889));
#20140=CARTESIAN_POINT('Ctrl Pts',(1.23986468595636,-0.199583889762953,
2.67386847260931));
#20141=CARTESIAN_POINT('Ctrl Pts',(1.24279664800391,-0.243296405000552,
2.67120672575759));
#20142=CARTESIAN_POINT('Ctrl Pts',(1.24500497259703,-0.270891122387398,
2.66953602686988));
#20143=CARTESIAN_POINT('Ctrl Pts',(1.25842914610231,-0.415224071405668,
2.66084307307456));
#20144=CARTESIAN_POINT('Ctrl Pts',(1.27565585472896,-0.531321008860896,
2.65401152422393));
#20145=CARTESIAN_POINT('Ctrl Pts',(1.30331604619479,-0.666460605696267,
2.64612661267374));
#20146=CARTESIAN_POINT('Ctrl Pts',(1.30765106493071,-0.686650507227025,
2.64495025211349));
#20147=CARTESIAN_POINT('Ctrl Pts',(1.35935395958566,-0.916658171206028,
2.63155920811023));
#20148=CARTESIAN_POINT('Ctrl Pts',(1.42741642687149,-1.12125714703055,2.61978619998866));
#20149=CARTESIAN_POINT('Ctrl Pts',(1.55778818771961,-1.41228301117058,2.60157650003628));
#20150=CARTESIAN_POINT('Ctrl Pts',(1.60477755459001,-1.50490702726582,2.59553343467051));
#20151=CARTESIAN_POINT('Ctrl Pts',(1.66467872842147,-1.61006866754962,2.58819446978672));
#20152=CARTESIAN_POINT('Ctrl Pts',(1.67332922825673,-1.62497600520683,2.58714249670317));
#20153=CARTESIAN_POINT('Ctrl Pts',(1.68682299455371,-1.64780587028186,2.58551234586619));
#20154=CARTESIAN_POINT('Ctrl Pts',(1.69158177488011,-1.65577830942292,2.58493945869309));
#20155=CARTESIAN_POINT('Ctrl Pts',(1.70041631222551,-1.67043462760341,2.58387937591637));
#20156=CARTESIAN_POINT('Ctrl Pts',(1.70448203217375,-1.67712432114842,2.58339282777401));
#20157=CARTESIAN_POINT('Ctrl Pts',(1.71376709020406,-1.69227718744503,2.58228464975907));
#20158=CARTESIAN_POINT('Ctrl Pts',(1.71900121778882,-1.7007310138355,2.58166207275952));
#20159=CARTESIAN_POINT('Ctrl Pts',(1.73271280215099,-1.72264979961774,2.58003688685625));
#20160=CARTESIAN_POINT('Ctrl Pts',(1.74125089231552,-1.73607625498422,2.57903051681592));
#20161=CARTESIAN_POINT('Ctrl Pts',(1.80066398761422,-1.82799509605761,2.57206877508557));
#20162=CARTESIAN_POINT('Ctrl Pts',(1.85483145816809,-1.90429647461469,2.5659272563331));
#20163=CARTESIAN_POINT('Ctrl Pts',(2.08422358152577,-2.19933697750453,2.54101240626791));
#20164=CARTESIAN_POINT('Ctrl Pts',(2.28436635280362,-2.39721522570006,2.52172622563897));
#20165=CARTESIAN_POINT('Ctrl Pts',(2.57818580305259,-2.62031054042873,2.49771522136086));
#20166=CARTESIAN_POINT('Ctrl Pts',(2.65097210029443,-2.67098455573032,2.49204668875813));
#20167=CARTESIAN_POINT('Ctrl Pts',(2.74665962795413,-2.73190095811372,2.48493854416513));
#20168=CARTESIAN_POINT('Ctrl Pts',(2.76771096851286,-2.74496398961727,2.48339505347836));
#20169=CARTESIAN_POINT('Ctrl Pts',(2.80203223493242,-2.76571714131716,2.48091071307703));
#20170=CARTESIAN_POINT('Ctrl Pts',(2.81520977258424,-2.77355736907932,2.47996439918888));
#20171=CARTESIAN_POINT('Ctrl Pts',(2.84059051386314,-2.78841389688691,2.47815594770866));
#20172=CARTESIAN_POINT('Ctrl Pts',(2.85278468263975,-2.79544485996068,2.47729329309791));
#20173=CARTESIAN_POINT('Ctrl Pts',(2.88076266824742,-2.81133319713251,2.47532798519566));
#20174=CARTESIAN_POINT('Ctrl Pts',(2.89657590831167,-2.82013800297365,2.47422723637995));
#20175=CARTESIAN_POINT('Ctrl Pts',(2.94685108544774,-2.84757894589775,2.47075855783552));
#20176=CARTESIAN_POINT('Ctrl Pts',(2.98157988881301,-2.86572057576469,2.46840813149915));
#20177=CARTESIAN_POINT('Ctrl Pts',(3.25096246978223,-3.0002459839599,2.4505022776045));
#20178=CARTESIAN_POINT('Ctrl Pts',(3.49868123701998,-3.08826468039805,2.43601843119229));
#20179=CARTESIAN_POINT('Ctrl Pts',(3.87332352426088,-3.17189551675349,2.41450529306424));
#20180=CARTESIAN_POINT('Ctrl Pts',(3.99370935379962,-3.19168122391711,2.40762930714677));
#20181=CARTESIAN_POINT('Ctrl Pts',(4.15422487698384,-3.20878928709383,2.39819188963642));
#20182=CARTESIAN_POINT('Ctrl Pts',(4.19360528869756,-3.21225506458201,2.39585503409401));
#20183=CARTESIAN_POINT('Ctrl Pts',(4.26024427348816,-3.21688625083731,2.39184954874845));
#20184=CARTESIAN_POINT('Ctrl Pts',(4.28747274326101,-3.21843152065529,2.39019854321635));
#20185=CARTESIAN_POINT('Ctrl Pts',(4.32587031984897,-3.22012207349703,2.38784594822452));
#20186=CARTESIAN_POINT('Ctrl Pts',(4.33702641884141,-3.22055517684282,2.38715952706558));
#20187=CARTESIAN_POINT('Ctrl Pts',(4.35616458891464,-3.22119858476464,2.3859766729185));
#20188=CARTESIAN_POINT('Ctrl Pts',(4.36414572619566,-3.22143721203675,2.38548180520032));
#20189=CARTESIAN_POINT('Ctrl Pts',(4.37966778272985,-3.22184357340249,2.38451616088276));
#20190=CARTESIAN_POINT('Ctrl Pts',(4.38720847410977,-3.22201449668491,2.38404558958097));
#20191=CARTESIAN_POINT('Ctrl Pts',(4.40782620165717,-3.22240942316101,2.38275510190075));
#20192=CARTESIAN_POINT('Ctrl Pts',(4.42090394251223,-3.22258029039911,2.38193231311119));
#20193=CARTESIAN_POINT('Ctrl Pts',(4.47159336370544,-3.22293398871823,2.37872769417013));
#20194=CARTESIAN_POINT('Ctrl Pts',(4.50920448875094,-3.22253796461204,2.37631687487083));
#20195=CARTESIAN_POINT('Ctrl Pts',(4.76491580081086,-3.21536793090091,2.35973963632905));
#20196=CARTESIAN_POINT('Ctrl Pts',(4.98183567129539,-3.18711650140904,2.34479680709835));
#20197=CARTESIAN_POINT('Ctrl Pts',(5.32851967263839,-3.10558814585225,2.32080385518719));
#20198=CARTESIAN_POINT('Ctrl Pts',(5.46065884560665,-3.06541348662698,2.31162117477715));
#20199=CARTESIAN_POINT('Ctrl Pts',(5.66357210137934,-2.98918477646024,2.29757783869267));
#20200=CARTESIAN_POINT('Ctrl Pts',(5.73628040224296,-2.9587848926759,2.29255597163309));
#20201=CARTESIAN_POINT('Ctrl Pts',(5.82942901312241,-2.91576163516891,2.28613207406645));
#20202=CARTESIAN_POINT('Ctrl Pts',(5.8509403031124,-2.90553522591516,2.28464918053248));
#20203=CARTESIAN_POINT('Ctrl Pts',(5.88592404100724,-2.88842602875519,2.28223806835214));
#20204=CARTESIAN_POINT('Ctrl Pts',(5.89946459113835,-2.88168533624427,2.28130496590441));
#20205=CARTESIAN_POINT('Ctrl Pts',(5.9255793475553,-2.86845478744269,2.27950540600963));
#20206=CARTESIAN_POINT('Ctrl Pts',(5.93815922901359,-2.86197696686913,2.27863855392636));
#20207=CARTESIAN_POINT('Ctrl Pts',(5.96715234031196,-2.84680499682379,2.27664054066455));
#20208=CARTESIAN_POINT('Ctrl Pts',(5.98353398891745,-2.83805133676436,2.27551150651134));
#20209=CARTESIAN_POINT('Ctrl Pts',(6.0365476703471,-2.80913114818228,2.27185658251019));
#20210=CARTESIAN_POINT('Ctrl Pts',(6.07286399447933,-2.7883927061523,2.26935103130209));
#20211=CARTESIAN_POINT('Ctrl Pts',(6.20193433149682,-2.71131775386986,2.2604271230675));
#20212=CARTESIAN_POINT('Ctrl Pts',(6.29218331063479,-2.65104180749099,2.25415409453453));
#20213=CARTESIAN_POINT('Ctrl Pts',(6.3791823737616,-2.58636641899648,2.24798337798073));
#20214=CARTESIAN_POINT('Ctrl Pts',(2.17296269996979,-3.20554048108048,-0.411765747138983));
#20215=CARTESIAN_POINT('Ctrl Pts',(1.10598262521586,-2.44554835076675,-0.345549597099719));
#20216=CARTESIAN_POINT('Ctrl Pts',(-0.190085171851759,0.209786400507346,
-0.213161407923235));
#20217=CARTESIAN_POINT('Ctrl Pts',(2.11904905146237,4.02596493684606,-0.0146011796095345));
#20218=CARTESIAN_POINT('Ctrl Pts',(6.57036830017086,4.14281137096193,0.183914937802122));
#20219=CARTESIAN_POINT('Ctrl Pts',(9.08469850437939,0.471525498888313,0.382431055213778));
#20220=CARTESIAN_POINT('Ctrl Pts',(7.36116941620609,-3.63455711911314,0.580947172625436));
#20221=CARTESIAN_POINT('Ctrl Pts',(2.97726580402431,-4.41062931823268,0.77946329003709));
#20222=CARTESIAN_POINT('Ctrl Pts',(-0.0518523842630756,-1.14834011450979,
0.977979407448747));
#20223=CARTESIAN_POINT('Ctrl Pts',(1.04758148582589,3.16599895701937,1.1764955248604));
#20224=CARTESIAN_POINT('Ctrl Pts',(5.26885307852876,4.58075644304919,1.37501164227206));
#20225=CARTESIAN_POINT('Ctrl Pts',(8.74613631193873,1.80065901519612,1.57352775968371));
#20226=CARTESIAN_POINT('Ctrl Pts',(8.2950356860829,-2.62850749839492,1.77204387709537));
#20227=CARTESIAN_POINT('Ctrl Pts',(4.32864266632258,-4.6505056552148,1.97055999450703));
#20228=CARTESIAN_POINT('Ctrl Pts',(0.479313869061077,-2.41367545883394,
2.16907611191868));
#20229=CARTESIAN_POINT('Ctrl Pts',(0.272186515624751,2.03356129066451,2.36759222933034));
#20230=CARTESIAN_POINT('Ctrl Pts',(3.89694643539194,4.61849687019083,2.56610834674199));
#20231=CARTESIAN_POINT('Ctrl Pts',(8.03410612006349,2.97390317522259,2.76462446415365));
#20232=CARTESIAN_POINT('Ctrl Pts',(8.89493411795877,-1.39413568050936,2.9631405815653));
#20233=CARTESIAN_POINT('Ctrl Pts',(5.69110016326603,-4.48545097223521,3.16165669897696));
#20234=CARTESIAN_POINT('Ctrl Pts',(1.35661463604595,-3.46907591290164,3.36017281638862));
#20235=CARTESIAN_POINT('Ctrl Pts',(-0.139083166427389,0.724213049156903,
3.55868893380027));
#20236=CARTESIAN_POINT('Ctrl Pts',(2.57373840321099,4.25428138787658,3.75720505121192));
#20237=CARTESIAN_POINT('Ctrl Pts',(7.01072892820446,3.88835980295648,3.95572116862359));
#20238=CARTESIAN_POINT('Ctrl Pts',(9.10857690015422,-0.0384477492421469,
4.15423728603523));
#20239=CARTESIAN_POINT('Ctrl Pts',(6.94611304441007,-3.93004557143118,4.3527534034469));
#20240=CARTESIAN_POINT('Ctrl Pts',(2.50368062941278,-4.22258242327136,4.55126952085854));
#20241=CARTESIAN_POINT('Ctrl Pts',(-0.15042524517621,-0.648158610486061,
4.74978563827021));
#20242=CARTESIAN_POINT('Ctrl Pts',(1.41437509517098,3.51983652671062,4.94830175568186));
#20243=CARTESIAN_POINT('Ctrl Pts',(5.76506726388787,4.46443232806813,5.14681787309352));
#20244=CARTESIAN_POINT('Ctrl Pts',(8.91737013208296,1.32058592540232,5.34533399050517));
#20245=CARTESIAN_POINT('Ctrl Pts',(7.98446469607637,-3.03262794728552,5.54385010791683));
#20246=CARTESIAN_POINT('Ctrl Pts',(3.82068800849579,-4.60861883268182,5.74236622532849));
#20247=CARTESIAN_POINT('Ctrl Pts',(0.239147556357015,-1.9641242562649,5.94088234274014));
#20248=CARTESIAN_POINT('Ctrl Pts',(0.519749957626067,2.47907795239849,6.13939846015179));
#20249=CARTESIAN_POINT('Ctrl Pts',(4.40552487083362,4.65198772933701,6.33791457756345));
#20250=CARTESIAN_POINT('Ctrl Pts',(8.33795354574623,2.56469563392857,6.53643069497511));
#20251=CARTESIAN_POINT('Ctrl Pts',(8.71579260460107,-1.87129593734266,6.73494681238676));
#20252=CARTESIAN_POINT('Ctrl Pts',(5.19302422456139,-4.59359028502123,6.93346292979842));
#20253=CARTESIAN_POINT('Ctrl Pts',(0.995732677906764,-3.10916202902842,
7.13197904721008));
#20254=CARTESIAN_POINT('Ctrl Pts',(-0.0322822778871914,1.22257767061497,
7.33049516462173));
#20255=CARTESIAN_POINT('Ctrl Pts',(3.05041589877745,4.43470399540276,7.52901128203338));
#20256=CARTESIAN_POINT('Ctrl Pts',(7.42075085684839,3.58561275821527,7.72752739944505));
#20257=CARTESIAN_POINT('Ctrl Pts',(9.07645297431008,-0.547114437358846,
7.9260435168567));
#20258=CARTESIAN_POINT('Ctrl Pts',(6.5012617467849,-4.17880463841992,8.12455963426836));
#20259=CARTESIAN_POINT('Ctrl Pts',(2.05348831510913,-3.98362504090881,8.32307575168001));
#20260=CARTESIAN_POINT('Ctrl Pts',(-0.193681017610346,-0.140317407516647,
8.52159186909167));
#20261=CARTESIAN_POINT('Ctrl Pts',(1.81766867783776,3.83149023855917,8.72010798650331));
#20262=CARTESIAN_POINT('Ctrl Pts',(6.24558161029013,4.2944920068349,8.91862410391498));
#20263=CARTESIAN_POINT('Ctrl Pts',(9.03505934404192,0.824679685151172,9.11714022132663));
#20264=CARTESIAN_POINT('Ctrl Pts',(7.6315512320161,-3.40035860512303,9.31565633873829));
#20265=CARTESIAN_POINT('Ctrl Pts',(3.32036330565075,-4.51141316650472,9.51417245614994));
#20266=CARTESIAN_POINT('Ctrl Pts',(0.0495994604212725,-1.49100136617927,
9.71268857356161));
#20267=CARTESIAN_POINT('Ctrl Pts',(0.814563009263402,2.89484112343983,9.91120469097325));
#20268=CARTESIAN_POINT('Ctrl Pts',(4.91471488529713,4.62964317792977,10.1097208083849));
#20269=CARTESIAN_POINT('Ctrl Pts',(8.59521399360942,2.1247060752228,10.3082369257966));
#20270=CARTESIAN_POINT('Ctrl Pts',(8.48552926132444,-2.32599643497811,10.5067530432082));
#20271=CARTESIAN_POINT('Ctrl Pts',(4.68610787984395,-4.64659565516981,10.7052691606199));
#20272=CARTESIAN_POINT('Ctrl Pts',(0.676387677669684,-2.71193096197848,
10.9037852780315));
#20273=CARTESIAN_POINT('Ctrl Pts',(0.128394142987057,1.70626851979591,11.1023013954432));
#20274=CARTESIAN_POINT('Ctrl Pts',(3.54396933091606,4.56189974780998,11.3008175128549));
#20275=CARTESIAN_POINT('Ctrl Pts',(7.79519445548059,3.23982996331418,11.4993336302665));
#20276=CARTESIAN_POINT('Ctrl Pts',(8.98887841448097,-1.04921447348414,11.6978497476782));
#20277=CARTESIAN_POINT('Ctrl Pts',(6.03186814454124,-4.3774082536412,11.8963658650898));
#20278=CARTESIAN_POINT('Ctrl Pts',(1.63213740257258,-3.69685482224785,12.0948819825015));
#20279=CARTESIAN_POINT('Ctrl Pts',(-0.181124089683036,0.369207933724872,
12.2933980999131));
#20280=CARTESIAN_POINT('Ctrl Pts',(2.2526340504912,4.09715708707193,12.4919142173248));
#20281=CARTESIAN_POINT('Ctrl Pts',(6.70462241331237,4.07300771627025,12.6904303347364));
#20282=CARTESIAN_POINT('Ctrl Pts',(9.09779474190718,0.318875355730261,12.8889464521481));
#20283=CARTESIAN_POINT('Ctrl Pts',(7.24052934071316,-3.72727698993507,13.0874625695597));
#20284=CARTESIAN_POINT('Ctrl Pts',(2.83367453520978,-4.36005996854408,13.2859786869714));
#20285=CARTESIAN_POINT('Ctrl Pts',(-0.0870558709899348,-0.999982965095223,
13.4844948043831));
#20286=CARTESIAN_POINT('Ctrl Pts',(1.1530874699283,3.2758594160949,13.6830109217947));
#20287=CARTESIAN_POINT('Ctrl Pts',(5.41840487637927,4.55173205747878,13.8815270392064));
#20288=CARTESIAN_POINT('Ctrl Pts',(8.80279980247531,1.65921506374814,14.080043156618));
#20289=CARTESIAN_POINT('Ctrl Pts',(8.20690775291552,-2.75277952374592,14.2785592740297));
#20290=CARTESIAN_POINT('Ctrl Pts',(4.17643533161801,-4.64383098681233,14.4770753914414));
#20291=CARTESIAN_POINT('Ctrl Pts',(0.402412514292184,-2.28215036718792,
14.675591508853));
#20292=CARTESIAN_POINT('Ctrl Pts',(0.341017607518878,2.16948014760412,14.8741076262646));
#20293=CARTESIAN_POINT('Ctrl Pts',(4.04847489906614,4.63434201110855,15.0726237436763));
#20294=CARTESIAN_POINT('Ctrl Pts',(8.12956552465056,2.85516161537223,15.271139861088));
#20295=CARTESIAN_POINT('Ctrl Pts',(8.84690431993714,-1.53872147678918,15.4696559784996));
#20296=CARTESIAN_POINT('Ctrl Pts',(5.54356606143321,-4.52347271009317,15.6681720959113));
#20297=CARTESIAN_POINT('Ctrl Pts',(1.24468509012015,-3.36571368106855,15.8666882133229));
#20298=CARTESIAN_POINT('Ctrl Pts',(-0.112905173860372,0.874301914415817,
16.0652043307346));
#20299=CARTESIAN_POINT('Ctrl Pts',(2.71405060913991,4.31364844766405,16.2637204481462));
#20300=CARTESIAN_POINT('Ctrl Pts',(7.1366801074503,3.80263778683562,16.4622365655579));
#20301=CARTESIAN_POINT('Ctrl Pts',(9.10482335385156,-0.190756225336315,
16.6607526829696));
#20302=CARTESIAN_POINT('Ctrl Pts',(6.81609220134375,-4.00945931491334,16.8592688003812));
#20303=CARTESIAN_POINT('Ctrl Pts',(2.36646310311057,-4.15637583189606,17.0577849177929));
#20304=CARTESIAN_POINT('Ctrl Pts',(-0.16917825360623,-0.496962424679848,
17.2563010352045));
#20305=CARTESIAN_POINT('Ctrl Pts',(1.53126025266144,3.61755971783011,17.4548171526162));
#20306=CARTESIAN_POINT('Ctrl Pts',(5.91054938364417,4.41918948403437,17.6533332700278));
#20307=CARTESIAN_POINT('Ctrl Pts',(8.95821945609951,1.17380958265607,17.8518493874395));
#20308=CARTESIAN_POINT('Ctrl Pts',(7.88327219050615,-3.14652280629029,18.0503655048511));
#20309=CARTESIAN_POINT('Ctrl Pts',(3.67012384502666,-4.58532946245115,18.2488816222628));
#20310=CARTESIAN_POINT('Ctrl Pts',(0.177095531876928,-1.82497861910485,
18.4473977396744));
#20311=CARTESIAN_POINT('Ctrl Pts',(0.603036135785551,2.60665292882547,18.6459138570862));
#20312=CARTESIAN_POINT('Ctrl Pts',(4.55787735396168,4.65116130836808,18.8444299744978));
#20313=CARTESIAN_POINT('Ctrl Pts',(8.41985082781949,2.43622463611074,19.0429460919094));
#20314=CARTESIAN_POINT('Ctrl Pts',(8.65223471259592,-2.00976021586402,19.2414622093211));
#20315=CARTESIAN_POINT('Ctrl Pts',(5.04221626688697,-4.61524489208584,19.4399783267328));
#20316=CARTESIAN_POINT('Ctrl Pts',(0.895781713701428,-2.99417608693739,
19.6384944441444));
#20317=CARTESIAN_POINT('Ctrl Pts',(0.0101569427980723,1.36890222246852,
19.8370105615561));
#20318=CARTESIAN_POINT('Ctrl Pts',(3.1963802739596,4.47836591752857,20.0355266789677));
#20319=CARTESIAN_POINT('Ctrl Pts',(7.53656898706393,3.48662728959027,20.2340427963793));
#20320=CARTESIAN_POINT('Ctrl Pts',(9.05606082131957,-0.698098281184544,
20.432558913791));
#20321=CARTESIAN_POINT('Ctrl Pts',(6.36333405195284,-4.24351873734398,20.6310750312027));
#20322=CARTESIAN_POINT('Ctrl Pts',(1.9243366462227,-3.90280543100934,20.8295911486144));
#20323=CARTESIAN_POINT('Ctrl Pts',(-0.195782035254683,0.0120228054752082,
21.028107266026));
#20324=CARTESIAN_POINT('Ctrl Pts',(1.94454241477252,3.91584087042925,21.2266233834376));
#20325=CARTESIAN_POINT('Ctrl Pts',(6.38524148680512,4.23360619038166,21.4251395008493));
#20326=CARTESIAN_POINT('Ctrl Pts',(9.05960761710739,0.674315805600993,21.623655618261));
#20327=CARTESIAN_POINT('Ctrl Pts',(7.5185068390623,-3.50250076674849,21.8221717356726));
#20328=CARTESIAN_POINT('Ctrl Pts',(3.17325057532877,-4.47179261159471,22.0206878530843));
#20329=CARTESIAN_POINT('Ctrl Pts',(0.0031406198327811,-1.34590405051051,
22.2192039704959));
#20330=CARTESIAN_POINT('Ctrl Pts',(0.911305739869395,3.01254206724522,22.4177200879076));
#20331=CARTESIAN_POINT('Ctrl Pts',(5.06606104496655,4.6121513544261,22.6162362053192));
#20332=CARTESIAN_POINT('Ctrl Pts',(8.66256938155685,1.98805571626367,22.8147523227309));
#20333=CARTESIAN_POINT('Ctrl Pts',(8.4072000996685,-2.45669335535235,23.0132684401425));
#20334=CARTESIAN_POINT('Ctrl Pts',(4.53384760969594,-4.65159218721967,23.2117845575542));
#20335=CARTESIAN_POINT('Ctrl Pts',(0.589592923617338,-2.58676106216746,
23.4103006749659));
#20336=CARTESIAN_POINT('Ctrl Pts',(0.186627431348294,1.84718698340797,23.6088167923775));
#20337=CARTESIAN_POINT('Ctrl Pts',(3.69375302108596,4.58911293885384,23.8073329097892));
#20338=CARTESIAN_POINT('Ctrl Pts',(7.89964467060016,3.12919021086655,24.0058490272008));
#20339=CARTESIAN_POINT('Ctrl Pts',(8.95179466357075,-1.19786968887199,24.2043651446125));
#20340=CARTESIAN_POINT('Ctrl Pts',(5.88826072308503,-4.42509080397621,24.4028812620241));
#20341=CARTESIAN_POINT('Ctrl Pts',(1.51149918181804,-3.60542346049212,24.6013973794358));
#20342=CARTESIAN_POINT('Ctrl Pts',(-0.164376056275096,0.527120914407128,
24.7999134968474));
#20343=CARTESIAN_POINT('Ctrl Pts',(1.53399129555416,2.94325066577138,24.9322575751219));
#20344=CARTESIAN_POINT('Ctrl Pts',(2.70656526709436,3.52529833870864,24.9984296142591));
#20345=CARTESIAN_POINT('Ctrl Pts',(2.31196529717974,-3.01041142380583,-0.273445981108207));
#20346=CARTESIAN_POINT('Ctrl Pts',(1.30993489857133,-2.29668186568531,-0.207229831068943));
#20347=CARTESIAN_POINT('Ctrl Pts',(0.0927619053280601,0.197016191301887,
-0.0748416418924601));
#20348=CARTESIAN_POINT('Ctrl Pts',(2.26133350378215,3.78089464452436,0.123718586421241));
#20349=CARTESIAN_POINT('Ctrl Pts',(6.44169010710979,3.89062835157607,0.322234703832897));
#20350=CARTESIAN_POINT('Ctrl Pts',(8.80296690727615,0.442822593209179,0.520750821244553));
#20351=CARTESIAN_POINT('Ctrl Pts',(7.18435323294509,-3.41331277406459,0.719266938656211));
#20352=CARTESIAN_POINT('Ctrl Pts',(3.06730851213489,-4.14214356803415,0.917783056067867));
#20353=CARTESIAN_POINT('Ctrl Pts',(0.222580126422941,-1.07843785456408,
1.11629917347952));
#20354=CARTESIAN_POINT('Ctrl Pts',(1.25508877879203,2.97327688863128,1.31481529089117));
#20355=CARTESIAN_POINT('Ctrl Pts',(5.21940128729496,4.30191464036023,1.51333140830283));
#20356=CARTESIAN_POINT('Ctrl Pts',(8.48501382017349,1.69104851481962,1.71184752571448));
#20357=CARTESIAN_POINT('Ctrl Pts',(8.06137278822348,-2.46850384433775,1.91036364312614));
#20358=CARTESIAN_POINT('Ctrl Pts',(4.33642377308406,-4.36741804808325,2.1088797605378));
#20359=CARTESIAN_POINT('Ctrl Pts',(0.721412996069988,-2.26674915432179,
2.30739587794946));
#20360=CARTESIAN_POINT('Ctrl Pts',(0.526893989166935,1.90977346146706,2.50591199536111));
#20361=CARTESIAN_POINT('Ctrl Pts',(3.93100594327419,4.33735771577206,2.70442811277276));
#20362=CARTESIAN_POINT('Ctrl Pts',(7.81632664047099,2.79287444498747,2.90294423018442));
#20363=CARTESIAN_POINT('Ctrl Pts',(8.62475394129306,-1.30927124574203,3.10146034759608));
#20364=CARTESIAN_POINT('Ctrl Pts',(5.61594516345689,-4.21241064570382,3.29997646500774));
#20365=CARTESIAN_POINT('Ctrl Pts',(1.54531032840212,-3.25790481196126,3.49849258241939));
#20366=CARTESIAN_POINT('Ctrl Pts',(0.140659294449413,0.680128436785933,
3.69700869983105));
#20367=CARTESIAN_POINT('Ctrl Pts',(2.68834480713824,3.99531291703776,3.8955248172427));
#20368=CARTESIAN_POINT('Ctrl Pts',(6.85524491106594,3.65166587031902,4.09404093465435));
#20369=CARTESIAN_POINT('Ctrl Pts',(8.82539176693615,-0.0361073410931478,
4.29255705206602));
#20370=CARTESIAN_POINT('Ctrl Pts',(6.79456235351217,-3.69081412452673,4.49107316947766));
#20371=CARTESIAN_POINT('Ctrl Pts',(2.62255162068078,-3.96554354562172,4.68958928688933));
#20372=CARTESIAN_POINT('Ctrl Pts',(0.130007635661538,-0.608703617053558,
4.88810540430098));
#20373=CARTESIAN_POINT('Ctrl Pts',(1.59955476768487,3.30557550356288,5.08662152171263));
#20374=CARTESIAN_POINT('Ctrl Pts',(5.68540970649173,4.19267145760527,5.28513763912429));
#20375=CARTESIAN_POINT('Ctrl Pts',(8.64582422058695,1.24019864338394,5.48365375653594));
#20376=CARTESIAN_POINT('Ctrl Pts',(7.76970701088062,-2.84802449713069,5.68216987394761));
#20377=CARTESIAN_POINT('Ctrl Pts',(3.85938955257665,-4.32808097846753,5.88068599135924));
#20378=CARTESIAN_POINT('Ctrl Pts',(0.495866191827503,-1.844563228489,6.07920210877092));
#20379=CARTESIAN_POINT('Ctrl Pts',(0.759387641428115,2.32817043879295,6.27771822618256));
#20380=CARTESIAN_POINT('Ctrl Pts',(4.40862597053364,4.36880990474354,6.47623434359423));
#20381=CARTESIAN_POINT('Ctrl Pts',(8.10167813322798,2.40857636349708,6.67475046100588));
#20382=CARTESIAN_POINT('Ctrl Pts',(8.45651720821394,-1.75738559545474,6.87326657841754));
#20383=CARTESIAN_POINT('Ctrl Pts',(5.14818832037566,-4.31396725511023,7.0717826958292));
#20384=CARTESIAN_POINT('Ctrl Pts',(1.20639613410644,-2.9198997628929,7.27029881324085));
#20385=CARTESIAN_POINT('Ctrl Pts',(0.240958952754043,1.14815638979818,7.4688149306525));
#20386=CARTESIAN_POINT('Ctrl Pts',(3.13600578243834,4.16475276096279,7.66733104806417));
#20387=CARTESIAN_POINT('Ctrl Pts',(7.24030780616454,3.36734777563528,7.86584716547581));
#20388=CARTESIAN_POINT('Ctrl Pts',(8.79522330270695,-0.513810248872322,
8.06436328288747));
#20389=CARTESIAN_POINT('Ctrl Pts',(6.37679023796107,-3.92443062116999,8.26287940029913));
#20390=CARTESIAN_POINT('Ctrl Pts',(2.1997636091463,-3.74113208118609,8.46139551771078));
#20391=CARTESIAN_POINT('Ctrl Pts',(0.089384947459713,-0.131775945129999,
8.65991163512245));
#20392=CARTESIAN_POINT('Ctrl Pts',(1.97829888761515,3.5982580948319,8.8584277525341));
#20393=CARTESIAN_POINT('Ctrl Pts',(6.13667397417128,4.03307581767334,9.05694386994575));
#20394=CARTESIAN_POINT('Ctrl Pts',(8.75634940354159,0.774479423926291,9.2554599873574));
#20395=CARTESIAN_POINT('Ctrl Pts',(7.43827624901926,-3.19337049409171,9.45397610476906));
#20396=CARTESIAN_POINT('Ctrl Pts',(3.38952083310589,-4.23679245796831,9.65249222218073));
#20397=CARTESIAN_POINT('Ctrl Pts',(0.317856350200649,-1.40024048117564,
9.85100833959237));
#20398=CARTESIAN_POINT('Ctrl Pts',(1.03625470449417,2.71862509287945,10.049524457004));
#20399=CARTESIAN_POINT('Ctrl Pts',(4.88682034851015,4.34782552060827,10.2480405744157));
#20400=CARTESIAN_POINT('Ctrl Pts',(8.34327851098385,1.99537004097493,10.4465566918273));
#20401=CARTESIAN_POINT('Ctrl Pts',(8.24027055552775,-2.18440736622039,10.645072809239));
#20402=CARTESIAN_POINT('Ctrl Pts',(4.67212920832948,-4.36374605926514,10.8435889266506));
#20403=CARTESIAN_POINT('Ctrl Pts',(0.906490441907856,-2.54684911848653,
11.0421050440623));
#20404=CARTESIAN_POINT('Ctrl Pts',(0.391854608507251,1.60240379879482,11.2406211614739));
#20405=CARTESIAN_POINT('Ctrl Pts',(3.59951541494433,4.28420579809219,11.4391372788856));
#20406=CARTESIAN_POINT('Ctrl Pts',(7.59195811086242,3.04261362173219,11.6376533962972));
#20407=CARTESIAN_POINT('Ctrl Pts',(8.71297961965247,-0.98534623276214,11.8361695137089));
#20408=CARTESIAN_POINT('Ctrl Pts',(5.93596976765481,-4.11094475056566,12.0346856311206));
#20409=CARTESIAN_POINT('Ctrl Pts',(1.80406135300024,-3.47181826426207,12.2332017485322));
#20410=CARTESIAN_POINT('Ctrl Pts',(0.101177504597399,0.346733347466743,
12.4317178659439));
#20411=CARTESIAN_POINT('Ctrl Pts',(2.38678685852808,3.84775315515312,12.6302339833555));
#20412=CARTESIAN_POINT('Ctrl Pts',(6.56777184536255,3.82507381537617,12.8287501007672));
#20413=CARTESIAN_POINT('Ctrl Pts',(8.81526594492522,0.29946463609684,13.0272662181788));
#20414=CARTESIAN_POINT('Ctrl Pts',(7.07105681270762,-3.5003885604986,13.2257823355905));
#20415=CARTESIAN_POINT('Ctrl Pts',(2.93245799361878,-4.09465249784007,13.4242984530022));
#20416=CARTESIAN_POINT('Ctrl Pts',(0.189519561683291,-0.939111566208993,
13.6228145704138));
#20417=CARTESIAN_POINT('Ctrl Pts',(1.35417235664619,3.07644987396012,13.8213306878255));
#20418=CARTESIAN_POINT('Ctrl Pts',(5.3598495029257,4.27465703983832,14.0198468052371));
#20419=CARTESIAN_POINT('Ctrl Pts',(8.53822806601778,1.55821460123144,14.2183629226488));
#20420=CARTESIAN_POINT('Ctrl Pts',(7.97860941701375,-2.58521112879858,14.4168790400604));
#20421=CARTESIAN_POINT('Ctrl Pts',(4.19348166959603,-4.36114968300486,14.6153951574721));
#20422=CARTESIAN_POINT('Ctrl Pts',(0.649192814085452,-2.14323031537866,
14.8139112748837));
#20423=CARTESIAN_POINT('Ctrl Pts',(0.59153516483578,2.03741860650786,15.0124273922954));
#20424=CARTESIAN_POINT('Ctrl Pts',(4.07331050026509,4.35223832436584,15.2109435097071));
#20425=CARTESIAN_POINT('Ctrl Pts',(7.9059751985768,2.68136097312093,15.4094596271187));
#20426=CARTESIAN_POINT('Ctrl Pts',(8.57964783407003,-1.44505575241412,15.6079757445304));
#20427=CARTESIAN_POINT('Ctrl Pts',(5.47739182177246,-4.24811790776339,15.806491861942));
#20428=CARTESIAN_POINT('Ctrl Pts',(1.44019420657955,-3.16083449095397,16.0050079793537));
#20429=CARTESIAN_POINT('Ctrl Pts',(0.165243768843413,0.821081027223728,
16.2035240967653));
#20430=CARTESIAN_POINT('Ctrl Pts',(2.82011586731386,4.05106615928717,16.402040214177));
#20431=CARTESIAN_POINT('Ctrl Pts',(6.97352913523386,3.57116196212476,16.6005563315886));
#20432=CARTESIAN_POINT('Ctrl Pts',(8.82186670813997,-0.17914442924803,16.7990724490003));
#20433=CARTESIAN_POINT('Ctrl Pts',(6.67245619587356,-3.76539376000376,16.997588566412));
#20434=CARTESIAN_POINT('Ctrl Pts',(2.49368685944485,-3.90336711073225,17.1961046838236));
#20435=CARTESIAN_POINT('Ctrl Pts',(0.112396168534027,-0.466711111367439,
17.3946208012353));
#20436=CARTESIAN_POINT('Ctrl Pts',(1.70932484092508,3.39735004600064,17.5931369186469));
#20437=CARTESIAN_POINT('Ctrl Pts',(5.82203597524696,4.15018265569229,17.7916530360586));
#20438=CARTESIAN_POINT('Ctrl Pts',(8.68418694674809,1.10235693414467,17.9901691534703));
#20439=CARTESIAN_POINT('Ctrl Pts',(7.67467433961344,-2.9549862986379,18.1886852708819));
#20440=CARTESIAN_POINT('Ctrl Pts',(3.71799059648846,-4.30620928893205,18.3872013882936));
#20441=CARTESIAN_POINT('Ctrl Pts',(0.437591425226463,-1.7138877251997,18.5857175057052));
#20442=CARTESIAN_POINT('Ctrl Pts',(0.837603987051035,2.44797961565228,18.7842336231169));
#20443=CARTESIAN_POINT('Ctrl Pts',(4.55170438690705,4.36803379003202,18.9827497405285));
#20444=CARTESIAN_POINT('Ctrl Pts',(8.17859012825258,2.28792570825151,19.1812658579402));
#20445=CARTESIAN_POINT('Ctrl Pts',(8.39682823991214,-1.88742121606535,19.3797819753518));
#20446=CARTESIAN_POINT('Ctrl Pts',(5.0065604104293,-4.33430369349561,19.5782980927635));
#20447=CARTESIAN_POINT('Ctrl Pts',(1.11252942855707,-2.81191329518458,19.7768142101752));
#20448=CARTESIAN_POINT('Ctrl Pts',(0.280814794700937,1.28557380975688,19.9753303275868));
#20449=CARTESIAN_POINT('Ctrl Pts',(3.27308495055695,4.20575687553525,20.1738464449984));
#20450=CARTESIAN_POINT('Ctrl Pts',(7.34907580467911,3.27438779359847,20.3723625624101));
#20451=CARTESIAN_POINT('Ctrl Pts',(8.77607246974106,-0.65560333835151,20.5708786798217));
#20452=CARTESIAN_POINT('Ctrl Pts',(6.24725853788356,-3.98520541525919,20.7693947972334));
#20453=CARTESIAN_POINT('Ctrl Pts',(2.07847371693811,-3.66523215780504,20.9679109146451));
#20454=CARTESIAN_POINT('Ctrl Pts',(0.0874118238771355,0.0112909480203034,
21.1664270320568));
#20455=CARTESIAN_POINT('Ctrl Pts',(2.09744951113826,3.6774740982752,21.3649431494684));
#20456=CARTESIAN_POINT('Ctrl Pts',(6.26783241381338,3.97589626917586,21.56345926688));
#20457=CARTESIAN_POINT('Ctrl Pts',(8.77940336342984,0.633268559987037,21.7619753842917));
#20458=CARTESIAN_POINT('Ctrl Pts',(7.33211314362288,-3.28929501353682,21.9604915017033));
#20459=CARTESIAN_POINT('Ctrl Pts',(3.25136321302202,-4.1995837027451,22.159007619115));
#20460=CARTESIAN_POINT('Ctrl Pts',(0.274225572405194,-1.26397559254583,
22.3575237365266));
#20461=CARTESIAN_POINT('Ctrl Pts',(1.12710846943813,2.82916129353447,22.5560398539383));
#20462=CARTESIAN_POINT('Ctrl Pts',(5.0289536987851,4.33139846700858,22.75455597135));
#20463=CARTESIAN_POINT('Ctrl Pts',(8.40653381239982,1.86703792222437,22.9530720887616));
#20464=CARTESIAN_POINT('Ctrl Pts',(8.1667094807393,-2.30714844669435,23.1515882061733));
#20465=CARTESIAN_POINT('Ctrl Pts',(4.52913739170739,-4.36843844023836,23.3501043235849));
#20466=CARTESIAN_POINT('Ctrl Pts',(0.824979095953012,-2.42929861537115,
23.5486204409966));
#20467=CARTESIAN_POINT('Ctrl Pts',(0.44654309475883,1.73474421227166,23.7471365584082));
#20468=CARTESIAN_POINT('Ctrl Pts',(3.74018140704413,4.30976245591016,23.9456526758199));
#20469=CARTESIAN_POINT('Ctrl Pts',(7.69005018696339,2.93870878051704,24.1441687932315));
#20470=CARTESIAN_POINT('Ctrl Pts',(8.67815324699032,-1.12495244308866,24.3426849106432));
#20471=CARTESIAN_POINT('Ctrl Pts',(5.80110407974766,-4.15572474791461,24.5412010280549));
#20472=CARTESIAN_POINT('Ctrl Pts',(1.69076667459873,-3.38595255220879,24.7397171454665));
#20473=CARTESIAN_POINT('Ctrl Pts',(0.116906044416222,0.495033780363739,
24.9382332628782));
#20474=CARTESIAN_POINT('Ctrl Pts',(1.71188963858453,2.76408782845127,25.0705773411526));
#20475=CARTESIAN_POINT('Ctrl Pts',(2.81308617627174,3.31070484176046,25.1367493802898));
#20476=CARTESIAN_POINT('Ctrl Pts',(2.45096789438968,-2.81528236653118,-0.135126215077433));
#20477=CARTESIAN_POINT('Ctrl Pts',(1.5138871719268,-2.14781538060387,-0.0689100650381678));
#20478=CARTESIAN_POINT('Ctrl Pts',(0.375608982507884,0.184245982096433,
0.0634781241383155));
#20479=CARTESIAN_POINT('Ctrl Pts',(2.40361795610193,3.53582435220265,0.262038352452016));
#20480=CARTESIAN_POINT('Ctrl Pts',(6.31301191404873,3.63844533219021,0.460554469863673));
#20481=CARTESIAN_POINT('Ctrl Pts',(8.52123531017291,0.41411968753004,0.659070587275328));
#20482=CARTESIAN_POINT('Ctrl Pts',(7.00753704968407,-3.19206842901602,0.857586704686986));
#20483=CARTESIAN_POINT('Ctrl Pts',(3.15735122024546,-3.87365781783563,1.05610282209864));
#20484=CARTESIAN_POINT('Ctrl Pts',(0.497012637108953,-1.00853559461836,
1.25461893951029));
#20485=CARTESIAN_POINT('Ctrl Pts',(1.46259607175817,2.78055482024318,1.45313505692195));
#20486=CARTESIAN_POINT('Ctrl Pts',(5.16994949606116,4.02307283767128,1.6516511743336));
#20487=CARTESIAN_POINT('Ctrl Pts',(8.22389132840824,1.58143801444312,1.85016729174526));
#20488=CARTESIAN_POINT('Ctrl Pts',(7.82770989036406,-2.30850019028058,2.04868340915692));
#20489=CARTESIAN_POINT('Ctrl Pts',(4.34420487984554,-4.08433044095169,2.24719952656857));
#20490=CARTESIAN_POINT('Ctrl Pts',(0.963512123078899,-2.11982284980964,
2.44571564398023));
#20491=CARTESIAN_POINT('Ctrl Pts',(0.781601462709117,1.78598563226962,2.64423176139188));
#20492=CARTESIAN_POINT('Ctrl Pts',(3.96506545115642,4.05621856135326,2.84274787880354));
#20493=CARTESIAN_POINT('Ctrl Pts',(7.59854716087849,2.61184571475234,3.0412639962152));
#20494=CARTESIAN_POINT('Ctrl Pts',(8.35457376462735,-1.22440681097471,3.23978011362686));
#20495=CARTESIAN_POINT('Ctrl Pts',(5.54079016364776,-3.93937031917242,3.43829623103851));
#20496=CARTESIAN_POINT('Ctrl Pts',(1.7340060207583,-3.04673371102089,3.63681234845017));
#20497=CARTESIAN_POINT('Ctrl Pts',(0.420401755326215,0.636043824414959,
3.83532846586182));
#20498=CARTESIAN_POINT('Ctrl Pts',(2.8029512110655,3.73634444619894,4.03384458327349));
#20499=CARTESIAN_POINT('Ctrl Pts',(6.6997608939274,3.41497193768155,4.23236070068513));
#20500=CARTESIAN_POINT('Ctrl Pts',(8.54220663371807,-0.0337669329441494,
4.4308768180968));
#20501=CARTESIAN_POINT('Ctrl Pts',(6.64301166261426,-3.45158267762228,4.62939293550844));
#20502=CARTESIAN_POINT('Ctrl Pts',(2.74142261194879,-3.70850466797209,4.82790905292011));
#20503=CARTESIAN_POINT('Ctrl Pts',(0.410440516499291,-0.569248623621048,
5.02642517033176));
#20504=CARTESIAN_POINT('Ctrl Pts',(1.78473444019877,3.09131448041513,5.22494128774342));
#20505=CARTESIAN_POINT('Ctrl Pts',(5.60575214909559,3.92091058714242,5.42345740515506));
#20506=CARTESIAN_POINT('Ctrl Pts',(8.37427830909092,1.15981136136555,5.62197352256674));
#20507=CARTESIAN_POINT('Ctrl Pts',(7.55494932568486,-2.66342104697584,5.82048963997839));
#20508=CARTESIAN_POINT('Ctrl Pts',(3.89809109665752,-4.04754312425325,6.01900575739004));
#20509=CARTESIAN_POINT('Ctrl Pts',(0.752584827297987,-1.72500220071308,
6.21752187480171));
#20510=CARTESIAN_POINT('Ctrl Pts',(0.999025325230166,2.17726292518741,6.41603799221334));
#20511=CARTESIAN_POINT('Ctrl Pts',(4.41172707023364,4.08563208015006,6.61455410962502));
#20512=CARTESIAN_POINT('Ctrl Pts',(7.86540272070975,2.25245709306557,6.81307022703666));
#20513=CARTESIAN_POINT('Ctrl Pts',(8.1972418118268,-1.64347525356681,7.01158634444832));
#20514=CARTESIAN_POINT('Ctrl Pts',(5.10335241618994,-4.03434422519923,7.21010246185998));
#20515=CARTESIAN_POINT('Ctrl Pts',(1.4170595903061,-2.73063749675737,7.40861857927163));
#20516=CARTESIAN_POINT('Ctrl Pts',(0.514200183395272,1.07373510898141,7.60713469668328));
#20517=CARTESIAN_POINT('Ctrl Pts',(3.22159566609925,3.89480152652282,7.80565081409495));
#20518=CARTESIAN_POINT('Ctrl Pts',(7.05986475548066,3.14908279305528,8.0041669315066));
#20519=CARTESIAN_POINT('Ctrl Pts',(8.51399363110384,-0.480506060385796,
8.20268304891826));
#20520=CARTESIAN_POINT('Ctrl Pts',(6.25231872913724,-3.67005660392007,8.40119916632992));
#20521=CARTESIAN_POINT('Ctrl Pts',(2.34603890318347,-3.49863912146337,8.59971528374156));
#20522=CARTESIAN_POINT('Ctrl Pts',(0.372450912529775,-0.123234482743352,
8.79823140115322));
#20523=CARTESIAN_POINT('Ctrl Pts',(2.13892909739252,3.36502595110463,8.99674751856487));
#20524=CARTESIAN_POINT('Ctrl Pts',(6.02776633805246,3.77165962851178,9.19526363597655));
#20525=CARTESIAN_POINT('Ctrl Pts',(8.47763946304124,0.72427916270141,9.39377975338818));
#20526=CARTESIAN_POINT('Ctrl Pts',(7.24500126602242,-2.98638238306039,9.59229587079984));
#20527=CARTESIAN_POINT('Ctrl Pts',(3.45867836056103,-3.9621717494319,9.79081198821151));
#20528=CARTESIAN_POINT('Ctrl Pts',(0.586113239980029,-1.30947959617202,
9.98932810562315));
#20529=CARTESIAN_POINT('Ctrl Pts',(1.25794639972494,2.54240906231909,10.1878442230349));
#20530=CARTESIAN_POINT('Ctrl Pts',(4.85892581172318,4.06600786328675,10.3863603404465));
#20531=CARTESIAN_POINT('Ctrl Pts',(8.09134302835829,1.86603400672705,10.5848764578582));
#20532=CARTESIAN_POINT('Ctrl Pts',(7.99501184973105,-2.04281829746266,10.7833925752698));
#20533=CARTESIAN_POINT('Ctrl Pts',(4.658150536815,-4.08089646336047,10.9819086926815));
#20534=CARTESIAN_POINT('Ctrl Pts',(1.13659320614603,-2.38176727499459,11.1804248100931));
#20535=CARTESIAN_POINT('Ctrl Pts',(0.655315074027438,1.49853907779376,11.3789409275048));
#20536=CARTESIAN_POINT('Ctrl Pts',(3.6550614989726,4.00651184837438,11.5774570449165));
#20537=CARTESIAN_POINT('Ctrl Pts',(7.38872176624422,2.84539728015019,11.7759731623281));
#20538=CARTESIAN_POINT('Ctrl Pts',(8.43708082482397,-0.921477992040132,
11.9744892797398));
#20539=CARTESIAN_POINT('Ctrl Pts',(5.84007139076835,-3.84448124749012,12.1730053971514));
#20540=CARTESIAN_POINT('Ctrl Pts',(1.97598530342792,-3.24678170627628,12.3715215145631));
#20541=CARTESIAN_POINT('Ctrl Pts',(0.383479098877827,0.324258761208613,
12.5700376319747));
#20542=CARTESIAN_POINT('Ctrl Pts',(2.52093966656498,3.59834922323431,12.7685537493864));
#20543=CARTESIAN_POINT('Ctrl Pts',(6.43092127741269,3.5771399144821,12.967069866798));
#20544=CARTESIAN_POINT('Ctrl Pts',(8.53273714794332,0.280053916463419,13.1655859842097));
#20545=CARTESIAN_POINT('Ctrl Pts',(6.90158428470204,-3.27350013106212,13.3641021016213));
#20546=CARTESIAN_POINT('Ctrl Pts',(3.0312414520278,-3.82924502713605,13.562618219033));
#20547=CARTESIAN_POINT('Ctrl Pts',(0.466094994356506,-0.878240167322765,
13.7611343364446));
#20548=CARTESIAN_POINT('Ctrl Pts',(1.55525724336407,2.87704033182534,13.9596504538563));
#20549=CARTESIAN_POINT('Ctrl Pts',(5.30129412947213,3.99758202219787,14.1581665712679));
#20550=CARTESIAN_POINT('Ctrl Pts',(8.27365632956023,1.45721413871475,14.3566826886797));
#20551=CARTESIAN_POINT('Ctrl Pts',(7.75031108111198,-2.41764273385123,14.5551988060912));
#20552=CARTESIAN_POINT('Ctrl Pts',(4.21052800757405,-4.07846837919741,14.753714923503));
#20553=CARTESIAN_POINT('Ctrl Pts',(0.895973113878727,-2.00431026356939,
14.9522310409146));
#20554=CARTESIAN_POINT('Ctrl Pts',(0.842052722152676,1.9053570654116,15.1507471583263));
#20555=CARTESIAN_POINT('Ctrl Pts',(4.09814610146403,4.07013463762311,15.3492632757379));
#20556=CARTESIAN_POINT('Ctrl Pts',(7.682384872503,2.50756033086961,15.5477793931496));
#20557=CARTESIAN_POINT('Ctrl Pts',(8.31239134820293,-1.35139002803904,15.7462955105612));
#20558=CARTESIAN_POINT('Ctrl Pts',(5.41121758211169,-3.97276310543362,15.9448116279729));
#20559=CARTESIAN_POINT('Ctrl Pts',(1.63570332303896,-2.95595530083938,16.1433277453845));
#20560=CARTESIAN_POINT('Ctrl Pts',(0.443392711547191,0.767860140031627,
16.3418438627962));
#20561=CARTESIAN_POINT('Ctrl Pts',(2.92618112548781,3.7884838709103,16.5403599802078));
#20562=CARTESIAN_POINT('Ctrl Pts',(6.8103781630174,3.33968613741389,16.7388760976195));
#20563=CARTESIAN_POINT('Ctrl Pts',(8.5389100624284,-0.167532633159739,16.9373922150311));
#20564=CARTESIAN_POINT('Ctrl Pts',(6.52882019040339,-3.5213282050942,17.1359083324428));
#20565=CARTESIAN_POINT('Ctrl Pts',(2.62091061577914,-3.65035838956845,17.3344244498544));
#20566=CARTESIAN_POINT('Ctrl Pts',(0.393970590674286,-0.43645979805503,
17.5329405672661));
#20567=CARTESIAN_POINT('Ctrl Pts',(1.88738942918871,3.17714037417117,17.7314566846778));
#20568=CARTESIAN_POINT('Ctrl Pts',(5.73352256684974,3.8811758273502,17.9299728020894));
#20569=CARTESIAN_POINT('Ctrl Pts',(8.41015443739666,1.03090428563328,18.1284889195011));
#20570=CARTESIAN_POINT('Ctrl Pts',(7.46607648872073,-2.76344979098553,18.3270050369127));
#20571=CARTESIAN_POINT('Ctrl Pts',(3.76585734795025,-4.02708911541293,18.5255211543244));
#20572=CARTESIAN_POINT('Ctrl Pts',(0.698087318576006,-1.60279683129456,
18.724037271736));
#20573=CARTESIAN_POINT('Ctrl Pts',(1.07217183831651,2.28930630247911,18.9225533891477));
#20574=CARTESIAN_POINT('Ctrl Pts',(4.54553141985243,4.08490627169594,19.1210695065593));
#20575=CARTESIAN_POINT('Ctrl Pts',(7.93732942868568,2.13962678039228,19.319585623971));
#20576=CARTESIAN_POINT('Ctrl Pts',(8.14142176722837,-1.76508221626667,19.5181017413827));
#20577=CARTESIAN_POINT('Ctrl Pts',(4.97090455397163,-4.05336249490537,19.7166178587943));
#20578=CARTESIAN_POINT('Ctrl Pts',(1.3292771434127,-2.62965050343175,19.915133976206));
#20579=CARTESIAN_POINT('Ctrl Pts',(0.551472646603815,1.20224539704524,20.1136500936177));
#20580=CARTESIAN_POINT('Ctrl Pts',(3.3497896271543,3.93314783354192,20.3121662110293));
#20581=CARTESIAN_POINT('Ctrl Pts',(7.16158262229433,3.06214829760668,20.510682328441));
#20582=CARTESIAN_POINT('Ctrl Pts',(8.49608411816253,-0.613108395518473,
20.7091984458526));
#20583=CARTESIAN_POINT('Ctrl Pts',(6.13118302381429,-3.72689209317441,20.9077145632643));
#20584=CARTESIAN_POINT('Ctrl Pts',(2.23261078765349,-3.42765888460072,21.1062306806759));
#20585=CARTESIAN_POINT('Ctrl Pts',(0.370605683008962,0.0105590905653954,
21.3047467980876));
#20586=CARTESIAN_POINT('Ctrl Pts',(2.250356607504,3.43910732612115,21.5032629154992));
#20587=CARTESIAN_POINT('Ctrl Pts',(6.15042334082164,3.71818634797007,21.7017790329109));
#20588=CARTESIAN_POINT('Ctrl Pts',(8.49919910975228,0.592221314373082,21.9002951503225));
#20589=CARTESIAN_POINT('Ctrl Pts',(7.14571944818345,-3.07608926032515,22.0988112677342));
#20590=CARTESIAN_POINT('Ctrl Pts',(3.32947585071529,-3.92737479389549,22.2973273851459));
#20591=CARTESIAN_POINT('Ctrl Pts',(0.545310524977601,-1.18204713458114,
22.4958435025575));
#20592=CARTESIAN_POINT('Ctrl Pts',(1.34291119900688,2.64578051982372,22.6943596199692));
#20593=CARTESIAN_POINT('Ctrl Pts',(4.99184635260365,4.05064557959106,22.8928757373808));
#20594=CARTESIAN_POINT('Ctrl Pts',(8.15049824324278,1.74602012818506,23.0913918547925));
#20595=CARTESIAN_POINT('Ctrl Pts',(7.92621886181009,-2.15760353803636,23.2899079722041));
#20596=CARTESIAN_POINT('Ctrl Pts',(4.52442717371885,-4.08528469325705,23.4884240896158));
#20597=CARTESIAN_POINT('Ctrl Pts',(1.06036526828869,-2.27183616857484,23.6869402070274));
#20598=CARTESIAN_POINT('Ctrl Pts',(0.706458758169362,1.62230144113535,23.8854563244391));
#20599=CARTESIAN_POINT('Ctrl Pts',(3.78660979300229,4.03041197296648,24.0839724418507));
#20600=CARTESIAN_POINT('Ctrl Pts',(7.48045570332662,2.74822735016753,24.2824885592624));
#20601=CARTESIAN_POINT('Ctrl Pts',(8.40451183040988,-1.05203519730533,24.481004676674));
#20602=CARTESIAN_POINT('Ctrl Pts',(5.71394743641032,-3.88635869185298,24.6795207940858));
#20603=CARTESIAN_POINT('Ctrl Pts',(1.87003416737941,-3.16648164392546,24.8780369114974));
#20604=CARTESIAN_POINT('Ctrl Pts',(0.398188145107553,0.462946646320358,
25.076553028909));
#20605=CARTESIAN_POINT('Ctrl Pts',(1.88978798161488,2.58492499113116,25.2088971071835));
#20606=CARTESIAN_POINT('Ctrl Pts',(2.91960708544911,3.09611134481228,25.2750691463207));
#20607=CARTESIAN_POINT('Ctrl Pts',(2.58997049159961,-2.62015330925654,0.00319355095334283));
#20608=CARTESIAN_POINT('Ctrl Pts',(1.71783944528228,-1.99894889552244,0.0694097009926075));
#20609=CARTESIAN_POINT('Ctrl Pts',(0.65845605968771,0.171475772890977,0.20179789016909));
#20610=CARTESIAN_POINT('Ctrl Pts',(2.5459024084217,3.29075405988094,0.400358118482792));
#20611=CARTESIAN_POINT('Ctrl Pts',(6.18433372098768,3.38626231280436,0.598874235894448));
#20612=CARTESIAN_POINT('Ctrl Pts',(8.23950371306965,0.385416781850904,0.797390353306103));
#20613=CARTESIAN_POINT('Ctrl Pts',(6.83072086642306,-2.97082408396747,0.995906470717762));
#20614=CARTESIAN_POINT('Ctrl Pts',(3.24739392835603,-3.60517206763711,1.19442258812942));
#20615=CARTESIAN_POINT('Ctrl Pts',(0.771445147794971,-0.938633334672633,
1.39293870554108));
#20616=CARTESIAN_POINT('Ctrl Pts',(1.6701033647243,2.58783275185508,1.59145482295273));
#20617=CARTESIAN_POINT('Ctrl Pts',(5.12049770482736,3.74423103498232,1.78997094036439));
#20618=CARTESIAN_POINT('Ctrl Pts',(7.96276883664299,1.47182751406662,1.98848705777604));
#20619=CARTESIAN_POINT('Ctrl Pts',(7.59404699250464,-2.14849653622342,2.1870031751877));
#20620=CARTESIAN_POINT('Ctrl Pts',(4.35198598660702,-3.80124283382013,2.38551929259936));
#20621=CARTESIAN_POINT('Ctrl Pts',(1.20561125008781,-1.97289654529749,2.58403541001101));
#20622=CARTESIAN_POINT('Ctrl Pts',(1.0363089362513,1.66219780307218,2.78255152742267));
#20623=CARTESIAN_POINT('Ctrl Pts',(3.99912495903867,3.77507940693446,2.98106764483432));
#20624=CARTESIAN_POINT('Ctrl Pts',(7.38076768128599,2.43081698451723,3.17958376224598));
#20625=CARTESIAN_POINT('Ctrl Pts',(8.08439358796167,-1.13954237620741,3.37809987965763));
#20626=CARTESIAN_POINT('Ctrl Pts',(5.4656351638386,-3.66632999264102,3.5766159970693));
#20627=CARTESIAN_POINT('Ctrl Pts',(1.92270171311447,-2.83556261008053,3.77513211448094));
#20628=CARTESIAN_POINT('Ctrl Pts',(0.700144216203009,0.591959212043988,
3.97364823189261));
#20629=CARTESIAN_POINT('Ctrl Pts',(2.91755761499276,3.47737597536012,4.17216434930425));
#20630=CARTESIAN_POINT('Ctrl Pts',(6.54427687678886,3.1782780050441,4.37068046671592));
#20631=CARTESIAN_POINT('Ctrl Pts',(8.2590215005,-0.0314265247951463,4.56919658412757));
#20632=CARTESIAN_POINT('Ctrl Pts',(6.49146097171637,-3.21235123071783,4.76771270153922));
#20633=CARTESIAN_POINT('Ctrl Pts',(2.86029360321679,-3.45146579032245,4.96622881895089));
#20634=CARTESIAN_POINT('Ctrl Pts',(0.690873397337037,-0.529793630188544,
5.16474493636253));
#20635=CARTESIAN_POINT('Ctrl Pts',(1.96991411271267,2.8770534572674,5.36326105377419));
#20636=CARTESIAN_POINT('Ctrl Pts',(5.52609459169944,3.64914971667956,5.56177717118585));
#20637=CARTESIAN_POINT('Ctrl Pts',(8.1027323975949,1.07942407934716,5.7602932885975));
#20638=CARTESIAN_POINT('Ctrl Pts',(7.34019164048911,-2.47881759682101,5.95880940600916));
#20639=CARTESIAN_POINT('Ctrl Pts',(3.93679264073839,-3.76700527003896,6.15732552342081));
#20640=CARTESIAN_POINT('Ctrl Pts',(1.00930346276847,-1.60544117293717,6.35584164083248));
#20641=CARTESIAN_POINT('Ctrl Pts',(1.23866300903221,2.02635541158186,6.55435775824412));
#20642=CARTESIAN_POINT('Ctrl Pts',(4.41482816993367,3.80245425555658,6.75287387565579));
#20643=CARTESIAN_POINT('Ctrl Pts',(7.6291273081915,2.09633782263408,6.95138999306744));
#20644=CARTESIAN_POINT('Ctrl Pts',(7.93796641543966,-1.5295649116789,7.14990611047909));
#20645=CARTESIAN_POINT('Ctrl Pts',(5.05851651200422,-3.75472119528823,7.34842222789076));
#20646=CARTESIAN_POINT('Ctrl Pts',(1.62772304650576,-2.54137523062185,7.5469383453024));
#20647=CARTESIAN_POINT('Ctrl Pts',(0.787441414036509,0.999313828164636,
7.74545446271406));
#20648=CARTESIAN_POINT('Ctrl Pts',(3.30718554976015,3.62485029208286,7.94397058012572));
#20649=CARTESIAN_POINT('Ctrl Pts',(6.8794217047968,2.93081781047529,8.14248669753737));
#20650=CARTESIAN_POINT('Ctrl Pts',(8.23276395950072,-0.447201871899268,
8.34100281494903));
#20651=CARTESIAN_POINT('Ctrl Pts',(6.12784722031342,-3.41568258667014,8.53951893236069));
#20652=CARTESIAN_POINT('Ctrl Pts',(2.49231419722064,-3.25614616174064,8.73803504977233));
#20653=CARTESIAN_POINT('Ctrl Pts',(0.655516877599837,-0.114693020356707,
8.93655116718401));
#20654=CARTESIAN_POINT('Ctrl Pts',(2.29955930716991,3.13179380737736,9.13506728459565));
#20655=CARTESIAN_POINT('Ctrl Pts',(5.9188587019336,3.51024343935022,9.33358340200731));
#20656=CARTESIAN_POINT('Ctrl Pts',(8.19892952254092,0.674078901476532,9.53209951941897));
#20657=CARTESIAN_POINT('Ctrl Pts',(7.05172628302556,-2.77939427202906,9.73061563683061));
#20658=CARTESIAN_POINT('Ctrl Pts',(3.52783588801619,-3.68755104089551,9.92913175424228));
#20659=CARTESIAN_POINT('Ctrl Pts',(0.854370129759403,-1.21871871116838,
10.1276478716539));
#20660=CARTESIAN_POINT('Ctrl Pts',(1.47963809495571,2.36619303175871,10.3261639890656));
#20661=CARTESIAN_POINT('Ctrl Pts',(4.83103127493619,3.78419020596524,10.5246801064772));
#20662=CARTESIAN_POINT('Ctrl Pts',(7.83940754573271,1.73669797247918,10.7231962238889));
#20663=CARTESIAN_POINT('Ctrl Pts',(7.74975314393437,-1.90122922870495,10.9217123413006));
#20664=CARTESIAN_POINT('Ctrl Pts',(4.64417186530054,-3.79804686745578,11.1202284587122));
#20665=CARTESIAN_POINT('Ctrl Pts',(1.36669597038421,-2.21668543150265,11.3187445761239));
#20666=CARTESIAN_POINT('Ctrl Pts',(0.91877553954763,1.39467435679268,11.5172606935355));
#20667=CARTESIAN_POINT('Ctrl Pts',(3.71060758300086,3.72881789865659,11.7157768109472));
#20668=CARTESIAN_POINT('Ctrl Pts',(7.18548542162604,2.64818093856821,11.9142929283589));
#20669=CARTESIAN_POINT('Ctrl Pts',(8.16118202999545,-0.857609751318129,
12.1128090457705));
#20670=CARTESIAN_POINT('Ctrl Pts',(5.74417301388192,-3.57801774441457,12.3113251631822));
#20671=CARTESIAN_POINT('Ctrl Pts',(2.14790925385559,-3.02174514829049,12.5098412805938));
#20672=CARTESIAN_POINT('Ctrl Pts',(0.665780693158256,0.301784174950485,
12.7083573980055));
#20673=CARTESIAN_POINT('Ctrl Pts',(2.65509247460188,3.34894529131551,12.9068735154171));
#20674=CARTESIAN_POINT('Ctrl Pts',(6.29407070946287,3.32920601358802,13.1053896328288));
#20675=CARTESIAN_POINT('Ctrl Pts',(8.25020835096136,0.260643196829997,13.3039057502404));
#20676=CARTESIAN_POINT('Ctrl Pts',(6.7321117566965,-3.04661170162563,13.5024218676521));
#20677=CARTESIAN_POINT('Ctrl Pts',(3.1300249104368,-3.56383755643203,13.7009379850637));
#20678=CARTESIAN_POINT('Ctrl Pts',(0.742670427029733,-0.817368768436538,
13.8994541024754));
#20679=CARTESIAN_POINT('Ctrl Pts',(1.75634213008195,2.67763078969056,14.0979702198871));
#20680=CARTESIAN_POINT('Ctrl Pts',(5.24273875601857,3.7205070045574,14.2964863372987));
#20681=CARTESIAN_POINT('Ctrl Pts',(8.0090845931027,1.35621367619806,14.4950024547104));
#20682=CARTESIAN_POINT('Ctrl Pts',(7.52201274521021,-2.25007433890389,14.693518572122));
#20683=CARTESIAN_POINT('Ctrl Pts',(4.22757434555207,-3.79578707538995,14.8920346895337));
#20684=CARTESIAN_POINT('Ctrl Pts',(1.14275341367199,-1.86539021176013,15.0905508069453));
#20685=CARTESIAN_POINT('Ctrl Pts',(1.09257027946957,1.77329552431533,15.289066924357));
#20686=CARTESIAN_POINT('Ctrl Pts',(4.12298170266298,3.78803095088039,15.4875830417686));
#20687=CARTESIAN_POINT('Ctrl Pts',(7.45879454642923,2.3337596886183,15.6860991591803));
#20688=CARTESIAN_POINT('Ctrl Pts',(8.04513486233581,-1.25772430366396,15.8846152765919));
#20689=CARTESIAN_POINT('Ctrl Pts',(5.34504334245093,-3.69740830310385,16.0831313940036));
#20690=CARTESIAN_POINT('Ctrl Pts',(1.83121243949837,-2.75107611072479,16.2816475114153));
#20691=CARTESIAN_POINT('Ctrl Pts',(0.721541654250978,0.714639252839528,
16.4801636288269));
#20692=CARTESIAN_POINT('Ctrl Pts',(3.03224638366176,3.52590158253341,16.6786797462386));
#20693=CARTESIAN_POINT('Ctrl Pts',(6.64722719080097,3.10821031270302,16.8771958636502));
#20694=CARTESIAN_POINT('Ctrl Pts',(8.25595341671681,-0.155920837071448,
17.0757119810619));
#20695=CARTESIAN_POINT('Ctrl Pts',(6.38518418493321,-3.27726265018464,17.2742280984735));
#20696=CARTESIAN_POINT('Ctrl Pts',(2.74813437211341,-3.39734966840464,17.4727442158852));
#20697=CARTESIAN_POINT('Ctrl Pts',(0.675545012814546,-0.406208484742623,
17.6712603332969));
#20698=CARTESIAN_POINT('Ctrl Pts',(2.06545401745235,2.9569307023417,17.8697764507085));
#20699=CARTESIAN_POINT('Ctrl Pts',(5.64500915845253,3.61216899900811,18.0682925681202));
#20700=CARTESIAN_POINT('Ctrl Pts',(8.13612192804524,0.959451637121888,18.2668086855318));
#20701=CARTESIAN_POINT('Ctrl Pts',(7.25747863782803,-2.57191328333314,18.4653248029435));
#20702=CARTESIAN_POINT('Ctrl Pts',(3.81372409941205,-3.74796894189382,18.6638409203551));
#20703=CARTESIAN_POINT('Ctrl Pts',(0.958583211925542,-1.49170593738941,
18.8623570377668));
#20704=CARTESIAN_POINT('Ctrl Pts',(1.306739689582,2.13063298930591,19.0608731551785));
#20705=CARTESIAN_POINT('Ctrl Pts',(4.53935845279781,3.80177875335989,19.2593892725901));
#20706=CARTESIAN_POINT('Ctrl Pts',(7.69606872911877,1.99132785253305,19.4579053900018));
#20707=CARTESIAN_POINT('Ctrl Pts',(7.88601529454458,-1.64274321646801,19.6564215074134));
#20708=CARTESIAN_POINT('Ctrl Pts',(4.93524869751396,-3.77242129631514,19.8549376248251));
#20709=CARTESIAN_POINT('Ctrl Pts',(1.54602485826833,-2.44738771167893,20.0534537422367));
#20710=CARTESIAN_POINT('Ctrl Pts',(0.822130498506685,1.11891698433359,20.2519698596484));
#20711=CARTESIAN_POINT('Ctrl Pts',(3.42649430375165,3.66053879154859,20.45048597706));
#20712=CARTESIAN_POINT('Ctrl Pts',(6.97408943990954,2.84990880161489,20.6490020944717));
#20713=CARTESIAN_POINT('Ctrl Pts',(8.21609576658401,-0.570613452685432,
20.8475182118833));
#20714=CARTESIAN_POINT('Ctrl Pts',(6.015107509745,-3.46857877108964,21.046034329295));
#20715=CARTESIAN_POINT('Ctrl Pts',(2.38674785836889,-3.19008561139642,21.2445504467067));
#20716=CARTESIAN_POINT('Ctrl Pts',(0.653799542140776,0.00982723311048271,
21.4430665641183));
#20717=CARTESIAN_POINT('Ctrl Pts',(2.40326370386975,3.2007405539671,21.64158268153));
#20718=CARTESIAN_POINT('Ctrl Pts',(6.03301426782987,3.46047642676426,21.8400987989417));
#20719=CARTESIAN_POINT('Ctrl Pts',(8.21899485607472,0.551174068759129,22.0386149163533));
#20720=CARTESIAN_POINT('Ctrl Pts',(6.95932575274402,-2.86288350711349,22.2371310337649));
#20721=CARTESIAN_POINT('Ctrl Pts',(3.40758848840856,-3.65516588504588,22.4356471511766));
#20722=CARTESIAN_POINT('Ctrl Pts',(0.816395477550012,-1.10011867661645,
22.6341632685882));
#20723=CARTESIAN_POINT('Ctrl Pts',(1.55871392857562,2.46239974611297,22.8326793859999));
#20724=CARTESIAN_POINT('Ctrl Pts',(4.95473900642221,3.76989269217354,23.0311955034116));
#20725=CARTESIAN_POINT('Ctrl Pts',(7.89446267408575,1.62500233414576,23.2297116208232));
#20726=CARTESIAN_POINT('Ctrl Pts',(7.68572824288089,-2.00805862937836,23.4282277382349));
#20727=CARTESIAN_POINT('Ctrl Pts',(4.5197169557303,-3.80213094627573,23.6267438556465));
#20728=CARTESIAN_POINT('Ctrl Pts',(1.29575144062437,-2.11437372177854,23.8252599730582));
#20729=CARTESIAN_POINT('Ctrl Pts',(0.966374421579891,1.50985866999905,24.0237760904698));
#20730=CARTESIAN_POINT('Ctrl Pts',(3.83303817896047,3.7510614900228,24.2222922078815));
#20731=CARTESIAN_POINT('Ctrl Pts',(7.27086121968984,2.55774591981802,24.4208083252931));
#20732=CARTESIAN_POINT('Ctrl Pts',(8.13087041382945,-0.979117951521988,
24.6193244427048));
#20733=CARTESIAN_POINT('Ctrl Pts',(5.62679079307294,-3.61699263579137,24.8178405601165));
#20734=CARTESIAN_POINT('Ctrl Pts',(2.04930166016011,-2.94701073564213,25.0163566775281));
#20735=CARTESIAN_POINT('Ctrl Pts',(0.679470245798868,0.430859512276974,
25.2148727949398));
#20736=CARTESIAN_POINT('Ctrl Pts',(2.06768632464525,2.40576215381105,25.3472168732142));
#20737=CARTESIAN_POINT('Ctrl Pts',(3.02612799462649,2.8815178478641,25.4133889123514));
#20738=CARTESIAN_POINT('Ctrl Pts',(6.37917532696298,2.58637165759475,1.87594439571473));
#20739=CARTESIAN_POINT('Ctrl Pts',(6.35746818924401,2.60250872304869,1.87431323785475));
#20740=CARTESIAN_POINT('Ctrl Pts',(6.33555795831466,2.6183724646154,1.87269246732624));
#20741=CARTESIAN_POINT('Ctrl Pts',(6.19727492500446,2.71586407695624,1.86261629455797));
#20742=CARTESIAN_POINT('Ctrl Pts',(6.07580181006572,2.78999834520196,1.85444429514));
#20743=CARTESIAN_POINT('Ctrl Pts',(5.74237257220235,2.96434989857594,1.83317918573207));
#20744=CARTESIAN_POINT('Ctrl Pts',(5.523745245102,3.0498889011599,1.82041424434255));
#20745=CARTESIAN_POINT('Ctrl Pts',(5.23269930128191,3.12859918522094,1.80289072059331));
#20746=CARTESIAN_POINT('Ctrl Pts',(5.167062952266,3.14415666864464,1.79890198363588));
#20747=CARTESIAN_POINT('Ctrl Pts',(5.08538680607657,3.16082801904366,1.79383948934339));
#20748=CARTESIAN_POINT('Ctrl Pts',(5.06975831167358,3.16389752770189,1.79286635151808));
#20749=CARTESIAN_POINT('Ctrl Pts',(5.04516765851111,3.16853820472167,1.79132728319329));
#20750=CARTESIAN_POINT('Ctrl Pts',(5.0362202642569,3.17018752288347,1.79076565250961));
#20751=CARTESIAN_POINT('Ctrl Pts',(5.01960989374187,3.17317672567073,1.78971978245498));
#20752=CARTESIAN_POINT('Ctrl Pts',(5.01194893954713,3.17452677246842,1.78923612092467));
#20753=CARTESIAN_POINT('Ctrl Pts',(4.99426044855479,3.17757792655571,1.78811645356316));
#20754=CARTESIAN_POINT('Ctrl Pts',(4.9842297177955,3.17925930642477,1.78747936020121));
#20755=CARTESIAN_POINT('Ctrl Pts',(4.9528608055175,3.18436491139823,1.78548061603729));
#20756=CARTESIAN_POINT('Ctrl Pts',(4.93149653332297,3.18762191813225,1.7841101395166));
#20757=CARTESIAN_POINT('Ctrl Pts',(4.72526985244489,3.21694220194011,1.77080296572706));
#20758=CARTESIAN_POINT('Ctrl Pts',(4.53852237901646,3.22710773378337,1.75816929017416));
#20759=CARTESIAN_POINT('Ctrl Pts',(4.10975007637841,3.21319690026204,1.7291489467187));
#20760=CARTESIAN_POINT('Ctrl Pts',(3.86914891378651,3.17804088866835,1.71290336056405));
#20761=CARTESIAN_POINT('Ctrl Pts',(3.5992748360651,3.10687629774973,1.69520021938423));
#20762=CARTESIAN_POINT('Ctrl Pts',(3.56397672532074,3.09692103132523,1.69289331884349));
#20763=CARTESIAN_POINT('Ctrl Pts',(3.51146701374181,3.08113911750864,1.6894733305407));
#20764=CARTESIAN_POINT('Ctrl Pts',(3.49412320794559,3.07576618258719,1.68834564908029));
#20765=CARTESIAN_POINT('Ctrl Pts',(3.46423894478094,3.06623081615572,1.68640569433679));
#20766=CARTESIAN_POINT('Ctrl Pts',(3.45167711255051,3.06213735305142,1.68559118674377));
#20767=CARTESIAN_POINT('Ctrl Pts',(3.42566014199035,3.05348199253439,1.68390608985396));
#20768=CARTESIAN_POINT('Ctrl Pts',(3.4122092627877,3.04890813063507,1.68303591541222));
#20769=CARTESIAN_POINT('Ctrl Pts',(3.38062402109995,3.03793428309482,1.68099477896871));
#20770=CARTESIAN_POINT('Ctrl Pts',(3.36251570080964,3.03146059304165,1.67982628100462));
#20771=CARTESIAN_POINT('Ctrl Pts',(3.30280125605346,3.00950803713889,1.67597781096476));
#20772=CARTESIAN_POINT('Ctrl Pts',(3.2614559128536,2.99333123621255,1.67332102454893));
#20773=CARTESIAN_POINT('Ctrl Pts',(3.16372568218563,2.95274540414727,1.66704977644844));
#20774=CARTESIAN_POINT('Ctrl Pts',(3.1076779331469,2.9275679335125,1.66346049577536));
#20775=CARTESIAN_POINT('Ctrl Pts',(2.88871690118901,2.8215833150003,1.6494082159528));
#20776=CARTESIAN_POINT('Ctrl Pts',(2.73204847362243,2.72865485571952,1.63930708277088));
#20777=CARTESIAN_POINT('Ctrl Pts',(2.55338966493566,2.60111995887127,1.62701924739219));
#20778=CARTESIAN_POINT('Ctrl Pts',(2.52311833550173,2.57869950653125,1.62490735852054));
#20779=CARTESIAN_POINT('Ctrl Pts',(2.37642094346987,2.46601278327509,1.61449188041826));
#20780=CARTESIAN_POINT('Ctrl Pts',(2.2658994828539,2.36837774636692,1.606077629023));
#20781=CARTESIAN_POINT('Ctrl Pts',(2.14940807192336,2.25031822012699,1.59603999818292));
#20782=CARTESIAN_POINT('Ctrl Pts',(2.13647444372387,2.23698176940727,1.59490784905773));
#20783=CARTESIAN_POINT('Ctrl Pts',(2.11697321907695,2.21652214215941,1.59317222555267));
#20784=CARTESIAN_POINT('Ctrl Pts',(2.11032100024688,2.20947968349679,1.59257501882737));
#20785=CARTESIAN_POINT('Ctrl Pts',(2.09836047923665,2.19670260377342,1.59149166433327));
#20786=CARTESIAN_POINT('Ctrl Pts',(2.0930411741091,2.19097855606262,1.59100636978853));
#20787=CARTESIAN_POINT('Ctrl Pts',(2.0813054934234,2.17825744587329,1.58992790874209));
#20788=CARTESIAN_POINT('Ctrl Pts',(2.07489927521574,2.17125144160783,1.58933402028445));
#20789=CARTESIAN_POINT('Ctrl Pts',(2.05626385387461,2.15068956984932,1.58759147284775));
#20790=CARTESIAN_POINT('Ctrl Pts',(2.04411900823446,2.13705822286543,1.58643683323208));
#20791=CARTESIAN_POINT('Ctrl Pts',(1.93717851777626,2.01495528921416,1.57610498041153));
#20792=CARTESIAN_POINT('Ctrl Pts',(1.84964933744078,1.9003555296462,1.56649003599813));
#20793=CARTESIAN_POINT('Ctrl Pts',(1.64333323951227,1.58903548256601,1.54129901712155));
#20794=CARTESIAN_POINT('Ctrl Pts',(1.53735010744345,1.3847512085533,1.52568539709475));
#20795=CARTESIAN_POINT('Ctrl Pts',(1.42252413795245,1.09031305146266,1.50512106213752));
#20796=CARTESIAN_POINT('Ctrl Pts',(1.3943430716333,1.00845973638979,1.49958705881355));
#20797=CARTESIAN_POINT('Ctrl Pts',(1.36216740356011,0.901146159759775,1.49256202096957));
#20798=CARTESIAN_POINT('Ctrl Pts',(1.35513586551897,0.876641100171909,1.49097297731463));
#20799=CARTESIAN_POINT('Ctrl Pts',(1.34430274319641,0.837124689555323,1.48843416917684));
#20800=CARTESIAN_POINT('Ctrl Pts',(1.34031739319521,0.822165270353613,1.48747847875109));
#20801=CARTESIAN_POINT('Ctrl Pts',(1.33292886436729,0.793605969097431,1.48566403734921));
#20802=CARTESIAN_POINT('Ctrl Pts',(1.32950634031576,0.780011504483906,1.48480467920146));
#20803=CARTESIAN_POINT('Ctrl Pts',(1.32187804752054,0.748854177816674,1.48284479383397));
#20804=CARTESIAN_POINT('Ctrl Pts',(1.31773095647574,0.731277329663039,1.4817461756327));
#20805=CARTESIAN_POINT('Ctrl Pts',(1.30532273452457,0.676635847758998,1.47835191741383));
#20806=CARTESIAN_POINT('Ctrl Pts',(1.29756859784815,0.639458589344792,1.47607247493859));
#20807=CARTESIAN_POINT('Ctrl Pts',(1.26262802264064,0.455747884216578,1.46494311038925));
#20808=CARTESIAN_POINT('Ctrl Pts',(1.24496967374256,0.307580423469625,1.45639721513811));
#20809=CARTESIAN_POINT('Ctrl Pts',(1.228689965464,-0.0225959984325165,1.43775141445356));
#20810=CARTESIAN_POINT('Ctrl Pts',(1.23508488552788,-0.204323671620051,
1.42775637084742));
#20811=CARTESIAN_POINT('Ctrl Pts',(1.26964919262474,-0.491930673826586,
1.41125360369806));
#20812=CARTESIAN_POINT('Ctrl Pts',(1.28795231687946,-0.598592794204186,
1.40497435296812));
#20813=CARTESIAN_POINT('Ctrl Pts',(1.31516393348759,-0.720130921935759,
1.39743113501213));
#20814=CARTESIAN_POINT('Ctrl Pts',(1.31887059945707,-0.736112978916704,
1.39643135237084));
#20815=CARTESIAN_POINT('Ctrl Pts',(1.32505288367227,-0.761873837776047,
1.39480609843874));
#20816=CARTESIAN_POINT('Ctrl Pts',(1.32745272187494,-0.771670761154133,
1.39418478697599));
#20817=CARTESIAN_POINT('Ctrl Pts',(1.33179830248319,-0.789057233235905,
1.39307615832644));
#20818=CARTESIAN_POINT('Ctrl Pts',(1.33372577905735,-0.796651153117467,
1.39258989111248));
#20819=CARTESIAN_POINT('Ctrl Pts',(1.3379691473637,-0.813117238728657,1.39153099155264));
#20820=CARTESIAN_POINT('Ctrl Pts',(1.34029518146952,-0.821986437301457,
1.39095780468898));
#20821=CARTESIAN_POINT('Ctrl Pts',(1.34696417809225,-0.846980241954366,
1.38933479019491));
#20822=CARTESIAN_POINT('Ctrl Pts',(1.35139459402551,-0.863080919834322,
1.38828014641097));
#20823=CARTESIAN_POINT('Ctrl Pts',(1.3806601377049,-0.966292876861225,1.38146396062797));
#20824=CARTESIAN_POINT('Ctrl Pts',(1.40903139841715,-1.05235117592572,1.37552680524109));
#20825=CARTESIAN_POINT('Ctrl Pts',(1.55285099075795,-1.43375016951215,1.34839112790262));
#20826=CARTESIAN_POINT('Ctrl Pts',(1.70791862549142,-1.71236053840431,1.32651796330595));
#20827=CARTESIAN_POINT('Ctrl Pts',(1.93875599357569,-2.0127194568175,1.30217189147774));
#20828=CARTESIAN_POINT('Ctrl Pts',(1.97772359589434,-2.06051946385817,1.29826144142414));
#20829=CARTESIAN_POINT('Ctrl Pts',(2.03276832942079,-2.12421737454299,1.2929971592978));
#20830=CARTESIAN_POINT('Ctrl Pts',(2.04767430295176,-2.14110544973065,1.2915960762896));
#20831=CARTESIAN_POINT('Ctrl Pts',(2.07170644705166,-2.16776458536358,1.28937529364269));
#20832=CARTESIAN_POINT('Ctrl Pts',(2.0807182656183,-2.17763729534634,1.28855084484696));
#20833=CARTESIAN_POINT('Ctrl Pts',(2.09937550282305,-2.19782317023249,1.28686083992946));
#20834=CARTESIAN_POINT('Ctrl Pts',(2.10902781081721,-2.20812959706504,1.28599560298287));
#20835=CARTESIAN_POINT('Ctrl Pts',(2.13160406142546,-2.23192045627524,1.28399259870112));
#20836=CARTESIAN_POINT('Ctrl Pts',(2.1445781918029,-2.24535672493916,1.28285702623467));
#20837=CARTESIAN_POINT('Ctrl Pts',(2.1865695153516,-2.2880939385146,1.27923022181115));
#20838=CARTESIAN_POINT('Ctrl Pts',(2.21603323590006,-2.31695174039986,1.2767585685141));
#20839=CARTESIAN_POINT('Ctrl Pts',(2.2866523443305,-2.38351143551458,1.27099548261519));
#20840=CARTESIAN_POINT('Ctrl Pts',(2.32824969105022,-2.42072595863082,1.26772391419552));
#20841=CARTESIAN_POINT('Ctrl Pts',(2.48777406272148,-2.55615014524893,1.25558771499452));
#20842=CARTESIAN_POINT('Ctrl Pts',(2.61170280612446,-2.64698047305603,1.24697883892509));
#20843=CARTESIAN_POINT('Ctrl Pts',(2.92130934367302,-2.84155495632107,1.22652503606375));
#20844=CARTESIAN_POINT('Ctrl Pts',(3.11167151330051,-2.93643403866995,1.2147599773957));
#20845=CARTESIAN_POINT('Ctrl Pts',(3.33383261748784,-3.0210028651444,1.20048981068735));
#20846=CARTESIAN_POINT('Ctrl Pts',(3.35782913388204,-3.02981205948318,1.19894138686802));
#20847=CARTESIAN_POINT('Ctrl Pts',(3.39146274851147,-3.04170697527912,1.19675797779796));
#20848=CARTESIAN_POINT('Ctrl Pts',(3.40101413325445,-3.04503442659141,1.1961364589124));
#20849=CARTESIAN_POINT('Ctrl Pts',(3.41753881168727,-3.05070410195038,1.19505839356474));
#20850=CARTESIAN_POINT('Ctrl Pts',(3.42450481962554,-3.05306753662489,1.19460308113107));
#20851=CARTESIAN_POINT('Ctrl Pts',(3.43923812089619,-3.05801008306017,1.19363816397147));
#20852=CARTESIAN_POINT('Ctrl Pts',(3.44700724208598,-3.06058348793223,1.1931282219223));
#20853=CARTESIAN_POINT('Ctrl Pts',(3.46626875112046,-3.0668822562555,1.19186132029033));
#20854=CARTESIAN_POINT('Ctrl Pts',(3.47777234525126,-3.07057261047674,1.19110237139053));
#20855=CARTESIAN_POINT('Ctrl Pts',(3.52089764103687,-3.08414025181291,1.1882492520801));
#20856=CARTESIAN_POINT('Ctrl Pts',(3.55264909981536,-3.09359406787166,1.18613271570161));
#20857=CARTESIAN_POINT('Ctrl Pts',(3.79219819575261,-3.1609159816438,1.17007447922355));
#20858=CARTESIAN_POINT('Ctrl Pts',(4.00517766215825,-3.19827627834922,1.15533189525162));
#20859=CARTESIAN_POINT('Ctrl Pts',(4.43164769923035,-3.22961612740667,1.12650926895391));
#20860=CARTESIAN_POINT('Ctrl Pts',(4.64406716370717,-3.22426313447634,1.1124984498106));
#20861=CARTESIAN_POINT('Ctrl Pts',(4.88162605466237,-3.1947001219446,1.09742658096952));
#20862=CARTESIAN_POINT('Ctrl Pts',(4.90875424646882,-3.19097250473502,1.0957134719679));
#20863=CARTESIAN_POINT('Ctrl Pts',(4.95316394790896,-3.18429253967359,1.09292162964129));
#20864=CARTESIAN_POINT('Ctrl Pts',(4.97047428364735,-3.18154419125974,1.09183654739639));
#20865=CARTESIAN_POINT('Ctrl Pts',(5.00157511752,-3.17634587892235,1.08989243172842));
#20866=CARTESIAN_POINT('Ctrl Pts',(5.01537359201356,-3.1739469894221,1.08903181033593));
#20867=CARTESIAN_POINT('Ctrl Pts',(5.04479344599701,-3.16863449006096,1.08720079935052));
#20868=CARTESIAN_POINT('Ctrl Pts',(5.06040984258929,-3.16569513084344,1.0862312494149));
#20869=CARTESIAN_POINT('Ctrl Pts',(5.10270101251687,-3.15741064192127,1.08361164102233));
#20870=CARTESIAN_POINT('Ctrl Pts',(5.12933124873605,-3.1518429917002,1.08196866779826));
#20871=CARTESIAN_POINT('Ctrl Pts',(5.27356128668659,-3.11977711706809,1.07310139700947));
#20872=CARTESIAN_POINT('Ctrl Pts',(5.38968115929224,-3.0870323695469,1.06608013217971));
#20873=CARTESIAN_POINT('Ctrl Pts',(5.65510267094297,-2.99583426138442,1.05004550725694));
#20874=CARTESIAN_POINT('Ctrl Pts',(5.80241925226489,-2.93260388026925,1.041161498306));
#20875=CARTESIAN_POINT('Ctrl Pts',(6.08861324843494,-2.78363882719303,1.02308286470513));
#20876=CARTESIAN_POINT('Ctrl Pts',(6.22689818369351,-2.6977968469199,1.01390732908834));
#20877=CARTESIAN_POINT('Ctrl Pts',(6.36514710073905,-2.59675606037843,1.00364239908801));
#20878=CARTESIAN_POINT('Ctrl Pts',(6.37217184219401,-2.59157804146046,1.00311764554919));
#20879=CARTESIAN_POINT('Ctrl Pts',(6.37917532113595,-2.58637166192656,1.00259120688551));
#20880=CARTESIAN_POINT('Origin',(4.45646910621825,-5.13094777615093E-16,
-2.31077344927308));
#20881=CARTESIAN_POINT('Ctrl Pts',(7.67921910621823,3.83865910396161E-12,
6.06327685380577));
#20882=CARTESIAN_POINT('Ctrl Pts',(7.67921910621823,-0.00048391001007088,
6.0633051914467));
#20883=CARTESIAN_POINT('Ctrl Pts',(7.67921899722642,-0.000967821022726189,
6.06333352625195));
#20884=CARTESIAN_POINT('Ctrl Pts',(7.67917212283792,-0.105025812727111,
6.06942589124854));
#20885=CARTESIAN_POINT('Ctrl Pts',(7.67413246795198,-0.208542640984706,
6.07535155547207));
#20886=CARTESIAN_POINT('Ctrl Pts',(7.6420606122514,-0.53864869853577,6.0940950333389));
#20887=CARTESIAN_POINT('Ctrl Pts',(7.59597263080692,-0.762652150599657,
6.10654628211578));
#20888=CARTESIAN_POINT('Ctrl Pts',(7.50452302104189,-1.04917758523805,6.12397306485735));
#20889=CARTESIAN_POINT('Ctrl Pts',(7.48007404257778,-1.11768409440402,6.12826318255371));
#20890=CARTESIAN_POINT('Ctrl Pts',(7.44734176898383,-1.20044303755238,6.13366533835845));
#20891=CARTESIAN_POINT('Ctrl Pts',(7.44123764555465,-1.21554083125573,6.13465998003665));
#20892=CARTESIAN_POINT('Ctrl Pts',(7.43151441581216,-1.23907515062649,6.13622569490362));
#20893=CARTESIAN_POINT('Ctrl Pts',(7.42797314456913,-1.24754381414792,6.13679222042822));
#20894=CARTESIAN_POINT('Ctrl Pts',(7.42134030134804,-1.26321725180863,6.13784671089852));
#20895=CARTESIAN_POINT('Ctrl Pts',(7.418258575943,-1.27042597643201,6.13833408409028));
#20896=CARTESIAN_POINT('Ctrl Pts',(7.41115147309215,-1.28688438983048,6.13945223440697));
#20897=CARTESIAN_POINT('Ctrl Pts',(7.40710896466478,-1.2961264371954,6.14008402990406));
#20898=CARTESIAN_POINT('Ctrl Pts',(7.39443896504767,-1.32472632376073,6.14205094914058));
#20899=CARTESIAN_POINT('Ctrl Pts',(7.38566406168201,-1.34401770140436,6.14339452255131));
#20900=CARTESIAN_POINT('Ctrl Pts',(7.36467059356333,-1.38898898006688,6.14656381318704));
#20901=CARTESIAN_POINT('Ctrl Pts',(7.35230125483227,-1.41459617142862,6.14839718205939));
#20902=CARTESIAN_POINT('Ctrl Pts',(7.30719450615279,-1.50490537025683,6.15495711142845));
#20903=CARTESIAN_POINT('Ctrl Pts',(7.27261568508749,-1.56865949614297,6.15976135032848));
#20904=CARTESIAN_POINT('Ctrl Pts',(7.12164691893672,-1.82590134792096,6.17972206872809));
#20905=CARTESIAN_POINT('Ctrl Pts',(6.98721705230608,-2.00808803086824,6.19518778811049));
#20906=CARTESIAN_POINT('Ctrl Pts',(6.75183087139285,-2.26551680985559,6.21822014147556));
#20907=CARTESIAN_POINT('Ctrl Pts',(6.66367696821127,-2.35148714728407,6.22617234436212));
#20908=CARTESIAN_POINT('Ctrl Pts',(6.54964168690211,-2.4506189052801,6.23567053376896));
#20909=CARTESIAN_POINT('Ctrl Pts',(6.52823096756206,-2.46874610708932,6.23742248033569));
#20910=CARTESIAN_POINT('Ctrl Pts',(6.4940749899517,-2.49690663367201,6.24016903431721));
#20911=CARTESIAN_POINT('Ctrl Pts',(6.48148639754896,-2.507126933339,6.24117120223013));
#20912=CARTESIAN_POINT('Ctrl Pts',(6.45793522237783,-2.52595431079032,6.24302762824544));
#20913=CARTESIAN_POINT('Ctrl Pts',(6.44699295654035,-2.53458608164944,6.24388286388316));
#20914=CARTESIAN_POINT('Ctrl Pts',(6.42258759473381,-2.55358264332563,6.24577445636262));
#20915=CARTESIAN_POINT('Ctrl Pts',(6.40909777412277,-2.56391254329682,6.24680941752754));
#20916=CARTESIAN_POINT('Ctrl Pts',(6.36956542925041,-2.59369166525061,6.24981224504217));
#20917=CARTESIAN_POINT('Ctrl Pts',(6.34330912780274,-2.61285453949499,6.25176895903279));
#20918=CARTESIAN_POINT('Ctrl Pts',(6.14135721329509,-2.75561489916029,6.26654725313689));
#20919=CARTESIAN_POINT('Ctrl Pts',(5.95398379213897,-2.86176990562278,6.27866555039204));
#20920=CARTESIAN_POINT('Ctrl Pts',(5.55480133951951,-3.03789896576558,6.30307629519336));
#20921=CARTESIAN_POINT('Ctrl Pts',(5.34353643083463,-3.10616287874828,6.31531225761337));
#20922=CARTESIAN_POINT('Ctrl Pts',(5.10247529037649,-3.15743902642924,6.33011485045602));
#20923=CARTESIAN_POINT('Ctrl Pts',(5.07791181453018,-3.16236526487034,6.33163298382564));
#20924=CARTESIAN_POINT('Ctrl Pts',(5.04344952868219,-3.16885971715975,6.33377973801735));
#20925=CARTESIAN_POINT('Ctrl Pts',(5.03359634140045,-3.17066902587303,6.33439543971008));
#20926=CARTESIAN_POINT('Ctrl Pts',(5.01652521384103,-3.17372153193903,6.33546574139845));
#20927=CARTESIAN_POINT('Ctrl Pts',(5.00931110832481,-3.17498612975827,6.33591914227367));
#20928=CARTESIAN_POINT('Ctrl Pts',(4.99403824453613,-3.17760975813833,6.33688147732505));
#20929=CARTESIAN_POINT('Ctrl Pts',(4.98597854839038,-3.17896273960086,6.33739075875426));
#20930=CARTESIAN_POINT('Ctrl Pts',(4.96593639299222,-3.18224888470069,6.33866063549258));
#20931=CARTESIAN_POINT('Ctrl Pts',(4.95394808649034,-3.18414502396257,6.33942326867859));
#20932=CARTESIAN_POINT('Ctrl Pts',(4.90858324209756,-3.19105774535772,6.34231993218461));
#20933=CARTESIAN_POINT('Ctrl Pts',(4.87514060294697,-3.1956174197338,6.3444773701454));
#20934=CARTESIAN_POINT('Ctrl Pts',(4.61679406892825,-3.22671645238553,6.36128190363622));
#20935=CARTESIAN_POINT('Ctrl Pts',(4.38974140785457,-3.23000631896306,6.37680654875705));
#20936=CARTESIAN_POINT('Ctrl Pts',(3.96306792445177,-3.19115583727224,6.40566043609402));
#20937=CARTESIAN_POINT('Ctrl Pts',(3.76404202147251,-3.15396430240958,6.41898504479793));
#20938=CARTESIAN_POINT('Ctrl Pts',(3.54333496219127,-3.09080251638247,6.43344076151387));
#20939=CARTESIAN_POINT('Ctrl Pts',(3.51698756567261,-3.08289614982321,6.43516189075864));
#20940=CARTESIAN_POINT('Ctrl Pts',(3.47400786217016,-3.06939655237306,6.43796267066151));
#20941=CARTESIAN_POINT('Ctrl Pts',(3.45731471581481,-3.06400323358153,6.43904877947599));
#20942=CARTESIAN_POINT('Ctrl Pts',(3.42740300860117,-3.05406873616739,6.44099211392599));
#20943=CARTESIAN_POINT('Ctrl Pts',(3.41416847913398,-3.04957739548305,6.44185095169711));
#20944=CARTESIAN_POINT('Ctrl Pts',(3.38602443490044,-3.03982166532786,6.44367537458319));
#20945=CARTESIAN_POINT('Ctrl Pts',(3.37112356007344,-3.03453334315993,6.444640142819));
#20946=CARTESIAN_POINT('Ctrl Pts',(3.33092762369611,-3.01993384604648,6.44723985898657));
#20947=CARTESIAN_POINT('Ctrl Pts',(3.30570912542883,-3.0104145224515,6.44886786799746));
#20948=CARTESIAN_POINT('Ctrl Pts',(3.17146179822789,-2.95780614947448,6.45752254277157));
#20949=CARTESIAN_POINT('Ctrl Pts',(3.06471944041703,-2.9091060889055,6.46435756795522));
#20950=CARTESIAN_POINT('Ctrl Pts',(2.72914040728542,-2.73329193187802,6.48602695836141));
#20951=CARTESIAN_POINT('Ctrl Pts',(2.51308613861894,-2.58414291635044,6.50019868504366));
#20952=CARTESIAN_POINT('Ctrl Pts',(2.25718995935007,-2.35706983832039,6.51993688335784));
#20953=CARTESIAN_POINT('Ctrl Pts',(2.19896642337351,-2.30136619188119,6.52467172541004));
#20954=CARTESIAN_POINT('Ctrl Pts',(2.13225542105464,-2.23257293778352,6.53048479666582));
#20955=CARTESIAN_POINT('Ctrl Pts',(2.12169345093999,-2.22152510575018,6.53141735004696));
#20956=CARTESIAN_POINT('Ctrl Pts',(2.10452060179721,-2.20330454949227,6.53295457936054));
#20957=CARTESIAN_POINT('Ctrl Pts',(2.09786286312856,-2.19617606068154,6.53355580269414));
#20958=CARTESIAN_POINT('Ctrl Pts',(2.08592575774298,-2.18327802957213,6.53464353069165));
#20959=CARTESIAN_POINT('Ctrl Pts',(2.08063491888513,-2.17751937604288,6.5351291513768));
#20960=CARTESIAN_POINT('Ctrl Pts',(2.06900036266882,-2.16476321240039,6.53620484790273));
#20961=CARTESIAN_POINT('Ctrl Pts',(2.06266650265164,-2.15775713577978,6.53679561897515));
#20962=CARTESIAN_POINT('Ctrl Pts',(2.0443570680093,-2.13732467387981,6.53851817240934));
#20963=CARTESIAN_POINT('Ctrl Pts',(2.03246323693386,-2.12382597158592,6.53965572054656));
#20964=CARTESIAN_POINT('Ctrl Pts',(1.93565313950459,-2.0120804306145,6.54906375533661));
#20965=CARTESIAN_POINT('Ctrl Pts',(1.85664191543028,-1.90889283098158,6.55769123920622));
#20966=CARTESIAN_POINT('Ctrl Pts',(1.736910980754,-1.7312547884216,6.57210469166792));
#20967=CARTESIAN_POINT('Ctrl Pts',(1.69251077168293,-1.65944979631447,6.57782411451159));
#20968=CARTESIAN_POINT('Ctrl Pts',(1.54304557124267,-1.39505717242105,6.59835573859026));
#20969=CARTESIAN_POINT('Ctrl Pts',(1.45486622860033,-1.19357949543755,6.61298151427723));
#20970=CARTESIAN_POINT('Ctrl Pts',(1.37527813759098,-0.945551733204921,
6.62951403655511));
#20971=CARTESIAN_POINT('Ctrl Pts',(1.36347279275977,-0.906189781824136,
6.63209784173914));
#20972=CARTESIAN_POINT('Ctrl Pts',(1.34783704252929,-0.850185332091116,
6.6357194738507));
#20973=CARTESIAN_POINT('Ctrl Pts',(1.34338149796027,-0.833722956106937,
6.63677744223327));
#20974=CARTESIAN_POINT('Ctrl Pts',(1.33544736261817,-0.803457179499849,
6.63871063620847));
#20975=CARTESIAN_POINT('Ctrl Pts',(1.33192916534085,-0.789664695627758,
6.63958712275707));
#20976=CARTESIAN_POINT('Ctrl Pts',(1.32496729119795,-0.761596726930881,
6.64136184929989));
#20977=CARTESIAN_POINT('Ctrl Pts',(1.32152957394385,-0.747320100192161,
6.64225987914947));
#20978=CARTESIAN_POINT('Ctrl Pts',(1.31324314928973,-0.71184343214003,6.64448012396627));
#20979=CARTESIAN_POINT('Ctrl Pts',(1.30851117399277,-0.690616667015534,
6.64579857679885));
#20980=CARTESIAN_POINT('Ctrl Pts',(1.29130212692048,-0.609565443974385,
6.65079649226544));
#20981=CARTESIAN_POINT('Ctrl Pts',(1.2803121998971,-0.5494361356831,6.6544287047478));
#20982=CARTESIAN_POINT('Ctrl Pts',(1.25666904613559,-0.395429219256831,
6.66357084345649));
#20983=CARTESIAN_POINT('Ctrl Pts',(1.24643143758259,-0.301238787317273,
6.66901024966007));
#20984=CARTESIAN_POINT('Ctrl Pts',(1.22734227865672,-0.00426545225531576,
6.68588826779925));
#20985=CARTESIAN_POINT('Ctrl Pts',(1.23347572235375,0.198964642573343,6.69701909323654));
#20986=CARTESIAN_POINT('Ctrl Pts',(1.27219007398472,0.508263194311666,6.71477367561345));
#20987=CARTESIAN_POINT('Ctrl Pts',(1.29116959723874,0.615498497740809,6.72109074916244));
#20988=CARTESIAN_POINT('Ctrl Pts',(1.31921439696282,0.737577580902475,6.72867676931241));
#20989=CARTESIAN_POINT('Ctrl Pts',(1.32301741193638,0.753570336787383,6.72967849198895));
#20990=CARTESIAN_POINT('Ctrl Pts',(1.32935456798888,0.779342201713178,6.73130659389982));
#20991=CARTESIAN_POINT('Ctrl Pts',(1.33181268463803,0.789139938940349,6.73192879913158));
#20992=CARTESIAN_POINT('Ctrl Pts',(1.33626062447373,0.806522211024997,6.73303869694113));
#20993=CARTESIAN_POINT('Ctrl Pts',(1.33823211598968,0.814111243840464,6.73352533516172));
#20994=CARTESIAN_POINT('Ctrl Pts',(1.34256923735789,0.830559599938853,6.7345846092151));
#20995=CARTESIAN_POINT('Ctrl Pts',(1.34494495003538,0.839415905811248,6.73515779651135));
#20996=CARTESIAN_POINT('Ctrl Pts',(1.35175218751673,0.864366286028786,6.73678039073974));
#20997=CARTESIAN_POINT('Ctrl Pts',(1.35627093558577,0.880435969673518,6.73783460678149));
#20998=CARTESIAN_POINT('Ctrl Pts',(1.38605859410388,0.983294283141381,6.74463806126317));
#20999=CARTESIAN_POINT('Ctrl Pts',(1.41484249897827,1.06901487743942,6.75056208505726));
#21000=CARTESIAN_POINT('Ctrl Pts',(1.55987773123022,1.44741827309273,6.77753644088705));
#21001=CARTESIAN_POINT('Ctrl Pts',(1.7150857816945,1.72341145887595,6.79925596028994));
#21002=CARTESIAN_POINT('Ctrl Pts',(1.94648340785078,2.02239198160467,6.8235721235801));
#21003=CARTESIAN_POINT('Ctrl Pts',(1.98655474625124,2.07114014083156,6.82757537441182));
#21004=CARTESIAN_POINT('Ctrl Pts',(2.04297015749069,2.13580349802398,6.83294236377303));
#21005=CARTESIAN_POINT('Ctrl Pts',(2.05808749469571,2.15276553429368,6.83435579152175));
#21006=CARTESIAN_POINT('Ctrl Pts',(2.08240483731782,2.17947608280492,6.83659095860736));
#21007=CARTESIAN_POINT('Ctrl Pts',(2.09148824224688,2.18932927402222,6.83741756374947));
#21008=CARTESIAN_POINT('Ctrl Pts',(2.11025205306525,2.20943020098751,6.8391083058317));
#21009=CARTESIAN_POINT('Ctrl Pts',(2.11993877638182,2.21967166519366,6.83997214643809));
#21010=CARTESIAN_POINT('Ctrl Pts',(2.14252430470529,2.24323894260994,6.84196579892815));
#21011=CARTESIAN_POINT('Ctrl Pts',(2.15547164098749,2.25651771217994,6.84309347633249));
#21012=CARTESIAN_POINT('Ctrl Pts',(2.19707849418902,2.29845914963459,6.84667009963196));
#21013=CARTESIAN_POINT('Ctrl Pts',(2.22616510067534,2.32669393436031,6.84910021628417));
#21014=CARTESIAN_POINT('Ctrl Pts',(2.37995258298452,2.47044292114875,6.86160707766282));
#21015=CARTESIAN_POINT('Ctrl Pts',(2.5131216818637,2.57651303344542,6.8712818694728));
#21016=CARTESIAN_POINT('Ctrl Pts',(2.80579920626594,2.7739710629407,6.8911046832726));
#21017=CARTESIAN_POINT('Ctrl Pts',(2.96598484811098,2.86322817316442,6.90119741872582));
#21018=CARTESIAN_POINT('Ctrl Pts',(3.2091159361733,2.97274634008944,6.91655768780906));
#21019=CARTESIAN_POINT('Ctrl Pts',(3.28666395546687,3.00410787524317,6.92146593760884));
#21020=CARTESIAN_POINT('Ctrl Pts',(3.37986208188416,3.03764270456729,6.92747303888818));
#21021=CARTESIAN_POINT('Ctrl Pts',(3.39442509162186,3.04276492273715,6.92841478148956));
#21022=CARTESIAN_POINT('Ctrl Pts',(3.41829259973379,3.05096757722417,6.92996410491451));
#21023=CARTESIAN_POINT('Ctrl Pts',(3.42757552968203,3.05411061000787,6.93056814075081));
#21024=CARTESIAN_POINT('Ctrl Pts',(3.44429280328874,3.05968591186089,6.93165876948676));
#21025=CARTESIAN_POINT('Ctrl Pts',(3.45172182527721,3.06213351216891,6.93214445540951));
#21026=CARTESIAN_POINT('Ctrl Pts',(3.46810220147073,3.06746423938798,6.93321763363964));
#21027=CARTESIAN_POINT('Ctrl Pts',(3.47705717809547,3.07033520451832,6.93380580015834));
#21028=CARTESIAN_POINT('Ctrl Pts',(3.50299491118559,3.07852582193736,6.93551338886795));
#21029=CARTESIAN_POINT('Ctrl Pts',(3.52000901854027,3.08374394975419,6.93663842849694));
#21030=CARTESIAN_POINT('Ctrl Pts',(3.65388356231925,3.12359242690812,6.94552457751159));
#21031=CARTESIAN_POINT('Ctrl Pts',(3.77256848842467,3.15170535204232,6.9536009996361));
#21032=CARTESIAN_POINT('Ctrl Pts',(4.18426144440299,3.22487313080894,6.98168831383066));
#21033=CARTESIAN_POINT('Ctrl Pts',(4.48180789192737,3.23625183704567,7.00194454721374));
#21034=CARTESIAN_POINT('Ctrl Pts',(4.82841564804777,3.20163563062986,7.02420773547078));
#21035=CARTESIAN_POINT('Ctrl Pts',(4.87996476967972,3.19522563637173,7.02748949797031));
#21036=CARTESIAN_POINT('Ctrl Pts',(4.95214865905335,3.18447201250545,7.0320459773337));
#21037=CARTESIAN_POINT('Ctrl Pts',(4.97292789936862,3.18116811347642,7.03335309257909));
#21038=CARTESIAN_POINT('Ctrl Pts',(5.00657720365832,3.17547947603045,7.03546278416509));
#21039=CARTESIAN_POINT('Ctrl Pts',(5.01946745099429,3.17321945244702,7.03626928258139));
#21040=CARTESIAN_POINT('Ctrl Pts',(5.04640746463992,3.16832678368415,7.03795145636326));
#21041=CARTESIAN_POINT('Ctrl Pts',(5.06045422799504,3.1656790516403,7.03882663290923));
#21042=CARTESIAN_POINT('Ctrl Pts',(5.09386663125879,3.15915052245924,7.04090402060115));
#21043=CARTESIAN_POINT('Ctrl Pts',(5.11321526932264,3.15518496011883,7.04210350827674));
#21044=CARTESIAN_POINT('Ctrl Pts',(5.17899647375546,3.14107157214969,7.04617059025611));
#21045=CARTESIAN_POINT('Ctrl Pts',(5.22524181443309,3.13007432695933,7.04901111606527));
#21046=CARTESIAN_POINT('Ctrl Pts',(5.48754043585247,3.0615347494652,7.06504521513984));
#21047=CARTESIAN_POINT('Ctrl Pts',(5.69738702954598,2.98265627126743,7.07751761116157));
#21048=CARTESIAN_POINT('Ctrl Pts',(6.06522639528866,2.7987895192076,7.10051571123984));
#21049=CARTESIAN_POINT('Ctrl Pts',(6.22539012272862,2.70041166123858,7.11100835022457));
#21050=CARTESIAN_POINT('Ctrl Pts',(6.39748820079394,2.57279491793265,7.12385546821444));
#21051=CARTESIAN_POINT('Ctrl Pts',(6.41871159187087,2.55664489873432,7.12546964274457));
#21052=CARTESIAN_POINT('Ctrl Pts',(6.44783693839009,2.53390557615123,7.1277303225724));
#21053=CARTESIAN_POINT('Ctrl Pts',(6.45591208963528,2.52753853803787,7.12836203923669));
#21054=CARTESIAN_POINT('Ctrl Pts',(6.46973929987774,2.51652842885067,7.1294525146436));
#21055=CARTESIAN_POINT('Ctrl Pts',(6.47550616878975,2.51190396776234,7.1299099643905));
#21056=CARTESIAN_POINT('Ctrl Pts',(6.48743269058432,2.50227246591128,7.13086164948699));
#21057=CARTESIAN_POINT('Ctrl Pts',(6.49358980242966,2.49726246898597,7.13135610806044));
#21058=CARTESIAN_POINT('Ctrl Pts',(6.50817992737085,2.48530072887005,7.1325351749779));
#21059=CARTESIAN_POINT('Ctrl Pts',(6.51659617652789,2.47832876201568,7.13322121623042));
#21060=CARTESIAN_POINT('Ctrl Pts',(6.53484804685455,2.46305181707763,7.13472159508525));
#21061=CARTESIAN_POINT('Ctrl Pts',(6.54466965867426,2.45473047700132,7.13553703171702));
#21062=CARTESIAN_POINT('Ctrl Pts',(6.57197446462373,2.43131408169053,7.13782600052415));
#21063=CARTESIAN_POINT('Ctrl Pts',(6.58934527016644,2.41608987603887,7.13930767106706));
#21064=CARTESIAN_POINT('Ctrl Pts',(6.6463100814323,2.36507144113298,7.14424740557378));
#21065=CARTESIAN_POINT('Ctrl Pts',(6.68517690344684,2.32848176934814,7.14774929396284));
#21066=CARTESIAN_POINT('Ctrl Pts',(6.83331788943999,2.18191211754013,7.16156337650518));
#21067=CARTESIAN_POINT('Ctrl Pts',(6.93550628735614,2.06507209879258,7.17211448946801));
#21068=CARTESIAN_POINT('Ctrl Pts',(7.1504020014744,1.78031894256516,7.19619460345784));
#21069=CARTESIAN_POINT('Ctrl Pts',(7.25654816552784,1.60822620632392,7.20959062731156));
#21070=CARTESIAN_POINT('Ctrl Pts',(7.36443838644642,1.38981344704689,7.22505398471197));
#21071=CARTESIAN_POINT('Ctrl Pts',(7.38223031454333,1.35195723613556,7.22768387625487));
#21072=CARTESIAN_POINT('Ctrl Pts',(7.40685318288468,1.29680237324319,7.23144520197996));
#21073=CARTESIAN_POINT('Ctrl Pts',(7.41427869972579,1.27977538138872,7.23259686494628));
#21074=CARTESIAN_POINT('Ctrl Pts',(7.42710082773345,1.24966594207764,7.23461699180284));
#21075=CARTESIAN_POINT('Ctrl Pts',(7.43255920487138,1.23661049911037,7.23548753724335));
#21076=CARTESIAN_POINT('Ctrl Pts',(7.44367386923792,1.20952637217369,7.23728259964956));
#21077=CARTESIAN_POINT('Ctrl Pts',(7.44931774371867,1.19549294704685,7.23820668011825));
#21078=CARTESIAN_POINT('Ctrl Pts',(7.46359340724234,1.15926192538388,7.24057730334684));
#21079=CARTESIAN_POINT('Ctrl Pts',(7.47207840752938,1.13700719516733,7.2420189073332));
#21080=CARTESIAN_POINT('Ctrl Pts',(7.50755730295076,1.04076013059023,7.24819357147067));
#21081=CARTESIAN_POINT('Ctrl Pts',(7.53208173391118,0.965882643633223,7.25284475361226));
#21082=CARTESIAN_POINT('Ctrl Pts',(7.5919332169537,0.757629425777134,7.26544293426783));
#21083=CARTESIAN_POINT('Ctrl Pts',(7.62148147420242,0.622766670066883,7.27322356150208));
#21084=CARTESIAN_POINT('Ctrl Pts',(7.66687941955569,0.325430162093823,7.2900710493035));
#21085=CARTESIAN_POINT('Ctrl Pts',(7.67921910621661,0.162824882296941,7.29909016486001));
#21086=CARTESIAN_POINT('Ctrl Pts',(7.67921910621823,3.21015783399936E-11,
7.30846150265207));
#21087=CARTESIAN_POINT('Origin',(4.45646910621825,-5.13094777615093E-16,
-2.31077344927308));
#21088=CARTESIAN_POINT('Ctrl Pts',(6.37917568135534,-2.58637139413976,3.74329856950612));
#21089=CARTESIAN_POINT('Ctrl Pts',(6.34981776169284,-2.60819604983126,3.74545795803728));
#21090=CARTESIAN_POINT('Ctrl Pts',(6.32008641473289,-2.62952220215757,3.74764227516074));
#21091=CARTESIAN_POINT('Ctrl Pts',(6.27627241956155,-2.65983305279075,3.75086776268092));
#21092=CARTESIAN_POINT('Ctrl Pts',(6.26247734541822,-2.66921902081475,3.75188424917421));
#21093=CARTESIAN_POINT('Ctrl Pts',(6.24024382473343,-2.68409512710286,3.75352506513817));
#21094=CARTESIAN_POINT('Ctrl Pts',(6.2318512533263,-2.68965371807077,3.75414500494344));
#21095=CARTESIAN_POINT('Ctrl Pts',(6.21686488041954,-2.69947883145809,3.75525329482638));
#21096=CARTESIAN_POINT('Ctrl Pts',(6.21028135030926,-2.70376068730008,3.75574061418644));
#21097=CARTESIAN_POINT('Ctrl Pts',(6.19605368380114,-2.7129403748258,3.75679479687359));
#21098=CARTESIAN_POINT('Ctrl Pts',(6.18840461162385,-2.71782990274919,3.75736216293192));
#21099=CARTESIAN_POINT('Ctrl Pts',(6.16698862995532,-2.7313925521135,3.75895217233337));
#21100=CARTESIAN_POINT('Ctrl Pts',(6.15317676597574,-2.73999368727886,3.75997933010706));
#21101=CARTESIAN_POINT('Ctrl Pts',(6.06956539130074,-2.79118684463646,3.76620477497964));
#21102=CARTESIAN_POINT('Ctrl Pts',(5.99823637780219,-2.83121085230435,3.77154622617879));
#21103=CARTESIAN_POINT('Ctrl Pts',(5.7814661209703,-2.94222300142046,3.78770402297351));
#21104=CARTESIAN_POINT('Ctrl Pts',(5.63211739923204,-3.00501951589682,3.79872786137717));
#21105=CARTESIAN_POINT('Ctrl Pts',(5.27890143948994,-3.12315587311417,3.82384093072569));
#21106=CARTESIAN_POINT('Ctrl Pts',(5.07301360408779,-3.17023649998643,3.83776623513276));
#21107=CARTESIAN_POINT('Ctrl Pts',(4.8367836126848,-3.20034835269865,3.85276057963487));
#21108=CARTESIAN_POINT('Ctrl Pts',(4.809552911355,-3.20346696620147,3.85447537845611));
#21109=CARTESIAN_POINT('Ctrl Pts',(4.76486261607714,-3.20800836676478,3.85726799192259));
#21110=CARTESIAN_POINT('Ctrl Pts',(4.74742577447629,-3.20963681352515,3.85835220141562));
#21111=CARTESIAN_POINT('Ctrl Pts',(4.71605383436079,-3.21230891589858,3.86029345916461));
#21112=CARTESIAN_POINT('Ctrl Pts',(4.70212368809387,-3.21340421335462,3.86115210538209));
#21113=CARTESIAN_POINT('Ctrl Pts',(4.672397011315,-3.21554712476631,3.86297751253728));
#21114=CARTESIAN_POINT('Ctrl Pts',(4.65659895248147,-3.21656901533518,3.86394344645148));
#21115=CARTESIAN_POINT('Ctrl Pts',(4.61379440963783,-3.21902122856369,3.86654972858248));
#21116=CARTESIAN_POINT('Ctrl Pts',(4.58677603899122,-3.22022811179088,3.86818307653523));
#21117=CARTESIAN_POINT('Ctrl Pts',(4.44114121931691,-3.22489750916803,3.87692844797836));
#21118=CARTESIAN_POINT('Ctrl Pts',(4.32241035730945,-3.22214705596425,3.88384379947539));
#21119=CARTESIAN_POINT('Ctrl Pts',(4.04933038358868,-3.20069590628345,3.89950347711698));
#21120=CARTESIAN_POINT('Ctrl Pts',(3.89564590314937,-3.17737245428039,3.90812982625756));
#21121=CARTESIAN_POINT('Ctrl Pts',(3.57940300272826,-3.10571072657916,3.92628648859027));
#21122=CARTESIAN_POINT('Ctrl Pts',(3.41777903146608,-3.05545299974991,3.93580372816945));
#21123=CARTESIAN_POINT('Ctrl Pts',(3.23585077852002,-2.98277285361419,3.94754794881669));
#21124=CARTESIAN_POINT('Ctrl Pts',(3.21096611919768,-2.9724678635729,3.94917784262253));
#21125=CARTESIAN_POINT('Ctrl Pts',(3.17672933363865,-2.95778467653029,3.95145680682462));
#21126=CARTESIAN_POINT('Ctrl Pts',(3.1672639395666,-2.95367129345696,3.9520907675041));
#21127=CARTESIAN_POINT('Ctrl Pts',(3.15104430451888,-2.94652989757682,3.95318408480818));
#21128=CARTESIAN_POINT('Ctrl Pts',(3.14428036887951,-2.94352391959094,3.95364211688344));
#21129=CARTESIAN_POINT('Ctrl Pts',(3.13014465865495,-2.93718342715595,3.95460385618622));
#21130=CARTESIAN_POINT('Ctrl Pts',(3.12277503659694,-2.93384443155106,3.95510784792173));
#21131=CARTESIAN_POINT('Ctrl Pts',(3.10474858220154,-2.92559513064642,3.95634686079197));
#21132=CARTESIAN_POINT('Ctrl Pts',(3.09410590327748,-2.92065433366923,3.95708371473344));
#21133=CARTESIAN_POINT('Ctrl Pts',(3.05550885142972,-2.90247903176341,3.95977487505274));
#21134=CARTESIAN_POINT('Ctrl Pts',(3.02771938106358,-2.88890086780487,3.96174861661637));
#21135=CARTESIAN_POINT('Ctrl Pts',(2.95839315810366,-2.85378259030085,3.96675603041624));
#21136=CARTESIAN_POINT('Ctrl Pts',(2.91712289139339,-2.83173434590594,3.96981356369938));
#21137=CARTESIAN_POINT('Ctrl Pts',(2.58473013705096,-2.64474312009241,3.9949868584153));
#21138=CARTESIAN_POINT('Ctrl Pts',(2.3204092414957,-2.43626750367108,4.01819928517467));
#21139=CARTESIAN_POINT('Ctrl Pts',(2.04852514414407,-2.14293717908672,4.04395289853798));
#21140=CARTESIAN_POINT('Ctrl Pts',(2.00563630643055,-2.09375104874505,4.04809600219894));
#21141=CARTESIAN_POINT('Ctrl Pts',(1.9496742259047,-2.02549420697816,4.05361790596751));
#21142=CARTESIAN_POINT('Ctrl Pts',(1.93527162700832,-2.0075384602635,4.05505015026933));
#21143=CARTESIAN_POINT('Ctrl Pts',(1.91183183465776,-1.9776658730033,4.05740010762631));
#21144=CARTESIAN_POINT('Ctrl Pts',(1.90268320552073,-1.9658379217199,4.05832223824882));
#21145=CARTESIAN_POINT('Ctrl Pts',(1.88499002633847,-1.94263104364197,4.06011551552755));
#21146=CARTESIAN_POINT('Ctrl Pts',(1.87643787707972,-1.93125837134497,4.06098694855694));
#21147=CARTESIAN_POINT('Ctrl Pts',(1.85641545098851,-1.90426211275478,4.06303843772651));
#21148=CARTESIAN_POINT('Ctrl Pts',(1.84501015790563,-1.88859084790915,4.06421595315793));
#21149=CARTESIAN_POINT('Ctrl Pts',(1.80741981421603,-1.8359487502541,4.06812801253917));
#21150=CARTESIAN_POINT('Ctrl Pts',(1.78187232017805,-1.79852781535277,4.0708382650619));
#21151=CARTESIAN_POINT('Ctrl Pts',(1.72265089645832,-1.70772859580557,4.07725871707347));
#21152=CARTESIAN_POINT('Ctrl Pts',(1.68973867083592,-1.65387495270192,4.08094202096787));
#21153=CARTESIAN_POINT('Ctrl Pts',(1.49090226071539,-1.30595609949559,4.10406427265169));
#21154=CARTESIAN_POINT('Ctrl Pts',(1.37050983471422,-0.988380628069924,
4.12195529580339));
#21155=CARTESIAN_POINT('Ctrl Pts',(1.29400965244306,-0.621570516594846,
4.14420823992934));
#21156=CARTESIAN_POINT('Ctrl Pts',(1.28705016136918,-0.585049559637317,
4.14644298120553));
#21157=CARTESIAN_POINT('Ctrl Pts',(1.27850885236505,-0.535589097740135,
4.14950520689873));
#21158=CARTESIAN_POINT('Ctrl Pts',(1.27637120165279,-0.522746937552845,
4.15030353293756));
#21159=CARTESIAN_POINT('Ctrl Pts',(1.27311994748278,-0.502456376911369,
4.15157048580155));
#21160=CARTESIAN_POINT('Ctrl Pts',(1.27195451545177,-0.495016257898872,
4.15203623686493));
#21161=CARTESIAN_POINT('Ctrl Pts',(1.26960594735517,-0.479671402352096,
4.15299939449796));
#21162=CARTESIAN_POINT('Ctrl Pts',(1.26842613643813,-0.471766324443939,
4.15349699514388));
#21163=CARTESIAN_POINT('Ctrl Pts',(1.26566261849829,-0.452766090444523,
4.15469629780726));
#21164=CARTESIAN_POINT('Ctrl Pts',(1.26410736828276,-0.441666956134685,
4.15539956997679));
#21165=CARTESIAN_POINT('Ctrl Pts',(1.25893158098884,-0.403273398896135,
4.15784105658939));
#21166=CARTESIAN_POINT('Ctrl Pts',(1.25560306922828,-0.375941690990998,
4.1595943943965));
#21167=CARTESIAN_POINT('Ctrl Pts',(1.24829523057348,-0.308772817516369,
4.16393529758366));
#21168=CARTESIAN_POINT('Ctrl Pts',(1.2447073437145,-0.268898410902722,4.16653975920778));
#21169=CARTESIAN_POINT('Ctrl Pts',(1.23301500006768,-0.104744289972911,
4.1773478629858));
#21170=CARTESIAN_POINT('Ctrl Pts',(1.23137548864601,0.0198822758279329,
4.18575170872378));
#21171=CARTESIAN_POINT('Ctrl Pts',(1.24849105400465,0.401797934962905,4.2116107241368));
#21172=CARTESIAN_POINT('Ctrl Pts',(1.29088872305006,0.65704943899393,4.22894975426185));
#21173=CARTESIAN_POINT('Ctrl Pts',(1.37327146098075,0.938765450359666,4.24755331344584));
#21174=CARTESIAN_POINT('Ctrl Pts',(1.38384411194963,0.972812468348576,4.24979457995541));
#21175=CARTESIAN_POINT('Ctrl Pts',(1.40057205092747,1.02368513667787,4.25313381711095));
#21176=CARTESIAN_POINT('Ctrl Pts',(1.40630597499971,1.04064545609906,4.25424545897899));
#21177=CARTESIAN_POINT('Ctrl Pts',(1.41649451849129,1.06997422983963,4.25616519936816));
#21178=CARTESIAN_POINT('Ctrl Pts',(1.4208839889695,1.08236470315842,4.25697542637545));
#21179=CARTESIAN_POINT('Ctrl Pts',(1.43018871229421,1.10812793290962,4.25865857486128));
#21180=CARTESIAN_POINT('Ctrl Pts',(1.43511708969751,1.12149567136304,4.25953103913061));
#21181=CARTESIAN_POINT('Ctrl Pts',(1.44699531154754,1.15306752166063,4.26158978569447));
#21182=CARTESIAN_POINT('Ctrl Pts',(1.45402197571662,1.17124228264011,4.26277347616694));
#21183=CARTESIAN_POINT('Ctrl Pts',(1.4781601175877,1.23203158785901,4.26672863672215));
#21184=CARTESIAN_POINT('Ctrl Pts',(1.4960179203447,1.2743450706152,4.26947505950246));
#21185=CARTESIAN_POINT('Ctrl Pts',(1.54100919453519,1.37489524231377,4.27599670165879));
#21186=CARTESIAN_POINT('Ctrl Pts',(1.56899179505691,1.43273128526529,4.27974383347161));
#21187=CARTESIAN_POINT('Ctrl Pts',(1.68614662446461,1.65747737194452,4.29435702941941));
#21188=CARTESIAN_POINT('Ctrl Pts',(1.78821310664888,1.81723184052764,4.30483681489048));
#21189=CARTESIAN_POINT('Ctrl Pts',(1.95458853839343,2.03314026340757,4.32011603201655));
#21190=CARTESIAN_POINT('Ctrl Pts',(2.00800795817604,2.09716537979181,4.32481153799596));
#21191=CARTESIAN_POINT('Ctrl Pts',(2.12497231191156,2.22678357875538,4.33483072751014));
#21192=CARTESIAN_POINT('Ctrl Pts',(2.18894135851257,2.29188942760255,4.34016729457898));
#21193=CARTESIAN_POINT('Ctrl Pts',(2.26713397731344,2.36499037359676,4.34665564810149));
#21194=CARTESIAN_POINT('Ctrl Pts',(2.27876803591371,2.37570743132216,4.34762018773588));
#21195=CARTESIAN_POINT('Ctrl Pts',(2.29782246684684,2.39300241732182,4.34919948698004));
#21196=CARTESIAN_POINT('Ctrl Pts',(2.30519529004754,2.39963264787468,4.34981046784696));
#21197=CARTESIAN_POINT('Ctrl Pts',(2.31844298864866,2.41143591186017,4.35090835951223));
#21198=CARTESIAN_POINT('Ctrl Pts',(2.32430624967556,2.41662168891636,4.35139430679078));
#21199=CARTESIAN_POINT('Ctrl Pts',(2.33718366443557,2.42792780618445,4.35246171272344));
#21200=CARTESIAN_POINT('Ctrl Pts',(2.34420536408459,2.43403904947004,4.35304379614867));
#21201=CARTESIAN_POINT('Ctrl Pts',(2.36438624339256,2.45145012378544,4.35471665573849));
#21202=CARTESIAN_POINT('Ctrl Pts',(2.37761007141598,2.4626740540899,4.35581271206401));
#21203=CARTESIAN_POINT('Ctrl Pts',(2.47296777821088,2.54229506459685,4.36371162673015));
#21204=CARTESIAN_POINT('Ctrl Pts',(2.55836112002222,2.60666895006234,4.37075801376289));
#21205=CARTESIAN_POINT('Ctrl Pts',(2.83305520814657,2.79308451442682,4.39297258558839));
#21206=CARTESIAN_POINT('Ctrl Pts',(3.03207974890739,2.89964181234241,4.40839355098079));
#21207=CARTESIAN_POINT('Ctrl Pts',(3.35531660206728,3.03132453995996,4.43144666662687));
#21208=CARTESIAN_POINT('Ctrl Pts',(3.47265726603864,3.07141433160756,4.43945657855958));
#21209=CARTESIAN_POINT('Ctrl Pts',(3.61909755986484,3.11218829764507,4.44901240631823));
#21210=CARTESIAN_POINT('Ctrl Pts',(3.64626477154127,3.11937111018519,4.45076733456801));
#21211=CARTESIAN_POINT('Ctrl Pts',(3.68926226790782,3.1301396913184,4.45351751064787));
#21212=CARTESIAN_POINT('Ctrl Pts',(3.70503114552755,3.13396263962135,4.45452035199704));
#21213=CARTESIAN_POINT('Ctrl Pts',(3.73439664985469,3.1408475202904,4.45637742154078));
#21214=CARTESIAN_POINT('Ctrl Pts',(3.74798550034312,3.14394064317625,4.45723263252117));
#21215=CARTESIAN_POINT('Ctrl Pts',(3.77817207408652,3.15060612036469,4.45912342639666));
#21216=CARTESIAN_POINT('Ctrl Pts',(3.79477889718563,3.15413567779364,4.46015761974628));
#21217=CARTESIAN_POINT('Ctrl Pts',(3.84319676355824,3.16402701615015,4.46315592129958));
#21218=CARTESIAN_POINT('Ctrl Pts',(3.87507749553923,3.17004003690818,4.46510892966774));
#21219=CARTESIAN_POINT('Ctrl Pts',(4.11684838740508,3.21187027401117,4.47977122939964));
#21220=CARTESIAN_POINT('Ctrl Pts',(4.32974136686386,3.22729122010331,4.49179076533305));
#21221=CARTESIAN_POINT('Ctrl Pts',(4.76628115782701,3.21561702101713,4.5162261782402));
#21222=CARTESIAN_POINT('Ctrl Pts',(4.98867702377822,3.18636199397078,4.52857811974589));
#21223=CARTESIAN_POINT('Ctrl Pts',(5.23039511307756,3.12854187097451,4.54350880611434));
#21224=CARTESIAN_POINT('Ctrl Pts',(5.25450679679479,3.12247841648598,4.54501563242105));
#21225=CARTESIAN_POINT('Ctrl Pts',(5.28820028659546,3.11358965140443,4.54714890814396));
#21226=CARTESIAN_POINT('Ctrl Pts',(5.29784346338925,3.11099766292469,4.54776265004838));
#21227=CARTESIAN_POINT('Ctrl Pts',(5.31453069110011,3.10642904378486,4.5488304974479));
#21228=CARTESIAN_POINT('Ctrl Pts',(5.32158040991493,3.10447314648003,4.54928341714026));
#21229=CARTESIAN_POINT('Ctrl Pts',(5.33650045337289,3.10027891376274,4.55024590240835));
#21230=CARTESIAN_POINT('Ctrl Pts',(5.34436899384271,3.09803458669996,4.55075582228102));
#21231=CARTESIAN_POINT('Ctrl Pts',(5.36393354250173,3.09237357561683,4.55202934293306));
#21232=CARTESIAN_POINT('Ctrl Pts',(5.37561878692755,3.08892050522273,4.55279500592538));
#21233=CARTESIAN_POINT('Ctrl Pts',(5.41992743804611,3.07555331380205,4.55571668153471));
#21234=CARTESIAN_POINT('Ctrl Pts',(5.45241109207888,3.06518832818375,4.55789661161878));
#21235=CARTESIAN_POINT('Ctrl Pts',(5.53537963606106,3.03725642689589,4.56355175364656));
#21236=CARTESIAN_POINT('Ctrl Pts',(5.58560185195019,3.01894570199932,4.56705877981558));
#21237=CARTESIAN_POINT('Ctrl Pts',(5.83774851215238,2.91984273290741,4.58501856159581));
#21238=CARTESIAN_POINT('Ctrl Pts',(6.03158176459205,2.82000689038689,4.59994010379897));
#21239=CARTESIAN_POINT('Ctrl Pts',(6.34631745079664,2.61525352573873,4.62499961077273));
#21240=CARTESIAN_POINT('Ctrl Pts',(6.47224825476557,2.51946920452413,4.63530723888649));
#21241=CARTESIAN_POINT('Ctrl Pts',(6.61087638948587,2.39695114043158,4.64695182020448));
#21242=CARTESIAN_POINT('Ctrl Pts',(6.63086830738769,2.37883032116423,4.64863946606084));
#21243=CARTESIAN_POINT('Ctrl Pts',(6.66336265076748,2.34862525947712,4.65139702453477));
#21244=CARTESIAN_POINT('Ctrl Pts',(6.67599873016896,2.33668739753253,4.65247306345761));
#21245=CARTESIAN_POINT('Ctrl Pts',(6.6986088087269,2.31497776437926,4.65440543176101));
#21246=CARTESIAN_POINT('Ctrl Pts',(6.70861699119395,2.30524237534058,4.655263298122));
#21247=CARTESIAN_POINT('Ctrl Pts',(6.72790905935415,2.28623059358038,4.65692202656086));
#21248=CARTESIAN_POINT('Ctrl Pts',(6.73720015398694,2.27696194158973,4.65772320146893));
#21249=CARTESIAN_POINT('Ctrl Pts',(6.76220300293278,2.25171289762537,4.65988576667305));
#21250=CARTESIAN_POINT('Ctrl Pts',(6.77780529485408,2.23562477037519,4.66124235479986));
#21251=CARTESIAN_POINT('Ctrl Pts',(6.84409876582088,2.16582467693333,4.66703925873701));
#21252=CARTESIAN_POINT('Ctrl Pts',(6.89310548850275,2.11053933878044,4.67140774922145));
#21253=CARTESIAN_POINT('Ctrl Pts',(7.0200473036631,1.9570121681029,4.68301698341837));
#21254=CARTESIAN_POINT('Ctrl Pts',(7.09422246918846,1.85582609554176,4.69012332222034));
#21255=CARTESIAN_POINT('Ctrl Pts',(7.17200284155761,1.73560132735333,4.69816286885749));
#21256=CARTESIAN_POINT('Ctrl Pts',(7.18156139451602,1.72055434209397,4.69916231235919));
#21257=CARTESIAN_POINT('Ctrl Pts',(7.19099309084831,1.70543136478218,4.70016067061871));
#21258=CARTESIAN_POINT('Origin',(4.45646910621825,-5.13094777615093E-16,
-2.31077344927308));
#21259=CARTESIAN_POINT('Ctrl Pts',(6.37918196868372,-2.58636672013265,2.49808050559515));
#21260=CARTESIAN_POINT('Ctrl Pts',(6.28518486951706,-2.65624444868342,2.50481557244532));
#21261=CARTESIAN_POINT('Ctrl Pts',(6.18739743632227,-2.72098388076692,2.51140426454075));
#21262=CARTESIAN_POINT('Ctrl Pts',(5.89937864052687,-2.88981760055554,2.53009003280362));
#21263=CARTESIAN_POINT('Ctrl Pts',(5.70197263437052,-2.98022328862117,2.54204479930428));
#21264=CARTESIAN_POINT('Ctrl Pts',(5.46564045093849,-3.06084797756682,2.55693518690676));
#21265=CARTESIAN_POINT('Ctrl Pts',(5.4340945393033,-3.07106910732803,2.55893472520474));
#21266=CARTESIAN_POINT('Ctrl Pts',(5.39087364308137,-3.08433964641135,2.56169762132471));
#21267=CARTESIAN_POINT('Ctrl Pts',(5.37932977043503,-3.08781331635947,2.56243781562696));
#21268=CARTESIAN_POINT('Ctrl Pts',(5.3599441385493,-3.09352823525713,2.56368501597441));
#21269=CARTESIAN_POINT('Ctrl Pts',(5.35211273340421,-3.09580467196993,2.56419000257694));
#21270=CARTESIAN_POINT('Ctrl Pts',(5.33721807588775,-3.1000730107221,2.56515275866065));
#21271=CARTESIAN_POINT('Ctrl Pts',(5.33015650855711,-3.10207055687392,2.56561018281042));
#21272=CARTESIAN_POINT('Ctrl Pts',(5.31338352422811,-3.10675341247277,2.56669890190203));
#21273=CARTESIAN_POINT('Ctrl Pts',(5.30366628195886,-3.10941731274112,2.56733140317273));
#21274=CARTESIAN_POINT('Ctrl Pts',(5.2694152088243,-3.11863448547352,2.5695666371848));
#21275=CARTESIAN_POINT('Ctrl Pts',(5.24481728974322,-3.12494311441454,2.57118237184543));
#21276=CARTESIAN_POINT('Ctrl Pts',(5.0101758211773,-3.18217501660275,2.586677651492));
#21277=CARTESIAN_POINT('Ctrl Pts',(4.79560105169467,-3.21213399893489,2.60143593171232));
#21278=CARTESIAN_POINT('Ctrl Pts',(4.42874664045629,-3.22616768330515,2.62622546111055));
#21279=CARTESIAN_POINT('Ctrl Pts',(4.27759830218279,-3.22132586397863,2.63632107142302));
#21280=CARTESIAN_POINT('Ctrl Pts',(4.07233574230635,-3.20025245081135,2.64971826259662));
#21281=CARTESIAN_POINT('Ctrl Pts',(4.01749002079987,-3.19319152827772,2.65326866444437));
#21282=CARTESIAN_POINT('Ctrl Pts',(3.92239140019319,-3.17845163905746,2.65937374019091));
#21283=CARTESIAN_POINT('Ctrl Pts',(3.88205417113569,-3.17141002522392,2.66194719425168));
#21284=CARTESIAN_POINT('Ctrl Pts',(3.8235823979692,-3.16005042311833,2.66565569211455));
#21285=CARTESIAN_POINT('Ctrl Pts',(3.80533508374427,-3.15634104149528,2.66680989101781));
#21286=CARTESIAN_POINT('Ctrl Pts',(3.77332093682859,-3.14954364276837,2.66882968781259));
#21287=CARTESIAN_POINT('Ctrl Pts',(3.75954046034546,-3.14652300987291,2.66969740912508));
#21288=CARTESIAN_POINT('Ctrl Pts',(3.73273209211697,-3.14046194843547,2.67138231401274));
#21289=CARTESIAN_POINT('Ctrl Pts',(3.71970244092451,-3.13743070115226,2.67219977155121));
#21290=CARTESIAN_POINT('Ctrl Pts',(3.68471521075411,-3.12906121692898,2.67439111296566));
#21291=CARTESIAN_POINT('Ctrl Pts',(3.66279402101405,-3.12357296592664,2.67576016230111));
#21292=CARTESIAN_POINT('Ctrl Pts',(3.58074919234202,-3.1021125007785,2.68087108200045));
#21293=CARTESIAN_POINT('Ctrl Pts',(3.52103220021034,-3.08463059183433,2.68456435968236));
#21294=CARTESIAN_POINT('Ctrl Pts',(3.45424201160977,-3.06295975853678,2.68867919591175));
#21295=CARTESIAN_POINT('Ctrl Pts',(3.44663761583096,-3.06046107540552,2.68914746152703));
#21296=CARTESIAN_POINT('Ctrl Pts',(3.12513042069685,-2.95349017741802,2.70893700938461));
#21297=CARTESIAN_POINT('Ctrl Pts',(2.8292185517356,-2.80135398063382,2.72657394649185));
#21298=CARTESIAN_POINT('Ctrl Pts',(2.52393355506871,-2.5794570656971,2.74849368113489));
#21299=CARTESIAN_POINT('Ctrl Pts',(2.48681181532542,-2.55122365500893,2.75123502302096));
#21300=CARTESIAN_POINT('Ctrl Pts',(2.42617007866204,-2.50298929888503,2.75586531428964));
#21301=CARTESIAN_POINT('Ctrl Pts',(2.40230062469231,-2.48343738836674,2.7577286269456));
#21302=CARTESIAN_POINT('Ctrl Pts',(2.3697554610113,-2.45598883286712,2.76033189838433));
#21303=CARTESIAN_POINT('Ctrl Pts',(2.36083581310995,-2.44838233844631,2.76105201701385));
#21304=CARTESIAN_POINT('Ctrl Pts',(2.34583218041234,-2.43544549422176,2.76227498505889));
#21305=CARTESIAN_POINT('Ctrl Pts',(2.33972629396624,-2.43014050065552,2.76277598770714));
#21306=CARTESIAN_POINT('Ctrl Pts',(2.32806951112227,-2.41993544303534,2.76373894129266));
#21307=CARTESIAN_POINT('Ctrl Pts',(2.32251543657167,-2.41503915455816,2.76420059569364));
#21308=CARTESIAN_POINT('Ctrl Pts',(2.30925339980471,-2.40326631337749,2.76530964834268));
#21309=CARTESIAN_POINT('Ctrl Pts',(2.301561586026,-2.39637180660293,2.76595835667477));
#21310=CARTESIAN_POINT('Ctrl Pts',(2.27388432162737,-2.37132246648406,2.76831201436388));
#21311=CARTESIAN_POINT('Ctrl Pts',(2.25409470102397,-2.352954196432,2.77003179610513));
#21312=CARTESIAN_POINT('Ctrl Pts',(2.10913893262197,-2.21497876568062,2.78288992630603));
#21313=CARTESIAN_POINT('Ctrl Pts',(1.99357236233124,-2.08571771221435,2.79459093805212));
#21314=CARTESIAN_POINT('Ctrl Pts',(1.77964809002725,-1.80373364151393,2.81853648892629));
#21315=CARTESIAN_POINT('Ctrl Pts',(1.68265191754336,-1.65068982538436,2.83073398126935));
#21316=CARTESIAN_POINT('Ctrl Pts',(1.57068087793179,-1.43599959830357,2.84652031534988));
#21317=CARTESIAN_POINT('Ctrl Pts',(1.54391146500114,-1.38089728593823,2.85046657104193));
#21318=CARTESIAN_POINT('Ctrl Pts',(1.50051835996936,-1.28469220993171,2.85717645664701));
#21319=CARTESIAN_POINT('Ctrl Pts',(1.48314282106256,-1.24394935739802,2.85996428431486));
#21320=CARTESIAN_POINT('Ctrl Pts',(1.45944244009449,-1.18503911163739,2.86392058197347));
#21321=CARTESIAN_POINT('Ctrl Pts',(1.45243235860227,-1.16715456480946,2.86511198028158));
#21322=CARTESIAN_POINT('Ctrl Pts',(1.4405188916409,-1.1359416812938,2.86717476595096));
#21323=CARTESIAN_POINT('Ctrl Pts',(1.43554298274396,-1.12264178030261,2.86804856143227));
#21324=CARTESIAN_POINT('Ctrl Pts',(1.42548784973079,-1.09521483653803,2.86984007626873));
#21325=CARTESIAN_POINT('Ctrl Pts',(1.42041909753476,-1.08108430387859,2.87075742951432));
#21326=CARTESIAN_POINT('Ctrl Pts',(1.40773843960834,-1.04494084332239,2.87308978931931));
#21327=CARTESIAN_POINT('Ctrl Pts',(1.40026601470624,-1.02287963642323,2.8745001659332));
#21328=CARTESIAN_POINT('Ctrl Pts',(1.37212289717023,-0.936728658827347,
2.87995846036124));
#21329=CARTESIAN_POINT('Ctrl Pts',(1.35322291445947,-0.872075765366114,
2.88394860285795));
#21330=CARTESIAN_POINT('Ctrl Pts',(1.25319919964049,-0.485293519959753,
2.90729526881307));
#21331=CARTESIAN_POINT('Ctrl Pts',(1.22026002972698,-0.152839572016994,
2.92499853874331));
#21332=CARTESIAN_POINT('Ctrl Pts',(1.24126974780216,0.225367357612319,2.94699749744975));
#21333=CARTESIAN_POINT('Ctrl Pts',(1.24487190547074,0.271919749776895,2.94974184704032));
#21334=CARTESIAN_POINT('Ctrl Pts',(1.25253447154715,0.349104611388237,2.95437674566911));
#21335=CARTESIAN_POINT('Ctrl Pts',(1.25602655436483,0.379787421653811,2.9562415926886));
#21336=CARTESIAN_POINT('Ctrl Pts',(1.26145220339481,0.422045098901182,2.95884666759168));
#21337=CARTESIAN_POINT('Ctrl Pts',(1.26300901467856,0.433667739988653,2.95956701934933));
#21338=CARTESIAN_POINT('Ctrl Pts',(1.26574688723206,0.45329319608573,2.96079026815489));
#21339=CARTESIAN_POINT('Ctrl Pts',(1.26689473232787,0.46130067419336,2.96129131646005));
#21340=CARTESIAN_POINT('Ctrl Pts',(1.26915080822516,0.476628199260626,2.96225426473321));
#21341=CARTESIAN_POINT('Ctrl Pts',(1.27025413235005,0.483948872025284,2.96271586758078));
#21342=CARTESIAN_POINT('Ctrl Pts',(1.27295679562112,0.501471402258538,2.9638246723081));
#21343=CARTESIAN_POINT('Ctrl Pts',(1.27457995202293,0.511669427076917,2.96447318298709));
#21344=CARTESIAN_POINT('Ctrl Pts',(1.28062047076585,0.548480422393644,2.96682516733172));
#21345=CARTESIAN_POINT('Ctrl Pts',(1.28532280188968,0.575044637444286,2.96854344572162));
#21346=CARTESIAN_POINT('Ctrl Pts',(1.32135561407563,0.764695896638454,2.98094646137619));
#21347=CARTESIAN_POINT('Ctrl Pts',(1.36491486366795,0.92519096521642,2.99214979649443));
#21348=CARTESIAN_POINT('Ctrl Pts',(1.4734228316176,1.22975116498648,3.01401992145856));
#21349=CARTESIAN_POINT('Ctrl Pts',(1.536984695453,1.37385251149684,3.02465417590375));
#21350=CARTESIAN_POINT('Ctrl Pts',(1.6668715864945,1.61818507147743,3.04288998801567));
#21351=CARTESIAN_POINT('Ctrl Pts',(1.72874586729189,1.7204386016444,3.05059479169305));
#21352=CARTESIAN_POINT('Ctrl Pts',(1.81145160979574,1.84139454919563,3.0597956226882));
#21353=CARTESIAN_POINT('Ctrl Pts',(1.82702398548475,1.86356375561464,3.06148602139075));
#21354=CARTESIAN_POINT('Ctrl Pts',(1.85214241964481,1.89838115334209,3.06414795433224));
#21355=CARTESIAN_POINT('Ctrl Pts',(1.86150512405357,1.91115944895919,3.06512645882332));
#21356=CARTESIAN_POINT('Ctrl Pts',(1.87930227642939,1.9350772325466,3.0669611168412));
#21357=CARTESIAN_POINT('Ctrl Pts',(1.88771565622375,1.94623186885487,3.06781805980918));
#21358=CARTESIAN_POINT('Ctrl Pts',(1.90682805857651,1.97123165260524,3.06974179535838));
#21359=CARTESIAN_POINT('Ctrl Pts',(1.91756788227919,1.98504516168025,3.07080695213981));
#21360=CARTESIAN_POINT('Ctrl Pts',(1.94538628085664,2.02022992844962,3.07352624448694));
#21361=CARTESIAN_POINT('Ctrl Pts',(1.96262564563155,2.04147269956306,3.07517395835823));
#21362=CARTESIAN_POINT('Ctrl Pts',(2.11072293195473,2.21928585009176,3.08902464733973));
#21363=CARTESIAN_POINT('Ctrl Pts',(2.25591330654054,2.36332902778761,3.10059247973866));
#21364=CARTESIAN_POINT('Ctrl Pts',(2.58768383946716,2.63520721631527,3.12461965782392));
#21365=CARTESIAN_POINT('Ctrl Pts',(2.77601333675428,2.75911543555872,3.13699129080868));
#21366=CARTESIAN_POINT('Ctrl Pts',(3.00556458882084,2.87786837283464,3.15239621387373));
#21367=CARTESIAN_POINT('Ctrl Pts',(3.03569649450793,2.89286281596386,3.15442502550917));
#21368=CARTESIAN_POINT('Ctrl Pts',(3.07699414819286,2.91261281342183,3.15722210540213));
#21369=CARTESIAN_POINT('Ctrl Pts',(3.08796121636261,2.91778181248422,3.15796646208979));
#21370=CARTESIAN_POINT('Ctrl Pts',(3.10636662391309,2.92633005578013,3.15921870661804));
#21371=CARTESIAN_POINT('Ctrl Pts',(3.11378924493475,2.92974317911138,3.15972453864958));
#21372=CARTESIAN_POINT('Ctrl Pts',(3.12789273947022,2.93616349634336,3.16068735636654));
#21373=CARTESIAN_POINT('Ctrl Pts',(3.13457104003222,2.93917620084513,3.16114398704493));
#21374=CARTESIAN_POINT('Ctrl Pts',(3.15041365336089,2.94625817960258,3.16222882229064));
#21375=CARTESIAN_POINT('Ctrl Pts',(3.15958673718835,2.9503074791374,3.16285821347111));
#21376=CARTESIAN_POINT('Ctrl Pts',(3.19179359653387,2.96434541650362,3.16507202929224));
#21377=CARTESIAN_POINT('Ctrl Pts',(3.21492439685828,2.97410735143469,3.16666914156387));
#21378=CARTESIAN_POINT('Ctrl Pts',(3.44253734122585,3.06704935497796,3.18243839807141));
#21379=CARTESIAN_POINT('Ctrl Pts',(3.65492585154512,3.12927533109989,3.19752811313324));
#21380=CARTESIAN_POINT('Ctrl Pts',(4.08526167123623,3.20863764561537,3.22706297232233));
#21381=CARTESIAN_POINT('Ctrl Pts',(4.30199468346828,3.22634769695101,3.24143203436631));
#21382=CARTESIAN_POINT('Ctrl Pts',(4.55051967751224,3.22153262063662,3.25709756475171));
#21383=CARTESIAN_POINT('Ctrl Pts',(4.58213255193061,3.22045443202462,3.25907642553904));
#21384=CARTESIAN_POINT('Ctrl Pts',(4.63051476704922,3.21809077363217,3.26208472293813));
#21385=CARTESIAN_POINT('Ctrl Pts',(4.64729774586694,3.21713918984079,3.26312451608655));
#21386=CARTESIAN_POINT('Ctrl Pts',(4.67784243585196,3.21516746145702,3.26501034560159));
#21387=CARTESIAN_POINT('Ctrl Pts',(4.69160641772356,3.21419016400823,3.26585770087099));
#21388=CARTESIAN_POINT('Ctrl Pts',(4.7216327846948,3.21186426423241,3.26770108859904));
#21389=CARTESIAN_POINT('Ctrl Pts',(4.73789212118772,3.21048048275839,3.26869599595685));
#21390=CARTESIAN_POINT('Ctrl Pts',(4.78252594564014,3.20634015158037,3.27141852242898));
#21391=CARTESIAN_POINT('Ctrl Pts',(4.8108758805816,3.20333047738715,3.2731381941255));
#21392=CARTESIAN_POINT('Ctrl Pts',(4.96990108317588,3.18431104664116,3.28273615631727));
#21393=CARTESIAN_POINT('Ctrl Pts',(5.09954693954922,3.16068125056175,3.29037017949853));
#21394=CARTESIAN_POINT('Ctrl Pts',(5.43989282343945,3.07683132161021,3.31030831079949));
#21395=CARTESIAN_POINT('Ctrl Pts',(5.64649245559286,3.00297368077317,3.32227930301988));
#21396=CARTESIAN_POINT('Ctrl Pts',(5.93858482303338,2.86363947522782,3.34075167973917));
#21397=CARTESIAN_POINT('Ctrl Pts',(6.03089675623035,2.81394225257676,3.34684896211601));
#21398=CARTESIAN_POINT('Ctrl Pts',(6.13540541484197,2.75092507306508,3.35424897618752));
#21399=CARTESIAN_POINT('Ctrl Pts',(6.15012424308198,2.74188769522744,3.35530313743748));
#21400=CARTESIAN_POINT('Ctrl Pts',(6.17264957455036,2.7278065414261,3.35693601543223));
#21401=CARTESIAN_POINT('Ctrl Pts',(6.18050834635878,2.72284641886572,3.35750941471188));
#21402=CARTESIAN_POINT('Ctrl Pts',(6.19494787879044,2.71364522602656,3.35857003413021));
#21403=CARTESIAN_POINT('Ctrl Pts',(6.20153473924759,2.7094141041535,3.35905660289348));
#21404=CARTESIAN_POINT('Ctrl Pts',(6.21644572519887,2.69975898413953,3.36016430369359));
#21405=CARTESIAN_POINT('Ctrl Pts',(6.22476017946508,2.69432049799191,3.36078637852781));
#21406=CARTESIAN_POINT('Ctrl Pts',(6.24630104692054,2.68008795771658,3.36240926138875));
#21407=CARTESIAN_POINT('Ctrl Pts',(6.25948765263792,2.67123453380736,3.36341381286248));
#21408=CARTESIAN_POINT('Ctrl Pts',(6.30864628809099,2.63769983166925,3.36719878950639));
#21409=CARTESIAN_POINT('Ctrl Pts',(6.34417595802215,2.6123901579048,3.37001549160216));
#21410=CARTESIAN_POINT('Ctrl Pts',(6.37917546296132,2.5863715564937,3.37286375486987));
#21411=CARTESIAN_POINT('Origin',(4.45646910621825,-5.13094777615093E-16,
-2.31077344927308));
#21412=CARTESIAN_POINT('Ctrl Pts',(6.37917539807422,-2.58637160473072,1.24811343365893));
#21413=CARTESIAN_POINT('Ctrl Pts',(6.28432437072099,-2.65688377194887,1.25590601120793));
#21414=CARTESIAN_POINT('Ctrl Pts',(6.1856529462747,-2.72213483260349,1.26353878577593));
#21415=CARTESIAN_POINT('Ctrl Pts',(6.05922589129334,-2.79608400843386,1.27274709778538));
#21416=CARTESIAN_POINT('Ctrl Pts',(6.03466209627653,-2.81002171913176,1.27451103026261));
#21417=CARTESIAN_POINT('Ctrl Pts',(5.99567005221813,-2.8314735465297,1.27727240294704));
#21418=CARTESIAN_POINT('Ctrl Pts',(5.98136315220221,-2.83920414216325,1.27827753174099));
#21419=CARTESIAN_POINT('Ctrl Pts',(5.95468376549879,-2.85336025318346,1.28013717763507));
#21420=CARTESIAN_POINT('Ctrl Pts',(5.94232697522004,-2.85981438252857,1.2809926923703));
#21421=CARTESIAN_POINT('Ctrl Pts',(5.91485444263773,-2.87393755215874,1.28288212726527));
#21422=CARTESIAN_POINT('Ctrl Pts',(5.8997192276691,-2.88156796678734,1.28391467402853));
#21423=CARTESIAN_POINT('Ctrl Pts',(5.8555827449706,-2.90338437910215,1.28690199436515));
#21424=CARTESIAN_POINT('Ctrl Pts',(5.82642712111742,-2.91725469886676,1.28884580596293));
#21425=CARTESIAN_POINT('Ctrl Pts',(5.60776806123106,-3.01727702066677,1.30321652298663));
#21426=CARTESIAN_POINT('Ctrl Pts',(5.41051693879766,-3.08532944758594,1.31498741028267));
#21427=CARTESIAN_POINT('Ctrl Pts',(4.98481503975404,-3.18742399352355,1.33949496928203));
#21428=CARTESIAN_POINT('Ctrl Pts',(4.75652322532088,-3.21694859947992,1.35214588414229));
#21429=CARTESIAN_POINT('Ctrl Pts',(4.5023938504328,-3.22251730446222,1.36742821714461));
#21430=CARTESIAN_POINT('Ctrl Pts',(4.47771127978986,-3.22277451051547,1.36892536824358));
#21431=CARTESIAN_POINT('Ctrl Pts',(4.44336140790039,-3.22273784447202,1.37102976860697));
#21432=CARTESIAN_POINT('Ctrl Pts',(4.43369400327641,-3.22268402345997,1.37162433012077));
#21433=CARTESIAN_POINT('Ctrl Pts',(4.41606430057242,-3.2225065441803,1.37271301854345));
#21434=CARTESIAN_POINT('Ctrl Pts',(4.40810185569787,-3.22239686929489,1.37320637464648));
#21435=CARTESIAN_POINT('Ctrl Pts',(4.39165632370578,-3.22210938039964,1.37422889590243));
#21436=CARTESIAN_POINT('Ctrl Pts',(4.38317345330773,-3.22192757512915,1.37475826711537));
#21437=CARTESIAN_POINT('Ctrl Pts',(4.36112298766194,-3.22136786222245,1.37613918599357));
#21438=CARTESIAN_POINT('Ctrl Pts',(4.34755704958475,-3.22093774151957,1.37699354788008));
#21439=CARTESIAN_POINT('Ctrl Pts',(4.28835265631089,-3.21868616273685,1.3807418800653));
#21440=CARTESIAN_POINT('Ctrl Pts',(4.24275549244713,-3.2159803717525,1.38367987015236));
#21441=CARTESIAN_POINT('Ctrl Pts',(4.11634734579705,-3.20577915928023,1.3919393466081));
#21442=CARTESIAN_POINT('Ctrl Pts',(4.03574100624826,-3.19619915040328,1.39733604843425));
#21443=CARTESIAN_POINT('Ctrl Pts',(3.68842590158269,-3.14155525492517,1.42093825935699));
#21444=CARTESIAN_POINT('Ctrl Pts',(3.42756459874292,-3.06604909057105,1.43944520159311));
#21445=CARTESIAN_POINT('Ctrl Pts',(3.1114303943461,-2.92957947643918,1.46171457712721));
#21446=CARTESIAN_POINT('Ctrl Pts',(3.04468845325288,-2.89800653130501,1.46641550554881));
#21447=CARTESIAN_POINT('Ctrl Pts',(2.95767602809721,-2.8531241066922,1.47254683047114));
#21448=CARTESIAN_POINT('Ctrl Pts',(2.93639104685182,-2.84184105876041,1.47404696787047));
#21449=CARTESIAN_POINT('Ctrl Pts',(2.9018980398178,-2.82305808483701,1.4764789722661));
#21450=CARTESIAN_POINT('Ctrl Pts',(2.88861329237939,-2.81570174387441,1.47741588535205));
#21451=CARTESIAN_POINT('Ctrl Pts',(2.86307016917397,-2.80132057840447,1.47921798870632));
#21452=CARTESIAN_POINT('Ctrl Pts',(2.85080504454862,-2.79430851672815,1.48008360895036));
#21453=CARTESIAN_POINT('Ctrl Pts',(2.82236678084909,-2.77780108432146,1.48209157391351));
#21454=CARTESIAN_POINT('Ctrl Pts',(2.80622952311672,-2.76824468124391,1.48323168395863));
#21455=CARTESIAN_POINT('Ctrl Pts',(2.75449431872098,-2.73699418156885,1.4868898721696));
#21456=CARTESIAN_POINT('Ctrl Pts',(2.71923270367704,-2.7147495738661,1.48938786126209));
#21457=CARTESIAN_POINT('Ctrl Pts',(2.63714099610603,-2.66070773288696,1.49522257662628));
#21458=CARTESIAN_POINT('Ctrl Pts',(2.5906967986849,-2.6283482705324,1.49853871474661));
#21459=CARTESIAN_POINT('Ctrl Pts',(2.4186052335584,-2.50158386836181,1.51092696304993));
#21460=CARTESIAN_POINT('Ctrl Pts',(2.29906332063943,-2.39925321046001,1.51973031771063));
#21461=CARTESIAN_POINT('Ctrl Pts',(2.04042594866894,-2.14283048916025,1.54009510912807));
#21462=CARTESIAN_POINT('Ctrl Pts',(1.9078016113455,-1.98324427361955,1.5515932836182));
#21463=CARTESIAN_POINT('Ctrl Pts',(1.77688408952507,-1.79070084398704,1.56556645303265));
#21464=CARTESIAN_POINT('Ctrl Pts',(1.76261183642913,-1.76915750819852,1.56713150115008));
#21465=CARTESIAN_POINT('Ctrl Pts',(1.74309700717423,-1.73891703159205,1.56933404914046));
#21466=CARTESIAN_POINT('Ctrl Pts',(1.73763371297858,-1.73036258879075,1.56995773193926));
#21467=CARTESIAN_POINT('Ctrl Pts',(1.72828032993332,-1.71556337469762,1.57103803908136));
#21468=CARTESIAN_POINT('Ctrl Pts',(1.72437100834903,-1.70933076749649,1.57149340956568));
#21469=CARTESIAN_POINT('Ctrl Pts',(1.71618499225832,-1.69618002829124,1.57245520842259));
#21470=CARTESIAN_POINT('Ctrl Pts',(1.71191310956421,-1.68925903581498,1.57296195566111));
#21471=CARTESIAN_POINT('Ctrl Pts',(1.70142952859197,-1.67212956678769,1.57421741888454));
#21472=CARTESIAN_POINT('Ctrl Pts',(1.6952483656057,-1.66190263658152,1.57496807754542));
#21473=CARTESIAN_POINT('Ctrl Pts',(1.67250840076782,-1.62380156383968,1.57776808880217));
#21474=CARTESIAN_POINT('Ctrl Pts',(1.65631425900738,-1.5957134366868,1.5798389368044));
#21475=CARTESIAN_POINT('Ctrl Pts',(1.54086116826912,-1.38829379280759,1.59515339350298));
#21476=CARTESIAN_POINT('Ctrl Pts',(1.45849505369408,-1.20011230603677,1.60913454978702));
#21477=CARTESIAN_POINT('Ctrl Pts',(1.32983823276182,-0.808292809777138,
1.63698809362539));
#21478=CARTESIAN_POINT('Ctrl Pts',(1.28429097750638,-0.605367708302494,
1.65078410453559));
#21479=CARTESIAN_POINT('Ctrl Pts',(1.25338928457226,-0.357971930268893,
1.66660968803264));
#21480=CARTESIAN_POINT('Ctrl Pts',(1.24901623065826,-0.316402530620074,
1.66923765898355));
#21481=CARTESIAN_POINT('Ctrl Pts',(1.24386977488883,-0.256257453817599,
1.67299666990883));
#21482=CARTESIAN_POINT('Ctrl Pts',(1.2424466104044,-0.237743066846545,1.6741479090382));
#21483=CARTESIAN_POINT('Ctrl Pts',(1.24022116562331,-0.205102179782672,
1.6761674520122));
#21484=CARTESIAN_POINT('Ctrl Pts',(1.23935175919098,-0.190980902539523,
1.67703783514015));
#21485=CARTESIAN_POINT('Ctrl Pts',(1.23774534006146,-0.161751815801462,
1.67883271301947));
#21486=CARTESIAN_POINT('Ctrl Pts',(1.23702163822925,-0.146643601406856,
1.67975677029862));
#21487=CARTESIAN_POINT('Ctrl Pts',(1.23543211109036,-0.107729625951668,
1.68212764455932));
#21488=CARTESIAN_POINT('Ctrl Pts',(1.23472380317287,-0.0839180861933661,
1.68356951875863));
#21489=CARTESIAN_POINT('Ctrl Pts',(1.23280957768231,0.0187101694074913,
1.68974821475011));
#21490=CARTESIAN_POINT('Ctrl Pts',(1.23423139400789,0.0975522380866514,
1.69440300411715));
#21491=CARTESIAN_POINT('Ctrl Pts',(1.24609610761348,0.314153016811112,1.70701475805742));
#21492=CARTESIAN_POINT('Ctrl Pts',(1.26250392090779,0.451417090806418,1.71480483617002));
#21493=CARTESIAN_POINT('Ctrl Pts',(1.32749907840671,0.802153790944397,1.73478394794283));
#21494=CARTESIAN_POINT('Ctrl Pts',(1.38909113958491,1.01245919142645,1.74682213063857));
#21495=CARTESIAN_POINT('Ctrl Pts',(1.48550686650785,1.2493541908941,1.76201093224694));
#21496=CARTESIAN_POINT('Ctrl Pts',(1.50013121623719,1.28357646241496,1.76424789018086));
#21497=CARTESIAN_POINT('Ctrl Pts',(1.52066834507762,1.32942132463193,1.76731265456939));
#21498=CARTESIAN_POINT('Ctrl Pts',(1.52606444487834,1.34127390004303,1.76811123459308));
#21499=CARTESIAN_POINT('Ctrl Pts',(1.53469410466658,1.35992835107652,1.76937845264571));
#21500=CARTESIAN_POINT('Ctrl Pts',(1.53787999283507,1.36675230538042,1.76984421182392));
#21501=CARTESIAN_POINT('Ctrl Pts',(1.54449601274022,1.38079474873368,1.770807327498));
#21502=CARTESIAN_POINT('Ctrl Pts',(1.54792908803591,1.38801166868292,1.77130487766316));
#21503=CARTESIAN_POINT('Ctrl Pts',(1.55623926321043,1.40531489049167,1.77250387175784));
#21504=CARTESIAN_POINT('Ctrl Pts',(1.56114216227308,1.41538862600662,1.77320688391706));
#21505=CARTESIAN_POINT('Ctrl Pts',(1.5782640472204,1.45010684370797,1.77564644487831));
#21506=CARTESIAN_POINT('Ctrl Pts',(1.59074558636522,1.47461954760107,1.77739808538057));
#21507=CARTESIAN_POINT('Ctrl Pts',(1.62213579785259,1.53436335348133,1.78173393781648));
#21508=CARTESIAN_POINT('Ctrl Pts',(1.64138897824218,1.56940746230951,1.7843349973596));
#21509=CARTESIAN_POINT('Ctrl Pts',(1.72314204425424,1.71186558948067,1.79512159394847));
#21510=CARTESIAN_POINT('Ctrl Pts',(1.79117483671061,1.81597453069043,1.80350660991975));
#21511=CARTESIAN_POINT('Ctrl Pts',(2.01853885950442,2.12350641620846,1.82937568827534));
#21512=CARTESIAN_POINT('Ctrl Pts',(2.19645937059511,2.31196625724159,1.84674473255027));
#21513=CARTESIAN_POINT('Ctrl Pts',(2.42237089471476,2.49996606705262,1.8653725266059));
#21514=CARTESIAN_POINT('Ctrl Pts',(2.45012183508567,2.52229194606669,1.86761161614946));
#21515=CARTESIAN_POINT('Ctrl Pts',(2.49236499678626,2.55513851678946,1.87094821459012));
#21516=CARTESIAN_POINT('Ctrl Pts',(2.50658339846922,2.56600536634488,1.87205936320115));
#21517=CARTESIAN_POINT('Ctrl Pts',(2.53140058791155,2.58464726991907,1.8739785236849));
#21518=CARTESIAN_POINT('Ctrl Pts',(2.54195767965379,2.59247686890071,1.87478866039092));
#21519=CARTESIAN_POINT('Ctrl Pts',(2.56405965146715,2.60866001418015,1.87647187775748));
#21520=CARTESIAN_POINT('Ctrl Pts',(2.57561265110091,2.61700202895191,1.87734449960534));
#21521=CARTESIAN_POINT('Ctrl Pts',(2.60310246705791,2.63657538604247,1.87940407685979));
#21522=CARTESIAN_POINT('Ctrl Pts',(2.61908673514986,2.64773935910417,1.88058843540739));
#21523=CARTESIAN_POINT('Ctrl Pts',(2.67310743913949,2.6847445250957,1.88454800274269));
#21524=CARTESIAN_POINT('Ctrl Pts',(2.71159643474556,2.70991728285408,1.88729808959648));
#21525=CARTESIAN_POINT('Ctrl Pts',(2.80520640138743,2.76831891875407,1.89382997636857));
#21526=CARTESIAN_POINT('Ctrl Pts',(2.86081035045357,2.80073776514723,1.89758356995579));
#21527=CARTESIAN_POINT('Ctrl Pts',(3.08415071533901,2.92214013477198,1.91223931768102));
#21528=CARTESIAN_POINT('Ctrl Pts',(3.25863645153879,2.99789282083081,1.92275256765801));
#21529=CARTESIAN_POINT('Ctrl Pts',(3.51886224504409,3.08449900862795,1.93812820688402));
#21530=CARTESIAN_POINT('Ctrl Pts',(3.59995567257934,3.10799362183085,1.94288397493816));
#21531=CARTESIAN_POINT('Ctrl Pts',(3.76870892624601,3.14977873825397,1.95286919072498));
#21532=CARTESIAN_POINT('Ctrl Pts',(3.85639348047208,3.1676531372025,1.95810566431655));
#21533=CARTESIAN_POINT('Ctrl Pts',(3.96024328092333,3.18435635069918,1.96448215351545));
#21534=CARTESIAN_POINT('Ctrl Pts',(3.97580531962413,3.18674249657521,1.9654422595561));
#21535=CARTESIAN_POINT('Ctrl Pts',(4.00117414241517,3.19044228074222,1.96701576185162));
#21536=CARTESIAN_POINT('Ctrl Pts',(4.01097079832151,3.19182497991703,1.96762542596179));
#21537=CARTESIAN_POINT('Ctrl Pts',(4.02852864087191,3.19422068466063,1.96872195905145));
#21538=CARTESIAN_POINT('Ctrl Pts',(4.03628732985413,3.19525055304027,1.96920787546485));
#21539=CARTESIAN_POINT('Ctrl Pts',(4.05330045459496,3.19744579311992,1.97027642563613));
#21540=CARTESIAN_POINT('Ctrl Pts',(4.06255609662174,3.19859923987284,1.97085969354372));
#21541=CARTESIAN_POINT('Ctrl Pts',(4.08912396716185,3.20179308973439,1.9725392590116));
#21542=CARTESIAN_POINT('Ctrl Pts',(4.1064476083125,3.20373319116,1.97364090088938));
#21543=CARTESIAN_POINT('Ctrl Pts',(4.2326786308378,3.21683396852926,1.9817111221626));
#21544=CARTESIAN_POINT('Ctrl Pts',(4.34206581741018,3.22257812747055,1.98893501374306));
#21545=CARTESIAN_POINT('Ctrl Pts',(4.69087246143503,3.22311373764159,2.01229276444122));
#21546=CARTESIAN_POINT('Ctrl Pts',(4.92955310009338,3.19681388845523,2.02869410108571));
#21547=CARTESIAN_POINT('Ctrl Pts',(5.26923103824124,3.12047486257552,2.05156072694335));
#21548=CARTESIAN_POINT('Ctrl Pts',(5.37407343638804,3.0912702945058,2.05856257610921));
#21549=CARTESIAN_POINT('Ctrl Pts',(5.50295735169327,3.04823138210278,2.06709721422406));
#21550=CARTESIAN_POINT('Ctrl Pts',(5.5285573998072,3.0393221233745,2.0687889785881));
#21551=CARTESIAN_POINT('Ctrl Pts',(5.56908507983875,3.02464199885521,2.07146235020954));
#21552=CARTESIAN_POINT('Ctrl Pts',(5.58408693988634,3.01908124467358,2.07245086438306));
#21553=CARTESIAN_POINT('Ctrl Pts',(5.61209378344675,3.00846204204178,2.07429451435462));
#21554=CARTESIAN_POINT('Ctrl Pts',(5.62510847361357,3.00343042065004,2.07515052011989));
#21555=CARTESIAN_POINT('Ctrl Pts',(5.65383655843253,2.99210882193038,2.07703859973636));
#21556=CARTESIAN_POINT('Ctrl Pts',(5.66953397654492,2.98577923753363,2.07806931719305));
#21557=CARTESIAN_POINT('Ctrl Pts',(5.71528035578434,2.96691285013587,2.08107082056864));
#21558=CARTESIAN_POINT('Ctrl Pts',(5.74519061721309,2.95404377183853,2.08303037529159));
#21559=CARTESIAN_POINT('Ctrl Pts',(5.81296490668127,2.92365810985191,2.08746740799169));
#21560=CARTESIAN_POINT('Ctrl Pts',(5.85069447942567,2.90585502620798,2.08993515888191));
#21561=CARTESIAN_POINT('Ctrl Pts',(5.97498579920238,2.84422860181653,2.09807036397128));
#21562=CARTESIAN_POINT('Ctrl Pts',(6.05991623655735,2.79722874427635,2.10363704431509));
#21563=CARTESIAN_POINT('Ctrl Pts',(6.22383374807,2.69659516588618,2.1145353227027));
#21564=CARTESIAN_POINT('Ctrl Pts',(6.30276803677694,2.64317303334387,2.11986096441958));
#21565=CARTESIAN_POINT('Ctrl Pts',(6.37918119522423,2.5863672951246,2.12518466390817));
#21566=CARTESIAN_POINT('Ctrl Pts',(5.88688308661327,2.88166464694226,-0.413294290592403));
#21567=CARTESIAN_POINT('Ctrl Pts',(6.84537358445575,2.40588471549031,-0.347122251455184));
#21568=CARTESIAN_POINT('Ctrl Pts',(8.23365752427788,0.430873938343679,-0.214778173180747));
#21569=CARTESIAN_POINT('Ctrl Pts',(6.86376121760315,-2.94715670275194,-0.0162620557690901));
#21570=CARTESIAN_POINT('Ctrl Pts',(3.28608690294124,-3.61718018023642,0.182254061642566));
#21571=CARTESIAN_POINT('Ctrl Pts',(0.781880406995935,-0.979166244321737,
0.380770179054222));
#21572=CARTESIAN_POINT('Ctrl Pts',(1.64193314359211,2.55787552455616,0.579286296465875));
#21573=CARTESIAN_POINT('Ctrl Pts',(5.07993189931123,3.75125370222575,0.777802413877532));
#21574=CARTESIAN_POINT('Ctrl Pts',(7.94674205925474,1.50993542852403,0.976318531289188));
#21575=CARTESIAN_POINT('Ctrl Pts',(7.61734820438694,-2.11448150974993,1.17483464870084));
#21576=CARTESIAN_POINT('Ctrl Pts',(4.39321803491158,-3.80232526959411,1.3733507661125));
#21577=CARTESIAN_POINT('Ctrl Pts',(1.22704502026327,-2.0081611280352,1.57186688352415));
#21578=CARTESIAN_POINT('Ctrl Pts',(1.01829993859556,1.62508529687376,1.77038300093581));
#21579=CARTESIAN_POINT('Ctrl Pts',(3.95817375267475,3.77008527062174,1.96889911834747));
#21580=CARTESIAN_POINT('Ctrl Pts',(7.35437229592725,2.462525507432,2.16741523575912));
#21581=CARTESIAN_POINT('Ctrl Pts',(8.09672865983581,-1.10017486129741,2.36593135317078));
#21582=CARTESIAN_POINT('Ctrl Pts',(5.50540329893836,-3.65535258567839,2.56444747058243));
#21583=CARTESIAN_POINT('Ctrl Pts',(1.95348461951634,-2.8630297341532,2.76296358799409));
#21584=CARTESIAN_POINT('Ctrl Pts',(0.693751175975549,0.551202220257554,
2.96147970540574));
#21585=CARTESIAN_POINT('Ctrl Pts',(2.87984341841113,3.46065318004877,3.1599958228174));
#21586=CARTESIAN_POINT('Ctrl Pts',(6.50977938134639,3.20090403962421,3.35851194022905));
#21587=CARTESIAN_POINT('Ctrl Pts',(8.25933290131072,0.00982773524565914,
3.55702805764071));
#21588=CARTESIAN_POINT('Ctrl Pts',(6.52629607038668,-3.19024855326339,3.75554417505237));
#21589=CARTESIAN_POINT('Ctrl Pts',(2.89775109124319,-3.46875593755042,3.95406029246402));
#21590=CARTESIAN_POINT('Ctrl Pts',(0.69665041333009,-0.570642598253718,
4.15257640987568));
#21591=CARTESIAN_POINT('Ctrl Pts',(1.93872017863753,2.85005436799852,4.35109252728733));
#21592=CARTESIAN_POINT('Ctrl Pts',(5.48649651727959,3.66072576290342,4.54960864469899));
#21593=CARTESIAN_POINT('Ctrl Pts',(8.09099334705098,1.11897413587954,4.74812476211065));
#21594=CARTESIAN_POINT('Ctrl Pts',(7.36706201253862,-2.44751271825679,4.9466408795223));
#21595=CARTESIAN_POINT('Ctrl Pts',(3.97766506003213,-3.7726139823619,5.14515699693396));
#21596=CARTESIAN_POINT('Ctrl Pts',(1.02674774506536,-1.64282712377203,5.34367311434561));
#21597=CARTESIAN_POINT('Ctrl Pts',(1.21670401249677,1.99142956468722,5.54218923175727));
#21598=CARTESIAN_POINT('Ctrl Pts',(4.37357552585394,3.80197293891488,5.74070534916892));
#21599=CARTESIAN_POINT('Ctrl Pts',(7.60635940332531,2.13074181682499,5.93922146658058));
#21600=CARTESIAN_POINT('Ctrl Pts',(7.95453366396254,-1.49178213007847,6.13773758399224));
#21601=CARTESIAN_POINT('Ctrl Pts',(5.09924694286633,-3.74816037897555,6.33625370140389));
#21602=CARTESIAN_POINT('Ctrl Pts',(1.65531650589596,-2.57204465036969,6.53476981881556));
#21603=CARTESIAN_POINT('Ctrl Pts',(0.776628336729841,0.959500643563771,
6.7332859362272));
#21604=CARTESIAN_POINT('Ctrl Pts',(3.26786834626679,3.6123534997611,6.93180205363886));
#21605=CARTESIAN_POINT('Ctrl Pts',(6.84760632218384,2.95708173512582,7.1303181710505));
#21606=CARTESIAN_POINT('Ctrl Pts',(8.23758631997216,-0.406229232878139,
7.32883428846218));
#21607=CARTESIAN_POINT('Ctrl Pts',(6.16489109788061,-3.39752319671194,7.52735040587382));
#21608=CARTESIAN_POINT('Ctrl Pts',(2.52765551345678,-3.27743004474078,7.72586652328549));
#21609=CARTESIAN_POINT('Ctrl Pts',(0.656790727359,-0.155928801126063,7.92438264069713));
#21610=CARTESIAN_POINT('Ctrl Pts',(2.26559912307384,3.10836907247963,8.1228987581088));
#21611=CARTESIAN_POINT('Ctrl Pts',(5.88076457458627,3.52608167695778,8.32141487552045));
#21612=CARTESIAN_POINT('Ctrl Pts',(8.19158732913988,0.714675754863574,8.5199309929321));
#21613=CARTESIAN_POINT('Ctrl Pts',(7.08185986462416,-2.75121662896035,8.71844711034376));
#21614=CARTESIAN_POINT('Ctrl Pts',(3.56784948378791,-3.69759715767183,8.91696322775543));
#21615=CARTESIAN_POINT('Ctrl Pts',(0.867620049835816,-1.2577885451434,9.11547934516706));
#21616=CARTESIAN_POINT('Ctrl Pts',(1.45399031457103,2.33387889135228,9.31399546257875));
#21617=CARTESIAN_POINT('Ctrl Pts',(4.78997354349419,3.78822443423146,9.51251157999037));
#21618=CARTESIAN_POINT('Ctrl Pts',(7.8205397526871,1.77338609991104,9.71102769740205));
#21619=CARTESIAN_POINT('Ctrl Pts',(7.77035405525285,-1.8654854913274,9.90954381481369));
#21620=CARTESIAN_POINT('Ctrl Pts',(4.68537555826851,-3.79598095490491,10.1080599322253));
#21621=CARTESIAN_POINT('Ctrl Pts',(1.39076888675897,-2.25018926719472,10.306576049637));
#21622=CARTESIAN_POINT('Ctrl Pts',(0.903672160428571,1.35628294827392,10.5050921670486));
#21623=CARTESIAN_POINT('Ctrl Pts',(3.67015929568852,3.72069703895061,10.7036082844603));
#21624=CARTESIAN_POINT('Ctrl Pts',(7.156733998233,2.67776755651859,10.902124401872));
#21625=CARTESIAN_POINT('Ctrl Pts',(8.17045747715504,-0.817410517633158,
11.1006405192836));
#21626=CARTESIAN_POINT('Ctrl Pts',(5.78298105352307,-3.56401958853324,11.2991566366953));
#21627=CARTESIAN_POINT('Ctrl Pts',(2.18071022148213,-3.04676731509573,11.4976727541069));
#21628=CARTESIAN_POINT('Ctrl Pts',(0.662536086558379,0.260656509846819,
11.6961888715186));
#21629=CARTESIAN_POINT('Ctrl Pts',(2.61877364278075,3.32937606128419,11.8947049889302));
#21630=CARTESIAN_POINT('Ctrl Pts',(6.25793774774488,3.34911634724554,12.0932211063419));
#21631=CARTESIAN_POINT('Ctrl Pts',(8.24735113836601,0.301799589347462,12.2917372237535));
#21632=CARTESIAN_POINT('Ctrl Pts',(6.76514687416864,-3.02189949163811,12.4902533411652));
#21633=CARTESIAN_POINT('Ctrl Pts',(3.16869942579002,-3.57820050080496,12.6887694585768));
#21634=CARTESIAN_POINT('Ctrl Pts',(0.751566954770839,-0.857653555925328,
12.8872855759885));
#21635=CARTESIAN_POINT('Ctrl Pts',(1.72731339933552,2.64831620117018,13.0858016934002));
#21636=CARTESIAN_POINT('Ctrl Pts',(5.20236872621718,3.72900835754984,13.2843178108118));
#21637=CARTESIAN_POINT('Ctrl Pts',(7.99434336961907,1.39474559334568,13.4828339282235));
#21638=CARTESIAN_POINT('Ctrl Pts',(7.54640006010282,-2.21679865437008,13.6813500456351));
#21639=CARTESIAN_POINT('Ctrl Pts',(4.26875675973819,-3.79824086239538,13.8798661630468));
#21640=CARTESIAN_POINT('Ctrl Pts',(1.16301685561255,-1.9013263388412,14.0783822804584));
#21641=CARTESIAN_POINT('Ctrl Pts',(1.07335787448695,1.73678667876183,14.2768983978701));
#21642=CARTESIAN_POINT('Ctrl Pts',(4.08188780578152,3.78438349314049,14.4754145152818));
#21643=CARTESIAN_POINT('Ctrl Pts',(7.43345216672421,2.36631389110821,14.6739306326934));
#21644=CARTESIAN_POINT('Ctrl Pts',(8.05875206907788,-1.21878096033793,14.8724467501051));
#21645=CARTESIAN_POINT('Ctrl Pts',(5.38514975673243,-3.68773939197872,15.0709628675167));
#21646=CARTESIAN_POINT('Ctrl Pts',(1.86107937002522,-2.77953623668677,15.2694789849284));
#21647=CARTESIAN_POINT('Ctrl Pts',(0.713817534175901,0.674113331777405,
15.46799510234));
#21648=CARTESIAN_POINT('Ctrl Pts',(2.9940048152212,3.5104227339951,15.6665112197517));
#21649=CARTESIAN_POINT('Ctrl Pts',(6.61348907494099,3.13195377174095,15.8650273371633));
#21650=CARTESIAN_POINT('Ctrl Pts',(8.257615478175,-0.114698878595687,16.063543454575));
#21651=CARTESIAN_POINT('Ctrl Pts',(6.42072433944188,-3.25631247771842,16.2620595719866));
#21652=CARTESIAN_POINT('Ctrl Pts',(2.78500562221897,-3.41585705137789,16.4605756893983));
#21653=CARTESIAN_POINT('Ctrl Pts',(0.67998136903583,-0.447224713876356,
16.65909180681));
#21654=CARTESIAN_POINT('Ctrl Pts',(2.03339274915041,2.93096750947701,16.8576079242216));
#21655=CARTESIAN_POINT('Ctrl Pts',(5.60581136526813,3.62503544056518,17.0561240416333));
#21656=CARTESIAN_POINT('Ctrl Pts',(8.12568420335589,0.999364870669326,17.2546401590449));
#21657=CARTESIAN_POINT('Ctrl Pts',(7.28535965135699,-2.54150503784963,17.4531562764566));
#21658=CARTESIAN_POINT('Ctrl Pts',(3.85439094932391,-3.75491297725849,17.6516723938682));
#21659=CARTESIAN_POINT('Ctrl Pts',(0.974793970633971,-1.52964303811135,
17.8501885112799));
#21660=CARTESIAN_POINT('Ctrl Pts',(1.2836488526281,2.09644489844015,18.0487046286916));
#21661=CARTESIAN_POINT('Ctrl Pts',(4.49811216942012,3.80264847561477,18.2472207461032));
#21662=CARTESIAN_POINT('Ctrl Pts',(7.67443956106538,2.02645891285741,18.4457368635149));
#21663=CARTESIAN_POINT('Ctrl Pts',(7.90381082245328,-1.60552317494378,18.6442529809265));
#21664=CARTESIAN_POINT('Ctrl Pts',(4.9761721155001,-3.76719767944954,18.8427690983382));
#21665=CARTESIAN_POINT('Ctrl Pts',(1.57259927845708,-2.47894420875808,19.0412852157498));
#21666=CARTESIAN_POINT('Ctrl Pts',(0.810019572635768,1.07947921368855,19.2398013331615));
#21667=CARTESIAN_POINT('Ctrl Pts',(3.38678898688482,3.6493361063157,19.4383174505731));
#21668=CARTESIAN_POINT('Ctrl Pts',(6.94315110686829,2.87720041011993,19.6368335679848));
#21669=CARTESIAN_POINT('Ctrl Pts',(8.22225715251285,-0.529820690755693,
19.8353496853965));
#21670=CARTESIAN_POINT('Ctrl Pts',(6.05272613795891,-3.45164208273989,20.0338658028081));
#21671=CARTESIAN_POINT('Ctrl Pts',(2.42137329831411,-3.212515309774,20.2323819202198));
#21672=CARTESIAN_POINT('Ctrl Pts',(0.65372248686789,-0.0314281299545405,
20.4308980376314));
#21673=CARTESIAN_POINT('Ctrl Pts',(2.36855469553213,3.178440343651,20.6294141550431));
#21674=CARTESIAN_POINT('Ctrl Pts',(5.99545920128352,3.47755359131801,20.8279302724548));
#21675=CARTESIAN_POINT('Ctrl Pts',(8.21298586010566,0.591989447683331,21.0264463898664));
#21676=CARTESIAN_POINT('Ctrl Pts',(6.99036591797756,-2.83570744333498,21.2249625072781));
#21677=CARTESIAN_POINT('Ctrl Pts',(3.44725150283742,-3.6665172604341,21.4234786246897));
#21678=CARTESIAN_POINT('Ctrl Pts',(0.828359319011244,-1.13960058009792,
21.6219947421014));
#21679=CARTESIAN_POINT('Ctrl Pts',(1.53202116508044,2.43094114262164,21.820510859513));
#21680=CARTESIAN_POINT('Ctrl Pts',(4.91383661347899,3.77527223251319,22.0190269769247));
#21681=CARTESIAN_POINT('Ctrl Pts',(7.87680396956558,1.66228269728872,22.2175430943363));
#21682=CARTESIAN_POINT('Ctrl Pts',(7.7074930081086,-1.97299730385434,22.416059211748));
#21683=CARTESIAN_POINT('Ctrl Pts',(4.56095756308617,-3.80143701374933,22.6145753291597));
#21684=CARTESIAN_POINT('Ctrl Pts',(1.31873095853907,-2.14860623751896,22.8130914465713));
#21685=CARTESIAN_POINT('Ctrl Pts',(0.949990286798536,1.47190262315773,23.011607563983));
#21686=CARTESIAN_POINT('Ctrl Pts',(3.7924065803434,3.74442240079083,23.2101236813946));
#21687=CARTESIAN_POINT('Ctrl Pts',(7.24297719250067,2.58796472414074,23.4086397988063));
#21688=CARTESIAN_POINT('Ctrl Pts',(8.14168123233833,-0.938680920498277,
23.6071559162179));
#21689=CARTESIAN_POINT('Ctrl Pts',(5.66560616055497,-3.60535681683013,23.8056720336296));
#21690=CARTESIAN_POINT('Ctrl Pts',(2.08209581503262,-2.97097481614092,24.0041881510412));
#21691=CARTESIAN_POINT('Ctrl Pts',(0.673241827254791,0.385434817028999,
24.2027042684529));
#21692=CARTESIAN_POINT('Ctrl Pts',(2.72851506381635,3.38643791990783,24.4012203858645));
#21693=CARTESIAN_POINT('Ctrl Pts',(6.36713580394013,3.29091791303403,24.5997365032762));
#21694=CARTESIAN_POINT('Ctrl Pts',(8.25465969525897,0.17151120336101,24.7982954766299));
#21695=CARTESIAN_POINT('Ctrl Pts',(7.19525837483205,-1.99900958588141,24.9306824108463));
#21696=CARTESIAN_POINT('Ctrl Pts',(6.32311239899223,-2.62025147071356,24.9968973059255));
#21697=CARTESIAN_POINT('Ctrl Pts',(5.99341579333084,3.0962819108244,-0.27495920519366));
#21698=CARTESIAN_POINT('Ctrl Pts',(7.02329163031133,2.58506739568259,-0.208787166056442));
#21699=CARTESIAN_POINT('Ctrl Pts',(8.51497056474962,0.462964065771816,-0.0764430877820045));
#21700=CARTESIAN_POINT('Ctrl Pts',(7.04304871618797,-3.16665160770128,0.122073029629653));
#21701=CARTESIAN_POINT('Ctrl Pts',(3.19892054011338,-3.88657631350085,0.320589147041309));
#21702=CARTESIAN_POINT('Ctrl Pts',(0.508208668906595,-1.05209144762919,
0.519105264452963));
#21703=CARTESIAN_POINT('Ctrl Pts',(1.43231541168923,2.74837799923302,0.717621381864618));
#21704=CARTESIAN_POINT('Ctrl Pts',(5.12636543519397,4.03063520713254,0.916137499276276));
#21705=CARTESIAN_POINT('Ctrl Pts',(8.20668654383497,1.62239064105283,1.11465361668793));
#21706=CARTESIAN_POINT('Ctrl Pts',(7.85276047702285,-2.27196140132349,1.31316973409959));
#21707=CARTESIAN_POINT('Ctrl Pts',(4.38850729527858,-4.08551042322263,1.51168585151124));
#21708=CARTESIAN_POINT('Ctrl Pts',(0.986527733847538,-2.15772261402933,
1.7102019689229));
#21709=CARTESIAN_POINT('Ctrl Pts',(0.7622359790706,1.74611650720567,1.90871808633455));
#21710=CARTESIAN_POINT('Ctrl Pts',(3.92106229159746,4.0508692911502,2.10723420374621));
#21711=CARTESIAN_POINT('Ctrl Pts',(7.57019895508782,2.64592661456843,2.30575032115786));
#21712=CARTESIAN_POINT('Ctrl Pts',(8.36784367179503,-1.18211240346562,2.50426643856952));
#21713=CARTESIAN_POINT('Ctrl Pts',(5.58352459826198,-3.92759167890361,2.70278255598118));
#21714=CARTESIAN_POINT('Ctrl Pts',(1.7670702556363,-3.07625912870098,2.90129867339283));
#21715=CARTESIAN_POINT('Ctrl Pts',(0.413515851644582,0.592254017343965,
3.09981479080449));
#21716=CARTESIAN_POINT('Ctrl Pts',(2.76242132641212,3.7183916776686,3.29833090821614));
#21717=CARTESIAN_POINT('Ctrl Pts',(6.66270343294158,3.43929724324088,3.4968470256278));
#21718=CARTESIAN_POINT('Ctrl Pts',(8.54255816261418,0.0105596738669375,
3.69536314303945));
#21719=CARTESIAN_POINT('Ctrl Pts',(6.6804502327146,-3.42784816997514,3.89387926045112));
#21720=CARTESIAN_POINT('Ctrl Pts',(2.78166270604797,-3.72709790290783,4.09239537786277));
#21721=CARTESIAN_POINT('Ctrl Pts',(0.416631015022661,-0.613142253174304,
4.29091149527442));
#21722=CARTESIAN_POINT('Ctrl Pts',(1.75120620592284,3.06231739833558,4.48942761268608));
#21723=CARTESIAN_POINT('Ctrl Pts',(5.56320969933569,3.93336503336498,4.68794373009773));
#21724=CARTESIAN_POINT('Ctrl Pts',(8.36168121106336,1.20231178852842,4.88645984750939));
#21725=CARTESIAN_POINT('Ctrl Pts',(7.58383376163584,-2.62979572036334,5.08497596492104));
#21726=CARTESIAN_POINT('Ctrl Pts',(3.94200524984668,-4.05358633333867,5.2834920823327));
#21727=CARTESIAN_POINT('Ctrl Pts',(0.771312951433223,-1.76517968922739,
5.48200819974436));
#21728=CARTESIAN_POINT('Ctrl Pts',(0.97541656054666,2.13974493679014,5.68052431715601));
#21729=CARTESIAN_POINT('Ctrl Pts',(4.36740187430494,4.08513185206935,5.87904043456767));
#21730=CARTESIAN_POINT('Ctrl Pts',(7.84095326483218,2.28943272461384,6.07755655197932));
#21731=CARTESIAN_POINT('Ctrl Pts',(8.21505844260491,-1.60288534238506,6.27607266939098));
#21732=CARTESIAN_POINT('Ctrl Pts',(5.14711900207072,-4.02731150295548,6.47458878680263));
#21733=CARTESIAN_POINT('Ctrl Pts',(1.44669552446588,-2.76360239669899,6.6731049042143));
#21734=CARTESIAN_POINT('Ctrl Pts',(0.502565441067234,1.03096121515846,6.87162102162594));
#21735=CARTESIAN_POINT('Ctrl Pts',(3.17934512299035,3.88139015713774,7.07013713903761));
#21736=CARTESIAN_POINT('Ctrl Pts',(7.0256906552799,3.17731582507866,7.26865325644925));
#21737=CARTESIAN_POINT('Ctrl Pts',(8.51919196471455,-0.436483900631263,
7.46716937386092));
#21738=CARTESIAN_POINT('Ctrl Pts',(6.2921289615216,-3.65055997294754,7.66568549127257));
#21739=CARTESIAN_POINT('Ctrl Pts',(2.38400358079477,-3.52152266305215,7.86420160868423));
#21740=CARTESIAN_POINT('Ctrl Pts',(0.373802705776339,-0.16754188479758,
8.06271772609589));
#21741=CARTESIAN_POINT('Ctrl Pts',(2.10243005973299,3.33987056457006,8.26123384350753));
#21742=CARTESIAN_POINT('Ctrl Pts',(5.98684159389007,3.78869308197905,8.4597499609192));
#21743=CARTESIAN_POINT('Ctrl Pts',(8.4697671146088,0.767902543495819,8.65826607833084));
#21744=CARTESIAN_POINT('Ctrl Pts',(7.27739066026635,-2.95611853726567,8.85678219574251));
#21745=CARTESIAN_POINT('Ctrl Pts',(3.50166790634439,-3.97298249293629,9.05529831315416));
#21746=CARTESIAN_POINT('Ctrl Pts',(0.600333929022254,-1.35146465571633,
9.25381443056581));
#21747=CARTESIAN_POINT('Ctrl Pts',(1.23037519550738,2.50769880562501,9.45233054797748));
#21748=CARTESIAN_POINT('Ctrl Pts',(4.81481189860833,4.07035940226423,9.65084666538912));
#21749=CARTESIAN_POINT('Ctrl Pts',(8.07108508884113,1.90546228475562,9.84936278280079));
#21750=CARTESIAN_POINT('Ctrl Pts',(8.01716171947454,-2.00442094739626,10.0478789002124));
#21751=CARTESIAN_POINT('Ctrl Pts',(4.70242378644322,-4.07869360405195,10.2463950176241));
#21752=CARTESIAN_POINT('Ctrl Pts',(1.16244523581599,-2.41777624309588,10.4449111350357));
#21753=CARTESIAN_POINT('Ctrl Pts',(0.639071086725107,1.45729461030662,10.6434272524474));
#21754=CARTESIAN_POINT('Ctrl Pts',(3.61159742927608,3.99780278027315,10.841943369859));
#21755=CARTESIAN_POINT('Ctrl Pts',(7.35784118240728,2.87719921033794,11.0404594872707));
#21756=CARTESIAN_POINT('Ctrl Pts',(8.44706357811351,-0.878288666292467,
11.2389756046823));
#21757=CARTESIAN_POINT('Ctrl Pts',(5.88177546561389,-3.82945648915419,11.437491722094));
#21758=CARTESIAN_POINT('Ctrl Pts',(2.01121890138154,-3.27368090323489,11.6360078395057));
#21759=CARTESIAN_POINT('Ctrl Pts',(0.379975961147697,0.280069381853164,
11.8345239569173));
#21760=CARTESIAN_POINT('Ctrl Pts',(2.4819079000476,3.57733745452462,12.033040074329));
#21761=CARTESIAN_POINT('Ctrl Pts',(6.39210543142176,3.59854793451629,12.2315561917406));
#21762=CARTESIAN_POINT('Ctrl Pts',(8.52968403588164,0.324276667717884,12.4300723091523));
#21763=CARTESIAN_POINT('Ctrl Pts',(6.93708988851933,-3.24696100298028,12.6285884265639));
#21764=CARTESIAN_POINT('Ctrl Pts',(3.07279041513639,-3.84469355089646,12.8271045439756));
#21765=CARTESIAN_POINT('Ctrl Pts',(0.475637566686629,-0.921528878727684,
13.0256206613872));
#21766=CARTESIAN_POINT('Ctrl Pts',(1.52405451869475,2.84555441124189,13.2241367787989));
#21767=CARTESIAN_POINT('Ctrl Pts',(5.25792096951678,4.00673309958052,13.4226528962106));
#21768=CARTESIAN_POINT('Ctrl Pts',(8.257833049161,1.4986218314684,13.6211690136222));
#21769=CARTESIAN_POINT('Ctrl Pts',(7.77652833946771,-2.38189880309254,13.8196851310339));
#21770=CARTESIAN_POINT('Ctrl Pts',(4.25477653818775,-4.08112182230083,14.0182012484455));
#21771=CARTESIAN_POINT('Ctrl Pts',(0.917730954110628,-2.04293110781465,
14.2167173658572));
#21772=CARTESIAN_POINT('Ctrl Pts',(0.821394455796449,1.86613705453794,14.4152334832688));
#21773=CARTESIAN_POINT('Ctrl Pts',(4.05399017588675,4.06623240003544,14.6137496006805));
#21774=CARTESIAN_POINT('Ctrl Pts',(7.65516844441363,2.54254946152231,14.8122657180922));
#21775=CARTESIAN_POINT('Ctrl Pts',(8.32703870473431,-1.30955190943392,15.0107818355038));
#21776=CARTESIAN_POINT('Ctrl Pts',(5.45431495277465,-3.96239055204922,15.2092979529155));
#21777=CARTESIAN_POINT('Ctrl Pts',(1.66778295557931,-2.98654729975826,15.4078140703271));
#21778=CARTESIAN_POINT('Ctrl Pts',(0.435076688703739,0.724319159497842,
15.6063301877388));
#21779=CARTESIAN_POINT('Ctrl Pts',(2.88508510279309,3.77186791049719,15.8048463051504));
#21780=CARTESIAN_POINT('Ctrl Pts',(6.77413709632598,3.36521177759866,16.0033624225621));
#21781=CARTESIAN_POINT('Ctrl Pts',(8.54071283123811,-0.123241288109086,
16.2018785399737));
#21782=CARTESIAN_POINT('Ctrl Pts',(6.56701585333057,-3.49883232646441,16.4003946573854));
#21783=CARTESIAN_POINT('Ctrl Pts',(2.66052031127365,-3.67025927509159,16.598910774797));
#21784=CARTESIAN_POINT('Ctrl Pts',(0.398720513058523,-0.480532595324168,
16.7974268922087));
#21785=CARTESIAN_POINT('Ctrl Pts',(1.85292968989636,3.14925669454191,16.9959430096203));
#21786=CARTESIAN_POINT('Ctrl Pts',(5.69141073963082,3.89501660876095,17.194459127032));
#21787=CARTESIAN_POINT('Ctrl Pts',(8.39895573256671,1.07379440374864,17.3929752444437));
#21788=CARTESIAN_POINT('Ctrl Pts',(7.49604646714037,-2.73078829048094,17.5914913618553));
#21789=CARTESIAN_POINT('Ctrl Pts',(3.80955007347359,-4.03456701338995,17.790007479267));
#21790=CARTESIAN_POINT('Ctrl Pts',(0.715489824289806,-1.64356601103751,
17.9885235966786));
#21791=CARTESIAN_POINT('Ctrl Pts',(1.04734724052415,2.25258148028018,18.1870397140903));
#21792=CARTESIAN_POINT('Ctrl Pts',(4.50121361298798,4.08585770060491,18.3855558315019));
#21793=CARTESIAN_POINT('Ctrl Pts',(7.91410381728119,2.1773831599618,18.5840719489136));
#21794=CARTESIAN_POINT('Ctrl Pts',(8.16055792437237,-1.72509746033864,18.7825880663253));
#21795=CARTESIAN_POINT('Ctrl Pts',(5.0148779510323,-4.04776664132528,18.9811041837369));
#21796=CARTESIAN_POINT('Ctrl Pts',(1.35781777968586,-2.66356812881232,19.1796203011486));
#21797=CARTESIAN_POINT('Ctrl Pts',(0.538443550556935,1.1598754095142,19.3781364185603));
#21798=CARTESIAN_POINT('Ctrl Pts',(3.30712259659747,3.92112711119714,19.5766525359719));
#21799=CARTESIAN_POINT('Ctrl Pts',(7.12835131317638,3.09148519177063,19.7751686533836));
#21800=CARTESIAN_POINT('Ctrl Pts',(8.50272112937199,-0.569280059186615,
19.9736847707952));
#21801=CARTESIAN_POINT('Ctrl Pts',(6.17161031033075,-3.70870946234774,20.1722008882069));
#21802=CARTESIAN_POINT('Ctrl Pts',(2.26980580259814,-3.45177328404759,20.3707170056185));
#21803=CARTESIAN_POINT('Ctrl Pts',(0.370505952442893,-0.0337687976193256,
20.5692331230302));
#21804=CARTESIAN_POINT('Ctrl Pts',(2.21305343742525,3.41516052227788,20.7677492404418));
#21805=CARTESIAN_POINT('Ctrl Pts',(6.11007831343283,3.73655077808788,20.9662653578534));
#21806=CARTESIAN_POINT('Ctrl Pts',(8.49275934044528,0.636078948397367,21.1647814752652));
#21807=CARTESIAN_POINT('Ctrl Pts',(7.17908253400595,-3.04690196012391,21.3632975926768));
#21808=CARTESIAN_POINT('Ctrl Pts',(3.37208816940477,-3.93958786330456,21.5618137100885));
#21809=CARTESIAN_POINT('Ctrl Pts',(0.558149183206385,-1.22447442503984,
21.7603298275001));
#21810=CARTESIAN_POINT('Ctrl Pts',(1.31421753683424,2.61198994621562,21.9588459449118));
#21811=CARTESIAN_POINT('Ctrl Pts',(4.94789989808116,4.05644256154919,22.1573620623234));
#21812=CARTESIAN_POINT('Ctrl Pts',(8.13153968654471,1.78608425229248,22.3558781797351));
#21813=CARTESIAN_POINT('Ctrl Pts',(7.94961898046267,-2.11993989949929,22.5543942971467));
#21814=CARTESIAN_POINT('Ctrl Pts',(4.56873953270021,-4.0845560128934,22.7529104145584));
#21815=CARTESIAN_POINT('Ctrl Pts',(1.08504215066615,-2.30862763082918,22.95142653197));
#21816=CARTESIAN_POINT('Ctrl Pts',(0.688838840573486,1.58152527269752,23.1499426493817));
#21817=CARTESIAN_POINT('Ctrl Pts',(3.74294930484078,4.02329513198439,23.3484587667933));
#21818=CARTESIAN_POINT('Ctrl Pts',(7.45050749686758,2.78070814718547,23.546974884205));
#21819=CARTESIAN_POINT('Ctrl Pts',(8.41614416964521,-1.00859090500303,23.7454910016166));
#21820=CARTESIAN_POINT('Ctrl Pts',(5.75565886205016,-3.87387238340306,23.9440071190283));
#21821=CARTESIAN_POINT('Ctrl Pts',(1.90526000600476,-3.19224361880315,24.14252323644));
#21822=CARTESIAN_POINT('Ctrl Pts',(0.391479031532891,0.414140782493564,
24.3410393538516));
#21823=CARTESIAN_POINT('Ctrl Pts',(2.59982251484541,3.6386490998064,24.5395554712633));
#21824=CARTESIAN_POINT('Ctrl Pts',(6.50943621328541,3.53601506509354,24.7380715886749));
#21825=CARTESIAN_POINT('Ctrl Pts',(8.53753691096405,0.184284815040506,24.9366305620286));
#21826=CARTESIAN_POINT('Ctrl Pts',(7.39923473266516,-2.14788949397592,25.069017496245));
#21827=CARTESIAN_POINT('Ctrl Pts',(6.46213408444902,-2.81539950847165,25.1352323913243));
#21828=CARTESIAN_POINT('Ctrl Pts',(6.0999485000484,3.31089917470656,-0.136624119794918));
#21829=CARTESIAN_POINT('Ctrl Pts',(7.2012096761669,2.76425007587486,-0.0704520806576993));
#21830=CARTESIAN_POINT('Ctrl Pts',(8.79628360522135,0.495054193199949,0.061891997616738));
#21831=CARTESIAN_POINT('Ctrl Pts',(7.22233621477278,-3.38614651265062,0.260408115028396));
#21832=CARTESIAN_POINT('Ctrl Pts',(3.11175417728552,-4.15597244676529,0.458924232440051));
#21833=CARTESIAN_POINT('Ctrl Pts',(0.234536930817258,-1.12501665093665,
0.657440349851707));
#21834=CARTESIAN_POINT('Ctrl Pts',(1.22269767978634,2.93888047390986,0.855956467263361));
#21835=CARTESIAN_POINT('Ctrl Pts',(5.17279897107673,4.31001671203934,1.05447258467502));
#21836=CARTESIAN_POINT('Ctrl Pts',(8.46663102841521,1.73484585358162,1.25298870208667));
#21837=CARTESIAN_POINT('Ctrl Pts',(8.08817274965877,-2.42944129289705,1.45150481949833));
#21838=CARTESIAN_POINT('Ctrl Pts',(4.38379655564558,-4.36869557685114,1.65002093690999));
#21839=CARTESIAN_POINT('Ctrl Pts',(0.746010447431816,-2.30728410002347,
1.84853705432164));
#21840=CARTESIAN_POINT('Ctrl Pts',(0.506172019545635,1.86714771753756,2.04705317173329));
#21841=CARTESIAN_POINT('Ctrl Pts',(3.88395083052018,4.33165331167866,2.24556928914495));
#21842=CARTESIAN_POINT('Ctrl Pts',(7.78602561424836,2.82932772170484,2.4440854065566));
#21843=CARTESIAN_POINT('Ctrl Pts',(8.63895868375428,-1.26404994563383,2.64260152396827));
#21844=CARTESIAN_POINT('Ctrl Pts',(5.66164589758561,-4.19983077212884,2.84111764137992));
#21845=CARTESIAN_POINT('Ctrl Pts',(1.58065589175627,-3.28948852324876,3.03963375879158));
#21846=CARTESIAN_POINT('Ctrl Pts',(0.133280527313607,0.633305814430374,
3.23814987620323));
#21847=CARTESIAN_POINT('Ctrl Pts',(2.6449992344131,3.97613017528841,3.43666599361489));
#21848=CARTESIAN_POINT('Ctrl Pts',(6.81562748453676,3.67769044685756,3.63518211102655));
#21849=CARTESIAN_POINT('Ctrl Pts',(8.82578342391765,0.0112916124882134,
3.8336982284382));
#21850=CARTESIAN_POINT('Ctrl Pts',(6.83460439504253,-3.66544778668689,4.03221434584986));
#21851=CARTESIAN_POINT('Ctrl Pts',(2.66557432085276,-3.98543986826524,4.23073046326151));
#21852=CARTESIAN_POINT('Ctrl Pts',(0.13661161671523,-0.655641908094887,
4.42924658067317));
#21853=CARTESIAN_POINT('Ctrl Pts',(1.56369223320815,3.27458042867263,4.62776269808482));
#21854=CARTESIAN_POINT('Ctrl Pts',(5.63992288139177,4.20600430382654,4.82627881549648));
#21855=CARTESIAN_POINT('Ctrl Pts',(8.63236907507575,1.28564944117731,5.02479493290813));
#21856=CARTESIAN_POINT('Ctrl Pts',(7.80060551073305,-2.81207872246989,5.22331105031979));
#21857=CARTESIAN_POINT('Ctrl Pts',(3.90634543966123,-4.33455868431544,5.42182716773146));
#21858=CARTESIAN_POINT('Ctrl Pts',(0.515878157801087,-1.88753225468275,
5.62034328514309));
#21859=CARTESIAN_POINT('Ctrl Pts',(0.734129108596551,2.28806030889307,5.81885940255477));
#21860=CARTESIAN_POINT('Ctrl Pts',(4.36122822275595,4.36829076522382,6.0173755199664));
#21861=CARTESIAN_POINT('Ctrl Pts',(8.07554712633902,2.44812363240269,6.21589163737808));
#21862=CARTESIAN_POINT('Ctrl Pts',(8.47558322124728,-1.71398855469165,6.41440775478972));
#21863=CARTESIAN_POINT('Ctrl Pts',(5.19499106127511,-4.3064626269354,6.61292387220138));
#21864=CARTESIAN_POINT('Ctrl Pts',(1.2380745430358,-2.9551601430283,6.81143998961304));
#21865=CARTESIAN_POINT('Ctrl Pts',(0.228502545404632,1.10242178675316,7.00995610702469));
#21866=CARTESIAN_POINT('Ctrl Pts',(3.09082189971391,4.15042681451437,7.20847222443635));
#21867=CARTESIAN_POINT('Ctrl Pts',(7.20377498837598,3.39754991503151,7.406988341848));
#21868=CARTESIAN_POINT('Ctrl Pts',(8.80079760945692,-0.466738568384383,
7.60550445925966));
#21869=CARTESIAN_POINT('Ctrl Pts',(6.41936682516261,-3.90359674918315,7.80402057667131));
#21870=CARTESIAN_POINT('Ctrl Pts',(2.24035164813274,-3.7656152813635,8.00253669408298));
#21871=CARTESIAN_POINT('Ctrl Pts',(0.0908146841936848,-0.179154968469096,
8.20105281149462));
#21872=CARTESIAN_POINT('Ctrl Pts',(1.93926099639212,3.57137205666049,8.39956892890629));
#21873=CARTESIAN_POINT('Ctrl Pts',(6.09291861319388,4.05130448700034,8.59808504631793));
#21874=CARTESIAN_POINT('Ctrl Pts',(8.7479469000777,0.821129332128062,8.7966011637296));
#21875=CARTESIAN_POINT('Ctrl Pts',(7.47292145590854,-3.16102044557099,8.99511728114126));
#21876=CARTESIAN_POINT('Ctrl Pts',(3.43548632890085,-4.24836782820074,9.19363339855291));
#21877=CARTESIAN_POINT('Ctrl Pts',(0.333047808208697,-1.44514076628925,
9.39214951596456));
#21878=CARTESIAN_POINT('Ctrl Pts',(1.00676007644372,2.68151871989772,9.59066563337622));
#21879=CARTESIAN_POINT('Ctrl Pts',(4.83965025372247,4.352494370297,9.78918175078787));
#21880=CARTESIAN_POINT('Ctrl Pts',(8.32163042499515,2.03753846960017,9.98769786819953));
#21881=CARTESIAN_POINT('Ctrl Pts',(8.26396938369623,-2.14335640346512,10.1862139856111));
#21882=CARTESIAN_POINT('Ctrl Pts',(4.71947201461794,-4.36140625319899,10.3847301030228));
#21883=CARTESIAN_POINT('Ctrl Pts',(0.934121584873003,-2.58536321899705,
10.5832462204345));
#21884=CARTESIAN_POINT('Ctrl Pts',(0.37447001302165,1.5583062723393,10.7817623378461));
#21885=CARTESIAN_POINT('Ctrl Pts',(3.55303556286365,4.27490852159572,10.9802784552578));
#21886=CARTESIAN_POINT('Ctrl Pts',(7.55894836658157,3.07663086415728,11.1787945726694));
#21887=CARTESIAN_POINT('Ctrl Pts',(8.72366967907197,-0.939166814951776,
11.3773106900811));
#21888=CARTESIAN_POINT('Ctrl Pts',(5.98056987770475,-4.09489338977514,11.5758268074927));
#21889=CARTESIAN_POINT('Ctrl Pts',(1.84172758128094,-3.50059449137405,11.7743429249044));
#21890=CARTESIAN_POINT('Ctrl Pts',(0.0974158357370281,0.299482253859507,
11.9728590423161));
#21891=CARTESIAN_POINT('Ctrl Pts',(2.34504215731444,3.82529884776504,12.1713751597277));
#21892=CARTESIAN_POINT('Ctrl Pts',(6.52627311509865,3.84797952178704,12.3698912771394));
#21893=CARTESIAN_POINT('Ctrl Pts',(8.81201693339725,0.346753746088307,12.568407394551));
#21894=CARTESIAN_POINT('Ctrl Pts',(7.10903290287004,-3.47202251432246,12.7669235119627));
#21895=CARTESIAN_POINT('Ctrl Pts',(2.97688140448274,-4.11118660098796,12.9654396293744));
#21896=CARTESIAN_POINT('Ctrl Pts',(0.199708178602426,-0.985404201530036,
13.163955746786));
#21897=CARTESIAN_POINT('Ctrl Pts',(1.32079563805398,3.0427926213136,13.3624718641977));
#21898=CARTESIAN_POINT('Ctrl Pts',(5.3134732128164,4.28445784161121,13.5609879816093));
#21899=CARTESIAN_POINT('Ctrl Pts',(8.52132272870291,1.60249806959112,13.759504099021));
#21900=CARTESIAN_POINT('Ctrl Pts',(8.00665661883263,-2.546998951815,13.9580202164326));
#21901=CARTESIAN_POINT('Ctrl Pts',(4.24079631663729,-4.36400278220629,14.1565363338443));
#21902=CARTESIAN_POINT('Ctrl Pts',(0.672445052608722,-2.18453587678811,
14.3550524512559));
#21903=CARTESIAN_POINT('Ctrl Pts',(0.569431037105937,1.99548743031406,14.5535685686676));
#21904=CARTESIAN_POINT('Ctrl Pts',(4.02609254599198,4.3480813069304,14.7520846860792));
#21905=CARTESIAN_POINT('Ctrl Pts',(7.87688472210303,2.7187850319364,14.9506008034909));
#21906=CARTESIAN_POINT('Ctrl Pts',(8.59532534039074,-1.40032285852991,15.1491169209026));
#21907=CARTESIAN_POINT('Ctrl Pts',(5.52348014881688,-4.2370417121197,15.3476330383142));
#21908=CARTESIAN_POINT('Ctrl Pts',(1.47448654113341,-3.19355836282975,15.5461491557259));
#21909=CARTESIAN_POINT('Ctrl Pts',(0.156335843231577,0.774524987218279,
15.7446652731375));
#21910=CARTESIAN_POINT('Ctrl Pts',(2.77616539036498,4.03331308699926,15.9431813905492));
#21911=CARTESIAN_POINT('Ctrl Pts',(6.93478511771097,3.59846978345639,16.1416975079608));
#21912=CARTESIAN_POINT('Ctrl Pts',(8.82381018430121,-0.131783697622486,
16.3402136253725));
#21913=CARTESIAN_POINT('Ctrl Pts',(6.71330736721926,-3.74135217521042,16.5387297427841));
#21914=CARTESIAN_POINT('Ctrl Pts',(2.53603500032833,-3.92466149880528,16.7372458601958));
#21915=CARTESIAN_POINT('Ctrl Pts',(0.117459657081213,-0.513840476771981,
16.9357619776075));
#21916=CARTESIAN_POINT('Ctrl Pts',(1.6724666306423,3.3675458796068,17.1342780950191));
#21917=CARTESIAN_POINT('Ctrl Pts',(5.77701011399349,4.16499777695671,17.3327942124308));
#21918=CARTESIAN_POINT('Ctrl Pts',(8.67222726177754,1.14822393682795,17.5313103298424));
#21919=CARTESIAN_POINT('Ctrl Pts',(7.70673328292373,-2.92007154311226,17.7298264472541));
#21920=CARTESIAN_POINT('Ctrl Pts',(3.76470919762329,-4.31422104952143,17.9283425646657));
#21921=CARTESIAN_POINT('Ctrl Pts',(0.456185677945633,-1.75748898396369,
18.1268586820774));
#21922=CARTESIAN_POINT('Ctrl Pts',(0.811045628420214,2.40871806212022,18.3253747994891));
#21923=CARTESIAN_POINT('Ctrl Pts',(4.50431505655582,4.36906692559506,18.5238909169007));
#21924=CARTESIAN_POINT('Ctrl Pts',(8.153768073497,2.32830740706619,18.7224070343124));
#21925=CARTESIAN_POINT('Ctrl Pts',(8.41730502629147,-1.84467174573349,18.920923151724));
#21926=CARTESIAN_POINT('Ctrl Pts',(5.05358378656449,-4.328335603201,19.1194392691357));
#21927=CARTESIAN_POINT('Ctrl Pts',(1.14303628091464,-2.84819204886657,19.3179553865473));
#21928=CARTESIAN_POINT('Ctrl Pts',(0.266867528478102,1.24027160533984,19.516471503959));
#21929=CARTESIAN_POINT('Ctrl Pts',(3.22745620631011,4.19291811607857,19.7149876213706));
#21930=CARTESIAN_POINT('Ctrl Pts',(7.31355151948446,3.30576997342133,19.9135037387823));
#21931=CARTESIAN_POINT('Ctrl Pts',(8.78318510623113,-0.60873942761753,20.112019856194));
#21932=CARTESIAN_POINT('Ctrl Pts',(6.29049448270258,-3.96577684195559,20.3105359736056));
#21933=CARTESIAN_POINT('Ctrl Pts',(2.11823830688215,-3.69103125832118,20.5090520910173));
#21934=CARTESIAN_POINT('Ctrl Pts',(0.0872894180178925,-0.0361094652841183,
20.7075682084289));
#21935=CARTESIAN_POINT('Ctrl Pts',(2.05755217931839,3.65188070090475,20.9060843258406));
#21936=CARTESIAN_POINT('Ctrl Pts',(6.2246974255821,3.99554796485774,21.1046004432522));
#21937=CARTESIAN_POINT('Ctrl Pts',(8.77253282078492,0.680168449111409,21.3031165606639));
#21938=CARTESIAN_POINT('Ctrl Pts',(7.36779915003431,-3.25809647691284,21.5016326780756));
#21939=CARTESIAN_POINT('Ctrl Pts',(3.29692483597213,-4.21265846617502,21.7001487954872));
#21940=CARTESIAN_POINT('Ctrl Pts',(0.287939047401517,-1.30934826998177,
21.8986649128989));
#21941=CARTESIAN_POINT('Ctrl Pts',(1.09641390858805,2.79303874980958,22.0971810303105));
#21942=CARTESIAN_POINT('Ctrl Pts',(4.98196318268333,4.33761289058522,22.2956971477222));
#21943=CARTESIAN_POINT('Ctrl Pts',(8.38627540352384,1.90988580729624,22.4942132651338));
#21944=CARTESIAN_POINT('Ctrl Pts',(8.19174495281671,-2.26688249514424,22.6927293825455));
#21945=CARTESIAN_POINT('Ctrl Pts',(4.57652150231426,-4.36767501203749,22.8912454999571));
#21946=CARTESIAN_POINT('Ctrl Pts',(0.851353342793238,-2.46864902413938,
23.0897616173688));
#21947=CARTESIAN_POINT('Ctrl Pts',(0.42768739434844,1.69114792223732,23.2882777347804));
#21948=CARTESIAN_POINT('Ctrl Pts',(3.69349202933814,4.30216786317793,23.4867938521921));
#21949=CARTESIAN_POINT('Ctrl Pts',(7.65803780123451,2.9734515702302,23.6853099696038));
#21950=CARTESIAN_POINT('Ctrl Pts',(8.6906071069521,-1.07850088950778,23.8838260870154));
#21951=CARTESIAN_POINT('Ctrl Pts',(5.84571156354535,-4.14238794997599,24.0823422044271));
#21952=CARTESIAN_POINT('Ctrl Pts',(1.7284241969769,-3.41351242146536,24.2808583218387));
#21953=CARTESIAN_POINT('Ctrl Pts',(0.109716235810993,0.442846747958131,
24.4793744392504));
#21954=CARTESIAN_POINT('Ctrl Pts',(2.47112996587446,3.89086027970496,24.677890556662));
#21955=CARTESIAN_POINT('Ctrl Pts',(6.6517366226307,3.78111221715306,24.8764066740737));
#21956=CARTESIAN_POINT('Ctrl Pts',(8.82041412666913,0.197058426719993,25.0749656474274));
#21957=CARTESIAN_POINT('Ctrl Pts',(7.60321109049825,-2.29676940207044,25.2073525816438));
#21958=CARTESIAN_POINT('Ctrl Pts',(6.60115576990582,-3.01054754622974,25.273567476723));
#21959=CARTESIAN_POINT('Ctrl Pts',(6.20648120676596,3.5255164385887,0.00171096560382468));
#21960=CARTESIAN_POINT('Ctrl Pts',(7.37912772202248,2.94343275606714,0.0678830047410433));
#21961=CARTESIAN_POINT('Ctrl Pts',(9.07759664569311,0.527144320628084,0.200227083015481));
#21962=CARTESIAN_POINT('Ctrl Pts',(7.40162371335757,-3.60564141759996,0.398743200427137));
#21963=CARTESIAN_POINT('Ctrl Pts',(3.02458781445768,-4.42536858002973,0.597259317838794));
#21964=CARTESIAN_POINT('Ctrl Pts',(-0.0391348072720899,-1.19794185424409,
0.795775435250448));
#21965=CARTESIAN_POINT('Ctrl Pts',(1.01307994788347,3.12938294858669,0.994291552662105));
#21966=CARTESIAN_POINT('Ctrl Pts',(5.21923250695947,4.58939821694615,1.19280767007376));
#21967=CARTESIAN_POINT('Ctrl Pts',(8.72657551299543,1.84730106611042,1.39132378748542));
#21968=CARTESIAN_POINT('Ctrl Pts',(8.32358502229467,-2.58692118447061,1.58983990489707));
#21969=CARTESIAN_POINT('Ctrl Pts',(4.37908581601258,-4.65188073047965,1.78835602230873));
#21970=CARTESIAN_POINT('Ctrl Pts',(0.505493161016087,-2.45684558601761,
1.98687213972038));
#21971=CARTESIAN_POINT('Ctrl Pts',(0.250108060020668,1.98817892786946,2.18538825713204));
#21972=CARTESIAN_POINT('Ctrl Pts',(3.8468393694429,4.61243733220712,2.38390437454369));
#21973=CARTESIAN_POINT('Ctrl Pts',(8.0018522734089,3.01272882884126,2.58242049195535));
#21974=CARTESIAN_POINT('Ctrl Pts',(8.91007369571349,-1.34598748780205,2.78093660936701));
#21975=CARTESIAN_POINT('Ctrl Pts',(5.73976719690925,-4.47206986535408,2.97945272677866));
#21976=CARTESIAN_POINT('Ctrl Pts',(1.39424152787623,-3.50271791779653,3.17796884419032));
#21977=CARTESIAN_POINT('Ctrl Pts',(-0.146954797017362,0.674357611516781,
3.37648496160198));
#21978=CARTESIAN_POINT('Ctrl Pts',(2.5275771424141,4.23386867290823,3.57500107901363));
#21979=CARTESIAN_POINT('Ctrl Pts',(6.96855153613195,3.91608365047424,3.77351719642529));
#21980=CARTESIAN_POINT('Ctrl Pts',(9.10900868522111,0.0120235511094912,
3.97203331383693));
#21981=CARTESIAN_POINT('Ctrl Pts',(6.98875855737045,-3.90304740339865,4.17054943124861));
#21982=CARTESIAN_POINT('Ctrl Pts',(2.54948593565754,-4.24378183362265,4.36906554866025));
#21983=CARTESIAN_POINT('Ctrl Pts',(-0.143407781592193,-0.698141563015474,
4.56758166607191));
#21984=CARTESIAN_POINT('Ctrl Pts',(1.37617826049345,3.48684345900968,4.76609778348356));
#21985=CARTESIAN_POINT('Ctrl Pts',(5.71663606344787,4.47864357428809,4.96461390089523));
#21986=CARTESIAN_POINT('Ctrl Pts',(8.90305693908813,1.36898709382619,5.16313001830687));
#21987=CARTESIAN_POINT('Ctrl Pts',(8.01737725983028,-2.99436172457643,5.36164613571854));
#21988=CARTESIAN_POINT('Ctrl Pts',(3.87068562947579,-4.61553103529222,5.56016225313019));
#21989=CARTESIAN_POINT('Ctrl Pts',(0.260443364168955,-2.00988482013811,
5.75867837054185));
#21990=CARTESIAN_POINT('Ctrl Pts',(0.492841656646439,2.436375680996,5.95719448795349));
#21991=CARTESIAN_POINT('Ctrl Pts',(4.35505457120696,4.6514496783783,6.15571060536516));
#21992=CARTESIAN_POINT('Ctrl Pts',(8.31014098784587,2.60681454019155,6.35422672277681));
#21993=CARTESIAN_POINT('Ctrl Pts',(8.73610799988966,-1.82509176699825,6.55274284018847));
#21994=CARTESIAN_POINT('Ctrl Pts',(5.24286312047947,-4.58561375091533,6.75125895760012));
#21995=CARTESIAN_POINT('Ctrl Pts',(1.02945356160573,-3.14671788935761,6.94977507501179));
#21996=CARTESIAN_POINT('Ctrl Pts',(-0.0455603502579819,1.17388235834786,
7.14829119242343));
#21997=CARTESIAN_POINT('Ctrl Pts',(3.00229867643747,4.41946347189101,7.34680730983509));
#21998=CARTESIAN_POINT('Ctrl Pts',(7.38185932147204,3.61778400498435,7.54532342724674));
#21999=CARTESIAN_POINT('Ctrl Pts',(9.08240325419932,-0.496993236137507,
7.7438395446584));
#22000=CARTESIAN_POINT('Ctrl Pts',(6.5466046888036,-4.15663352541875,7.94235566207006));
#22001=CARTESIAN_POINT('Ctrl Pts',(2.09669971547073,-4.00970789967487,8.1408717794817));
#22002=CARTESIAN_POINT('Ctrl Pts',(-0.192173337388976,-0.19076805214061,
8.33938789689338));
#22003=CARTESIAN_POINT('Ctrl Pts',(1.77609193305126,3.80287354875093,8.53790401430502));
#22004=CARTESIAN_POINT('Ctrl Pts',(6.1989956324977,4.3139158920216,8.73642013171668));
#22005=CARTESIAN_POINT('Ctrl Pts',(9.0261266855466,0.874356120760312,8.93493624912834));
#22006=CARTESIAN_POINT('Ctrl Pts',(7.66845225155073,-3.36592235387631,9.13345236653999));
#22007=CARTESIAN_POINT('Ctrl Pts',(3.36930475145732,-4.52375316346519,9.33196848395166));
#22008=CARTESIAN_POINT('Ctrl Pts',(0.0657616873951493,-1.53881687686219,
9.53048460136329));
#22009=CARTESIAN_POINT('Ctrl Pts',(0.783144957380055,2.85533863417045,9.72900071877498));
#22010=CARTESIAN_POINT('Ctrl Pts',(4.86448860883662,4.63462933832978,9.92751683618659));
#22011=CARTESIAN_POINT('Ctrl Pts',(8.57217576114917,2.16961465444475,10.1260329535983));
#22012=CARTESIAN_POINT('Ctrl Pts',(8.51077704791793,-2.28229185953398,10.3245490710099));
#22013=CARTESIAN_POINT('Ctrl Pts',(4.73652024279266,-4.644118902346,10.5230651884216));
#22014=CARTESIAN_POINT('Ctrl Pts',(0.705797933930029,-2.75295019489822,
10.7215813058332));
#22015=CARTESIAN_POINT('Ctrl Pts',(0.109868939318185,1.65931793437198,10.9200974232449));
#22016=CARTESIAN_POINT('Ctrl Pts',(3.49447369645122,4.55201426291826,11.1186135406565));
#22017=CARTESIAN_POINT('Ctrl Pts',(7.76005555075585,3.27606251797663,11.3171296580682));
#22018=CARTESIAN_POINT('Ctrl Pts',(9.00027578003045,-1.00004496361109,11.5156457754798));
#22019=CARTESIAN_POINT('Ctrl Pts',(6.07936428979557,-4.36033029039609,11.7141618928915));
#22020=CARTESIAN_POINT('Ctrl Pts',(1.67223626118035,-3.72750807951321,11.9126780103032));
#22021=CARTESIAN_POINT('Ctrl Pts',(-0.185144289673645,0.31889512586586,
12.1111941277148));
#22022=CARTESIAN_POINT('Ctrl Pts',(2.20817641458127,4.07326024100545,12.3097102451265));
#22023=CARTESIAN_POINT('Ctrl Pts',(6.66044079877556,4.09741110905781,12.5082263625381));
#22024=CARTESIAN_POINT('Ctrl Pts',(9.09434983091284,0.369230824458725,12.7067424799498));
#22025=CARTESIAN_POINT('Ctrl Pts',(7.28097591722075,-3.69708402566464,12.9052585973614));
#22026=CARTESIAN_POINT('Ctrl Pts',(2.8809723938291,-4.37767965107946,13.1037747147731));
#22027=CARTESIAN_POINT('Ctrl Pts',(-0.0762212094817758,-1.04927952433239,
13.3022908321848));
#22028=CARTESIAN_POINT('Ctrl Pts',(1.11753675741321,3.24003083138531,13.5008069495964));
#22029=CARTESIAN_POINT('Ctrl Pts',(5.369025456116,4.5621825836419,13.6993230670081));
#22030=CARTESIAN_POINT('Ctrl Pts',(8.78481240824481,1.70637430771384,13.8978391844197));
#22031=CARTESIAN_POINT('Ctrl Pts',(8.23678489819753,-2.71209910053747,14.0963553018314));
#22032=CARTESIAN_POINT('Ctrl Pts',(4.22681609508684,-4.64688374211174,14.294871419243));
#22033=CARTESIAN_POINT('Ctrl Pts',(0.427159151106815,-2.32614064576156,
14.4933875366547));
#22034=CARTESIAN_POINT('Ctrl Pts',(0.317467618415429,2.12483780609018,14.6919036540663));
#22035=CARTESIAN_POINT('Ctrl Pts',(3.99819491609722,4.62993021382537,14.890419771478));
#22036=CARTESIAN_POINT('Ctrl Pts',(8.09860099979244,2.8950206023505,15.0889358888896));
#22037=CARTESIAN_POINT('Ctrl Pts',(8.86361197604717,-1.49109380762589,15.2874520063013));
#22038=CARTESIAN_POINT('Ctrl Pts',(5.59264534485911,-4.5116928721902,15.485968123713));
#22039=CARTESIAN_POINT('Ctrl Pts',(1.2811901266875,-3.40056942590122,15.6844842411246));
#22040=CARTESIAN_POINT('Ctrl Pts',(-0.122405002240585,0.824730814938715,
15.8830003585363));
#22041=CARTESIAN_POINT('Ctrl Pts',(2.66724567793686,4.29475826350135,16.0815164759479));
#22042=CARTESIAN_POINT('Ctrl Pts',(7.09543313909595,3.83172778931411,16.2800325933596));
#22043=CARTESIAN_POINT('Ctrl Pts',(9.10690753736432,-0.140326107135887,
16.4785487107712));
#22044=CARTESIAN_POINT('Ctrl Pts',(6.85959888110794,-3.98387202395643,16.6770648281829));
#22045=CARTESIAN_POINT('Ctrl Pts',(2.41154968938301,-4.179063722519,16.8755809455945));
#22046=CARTESIAN_POINT('Ctrl Pts',(-0.163801198896094,-0.547148358219792,
17.0740970630062));
#22047=CARTESIAN_POINT('Ctrl Pts',(1.49200357138825,3.5858350646717,17.2726131804178));
#22048=CARTESIAN_POINT('Ctrl Pts',(5.86260948835618,4.43497894515246,17.4711292978295));
#22049=CARTESIAN_POINT('Ctrl Pts',(8.94549879098837,1.22265346990726,17.6696454152412));
#22050=CARTESIAN_POINT('Ctrl Pts',(7.91742009870712,-3.10935479574357,17.8681615326528));
#22051=CARTESIAN_POINT('Ctrl Pts',(3.71986832177296,-4.59387508565289,18.0666776500645));
#22052=CARTESIAN_POINT('Ctrl Pts',(0.196881531601468,-1.87141195688986,
18.2651937674761));
#22053=CARTESIAN_POINT('Ctrl Pts',(0.574744016316265,2.56485464396025,18.4637098848878));
#22054=CARTESIAN_POINT('Ctrl Pts',(4.50741650012369,4.6522761505852,18.6622260022994));
#22055=CARTESIAN_POINT('Ctrl Pts',(8.3934323297128,2.47923165417059,18.8607421197111));
#22056=CARTESIAN_POINT('Ctrl Pts',(8.67405212821057,-1.96424603112833,19.0592582371228));
#22057=CARTESIAN_POINT('Ctrl Pts',(5.09228962209667,-4.60890456507674,19.2577743545344));
#22058=CARTESIAN_POINT('Ctrl Pts',(0.928254782143413,-3.0328159689208,19.4562904719461));
#22059=CARTESIAN_POINT('Ctrl Pts',(-0.00470849360073685,1.32066780116548,
19.6548065893577));
#22060=CARTESIAN_POINT('Ctrl Pts',(3.14778981602278,4.46470912096001,19.8533227067694));
#22061=CARTESIAN_POINT('Ctrl Pts',(7.49875172579254,3.52005475507203,20.051838824181));
#22062=CARTESIAN_POINT('Ctrl Pts',(9.06364908309027,-0.648198796048447,
20.2503549415927));
#22063=CARTESIAN_POINT('Ctrl Pts',(6.4093786550744,-4.22284422156345,20.4488710590044));
#22064=CARTESIAN_POINT('Ctrl Pts',(1.96667081116617,-3.93028923259476,20.647387176416));
#22065=CARTESIAN_POINT('Ctrl Pts',(-0.195927116407106,-0.0384501329489085,
20.8459032938277));
#22066=CARTESIAN_POINT('Ctrl Pts',(1.90205092121151,3.88860087953163,21.0444194112393));
#22067=CARTESIAN_POINT('Ctrl Pts',(6.3393165377314,4.25454515162759,21.242935528651));
#22068=CARTESIAN_POINT('Ctrl Pts',(9.05230630112455,0.724257949825445,21.4414516460626));
#22069=CARTESIAN_POINT('Ctrl Pts',(7.55651576606266,-3.46929099370176,21.6399677634743));
#22070=CARTESIAN_POINT('Ctrl Pts',(3.22176150253947,-4.48572906904549,21.838483880886));
#22071=CARTESIAN_POINT('Ctrl Pts',(0.0177289115966501,-1.39422211492368,
22.0369999982976));
#22072=CARTESIAN_POINT('Ctrl Pts',(0.878610280341868,2.97408755340353,22.2355161157093));
#22073=CARTESIAN_POINT('Ctrl Pts',(5.01602646728549,4.61878321962123,22.4340322331209));
#22074=CARTESIAN_POINT('Ctrl Pts',(8.64101112050298,2.03368736229999,22.6325483505326));
#22075=CARTESIAN_POINT('Ctrl Pts',(8.43387092517075,-2.41382509078919,22.8310644679442));
#22076=CARTESIAN_POINT('Ctrl Pts',(4.58430347192829,-4.65079401118156,23.0295805853559));
#22077=CARTESIAN_POINT('Ctrl Pts',(0.617664534920323,-2.6286704174496,23.2280967027675));
#22078=CARTESIAN_POINT('Ctrl Pts',(0.166535948123391,1.80077057177711,23.4266128201792));
#22079=CARTESIAN_POINT('Ctrl Pts',(3.64403475383551,4.58104059437149,23.6251289375908));
#22080=CARTESIAN_POINT('Ctrl Pts',(7.86556810560143,3.16619499327494,23.8236450550025));
#22081=CARTESIAN_POINT('Ctrl Pts',(8.96507004425898,-1.14841087401253,24.0221611724142));
#22082=CARTESIAN_POINT('Ctrl Pts',(5.93576426504054,-4.41090351654891,24.2206772898258));
#22083=CARTESIAN_POINT('Ctrl Pts',(1.55158838794904,-3.63478122412758,24.4191934072375));
#22084=CARTESIAN_POINT('Ctrl Pts',(-0.172046559910909,0.471552713422697,
24.6177095246491));
#22085=CARTESIAN_POINT('Ctrl Pts',(2.34243741690352,4.14307145960353,24.8162256420608));
#22086=CARTESIAN_POINT('Ctrl Pts',(6.79403703197597,4.02620936921257,25.0147417594724));
#22087=CARTESIAN_POINT('Ctrl Pts',(9.10329134237422,0.209832038399488,25.2133007328261));
#22088=CARTESIAN_POINT('Ctrl Pts',(7.80718744833136,-2.44564931016495,25.3456876670425));
#22089=CARTESIAN_POINT('Ctrl Pts',(6.7401774553626,-3.20569558398784,25.4119025621217));
#22090=CARTESIAN_POINT('Ctrl Pts',(6.20927333103823,3.52819356681411,25.));
#22091=CARTESIAN_POINT('Ctrl Pts',(6.28261154412738,3.4838260879241,25.0000000000001));
#22092=CARTESIAN_POINT('Ctrl Pts',(6.35424941973236,3.43697508500066,25.0000000000001));
#22093=CARTESIAN_POINT('Ctrl Pts',(6.42404893624125,3.38764089866559,25.0000000000001));
#22094=CARTESIAN_POINT('Ctrl Pts',(6.52206241532727,3.3183651288261,25.));
#22095=CARTESIAN_POINT('Ctrl Pts',(6.61645276431289,3.24419440233525,25.));
#22096=CARTESIAN_POINT('Ctrl Pts',(6.70706507635195,3.16554216285713,25.));
#22097=CARTESIAN_POINT('Ctrl Pts',(6.80025007628785,3.08465680891572,25.));
#22098=CARTESIAN_POINT('Ctrl Pts',(6.88944003016716,2.99903106588321,25.));
#22099=CARTESIAN_POINT('Ctrl Pts',(6.97442221394972,2.90907978105801,25.));
#22100=CARTESIAN_POINT('Ctrl Pts',(7.05940439773228,2.81912849623282,25.));
#22101=CARTESIAN_POINT('Ctrl Pts',(7.14017919450627,2.72485071100732,25.));
#22102=CARTESIAN_POINT('Ctrl Pts',(7.21648332556474,2.62664039331786,25.));
#22103=CARTESIAN_POINT('Ctrl Pts',(7.2390189568644,2.59763499769156,25.));
#22104=CARTESIAN_POINT('Ctrl Pts',(7.26116427578476,2.56828649887293,25.));
#22105=CARTESIAN_POINT('Ctrl Pts',(7.28291158066946,2.53860488576137,25.));
#22106=CARTESIAN_POINT('Ctrl Pts',(7.29537914461769,2.52158864344917,25.));
#22107=CARTESIAN_POINT('Ctrl Pts',(7.30771776574352,2.50446012174108,25.));
#22108=CARTESIAN_POINT('Ctrl Pts',(7.31991133794954,2.48724223290588,25.));
#22109=CARTESIAN_POINT('Ctrl Pts',(7.3892179063549,2.38937814761646,25.));
#22110=CARTESIAN_POINT('Ctrl Pts',(7.45393979874638,2.28849903006182,25.));
#22111=CARTESIAN_POINT('Ctrl Pts',(7.51391284145599,2.18499970732938,25.));
#22112=CARTESIAN_POINT('Ctrl Pts',(7.57376716649844,2.08170526328231,25.));
#22113=CARTESIAN_POINT('Ctrl Pts',(7.6288917223817,1.97580008382021,25.));
#22114=CARTESIAN_POINT('Ctrl Pts',(7.67907542985071,1.86765710889506,25.));
#22115=CARTESIAN_POINT('Ctrl Pts',(7.72818555256263,1.76182764676762,25.));
#22116=CARTESIAN_POINT('Ctrl Pts',(7.77256407814287,1.65385429361903,25.));
#22117=CARTESIAN_POINT('Ctrl Pts',(7.81196451615951,1.5440804949319,25.));
#22118=CARTESIAN_POINT('Ctrl Pts',(7.84315387284692,1.45718363960404,25.));
#22119=CARTESIAN_POINT('Ctrl Pts',(7.87122292435585,1.36915832449176,25.));
#22120=CARTESIAN_POINT('Ctrl Pts',(7.89602624090641,1.28017705305137,25.));
#22121=CARTESIAN_POINT('Ctrl Pts',(7.90166022982024,1.25996526017227,25.));
#22122=CARTESIAN_POINT('Ctrl Pts',(7.90712563430273,1.2397041612825,25.));
#22123=CARTESIAN_POINT('Ctrl Pts',(7.91242059476302,1.21939581318014,25.));
#22124=CARTESIAN_POINT('Ctrl Pts',(7.91644877919605,1.2039460714304,25.));
#22125=CARTESIAN_POINT('Ctrl Pts',(7.92037774257214,1.18847099664305,25.));
#22126=CARTESIAN_POINT('Ctrl Pts',(7.92420415205769,1.1729825292745,25.));
#22127=CARTESIAN_POINT('Ctrl Pts',(7.95174043373912,1.06152169323888,25.));
#22128=CARTESIAN_POINT('Ctrl Pts',(7.97401184054752,0.949208236392413,25.));
#22129=CARTESIAN_POINT('Ctrl Pts',(7.99082766139777,0.836380380640087,25.));
#22130=CARTESIAN_POINT('Ctrl Pts',(8.00740128583895,0.725177572023492,25.));
#22131=CARTESIAN_POINT('Ctrl Pts',(8.01867545985289,0.613474332036543,25.));
#22132=CARTESIAN_POINT('Ctrl Pts',(8.02441717531606,0.501595548678134,25.));
#22133=CARTESIAN_POINT('Ctrl Pts',(8.03015889077922,0.389716765319841,25.));
#22134=CARTESIAN_POINT('Ctrl Pts',(8.03036837961706,0.277661727596636,25.));
#22135=CARTESIAN_POINT('Ctrl Pts',(8.02475908266942,0.165767231301056,25.));
#22136=CARTESIAN_POINT('Ctrl Pts',(8.02123118697422,0.0953926165353414,
25.));
#22137=CARTESIAN_POINT('Ctrl Pts',(8.01540028668034,0.0250817784959784,
25.));
#22138=CARTESIAN_POINT('Ctrl Pts',(8.00730734899356,-0.0450760163560306,
25.));
#22139=CARTESIAN_POINT('Ctrl Pts',(8.00445998309532,-0.0697598728602317,
25.));
#22140=CARTESIAN_POINT('Ctrl Pts',(8.0013325513392,-0.0944247476893036,
25.));
#22141=CARTESIAN_POINT('Ctrl Pts',(7.99792666298958,-0.119066624073926,
25.));
#22142=CARTESIAN_POINT('Ctrl Pts',(7.99555860106597,-0.136199742721088,
25.));
#22143=CARTESIAN_POINT('Ctrl Pts',(7.99305592559248,-0.15332174198476,25.));
#22144=CARTESIAN_POINT('Ctrl Pts',(7.99041915317417,-0.170431250299178,
25.));
#22145=CARTESIAN_POINT('Ctrl Pts',(7.98799100859738,-0.186187012736873,
25.));
#22146=CARTESIAN_POINT('Ctrl Pts',(7.9854507348484,-0.201921874689769,25.));
#22147=CARTESIAN_POINT('Ctrl Pts',(7.98279921776876,-0.217634511774155,
25.));
#22148=CARTESIAN_POINT('Ctrl Pts',(7.96426655575293,-0.327457297642062,
25.));
#22149=CARTESIAN_POINT('Ctrl Pts',(7.94030270069075,-0.436201906481619,
25.));
#22150=CARTESIAN_POINT('Ctrl Pts',(7.9111583335056,-0.543544308822202,25.));
#22151=CARTESIAN_POINT('Ctrl Pts',(7.88176382174181,-0.651808025385636,
25.));
#22152=CARTESIAN_POINT('Ctrl Pts',(7.84709896318544,-0.758646156812924,
25.));
#22153=CARTESIAN_POINT('Ctrl Pts',(7.80737187366647,-0.863705046597303,
25.));
#22154=CARTESIAN_POINT('Ctrl Pts',(7.76796016818941,-0.967929898507259,
25.));
#22155=CARTESIAN_POINT('Ctrl Pts',(7.72356567274187,-1.07040433957342,25.));
#22156=CARTESIAN_POINT('Ctrl Pts',(7.67435221978444,-1.1707512522537,25.));
#22157=CARTESIAN_POINT('Ctrl Pts',(7.63780678964462,-1.24526789082966,25.));
#22158=CARTESIAN_POINT('Ctrl Pts',(7.59860314278265,-1.3186107266499,25.));
#22159=CARTESIAN_POINT('Ctrl Pts',(7.55679710264817,-1.39061045069194,25.));
#22160=CARTESIAN_POINT('Ctrl Pts',(7.54382354621943,-1.41295393215319,25.));
#22161=CARTESIAN_POINT('Ctrl Pts',(7.53059592920725,-1.43517328189461,25.));
#22162=CARTESIAN_POINT('Ctrl Pts',(7.5171342266019,-1.45723356452538,25.));
#22163=CARTESIAN_POINT('Ctrl Pts',(7.45980912985136,-1.5511747154502,25.));
#22164=CARTESIAN_POINT('Ctrl Pts',(7.39819567619662,-1.6423191515338,25.));
#22165=CARTESIAN_POINT('Ctrl Pts',(7.33247571024972,-1.73031495540587,25.));
#22166=CARTESIAN_POINT('Ctrl Pts',(7.26804518737958,-1.81658425838204,25.));
#22167=CARTESIAN_POINT('Ctrl Pts',(7.19966708766734,-1.89982778265251,25.));
#22168=CARTESIAN_POINT('Ctrl Pts',(7.12748327748908,-1.97967407510293,25.));
#22169=CARTESIAN_POINT('Ctrl Pts',(7.0897166865762,-2.02144967901518,25.));
#22170=CARTESIAN_POINT('Ctrl Pts',(7.05090789035874,-2.06229461737513,25.));
#22171=CARTESIAN_POINT('Ctrl Pts',(7.01107473761725,-2.10215051102057,25.));
#22172=CARTESIAN_POINT('Ctrl Pts',(6.99916885841126,-2.11406318733992,25.));
#22173=CARTESIAN_POINT('Ctrl Pts',(6.98717216270953,-2.12588669985116,25.));
#22174=CARTESIAN_POINT('Ctrl Pts',(6.97509242397457,-2.13761259353056,25.));
#22175=CARTESIAN_POINT('Ctrl Pts',(6.89922337743233,-2.21125925036905,25.));
#22176=CARTESIAN_POINT('Ctrl Pts',(6.8200049496152,-2.28113499295858,25.));
#22177=CARTESIAN_POINT('Ctrl Pts',(6.73758357244001,-2.34689524282683,25.));
#22178=CARTESIAN_POINT('Ctrl Pts',(6.65741395726351,-2.41085891471067,25.));
#22179=CARTESIAN_POINT('Ctrl Pts',(6.5742134611503,-2.47092921323422,25.));
#22180=CARTESIAN_POINT('Ctrl Pts',(6.48809738068911,-2.52674429457259,25.));
#22181=CARTESIAN_POINT('Ctrl Pts',(6.4358172361143,-2.56062902906351,25.));
#22182=CARTESIAN_POINT('Ctrl Pts',(6.3824621897991,-2.59294458138693,25.));
#22183=CARTESIAN_POINT('Ctrl Pts',(6.32805563795715,-2.62360084935064,25.));
#22184=CARTESIAN_POINT('Ctrl Pts',(5.88688308661327,2.88166464694226,-0.413294290592403));
#22185=CARTESIAN_POINT('Ctrl Pts',(6.84537358445575,2.40588471549031,-0.347122251455184));
#22186=CARTESIAN_POINT('Ctrl Pts',(8.23365752427788,0.430873938343679,-0.214778173180747));
#22187=CARTESIAN_POINT('Ctrl Pts',(6.86376121760315,-2.94715670275194,-0.0162620557690901));
#22188=CARTESIAN_POINT('Ctrl Pts',(3.28608690294124,-3.61718018023642,0.182254061642566));
#22189=CARTESIAN_POINT('Ctrl Pts',(0.781880406995935,-0.979166244321737,
0.380770179054222));
#22190=CARTESIAN_POINT('Ctrl Pts',(1.64193314359211,2.55787552455616,0.579286296465875));
#22191=CARTESIAN_POINT('Ctrl Pts',(5.07993189931123,3.75125370222575,0.777802413877532));
#22192=CARTESIAN_POINT('Ctrl Pts',(7.94674205925474,1.50993542852403,0.976318531289188));
#22193=CARTESIAN_POINT('Ctrl Pts',(7.61734820438694,-2.11448150974993,1.17483464870084));
#22194=CARTESIAN_POINT('Ctrl Pts',(4.39321803491158,-3.80232526959411,1.3733507661125));
#22195=CARTESIAN_POINT('Ctrl Pts',(1.22704502026327,-2.0081611280352,1.57186688352415));
#22196=CARTESIAN_POINT('Ctrl Pts',(1.01829993859556,1.62508529687376,1.77038300093581));
#22197=CARTESIAN_POINT('Ctrl Pts',(3.95817375267475,3.77008527062174,1.96889911834747));
#22198=CARTESIAN_POINT('Ctrl Pts',(7.35437229592725,2.462525507432,2.16741523575912));
#22199=CARTESIAN_POINT('Ctrl Pts',(8.09672865983581,-1.10017486129741,2.36593135317078));
#22200=CARTESIAN_POINT('Ctrl Pts',(5.50540329893836,-3.65535258567839,2.56444747058243));
#22201=CARTESIAN_POINT('Ctrl Pts',(1.95348461951634,-2.8630297341532,2.76296358799409));
#22202=CARTESIAN_POINT('Ctrl Pts',(0.693751175975549,0.551202220257554,
2.96147970540574));
#22203=CARTESIAN_POINT('Ctrl Pts',(2.87984341841113,3.46065318004877,3.1599958228174));
#22204=CARTESIAN_POINT('Ctrl Pts',(6.50977938134639,3.20090403962421,3.35851194022905));
#22205=CARTESIAN_POINT('Ctrl Pts',(8.25933290131072,0.00982773524565914,
3.55702805764071));
#22206=CARTESIAN_POINT('Ctrl Pts',(6.52629607038668,-3.19024855326339,3.75554417505237));
#22207=CARTESIAN_POINT('Ctrl Pts',(2.89775109124319,-3.46875593755042,3.95406029246402));
#22208=CARTESIAN_POINT('Ctrl Pts',(0.69665041333009,-0.570642598253718,
4.15257640987568));
#22209=CARTESIAN_POINT('Ctrl Pts',(1.93872017863753,2.85005436799852,4.35109252728733));
#22210=CARTESIAN_POINT('Ctrl Pts',(5.48649651727959,3.66072576290342,4.54960864469899));
#22211=CARTESIAN_POINT('Ctrl Pts',(8.09099334705098,1.11897413587954,4.74812476211065));
#22212=CARTESIAN_POINT('Ctrl Pts',(7.36706201253862,-2.44751271825679,4.9466408795223));
#22213=CARTESIAN_POINT('Ctrl Pts',(3.97766506003213,-3.7726139823619,5.14515699693396));
#22214=CARTESIAN_POINT('Ctrl Pts',(1.02674774506536,-1.64282712377203,5.34367311434561));
#22215=CARTESIAN_POINT('Ctrl Pts',(1.21670401249677,1.99142956468722,5.54218923175727));
#22216=CARTESIAN_POINT('Ctrl Pts',(4.37357552585394,3.80197293891488,5.74070534916892));
#22217=CARTESIAN_POINT('Ctrl Pts',(7.60635940332531,2.13074181682499,5.93922146658058));
#22218=CARTESIAN_POINT('Ctrl Pts',(7.95453366396254,-1.49178213007847,6.13773758399224));
#22219=CARTESIAN_POINT('Ctrl Pts',(5.09924694286633,-3.74816037897555,6.33625370140389));
#22220=CARTESIAN_POINT('Ctrl Pts',(1.65531650589596,-2.57204465036969,6.53476981881556));
#22221=CARTESIAN_POINT('Ctrl Pts',(0.776628336729841,0.959500643563771,
6.7332859362272));
#22222=CARTESIAN_POINT('Ctrl Pts',(3.26786834626679,3.6123534997611,6.93180205363886));
#22223=CARTESIAN_POINT('Ctrl Pts',(6.84760632218384,2.95708173512582,7.1303181710505));
#22224=CARTESIAN_POINT('Ctrl Pts',(8.23758631997216,-0.406229232878139,
7.32883428846218));
#22225=CARTESIAN_POINT('Ctrl Pts',(6.16489109788061,-3.39752319671194,7.52735040587382));
#22226=CARTESIAN_POINT('Ctrl Pts',(2.52765551345678,-3.27743004474078,7.72586652328549));
#22227=CARTESIAN_POINT('Ctrl Pts',(0.656790727359,-0.155928801126063,7.92438264069713));
#22228=CARTESIAN_POINT('Ctrl Pts',(2.26559912307384,3.10836907247963,8.1228987581088));
#22229=CARTESIAN_POINT('Ctrl Pts',(5.88076457458627,3.52608167695778,8.32141487552045));
#22230=CARTESIAN_POINT('Ctrl Pts',(8.19158732913988,0.714675754863574,8.5199309929321));
#22231=CARTESIAN_POINT('Ctrl Pts',(7.08185986462416,-2.75121662896035,8.71844711034376));
#22232=CARTESIAN_POINT('Ctrl Pts',(3.56784948378791,-3.69759715767183,8.91696322775543));
#22233=CARTESIAN_POINT('Ctrl Pts',(0.867620049835816,-1.2577885451434,9.11547934516706));
#22234=CARTESIAN_POINT('Ctrl Pts',(1.45399031457103,2.33387889135228,9.31399546257875));
#22235=CARTESIAN_POINT('Ctrl Pts',(4.78997354349419,3.78822443423146,9.51251157999037));
#22236=CARTESIAN_POINT('Ctrl Pts',(7.8205397526871,1.77338609991104,9.71102769740205));
#22237=CARTESIAN_POINT('Ctrl Pts',(7.77035405525285,-1.8654854913274,9.90954381481369));
#22238=CARTESIAN_POINT('Ctrl Pts',(4.68537555826851,-3.79598095490491,10.1080599322253));
#22239=CARTESIAN_POINT('Ctrl Pts',(1.39076888675897,-2.25018926719472,10.306576049637));
#22240=CARTESIAN_POINT('Ctrl Pts',(0.903672160428571,1.35628294827392,10.5050921670486));
#22241=CARTESIAN_POINT('Ctrl Pts',(3.67015929568852,3.72069703895061,10.7036082844603));
#22242=CARTESIAN_POINT('Ctrl Pts',(7.156733998233,2.67776755651859,10.902124401872));
#22243=CARTESIAN_POINT('Ctrl Pts',(8.17045747715504,-0.817410517633158,
11.1006405192836));
#22244=CARTESIAN_POINT('Ctrl Pts',(5.78298105352307,-3.56401958853324,11.2991566366953));
#22245=CARTESIAN_POINT('Ctrl Pts',(2.18071022148213,-3.04676731509573,11.4976727541069));
#22246=CARTESIAN_POINT('Ctrl Pts',(0.662536086558379,0.260656509846819,
11.6961888715186));
#22247=CARTESIAN_POINT('Ctrl Pts',(2.61877364278075,3.32937606128419,11.8947049889302));
#22248=CARTESIAN_POINT('Ctrl Pts',(6.25793774774488,3.34911634724554,12.0932211063419));
#22249=CARTESIAN_POINT('Ctrl Pts',(8.24735113836601,0.301799589347462,12.2917372237535));
#22250=CARTESIAN_POINT('Ctrl Pts',(6.76514687416864,-3.02189949163811,12.4902533411652));
#22251=CARTESIAN_POINT('Ctrl Pts',(3.16869942579002,-3.57820050080496,12.6887694585768));
#22252=CARTESIAN_POINT('Ctrl Pts',(0.751566954770839,-0.857653555925328,
12.8872855759885));
#22253=CARTESIAN_POINT('Ctrl Pts',(1.72731339933552,2.64831620117018,13.0858016934002));
#22254=CARTESIAN_POINT('Ctrl Pts',(5.20236872621718,3.72900835754984,13.2843178108118));
#22255=CARTESIAN_POINT('Ctrl Pts',(7.99434336961907,1.39474559334568,13.4828339282235));
#22256=CARTESIAN_POINT('Ctrl Pts',(7.54640006010282,-2.21679865437008,13.6813500456351));
#22257=CARTESIAN_POINT('Ctrl Pts',(4.26875675973819,-3.79824086239538,13.8798661630468));
#22258=CARTESIAN_POINT('Ctrl Pts',(1.16301685561255,-1.9013263388412,14.0783822804584));
#22259=CARTESIAN_POINT('Ctrl Pts',(1.07335787448695,1.73678667876183,14.2768983978701));
#22260=CARTESIAN_POINT('Ctrl Pts',(4.08188780578152,3.78438349314049,14.4754145152818));
#22261=CARTESIAN_POINT('Ctrl Pts',(7.43345216672421,2.36631389110821,14.6739306326934));
#22262=CARTESIAN_POINT('Ctrl Pts',(8.05875206907788,-1.21878096033793,14.8724467501051));
#22263=CARTESIAN_POINT('Ctrl Pts',(5.38514975673243,-3.68773939197872,15.0709628675167));
#22264=CARTESIAN_POINT('Ctrl Pts',(1.86107937002522,-2.77953623668677,15.2694789849284));
#22265=CARTESIAN_POINT('Ctrl Pts',(0.713817534175901,0.674113331777405,
15.46799510234));
#22266=CARTESIAN_POINT('Ctrl Pts',(2.9940048152212,3.5104227339951,15.6665112197517));
#22267=CARTESIAN_POINT('Ctrl Pts',(6.61348907494099,3.13195377174095,15.8650273371633));
#22268=CARTESIAN_POINT('Ctrl Pts',(8.257615478175,-0.114698878595687,16.063543454575));
#22269=CARTESIAN_POINT('Ctrl Pts',(6.42072433944188,-3.25631247771842,16.2620595719866));
#22270=CARTESIAN_POINT('Ctrl Pts',(2.78500562221897,-3.41585705137789,16.4605756893983));
#22271=CARTESIAN_POINT('Ctrl Pts',(0.67998136903583,-0.447224713876356,
16.65909180681));
#22272=CARTESIAN_POINT('Ctrl Pts',(2.03339274915041,2.93096750947701,16.8576079242216));
#22273=CARTESIAN_POINT('Ctrl Pts',(5.60581136526813,3.62503544056518,17.0561240416333));
#22274=CARTESIAN_POINT('Ctrl Pts',(8.12568420335589,0.999364870669326,17.2546401590449));
#22275=CARTESIAN_POINT('Ctrl Pts',(7.28535965135699,-2.54150503784963,17.4531562764566));
#22276=CARTESIAN_POINT('Ctrl Pts',(3.85439094932391,-3.75491297725849,17.6516723938682));
#22277=CARTESIAN_POINT('Ctrl Pts',(0.974793970633971,-1.52964303811135,
17.8501885112799));
#22278=CARTESIAN_POINT('Ctrl Pts',(1.2836488526281,2.09644489844015,18.0487046286916));
#22279=CARTESIAN_POINT('Ctrl Pts',(4.49811216942012,3.80264847561477,18.2472207461032));
#22280=CARTESIAN_POINT('Ctrl Pts',(7.67443956106538,2.02645891285741,18.4457368635149));
#22281=CARTESIAN_POINT('Ctrl Pts',(7.90381082245328,-1.60552317494378,18.6442529809265));
#22282=CARTESIAN_POINT('Ctrl Pts',(4.9761721155001,-3.76719767944954,18.8427690983382));
#22283=CARTESIAN_POINT('Ctrl Pts',(1.57259927845708,-2.47894420875808,19.0412852157498));
#22284=CARTESIAN_POINT('Ctrl Pts',(0.810019572635768,1.07947921368855,19.2398013331615));
#22285=CARTESIAN_POINT('Ctrl Pts',(3.38678898688482,3.6493361063157,19.4383174505731));
#22286=CARTESIAN_POINT('Ctrl Pts',(6.94315110686829,2.87720041011993,19.6368335679848));
#22287=CARTESIAN_POINT('Ctrl Pts',(8.22225715251285,-0.529820690755693,
19.8353496853965));
#22288=CARTESIAN_POINT('Ctrl Pts',(6.05272613795891,-3.45164208273989,20.0338658028081));
#22289=CARTESIAN_POINT('Ctrl Pts',(2.42137329831411,-3.212515309774,20.2323819202198));
#22290=CARTESIAN_POINT('Ctrl Pts',(0.65372248686789,-0.0314281299545405,
20.4308980376314));
#22291=CARTESIAN_POINT('Ctrl Pts',(2.36855469553213,3.178440343651,20.6294141550431));
#22292=CARTESIAN_POINT('Ctrl Pts',(5.99545920128352,3.47755359131801,20.8279302724548));
#22293=CARTESIAN_POINT('Ctrl Pts',(8.21298586010566,0.591989447683331,21.0264463898664));
#22294=CARTESIAN_POINT('Ctrl Pts',(6.99036591797756,-2.83570744333498,21.2249625072781));
#22295=CARTESIAN_POINT('Ctrl Pts',(3.44725150283742,-3.6665172604341,21.4234786246897));
#22296=CARTESIAN_POINT('Ctrl Pts',(0.828359319011244,-1.13960058009792,
21.6219947421014));
#22297=CARTESIAN_POINT('Ctrl Pts',(1.53202116508044,2.43094114262164,21.820510859513));
#22298=CARTESIAN_POINT('Ctrl Pts',(4.91383661347899,3.77527223251319,22.0190269769247));
#22299=CARTESIAN_POINT('Ctrl Pts',(7.87680396956558,1.66228269728872,22.2175430943363));
#22300=CARTESIAN_POINT('Ctrl Pts',(7.7074930081086,-1.97299730385434,22.416059211748));
#22301=CARTESIAN_POINT('Ctrl Pts',(4.56095756308617,-3.80143701374933,22.6145753291597));
#22302=CARTESIAN_POINT('Ctrl Pts',(1.31873095853907,-2.14860623751896,22.8130914465713));
#22303=CARTESIAN_POINT('Ctrl Pts',(0.949990286798536,1.47190262315773,23.011607563983));
#22304=CARTESIAN_POINT('Ctrl Pts',(3.7924065803434,3.74442240079083,23.2101236813946));
#22305=CARTESIAN_POINT('Ctrl Pts',(7.24297719250067,2.58796472414074,23.4086397988063));
#22306=CARTESIAN_POINT('Ctrl Pts',(8.14168123233833,-0.938680920498277,
23.6071559162179));
#22307=CARTESIAN_POINT('Ctrl Pts',(5.66560616055497,-3.60535681683013,23.8056720336296));
#22308=CARTESIAN_POINT('Ctrl Pts',(2.08209581503262,-2.97097481614092,24.0041881510412));
#22309=CARTESIAN_POINT('Ctrl Pts',(0.673241827254791,0.385434817028999,
24.2027042684529));
#22310=CARTESIAN_POINT('Ctrl Pts',(2.72851506381635,3.38643791990783,24.4012203858645));
#22311=CARTESIAN_POINT('Ctrl Pts',(6.36713580394013,3.29091791303403,24.5997365032762));
#22312=CARTESIAN_POINT('Ctrl Pts',(8.25465969525897,0.17151120336101,24.7982954766299));
#22313=CARTESIAN_POINT('Ctrl Pts',(7.19525837483205,-1.99900958588141,24.9306824108463));
#22314=CARTESIAN_POINT('Ctrl Pts',(6.32311239899223,-2.62025147071356,24.9968973059255));
#22315=CARTESIAN_POINT('Ctrl Pts',(5.99341579333084,3.0962819108244,-0.27495920519366));
#22316=CARTESIAN_POINT('Ctrl Pts',(7.02329163031133,2.58506739568259,-0.208787166056442));
#22317=CARTESIAN_POINT('Ctrl Pts',(8.51497056474962,0.462964065771816,-0.0764430877820045));
#22318=CARTESIAN_POINT('Ctrl Pts',(7.04304871618797,-3.16665160770128,0.122073029629653));
#22319=CARTESIAN_POINT('Ctrl Pts',(3.19892054011338,-3.88657631350085,0.320589147041309));
#22320=CARTESIAN_POINT('Ctrl Pts',(0.508208668906595,-1.05209144762919,
0.519105264452963));
#22321=CARTESIAN_POINT('Ctrl Pts',(1.43231541168923,2.74837799923302,0.717621381864618));
#22322=CARTESIAN_POINT('Ctrl Pts',(5.12636543519397,4.03063520713254,0.916137499276276));
#22323=CARTESIAN_POINT('Ctrl Pts',(8.20668654383497,1.62239064105283,1.11465361668793));
#22324=CARTESIAN_POINT('Ctrl Pts',(7.85276047702285,-2.27196140132349,1.31316973409959));
#22325=CARTESIAN_POINT('Ctrl Pts',(4.38850729527858,-4.08551042322263,1.51168585151124));
#22326=CARTESIAN_POINT('Ctrl Pts',(0.986527733847538,-2.15772261402933,
1.7102019689229));
#22327=CARTESIAN_POINT('Ctrl Pts',(0.7622359790706,1.74611650720567,1.90871808633455));
#22328=CARTESIAN_POINT('Ctrl Pts',(3.92106229159746,4.0508692911502,2.10723420374621));
#22329=CARTESIAN_POINT('Ctrl Pts',(7.57019895508782,2.64592661456843,2.30575032115786));
#22330=CARTESIAN_POINT('Ctrl Pts',(8.36784367179503,-1.18211240346562,2.50426643856952));
#22331=CARTESIAN_POINT('Ctrl Pts',(5.58352459826198,-3.92759167890361,2.70278255598118));
#22332=CARTESIAN_POINT('Ctrl Pts',(1.7670702556363,-3.07625912870098,2.90129867339283));
#22333=CARTESIAN_POINT('Ctrl Pts',(0.413515851644582,0.592254017343965,
3.09981479080449));
#22334=CARTESIAN_POINT('Ctrl Pts',(2.76242132641212,3.7183916776686,3.29833090821614));
#22335=CARTESIAN_POINT('Ctrl Pts',(6.66270343294158,3.43929724324088,3.4968470256278));
#22336=CARTESIAN_POINT('Ctrl Pts',(8.54255816261418,0.0105596738669375,
3.69536314303945));
#22337=CARTESIAN_POINT('Ctrl Pts',(6.6804502327146,-3.42784816997514,3.89387926045112));
#22338=CARTESIAN_POINT('Ctrl Pts',(2.78166270604797,-3.72709790290783,4.09239537786277));
#22339=CARTESIAN_POINT('Ctrl Pts',(0.416631015022661,-0.613142253174304,
4.29091149527442));
#22340=CARTESIAN_POINT('Ctrl Pts',(1.75120620592284,3.06231739833558,4.48942761268608));
#22341=CARTESIAN_POINT('Ctrl Pts',(5.56320969933569,3.93336503336498,4.68794373009773));
#22342=CARTESIAN_POINT('Ctrl Pts',(8.36168121106336,1.20231178852842,4.88645984750939));
#22343=CARTESIAN_POINT('Ctrl Pts',(7.58383376163584,-2.62979572036334,5.08497596492104));
#22344=CARTESIAN_POINT('Ctrl Pts',(3.94200524984668,-4.05358633333867,5.2834920823327));
#22345=CARTESIAN_POINT('Ctrl Pts',(0.771312951433223,-1.76517968922739,
5.48200819974436));
#22346=CARTESIAN_POINT('Ctrl Pts',(0.97541656054666,2.13974493679014,5.68052431715601));
#22347=CARTESIAN_POINT('Ctrl Pts',(4.36740187430494,4.08513185206935,5.87904043456767));
#22348=CARTESIAN_POINT('Ctrl Pts',(7.84095326483218,2.28943272461384,6.07755655197932));
#22349=CARTESIAN_POINT('Ctrl Pts',(8.21505844260491,-1.60288534238506,6.27607266939098));
#22350=CARTESIAN_POINT('Ctrl Pts',(5.14711900207072,-4.02731150295548,6.47458878680263));
#22351=CARTESIAN_POINT('Ctrl Pts',(1.44669552446588,-2.76360239669899,6.6731049042143));
#22352=CARTESIAN_POINT('Ctrl Pts',(0.502565441067234,1.03096121515846,6.87162102162594));
#22353=CARTESIAN_POINT('Ctrl Pts',(3.17934512299035,3.88139015713774,7.07013713903761));
#22354=CARTESIAN_POINT('Ctrl Pts',(7.0256906552799,3.17731582507866,7.26865325644925));
#22355=CARTESIAN_POINT('Ctrl Pts',(8.51919196471455,-0.436483900631263,
7.46716937386092));
#22356=CARTESIAN_POINT('Ctrl Pts',(6.2921289615216,-3.65055997294754,7.66568549127257));
#22357=CARTESIAN_POINT('Ctrl Pts',(2.38400358079477,-3.52152266305215,7.86420160868423));
#22358=CARTESIAN_POINT('Ctrl Pts',(0.373802705776339,-0.16754188479758,
8.06271772609589));
#22359=CARTESIAN_POINT('Ctrl Pts',(2.10243005973299,3.33987056457006,8.26123384350753));
#22360=CARTESIAN_POINT('Ctrl Pts',(5.98684159389007,3.78869308197905,8.4597499609192));
#22361=CARTESIAN_POINT('Ctrl Pts',(8.4697671146088,0.767902543495819,8.65826607833084));
#22362=CARTESIAN_POINT('Ctrl Pts',(7.27739066026635,-2.95611853726567,8.85678219574251));
#22363=CARTESIAN_POINT('Ctrl Pts',(3.50166790634439,-3.97298249293629,9.05529831315416));
#22364=CARTESIAN_POINT('Ctrl Pts',(0.600333929022254,-1.35146465571633,
9.25381443056581));
#22365=CARTESIAN_POINT('Ctrl Pts',(1.23037519550738,2.50769880562501,9.45233054797748));
#22366=CARTESIAN_POINT('Ctrl Pts',(4.81481189860833,4.07035940226423,9.65084666538912));
#22367=CARTESIAN_POINT('Ctrl Pts',(8.07108508884113,1.90546228475562,9.84936278280079));
#22368=CARTESIAN_POINT('Ctrl Pts',(8.01716171947454,-2.00442094739626,10.0478789002124));
#22369=CARTESIAN_POINT('Ctrl Pts',(4.70242378644322,-4.07869360405195,10.2463950176241));
#22370=CARTESIAN_POINT('Ctrl Pts',(1.16244523581599,-2.41777624309588,10.4449111350357));
#22371=CARTESIAN_POINT('Ctrl Pts',(0.639071086725107,1.45729461030662,10.6434272524474));
#22372=CARTESIAN_POINT('Ctrl Pts',(3.61159742927608,3.99780278027315,10.841943369859));
#22373=CARTESIAN_POINT('Ctrl Pts',(7.35784118240728,2.87719921033794,11.0404594872707));
#22374=CARTESIAN_POINT('Ctrl Pts',(8.44706357811351,-0.878288666292467,
11.2389756046823));
#22375=CARTESIAN_POINT('Ctrl Pts',(5.88177546561389,-3.82945648915419,11.437491722094));
#22376=CARTESIAN_POINT('Ctrl Pts',(2.01121890138154,-3.27368090323489,11.6360078395057));
#22377=CARTESIAN_POINT('Ctrl Pts',(0.379975961147697,0.280069381853164,
11.8345239569173));
#22378=CARTESIAN_POINT('Ctrl Pts',(2.4819079000476,3.57733745452462,12.033040074329));
#22379=CARTESIAN_POINT('Ctrl Pts',(6.39210543142176,3.59854793451629,12.2315561917406));
#22380=CARTESIAN_POINT('Ctrl Pts',(8.52968403588164,0.324276667717884,12.4300723091523));
#22381=CARTESIAN_POINT('Ctrl Pts',(6.93708988851933,-3.24696100298028,12.6285884265639));
#22382=CARTESIAN_POINT('Ctrl Pts',(3.07279041513639,-3.84469355089646,12.8271045439756));
#22383=CARTESIAN_POINT('Ctrl Pts',(0.475637566686629,-0.921528878727684,
13.0256206613872));
#22384=CARTESIAN_POINT('Ctrl Pts',(1.52405451869475,2.84555441124189,13.2241367787989));
#22385=CARTESIAN_POINT('Ctrl Pts',(5.25792096951678,4.00673309958052,13.4226528962106));
#22386=CARTESIAN_POINT('Ctrl Pts',(8.257833049161,1.4986218314684,13.6211690136222));
#22387=CARTESIAN_POINT('Ctrl Pts',(7.77652833946771,-2.38189880309254,13.8196851310339));
#22388=CARTESIAN_POINT('Ctrl Pts',(4.25477653818775,-4.08112182230083,14.0182012484455));
#22389=CARTESIAN_POINT('Ctrl Pts',(0.917730954110628,-2.04293110781465,
14.2167173658572));
#22390=CARTESIAN_POINT('Ctrl Pts',(0.821394455796449,1.86613705453794,14.4152334832688));
#22391=CARTESIAN_POINT('Ctrl Pts',(4.05399017588675,4.06623240003544,14.6137496006805));
#22392=CARTESIAN_POINT('Ctrl Pts',(7.65516844441363,2.54254946152231,14.8122657180922));
#22393=CARTESIAN_POINT('Ctrl Pts',(8.32703870473431,-1.30955190943392,15.0107818355038));
#22394=CARTESIAN_POINT('Ctrl Pts',(5.45431495277465,-3.96239055204922,15.2092979529155));
#22395=CARTESIAN_POINT('Ctrl Pts',(1.66778295557931,-2.98654729975826,15.4078140703271));
#22396=CARTESIAN_POINT('Ctrl Pts',(0.435076688703739,0.724319159497842,
15.6063301877388));
#22397=CARTESIAN_POINT('Ctrl Pts',(2.88508510279309,3.77186791049719,15.8048463051504));
#22398=CARTESIAN_POINT('Ctrl Pts',(6.77413709632598,3.36521177759866,16.0033624225621));
#22399=CARTESIAN_POINT('Ctrl Pts',(8.54071283123811,-0.123241288109086,
16.2018785399737));
#22400=CARTESIAN_POINT('Ctrl Pts',(6.56701585333057,-3.49883232646441,16.4003946573854));
#22401=CARTESIAN_POINT('Ctrl Pts',(2.66052031127365,-3.67025927509159,16.598910774797));
#22402=CARTESIAN_POINT('Ctrl Pts',(0.398720513058523,-0.480532595324168,
16.7974268922087));
#22403=CARTESIAN_POINT('Ctrl Pts',(1.85292968989636,3.14925669454191,16.9959430096203));
#22404=CARTESIAN_POINT('Ctrl Pts',(5.69141073963082,3.89501660876095,17.194459127032));
#22405=CARTESIAN_POINT('Ctrl Pts',(8.39895573256671,1.07379440374864,17.3929752444437));
#22406=CARTESIAN_POINT('Ctrl Pts',(7.49604646714037,-2.73078829048094,17.5914913618553));
#22407=CARTESIAN_POINT('Ctrl Pts',(3.80955007347359,-4.03456701338995,17.790007479267));
#22408=CARTESIAN_POINT('Ctrl Pts',(0.715489824289806,-1.64356601103751,
17.9885235966786));
#22409=CARTESIAN_POINT('Ctrl Pts',(1.04734724052415,2.25258148028018,18.1870397140903));
#22410=CARTESIAN_POINT('Ctrl Pts',(4.50121361298798,4.08585770060491,18.3855558315019));
#22411=CARTESIAN_POINT('Ctrl Pts',(7.91410381728119,2.1773831599618,18.5840719489136));
#22412=CARTESIAN_POINT('Ctrl Pts',(8.16055792437237,-1.72509746033864,18.7825880663253));
#22413=CARTESIAN_POINT('Ctrl Pts',(5.0148779510323,-4.04776664132528,18.9811041837369));
#22414=CARTESIAN_POINT('Ctrl Pts',(1.35781777968586,-2.66356812881232,19.1796203011486));
#22415=CARTESIAN_POINT('Ctrl Pts',(0.538443550556935,1.1598754095142,19.3781364185603));
#22416=CARTESIAN_POINT('Ctrl Pts',(3.30712259659747,3.92112711119714,19.5766525359719));
#22417=CARTESIAN_POINT('Ctrl Pts',(7.12835131317638,3.09148519177063,19.7751686533836));
#22418=CARTESIAN_POINT('Ctrl Pts',(8.50272112937199,-0.569280059186615,
19.9736847707952));
#22419=CARTESIAN_POINT('Ctrl Pts',(6.17161031033075,-3.70870946234774,20.1722008882069));
#22420=CARTESIAN_POINT('Ctrl Pts',(2.26980580259814,-3.45177328404759,20.3707170056185));
#22421=CARTESIAN_POINT('Ctrl Pts',(0.370505952442893,-0.0337687976193256,
20.5692331230302));
#22422=CARTESIAN_POINT('Ctrl Pts',(2.21305343742525,3.41516052227788,20.7677492404418));
#22423=CARTESIAN_POINT('Ctrl Pts',(6.11007831343283,3.73655077808788,20.9662653578534));
#22424=CARTESIAN_POINT('Ctrl Pts',(8.49275934044528,0.636078948397367,21.1647814752652));
#22425=CARTESIAN_POINT('Ctrl Pts',(7.17908253400595,-3.04690196012391,21.3632975926768));
#22426=CARTESIAN_POINT('Ctrl Pts',(3.37208816940477,-3.93958786330456,21.5618137100885));
#22427=CARTESIAN_POINT('Ctrl Pts',(0.558149183206385,-1.22447442503984,
21.7603298275001));
#22428=CARTESIAN_POINT('Ctrl Pts',(1.31421753683424,2.61198994621562,21.9588459449118));
#22429=CARTESIAN_POINT('Ctrl Pts',(4.94789989808116,4.05644256154919,22.1573620623234));
#22430=CARTESIAN_POINT('Ctrl Pts',(8.13153968654471,1.78608425229248,22.3558781797351));
#22431=CARTESIAN_POINT('Ctrl Pts',(7.94961898046267,-2.11993989949929,22.5543942971467));
#22432=CARTESIAN_POINT('Ctrl Pts',(4.56873953270021,-4.0845560128934,22.7529104145584));
#22433=CARTESIAN_POINT('Ctrl Pts',(1.08504215066615,-2.30862763082918,22.95142653197));
#22434=CARTESIAN_POINT('Ctrl Pts',(0.688838840573486,1.58152527269752,23.1499426493817));
#22435=CARTESIAN_POINT('Ctrl Pts',(3.74294930484078,4.02329513198439,23.3484587667933));
#22436=CARTESIAN_POINT('Ctrl Pts',(7.45050749686758,2.78070814718547,23.546974884205));
#22437=CARTESIAN_POINT('Ctrl Pts',(8.41614416964521,-1.00859090500303,23.7454910016166));
#22438=CARTESIAN_POINT('Ctrl Pts',(5.75565886205016,-3.87387238340306,23.9440071190283));
#22439=CARTESIAN_POINT('Ctrl Pts',(1.90526000600476,-3.19224361880315,24.14252323644));
#22440=CARTESIAN_POINT('Ctrl Pts',(0.391479031532891,0.414140782493564,
24.3410393538516));
#22441=CARTESIAN_POINT('Ctrl Pts',(2.59982251484541,3.6386490998064,24.5395554712633));
#22442=CARTESIAN_POINT('Ctrl Pts',(6.50943621328541,3.53601506509354,24.7380715886749));
#22443=CARTESIAN_POINT('Ctrl Pts',(8.53753691096405,0.184284815040506,24.9366305620286));
#22444=CARTESIAN_POINT('Ctrl Pts',(7.39923473266516,-2.14788949397592,25.069017496245));
#22445=CARTESIAN_POINT('Ctrl Pts',(6.46213408444902,-2.81539950847165,25.1352323913243));
#22446=CARTESIAN_POINT('Ctrl Pts',(6.0999485000484,3.31089917470656,-0.136624119794918));
#22447=CARTESIAN_POINT('Ctrl Pts',(7.2012096761669,2.76425007587486,-0.0704520806576993));
#22448=CARTESIAN_POINT('Ctrl Pts',(8.79628360522135,0.495054193199949,0.061891997616738));
#22449=CARTESIAN_POINT('Ctrl Pts',(7.22233621477278,-3.38614651265062,0.260408115028396));
#22450=CARTESIAN_POINT('Ctrl Pts',(3.11175417728552,-4.15597244676529,0.458924232440051));
#22451=CARTESIAN_POINT('Ctrl Pts',(0.234536930817258,-1.12501665093665,
0.657440349851707));
#22452=CARTESIAN_POINT('Ctrl Pts',(1.22269767978634,2.93888047390986,0.855956467263361));
#22453=CARTESIAN_POINT('Ctrl Pts',(5.17279897107673,4.31001671203934,1.05447258467502));
#22454=CARTESIAN_POINT('Ctrl Pts',(8.46663102841521,1.73484585358162,1.25298870208667));
#22455=CARTESIAN_POINT('Ctrl Pts',(8.08817274965877,-2.42944129289705,1.45150481949833));
#22456=CARTESIAN_POINT('Ctrl Pts',(4.38379655564558,-4.36869557685114,1.65002093690999));
#22457=CARTESIAN_POINT('Ctrl Pts',(0.746010447431816,-2.30728410002347,
1.84853705432164));
#22458=CARTESIAN_POINT('Ctrl Pts',(0.506172019545635,1.86714771753756,2.04705317173329));
#22459=CARTESIAN_POINT('Ctrl Pts',(3.88395083052018,4.33165331167866,2.24556928914495));
#22460=CARTESIAN_POINT('Ctrl Pts',(7.78602561424836,2.82932772170484,2.4440854065566));
#22461=CARTESIAN_POINT('Ctrl Pts',(8.63895868375428,-1.26404994563383,2.64260152396827));
#22462=CARTESIAN_POINT('Ctrl Pts',(5.66164589758561,-4.19983077212884,2.84111764137992));
#22463=CARTESIAN_POINT('Ctrl Pts',(1.58065589175627,-3.28948852324876,3.03963375879158));
#22464=CARTESIAN_POINT('Ctrl Pts',(0.133280527313607,0.633305814430374,
3.23814987620323));
#22465=CARTESIAN_POINT('Ctrl Pts',(2.6449992344131,3.97613017528841,3.43666599361489));
#22466=CARTESIAN_POINT('Ctrl Pts',(6.81562748453676,3.67769044685756,3.63518211102655));
#22467=CARTESIAN_POINT('Ctrl Pts',(8.82578342391765,0.0112916124882134,
3.8336982284382));
#22468=CARTESIAN_POINT('Ctrl Pts',(6.83460439504253,-3.66544778668689,4.03221434584986));
#22469=CARTESIAN_POINT('Ctrl Pts',(2.66557432085276,-3.98543986826524,4.23073046326151));
#22470=CARTESIAN_POINT('Ctrl Pts',(0.13661161671523,-0.655641908094887,
4.42924658067317));
#22471=CARTESIAN_POINT('Ctrl Pts',(1.56369223320815,3.27458042867263,4.62776269808482));
#22472=CARTESIAN_POINT('Ctrl Pts',(5.63992288139177,4.20600430382654,4.82627881549648));
#22473=CARTESIAN_POINT('Ctrl Pts',(8.63236907507575,1.28564944117731,5.02479493290813));
#22474=CARTESIAN_POINT('Ctrl Pts',(7.80060551073305,-2.81207872246989,5.22331105031979));
#22475=CARTESIAN_POINT('Ctrl Pts',(3.90634543966123,-4.33455868431544,5.42182716773146));
#22476=CARTESIAN_POINT('Ctrl Pts',(0.515878157801087,-1.88753225468275,
5.62034328514309));
#22477=CARTESIAN_POINT('Ctrl Pts',(0.734129108596551,2.28806030889307,5.81885940255477));
#22478=CARTESIAN_POINT('Ctrl Pts',(4.36122822275595,4.36829076522382,6.0173755199664));
#22479=CARTESIAN_POINT('Ctrl Pts',(8.07554712633902,2.44812363240269,6.21589163737808));
#22480=CARTESIAN_POINT('Ctrl Pts',(8.47558322124728,-1.71398855469165,6.41440775478972));
#22481=CARTESIAN_POINT('Ctrl Pts',(5.19499106127511,-4.3064626269354,6.61292387220138));
#22482=CARTESIAN_POINT('Ctrl Pts',(1.2380745430358,-2.9551601430283,6.81143998961304));
#22483=CARTESIAN_POINT('Ctrl Pts',(0.228502545404632,1.10242178675316,7.00995610702469));
#22484=CARTESIAN_POINT('Ctrl Pts',(3.09082189971391,4.15042681451437,7.20847222443635));
#22485=CARTESIAN_POINT('Ctrl Pts',(7.20377498837598,3.39754991503151,7.406988341848));
#22486=CARTESIAN_POINT('Ctrl Pts',(8.80079760945692,-0.466738568384383,
7.60550445925966));
#22487=CARTESIAN_POINT('Ctrl Pts',(6.41936682516261,-3.90359674918315,7.80402057667131));
#22488=CARTESIAN_POINT('Ctrl Pts',(2.24035164813274,-3.7656152813635,8.00253669408298));
#22489=CARTESIAN_POINT('Ctrl Pts',(0.0908146841936848,-0.179154968469096,
8.20105281149462));
#22490=CARTESIAN_POINT('Ctrl Pts',(1.93926099639212,3.57137205666049,8.39956892890629));
#22491=CARTESIAN_POINT('Ctrl Pts',(6.09291861319388,4.05130448700034,8.59808504631793));
#22492=CARTESIAN_POINT('Ctrl Pts',(8.7479469000777,0.821129332128062,8.7966011637296));
#22493=CARTESIAN_POINT('Ctrl Pts',(7.47292145590854,-3.16102044557099,8.99511728114126));
#22494=CARTESIAN_POINT('Ctrl Pts',(3.43548632890085,-4.24836782820074,9.19363339855291));
#22495=CARTESIAN_POINT('Ctrl Pts',(0.333047808208697,-1.44514076628925,
9.39214951596456));
#22496=CARTESIAN_POINT('Ctrl Pts',(1.00676007644372,2.68151871989772,9.59066563337622));
#22497=CARTESIAN_POINT('Ctrl Pts',(4.83965025372247,4.352494370297,9.78918175078787));
#22498=CARTESIAN_POINT('Ctrl Pts',(8.32163042499515,2.03753846960017,9.98769786819953));
#22499=CARTESIAN_POINT('Ctrl Pts',(8.26396938369623,-2.14335640346512,10.1862139856111));
#22500=CARTESIAN_POINT('Ctrl Pts',(4.71947201461794,-4.36140625319899,10.3847301030228));
#22501=CARTESIAN_POINT('Ctrl Pts',(0.934121584873003,-2.58536321899705,
10.5832462204345));
#22502=CARTESIAN_POINT('Ctrl Pts',(0.37447001302165,1.5583062723393,10.7817623378461));
#22503=CARTESIAN_POINT('Ctrl Pts',(3.55303556286365,4.27490852159572,10.9802784552578));
#22504=CARTESIAN_POINT('Ctrl Pts',(7.55894836658157,3.07663086415728,11.1787945726694));
#22505=CARTESIAN_POINT('Ctrl Pts',(8.72366967907197,-0.939166814951776,
11.3773106900811));
#22506=CARTESIAN_POINT('Ctrl Pts',(5.98056987770475,-4.09489338977514,11.5758268074927));
#22507=CARTESIAN_POINT('Ctrl Pts',(1.84172758128094,-3.50059449137405,11.7743429249044));
#22508=CARTESIAN_POINT('Ctrl Pts',(0.0974158357370281,0.299482253859507,
11.9728590423161));
#22509=CARTESIAN_POINT('Ctrl Pts',(2.34504215731444,3.82529884776504,12.1713751597277));
#22510=CARTESIAN_POINT('Ctrl Pts',(6.52627311509865,3.84797952178704,12.3698912771394));
#22511=CARTESIAN_POINT('Ctrl Pts',(8.81201693339725,0.346753746088307,12.568407394551));
#22512=CARTESIAN_POINT('Ctrl Pts',(7.10903290287004,-3.47202251432246,12.7669235119627));
#22513=CARTESIAN_POINT('Ctrl Pts',(2.97688140448274,-4.11118660098796,12.9654396293744));
#22514=CARTESIAN_POINT('Ctrl Pts',(0.199708178602426,-0.985404201530036,
13.163955746786));
#22515=CARTESIAN_POINT('Ctrl Pts',(1.32079563805398,3.0427926213136,13.3624718641977));
#22516=CARTESIAN_POINT('Ctrl Pts',(5.3134732128164,4.28445784161121,13.5609879816093));
#22517=CARTESIAN_POINT('Ctrl Pts',(8.52132272870291,1.60249806959112,13.759504099021));
#22518=CARTESIAN_POINT('Ctrl Pts',(8.00665661883263,-2.546998951815,13.9580202164326));
#22519=CARTESIAN_POINT('Ctrl Pts',(4.24079631663729,-4.36400278220629,14.1565363338443));
#22520=CARTESIAN_POINT('Ctrl Pts',(0.672445052608722,-2.18453587678811,
14.3550524512559));
#22521=CARTESIAN_POINT('Ctrl Pts',(0.569431037105937,1.99548743031406,14.5535685686676));
#22522=CARTESIAN_POINT('Ctrl Pts',(4.02609254599198,4.3480813069304,14.7520846860792));
#22523=CARTESIAN_POINT('Ctrl Pts',(7.87688472210303,2.7187850319364,14.9506008034909));
#22524=CARTESIAN_POINT('Ctrl Pts',(8.59532534039074,-1.40032285852991,15.1491169209026));
#22525=CARTESIAN_POINT('Ctrl Pts',(5.52348014881688,-4.2370417121197,15.3476330383142));
#22526=CARTESIAN_POINT('Ctrl Pts',(1.47448654113341,-3.19355836282975,15.5461491557259));
#22527=CARTESIAN_POINT('Ctrl Pts',(0.156335843231577,0.774524987218279,
15.7446652731375));
#22528=CARTESIAN_POINT('Ctrl Pts',(2.77616539036498,4.03331308699926,15.9431813905492));
#22529=CARTESIAN_POINT('Ctrl Pts',(6.93478511771097,3.59846978345639,16.1416975079608));
#22530=CARTESIAN_POINT('Ctrl Pts',(8.82381018430121,-0.131783697622486,
16.3402136253725));
#22531=CARTESIAN_POINT('Ctrl Pts',(6.71330736721926,-3.74135217521042,16.5387297427841));
#22532=CARTESIAN_POINT('Ctrl Pts',(2.53603500032833,-3.92466149880528,16.7372458601958));
#22533=CARTESIAN_POINT('Ctrl Pts',(0.117459657081213,-0.513840476771981,
16.9357619776075));
#22534=CARTESIAN_POINT('Ctrl Pts',(1.6724666306423,3.3675458796068,17.1342780950191));
#22535=CARTESIAN_POINT('Ctrl Pts',(5.77701011399349,4.16499777695671,17.3327942124308));
#22536=CARTESIAN_POINT('Ctrl Pts',(8.67222726177754,1.14822393682795,17.5313103298424));
#22537=CARTESIAN_POINT('Ctrl Pts',(7.70673328292373,-2.92007154311226,17.7298264472541));
#22538=CARTESIAN_POINT('Ctrl Pts',(3.76470919762329,-4.31422104952143,17.9283425646657));
#22539=CARTESIAN_POINT('Ctrl Pts',(0.456185677945633,-1.75748898396369,
18.1268586820774));
#22540=CARTESIAN_POINT('Ctrl Pts',(0.811045628420214,2.40871806212022,18.3253747994891));
#22541=CARTESIAN_POINT('Ctrl Pts',(4.50431505655582,4.36906692559506,18.5238909169007));
#22542=CARTESIAN_POINT('Ctrl Pts',(8.153768073497,2.32830740706619,18.7224070343124));
#22543=CARTESIAN_POINT('Ctrl Pts',(8.41730502629147,-1.84467174573349,18.920923151724));
#22544=CARTESIAN_POINT('Ctrl Pts',(5.05358378656449,-4.328335603201,19.1194392691357));
#22545=CARTESIAN_POINT('Ctrl Pts',(1.14303628091464,-2.84819204886657,19.3179553865473));
#22546=CARTESIAN_POINT('Ctrl Pts',(0.266867528478102,1.24027160533984,19.516471503959));
#22547=CARTESIAN_POINT('Ctrl Pts',(3.22745620631011,4.19291811607857,19.7149876213706));
#22548=CARTESIAN_POINT('Ctrl Pts',(7.31355151948446,3.30576997342133,19.9135037387823));
#22549=CARTESIAN_POINT('Ctrl Pts',(8.78318510623113,-0.60873942761753,20.112019856194));
#22550=CARTESIAN_POINT('Ctrl Pts',(6.29049448270258,-3.96577684195559,20.3105359736056));
#22551=CARTESIAN_POINT('Ctrl Pts',(2.11823830688215,-3.69103125832118,20.5090520910173));
#22552=CARTESIAN_POINT('Ctrl Pts',(0.0872894180178925,-0.0361094652841183,
20.7075682084289));
#22553=CARTESIAN_POINT('Ctrl Pts',(2.05755217931839,3.65188070090475,20.9060843258406));
#22554=CARTESIAN_POINT('Ctrl Pts',(6.2246974255821,3.99554796485774,21.1046004432522));
#22555=CARTESIAN_POINT('Ctrl Pts',(8.77253282078492,0.680168449111409,21.3031165606639));
#22556=CARTESIAN_POINT('Ctrl Pts',(7.36779915003431,-3.25809647691284,21.5016326780756));
#22557=CARTESIAN_POINT('Ctrl Pts',(3.29692483597213,-4.21265846617502,21.7001487954872));
#22558=CARTESIAN_POINT('Ctrl Pts',(0.287939047401517,-1.30934826998177,
21.8986649128989));
#22559=CARTESIAN_POINT('Ctrl Pts',(1.09641390858805,2.79303874980958,22.0971810303105));
#22560=CARTESIAN_POINT('Ctrl Pts',(4.98196318268333,4.33761289058522,22.2956971477222));
#22561=CARTESIAN_POINT('Ctrl Pts',(8.38627540352384,1.90988580729624,22.4942132651338));
#22562=CARTESIAN_POINT('Ctrl Pts',(8.19174495281671,-2.26688249514424,22.6927293825455));
#22563=CARTESIAN_POINT('Ctrl Pts',(4.57652150231426,-4.36767501203749,22.8912454999571));
#22564=CARTESIAN_POINT('Ctrl Pts',(0.851353342793238,-2.46864902413938,
23.0897616173688));
#22565=CARTESIAN_POINT('Ctrl Pts',(0.42768739434844,1.69114792223732,23.2882777347804));
#22566=CARTESIAN_POINT('Ctrl Pts',(3.69349202933814,4.30216786317793,23.4867938521921));
#22567=CARTESIAN_POINT('Ctrl Pts',(7.65803780123451,2.9734515702302,23.6853099696038));
#22568=CARTESIAN_POINT('Ctrl Pts',(8.6906071069521,-1.07850088950778,23.8838260870154));
#22569=CARTESIAN_POINT('Ctrl Pts',(5.84571156354535,-4.14238794997599,24.0823422044271));
#22570=CARTESIAN_POINT('Ctrl Pts',(1.7284241969769,-3.41351242146536,24.2808583218387));
#22571=CARTESIAN_POINT('Ctrl Pts',(0.109716235810993,0.442846747958131,
24.4793744392504));
#22572=CARTESIAN_POINT('Ctrl Pts',(2.47112996587446,3.89086027970496,24.677890556662));
#22573=CARTESIAN_POINT('Ctrl Pts',(6.6517366226307,3.78111221715306,24.8764066740737));
#22574=CARTESIAN_POINT('Ctrl Pts',(8.82041412666913,0.197058426719993,25.0749656474274));
#22575=CARTESIAN_POINT('Ctrl Pts',(7.60321109049825,-2.29676940207044,25.2073525816438));
#22576=CARTESIAN_POINT('Ctrl Pts',(6.60115576990582,-3.01054754622974,25.273567476723));
#22577=CARTESIAN_POINT('Ctrl Pts',(6.20648120676596,3.5255164385887,0.00171096560382468));
#22578=CARTESIAN_POINT('Ctrl Pts',(7.37912772202248,2.94343275606714,0.0678830047410433));
#22579=CARTESIAN_POINT('Ctrl Pts',(9.07759664569311,0.527144320628084,0.200227083015481));
#22580=CARTESIAN_POINT('Ctrl Pts',(7.40162371335757,-3.60564141759996,0.398743200427137));
#22581=CARTESIAN_POINT('Ctrl Pts',(3.02458781445768,-4.42536858002973,0.597259317838794));
#22582=CARTESIAN_POINT('Ctrl Pts',(-0.0391348072720899,-1.19794185424409,
0.795775435250448));
#22583=CARTESIAN_POINT('Ctrl Pts',(1.01307994788347,3.12938294858669,0.994291552662105));
#22584=CARTESIAN_POINT('Ctrl Pts',(5.21923250695947,4.58939821694615,1.19280767007376));
#22585=CARTESIAN_POINT('Ctrl Pts',(8.72657551299543,1.84730106611042,1.39132378748542));
#22586=CARTESIAN_POINT('Ctrl Pts',(8.32358502229467,-2.58692118447061,1.58983990489707));
#22587=CARTESIAN_POINT('Ctrl Pts',(4.37908581601258,-4.65188073047965,1.78835602230873));
#22588=CARTESIAN_POINT('Ctrl Pts',(0.505493161016087,-2.45684558601761,
1.98687213972038));
#22589=CARTESIAN_POINT('Ctrl Pts',(0.250108060020668,1.98817892786946,2.18538825713204));
#22590=CARTESIAN_POINT('Ctrl Pts',(3.8468393694429,4.61243733220712,2.38390437454369));
#22591=CARTESIAN_POINT('Ctrl Pts',(8.0018522734089,3.01272882884126,2.58242049195535));
#22592=CARTESIAN_POINT('Ctrl Pts',(8.91007369571349,-1.34598748780205,2.78093660936701));
#22593=CARTESIAN_POINT('Ctrl Pts',(5.73976719690925,-4.47206986535408,2.97945272677866));
#22594=CARTESIAN_POINT('Ctrl Pts',(1.39424152787623,-3.50271791779653,3.17796884419032));
#22595=CARTESIAN_POINT('Ctrl Pts',(-0.146954797017362,0.674357611516781,
3.37648496160198));
#22596=CARTESIAN_POINT('Ctrl Pts',(2.5275771424141,4.23386867290823,3.57500107901363));
#22597=CARTESIAN_POINT('Ctrl Pts',(6.96855153613195,3.91608365047424,3.77351719642529));
#22598=CARTESIAN_POINT('Ctrl Pts',(9.10900868522111,0.0120235511094912,
3.97203331383693));
#22599=CARTESIAN_POINT('Ctrl Pts',(6.98875855737045,-3.90304740339865,4.17054943124861));
#22600=CARTESIAN_POINT('Ctrl Pts',(2.54948593565754,-4.24378183362265,4.36906554866025));
#22601=CARTESIAN_POINT('Ctrl Pts',(-0.143407781592193,-0.698141563015474,
4.56758166607191));
#22602=CARTESIAN_POINT('Ctrl Pts',(1.37617826049345,3.48684345900968,4.76609778348356));
#22603=CARTESIAN_POINT('Ctrl Pts',(5.71663606344787,4.47864357428809,4.96461390089523));
#22604=CARTESIAN_POINT('Ctrl Pts',(8.90305693908813,1.36898709382619,5.16313001830687));
#22605=CARTESIAN_POINT('Ctrl Pts',(8.01737725983028,-2.99436172457643,5.36164613571854));
#22606=CARTESIAN_POINT('Ctrl Pts',(3.87068562947579,-4.61553103529222,5.56016225313019));
#22607=CARTESIAN_POINT('Ctrl Pts',(0.260443364168955,-2.00988482013811,
5.75867837054185));
#22608=CARTESIAN_POINT('Ctrl Pts',(0.492841656646439,2.436375680996,5.95719448795349));
#22609=CARTESIAN_POINT('Ctrl Pts',(4.35505457120696,4.6514496783783,6.15571060536516));
#22610=CARTESIAN_POINT('Ctrl Pts',(8.31014098784587,2.60681454019155,6.35422672277681));
#22611=CARTESIAN_POINT('Ctrl Pts',(8.73610799988966,-1.82509176699825,6.55274284018847));
#22612=CARTESIAN_POINT('Ctrl Pts',(5.24286312047947,-4.58561375091533,6.75125895760012));
#22613=CARTESIAN_POINT('Ctrl Pts',(1.02945356160573,-3.14671788935761,6.94977507501179));
#22614=CARTESIAN_POINT('Ctrl Pts',(-0.0455603502579819,1.17388235834786,
7.14829119242343));
#22615=CARTESIAN_POINT('Ctrl Pts',(3.00229867643747,4.41946347189101,7.34680730983509));
#22616=CARTESIAN_POINT('Ctrl Pts',(7.38185932147204,3.61778400498435,7.54532342724674));
#22617=CARTESIAN_POINT('Ctrl Pts',(9.08240325419932,-0.496993236137507,
7.7438395446584));
#22618=CARTESIAN_POINT('Ctrl Pts',(6.5466046888036,-4.15663352541875,7.94235566207006));
#22619=CARTESIAN_POINT('Ctrl Pts',(2.09669971547073,-4.00970789967487,8.1408717794817));
#22620=CARTESIAN_POINT('Ctrl Pts',(-0.192173337388976,-0.19076805214061,
8.33938789689338));
#22621=CARTESIAN_POINT('Ctrl Pts',(1.77609193305126,3.80287354875093,8.53790401430502));
#22622=CARTESIAN_POINT('Ctrl Pts',(6.1989956324977,4.3139158920216,8.73642013171668));
#22623=CARTESIAN_POINT('Ctrl Pts',(9.0261266855466,0.874356120760312,8.93493624912834));
#22624=CARTESIAN_POINT('Ctrl Pts',(7.66845225155073,-3.36592235387631,9.13345236653999));
#22625=CARTESIAN_POINT('Ctrl Pts',(3.36930475145732,-4.52375316346519,9.33196848395166));
#22626=CARTESIAN_POINT('Ctrl Pts',(0.0657616873951493,-1.53881687686219,
9.53048460136329));
#22627=CARTESIAN_POINT('Ctrl Pts',(0.783144957380055,2.85533863417045,9.72900071877498));
#22628=CARTESIAN_POINT('Ctrl Pts',(4.86448860883662,4.63462933832978,9.92751683618659));
#22629=CARTESIAN_POINT('Ctrl Pts',(8.57217576114917,2.16961465444475,10.1260329535983));
#22630=CARTESIAN_POINT('Ctrl Pts',(8.51077704791793,-2.28229185953398,10.3245490710099));
#22631=CARTESIAN_POINT('Ctrl Pts',(4.73652024279266,-4.644118902346,10.5230651884216));
#22632=CARTESIAN_POINT('Ctrl Pts',(0.705797933930029,-2.75295019489822,
10.7215813058332));
#22633=CARTESIAN_POINT('Ctrl Pts',(0.109868939318185,1.65931793437198,10.9200974232449));
#22634=CARTESIAN_POINT('Ctrl Pts',(3.49447369645122,4.55201426291826,11.1186135406565));
#22635=CARTESIAN_POINT('Ctrl Pts',(7.76005555075585,3.27606251797663,11.3171296580682));
#22636=CARTESIAN_POINT('Ctrl Pts',(9.00027578003045,-1.00004496361109,11.5156457754798));
#22637=CARTESIAN_POINT('Ctrl Pts',(6.07936428979557,-4.36033029039609,11.7141618928915));
#22638=CARTESIAN_POINT('Ctrl Pts',(1.67223626118035,-3.72750807951321,11.9126780103032));
#22639=CARTESIAN_POINT('Ctrl Pts',(-0.185144289673645,0.31889512586586,
12.1111941277148));
#22640=CARTESIAN_POINT('Ctrl Pts',(2.20817641458127,4.07326024100545,12.3097102451265));
#22641=CARTESIAN_POINT('Ctrl Pts',(6.66044079877556,4.09741110905781,12.5082263625381));
#22642=CARTESIAN_POINT('Ctrl Pts',(9.09434983091284,0.369230824458725,12.7067424799498));
#22643=CARTESIAN_POINT('Ctrl Pts',(7.28097591722075,-3.69708402566464,12.9052585973614));
#22644=CARTESIAN_POINT('Ctrl Pts',(2.8809723938291,-4.37767965107946,13.1037747147731));
#22645=CARTESIAN_POINT('Ctrl Pts',(-0.0762212094817758,-1.04927952433239,
13.3022908321848));
#22646=CARTESIAN_POINT('Ctrl Pts',(1.11753675741321,3.24003083138531,13.5008069495964));
#22647=CARTESIAN_POINT('Ctrl Pts',(5.369025456116,4.5621825836419,13.6993230670081));
#22648=CARTESIAN_POINT('Ctrl Pts',(8.78481240824481,1.70637430771384,13.8978391844197));
#22649=CARTESIAN_POINT('Ctrl Pts',(8.23678489819753,-2.71209910053747,14.0963553018314));
#22650=CARTESIAN_POINT('Ctrl Pts',(4.22681609508684,-4.64688374211174,14.294871419243));
#22651=CARTESIAN_POINT('Ctrl Pts',(0.427159151106815,-2.32614064576156,
14.4933875366547));
#22652=CARTESIAN_POINT('Ctrl Pts',(0.317467618415429,2.12483780609018,14.6919036540663));
#22653=CARTESIAN_POINT('Ctrl Pts',(3.99819491609722,4.62993021382537,14.890419771478));
#22654=CARTESIAN_POINT('Ctrl Pts',(8.09860099979244,2.8950206023505,15.0889358888896));
#22655=CARTESIAN_POINT('Ctrl Pts',(8.86361197604717,-1.49109380762589,15.2874520063013));
#22656=CARTESIAN_POINT('Ctrl Pts',(5.59264534485911,-4.5116928721902,15.485968123713));
#22657=CARTESIAN_POINT('Ctrl Pts',(1.2811901266875,-3.40056942590122,15.6844842411246));
#22658=CARTESIAN_POINT('Ctrl Pts',(-0.122405002240585,0.824730814938715,
15.8830003585363));
#22659=CARTESIAN_POINT('Ctrl Pts',(2.66724567793686,4.29475826350135,16.0815164759479));
#22660=CARTESIAN_POINT('Ctrl Pts',(7.09543313909595,3.83172778931411,16.2800325933596));
#22661=CARTESIAN_POINT('Ctrl Pts',(9.10690753736432,-0.140326107135887,
16.4785487107712));
#22662=CARTESIAN_POINT('Ctrl Pts',(6.85959888110794,-3.98387202395643,16.6770648281829));
#22663=CARTESIAN_POINT('Ctrl Pts',(2.41154968938301,-4.179063722519,16.8755809455945));
#22664=CARTESIAN_POINT('Ctrl Pts',(-0.163801198896094,-0.547148358219792,
17.0740970630062));
#22665=CARTESIAN_POINT('Ctrl Pts',(1.49200357138825,3.5858350646717,17.2726131804178));
#22666=CARTESIAN_POINT('Ctrl Pts',(5.86260948835618,4.43497894515246,17.4711292978295));
#22667=CARTESIAN_POINT('Ctrl Pts',(8.94549879098837,1.22265346990726,17.6696454152412));
#22668=CARTESIAN_POINT('Ctrl Pts',(7.91742009870712,-3.10935479574357,17.8681615326528));
#22669=CARTESIAN_POINT('Ctrl Pts',(3.71986832177296,-4.59387508565289,18.0666776500645));
#22670=CARTESIAN_POINT('Ctrl Pts',(0.196881531601468,-1.87141195688986,
18.2651937674761));
#22671=CARTESIAN_POINT('Ctrl Pts',(0.574744016316265,2.56485464396025,18.4637098848878));
#22672=CARTESIAN_POINT('Ctrl Pts',(4.50741650012369,4.6522761505852,18.6622260022994));
#22673=CARTESIAN_POINT('Ctrl Pts',(8.3934323297128,2.47923165417059,18.8607421197111));
#22674=CARTESIAN_POINT('Ctrl Pts',(8.67405212821057,-1.96424603112833,19.0592582371228));
#22675=CARTESIAN_POINT('Ctrl Pts',(5.09228962209667,-4.60890456507674,19.2577743545344));
#22676=CARTESIAN_POINT('Ctrl Pts',(0.928254782143413,-3.0328159689208,19.4562904719461));
#22677=CARTESIAN_POINT('Ctrl Pts',(-0.00470849360073685,1.32066780116548,
19.6548065893577));
#22678=CARTESIAN_POINT('Ctrl Pts',(3.14778981602278,4.46470912096001,19.8533227067694));
#22679=CARTESIAN_POINT('Ctrl Pts',(7.49875172579254,3.52005475507203,20.051838824181));
#22680=CARTESIAN_POINT('Ctrl Pts',(9.06364908309027,-0.648198796048447,
20.2503549415927));
#22681=CARTESIAN_POINT('Ctrl Pts',(6.4093786550744,-4.22284422156345,20.4488710590044));
#22682=CARTESIAN_POINT('Ctrl Pts',(1.96667081116617,-3.93028923259476,20.647387176416));
#22683=CARTESIAN_POINT('Ctrl Pts',(-0.195927116407106,-0.0384501329489085,
20.8459032938277));
#22684=CARTESIAN_POINT('Ctrl Pts',(1.90205092121151,3.88860087953163,21.0444194112393));
#22685=CARTESIAN_POINT('Ctrl Pts',(6.3393165377314,4.25454515162759,21.242935528651));
#22686=CARTESIAN_POINT('Ctrl Pts',(9.05230630112455,0.724257949825445,21.4414516460626));
#22687=CARTESIAN_POINT('Ctrl Pts',(7.55651576606266,-3.46929099370176,21.6399677634743));
#22688=CARTESIAN_POINT('Ctrl Pts',(3.22176150253947,-4.48572906904549,21.838483880886));
#22689=CARTESIAN_POINT('Ctrl Pts',(0.0177289115966501,-1.39422211492368,
22.0369999982976));
#22690=CARTESIAN_POINT('Ctrl Pts',(0.878610280341868,2.97408755340353,22.2355161157093));
#22691=CARTESIAN_POINT('Ctrl Pts',(5.01602646728549,4.61878321962123,22.4340322331209));
#22692=CARTESIAN_POINT('Ctrl Pts',(8.64101112050298,2.03368736229999,22.6325483505326));
#22693=CARTESIAN_POINT('Ctrl Pts',(8.43387092517075,-2.41382509078919,22.8310644679442));
#22694=CARTESIAN_POINT('Ctrl Pts',(4.58430347192829,-4.65079401118156,23.0295805853559));
#22695=CARTESIAN_POINT('Ctrl Pts',(0.617664534920323,-2.6286704174496,23.2280967027675));
#22696=CARTESIAN_POINT('Ctrl Pts',(0.166535948123391,1.80077057177711,23.4266128201792));
#22697=CARTESIAN_POINT('Ctrl Pts',(3.64403475383551,4.58104059437149,23.6251289375908));
#22698=CARTESIAN_POINT('Ctrl Pts',(7.86556810560143,3.16619499327494,23.8236450550025));
#22699=CARTESIAN_POINT('Ctrl Pts',(8.96507004425898,-1.14841087401253,24.0221611724142));
#22700=CARTESIAN_POINT('Ctrl Pts',(5.93576426504054,-4.41090351654891,24.2206772898258));
#22701=CARTESIAN_POINT('Ctrl Pts',(1.55158838794904,-3.63478122412758,24.4191934072375));
#22702=CARTESIAN_POINT('Ctrl Pts',(-0.172046559910909,0.471552713422697,
24.6177095246491));
#22703=CARTESIAN_POINT('Ctrl Pts',(2.34243741690352,4.14307145960353,24.8162256420608));
#22704=CARTESIAN_POINT('Ctrl Pts',(6.79403703197597,4.02620936921257,25.0147417594724));
#22705=CARTESIAN_POINT('Ctrl Pts',(9.10329134237422,0.209832038399488,25.2133007328261));
#22706=CARTESIAN_POINT('Ctrl Pts',(7.80718744833136,-2.44564931016495,25.3456876670425));
#22707=CARTESIAN_POINT('Ctrl Pts',(6.7401774553626,-3.20569558398784,25.4119025621217));
#22708=CARTESIAN_POINT('Ctrl Pts',(5.88688308661327,2.88166464694226,-0.413294290592403));
#22709=CARTESIAN_POINT('Ctrl Pts',(6.84537358445575,2.40588471549031,-0.347122251455184));
#22710=CARTESIAN_POINT('Ctrl Pts',(8.23365752427788,0.430873938343679,-0.214778173180747));
#22711=CARTESIAN_POINT('Ctrl Pts',(6.86376121760315,-2.94715670275194,-0.0162620557690901));
#22712=CARTESIAN_POINT('Ctrl Pts',(3.28608690294124,-3.61718018023642,0.182254061642566));
#22713=CARTESIAN_POINT('Ctrl Pts',(0.781880406995935,-0.979166244321737,
0.380770179054222));
#22714=CARTESIAN_POINT('Ctrl Pts',(1.64193314359211,2.55787552455616,0.579286296465875));
#22715=CARTESIAN_POINT('Ctrl Pts',(5.07993189931123,3.75125370222575,0.777802413877532));
#22716=CARTESIAN_POINT('Ctrl Pts',(7.94674205925474,1.50993542852403,0.976318531289188));
#22717=CARTESIAN_POINT('Ctrl Pts',(7.61734820438694,-2.11448150974993,1.17483464870084));
#22718=CARTESIAN_POINT('Ctrl Pts',(4.39321803491158,-3.80232526959411,1.3733507661125));
#22719=CARTESIAN_POINT('Ctrl Pts',(1.22704502026327,-2.0081611280352,1.57186688352415));
#22720=CARTESIAN_POINT('Ctrl Pts',(1.01829993859556,1.62508529687376,1.77038300093581));
#22721=CARTESIAN_POINT('Ctrl Pts',(3.95817375267475,3.77008527062174,1.96889911834747));
#22722=CARTESIAN_POINT('Ctrl Pts',(7.35437229592725,2.462525507432,2.16741523575912));
#22723=CARTESIAN_POINT('Ctrl Pts',(8.09672865983581,-1.10017486129741,2.36593135317078));
#22724=CARTESIAN_POINT('Ctrl Pts',(5.50540329893836,-3.65535258567839,2.56444747058243));
#22725=CARTESIAN_POINT('Ctrl Pts',(1.95348461951634,-2.8630297341532,2.76296358799409));
#22726=CARTESIAN_POINT('Ctrl Pts',(0.693751175975549,0.551202220257554,
2.96147970540574));
#22727=CARTESIAN_POINT('Ctrl Pts',(2.87984341841113,3.46065318004877,3.1599958228174));
#22728=CARTESIAN_POINT('Ctrl Pts',(6.50977938134639,3.20090403962421,3.35851194022905));
#22729=CARTESIAN_POINT('Ctrl Pts',(8.25933290131072,0.00982773524565914,
3.55702805764071));
#22730=CARTESIAN_POINT('Ctrl Pts',(6.52629607038668,-3.19024855326339,3.75554417505237));
#22731=CARTESIAN_POINT('Ctrl Pts',(2.89775109124319,-3.46875593755042,3.95406029246402));
#22732=CARTESIAN_POINT('Ctrl Pts',(0.69665041333009,-0.570642598253718,
4.15257640987568));
#22733=CARTESIAN_POINT('Ctrl Pts',(1.93872017863753,2.85005436799852,4.35109252728733));
#22734=CARTESIAN_POINT('Ctrl Pts',(5.48649651727959,3.66072576290342,4.54960864469899));
#22735=CARTESIAN_POINT('Ctrl Pts',(8.09099334705098,1.11897413587954,4.74812476211065));
#22736=CARTESIAN_POINT('Ctrl Pts',(7.36706201253862,-2.44751271825679,4.9466408795223));
#22737=CARTESIAN_POINT('Ctrl Pts',(3.97766506003213,-3.7726139823619,5.14515699693396));
#22738=CARTESIAN_POINT('Ctrl Pts',(1.02674774506536,-1.64282712377203,5.34367311434561));
#22739=CARTESIAN_POINT('Ctrl Pts',(1.21670401249677,1.99142956468722,5.54218923175727));
#22740=CARTESIAN_POINT('Ctrl Pts',(4.37357552585394,3.80197293891488,5.74070534916892));
#22741=CARTESIAN_POINT('Ctrl Pts',(7.60635940332531,2.13074181682499,5.93922146658058));
#22742=CARTESIAN_POINT('Ctrl Pts',(7.95453366396254,-1.49178213007847,6.13773758399224));
#22743=CARTESIAN_POINT('Ctrl Pts',(5.09924694286633,-3.74816037897555,6.33625370140389));
#22744=CARTESIAN_POINT('Ctrl Pts',(1.65531650589596,-2.57204465036969,6.53476981881556));
#22745=CARTESIAN_POINT('Ctrl Pts',(0.776628336729841,0.959500643563771,
6.7332859362272));
#22746=CARTESIAN_POINT('Ctrl Pts',(3.26786834626679,3.6123534997611,6.93180205363886));
#22747=CARTESIAN_POINT('Ctrl Pts',(6.84760632218384,2.95708173512582,7.1303181710505));
#22748=CARTESIAN_POINT('Ctrl Pts',(8.23758631997216,-0.406229232878139,
7.32883428846218));
#22749=CARTESIAN_POINT('Ctrl Pts',(6.16489109788061,-3.39752319671194,7.52735040587382));
#22750=CARTESIAN_POINT('Ctrl Pts',(2.52765551345678,-3.27743004474078,7.72586652328549));
#22751=CARTESIAN_POINT('Ctrl Pts',(0.656790727359,-0.155928801126063,7.92438264069713));
#22752=CARTESIAN_POINT('Ctrl Pts',(2.26559912307384,3.10836907247963,8.1228987581088));
#22753=CARTESIAN_POINT('Ctrl Pts',(5.88076457458627,3.52608167695778,8.32141487552045));
#22754=CARTESIAN_POINT('Ctrl Pts',(8.19158732913988,0.714675754863574,8.5199309929321));
#22755=CARTESIAN_POINT('Ctrl Pts',(7.08185986462416,-2.75121662896035,8.71844711034376));
#22756=CARTESIAN_POINT('Ctrl Pts',(3.56784948378791,-3.69759715767183,8.91696322775543));
#22757=CARTESIAN_POINT('Ctrl Pts',(0.867620049835816,-1.2577885451434,9.11547934516706));
#22758=CARTESIAN_POINT('Ctrl Pts',(1.45399031457103,2.33387889135228,9.31399546257875));
#22759=CARTESIAN_POINT('Ctrl Pts',(4.78997354349419,3.78822443423146,9.51251157999037));
#22760=CARTESIAN_POINT('Ctrl Pts',(7.8205397526871,1.77338609991104,9.71102769740205));
#22761=CARTESIAN_POINT('Ctrl Pts',(7.77035405525285,-1.8654854913274,9.90954381481369));
#22762=CARTESIAN_POINT('Ctrl Pts',(4.68537555826851,-3.79598095490491,10.1080599322253));
#22763=CARTESIAN_POINT('Ctrl Pts',(1.39076888675897,-2.25018926719472,10.306576049637));
#22764=CARTESIAN_POINT('Ctrl Pts',(0.903672160428571,1.35628294827392,10.5050921670486));
#22765=CARTESIAN_POINT('Ctrl Pts',(3.67015929568852,3.72069703895061,10.7036082844603));
#22766=CARTESIAN_POINT('Ctrl Pts',(7.156733998233,2.67776755651859,10.902124401872));
#22767=CARTESIAN_POINT('Ctrl Pts',(8.17045747715504,-0.817410517633158,
11.1006405192836));
#22768=CARTESIAN_POINT('Ctrl Pts',(5.78298105352307,-3.56401958853324,11.2991566366953));
#22769=CARTESIAN_POINT('Ctrl Pts',(2.18071022148213,-3.04676731509573,11.4976727541069));
#22770=CARTESIAN_POINT('Ctrl Pts',(0.662536086558379,0.260656509846819,
11.6961888715186));
#22771=CARTESIAN_POINT('Ctrl Pts',(2.61877364278075,3.32937606128419,11.8947049889302));
#22772=CARTESIAN_POINT('Ctrl Pts',(6.25793774774488,3.34911634724554,12.0932211063419));
#22773=CARTESIAN_POINT('Ctrl Pts',(8.24735113836601,0.301799589347462,12.2917372237535));
#22774=CARTESIAN_POINT('Ctrl Pts',(6.76514687416864,-3.02189949163811,12.4902533411652));
#22775=CARTESIAN_POINT('Ctrl Pts',(3.16869942579002,-3.57820050080496,12.6887694585768));
#22776=CARTESIAN_POINT('Ctrl Pts',(0.751566954770839,-0.857653555925328,
12.8872855759885));
#22777=CARTESIAN_POINT('Ctrl Pts',(1.72731339933552,2.64831620117018,13.0858016934002));
#22778=CARTESIAN_POINT('Ctrl Pts',(5.20236872621718,3.72900835754984,13.2843178108118));
#22779=CARTESIAN_POINT('Ctrl Pts',(7.99434336961907,1.39474559334568,13.4828339282235));
#22780=CARTESIAN_POINT('Ctrl Pts',(7.54640006010282,-2.21679865437008,13.6813500456351));
#22781=CARTESIAN_POINT('Ctrl Pts',(4.26875675973819,-3.79824086239538,13.8798661630468));
#22782=CARTESIAN_POINT('Ctrl Pts',(1.16301685561255,-1.9013263388412,14.0783822804584));
#22783=CARTESIAN_POINT('Ctrl Pts',(1.07335787448695,1.73678667876183,14.2768983978701));
#22784=CARTESIAN_POINT('Ctrl Pts',(4.08188780578152,3.78438349314049,14.4754145152818));
#22785=CARTESIAN_POINT('Ctrl Pts',(7.43345216672421,2.36631389110821,14.6739306326934));
#22786=CARTESIAN_POINT('Ctrl Pts',(8.05875206907788,-1.21878096033793,14.8724467501051));
#22787=CARTESIAN_POINT('Ctrl Pts',(5.38514975673243,-3.68773939197872,15.0709628675167));
#22788=CARTESIAN_POINT('Ctrl Pts',(1.86107937002522,-2.77953623668677,15.2694789849284));
#22789=CARTESIAN_POINT('Ctrl Pts',(0.713817534175901,0.674113331777405,
15.46799510234));
#22790=CARTESIAN_POINT('Ctrl Pts',(2.9940048152212,3.5104227339951,15.6665112197517));
#22791=CARTESIAN_POINT('Ctrl Pts',(6.61348907494099,3.13195377174095,15.8650273371633));
#22792=CARTESIAN_POINT('Ctrl Pts',(8.257615478175,-0.114698878595687,16.063543454575));
#22793=CARTESIAN_POINT('Ctrl Pts',(6.42072433944188,-3.25631247771842,16.2620595719866));
#22794=CARTESIAN_POINT('Ctrl Pts',(2.78500562221897,-3.41585705137789,16.4605756893983));
#22795=CARTESIAN_POINT('Ctrl Pts',(0.67998136903583,-0.447224713876356,
16.65909180681));
#22796=CARTESIAN_POINT('Ctrl Pts',(2.03339274915041,2.93096750947701,16.8576079242216));
#22797=CARTESIAN_POINT('Ctrl Pts',(5.60581136526813,3.62503544056518,17.0561240416333));
#22798=CARTESIAN_POINT('Ctrl Pts',(8.12568420335589,0.999364870669326,17.2546401590449));
#22799=CARTESIAN_POINT('Ctrl Pts',(7.28535965135699,-2.54150503784963,17.4531562764566));
#22800=CARTESIAN_POINT('Ctrl Pts',(3.85439094932391,-3.75491297725849,17.6516723938682));
#22801=CARTESIAN_POINT('Ctrl Pts',(0.974793970633971,-1.52964303811135,
17.8501885112799));
#22802=CARTESIAN_POINT('Ctrl Pts',(1.2836488526281,2.09644489844015,18.0487046286916));
#22803=CARTESIAN_POINT('Ctrl Pts',(4.49811216942012,3.80264847561477,18.2472207461032));
#22804=CARTESIAN_POINT('Ctrl Pts',(7.67443956106538,2.02645891285741,18.4457368635149));
#22805=CARTESIAN_POINT('Ctrl Pts',(7.90381082245328,-1.60552317494378,18.6442529809265));
#22806=CARTESIAN_POINT('Ctrl Pts',(4.9761721155001,-3.76719767944954,18.8427690983382));
#22807=CARTESIAN_POINT('Ctrl Pts',(1.57259927845708,-2.47894420875808,19.0412852157498));
#22808=CARTESIAN_POINT('Ctrl Pts',(0.810019572635768,1.07947921368855,19.2398013331615));
#22809=CARTESIAN_POINT('Ctrl Pts',(3.38678898688482,3.6493361063157,19.4383174505731));
#22810=CARTESIAN_POINT('Ctrl Pts',(6.94315110686829,2.87720041011993,19.6368335679848));
#22811=CARTESIAN_POINT('Ctrl Pts',(8.22225715251285,-0.529820690755693,
19.8353496853965));
#22812=CARTESIAN_POINT('Ctrl Pts',(6.05272613795891,-3.45164208273989,20.0338658028081));
#22813=CARTESIAN_POINT('Ctrl Pts',(2.42137329831411,-3.212515309774,20.2323819202198));
#22814=CARTESIAN_POINT('Ctrl Pts',(0.65372248686789,-0.0314281299545405,
20.4308980376314));
#22815=CARTESIAN_POINT('Ctrl Pts',(2.36855469553213,3.178440343651,20.6294141550431));
#22816=CARTESIAN_POINT('Ctrl Pts',(5.99545920128352,3.47755359131801,20.8279302724548));
#22817=CARTESIAN_POINT('Ctrl Pts',(8.21298586010566,0.591989447683331,21.0264463898664));
#22818=CARTESIAN_POINT('Ctrl Pts',(6.99036591797756,-2.83570744333498,21.2249625072781));
#22819=CARTESIAN_POINT('Ctrl Pts',(3.44725150283742,-3.6665172604341,21.4234786246897));
#22820=CARTESIAN_POINT('Ctrl Pts',(0.828359319011244,-1.13960058009792,
21.6219947421014));
#22821=CARTESIAN_POINT('Ctrl Pts',(1.53202116508044,2.43094114262164,21.820510859513));
#22822=CARTESIAN_POINT('Ctrl Pts',(4.91383661347899,3.77527223251319,22.0190269769247));
#22823=CARTESIAN_POINT('Ctrl Pts',(7.87680396956558,1.66228269728872,22.2175430943363));
#22824=CARTESIAN_POINT('Ctrl Pts',(7.7074930081086,-1.97299730385434,22.416059211748));
#22825=CARTESIAN_POINT('Ctrl Pts',(4.56095756308617,-3.80143701374933,22.6145753291597));
#22826=CARTESIAN_POINT('Ctrl Pts',(1.31873095853907,-2.14860623751896,22.8130914465713));
#22827=CARTESIAN_POINT('Ctrl Pts',(0.949990286798536,1.47190262315773,23.011607563983));
#22828=CARTESIAN_POINT('Ctrl Pts',(3.7924065803434,3.74442240079083,23.2101236813946));
#22829=CARTESIAN_POINT('Ctrl Pts',(7.24297719250067,2.58796472414074,23.4086397988063));
#22830=CARTESIAN_POINT('Ctrl Pts',(8.14168123233833,-0.938680920498277,
23.6071559162179));
#22831=CARTESIAN_POINT('Ctrl Pts',(5.66560616055497,-3.60535681683013,23.8056720336296));
#22832=CARTESIAN_POINT('Ctrl Pts',(2.08209581503262,-2.97097481614092,24.0041881510412));
#22833=CARTESIAN_POINT('Ctrl Pts',(0.673241827254791,0.385434817028999,
24.2027042684529));
#22834=CARTESIAN_POINT('Ctrl Pts',(2.72851506381635,3.38643791990783,24.4012203858645));
#22835=CARTESIAN_POINT('Ctrl Pts',(6.36713580394013,3.29091791303403,24.5997365032762));
#22836=CARTESIAN_POINT('Ctrl Pts',(8.25465969525897,0.17151120336101,24.7982954766299));
#22837=CARTESIAN_POINT('Ctrl Pts',(7.19525837483205,-1.99900958588141,24.9306824108463));
#22838=CARTESIAN_POINT('Ctrl Pts',(6.32311239899223,-2.62025147071356,24.9968973059255));
#22839=CARTESIAN_POINT('Ctrl Pts',(5.99341579333084,3.0962819108244,-0.27495920519366));
#22840=CARTESIAN_POINT('Ctrl Pts',(7.02329163031133,2.58506739568259,-0.208787166056442));
#22841=CARTESIAN_POINT('Ctrl Pts',(8.51497056474962,0.462964065771816,-0.0764430877820045));
#22842=CARTESIAN_POINT('Ctrl Pts',(7.04304871618797,-3.16665160770128,0.122073029629653));
#22843=CARTESIAN_POINT('Ctrl Pts',(3.19892054011338,-3.88657631350085,0.320589147041309));
#22844=CARTESIAN_POINT('Ctrl Pts',(0.508208668906595,-1.05209144762919,
0.519105264452963));
#22845=CARTESIAN_POINT('Ctrl Pts',(1.43231541168923,2.74837799923302,0.717621381864618));
#22846=CARTESIAN_POINT('Ctrl Pts',(5.12636543519397,4.03063520713254,0.916137499276276));
#22847=CARTESIAN_POINT('Ctrl Pts',(8.20668654383497,1.62239064105283,1.11465361668793));
#22848=CARTESIAN_POINT('Ctrl Pts',(7.85276047702285,-2.27196140132349,1.31316973409959));
#22849=CARTESIAN_POINT('Ctrl Pts',(4.38850729527858,-4.08551042322263,1.51168585151124));
#22850=CARTESIAN_POINT('Ctrl Pts',(0.986527733847538,-2.15772261402933,
1.7102019689229));
#22851=CARTESIAN_POINT('Ctrl Pts',(0.7622359790706,1.74611650720567,1.90871808633455));
#22852=CARTESIAN_POINT('Ctrl Pts',(3.92106229159746,4.0508692911502,2.10723420374621));
#22853=CARTESIAN_POINT('Ctrl Pts',(7.57019895508782,2.64592661456843,2.30575032115786));
#22854=CARTESIAN_POINT('Ctrl Pts',(8.36784367179503,-1.18211240346562,2.50426643856952));
#22855=CARTESIAN_POINT('Ctrl Pts',(5.58352459826198,-3.92759167890361,2.70278255598118));
#22856=CARTESIAN_POINT('Ctrl Pts',(1.7670702556363,-3.07625912870098,2.90129867339283));
#22857=CARTESIAN_POINT('Ctrl Pts',(0.413515851644582,0.592254017343965,
3.09981479080449));
#22858=CARTESIAN_POINT('Ctrl Pts',(2.76242132641212,3.7183916776686,3.29833090821614));
#22859=CARTESIAN_POINT('Ctrl Pts',(6.66270343294158,3.43929724324088,3.4968470256278));
#22860=CARTESIAN_POINT('Ctrl Pts',(8.54255816261418,0.0105596738669375,
3.69536314303945));
#22861=CARTESIAN_POINT('Ctrl Pts',(6.6804502327146,-3.42784816997514,3.89387926045112));
#22862=CARTESIAN_POINT('Ctrl Pts',(2.78166270604797,-3.72709790290783,4.09239537786277));
#22863=CARTESIAN_POINT('Ctrl Pts',(0.416631015022661,-0.613142253174304,
4.29091149527442));
#22864=CARTESIAN_POINT('Ctrl Pts',(1.75120620592284,3.06231739833558,4.48942761268608));
#22865=CARTESIAN_POINT('Ctrl Pts',(5.56320969933569,3.93336503336498,4.68794373009773));
#22866=CARTESIAN_POINT('Ctrl Pts',(8.36168121106336,1.20231178852842,4.88645984750939));
#22867=CARTESIAN_POINT('Ctrl Pts',(7.58383376163584,-2.62979572036334,5.08497596492104));
#22868=CARTESIAN_POINT('Ctrl Pts',(3.94200524984668,-4.05358633333867,5.2834920823327));
#22869=CARTESIAN_POINT('Ctrl Pts',(0.771312951433223,-1.76517968922739,
5.48200819974436));
#22870=CARTESIAN_POINT('Ctrl Pts',(0.97541656054666,2.13974493679014,5.68052431715601));
#22871=CARTESIAN_POINT('Ctrl Pts',(4.36740187430494,4.08513185206935,5.87904043456767));
#22872=CARTESIAN_POINT('Ctrl Pts',(7.84095326483218,2.28943272461384,6.07755655197932));
#22873=CARTESIAN_POINT('Ctrl Pts',(8.21505844260491,-1.60288534238506,6.27607266939098));
#22874=CARTESIAN_POINT('Ctrl Pts',(5.14711900207072,-4.02731150295548,6.47458878680263));
#22875=CARTESIAN_POINT('Ctrl Pts',(1.44669552446588,-2.76360239669899,6.6731049042143));
#22876=CARTESIAN_POINT('Ctrl Pts',(0.502565441067234,1.03096121515846,6.87162102162594));
#22877=CARTESIAN_POINT('Ctrl Pts',(3.17934512299035,3.88139015713774,7.07013713903761));
#22878=CARTESIAN_POINT('Ctrl Pts',(7.0256906552799,3.17731582507866,7.26865325644925));
#22879=CARTESIAN_POINT('Ctrl Pts',(8.51919196471455,-0.436483900631263,
7.46716937386092));
#22880=CARTESIAN_POINT('Ctrl Pts',(6.2921289615216,-3.65055997294754,7.66568549127257));
#22881=CARTESIAN_POINT('Ctrl Pts',(2.38400358079477,-3.52152266305215,7.86420160868423));
#22882=CARTESIAN_POINT('Ctrl Pts',(0.373802705776339,-0.16754188479758,
8.06271772609589));
#22883=CARTESIAN_POINT('Ctrl Pts',(2.10243005973299,3.33987056457006,8.26123384350753));
#22884=CARTESIAN_POINT('Ctrl Pts',(5.98684159389007,3.78869308197905,8.4597499609192));
#22885=CARTESIAN_POINT('Ctrl Pts',(8.4697671146088,0.767902543495819,8.65826607833084));
#22886=CARTESIAN_POINT('Ctrl Pts',(7.27739066026635,-2.95611853726567,8.85678219574251));
#22887=CARTESIAN_POINT('Ctrl Pts',(3.50166790634439,-3.97298249293629,9.05529831315416));
#22888=CARTESIAN_POINT('Ctrl Pts',(0.600333929022254,-1.35146465571633,
9.25381443056581));
#22889=CARTESIAN_POINT('Ctrl Pts',(1.23037519550738,2.50769880562501,9.45233054797748));
#22890=CARTESIAN_POINT('Ctrl Pts',(4.81481189860833,4.07035940226423,9.65084666538912));
#22891=CARTESIAN_POINT('Ctrl Pts',(8.07108508884113,1.90546228475562,9.84936278280079));
#22892=CARTESIAN_POINT('Ctrl Pts',(8.01716171947454,-2.00442094739626,10.0478789002124));
#22893=CARTESIAN_POINT('Ctrl Pts',(4.70242378644322,-4.07869360405195,10.2463950176241));
#22894=CARTESIAN_POINT('Ctrl Pts',(1.16244523581599,-2.41777624309588,10.4449111350357));
#22895=CARTESIAN_POINT('Ctrl Pts',(0.639071086725107,1.45729461030662,10.6434272524474));
#22896=CARTESIAN_POINT('Ctrl Pts',(3.61159742927608,3.99780278027315,10.841943369859));
#22897=CARTESIAN_POINT('Ctrl Pts',(7.35784118240728,2.87719921033794,11.0404594872707));
#22898=CARTESIAN_POINT('Ctrl Pts',(8.44706357811351,-0.878288666292467,
11.2389756046823));
#22899=CARTESIAN_POINT('Ctrl Pts',(5.88177546561389,-3.82945648915419,11.437491722094));
#22900=CARTESIAN_POINT('Ctrl Pts',(2.01121890138154,-3.27368090323489,11.6360078395057));
#22901=CARTESIAN_POINT('Ctrl Pts',(0.379975961147697,0.280069381853164,
11.8345239569173));
#22902=CARTESIAN_POINT('Ctrl Pts',(2.4819079000476,3.57733745452462,12.033040074329));
#22903=CARTESIAN_POINT('Ctrl Pts',(6.39210543142176,3.59854793451629,12.2315561917406));
#22904=CARTESIAN_POINT('Ctrl Pts',(8.52968403588164,0.324276667717884,12.4300723091523));
#22905=CARTESIAN_POINT('Ctrl Pts',(6.93708988851933,-3.24696100298028,12.6285884265639));
#22906=CARTESIAN_POINT('Ctrl Pts',(3.07279041513639,-3.84469355089646,12.8271045439756));
#22907=CARTESIAN_POINT('Ctrl Pts',(0.475637566686629,-0.921528878727684,
13.0256206613872));
#22908=CARTESIAN_POINT('Ctrl Pts',(1.52405451869475,2.84555441124189,13.2241367787989));
#22909=CARTESIAN_POINT('Ctrl Pts',(5.25792096951678,4.00673309958052,13.4226528962106));
#22910=CARTESIAN_POINT('Ctrl Pts',(8.257833049161,1.4986218314684,13.6211690136222));
#22911=CARTESIAN_POINT('Ctrl Pts',(7.77652833946771,-2.38189880309254,13.8196851310339));
#22912=CARTESIAN_POINT('Ctrl Pts',(4.25477653818775,-4.08112182230083,14.0182012484455));
#22913=CARTESIAN_POINT('Ctrl Pts',(0.917730954110628,-2.04293110781465,
14.2167173658572));
#22914=CARTESIAN_POINT('Ctrl Pts',(0.821394455796449,1.86613705453794,14.4152334832688));
#22915=CARTESIAN_POINT('Ctrl Pts',(4.05399017588675,4.06623240003544,14.6137496006805));
#22916=CARTESIAN_POINT('Ctrl Pts',(7.65516844441363,2.54254946152231,14.8122657180922));
#22917=CARTESIAN_POINT('Ctrl Pts',(8.32703870473431,-1.30955190943392,15.0107818355038));
#22918=CARTESIAN_POINT('Ctrl Pts',(5.45431495277465,-3.96239055204922,15.2092979529155));
#22919=CARTESIAN_POINT('Ctrl Pts',(1.66778295557931,-2.98654729975826,15.4078140703271));
#22920=CARTESIAN_POINT('Ctrl Pts',(0.435076688703739,0.724319159497842,
15.6063301877388));
#22921=CARTESIAN_POINT('Ctrl Pts',(2.88508510279309,3.77186791049719,15.8048463051504));
#22922=CARTESIAN_POINT('Ctrl Pts',(6.77413709632598,3.36521177759866,16.0033624225621));
#22923=CARTESIAN_POINT('Ctrl Pts',(8.54071283123811,-0.123241288109086,
16.2018785399737));
#22924=CARTESIAN_POINT('Ctrl Pts',(6.56701585333057,-3.49883232646441,16.4003946573854));
#22925=CARTESIAN_POINT('Ctrl Pts',(2.66052031127365,-3.67025927509159,16.598910774797));
#22926=CARTESIAN_POINT('Ctrl Pts',(0.398720513058523,-0.480532595324168,
16.7974268922087));
#22927=CARTESIAN_POINT('Ctrl Pts',(1.85292968989636,3.14925669454191,16.9959430096203));
#22928=CARTESIAN_POINT('Ctrl Pts',(5.69141073963082,3.89501660876095,17.194459127032));
#22929=CARTESIAN_POINT('Ctrl Pts',(8.39895573256671,1.07379440374864,17.3929752444437));
#22930=CARTESIAN_POINT('Ctrl Pts',(7.49604646714037,-2.73078829048094,17.5914913618553));
#22931=CARTESIAN_POINT('Ctrl Pts',(3.80955007347359,-4.03456701338995,17.790007479267));
#22932=CARTESIAN_POINT('Ctrl Pts',(0.715489824289806,-1.64356601103751,
17.9885235966786));
#22933=CARTESIAN_POINT('Ctrl Pts',(1.04734724052415,2.25258148028018,18.1870397140903));
#22934=CARTESIAN_POINT('Ctrl Pts',(4.50121361298798,4.08585770060491,18.3855558315019));
#22935=CARTESIAN_POINT('Ctrl Pts',(7.91410381728119,2.1773831599618,18.5840719489136));
#22936=CARTESIAN_POINT('Ctrl Pts',(8.16055792437237,-1.72509746033864,18.7825880663253));
#22937=CARTESIAN_POINT('Ctrl Pts',(5.0148779510323,-4.04776664132528,18.9811041837369));
#22938=CARTESIAN_POINT('Ctrl Pts',(1.35781777968586,-2.66356812881232,19.1796203011486));
#22939=CARTESIAN_POINT('Ctrl Pts',(0.538443550556935,1.1598754095142,19.3781364185603));
#22940=CARTESIAN_POINT('Ctrl Pts',(3.30712259659747,3.92112711119714,19.5766525359719));
#22941=CARTESIAN_POINT('Ctrl Pts',(7.12835131317638,3.09148519177063,19.7751686533836));
#22942=CARTESIAN_POINT('Ctrl Pts',(8.50272112937199,-0.569280059186615,
19.9736847707952));
#22943=CARTESIAN_POINT('Ctrl Pts',(6.17161031033075,-3.70870946234774,20.1722008882069));
#22944=CARTESIAN_POINT('Ctrl Pts',(2.26980580259814,-3.45177328404759,20.3707170056185));
#22945=CARTESIAN_POINT('Ctrl Pts',(0.370505952442893,-0.0337687976193256,
20.5692331230302));
#22946=CARTESIAN_POINT('Ctrl Pts',(2.21305343742525,3.41516052227788,20.7677492404418));
#22947=CARTESIAN_POINT('Ctrl Pts',(6.11007831343283,3.73655077808788,20.9662653578534));
#22948=CARTESIAN_POINT('Ctrl Pts',(8.49275934044528,0.636078948397367,21.1647814752652));
#22949=CARTESIAN_POINT('Ctrl Pts',(7.17908253400595,-3.04690196012391,21.3632975926768));
#22950=CARTESIAN_POINT('Ctrl Pts',(3.37208816940477,-3.93958786330456,21.5618137100885));
#22951=CARTESIAN_POINT('Ctrl Pts',(0.558149183206385,-1.22447442503984,
21.7603298275001));
#22952=CARTESIAN_POINT('Ctrl Pts',(1.31421753683424,2.61198994621562,21.9588459449118));
#22953=CARTESIAN_POINT('Ctrl Pts',(4.94789989808116,4.05644256154919,22.1573620623234));
#22954=CARTESIAN_POINT('Ctrl Pts',(8.13153968654471,1.78608425229248,22.3558781797351));
#22955=CARTESIAN_POINT('Ctrl Pts',(7.94961898046267,-2.11993989949929,22.5543942971467));
#22956=CARTESIAN_POINT('Ctrl Pts',(4.56873953270021,-4.0845560128934,22.7529104145584));
#22957=CARTESIAN_POINT('Ctrl Pts',(1.08504215066615,-2.30862763082918,22.95142653197));
#22958=CARTESIAN_POINT('Ctrl Pts',(0.688838840573486,1.58152527269752,23.1499426493817));
#22959=CARTESIAN_POINT('Ctrl Pts',(3.74294930484078,4.02329513198439,23.3484587667933));
#22960=CARTESIAN_POINT('Ctrl Pts',(7.45050749686758,2.78070814718547,23.546974884205));
#22961=CARTESIAN_POINT('Ctrl Pts',(8.41614416964521,-1.00859090500303,23.7454910016166));
#22962=CARTESIAN_POINT('Ctrl Pts',(5.75565886205016,-3.87387238340306,23.9440071190283));
#22963=CARTESIAN_POINT('Ctrl Pts',(1.90526000600476,-3.19224361880315,24.14252323644));
#22964=CARTESIAN_POINT('Ctrl Pts',(0.391479031532891,0.414140782493564,
24.3410393538516));
#22965=CARTESIAN_POINT('Ctrl Pts',(2.59982251484541,3.6386490998064,24.5395554712633));
#22966=CARTESIAN_POINT('Ctrl Pts',(6.50943621328541,3.53601506509354,24.7380715886749));
#22967=CARTESIAN_POINT('Ctrl Pts',(8.53753691096405,0.184284815040506,24.9366305620286));
#22968=CARTESIAN_POINT('Ctrl Pts',(7.39923473266516,-2.14788949397592,25.069017496245));
#22969=CARTESIAN_POINT('Ctrl Pts',(6.46213408444902,-2.81539950847165,25.1352323913243));
#22970=CARTESIAN_POINT('Ctrl Pts',(6.0999485000484,3.31089917470656,-0.136624119794918));
#22971=CARTESIAN_POINT('Ctrl Pts',(7.2012096761669,2.76425007587486,-0.0704520806576993));
#22972=CARTESIAN_POINT('Ctrl Pts',(8.79628360522135,0.495054193199949,0.061891997616738));
#22973=CARTESIAN_POINT('Ctrl Pts',(7.22233621477278,-3.38614651265062,0.260408115028396));
#22974=CARTESIAN_POINT('Ctrl Pts',(3.11175417728552,-4.15597244676529,0.458924232440051));
#22975=CARTESIAN_POINT('Ctrl Pts',(0.234536930817258,-1.12501665093665,
0.657440349851707));
#22976=CARTESIAN_POINT('Ctrl Pts',(1.22269767978634,2.93888047390986,0.855956467263361));
#22977=CARTESIAN_POINT('Ctrl Pts',(5.17279897107673,4.31001671203934,1.05447258467502));
#22978=CARTESIAN_POINT('Ctrl Pts',(8.46663102841521,1.73484585358162,1.25298870208667));
#22979=CARTESIAN_POINT('Ctrl Pts',(8.08817274965877,-2.42944129289705,1.45150481949833));
#22980=CARTESIAN_POINT('Ctrl Pts',(4.38379655564558,-4.36869557685114,1.65002093690999));
#22981=CARTESIAN_POINT('Ctrl Pts',(0.746010447431816,-2.30728410002347,
1.84853705432164));
#22982=CARTESIAN_POINT('Ctrl Pts',(0.506172019545635,1.86714771753756,2.04705317173329));
#22983=CARTESIAN_POINT('Ctrl Pts',(3.88395083052018,4.33165331167866,2.24556928914495));
#22984=CARTESIAN_POINT('Ctrl Pts',(7.78602561424836,2.82932772170484,2.4440854065566));
#22985=CARTESIAN_POINT('Ctrl Pts',(8.63895868375428,-1.26404994563383,2.64260152396827));
#22986=CARTESIAN_POINT('Ctrl Pts',(5.66164589758561,-4.19983077212884,2.84111764137992));
#22987=CARTESIAN_POINT('Ctrl Pts',(1.58065589175627,-3.28948852324876,3.03963375879158));
#22988=CARTESIAN_POINT('Ctrl Pts',(0.133280527313607,0.633305814430374,
3.23814987620323));
#22989=CARTESIAN_POINT('Ctrl Pts',(2.6449992344131,3.97613017528841,3.43666599361489));
#22990=CARTESIAN_POINT('Ctrl Pts',(6.81562748453676,3.67769044685756,3.63518211102655));
#22991=CARTESIAN_POINT('Ctrl Pts',(8.82578342391765,0.0112916124882134,
3.8336982284382));
#22992=CARTESIAN_POINT('Ctrl Pts',(6.83460439504253,-3.66544778668689,4.03221434584986));
#22993=CARTESIAN_POINT('Ctrl Pts',(2.66557432085276,-3.98543986826524,4.23073046326151));
#22994=CARTESIAN_POINT('Ctrl Pts',(0.13661161671523,-0.655641908094887,
4.42924658067317));
#22995=CARTESIAN_POINT('Ctrl Pts',(1.56369223320815,3.27458042867263,4.62776269808482));
#22996=CARTESIAN_POINT('Ctrl Pts',(5.63992288139177,4.20600430382654,4.82627881549648));
#22997=CARTESIAN_POINT('Ctrl Pts',(8.63236907507575,1.28564944117731,5.02479493290813));
#22998=CARTESIAN_POINT('Ctrl Pts',(7.80060551073305,-2.81207872246989,5.22331105031979));
#22999=CARTESIAN_POINT('Ctrl Pts',(3.90634543966123,-4.33455868431544,5.42182716773146));
#23000=CARTESIAN_POINT('Ctrl Pts',(0.515878157801087,-1.88753225468275,
5.62034328514309));
#23001=CARTESIAN_POINT('Ctrl Pts',(0.734129108596551,2.28806030889307,5.81885940255477));
#23002=CARTESIAN_POINT('Ctrl Pts',(4.36122822275595,4.36829076522382,6.0173755199664));
#23003=CARTESIAN_POINT('Ctrl Pts',(8.07554712633902,2.44812363240269,6.21589163737808));
#23004=CARTESIAN_POINT('Ctrl Pts',(8.47558322124728,-1.71398855469165,6.41440775478972));
#23005=CARTESIAN_POINT('Ctrl Pts',(5.19499106127511,-4.3064626269354,6.61292387220138));
#23006=CARTESIAN_POINT('Ctrl Pts',(1.2380745430358,-2.9551601430283,6.81143998961304));
#23007=CARTESIAN_POINT('Ctrl Pts',(0.228502545404632,1.10242178675316,7.00995610702469));
#23008=CARTESIAN_POINT('Ctrl Pts',(3.09082189971391,4.15042681451437,7.20847222443635));
#23009=CARTESIAN_POINT('Ctrl Pts',(7.20377498837598,3.39754991503151,7.406988341848));
#23010=CARTESIAN_POINT('Ctrl Pts',(8.80079760945692,-0.466738568384383,
7.60550445925966));
#23011=CARTESIAN_POINT('Ctrl Pts',(6.41936682516261,-3.90359674918315,7.80402057667131));
#23012=CARTESIAN_POINT('Ctrl Pts',(2.24035164813274,-3.7656152813635,8.00253669408298));
#23013=CARTESIAN_POINT('Ctrl Pts',(0.0908146841936848,-0.179154968469096,
8.20105281149462));
#23014=CARTESIAN_POINT('Ctrl Pts',(1.93926099639212,3.57137205666049,8.39956892890629));
#23015=CARTESIAN_POINT('Ctrl Pts',(6.09291861319388,4.05130448700034,8.59808504631793));
#23016=CARTESIAN_POINT('Ctrl Pts',(8.7479469000777,0.821129332128062,8.7966011637296));
#23017=CARTESIAN_POINT('Ctrl Pts',(7.47292145590854,-3.16102044557099,8.99511728114126));
#23018=CARTESIAN_POINT('Ctrl Pts',(3.43548632890085,-4.24836782820074,9.19363339855291));
#23019=CARTESIAN_POINT('Ctrl Pts',(0.333047808208697,-1.44514076628925,
9.39214951596456));
#23020=CARTESIAN_POINT('Ctrl Pts',(1.00676007644372,2.68151871989772,9.59066563337622));
#23021=CARTESIAN_POINT('Ctrl Pts',(4.83965025372247,4.352494370297,9.78918175078787));
#23022=CARTESIAN_POINT('Ctrl Pts',(8.32163042499515,2.03753846960017,9.98769786819953));
#23023=CARTESIAN_POINT('Ctrl Pts',(8.26396938369623,-2.14335640346512,10.1862139856111));
#23024=CARTESIAN_POINT('Ctrl Pts',(4.71947201461794,-4.36140625319899,10.3847301030228));
#23025=CARTESIAN_POINT('Ctrl Pts',(0.934121584873003,-2.58536321899705,
10.5832462204345));
#23026=CARTESIAN_POINT('Ctrl Pts',(0.37447001302165,1.5583062723393,10.7817623378461));
#23027=CARTESIAN_POINT('Ctrl Pts',(3.55303556286365,4.27490852159572,10.9802784552578));
#23028=CARTESIAN_POINT('Ctrl Pts',(7.55894836658157,3.07663086415728,11.1787945726694));
#23029=CARTESIAN_POINT('Ctrl Pts',(8.72366967907197,-0.939166814951776,
11.3773106900811));
#23030=CARTESIAN_POINT('Ctrl Pts',(5.98056987770475,-4.09489338977514,11.5758268074927));
#23031=CARTESIAN_POINT('Ctrl Pts',(1.84172758128094,-3.50059449137405,11.7743429249044));
#23032=CARTESIAN_POINT('Ctrl Pts',(0.0974158357370281,0.299482253859507,
11.9728590423161));
#23033=CARTESIAN_POINT('Ctrl Pts',(2.34504215731444,3.82529884776504,12.1713751597277));
#23034=CARTESIAN_POINT('Ctrl Pts',(6.52627311509865,3.84797952178704,12.3698912771394));
#23035=CARTESIAN_POINT('Ctrl Pts',(8.81201693339725,0.346753746088307,12.568407394551));
#23036=CARTESIAN_POINT('Ctrl Pts',(7.10903290287004,-3.47202251432246,12.7669235119627));
#23037=CARTESIAN_POINT('Ctrl Pts',(2.97688140448274,-4.11118660098796,12.9654396293744));
#23038=CARTESIAN_POINT('Ctrl Pts',(0.199708178602426,-0.985404201530036,
13.163955746786));
#23039=CARTESIAN_POINT('Ctrl Pts',(1.32079563805398,3.0427926213136,13.3624718641977));
#23040=CARTESIAN_POINT('Ctrl Pts',(5.3134732128164,4.28445784161121,13.5609879816093));
#23041=CARTESIAN_POINT('Ctrl Pts',(8.52132272870291,1.60249806959112,13.759504099021));
#23042=CARTESIAN_POINT('Ctrl Pts',(8.00665661883263,-2.546998951815,13.9580202164326));
#23043=CARTESIAN_POINT('Ctrl Pts',(4.24079631663729,-4.36400278220629,14.1565363338443));
#23044=CARTESIAN_POINT('Ctrl Pts',(0.672445052608722,-2.18453587678811,
14.3550524512559));
#23045=CARTESIAN_POINT('Ctrl Pts',(0.569431037105937,1.99548743031406,14.5535685686676));
#23046=CARTESIAN_POINT('Ctrl Pts',(4.02609254599198,4.3480813069304,14.7520846860792));
#23047=CARTESIAN_POINT('Ctrl Pts',(7.87688472210303,2.7187850319364,14.9506008034909));
#23048=CARTESIAN_POINT('Ctrl Pts',(8.59532534039074,-1.40032285852991,15.1491169209026));
#23049=CARTESIAN_POINT('Ctrl Pts',(5.52348014881688,-4.2370417121197,15.3476330383142));
#23050=CARTESIAN_POINT('Ctrl Pts',(1.47448654113341,-3.19355836282975,15.5461491557259));
#23051=CARTESIAN_POINT('Ctrl Pts',(0.156335843231577,0.774524987218279,
15.7446652731375));
#23052=CARTESIAN_POINT('Ctrl Pts',(2.77616539036498,4.03331308699926,15.9431813905492));
#23053=CARTESIAN_POINT('Ctrl Pts',(6.93478511771097,3.59846978345639,16.1416975079608));
#23054=CARTESIAN_POINT('Ctrl Pts',(8.82381018430121,-0.131783697622486,
16.3402136253725));
#23055=CARTESIAN_POINT('Ctrl Pts',(6.71330736721926,-3.74135217521042,16.5387297427841));
#23056=CARTESIAN_POINT('Ctrl Pts',(2.53603500032833,-3.92466149880528,16.7372458601958));
#23057=CARTESIAN_POINT('Ctrl Pts',(0.117459657081213,-0.513840476771981,
16.9357619776075));
#23058=CARTESIAN_POINT('Ctrl Pts',(1.6724666306423,3.3675458796068,17.1342780950191));
#23059=CARTESIAN_POINT('Ctrl Pts',(5.77701011399349,4.16499777695671,17.3327942124308));
#23060=CARTESIAN_POINT('Ctrl Pts',(8.67222726177754,1.14822393682795,17.5313103298424));
#23061=CARTESIAN_POINT('Ctrl Pts',(7.70673328292373,-2.92007154311226,17.7298264472541));
#23062=CARTESIAN_POINT('Ctrl Pts',(3.76470919762329,-4.31422104952143,17.9283425646657));
#23063=CARTESIAN_POINT('Ctrl Pts',(0.456185677945633,-1.75748898396369,
18.1268586820774));
#23064=CARTESIAN_POINT('Ctrl Pts',(0.811045628420214,2.40871806212022,18.3253747994891));
#23065=CARTESIAN_POINT('Ctrl Pts',(4.50431505655582,4.36906692559506,18.5238909169007));
#23066=CARTESIAN_POINT('Ctrl Pts',(8.153768073497,2.32830740706619,18.7224070343124));
#23067=CARTESIAN_POINT('Ctrl Pts',(8.41730502629147,-1.84467174573349,18.920923151724));
#23068=CARTESIAN_POINT('Ctrl Pts',(5.05358378656449,-4.328335603201,19.1194392691357));
#23069=CARTESIAN_POINT('Ctrl Pts',(1.14303628091464,-2.84819204886657,19.3179553865473));
#23070=CARTESIAN_POINT('Ctrl Pts',(0.266867528478102,1.24027160533984,19.516471503959));
#23071=CARTESIAN_POINT('Ctrl Pts',(3.22745620631011,4.19291811607857,19.7149876213706));
#23072=CARTESIAN_POINT('Ctrl Pts',(7.31355151948446,3.30576997342133,19.9135037387823));
#23073=CARTESIAN_POINT('Ctrl Pts',(8.78318510623113,-0.60873942761753,20.112019856194));
#23074=CARTESIAN_POINT('Ctrl Pts',(6.29049448270258,-3.96577684195559,20.3105359736056));
#23075=CARTESIAN_POINT('Ctrl Pts',(2.11823830688215,-3.69103125832118,20.5090520910173));
#23076=CARTESIAN_POINT('Ctrl Pts',(0.0872894180178925,-0.0361094652841183,
20.7075682084289));
#23077=CARTESIAN_POINT('Ctrl Pts',(2.05755217931839,3.65188070090475,20.9060843258406));
#23078=CARTESIAN_POINT('Ctrl Pts',(6.2246974255821,3.99554796485774,21.1046004432522));
#23079=CARTESIAN_POINT('Ctrl Pts',(8.77253282078492,0.680168449111409,21.3031165606639));
#23080=CARTESIAN_POINT('Ctrl Pts',(7.36779915003431,-3.25809647691284,21.5016326780756));
#23081=CARTESIAN_POINT('Ctrl Pts',(3.29692483597213,-4.21265846617502,21.7001487954872));
#23082=CARTESIAN_POINT('Ctrl Pts',(0.287939047401517,-1.30934826998177,
21.8986649128989));
#23083=CARTESIAN_POINT('Ctrl Pts',(1.09641390858805,2.79303874980958,22.0971810303105));
#23084=CARTESIAN_POINT('Ctrl Pts',(4.98196318268333,4.33761289058522,22.2956971477222));
#23085=CARTESIAN_POINT('Ctrl Pts',(8.38627540352384,1.90988580729624,22.4942132651338));
#23086=CARTESIAN_POINT('Ctrl Pts',(8.19174495281671,-2.26688249514424,22.6927293825455));
#23087=CARTESIAN_POINT('Ctrl Pts',(4.57652150231426,-4.36767501203749,22.8912454999571));
#23088=CARTESIAN_POINT('Ctrl Pts',(0.851353342793238,-2.46864902413938,
23.0897616173688));
#23089=CARTESIAN_POINT('Ctrl Pts',(0.42768739434844,1.69114792223732,23.2882777347804));
#23090=CARTESIAN_POINT('Ctrl Pts',(3.69349202933814,4.30216786317793,23.4867938521921));
#23091=CARTESIAN_POINT('Ctrl Pts',(7.65803780123451,2.9734515702302,23.6853099696038));
#23092=CARTESIAN_POINT('Ctrl Pts',(8.6906071069521,-1.07850088950778,23.8838260870154));
#23093=CARTESIAN_POINT('Ctrl Pts',(5.84571156354535,-4.14238794997599,24.0823422044271));
#23094=CARTESIAN_POINT('Ctrl Pts',(1.7284241969769,-3.41351242146536,24.2808583218387));
#23095=CARTESIAN_POINT('Ctrl Pts',(0.109716235810993,0.442846747958131,
24.4793744392504));
#23096=CARTESIAN_POINT('Ctrl Pts',(2.47112996587446,3.89086027970496,24.677890556662));
#23097=CARTESIAN_POINT('Ctrl Pts',(6.6517366226307,3.78111221715306,24.8764066740737));
#23098=CARTESIAN_POINT('Ctrl Pts',(8.82041412666913,0.197058426719993,25.0749656474274));
#23099=CARTESIAN_POINT('Ctrl Pts',(7.60321109049825,-2.29676940207044,25.2073525816438));
#23100=CARTESIAN_POINT('Ctrl Pts',(6.60115576990582,-3.01054754622974,25.273567476723));
#23101=CARTESIAN_POINT('Ctrl Pts',(6.20648120676596,3.5255164385887,0.00171096560382468));
#23102=CARTESIAN_POINT('Ctrl Pts',(7.37912772202248,2.94343275606714,0.0678830047410433));
#23103=CARTESIAN_POINT('Ctrl Pts',(9.07759664569311,0.527144320628084,0.200227083015481));
#23104=CARTESIAN_POINT('Ctrl Pts',(7.40162371335757,-3.60564141759996,0.398743200427137));
#23105=CARTESIAN_POINT('Ctrl Pts',(3.02458781445768,-4.42536858002973,0.597259317838794));
#23106=CARTESIAN_POINT('Ctrl Pts',(-0.0391348072720899,-1.19794185424409,
0.795775435250448));
#23107=CARTESIAN_POINT('Ctrl Pts',(1.01307994788347,3.12938294858669,0.994291552662105));
#23108=CARTESIAN_POINT('Ctrl Pts',(5.21923250695947,4.58939821694615,1.19280767007376));
#23109=CARTESIAN_POINT('Ctrl Pts',(8.72657551299543,1.84730106611042,1.39132378748542));
#23110=CARTESIAN_POINT('Ctrl Pts',(8.32358502229467,-2.58692118447061,1.58983990489707));
#23111=CARTESIAN_POINT('Ctrl Pts',(4.37908581601258,-4.65188073047965,1.78835602230873));
#23112=CARTESIAN_POINT('Ctrl Pts',(0.505493161016087,-2.45684558601761,
1.98687213972038));
#23113=CARTESIAN_POINT('Ctrl Pts',(0.250108060020668,1.98817892786946,2.18538825713204));
#23114=CARTESIAN_POINT('Ctrl Pts',(3.8468393694429,4.61243733220712,2.38390437454369));
#23115=CARTESIAN_POINT('Ctrl Pts',(8.0018522734089,3.01272882884126,2.58242049195535));
#23116=CARTESIAN_POINT('Ctrl Pts',(8.91007369571349,-1.34598748780205,2.78093660936701));
#23117=CARTESIAN_POINT('Ctrl Pts',(5.73976719690925,-4.47206986535408,2.97945272677866));
#23118=CARTESIAN_POINT('Ctrl Pts',(1.39424152787623,-3.50271791779653,3.17796884419032));
#23119=CARTESIAN_POINT('Ctrl Pts',(-0.146954797017362,0.674357611516781,
3.37648496160198));
#23120=CARTESIAN_POINT('Ctrl Pts',(2.5275771424141,4.23386867290823,3.57500107901363));
#23121=CARTESIAN_POINT('Ctrl Pts',(6.96855153613195,3.91608365047424,3.77351719642529));
#23122=CARTESIAN_POINT('Ctrl Pts',(9.10900868522111,0.0120235511094912,
3.97203331383693));
#23123=CARTESIAN_POINT('Ctrl Pts',(6.98875855737045,-3.90304740339865,4.17054943124861));
#23124=CARTESIAN_POINT('Ctrl Pts',(2.54948593565754,-4.24378183362265,4.36906554866025));
#23125=CARTESIAN_POINT('Ctrl Pts',(-0.143407781592193,-0.698141563015474,
4.56758166607191));
#23126=CARTESIAN_POINT('Ctrl Pts',(1.37617826049345,3.48684345900968,4.76609778348356));
#23127=CARTESIAN_POINT('Ctrl Pts',(5.71663606344787,4.47864357428809,4.96461390089523));
#23128=CARTESIAN_POINT('Ctrl Pts',(8.90305693908813,1.36898709382619,5.16313001830687));
#23129=CARTESIAN_POINT('Ctrl Pts',(8.01737725983028,-2.99436172457643,5.36164613571854));
#23130=CARTESIAN_POINT('Ctrl Pts',(3.87068562947579,-4.61553103529222,5.56016225313019));
#23131=CARTESIAN_POINT('Ctrl Pts',(0.260443364168955,-2.00988482013811,
5.75867837054185));
#23132=CARTESIAN_POINT('Ctrl Pts',(0.492841656646439,2.436375680996,5.95719448795349));
#23133=CARTESIAN_POINT('Ctrl Pts',(4.35505457120696,4.6514496783783,6.15571060536516));
#23134=CARTESIAN_POINT('Ctrl Pts',(8.31014098784587,2.60681454019155,6.35422672277681));
#23135=CARTESIAN_POINT('Ctrl Pts',(8.73610799988966,-1.82509176699825,6.55274284018847));
#23136=CARTESIAN_POINT('Ctrl Pts',(5.24286312047947,-4.58561375091533,6.75125895760012));
#23137=CARTESIAN_POINT('Ctrl Pts',(1.02945356160573,-3.14671788935761,6.94977507501179));
#23138=CARTESIAN_POINT('Ctrl Pts',(-0.0455603502579819,1.17388235834786,
7.14829119242343));
#23139=CARTESIAN_POINT('Ctrl Pts',(3.00229867643747,4.41946347189101,7.34680730983509));
#23140=CARTESIAN_POINT('Ctrl Pts',(7.38185932147204,3.61778400498435,7.54532342724674));
#23141=CARTESIAN_POINT('Ctrl Pts',(9.08240325419932,-0.496993236137507,
7.7438395446584));
#23142=CARTESIAN_POINT('Ctrl Pts',(6.5466046888036,-4.15663352541875,7.94235566207006));
#23143=CARTESIAN_POINT('Ctrl Pts',(2.09669971547073,-4.00970789967487,8.1408717794817));
#23144=CARTESIAN_POINT('Ctrl Pts',(-0.192173337388976,-0.19076805214061,
8.33938789689338));
#23145=CARTESIAN_POINT('Ctrl Pts',(1.77609193305126,3.80287354875093,8.53790401430502));
#23146=CARTESIAN_POINT('Ctrl Pts',(6.1989956324977,4.3139158920216,8.73642013171668));
#23147=CARTESIAN_POINT('Ctrl Pts',(9.0261266855466,0.874356120760312,8.93493624912834));
#23148=CARTESIAN_POINT('Ctrl Pts',(7.66845225155073,-3.36592235387631,9.13345236653999));
#23149=CARTESIAN_POINT('Ctrl Pts',(3.36930475145732,-4.52375316346519,9.33196848395166));
#23150=CARTESIAN_POINT('Ctrl Pts',(0.0657616873951493,-1.53881687686219,
9.53048460136329));
#23151=CARTESIAN_POINT('Ctrl Pts',(0.783144957380055,2.85533863417045,9.72900071877498));
#23152=CARTESIAN_POINT('Ctrl Pts',(4.86448860883662,4.63462933832978,9.92751683618659));
#23153=CARTESIAN_POINT('Ctrl Pts',(8.57217576114917,2.16961465444475,10.1260329535983));
#23154=CARTESIAN_POINT('Ctrl Pts',(8.51077704791793,-2.28229185953398,10.3245490710099));
#23155=CARTESIAN_POINT('Ctrl Pts',(4.73652024279266,-4.644118902346,10.5230651884216));
#23156=CARTESIAN_POINT('Ctrl Pts',(0.705797933930029,-2.75295019489822,
10.7215813058332));
#23157=CARTESIAN_POINT('Ctrl Pts',(0.109868939318185,1.65931793437198,10.9200974232449));
#23158=CARTESIAN_POINT('Ctrl Pts',(3.49447369645122,4.55201426291826,11.1186135406565));
#23159=CARTESIAN_POINT('Ctrl Pts',(7.76005555075585,3.27606251797663,11.3171296580682));
#23160=CARTESIAN_POINT('Ctrl Pts',(9.00027578003045,-1.00004496361109,11.5156457754798));
#23161=CARTESIAN_POINT('Ctrl Pts',(6.07936428979557,-4.36033029039609,11.7141618928915));
#23162=CARTESIAN_POINT('Ctrl Pts',(1.67223626118035,-3.72750807951321,11.9126780103032));
#23163=CARTESIAN_POINT('Ctrl Pts',(-0.185144289673645,0.31889512586586,
12.1111941277148));
#23164=CARTESIAN_POINT('Ctrl Pts',(2.20817641458127,4.07326024100545,12.3097102451265));
#23165=CARTESIAN_POINT('Ctrl Pts',(6.66044079877556,4.09741110905781,12.5082263625381));
#23166=CARTESIAN_POINT('Ctrl Pts',(9.09434983091284,0.369230824458725,12.7067424799498));
#23167=CARTESIAN_POINT('Ctrl Pts',(7.28097591722075,-3.69708402566464,12.9052585973614));
#23168=CARTESIAN_POINT('Ctrl Pts',(2.8809723938291,-4.37767965107946,13.1037747147731));
#23169=CARTESIAN_POINT('Ctrl Pts',(-0.0762212094817758,-1.04927952433239,
13.3022908321848));
#23170=CARTESIAN_POINT('Ctrl Pts',(1.11753675741321,3.24003083138531,13.5008069495964));
#23171=CARTESIAN_POINT('Ctrl Pts',(5.369025456116,4.5621825836419,13.6993230670081));
#23172=CARTESIAN_POINT('Ctrl Pts',(8.78481240824481,1.70637430771384,13.8978391844197));
#23173=CARTESIAN_POINT('Ctrl Pts',(8.23678489819753,-2.71209910053747,14.0963553018314));
#23174=CARTESIAN_POINT('Ctrl Pts',(4.22681609508684,-4.64688374211174,14.294871419243));
#23175=CARTESIAN_POINT('Ctrl Pts',(0.427159151106815,-2.32614064576156,
14.4933875366547));
#23176=CARTESIAN_POINT('Ctrl Pts',(0.317467618415429,2.12483780609018,14.6919036540663));
#23177=CARTESIAN_POINT('Ctrl Pts',(3.99819491609722,4.62993021382537,14.890419771478));
#23178=CARTESIAN_POINT('Ctrl Pts',(8.09860099979244,2.8950206023505,15.0889358888896));
#23179=CARTESIAN_POINT('Ctrl Pts',(8.86361197604717,-1.49109380762589,15.2874520063013));
#23180=CARTESIAN_POINT('Ctrl Pts',(5.59264534485911,-4.5116928721902,15.485968123713));
#23181=CARTESIAN_POINT('Ctrl Pts',(1.2811901266875,-3.40056942590122,15.6844842411246));
#23182=CARTESIAN_POINT('Ctrl Pts',(-0.122405002240585,0.824730814938715,
15.8830003585363));
#23183=CARTESIAN_POINT('Ctrl Pts',(2.66724567793686,4.29475826350135,16.0815164759479));
#23184=CARTESIAN_POINT('Ctrl Pts',(7.09543313909595,3.83172778931411,16.2800325933596));
#23185=CARTESIAN_POINT('Ctrl Pts',(9.10690753736432,-0.140326107135887,
16.4785487107712));
#23186=CARTESIAN_POINT('Ctrl Pts',(6.85959888110794,-3.98387202395643,16.6770648281829));
#23187=CARTESIAN_POINT('Ctrl Pts',(2.41154968938301,-4.179063722519,16.8755809455945));
#23188=CARTESIAN_POINT('Ctrl Pts',(-0.163801198896094,-0.547148358219792,
17.0740970630062));
#23189=CARTESIAN_POINT('Ctrl Pts',(1.49200357138825,3.5858350646717,17.2726131804178));
#23190=CARTESIAN_POINT('Ctrl Pts',(5.86260948835618,4.43497894515246,17.4711292978295));
#23191=CARTESIAN_POINT('Ctrl Pts',(8.94549879098837,1.22265346990726,17.6696454152412));
#23192=CARTESIAN_POINT('Ctrl Pts',(7.91742009870712,-3.10935479574357,17.8681615326528));
#23193=CARTESIAN_POINT('Ctrl Pts',(3.71986832177296,-4.59387508565289,18.0666776500645));
#23194=CARTESIAN_POINT('Ctrl Pts',(0.196881531601468,-1.87141195688986,
18.2651937674761));
#23195=CARTESIAN_POINT('Ctrl Pts',(0.574744016316265,2.56485464396025,18.4637098848878));
#23196=CARTESIAN_POINT('Ctrl Pts',(4.50741650012369,4.6522761505852,18.6622260022994));
#23197=CARTESIAN_POINT('Ctrl Pts',(8.3934323297128,2.47923165417059,18.8607421197111));
#23198=CARTESIAN_POINT('Ctrl Pts',(8.67405212821057,-1.96424603112833,19.0592582371228));
#23199=CARTESIAN_POINT('Ctrl Pts',(5.09228962209667,-4.60890456507674,19.2577743545344));
#23200=CARTESIAN_POINT('Ctrl Pts',(0.928254782143413,-3.0328159689208,19.4562904719461));
#23201=CARTESIAN_POINT('Ctrl Pts',(-0.00470849360073685,1.32066780116548,
19.6548065893577));
#23202=CARTESIAN_POINT('Ctrl Pts',(3.14778981602278,4.46470912096001,19.8533227067694));
#23203=CARTESIAN_POINT('Ctrl Pts',(7.49875172579254,3.52005475507203,20.051838824181));
#23204=CARTESIAN_POINT('Ctrl Pts',(9.06364908309027,-0.648198796048447,
20.2503549415927));
#23205=CARTESIAN_POINT('Ctrl Pts',(6.4093786550744,-4.22284422156345,20.4488710590044));
#23206=CARTESIAN_POINT('Ctrl Pts',(1.96667081116617,-3.93028923259476,20.647387176416));
#23207=CARTESIAN_POINT('Ctrl Pts',(-0.195927116407106,-0.0384501329489085,
20.8459032938277));
#23208=CARTESIAN_POINT('Ctrl Pts',(1.90205092121151,3.88860087953163,21.0444194112393));
#23209=CARTESIAN_POINT('Ctrl Pts',(6.3393165377314,4.25454515162759,21.242935528651));
#23210=CARTESIAN_POINT('Ctrl Pts',(9.05230630112455,0.724257949825445,21.4414516460626));
#23211=CARTESIAN_POINT('Ctrl Pts',(7.55651576606266,-3.46929099370176,21.6399677634743));
#23212=CARTESIAN_POINT('Ctrl Pts',(3.22176150253947,-4.48572906904549,21.838483880886));
#23213=CARTESIAN_POINT('Ctrl Pts',(0.0177289115966501,-1.39422211492368,
22.0369999982976));
#23214=CARTESIAN_POINT('Ctrl Pts',(0.878610280341868,2.97408755340353,22.2355161157093));
#23215=CARTESIAN_POINT('Ctrl Pts',(5.01602646728549,4.61878321962123,22.4340322331209));
#23216=CARTESIAN_POINT('Ctrl Pts',(8.64101112050298,2.03368736229999,22.6325483505326));
#23217=CARTESIAN_POINT('Ctrl Pts',(8.43387092517075,-2.41382509078919,22.8310644679442));
#23218=CARTESIAN_POINT('Ctrl Pts',(4.58430347192829,-4.65079401118156,23.0295805853559));
#23219=CARTESIAN_POINT('Ctrl Pts',(0.617664534920323,-2.6286704174496,23.2280967027675));
#23220=CARTESIAN_POINT('Ctrl Pts',(0.166535948123391,1.80077057177711,23.4266128201792));
#23221=CARTESIAN_POINT('Ctrl Pts',(3.64403475383551,4.58104059437149,23.6251289375908));
#23222=CARTESIAN_POINT('Ctrl Pts',(7.86556810560143,3.16619499327494,23.8236450550025));
#23223=CARTESIAN_POINT('Ctrl Pts',(8.96507004425898,-1.14841087401253,24.0221611724142));
#23224=CARTESIAN_POINT('Ctrl Pts',(5.93576426504054,-4.41090351654891,24.2206772898258));
#23225=CARTESIAN_POINT('Ctrl Pts',(1.55158838794904,-3.63478122412758,24.4191934072375));
#23226=CARTESIAN_POINT('Ctrl Pts',(-0.172046559910909,0.471552713422697,
24.6177095246491));
#23227=CARTESIAN_POINT('Ctrl Pts',(2.34243741690352,4.14307145960353,24.8162256420608));
#23228=CARTESIAN_POINT('Ctrl Pts',(6.79403703197597,4.02620936921257,25.0147417594724));
#23229=CARTESIAN_POINT('Ctrl Pts',(9.10329134237422,0.209832038399488,25.2133007328261));
#23230=CARTESIAN_POINT('Ctrl Pts',(7.80718744833136,-2.44564931016495,25.3456876670425));
#23231=CARTESIAN_POINT('Ctrl Pts',(6.7401774553626,-3.20569558398784,25.4119025621217));
#23232=CARTESIAN_POINT('Ctrl Pts',(5.88688308661327,2.88166464694226,-0.413294290592403));
#23233=CARTESIAN_POINT('Ctrl Pts',(6.84537358445575,2.40588471549031,-0.347122251455184));
#23234=CARTESIAN_POINT('Ctrl Pts',(8.23365752427788,0.430873938343679,-0.214778173180747));
#23235=CARTESIAN_POINT('Ctrl Pts',(6.86376121760315,-2.94715670275194,-0.0162620557690901));
#23236=CARTESIAN_POINT('Ctrl Pts',(3.28608690294124,-3.61718018023642,0.182254061642566));
#23237=CARTESIAN_POINT('Ctrl Pts',(0.781880406995935,-0.979166244321737,
0.380770179054222));
#23238=CARTESIAN_POINT('Ctrl Pts',(1.64193314359211,2.55787552455616,0.579286296465875));
#23239=CARTESIAN_POINT('Ctrl Pts',(5.07993189931123,3.75125370222575,0.777802413877532));
#23240=CARTESIAN_POINT('Ctrl Pts',(7.94674205925474,1.50993542852403,0.976318531289188));
#23241=CARTESIAN_POINT('Ctrl Pts',(7.61734820438694,-2.11448150974993,1.17483464870084));
#23242=CARTESIAN_POINT('Ctrl Pts',(4.39321803491158,-3.80232526959411,1.3733507661125));
#23243=CARTESIAN_POINT('Ctrl Pts',(1.22704502026327,-2.0081611280352,1.57186688352415));
#23244=CARTESIAN_POINT('Ctrl Pts',(1.01829993859556,1.62508529687376,1.77038300093581));
#23245=CARTESIAN_POINT('Ctrl Pts',(3.95817375267475,3.77008527062174,1.96889911834747));
#23246=CARTESIAN_POINT('Ctrl Pts',(7.35437229592725,2.462525507432,2.16741523575912));
#23247=CARTESIAN_POINT('Ctrl Pts',(8.09672865983581,-1.10017486129741,2.36593135317078));
#23248=CARTESIAN_POINT('Ctrl Pts',(5.50540329893836,-3.65535258567839,2.56444747058243));
#23249=CARTESIAN_POINT('Ctrl Pts',(1.95348461951634,-2.8630297341532,2.76296358799409));
#23250=CARTESIAN_POINT('Ctrl Pts',(0.693751175975549,0.551202220257554,
2.96147970540574));
#23251=CARTESIAN_POINT('Ctrl Pts',(2.87984341841113,3.46065318004877,3.1599958228174));
#23252=CARTESIAN_POINT('Ctrl Pts',(6.50977938134639,3.20090403962421,3.35851194022905));
#23253=CARTESIAN_POINT('Ctrl Pts',(8.25933290131072,0.00982773524565914,
3.55702805764071));
#23254=CARTESIAN_POINT('Ctrl Pts',(6.52629607038668,-3.19024855326339,3.75554417505237));
#23255=CARTESIAN_POINT('Ctrl Pts',(2.89775109124319,-3.46875593755042,3.95406029246402));
#23256=CARTESIAN_POINT('Ctrl Pts',(0.69665041333009,-0.570642598253718,
4.15257640987568));
#23257=CARTESIAN_POINT('Ctrl Pts',(1.93872017863753,2.85005436799852,4.35109252728733));
#23258=CARTESIAN_POINT('Ctrl Pts',(5.48649651727959,3.66072576290342,4.54960864469899));
#23259=CARTESIAN_POINT('Ctrl Pts',(8.09099334705098,1.11897413587954,4.74812476211065));
#23260=CARTESIAN_POINT('Ctrl Pts',(7.36706201253862,-2.44751271825679,4.9466408795223));
#23261=CARTESIAN_POINT('Ctrl Pts',(3.97766506003213,-3.7726139823619,5.14515699693396));
#23262=CARTESIAN_POINT('Ctrl Pts',(1.02674774506536,-1.64282712377203,5.34367311434561));
#23263=CARTESIAN_POINT('Ctrl Pts',(1.21670401249677,1.99142956468722,5.54218923175727));
#23264=CARTESIAN_POINT('Ctrl Pts',(4.37357552585394,3.80197293891488,5.74070534916892));
#23265=CARTESIAN_POINT('Ctrl Pts',(7.60635940332531,2.13074181682499,5.93922146658058));
#23266=CARTESIAN_POINT('Ctrl Pts',(7.95453366396254,-1.49178213007847,6.13773758399224));
#23267=CARTESIAN_POINT('Ctrl Pts',(5.09924694286633,-3.74816037897555,6.33625370140389));
#23268=CARTESIAN_POINT('Ctrl Pts',(1.65531650589596,-2.57204465036969,6.53476981881556));
#23269=CARTESIAN_POINT('Ctrl Pts',(0.776628336729841,0.959500643563771,
6.7332859362272));
#23270=CARTESIAN_POINT('Ctrl Pts',(3.26786834626679,3.6123534997611,6.93180205363886));
#23271=CARTESIAN_POINT('Ctrl Pts',(6.84760632218384,2.95708173512582,7.1303181710505));
#23272=CARTESIAN_POINT('Ctrl Pts',(8.23758631997216,-0.406229232878139,
7.32883428846218));
#23273=CARTESIAN_POINT('Ctrl Pts',(6.16489109788061,-3.39752319671194,7.52735040587382));
#23274=CARTESIAN_POINT('Ctrl Pts',(2.52765551345678,-3.27743004474078,7.72586652328549));
#23275=CARTESIAN_POINT('Ctrl Pts',(0.656790727359,-0.155928801126063,7.92438264069713));
#23276=CARTESIAN_POINT('Ctrl Pts',(2.26559912307384,3.10836907247963,8.1228987581088));
#23277=CARTESIAN_POINT('Ctrl Pts',(5.88076457458627,3.52608167695778,8.32141487552045));
#23278=CARTESIAN_POINT('Ctrl Pts',(8.19158732913988,0.714675754863574,8.5199309929321));
#23279=CARTESIAN_POINT('Ctrl Pts',(7.08185986462416,-2.75121662896035,8.71844711034376));
#23280=CARTESIAN_POINT('Ctrl Pts',(3.56784948378791,-3.69759715767183,8.91696322775543));
#23281=CARTESIAN_POINT('Ctrl Pts',(0.867620049835816,-1.2577885451434,9.11547934516706));
#23282=CARTESIAN_POINT('Ctrl Pts',(1.45399031457103,2.33387889135228,9.31399546257875));
#23283=CARTESIAN_POINT('Ctrl Pts',(4.78997354349419,3.78822443423146,9.51251157999037));
#23284=CARTESIAN_POINT('Ctrl Pts',(7.8205397526871,1.77338609991104,9.71102769740205));
#23285=CARTESIAN_POINT('Ctrl Pts',(7.77035405525285,-1.8654854913274,9.90954381481369));
#23286=CARTESIAN_POINT('Ctrl Pts',(4.68537555826851,-3.79598095490491,10.1080599322253));
#23287=CARTESIAN_POINT('Ctrl Pts',(1.39076888675897,-2.25018926719472,10.306576049637));
#23288=CARTESIAN_POINT('Ctrl Pts',(0.903672160428571,1.35628294827392,10.5050921670486));
#23289=CARTESIAN_POINT('Ctrl Pts',(3.67015929568852,3.72069703895061,10.7036082844603));
#23290=CARTESIAN_POINT('Ctrl Pts',(7.156733998233,2.67776755651859,10.902124401872));
#23291=CARTESIAN_POINT('Ctrl Pts',(8.17045747715504,-0.817410517633158,
11.1006405192836));
#23292=CARTESIAN_POINT('Ctrl Pts',(5.78298105352307,-3.56401958853324,11.2991566366953));
#23293=CARTESIAN_POINT('Ctrl Pts',(2.18071022148213,-3.04676731509573,11.4976727541069));
#23294=CARTESIAN_POINT('Ctrl Pts',(0.662536086558379,0.260656509846819,
11.6961888715186));
#23295=CARTESIAN_POINT('Ctrl Pts',(2.61877364278075,3.32937606128419,11.8947049889302));
#23296=CARTESIAN_POINT('Ctrl Pts',(6.25793774774488,3.34911634724554,12.0932211063419));
#23297=CARTESIAN_POINT('Ctrl Pts',(8.24735113836601,0.301799589347462,12.2917372237535));
#23298=CARTESIAN_POINT('Ctrl Pts',(6.76514687416864,-3.02189949163811,12.4902533411652));
#23299=CARTESIAN_POINT('Ctrl Pts',(3.16869942579002,-3.57820050080496,12.6887694585768));
#23300=CARTESIAN_POINT('Ctrl Pts',(0.751566954770839,-0.857653555925328,
12.8872855759885));
#23301=CARTESIAN_POINT('Ctrl Pts',(1.72731339933552,2.64831620117018,13.0858016934002));
#23302=CARTESIAN_POINT('Ctrl Pts',(5.20236872621718,3.72900835754984,13.2843178108118));
#23303=CARTESIAN_POINT('Ctrl Pts',(7.99434336961907,1.39474559334568,13.4828339282235));
#23304=CARTESIAN_POINT('Ctrl Pts',(7.54640006010282,-2.21679865437008,13.6813500456351));
#23305=CARTESIAN_POINT('Ctrl Pts',(4.26875675973819,-3.79824086239538,13.8798661630468));
#23306=CARTESIAN_POINT('Ctrl Pts',(1.16301685561255,-1.9013263388412,14.0783822804584));
#23307=CARTESIAN_POINT('Ctrl Pts',(1.07335787448695,1.73678667876183,14.2768983978701));
#23308=CARTESIAN_POINT('Ctrl Pts',(4.08188780578152,3.78438349314049,14.4754145152818));
#23309=CARTESIAN_POINT('Ctrl Pts',(7.43345216672421,2.36631389110821,14.6739306326934));
#23310=CARTESIAN_POINT('Ctrl Pts',(8.05875206907788,-1.21878096033793,14.8724467501051));
#23311=CARTESIAN_POINT('Ctrl Pts',(5.38514975673243,-3.68773939197872,15.0709628675167));
#23312=CARTESIAN_POINT('Ctrl Pts',(1.86107937002522,-2.77953623668677,15.2694789849284));
#23313=CARTESIAN_POINT('Ctrl Pts',(0.713817534175901,0.674113331777405,
15.46799510234));
#23314=CARTESIAN_POINT('Ctrl Pts',(2.9940048152212,3.5104227339951,15.6665112197517));
#23315=CARTESIAN_POINT('Ctrl Pts',(6.61348907494099,3.13195377174095,15.8650273371633));
#23316=CARTESIAN_POINT('Ctrl Pts',(8.257615478175,-0.114698878595687,16.063543454575));
#23317=CARTESIAN_POINT('Ctrl Pts',(6.42072433944188,-3.25631247771842,16.2620595719866));
#23318=CARTESIAN_POINT('Ctrl Pts',(2.78500562221897,-3.41585705137789,16.4605756893983));
#23319=CARTESIAN_POINT('Ctrl Pts',(0.67998136903583,-0.447224713876356,
16.65909180681));
#23320=CARTESIAN_POINT('Ctrl Pts',(2.03339274915041,2.93096750947701,16.8576079242216));
#23321=CARTESIAN_POINT('Ctrl Pts',(5.60581136526813,3.62503544056518,17.0561240416333));
#23322=CARTESIAN_POINT('Ctrl Pts',(8.12568420335589,0.999364870669326,17.2546401590449));
#23323=CARTESIAN_POINT('Ctrl Pts',(7.28535965135699,-2.54150503784963,17.4531562764566));
#23324=CARTESIAN_POINT('Ctrl Pts',(3.85439094932391,-3.75491297725849,17.6516723938682));
#23325=CARTESIAN_POINT('Ctrl Pts',(0.974793970633971,-1.52964303811135,
17.8501885112799));
#23326=CARTESIAN_POINT('Ctrl Pts',(1.2836488526281,2.09644489844015,18.0487046286916));
#23327=CARTESIAN_POINT('Ctrl Pts',(4.49811216942012,3.80264847561477,18.2472207461032));
#23328=CARTESIAN_POINT('Ctrl Pts',(7.67443956106538,2.02645891285741,18.4457368635149));
#23329=CARTESIAN_POINT('Ctrl Pts',(7.90381082245328,-1.60552317494378,18.6442529809265));
#23330=CARTESIAN_POINT('Ctrl Pts',(4.9761721155001,-3.76719767944954,18.8427690983382));
#23331=CARTESIAN_POINT('Ctrl Pts',(1.57259927845708,-2.47894420875808,19.0412852157498));
#23332=CARTESIAN_POINT('Ctrl Pts',(0.810019572635768,1.07947921368855,19.2398013331615));
#23333=CARTESIAN_POINT('Ctrl Pts',(3.38678898688482,3.6493361063157,19.4383174505731));
#23334=CARTESIAN_POINT('Ctrl Pts',(6.94315110686829,2.87720041011993,19.6368335679848));
#23335=CARTESIAN_POINT('Ctrl Pts',(8.22225715251285,-0.529820690755693,
19.8353496853965));
#23336=CARTESIAN_POINT('Ctrl Pts',(6.05272613795891,-3.45164208273989,20.0338658028081));
#23337=CARTESIAN_POINT('Ctrl Pts',(2.42137329831411,-3.212515309774,20.2323819202198));
#23338=CARTESIAN_POINT('Ctrl Pts',(0.65372248686789,-0.0314281299545405,
20.4308980376314));
#23339=CARTESIAN_POINT('Ctrl Pts',(2.36855469553213,3.178440343651,20.6294141550431));
#23340=CARTESIAN_POINT('Ctrl Pts',(5.99545920128352,3.47755359131801,20.8279302724548));
#23341=CARTESIAN_POINT('Ctrl Pts',(8.21298586010566,0.591989447683331,21.0264463898664));
#23342=CARTESIAN_POINT('Ctrl Pts',(6.99036591797756,-2.83570744333498,21.2249625072781));
#23343=CARTESIAN_POINT('Ctrl Pts',(3.44725150283742,-3.6665172604341,21.4234786246897));
#23344=CARTESIAN_POINT('Ctrl Pts',(0.828359319011244,-1.13960058009792,
21.6219947421014));
#23345=CARTESIAN_POINT('Ctrl Pts',(1.53202116508044,2.43094114262164,21.820510859513));
#23346=CARTESIAN_POINT('Ctrl Pts',(4.91383661347899,3.77527223251319,22.0190269769247));
#23347=CARTESIAN_POINT('Ctrl Pts',(7.87680396956558,1.66228269728872,22.2175430943363));
#23348=CARTESIAN_POINT('Ctrl Pts',(7.7074930081086,-1.97299730385434,22.416059211748));
#23349=CARTESIAN_POINT('Ctrl Pts',(4.56095756308617,-3.80143701374933,22.6145753291597));
#23350=CARTESIAN_POINT('Ctrl Pts',(1.31873095853907,-2.14860623751896,22.8130914465713));
#23351=CARTESIAN_POINT('Ctrl Pts',(0.949990286798536,1.47190262315773,23.011607563983));
#23352=CARTESIAN_POINT('Ctrl Pts',(3.7924065803434,3.74442240079083,23.2101236813946));
#23353=CARTESIAN_POINT('Ctrl Pts',(7.24297719250067,2.58796472414074,23.4086397988063));
#23354=CARTESIAN_POINT('Ctrl Pts',(8.14168123233833,-0.938680920498277,
23.6071559162179));
#23355=CARTESIAN_POINT('Ctrl Pts',(5.66560616055497,-3.60535681683013,23.8056720336296));
#23356=CARTESIAN_POINT('Ctrl Pts',(2.08209581503262,-2.97097481614092,24.0041881510412));
#23357=CARTESIAN_POINT('Ctrl Pts',(0.673241827254791,0.385434817028999,
24.2027042684529));
#23358=CARTESIAN_POINT('Ctrl Pts',(2.72851506381635,3.38643791990783,24.4012203858645));
#23359=CARTESIAN_POINT('Ctrl Pts',(6.36713580394013,3.29091791303403,24.5997365032762));
#23360=CARTESIAN_POINT('Ctrl Pts',(8.25465969525897,0.17151120336101,24.7982954766299));
#23361=CARTESIAN_POINT('Ctrl Pts',(7.19525837483205,-1.99900958588141,24.9306824108463));
#23362=CARTESIAN_POINT('Ctrl Pts',(6.32311239899223,-2.62025147071356,24.9968973059255));
#23363=CARTESIAN_POINT('Ctrl Pts',(5.99341579333084,3.0962819108244,-0.27495920519366));
#23364=CARTESIAN_POINT('Ctrl Pts',(7.02329163031133,2.58506739568259,-0.208787166056442));
#23365=CARTESIAN_POINT('Ctrl Pts',(8.51497056474962,0.462964065771816,-0.0764430877820045));
#23366=CARTESIAN_POINT('Ctrl Pts',(7.04304871618797,-3.16665160770128,0.122073029629653));
#23367=CARTESIAN_POINT('Ctrl Pts',(3.19892054011338,-3.88657631350085,0.320589147041309));
#23368=CARTESIAN_POINT('Ctrl Pts',(0.508208668906595,-1.05209144762919,
0.519105264452963));
#23369=CARTESIAN_POINT('Ctrl Pts',(1.43231541168923,2.74837799923302,0.717621381864618));
#23370=CARTESIAN_POINT('Ctrl Pts',(5.12636543519397,4.03063520713254,0.916137499276276));
#23371=CARTESIAN_POINT('Ctrl Pts',(8.20668654383497,1.62239064105283,1.11465361668793));
#23372=CARTESIAN_POINT('Ctrl Pts',(7.85276047702285,-2.27196140132349,1.31316973409959));
#23373=CARTESIAN_POINT('Ctrl Pts',(4.38850729527858,-4.08551042322263,1.51168585151124));
#23374=CARTESIAN_POINT('Ctrl Pts',(0.986527733847538,-2.15772261402933,
1.7102019689229));
#23375=CARTESIAN_POINT('Ctrl Pts',(0.7622359790706,1.74611650720567,1.90871808633455));
#23376=CARTESIAN_POINT('Ctrl Pts',(3.92106229159746,4.0508692911502,2.10723420374621));
#23377=CARTESIAN_POINT('Ctrl Pts',(7.57019895508782,2.64592661456843,2.30575032115786));
#23378=CARTESIAN_POINT('Ctrl Pts',(8.36784367179503,-1.18211240346562,2.50426643856952));
#23379=CARTESIAN_POINT('Ctrl Pts',(5.58352459826198,-3.92759167890361,2.70278255598118));
#23380=CARTESIAN_POINT('Ctrl Pts',(1.7670702556363,-3.07625912870098,2.90129867339283));
#23381=CARTESIAN_POINT('Ctrl Pts',(0.413515851644582,0.592254017343965,
3.09981479080449));
#23382=CARTESIAN_POINT('Ctrl Pts',(2.76242132641212,3.7183916776686,3.29833090821614));
#23383=CARTESIAN_POINT('Ctrl Pts',(6.66270343294158,3.43929724324088,3.4968470256278));
#23384=CARTESIAN_POINT('Ctrl Pts',(8.54255816261418,0.0105596738669375,
3.69536314303945));
#23385=CARTESIAN_POINT('Ctrl Pts',(6.6804502327146,-3.42784816997514,3.89387926045112));
#23386=CARTESIAN_POINT('Ctrl Pts',(2.78166270604797,-3.72709790290783,4.09239537786277));
#23387=CARTESIAN_POINT('Ctrl Pts',(0.416631015022661,-0.613142253174304,
4.29091149527442));
#23388=CARTESIAN_POINT('Ctrl Pts',(1.75120620592284,3.06231739833558,4.48942761268608));
#23389=CARTESIAN_POINT('Ctrl Pts',(5.56320969933569,3.93336503336498,4.68794373009773));
#23390=CARTESIAN_POINT('Ctrl Pts',(8.36168121106336,1.20231178852842,4.88645984750939));
#23391=CARTESIAN_POINT('Ctrl Pts',(7.58383376163584,-2.62979572036334,5.08497596492104));
#23392=CARTESIAN_POINT('Ctrl Pts',(3.94200524984668,-4.05358633333867,5.2834920823327));
#23393=CARTESIAN_POINT('Ctrl Pts',(0.771312951433223,-1.76517968922739,
5.48200819974436));
#23394=CARTESIAN_POINT('Ctrl Pts',(0.97541656054666,2.13974493679014,5.68052431715601));
#23395=CARTESIAN_POINT('Ctrl Pts',(4.36740187430494,4.08513185206935,5.87904043456767));
#23396=CARTESIAN_POINT('Ctrl Pts',(7.84095326483218,2.28943272461384,6.07755655197932));
#23397=CARTESIAN_POINT('Ctrl Pts',(8.21505844260491,-1.60288534238506,6.27607266939098));
#23398=CARTESIAN_POINT('Ctrl Pts',(5.14711900207072,-4.02731150295548,6.47458878680263));
#23399=CARTESIAN_POINT('Ctrl Pts',(1.44669552446588,-2.76360239669899,6.6731049042143));
#23400=CARTESIAN_POINT('Ctrl Pts',(0.502565441067234,1.03096121515846,6.87162102162594));
#23401=CARTESIAN_POINT('Ctrl Pts',(3.17934512299035,3.88139015713774,7.07013713903761));
#23402=CARTESIAN_POINT('Ctrl Pts',(7.0256906552799,3.17731582507866,7.26865325644925));
#23403=CARTESIAN_POINT('Ctrl Pts',(8.51919196471455,-0.436483900631263,
7.46716937386092));
#23404=CARTESIAN_POINT('Ctrl Pts',(6.2921289615216,-3.65055997294754,7.66568549127257));
#23405=CARTESIAN_POINT('Ctrl Pts',(2.38400358079477,-3.52152266305215,7.86420160868423));
#23406=CARTESIAN_POINT('Ctrl Pts',(0.373802705776339,-0.16754188479758,
8.06271772609589));
#23407=CARTESIAN_POINT('Ctrl Pts',(2.10243005973299,3.33987056457006,8.26123384350753));
#23408=CARTESIAN_POINT('Ctrl Pts',(5.98684159389007,3.78869308197905,8.4597499609192));
#23409=CARTESIAN_POINT('Ctrl Pts',(8.4697671146088,0.767902543495819,8.65826607833084));
#23410=CARTESIAN_POINT('Ctrl Pts',(7.27739066026635,-2.95611853726567,8.85678219574251));
#23411=CARTESIAN_POINT('Ctrl Pts',(3.50166790634439,-3.97298249293629,9.05529831315416));
#23412=CARTESIAN_POINT('Ctrl Pts',(0.600333929022254,-1.35146465571633,
9.25381443056581));
#23413=CARTESIAN_POINT('Ctrl Pts',(1.23037519550738,2.50769880562501,9.45233054797748));
#23414=CARTESIAN_POINT('Ctrl Pts',(4.81481189860833,4.07035940226423,9.65084666538912));
#23415=CARTESIAN_POINT('Ctrl Pts',(8.07108508884113,1.90546228475562,9.84936278280079));
#23416=CARTESIAN_POINT('Ctrl Pts',(8.01716171947454,-2.00442094739626,10.0478789002124));
#23417=CARTESIAN_POINT('Ctrl Pts',(4.70242378644322,-4.07869360405195,10.2463950176241));
#23418=CARTESIAN_POINT('Ctrl Pts',(1.16244523581599,-2.41777624309588,10.4449111350357));
#23419=CARTESIAN_POINT('Ctrl Pts',(0.639071086725107,1.45729461030662,10.6434272524474));
#23420=CARTESIAN_POINT('Ctrl Pts',(3.61159742927608,3.99780278027315,10.841943369859));
#23421=CARTESIAN_POINT('Ctrl Pts',(7.35784118240728,2.87719921033794,11.0404594872707));
#23422=CARTESIAN_POINT('Ctrl Pts',(8.44706357811351,-0.878288666292467,
11.2389756046823));
#23423=CARTESIAN_POINT('Ctrl Pts',(5.88177546561389,-3.82945648915419,11.437491722094));
#23424=CARTESIAN_POINT('Ctrl Pts',(2.01121890138154,-3.27368090323489,11.6360078395057));
#23425=CARTESIAN_POINT('Ctrl Pts',(0.379975961147697,0.280069381853164,
11.8345239569173));
#23426=CARTESIAN_POINT('Ctrl Pts',(2.4819079000476,3.57733745452462,12.033040074329));
#23427=CARTESIAN_POINT('Ctrl Pts',(6.39210543142176,3.59854793451629,12.2315561917406));
#23428=CARTESIAN_POINT('Ctrl Pts',(8.52968403588164,0.324276667717884,12.4300723091523));
#23429=CARTESIAN_POINT('Ctrl Pts',(6.93708988851933,-3.24696100298028,12.6285884265639));
#23430=CARTESIAN_POINT('Ctrl Pts',(3.07279041513639,-3.84469355089646,12.8271045439756));
#23431=CARTESIAN_POINT('Ctrl Pts',(0.475637566686629,-0.921528878727684,
13.0256206613872));
#23432=CARTESIAN_POINT('Ctrl Pts',(1.52405451869475,2.84555441124189,13.2241367787989));
#23433=CARTESIAN_POINT('Ctrl Pts',(5.25792096951678,4.00673309958052,13.4226528962106));
#23434=CARTESIAN_POINT('Ctrl Pts',(8.257833049161,1.4986218314684,13.6211690136222));
#23435=CARTESIAN_POINT('Ctrl Pts',(7.77652833946771,-2.38189880309254,13.8196851310339));
#23436=CARTESIAN_POINT('Ctrl Pts',(4.25477653818775,-4.08112182230083,14.0182012484455));
#23437=CARTESIAN_POINT('Ctrl Pts',(0.917730954110628,-2.04293110781465,
14.2167173658572));
#23438=CARTESIAN_POINT('Ctrl Pts',(0.821394455796449,1.86613705453794,14.4152334832688));
#23439=CARTESIAN_POINT('Ctrl Pts',(4.05399017588675,4.06623240003544,14.6137496006805));
#23440=CARTESIAN_POINT('Ctrl Pts',(7.65516844441363,2.54254946152231,14.8122657180922));
#23441=CARTESIAN_POINT('Ctrl Pts',(8.32703870473431,-1.30955190943392,15.0107818355038));
#23442=CARTESIAN_POINT('Ctrl Pts',(5.45431495277465,-3.96239055204922,15.2092979529155));
#23443=CARTESIAN_POINT('Ctrl Pts',(1.66778295557931,-2.98654729975826,15.4078140703271));
#23444=CARTESIAN_POINT('Ctrl Pts',(0.435076688703739,0.724319159497842,
15.6063301877388));
#23445=CARTESIAN_POINT('Ctrl Pts',(2.88508510279309,3.77186791049719,15.8048463051504));
#23446=CARTESIAN_POINT('Ctrl Pts',(6.77413709632598,3.36521177759866,16.0033624225621));
#23447=CARTESIAN_POINT('Ctrl Pts',(8.54071283123811,-0.123241288109086,
16.2018785399737));
#23448=CARTESIAN_POINT('Ctrl Pts',(6.56701585333057,-3.49883232646441,16.4003946573854));
#23449=CARTESIAN_POINT('Ctrl Pts',(2.66052031127365,-3.67025927509159,16.598910774797));
#23450=CARTESIAN_POINT('Ctrl Pts',(0.398720513058523,-0.480532595324168,
16.7974268922087));
#23451=CARTESIAN_POINT('Ctrl Pts',(1.85292968989636,3.14925669454191,16.9959430096203));
#23452=CARTESIAN_POINT('Ctrl Pts',(5.69141073963082,3.89501660876095,17.194459127032));
#23453=CARTESIAN_POINT('Ctrl Pts',(8.39895573256671,1.07379440374864,17.3929752444437));
#23454=CARTESIAN_POINT('Ctrl Pts',(7.49604646714037,-2.73078829048094,17.5914913618553));
#23455=CARTESIAN_POINT('Ctrl Pts',(3.80955007347359,-4.03456701338995,17.790007479267));
#23456=CARTESIAN_POINT('Ctrl Pts',(0.715489824289806,-1.64356601103751,
17.9885235966786));
#23457=CARTESIAN_POINT('Ctrl Pts',(1.04734724052415,2.25258148028018,18.1870397140903));
#23458=CARTESIAN_POINT('Ctrl Pts',(4.50121361298798,4.08585770060491,18.3855558315019));
#23459=CARTESIAN_POINT('Ctrl Pts',(7.91410381728119,2.1773831599618,18.5840719489136));
#23460=CARTESIAN_POINT('Ctrl Pts',(8.16055792437237,-1.72509746033864,18.7825880663253));
#23461=CARTESIAN_POINT('Ctrl Pts',(5.0148779510323,-4.04776664132528,18.9811041837369));
#23462=CARTESIAN_POINT('Ctrl Pts',(1.35781777968586,-2.66356812881232,19.1796203011486));
#23463=CARTESIAN_POINT('Ctrl Pts',(0.538443550556935,1.1598754095142,19.3781364185603));
#23464=CARTESIAN_POINT('Ctrl Pts',(3.30712259659747,3.92112711119714,19.5766525359719));
#23465=CARTESIAN_POINT('Ctrl Pts',(7.12835131317638,3.09148519177063,19.7751686533836));
#23466=CARTESIAN_POINT('Ctrl Pts',(8.50272112937199,-0.569280059186615,
19.9736847707952));
#23467=CARTESIAN_POINT('Ctrl Pts',(6.17161031033075,-3.70870946234774,20.1722008882069));
#23468=CARTESIAN_POINT('Ctrl Pts',(2.26980580259814,-3.45177328404759,20.3707170056185));
#23469=CARTESIAN_POINT('Ctrl Pts',(0.370505952442893,-0.0337687976193256,
20.5692331230302));
#23470=CARTESIAN_POINT('Ctrl Pts',(2.21305343742525,3.41516052227788,20.7677492404418));
#23471=CARTESIAN_POINT('Ctrl Pts',(6.11007831343283,3.73655077808788,20.9662653578534));
#23472=CARTESIAN_POINT('Ctrl Pts',(8.49275934044528,0.636078948397367,21.1647814752652));
#23473=CARTESIAN_POINT('Ctrl Pts',(7.17908253400595,-3.04690196012391,21.3632975926768));
#23474=CARTESIAN_POINT('Ctrl Pts',(3.37208816940477,-3.93958786330456,21.5618137100885));
#23475=CARTESIAN_POINT('Ctrl Pts',(0.558149183206385,-1.22447442503984,
21.7603298275001));
#23476=CARTESIAN_POINT('Ctrl Pts',(1.31421753683424,2.61198994621562,21.9588459449118));
#23477=CARTESIAN_POINT('Ctrl Pts',(4.94789989808116,4.05644256154919,22.1573620623234));
#23478=CARTESIAN_POINT('Ctrl Pts',(8.13153968654471,1.78608425229248,22.3558781797351));
#23479=CARTESIAN_POINT('Ctrl Pts',(7.94961898046267,-2.11993989949929,22.5543942971467));
#23480=CARTESIAN_POINT('Ctrl Pts',(4.56873953270021,-4.0845560128934,22.7529104145584));
#23481=CARTESIAN_POINT('Ctrl Pts',(1.08504215066615,-2.30862763082918,22.95142653197));
#23482=CARTESIAN_POINT('Ctrl Pts',(0.688838840573486,1.58152527269752,23.1499426493817));
#23483=CARTESIAN_POINT('Ctrl Pts',(3.74294930484078,4.02329513198439,23.3484587667933));
#23484=CARTESIAN_POINT('Ctrl Pts',(7.45050749686758,2.78070814718547,23.546974884205));
#23485=CARTESIAN_POINT('Ctrl Pts',(8.41614416964521,-1.00859090500303,23.7454910016166));
#23486=CARTESIAN_POINT('Ctrl Pts',(5.75565886205016,-3.87387238340306,23.9440071190283));
#23487=CARTESIAN_POINT('Ctrl Pts',(1.90526000600476,-3.19224361880315,24.14252323644));
#23488=CARTESIAN_POINT('Ctrl Pts',(0.391479031532891,0.414140782493564,
24.3410393538516));
#23489=CARTESIAN_POINT('Ctrl Pts',(2.59982251484541,3.6386490998064,24.5395554712633));
#23490=CARTESIAN_POINT('Ctrl Pts',(6.50943621328541,3.53601506509354,24.7380715886749));
#23491=CARTESIAN_POINT('Ctrl Pts',(8.53753691096405,0.184284815040506,24.9366305620286));
#23492=CARTESIAN_POINT('Ctrl Pts',(7.39923473266516,-2.14788949397592,25.069017496245));
#23493=CARTESIAN_POINT('Ctrl Pts',(6.46213408444902,-2.81539950847165,25.1352323913243));
#23494=CARTESIAN_POINT('Ctrl Pts',(6.0999485000484,3.31089917470656,-0.136624119794918));
#23495=CARTESIAN_POINT('Ctrl Pts',(7.2012096761669,2.76425007587486,-0.0704520806576993));
#23496=CARTESIAN_POINT('Ctrl Pts',(8.79628360522135,0.495054193199949,0.061891997616738));
#23497=CARTESIAN_POINT('Ctrl Pts',(7.22233621477278,-3.38614651265062,0.260408115028396));
#23498=CARTESIAN_POINT('Ctrl Pts',(3.11175417728552,-4.15597244676529,0.458924232440051));
#23499=CARTESIAN_POINT('Ctrl Pts',(0.234536930817258,-1.12501665093665,
0.657440349851707));
#23500=CARTESIAN_POINT('Ctrl Pts',(1.22269767978634,2.93888047390986,0.855956467263361));
#23501=CARTESIAN_POINT('Ctrl Pts',(5.17279897107673,4.31001671203934,1.05447258467502));
#23502=CARTESIAN_POINT('Ctrl Pts',(8.46663102841521,1.73484585358162,1.25298870208667));
#23503=CARTESIAN_POINT('Ctrl Pts',(8.08817274965877,-2.42944129289705,1.45150481949833));
#23504=CARTESIAN_POINT('Ctrl Pts',(4.38379655564558,-4.36869557685114,1.65002093690999));
#23505=CARTESIAN_POINT('Ctrl Pts',(0.746010447431816,-2.30728410002347,
1.84853705432164));
#23506=CARTESIAN_POINT('Ctrl Pts',(0.506172019545635,1.86714771753756,2.04705317173329));
#23507=CARTESIAN_POINT('Ctrl Pts',(3.88395083052018,4.33165331167866,2.24556928914495));
#23508=CARTESIAN_POINT('Ctrl Pts',(7.78602561424836,2.82932772170484,2.4440854065566));
#23509=CARTESIAN_POINT('Ctrl Pts',(8.63895868375428,-1.26404994563383,2.64260152396827));
#23510=CARTESIAN_POINT('Ctrl Pts',(5.66164589758561,-4.19983077212884,2.84111764137992));
#23511=CARTESIAN_POINT('Ctrl Pts',(1.58065589175627,-3.28948852324876,3.03963375879158));
#23512=CARTESIAN_POINT('Ctrl Pts',(0.133280527313607,0.633305814430374,
3.23814987620323));
#23513=CARTESIAN_POINT('Ctrl Pts',(2.6449992344131,3.97613017528841,3.43666599361489));
#23514=CARTESIAN_POINT('Ctrl Pts',(6.81562748453676,3.67769044685756,3.63518211102655));
#23515=CARTESIAN_POINT('Ctrl Pts',(8.82578342391765,0.0112916124882134,
3.8336982284382));
#23516=CARTESIAN_POINT('Ctrl Pts',(6.83460439504253,-3.66544778668689,4.03221434584986));
#23517=CARTESIAN_POINT('Ctrl Pts',(2.66557432085276,-3.98543986826524,4.23073046326151));
#23518=CARTESIAN_POINT('Ctrl Pts',(0.13661161671523,-0.655641908094887,
4.42924658067317));
#23519=CARTESIAN_POINT('Ctrl Pts',(1.56369223320815,3.27458042867263,4.62776269808482));
#23520=CARTESIAN_POINT('Ctrl Pts',(5.63992288139177,4.20600430382654,4.82627881549648));
#23521=CARTESIAN_POINT('Ctrl Pts',(8.63236907507575,1.28564944117731,5.02479493290813));
#23522=CARTESIAN_POINT('Ctrl Pts',(7.80060551073305,-2.81207872246989,5.22331105031979));
#23523=CARTESIAN_POINT('Ctrl Pts',(3.90634543966123,-4.33455868431544,5.42182716773146));
#23524=CARTESIAN_POINT('Ctrl Pts',(0.515878157801087,-1.88753225468275,
5.62034328514309));
#23525=CARTESIAN_POINT('Ctrl Pts',(0.734129108596551,2.28806030889307,5.81885940255477));
#23526=CARTESIAN_POINT('Ctrl Pts',(4.36122822275595,4.36829076522382,6.0173755199664));
#23527=CARTESIAN_POINT('Ctrl Pts',(8.07554712633902,2.44812363240269,6.21589163737808));
#23528=CARTESIAN_POINT('Ctrl Pts',(8.47558322124728,-1.71398855469165,6.41440775478972));
#23529=CARTESIAN_POINT('Ctrl Pts',(5.19499106127511,-4.3064626269354,6.61292387220138));
#23530=CARTESIAN_POINT('Ctrl Pts',(1.2380745430358,-2.9551601430283,6.81143998961304));
#23531=CARTESIAN_POINT('Ctrl Pts',(0.228502545404632,1.10242178675316,7.00995610702469));
#23532=CARTESIAN_POINT('Ctrl Pts',(3.09082189971391,4.15042681451437,7.20847222443635));
#23533=CARTESIAN_POINT('Ctrl Pts',(7.20377498837598,3.39754991503151,7.406988341848));
#23534=CARTESIAN_POINT('Ctrl Pts',(8.80079760945692,-0.466738568384383,
7.60550445925966));
#23535=CARTESIAN_POINT('Ctrl Pts',(6.41936682516261,-3.90359674918315,7.80402057667131));
#23536=CARTESIAN_POINT('Ctrl Pts',(2.24035164813274,-3.7656152813635,8.00253669408298));
#23537=CARTESIAN_POINT('Ctrl Pts',(0.0908146841936848,-0.179154968469096,
8.20105281149462));
#23538=CARTESIAN_POINT('Ctrl Pts',(1.93926099639212,3.57137205666049,8.39956892890629));
#23539=CARTESIAN_POINT('Ctrl Pts',(6.09291861319388,4.05130448700034,8.59808504631793));
#23540=CARTESIAN_POINT('Ctrl Pts',(8.7479469000777,0.821129332128062,8.7966011637296));
#23541=CARTESIAN_POINT('Ctrl Pts',(7.47292145590854,-3.16102044557099,8.99511728114126));
#23542=CARTESIAN_POINT('Ctrl Pts',(3.43548632890085,-4.24836782820074,9.19363339855291));
#23543=CARTESIAN_POINT('Ctrl Pts',(0.333047808208697,-1.44514076628925,
9.39214951596456));
#23544=CARTESIAN_POINT('Ctrl Pts',(1.00676007644372,2.68151871989772,9.59066563337622));
#23545=CARTESIAN_POINT('Ctrl Pts',(4.83965025372247,4.352494370297,9.78918175078787));
#23546=CARTESIAN_POINT('Ctrl Pts',(8.32163042499515,2.03753846960017,9.98769786819953));
#23547=CARTESIAN_POINT('Ctrl Pts',(8.26396938369623,-2.14335640346512,10.1862139856111));
#23548=CARTESIAN_POINT('Ctrl Pts',(4.71947201461794,-4.36140625319899,10.3847301030228));
#23549=CARTESIAN_POINT('Ctrl Pts',(0.934121584873003,-2.58536321899705,
10.5832462204345));
#23550=CARTESIAN_POINT('Ctrl Pts',(0.37447001302165,1.5583062723393,10.7817623378461));
#23551=CARTESIAN_POINT('Ctrl Pts',(3.55303556286365,4.27490852159572,10.9802784552578));
#23552=CARTESIAN_POINT('Ctrl Pts',(7.55894836658157,3.07663086415728,11.1787945726694));
#23553=CARTESIAN_POINT('Ctrl Pts',(8.72366967907197,-0.939166814951776,
11.3773106900811));
#23554=CARTESIAN_POINT('Ctrl Pts',(5.98056987770475,-4.09489338977514,11.5758268074927));
#23555=CARTESIAN_POINT('Ctrl Pts',(1.84172758128094,-3.50059449137405,11.7743429249044));
#23556=CARTESIAN_POINT('Ctrl Pts',(0.0974158357370281,0.299482253859507,
11.9728590423161));
#23557=CARTESIAN_POINT('Ctrl Pts',(2.34504215731444,3.82529884776504,12.1713751597277));
#23558=CARTESIAN_POINT('Ctrl Pts',(6.52627311509865,3.84797952178704,12.3698912771394));
#23559=CARTESIAN_POINT('Ctrl Pts',(8.81201693339725,0.346753746088307,12.568407394551));
#23560=CARTESIAN_POINT('Ctrl Pts',(7.10903290287004,-3.47202251432246,12.7669235119627));
#23561=CARTESIAN_POINT('Ctrl Pts',(2.97688140448274,-4.11118660098796,12.9654396293744));
#23562=CARTESIAN_POINT('Ctrl Pts',(0.199708178602426,-0.985404201530036,
13.163955746786));
#23563=CARTESIAN_POINT('Ctrl Pts',(1.32079563805398,3.0427926213136,13.3624718641977));
#23564=CARTESIAN_POINT('Ctrl Pts',(5.3134732128164,4.28445784161121,13.5609879816093));
#23565=CARTESIAN_POINT('Ctrl Pts',(8.52132272870291,1.60249806959112,13.759504099021));
#23566=CARTESIAN_POINT('Ctrl Pts',(8.00665661883263,-2.546998951815,13.9580202164326));
#23567=CARTESIAN_POINT('Ctrl Pts',(4.24079631663729,-4.36400278220629,14.1565363338443));
#23568=CARTESIAN_POINT('Ctrl Pts',(0.672445052608722,-2.18453587678811,
14.3550524512559));
#23569=CARTESIAN_POINT('Ctrl Pts',(0.569431037105937,1.99548743031406,14.5535685686676));
#23570=CARTESIAN_POINT('Ctrl Pts',(4.02609254599198,4.3480813069304,14.7520846860792));
#23571=CARTESIAN_POINT('Ctrl Pts',(7.87688472210303,2.7187850319364,14.9506008034909));
#23572=CARTESIAN_POINT('Ctrl Pts',(8.59532534039074,-1.40032285852991,15.1491169209026));
#23573=CARTESIAN_POINT('Ctrl Pts',(5.52348014881688,-4.2370417121197,15.3476330383142));
#23574=CARTESIAN_POINT('Ctrl Pts',(1.47448654113341,-3.19355836282975,15.5461491557259));
#23575=CARTESIAN_POINT('Ctrl Pts',(0.156335843231577,0.774524987218279,
15.7446652731375));
#23576=CARTESIAN_POINT('Ctrl Pts',(2.77616539036498,4.03331308699926,15.9431813905492));
#23577=CARTESIAN_POINT('Ctrl Pts',(6.93478511771097,3.59846978345639,16.1416975079608));
#23578=CARTESIAN_POINT('Ctrl Pts',(8.82381018430121,-0.131783697622486,
16.3402136253725));
#23579=CARTESIAN_POINT('Ctrl Pts',(6.71330736721926,-3.74135217521042,16.5387297427841));
#23580=CARTESIAN_POINT('Ctrl Pts',(2.53603500032833,-3.92466149880528,16.7372458601958));
#23581=CARTESIAN_POINT('Ctrl Pts',(0.117459657081213,-0.513840476771981,
16.9357619776075));
#23582=CARTESIAN_POINT('Ctrl Pts',(1.6724666306423,3.3675458796068,17.1342780950191));
#23583=CARTESIAN_POINT('Ctrl Pts',(5.77701011399349,4.16499777695671,17.3327942124308));
#23584=CARTESIAN_POINT('Ctrl Pts',(8.67222726177754,1.14822393682795,17.5313103298424));
#23585=CARTESIAN_POINT('Ctrl Pts',(7.70673328292373,-2.92007154311226,17.7298264472541));
#23586=CARTESIAN_POINT('Ctrl Pts',(3.76470919762329,-4.31422104952143,17.9283425646657));
#23587=CARTESIAN_POINT('Ctrl Pts',(0.456185677945633,-1.75748898396369,
18.1268586820774));
#23588=CARTESIAN_POINT('Ctrl Pts',(0.811045628420214,2.40871806212022,18.3253747994891));
#23589=CARTESIAN_POINT('Ctrl Pts',(4.50431505655582,4.36906692559506,18.5238909169007));
#23590=CARTESIAN_POINT('Ctrl Pts',(8.153768073497,2.32830740706619,18.7224070343124));
#23591=CARTESIAN_POINT('Ctrl Pts',(8.41730502629147,-1.84467174573349,18.920923151724));
#23592=CARTESIAN_POINT('Ctrl Pts',(5.05358378656449,-4.328335603201,19.1194392691357));
#23593=CARTESIAN_POINT('Ctrl Pts',(1.14303628091464,-2.84819204886657,19.3179553865473));
#23594=CARTESIAN_POINT('Ctrl Pts',(0.266867528478102,1.24027160533984,19.516471503959));
#23595=CARTESIAN_POINT('Ctrl Pts',(3.22745620631011,4.19291811607857,19.7149876213706));
#23596=CARTESIAN_POINT('Ctrl Pts',(7.31355151948446,3.30576997342133,19.9135037387823));
#23597=CARTESIAN_POINT('Ctrl Pts',(8.78318510623113,-0.60873942761753,20.112019856194));
#23598=CARTESIAN_POINT('Ctrl Pts',(6.29049448270258,-3.96577684195559,20.3105359736056));
#23599=CARTESIAN_POINT('Ctrl Pts',(2.11823830688215,-3.69103125832118,20.5090520910173));
#23600=CARTESIAN_POINT('Ctrl Pts',(0.0872894180178925,-0.0361094652841183,
20.7075682084289));
#23601=CARTESIAN_POINT('Ctrl Pts',(2.05755217931839,3.65188070090475,20.9060843258406));
#23602=CARTESIAN_POINT('Ctrl Pts',(6.2246974255821,3.99554796485774,21.1046004432522));
#23603=CARTESIAN_POINT('Ctrl Pts',(8.77253282078492,0.680168449111409,21.3031165606639));
#23604=CARTESIAN_POINT('Ctrl Pts',(7.36779915003431,-3.25809647691284,21.5016326780756));
#23605=CARTESIAN_POINT('Ctrl Pts',(3.29692483597213,-4.21265846617502,21.7001487954872));
#23606=CARTESIAN_POINT('Ctrl Pts',(0.287939047401517,-1.30934826998177,
21.8986649128989));
#23607=CARTESIAN_POINT('Ctrl Pts',(1.09641390858805,2.79303874980958,22.0971810303105));
#23608=CARTESIAN_POINT('Ctrl Pts',(4.98196318268333,4.33761289058522,22.2956971477222));
#23609=CARTESIAN_POINT('Ctrl Pts',(8.38627540352384,1.90988580729624,22.4942132651338));
#23610=CARTESIAN_POINT('Ctrl Pts',(8.19174495281671,-2.26688249514424,22.6927293825455));
#23611=CARTESIAN_POINT('Ctrl Pts',(4.57652150231426,-4.36767501203749,22.8912454999571));
#23612=CARTESIAN_POINT('Ctrl Pts',(0.851353342793238,-2.46864902413938,
23.0897616173688));
#23613=CARTESIAN_POINT('Ctrl Pts',(0.42768739434844,1.69114792223732,23.2882777347804));
#23614=CARTESIAN_POINT('Ctrl Pts',(3.69349202933814,4.30216786317793,23.4867938521921));
#23615=CARTESIAN_POINT('Ctrl Pts',(7.65803780123451,2.9734515702302,23.6853099696038));
#23616=CARTESIAN_POINT('Ctrl Pts',(8.6906071069521,-1.07850088950778,23.8838260870154));
#23617=CARTESIAN_POINT('Ctrl Pts',(5.84571156354535,-4.14238794997599,24.0823422044271));
#23618=CARTESIAN_POINT('Ctrl Pts',(1.7284241969769,-3.41351242146536,24.2808583218387));
#23619=CARTESIAN_POINT('Ctrl Pts',(0.109716235810993,0.442846747958131,
24.4793744392504));
#23620=CARTESIAN_POINT('Ctrl Pts',(2.47112996587446,3.89086027970496,24.677890556662));
#23621=CARTESIAN_POINT('Ctrl Pts',(6.6517366226307,3.78111221715306,24.8764066740737));
#23622=CARTESIAN_POINT('Ctrl Pts',(8.82041412666913,0.197058426719993,25.0749656474274));
#23623=CARTESIAN_POINT('Ctrl Pts',(7.60321109049825,-2.29676940207044,25.2073525816438));
#23624=CARTESIAN_POINT('Ctrl Pts',(6.60115576990582,-3.01054754622974,25.273567476723));
#23625=CARTESIAN_POINT('Ctrl Pts',(6.20648120676596,3.5255164385887,0.00171096560382468));
#23626=CARTESIAN_POINT('Ctrl Pts',(7.37912772202248,2.94343275606714,0.0678830047410433));
#23627=CARTESIAN_POINT('Ctrl Pts',(9.07759664569311,0.527144320628084,0.200227083015481));
#23628=CARTESIAN_POINT('Ctrl Pts',(7.40162371335757,-3.60564141759996,0.398743200427137));
#23629=CARTESIAN_POINT('Ctrl Pts',(3.02458781445768,-4.42536858002973,0.597259317838794));
#23630=CARTESIAN_POINT('Ctrl Pts',(-0.0391348072720899,-1.19794185424409,
0.795775435250448));
#23631=CARTESIAN_POINT('Ctrl Pts',(1.01307994788347,3.12938294858669,0.994291552662105));
#23632=CARTESIAN_POINT('Ctrl Pts',(5.21923250695947,4.58939821694615,1.19280767007376));
#23633=CARTESIAN_POINT('Ctrl Pts',(8.72657551299543,1.84730106611042,1.39132378748542));
#23634=CARTESIAN_POINT('Ctrl Pts',(8.32358502229467,-2.58692118447061,1.58983990489707));
#23635=CARTESIAN_POINT('Ctrl Pts',(4.37908581601258,-4.65188073047965,1.78835602230873));
#23636=CARTESIAN_POINT('Ctrl Pts',(0.505493161016087,-2.45684558601761,
1.98687213972038));
#23637=CARTESIAN_POINT('Ctrl Pts',(0.250108060020668,1.98817892786946,2.18538825713204));
#23638=CARTESIAN_POINT('Ctrl Pts',(3.8468393694429,4.61243733220712,2.38390437454369));
#23639=CARTESIAN_POINT('Ctrl Pts',(8.0018522734089,3.01272882884126,2.58242049195535));
#23640=CARTESIAN_POINT('Ctrl Pts',(8.91007369571349,-1.34598748780205,2.78093660936701));
#23641=CARTESIAN_POINT('Ctrl Pts',(5.73976719690925,-4.47206986535408,2.97945272677866));
#23642=CARTESIAN_POINT('Ctrl Pts',(1.39424152787623,-3.50271791779653,3.17796884419032));
#23643=CARTESIAN_POINT('Ctrl Pts',(-0.146954797017362,0.674357611516781,
3.37648496160198));
#23644=CARTESIAN_POINT('Ctrl Pts',(2.5275771424141,4.23386867290823,3.57500107901363));
#23645=CARTESIAN_POINT('Ctrl Pts',(6.96855153613195,3.91608365047424,3.77351719642529));
#23646=CARTESIAN_POINT('Ctrl Pts',(9.10900868522111,0.0120235511094912,
3.97203331383693));
#23647=CARTESIAN_POINT('Ctrl Pts',(6.98875855737045,-3.90304740339865,4.17054943124861));
#23648=CARTESIAN_POINT('Ctrl Pts',(2.54948593565754,-4.24378183362265,4.36906554866025));
#23649=CARTESIAN_POINT('Ctrl Pts',(-0.143407781592193,-0.698141563015474,
4.56758166607191));
#23650=CARTESIAN_POINT('Ctrl Pts',(1.37617826049345,3.48684345900968,4.76609778348356));
#23651=CARTESIAN_POINT('Ctrl Pts',(5.71663606344787,4.47864357428809,4.96461390089523));
#23652=CARTESIAN_POINT('Ctrl Pts',(8.90305693908813,1.36898709382619,5.16313001830687));
#23653=CARTESIAN_POINT('Ctrl Pts',(8.01737725983028,-2.99436172457643,5.36164613571854));
#23654=CARTESIAN_POINT('Ctrl Pts',(3.87068562947579,-4.61553103529222,5.56016225313019));
#23655=CARTESIAN_POINT('Ctrl Pts',(0.260443364168955,-2.00988482013811,
5.75867837054185));
#23656=CARTESIAN_POINT('Ctrl Pts',(0.492841656646439,2.436375680996,5.95719448795349));
#23657=CARTESIAN_POINT('Ctrl Pts',(4.35505457120696,4.6514496783783,6.15571060536516));
#23658=CARTESIAN_POINT('Ctrl Pts',(8.31014098784587,2.60681454019155,6.35422672277681));
#23659=CARTESIAN_POINT('Ctrl Pts',(8.73610799988966,-1.82509176699825,6.55274284018847));
#23660=CARTESIAN_POINT('Ctrl Pts',(5.24286312047947,-4.58561375091533,6.75125895760012));
#23661=CARTESIAN_POINT('Ctrl Pts',(1.02945356160573,-3.14671788935761,6.94977507501179));
#23662=CARTESIAN_POINT('Ctrl Pts',(-0.0455603502579819,1.17388235834786,
7.14829119242343));
#23663=CARTESIAN_POINT('Ctrl Pts',(3.00229867643747,4.41946347189101,7.34680730983509));
#23664=CARTESIAN_POINT('Ctrl Pts',(7.38185932147204,3.61778400498435,7.54532342724674));
#23665=CARTESIAN_POINT('Ctrl Pts',(9.08240325419932,-0.496993236137507,
7.7438395446584));
#23666=CARTESIAN_POINT('Ctrl Pts',(6.5466046888036,-4.15663352541875,7.94235566207006));
#23667=CARTESIAN_POINT('Ctrl Pts',(2.09669971547073,-4.00970789967487,8.1408717794817));
#23668=CARTESIAN_POINT('Ctrl Pts',(-0.192173337388976,-0.19076805214061,
8.33938789689338));
#23669=CARTESIAN_POINT('Ctrl Pts',(1.77609193305126,3.80287354875093,8.53790401430502));
#23670=CARTESIAN_POINT('Ctrl Pts',(6.1989956324977,4.3139158920216,8.73642013171668));
#23671=CARTESIAN_POINT('Ctrl Pts',(9.0261266855466,0.874356120760312,8.93493624912834));
#23672=CARTESIAN_POINT('Ctrl Pts',(7.66845225155073,-3.36592235387631,9.13345236653999));
#23673=CARTESIAN_POINT('Ctrl Pts',(3.36930475145732,-4.52375316346519,9.33196848395166));
#23674=CARTESIAN_POINT('Ctrl Pts',(0.0657616873951493,-1.53881687686219,
9.53048460136329));
#23675=CARTESIAN_POINT('Ctrl Pts',(0.783144957380055,2.85533863417045,9.72900071877498));
#23676=CARTESIAN_POINT('Ctrl Pts',(4.86448860883662,4.63462933832978,9.92751683618659));
#23677=CARTESIAN_POINT('Ctrl Pts',(8.57217576114917,2.16961465444475,10.1260329535983));
#23678=CARTESIAN_POINT('Ctrl Pts',(8.51077704791793,-2.28229185953398,10.3245490710099));
#23679=CARTESIAN_POINT('Ctrl Pts',(4.73652024279266,-4.644118902346,10.5230651884216));
#23680=CARTESIAN_POINT('Ctrl Pts',(0.705797933930029,-2.75295019489822,
10.7215813058332));
#23681=CARTESIAN_POINT('Ctrl Pts',(0.109868939318185,1.65931793437198,10.9200974232449));
#23682=CARTESIAN_POINT('Ctrl Pts',(3.49447369645122,4.55201426291826,11.1186135406565));
#23683=CARTESIAN_POINT('Ctrl Pts',(7.76005555075585,3.27606251797663,11.3171296580682));
#23684=CARTESIAN_POINT('Ctrl Pts',(9.00027578003045,-1.00004496361109,11.5156457754798));
#23685=CARTESIAN_POINT('Ctrl Pts',(6.07936428979557,-4.36033029039609,11.7141618928915));
#23686=CARTESIAN_POINT('Ctrl Pts',(1.67223626118035,-3.72750807951321,11.9126780103032));
#23687=CARTESIAN_POINT('Ctrl Pts',(-0.185144289673645,0.31889512586586,
12.1111941277148));
#23688=CARTESIAN_POINT('Ctrl Pts',(2.20817641458127,4.07326024100545,12.3097102451265));
#23689=CARTESIAN_POINT('Ctrl Pts',(6.66044079877556,4.09741110905781,12.5082263625381));
#23690=CARTESIAN_POINT('Ctrl Pts',(9.09434983091284,0.369230824458725,12.7067424799498));
#23691=CARTESIAN_POINT('Ctrl Pts',(7.28097591722075,-3.69708402566464,12.9052585973614));
#23692=CARTESIAN_POINT('Ctrl Pts',(2.8809723938291,-4.37767965107946,13.1037747147731));
#23693=CARTESIAN_POINT('Ctrl Pts',(-0.0762212094817758,-1.04927952433239,
13.3022908321848));
#23694=CARTESIAN_POINT('Ctrl Pts',(1.11753675741321,3.24003083138531,13.5008069495964));
#23695=CARTESIAN_POINT('Ctrl Pts',(5.369025456116,4.5621825836419,13.6993230670081));
#23696=CARTESIAN_POINT('Ctrl Pts',(8.78481240824481,1.70637430771384,13.8978391844197));
#23697=CARTESIAN_POINT('Ctrl Pts',(8.23678489819753,-2.71209910053747,14.0963553018314));
#23698=CARTESIAN_POINT('Ctrl Pts',(4.22681609508684,-4.64688374211174,14.294871419243));
#23699=CARTESIAN_POINT('Ctrl Pts',(0.427159151106815,-2.32614064576156,
14.4933875366547));
#23700=CARTESIAN_POINT('Ctrl Pts',(0.317467618415429,2.12483780609018,14.6919036540663));
#23701=CARTESIAN_POINT('Ctrl Pts',(3.99819491609722,4.62993021382537,14.890419771478));
#23702=CARTESIAN_POINT('Ctrl Pts',(8.09860099979244,2.8950206023505,15.0889358888896));
#23703=CARTESIAN_POINT('Ctrl Pts',(8.86361197604717,-1.49109380762589,15.2874520063013));
#23704=CARTESIAN_POINT('Ctrl Pts',(5.59264534485911,-4.5116928721902,15.485968123713));
#23705=CARTESIAN_POINT('Ctrl Pts',(1.2811901266875,-3.40056942590122,15.6844842411246));
#23706=CARTESIAN_POINT('Ctrl Pts',(-0.122405002240585,0.824730814938715,
15.8830003585363));
#23707=CARTESIAN_POINT('Ctrl Pts',(2.66724567793686,4.29475826350135,16.0815164759479));
#23708=CARTESIAN_POINT('Ctrl Pts',(7.09543313909595,3.83172778931411,16.2800325933596));
#23709=CARTESIAN_POINT('Ctrl Pts',(9.10690753736432,-0.140326107135887,
16.4785487107712));
#23710=CARTESIAN_POINT('Ctrl Pts',(6.85959888110794,-3.98387202395643,16.6770648281829));
#23711=CARTESIAN_POINT('Ctrl Pts',(2.41154968938301,-4.179063722519,16.8755809455945));
#23712=CARTESIAN_POINT('Ctrl Pts',(-0.163801198896094,-0.547148358219792,
17.0740970630062));
#23713=CARTESIAN_POINT('Ctrl Pts',(1.49200357138825,3.5858350646717,17.2726131804178));
#23714=CARTESIAN_POINT('Ctrl Pts',(5.86260948835618,4.43497894515246,17.4711292978295));
#23715=CARTESIAN_POINT('Ctrl Pts',(8.94549879098837,1.22265346990726,17.6696454152412));
#23716=CARTESIAN_POINT('Ctrl Pts',(7.91742009870712,-3.10935479574357,17.8681615326528));
#23717=CARTESIAN_POINT('Ctrl Pts',(3.71986832177296,-4.59387508565289,18.0666776500645));
#23718=CARTESIAN_POINT('Ctrl Pts',(0.196881531601468,-1.87141195688986,
18.2651937674761));
#23719=CARTESIAN_POINT('Ctrl Pts',(0.574744016316265,2.56485464396025,18.4637098848878));
#23720=CARTESIAN_POINT('Ctrl Pts',(4.50741650012369,4.6522761505852,18.6622260022994));
#23721=CARTESIAN_POINT('Ctrl Pts',(8.3934323297128,2.47923165417059,18.8607421197111));
#23722=CARTESIAN_POINT('Ctrl Pts',(8.67405212821057,-1.96424603112833,19.0592582371228));
#23723=CARTESIAN_POINT('Ctrl Pts',(5.09228962209667,-4.60890456507674,19.2577743545344));
#23724=CARTESIAN_POINT('Ctrl Pts',(0.928254782143413,-3.0328159689208,19.4562904719461));
#23725=CARTESIAN_POINT('Ctrl Pts',(-0.00470849360073685,1.32066780116548,
19.6548065893577));
#23726=CARTESIAN_POINT('Ctrl Pts',(3.14778981602278,4.46470912096001,19.8533227067694));
#23727=CARTESIAN_POINT('Ctrl Pts',(7.49875172579254,3.52005475507203,20.051838824181));
#23728=CARTESIAN_POINT('Ctrl Pts',(9.06364908309027,-0.648198796048447,
20.2503549415927));
#23729=CARTESIAN_POINT('Ctrl Pts',(6.4093786550744,-4.22284422156345,20.4488710590044));
#23730=CARTESIAN_POINT('Ctrl Pts',(1.96667081116617,-3.93028923259476,20.647387176416));
#23731=CARTESIAN_POINT('Ctrl Pts',(-0.195927116407106,-0.0384501329489085,
20.8459032938277));
#23732=CARTESIAN_POINT('Ctrl Pts',(1.90205092121151,3.88860087953163,21.0444194112393));
#23733=CARTESIAN_POINT('Ctrl Pts',(6.3393165377314,4.25454515162759,21.242935528651));
#23734=CARTESIAN_POINT('Ctrl Pts',(9.05230630112455,0.724257949825445,21.4414516460626));
#23735=CARTESIAN_POINT('Ctrl Pts',(7.55651576606266,-3.46929099370176,21.6399677634743));
#23736=CARTESIAN_POINT('Ctrl Pts',(3.22176150253947,-4.48572906904549,21.838483880886));
#23737=CARTESIAN_POINT('Ctrl Pts',(0.0177289115966501,-1.39422211492368,
22.0369999982976));
#23738=CARTESIAN_POINT('Ctrl Pts',(0.878610280341868,2.97408755340353,22.2355161157093));
#23739=CARTESIAN_POINT('Ctrl Pts',(5.01602646728549,4.61878321962123,22.4340322331209));
#23740=CARTESIAN_POINT('Ctrl Pts',(8.64101112050298,2.03368736229999,22.6325483505326));
#23741=CARTESIAN_POINT('Ctrl Pts',(8.43387092517075,-2.41382509078919,22.8310644679442));
#23742=CARTESIAN_POINT('Ctrl Pts',(4.58430347192829,-4.65079401118156,23.0295805853559));
#23743=CARTESIAN_POINT('Ctrl Pts',(0.617664534920323,-2.6286704174496,23.2280967027675));
#23744=CARTESIAN_POINT('Ctrl Pts',(0.166535948123391,1.80077057177711,23.4266128201792));
#23745=CARTESIAN_POINT('Ctrl Pts',(3.64403475383551,4.58104059437149,23.6251289375908));
#23746=CARTESIAN_POINT('Ctrl Pts',(7.86556810560143,3.16619499327494,23.8236450550025));
#23747=CARTESIAN_POINT('Ctrl Pts',(8.96507004425898,-1.14841087401253,24.0221611724142));
#23748=CARTESIAN_POINT('Ctrl Pts',(5.93576426504054,-4.41090351654891,24.2206772898258));
#23749=CARTESIAN_POINT('Ctrl Pts',(1.55158838794904,-3.63478122412758,24.4191934072375));
#23750=CARTESIAN_POINT('Ctrl Pts',(-0.172046559910909,0.471552713422697,
24.6177095246491));
#23751=CARTESIAN_POINT('Ctrl Pts',(2.34243741690352,4.14307145960353,24.8162256420608));
#23752=CARTESIAN_POINT('Ctrl Pts',(6.79403703197597,4.02620936921257,25.0147417594724));
#23753=CARTESIAN_POINT('Ctrl Pts',(9.10329134237422,0.209832038399488,25.2133007328261));
#23754=CARTESIAN_POINT('Ctrl Pts',(7.80718744833136,-2.44564931016495,25.3456876670425));
#23755=CARTESIAN_POINT('Ctrl Pts',(6.7401774553626,-3.20569558398784,25.4119025621217));
#23756=CARTESIAN_POINT('Ctrl Pts',(6.28979540306975,-2.65047774028997,2.34187669256869E-16));
#23757=CARTESIAN_POINT('Ctrl Pts',(6.07824975460912,-2.79680313454321,0.0168403156216635));
#23758=CARTESIAN_POINT('Ctrl Pts',(5.84989216698747,-2.91731508079941,0.0345979173544468));
#23759=CARTESIAN_POINT('Ctrl Pts',(5.51500906830149,-3.04563029082768,0.0584806141104239));
#23760=CARTESIAN_POINT('Ctrl Pts',(5.41879312933457,-3.07738628407187,0.0651272920591958));
#23761=CARTESIAN_POINT('Ctrl Pts',(5.2796709515883,-3.11613828015728,0.0744133179630824));
#23762=CARTESIAN_POINT('Ctrl Pts',(5.23787838666673,-3.12688005475488,0.0771625196878118));
#23763=CARTESIAN_POINT('Ctrl Pts',(5.16290892864459,-3.14455210035684,0.0820236116212797));
#23764=CARTESIAN_POINT('Ctrl Pts',(5.12981532258863,-3.15180426839707,0.0841452115614535));
#23765=CARTESIAN_POINT('Ctrl Pts',(5.07951773377748,-3.16199813479694,0.0873343454331657));
#23766=CARTESIAN_POINT('Ctrl Pts',(5.06239487350367,-3.1653239613259,0.0884138587685488));
#23767=CARTESIAN_POINT('Ctrl Pts',(5.0313026349073,-3.17110155867653,0.0903631796000517));
#23768=CARTESIAN_POINT('Ctrl Pts',(5.01734256342,-3.17360042478014,0.0912344378453712));
#23769=CARTESIAN_POINT('Ctrl Pts',(4.98724043292739,-3.17878390500948,0.0931048058941783));
#23770=CARTESIAN_POINT('Ctrl Pts',(4.97109345313393,-3.18143790017822,0.0941029416431362));
#23771=CARTESIAN_POINT('Ctrl Pts',(4.92727497325308,-3.18829778367847,0.0967981379299586));
#23772=CARTESIAN_POINT('Ctrl Pts',(4.89956738031451,-3.19226642284397,0.0984878499755184));
#23773=CARTESIAN_POINT('Ctrl Pts',(4.75398224404875,-3.21118694447669,0.107295236621157));
#23774=CARTESIAN_POINT('Ctrl Pts',(4.63538973943275,-3.21997319506732,0.114221706112698));
#23775=CARTESIAN_POINT('Ctrl Pts',(4.30095042759944,-3.22621149833508,0.13337700064414));
#23776=CARTESIAN_POINT('Ctrl Pts',(4.08547929171809,-3.20858045444597,0.145250495204097));
#23777=CARTESIAN_POINT('Ctrl Pts',(3.80133532677102,-3.156308727449,0.161766932561653));
#23778=CARTESIAN_POINT('Ctrl Pts',(3.72975840286589,-3.14060110737571,0.166006889533671));
#23779=CARTESIAN_POINT('Ctrl Pts',(3.61736503521311,-3.11188839215322,0.172876824823414));
#23780=CARTESIAN_POINT('Ctrl Pts',(3.57616339916112,-3.1004848786294,0.175441320926198));
#23781=CARTESIAN_POINT('Ctrl Pts',(3.52227753763667,-3.08441009116031,0.178870895262747));
#23782=CARTESIAN_POINT('Ctrl Pts',(3.50937666961836,-3.08047324277195,0.179697728734765));
#23783=CARTESIAN_POINT('Ctrl Pts',(3.48839742123833,-3.07392694119639,0.1810522852053));
#23784=CARTESIAN_POINT('Ctrl Pts',(3.48030382138514,-3.07136630181977,0.181577288984605));
#23785=CARTESIAN_POINT('Ctrl Pts',(3.46464166595954,-3.06634297482279,0.182598119865996));
#23786=CARTESIAN_POINT('Ctrl Pts',(3.45707206542002,-3.06388421131902,0.183093728839097));
#23787=CARTESIAN_POINT('Ctrl Pts',(3.43874556002866,-3.05785624189087,0.184299002209445));
#23788=CARTESIAN_POINT('Ctrl Pts',(3.42799835660854,-3.05425832581353,0.185010290454013));
#23789=CARTESIAN_POINT('Ctrl Pts',(3.39175714586998,-3.04191263431934,0.187423497374185));
#23790=CARTESIAN_POINT('Ctrl Pts',(3.36635472913545,-3.0329020045397,0.189139518999491));
#23791=CARTESIAN_POINT('Ctrl Pts',(3.18676606562611,-2.9666515504672,0.20143179357128));
#23792=CARTESIAN_POINT('Ctrl Pts',(3.03706086767606,-2.89800574240346,0.212511569449416));
#23793=CARTESIAN_POINT('Ctrl Pts',(2.75593821241035,-2.74207447322503,0.234233226407782));
#23794=CARTESIAN_POINT('Ctrl Pts',(2.6243541678938,-2.65596297714111,0.244842751365906));
#23795=CARTESIAN_POINT('Ctrl Pts',(2.40483061592065,-2.48819488821331,0.263043278354808));
#23796=CARTESIAN_POINT('Ctrl Pts',(2.31417740986267,-2.41058629886545,0.270735581712772));
#23797=CARTESIAN_POINT('Ctrl Pts',(2.2084003264213,-2.30933806977478,0.27993104622173));
#23798=CARTESIAN_POINT('Ctrl Pts',(2.1890133115413,-2.29030562382644,0.281626447688871));
#23799=CARTESIAN_POINT('Ctrl Pts',(2.15865709979275,-2.25974128583443,0.284297867569297));
#23800=CARTESIAN_POINT('Ctrl Pts',(2.14752900807433,-2.24836970567203,0.285280840394977));
#23801=CARTESIAN_POINT('Ctrl Pts',(2.1267340987307,-2.22680257934588,0.287124882972914));
#23802=CARTESIAN_POINT('Ctrl Pts',(2.11704888995185,-2.21662536168207,0.287986737897884));
#23803=CARTESIAN_POINT('Ctrl Pts',(2.09536992067828,-2.1935447400592,0.289922870727941));
#23804=CARTESIAN_POINT('Ctrl Pts',(2.08341472592883,-2.18060560805158,0.290995491095302));
#23805=CARTESIAN_POINT('Ctrl Pts',(2.05301110921061,-2.14715353240371,0.293736531578305));
#23806=CARTESIAN_POINT('Ctrl Pts',(2.03471867019213,-2.12650030132646,0.295398433992035));
#23807=CARTESIAN_POINT('Ctrl Pts',(1.88234579830737,-1.9499458084177,0.309358858105313));
#23808=CARTESIAN_POINT('Ctrl Pts',(1.76319789510205,-1.78177019902244,0.3210139179675));
#23809=CARTESIAN_POINT('Ctrl Pts',(1.58764529498356,-1.47568089556482,0.340776631952162));
#23810=CARTESIAN_POINT('Ctrl Pts',(1.52325019859249,-1.34313346058477,0.348939672724235));
#23811=CARTESIAN_POINT('Ctrl Pts',(1.44230346334175,-1.14266590260818,0.361295114701718));
#23812=CARTESIAN_POINT('Ctrl Pts',(1.41852858174535,-1.07786645243649,0.365291698488638));
#23813=CARTESIAN_POINT('Ctrl Pts',(1.3840003923293,-0.973513071877454,0.371804634554866));
#23814=CARTESIAN_POINT('Ctrl Pts',(1.37188904586178,-0.934428807614549,
0.374260799611263));
#23815=CARTESIAN_POINT('Ctrl Pts',(1.35689880148942,-0.882582572681532,
0.377553881129702));
#23816=CARTESIAN_POINT('Ctrl Pts',(1.353348278791,-0.870016774840268,0.378354696523691));
#23817=CARTESIAN_POINT('Ctrl Pts',(1.34764524460579,-0.849353844300361,
0.379676458285701));
#23818=CARTESIAN_POINT('Ctrl Pts',(1.34544773269429,-0.841269139498996,
0.380194850194701));
#23819=CARTESIAN_POINT('Ctrl Pts',(1.34121604497553,-0.825457311698112,
0.381211273027812));
#23820=CARTESIAN_POINT('Ctrl Pts',(1.3391790561386,-0.817731097122878,0.381709141636219));
#23821=CARTESIAN_POINT('Ctrl Pts',(1.33468755813399,-0.800434350578908,
0.382826319689283));
#23822=CARTESIAN_POINT('Ctrl Pts',(1.33224828992365,-0.790859955080673,
0.383446487637849));
#23823=CARTESIAN_POINT('Ctrl Pts',(1.32393629749912,-0.75759584165232,0.385606885925548));
#23824=CARTESIAN_POINT('Ctrl Pts',(1.31828885549605,-0.733851407024439,
0.387159129623654));
#23825=CARTESIAN_POINT('Ctrl Pts',(1.2626755135077,-0.487636749627222,0.403343102159934));
#23826=CARTESIAN_POINT('Ctrl Pts',(1.23618781672172,-0.260541477067284,
0.418962728927435));
#23827=CARTESIAN_POINT('Ctrl Pts',(1.23243065565391,0.111194142621663,0.444046930361003));
#23828=CARTESIAN_POINT('Ctrl Pts',(1.24059942131418,0.254907803355904,0.453638284958007));
#23829=CARTESIAN_POINT('Ctrl Pts',(1.26830131528543,0.477725481866437,0.46820130328789));
#23830=CARTESIAN_POINT('Ctrl Pts',(1.28126951186522,0.557444978040998,0.473351480650301));
#23831=CARTESIAN_POINT('Ctrl Pts',(1.30194285132137,0.660040507109251,0.479904653015137));
#23832=CARTESIAN_POINT('Ctrl Pts',(1.30692718052677,0.683428907810724,0.481393548603338));
#23833=CARTESIAN_POINT('Ctrl Pts',(1.31547759917252,0.721468771378009,0.483807449117055));
#23834=CARTESIAN_POINT('Ctrl Pts',(1.31888693478886,0.736154172267918,0.484737462799632));
#23835=CARTESIAN_POINT('Ctrl Pts',(1.32566686527217,0.764455107891654,0.486526288552673));
#23836=CARTESIAN_POINT('Ctrl Pts',(1.32902353900982,0.778073594161443,0.48738552793633));
#23837=CARTESIAN_POINT('Ctrl Pts',(1.33696390011297,0.809406967195871,0.489359097967962));
#23838=CARTESIAN_POINT('Ctrl Pts',(1.34160979225497,0.827105703792237,0.490471383566467));
#23839=CARTESIAN_POINT('Ctrl Pts',(1.35707337969441,0.884036062422387,0.494041901107027));
#23840=CARTESIAN_POINT('Ctrl Pts',(1.36848374583208,0.923103606732883,0.496480832792461));
#23841=CARTESIAN_POINT('Ctrl Pts',(1.45357435458562,1.19518220536396,0.513409151783491));
#23842=CARTESIAN_POINT('Ctrl Pts',(1.55280772962875,1.41936708491062,0.526981581655514));
#23843=CARTESIAN_POINT('Ctrl Pts',(1.74477144619794,1.74672892300823,0.548187431600153));
#23844=CARTESIAN_POINT('Ctrl Pts',(1.82035847873746,1.858838747653,0.55575927780709));
#23845=CARTESIAN_POINT('Ctrl Pts',(1.92832043772892,1.99908459132599,0.566076921365318));
#23846=CARTESIAN_POINT('Ctrl Pts',(1.95453634583702,2.03179896372779,0.568549147416395));
#23847=CARTESIAN_POINT('Ctrl Pts',(1.99960984760573,2.08585000050386,0.572763008061946));
#23848=CARTESIAN_POINT('Ctrl Pts',(2.01812614747818,2.10746557009875,0.574484240749538));
#23849=CARTESIAN_POINT('Ctrl Pts',(2.04439029989786,2.13731633065713,0.57691682031363));
#23850=CARTESIAN_POINT('Ctrl Pts',(2.05189948459756,2.14576098180312,0.577611332813173));
#23851=CARTESIAN_POINT('Ctrl Pts',(2.06478228629329,2.16009612980221,0.578801525782487));
#23852=CARTESIAN_POINT('Ctrl Pts',(2.07013360476026,2.16600646535647,0.579295537778655));
#23853=CARTESIAN_POINT('Ctrl Pts',(2.08054845969122,2.17742384642834,0.580256371139919));
#23854=CARTESIAN_POINT('Ctrl Pts',(2.08560917047652,2.18293304706993,0.580722954137346));
#23855=CARTESIAN_POINT('Ctrl Pts',(2.09935110683142,2.19778866584626,0.581988994081901));
#23856=CARTESIAN_POINT('Ctrl Pts',(2.10806861051188,2.20710112631449,0.582791141795677));
#23857=CARTESIAN_POINT('Ctrl Pts',(2.14111009866999,2.2419802729716,0.585826918297046));
#23858=CARTESIAN_POINT('Ctrl Pts',(2.1657972161716,2.26719759451342,0.588085888836404));
#23859=CARTESIAN_POINT('Ctrl Pts',(2.34770486563578,2.44700788611533,0.604631936191454));
#23860=CARTESIAN_POINT('Ctrl Pts',(2.52000102485704,2.58550114333554,0.619733168426974));
#23861=CARTESIAN_POINT('Ctrl Pts',(2.82158340239779,2.78074273679449,0.643940663509552));
#23862=CARTESIAN_POINT('Ctrl Pts',(2.94285408867079,2.84857123274083,0.653181261672033));
#23863=CARTESIAN_POINT('Ctrl Pts',(3.13955858634984,2.94246980027581,0.667304720540197));
#23864=CARTESIAN_POINT('Ctrl Pts',(3.21222130786266,2.97392518504451,0.672350674394824));
#23865=CARTESIAN_POINT('Ctrl Pts',(3.30823673738015,3.01135367129709,0.67880290808403));
#23866=CARTESIAN_POINT('Ctrl Pts',(3.33059576293847,3.01978439141837,0.680290666522021));
#23867=CARTESIAN_POINT('Ctrl Pts',(3.36729831834166,3.03315918289536,0.682709296296089));
#23868=CARTESIAN_POINT('Ctrl Pts',(3.38158633492913,3.0382519109594,0.68364507372935));
#23869=CARTESIAN_POINT('Ctrl Pts',(3.40930565845442,3.04791199250808,0.685449562534719));
#23870=CARTESIAN_POINT('Ctrl Pts',(3.42273218827009,3.05249189925252,0.68631867114754));
#23871=CARTESIAN_POINT('Ctrl Pts',(3.453847531493,3.06287677042547,0.688321612512623));
#23872=CARTESIAN_POINT('Ctrl Pts',(3.47155738560099,3.06861745057343,0.689453315858022));
#23873=CARTESIAN_POINT('Ctrl Pts',(3.52928504695514,3.08677872506566,0.693116135910914));
#23874=CARTESIAN_POINT('Ctrl Pts',(3.56949652694581,3.0985727461866,0.695626901293803));
#23875=CARTESIAN_POINT('Ctrl Pts',(3.80563017808011,3.16285694558108,0.710155383560904));
#23876=CARTESIAN_POINT('Ctrl Pts',(4.00593161318787,3.19754341870944,0.721581594756166));
#23877=CARTESIAN_POINT('Ctrl Pts',(4.41491592618508,3.22914602457896,0.744544645105131));
#23878=CARTESIAN_POINT('Ctrl Pts',(4.62268116641124,3.22512989545908,0.756035684623915));
#23879=CARTESIAN_POINT('Ctrl Pts',(4.86097535314046,3.19742946533819,0.770350365044164));
#23880=CARTESIAN_POINT('Ctrl Pts',(4.89329945355423,3.19317389942722,0.772317143053407));
#23881=CARTESIAN_POINT('Ctrl Pts',(4.93743154918083,3.18668116842424,0.775043475043542));
#23882=CARTESIAN_POINT('Ctrl Pts',(4.94930102138977,3.18486709826258,0.775780814329541));
#23883=CARTESIAN_POINT('Ctrl Pts',(4.96922863750572,3.18170739816267,0.777026015788556));
#23884=CARTESIAN_POINT('Ctrl Pts',(4.97729242935448,3.18039736001144,0.777531900574851));
#23885=CARTESIAN_POINT('Ctrl Pts',(4.9926217782942,3.17784710159476,0.778497564797928));
#23886=CARTESIAN_POINT('Ctrl Pts',(4.99988823540604,3.17661258833065,0.778957009798921));
#23887=CARTESIAN_POINT('Ctrl Pts',(5.01717103467575,3.17361534294314,0.780053710117017));
#23888=CARTESIAN_POINT('Ctrl Pts',(5.02718332294179,3.17183011428051,0.780692205754548));
#23889=CARTESIAN_POINT('Ctrl Pts',(5.06265609270367,3.1653317918268,0.782965136001058));
#23890=CARTESIAN_POINT('Ctrl Pts',(5.08806727625383,3.16035942076377,0.784613102857243));
#23891=CARTESIAN_POINT('Ctrl Pts',(5.31536599923246,3.11303166670219,0.799514700325313));
#23892=CARTESIAN_POINT('Ctrl Pts',(5.51279641204211,3.05169284891943,0.813566914622217));
#23893=CARTESIAN_POINT('Ctrl Pts',(5.84809026026377,2.91105907337854,0.838134275200583));
#23894=CARTESIAN_POINT('Ctrl Pts',(5.98854849914638,2.83965078211244,0.848672215806842));
#23895=CARTESIAN_POINT('Ctrl Pts',(6.17170786092387,2.7289706073794,0.862579864170383));
#23896=CARTESIAN_POINT('Ctrl Pts',(6.21939794582009,2.69840825166359,0.866219333358702));
#23897=CARTESIAN_POINT('Ctrl Pts',(6.30077041072072,2.64318175420469,0.872461399371499));
#23898=CARTESIAN_POINT('Ctrl Pts',(6.33482388456517,2.61909157455961,0.875083913608399));
#23899=CARTESIAN_POINT('Ctrl Pts',(6.37199826894543,2.59169549764984,0.87795954337468));
#23900=CARTESIAN_POINT('Ctrl Pts',(6.37558956385616,2.58903731045176,0.878237483634976));
#23901=CARTESIAN_POINT('Ctrl Pts',(6.37917532099386,2.58637166203218,0.878515132681521));
#23902=CARTESIAN_POINT('Origin',(4.45646910621825,0.,0.));
#23903=CARTESIAN_POINT('Ctrl Pts',(6.20516358154934,3.52286199445085,6.93889390390723E-16));
#23904=CARTESIAN_POINT('Ctrl Pts',(6.26399827345772,3.49365735888464,0.00332252301440561));
#23905=CARTESIAN_POINT('Ctrl Pts',(6.32201823097654,3.4628755617916,0.00664504602881051));
#23906=CARTESIAN_POINT('Ctrl Pts',(6.37917532067789,3.43058507618661,0.00996756904321544));
#23907=CARTESIAN_POINT('Ctrl Pts',(6.37857781428809,3.43132439655042,0.193274600733303));
#23908=CARTESIAN_POINT('Ctrl Pts',(6.33400076845272,3.45629490883027,0.190678175003209));
#23909=CARTESIAN_POINT('Ctrl Pts',(6.2889659255652,3.48038043910034,0.188081749273116));
#23910=CARTESIAN_POINT('Ctrl Pts',(6.24351184914418,3.50356493231619,0.185485323543022));
#23911=CARTESIAN_POINT('Ctrl Pts',(6.14158456595626,3.55555438170445,0.179663037809694));
#23912=CARTESIAN_POINT('Ctrl Pts',(6.03720488368621,3.6031847036311,0.173840752076367));
#23913=CARTESIAN_POINT('Ctrl Pts',(5.93078566897907,3.64621443044277,0.168018466343039));
#23914=CARTESIAN_POINT('Ctrl Pts',(5.82450213616912,3.68918929540468,0.162203603881687));
#23915=CARTESIAN_POINT('Ctrl Pts',(5.71618462699839,3.72757506957501,0.156388741420336));
#23916=CARTESIAN_POINT('Ctrl Pts',(5.6062707198183,3.76117604604766,0.150573878958984));
#23917=CARTESIAN_POINT('Ctrl Pts',(5.49646629703298,3.79474355284694,0.144764808637259));
#23918=CARTESIAN_POINT('Ctrl Pts',(5.38506903844422,3.82353561660776,0.138955738315534));
#23919=CARTESIAN_POINT('Ctrl Pts',(5.27253590588312,3.84740483683284,0.133146667993808));
#23920=CARTESIAN_POINT('Ctrl Pts',(5.16008059026756,3.87125755143182,0.12734161465889));
#23921=CARTESIAN_POINT('Ctrl Pts',(5.04649137320448,3.89019410488495,0.121536561323971));
#23922=CARTESIAN_POINT('Ctrl Pts',(4.93223904889052,3.90411730889962,0.115731507989053));
#23923=CARTESIAN_POINT('Ctrl Pts',(4.81802731698202,3.91803556617605,0.109928517116146));
#23924=CARTESIAN_POINT('Ctrl Pts',(4.70315336348797,3.92694396305522,0.10412552624324));
#23925=CARTESIAN_POINT('Ctrl Pts',(4.58809612746815,3.93079678020588,0.0983225353703337));
#23926=CARTESIAN_POINT('Ctrl Pts',(4.47305074147543,3.93464920054544,0.0925201421616984));
#23927=CARTESIAN_POINT('Ctrl Pts',(4.35782253127168,3.93344706257557,0.0867177489530631));
#23928=CARTESIAN_POINT('Ctrl Pts',(4.24289266529862,3.92719672334912,0.0809153557444278));
#23929=CARTESIAN_POINT('Ctrl Pts',(4.12794563917741,3.92094545088617,0.0751120961819844));
#23930=CARTESIAN_POINT('Ctrl Pts',(4.013297466179,3.909644502795,0.069308836619541));
#23931=CARTESIAN_POINT('Ctrl Pts',(3.89942559792773,3.89335222268309,0.0635055770570976));
#23932=CARTESIAN_POINT('Ctrl Pts',(3.78544212541581,3.87704397473027,0.0576966297993286));
#23933=CARTESIAN_POINT('Ctrl Pts',(3.67223689416757,3.85573468718041,0.0518876825415597));
#23934=CARTESIAN_POINT('Ctrl Pts',(3.56027855345575,3.82953410914947,0.0460787352837907));
#23935=CARTESIAN_POINT('Ctrl Pts',(3.44826087686546,3.80331964529008,0.0402667093899295));
#23936=CARTESIAN_POINT('Ctrl Pts',(3.33749181154649,3.77220884343344,0.0344546834960684));
#23937=CARTESIAN_POINT('Ctrl Pts',(3.22842443136256,3.73636123475214,0.0286426576022072));
#23938=CARTESIAN_POINT('Ctrl Pts',(3.11919320000295,3.7004597724547,0.0228219003417894));
#23939=CARTESIAN_POINT('Ctrl Pts',(3.01166915181536,3.65980744271886,0.0170011430813716));
#23940=CARTESIAN_POINT('Ctrl Pts',(2.90628516992032,3.61461184135224,0.0111803858209537));
#23941=CARTESIAN_POINT('Ctrl Pts',(2.8392122478765,3.58584654901203,0.00747569378955098));
#23942=CARTESIAN_POINT('Ctrl Pts',(2.77300576585457,3.5552417956376,0.00377100175814821));
#23943=CARTESIAN_POINT('Ctrl Pts',(2.70777160956256,3.52286049471024,6.63097267454378E-5));
#23944=CARTESIAN_POINT('Origin',(4.45646910621825,-5.13094777615093E-16,
-2.31077344927308));
#23945=CARTESIAN_POINT('Ctrl Pts',(2.58488257447924,-2.62360084935057,-3.5527136788005E-15));
#23946=CARTESIAN_POINT('Ctrl Pts',(2.50157068764126,-2.56416901718817,0.00631741419995904));
#23947=CARTESIAN_POINT('Ctrl Pts',(2.4210367769768,-2.50072579486678,0.0126348283999217));
#23948=CARTESIAN_POINT('Ctrl Pts',(2.34367228340277,-2.4335585359717,0.0189522425998843));
#23949=CARTESIAN_POINT('Ctrl Pts',(2.26635227642181,-2.36642989999491,0.02526602412261));
#23950=CARTESIAN_POINT('Ctrl Pts',(2.19219836315962,-2.29558175594025,0.0315798056453355));
#23951=CARTESIAN_POINT('Ctrl Pts',(2.12156918716279,-2.22134192111315,0.0378935871680612));
#23952=CARTESIAN_POINT('Ctrl Pts',(2.05096424093384,-2.14712755471238,0.0442052027096813));
#23953=CARTESIAN_POINT('Ctrl Pts',(1.98388190260799,-2.06952410786498,0.0505168182513019));
#23954=CARTESIAN_POINT('Ctrl Pts',(1.92064376403118,-1.98889602453766,0.0568284337929219));
#23955=CARTESIAN_POINT('Ctrl Pts',(1.85739487416585,-1.90825423340985,0.0631411223895259));
#23956=CARTESIAN_POINT('Ctrl Pts',(1.79799174587117,-1.82458709234475,0.0694538109861296));
#23957=CARTESIAN_POINT('Ctrl Pts',(1.74271535062685,-1.73829172365097,0.0757664995827336));
#23958=CARTESIAN_POINT('Ctrl Pts',(1.68743061602759,-1.65198333587902,0.0820801405524201));
#23959=CARTESIAN_POINT('Ctrl Pts',(1.63627407288981,-1.56304627215329,0.0883937815221068));
#23960=CARTESIAN_POINT('Ctrl Pts',(1.58948251426926,-1.47190537878104,0.0947074224917932));
#23961=CARTESIAN_POINT('Ctrl Pts',(1.54267402606718,-1.38073150986299,0.101023347790164));
#23962=CARTESIAN_POINT('Ctrl Pts',(1.50023385155733,-1.2873525843142,0.107339273088534));
#23963=CARTESIAN_POINT('Ctrl Pts',(1.46235182621787,-1.19221611971277,0.113655198386905));
#23964=CARTESIAN_POINT('Ctrl Pts',(1.42444809981949,-1.09702515533197,0.119974741819887));
#23965=CARTESIAN_POINT('Ctrl Pts',(1.39110787082884,-1.00007502359117,0.126294285252868));
#23966=CARTESIAN_POINT('Ctrl Pts',(1.36247182640407,-0.901830579988466,
0.13261382868585));
#23967=CARTESIAN_POINT('Ctrl Pts',(1.33379348022257,-0.803441007662954,
0.138942707479016));
#23968=CARTESIAN_POINT('Ctrl Pts',(1.3098333100831,-0.703753694545378,0.145271586272182));
#23969=CARTESIAN_POINT('Ctrl Pts',(1.2906814498789,-0.603246282598787,0.151600465065348));
#23970=CARTESIAN_POINT('Ctrl Pts',(1.27151389667214,-0.502656515045226,
0.15793452973132));
#23971=CARTESIAN_POINT('Ctrl Pts',(1.25716256324945,-0.401245709925989,
0.164268594397292));
#23972=CARTESIAN_POINT('Ctrl Pts',(1.24766576452444,-0.299497373668809,
0.170602659063265));
#23973=CARTESIAN_POINT('Ctrl Pts',(1.23815230744814,-0.197570560476596,
0.176947834323174));
#23974=CARTESIAN_POINT('Ctrl Pts',(1.23351041447289,-0.0953054378363929,
0.183293009583083));
#23975=CARTESIAN_POINT('Ctrl Pts',(1.23372630841194,0.00681334627341558,
0.189638184842992));
#23976=CARTESIAN_POINT('Ctrl Pts',(1.23382699866106,0.0544402776128069,
0.192597495699212));
#23977=CARTESIAN_POINT('Ctrl Pts',(1.23498360239768,0.102035435663407,0.195556806555432));
#23978=CARTESIAN_POINT('Ctrl Pts',(1.23719087673066,0.149550137569756,0.198516117411651));
#23979=CARTESIAN_POINT('Ctrl Pts',(1.24174932668504,0.247677220144283,0.204627668765258));
#23980=CARTESIAN_POINT('Ctrl Pts',(1.25080826090224,0.345803872861143,0.210739220118864));
#23981=CARTESIAN_POINT('Ctrl Pts',(1.26437801075032,0.443477170476924,0.21685077147247));
#23982=CARTESIAN_POINT('Ctrl Pts',(1.27792738297975,0.541003792639323,0.22295314514305));
#23983=CARTESIAN_POINT('Ctrl Pts',(1.29597405496826,0.638077977311205,0.229055518813629));
#23984=CARTESIAN_POINT('Ctrl Pts',(1.3184763837669,0.734247394508317,0.235157892484209));
#23985=CARTESIAN_POINT('Ctrl Pts',(1.34095191103269,0.830302268547761,0.241252997886249));
#23986=CARTESIAN_POINT('Ctrl Pts',(1.36787245042669,0.925454087006087,0.24734810328829));
#23987=CARTESIAN_POINT('Ctrl Pts',(1.3991447764821,1.01925733026713,0.25344320869033));
#23988=CARTESIAN_POINT('Ctrl Pts',(1.43038946774705,1.11297768129407,0.259532927957667));
#23989=CARTESIAN_POINT('Ctrl Pts',(1.46597816254694,1.20535140612818,0.265622647225003));
#23990=CARTESIAN_POINT('Ctrl Pts',(1.50576720162495,1.29594592199264,0.27171236649234));
#23991=CARTESIAN_POINT('Ctrl Pts',(1.54553752828296,1.38649783208751,0.27779922182058));
#23992=CARTESIAN_POINT('Ctrl Pts',(1.58950409832805,1.4752717888499,0.28388607714882));
#23993=CARTESIAN_POINT('Ctrl Pts',(1.6374746434305,1.56185395644788,0.28997293247706));
#23994=CARTESIAN_POINT('Ctrl Pts',(1.68543609785703,1.6484197162601,0.296058634313524));
#23995=CARTESIAN_POINT('Ctrl Pts',(1.73739980467476,1.73279412366717,0.302144336149989));
#23996=CARTESIAN_POINT('Ctrl Pts',(1.79312747173125,1.8145878045738,0.308230037986454));
#23997=CARTESIAN_POINT('Ctrl Pts',(1.84886022590844,1.89638895204685,0.314316295358462));
#23998=CARTESIAN_POINT('Ctrl Pts',(1.90835737172213,1.97560853862661,0.32040255273047));
#23999=CARTESIAN_POINT('Ctrl Pts',(1.97133786527822,2.051887004151,0.326488810102477));
#24000=CARTESIAN_POINT('Ctrl Pts',(2.03438354345234,2.12824441765368,0.332581366732233));
#24001=CARTESIAN_POINT('Ctrl Pts',(2.10091948534764,2.20165428819934,0.338673923361988));
#24002=CARTESIAN_POINT('Ctrl Pts',(2.17062515492173,2.27179114198929,0.344766479991743));
#24003=CARTESIAN_POINT('Ctrl Pts',(2.24036729840072,2.34196469530383,0.350862224587877));
#24004=CARTESIAN_POINT('Ctrl Pts',(2.31328214346588,2.40886152281209,0.356957969184011));
#24005=CARTESIAN_POINT('Ctrl Pts',(2.38901484496053,2.47219546963972,0.363053713780146));
#24006=CARTESIAN_POINT('Ctrl Pts',(2.46487788184523,2.53563841369709,0.369159949105304));
#24007=CARTESIAN_POINT('Ctrl Pts',(2.54356810737106,2.59550596129862,0.375266184430463));
#24008=CARTESIAN_POINT('Ctrl Pts',(2.62470032786385,2.65155439415183,0.381372419755621));
#24009=CARTESIAN_POINT('Ctrl Pts',(2.69405651331979,2.69946760890019,0.386592358111516));
#24010=CARTESIAN_POINT('Ctrl Pts',(2.76519663464012,2.74459057588682,0.391812296467411));
#24011=CARTESIAN_POINT('Ctrl Pts',(2.8378668229934,2.78679820066671,0.397032234823306));
#24012=CARTESIAN_POINT('Ctrl Pts',(2.92393480676644,2.8367874087171,0.403214543963986));
#24013=CARTESIAN_POINT('Ctrl Pts',(3.01246905677606,2.8828718115725,0.409396853104666));
#24014=CARTESIAN_POINT('Ctrl Pts',(3.10308063531525,2.92480037085041,0.415579162245345));
#24015=CARTESIAN_POINT('Ctrl Pts',(3.19357013044255,2.966672438655,0.42175314179498));
#24016=CARTESIAN_POINT('Ctrl Pts',(3.28613100122957,3.00439961290741,0.427927121344614));
#24017=CARTESIAN_POINT('Ctrl Pts',(3.38034775723902,3.03777556853218,0.434101100894248));
#24018=CARTESIAN_POINT('Ctrl Pts',(3.47446514659151,3.07111632386696,0.440268568993754));
#24019=CARTESIAN_POINT('Ctrl Pts',(3.57023454316161,3.10011484114296,0.44643603709326));
#24020=CARTESIAN_POINT('Ctrl Pts',(3.66721927955844,3.1246123397339,0.452603505192766));
#24021=CARTESIAN_POINT('Ctrl Pts',(3.76413288446316,3.14909187113027,0.458766449887613));
#24022=CARTESIAN_POINT('Ctrl Pts',(3.86225963847881,3.16907684231919,0.464929394582459));
#24023=CARTESIAN_POINT('Ctrl Pts',(3.96114733242027,3.18445818042905,0.471092339277305));
#24024=CARTESIAN_POINT('Ctrl Pts',(4.05999734800456,3.19983365791532,0.477252935756492));
#24025=CARTESIAN_POINT('Ctrl Pts',(4.15960730024591,3.21060892165472,0.48341353223568));
#24026=CARTESIAN_POINT('Ctrl Pts',(4.25951524489438,3.21672609014344,0.489574128714867));
#24027=CARTESIAN_POINT('Ctrl Pts',(4.35941159768095,3.22284254888507,0.495734010408219));
#24028=CARTESIAN_POINT('Ctrl Pts',(4.45960544222506,3.22430196059119,0.501893892101572));
#24029=CARTESIAN_POINT('Ctrl Pts',(4.55963116203887,3.2210984388464,0.508053773794924));
#24030=CARTESIAN_POINT('Ctrl Pts',(4.65967178229589,3.21789443988542,0.514214573101942));
#24031=CARTESIAN_POINT('Ctrl Pts',(4.75954379554351,3.21002614160735,0.520375372408959));
#24032=CARTESIAN_POINT('Ctrl Pts',(4.85878402884389,3.19753972071225,0.526536171715977));
#24033=CARTESIAN_POINT('Ctrl Pts',(4.95812767066414,3.18504028894183,0.532703390588088));
#24034=CARTESIAN_POINT('Ctrl Pts',(5.05683778779378,3.16791317936909,0.538870609460199));
#24035=CARTESIAN_POINT('Ctrl Pts',(5.15445887658851,3.14625616295914,0.54503782833231));
#24036=CARTESIAN_POINT('Ctrl Pts',(5.2521334743872,3.12458727569841,0.551208427639357));
#24037=CARTESIAN_POINT('Ctrl Pts',(5.34871743723497,3.09838364936585,0.557379026946404));
#24038=CARTESIAN_POINT('Ctrl Pts',(5.44376994753617,3.06779311741076,0.563549626253451));
#24039=CARTESIAN_POINT('Ctrl Pts',(5.53897697405659,3.0371528578543,0.569730256412626));
#24040=CARTESIAN_POINT('Ctrl Pts',(5.63264716982046,3.00211159976873,0.575910886571802));
#24041=CARTESIAN_POINT('Ctrl Pts',(5.72435912365468,2.96286558354997,0.582091516730978));
#24042=CARTESIAN_POINT('Ctrl Pts',(5.79091936345287,2.93438266347866,0.586577128565639));
#24043=CARTESIAN_POINT('Ctrl Pts',(5.85644859621518,2.90368603370804,0.5910627404003));
#24044=CARTESIAN_POINT('Ctrl Pts',(5.92079455746785,2.87086546799437,0.595548352234962));
#24045=CARTESIAN_POINT('Ctrl Pts',(6.00948985732504,2.82562517845972,0.601731377229428));
#24046=CARTESIAN_POINT('Ctrl Pts',(6.09623580561817,2.77619461905173,0.607914402223895));
#24047=CARTESIAN_POINT('Ctrl Pts',(6.18061096190255,2.72276558373602,0.614097427218362));
#24048=CARTESIAN_POINT('Ctrl Pts',(6.24884961276234,2.6795546974131,0.619097966505455));
#24049=CARTESIAN_POINT('Ctrl Pts',(6.31553778122664,2.63372945712145,0.62409850579255));
#24050=CARTESIAN_POINT('Ctrl Pts',(6.38046276496377,2.58541407971855,0.629099045079643));
#24051=CARTESIAN_POINT('Ctrl Pts',(5.88688308661327,2.88166464694226,-0.413294290592403));
#24052=CARTESIAN_POINT('Ctrl Pts',(6.84537358445575,2.40588471549031,-0.347122251455184));
#24053=CARTESIAN_POINT('Ctrl Pts',(8.23365752427788,0.430873938343679,-0.214778173180747));
#24054=CARTESIAN_POINT('Ctrl Pts',(6.86376121760315,-2.94715670275194,-0.0162620557690901));
#24055=CARTESIAN_POINT('Ctrl Pts',(3.28608690294124,-3.61718018023642,0.182254061642566));
#24056=CARTESIAN_POINT('Ctrl Pts',(0.781880406995935,-0.979166244321737,
0.380770179054222));
#24057=CARTESIAN_POINT('Ctrl Pts',(1.64193314359211,2.55787552455616,0.579286296465875));
#24058=CARTESIAN_POINT('Ctrl Pts',(5.07993189931123,3.75125370222575,0.777802413877532));
#24059=CARTESIAN_POINT('Ctrl Pts',(7.94674205925474,1.50993542852403,0.976318531289188));
#24060=CARTESIAN_POINT('Ctrl Pts',(7.61734820438694,-2.11448150974993,1.17483464870084));
#24061=CARTESIAN_POINT('Ctrl Pts',(4.39321803491158,-3.80232526959411,1.3733507661125));
#24062=CARTESIAN_POINT('Ctrl Pts',(1.22704502026327,-2.0081611280352,1.57186688352415));
#24063=CARTESIAN_POINT('Ctrl Pts',(1.01829993859556,1.62508529687376,1.77038300093581));
#24064=CARTESIAN_POINT('Ctrl Pts',(3.95817375267475,3.77008527062174,1.96889911834747));
#24065=CARTESIAN_POINT('Ctrl Pts',(7.35437229592725,2.462525507432,2.16741523575912));
#24066=CARTESIAN_POINT('Ctrl Pts',(8.09672865983581,-1.10017486129741,2.36593135317078));
#24067=CARTESIAN_POINT('Ctrl Pts',(5.50540329893836,-3.65535258567839,2.56444747058243));
#24068=CARTESIAN_POINT('Ctrl Pts',(1.95348461951634,-2.8630297341532,2.76296358799409));
#24069=CARTESIAN_POINT('Ctrl Pts',(0.693751175975549,0.551202220257554,
2.96147970540574));
#24070=CARTESIAN_POINT('Ctrl Pts',(2.87984341841113,3.46065318004877,3.1599958228174));
#24071=CARTESIAN_POINT('Ctrl Pts',(6.50977938134639,3.20090403962421,3.35851194022905));
#24072=CARTESIAN_POINT('Ctrl Pts',(8.25933290131072,0.00982773524565914,
3.55702805764071));
#24073=CARTESIAN_POINT('Ctrl Pts',(6.52629607038668,-3.19024855326339,3.75554417505237));
#24074=CARTESIAN_POINT('Ctrl Pts',(2.89775109124319,-3.46875593755042,3.95406029246402));
#24075=CARTESIAN_POINT('Ctrl Pts',(0.69665041333009,-0.570642598253718,
4.15257640987568));
#24076=CARTESIAN_POINT('Ctrl Pts',(1.93872017863753,2.85005436799852,4.35109252728733));
#24077=CARTESIAN_POINT('Ctrl Pts',(5.48649651727959,3.66072576290342,4.54960864469899));
#24078=CARTESIAN_POINT('Ctrl Pts',(8.09099334705098,1.11897413587954,4.74812476211065));
#24079=CARTESIAN_POINT('Ctrl Pts',(7.36706201253862,-2.44751271825679,4.9466408795223));
#24080=CARTESIAN_POINT('Ctrl Pts',(3.97766506003213,-3.7726139823619,5.14515699693396));
#24081=CARTESIAN_POINT('Ctrl Pts',(1.02674774506536,-1.64282712377203,5.34367311434561));
#24082=CARTESIAN_POINT('Ctrl Pts',(1.21670401249677,1.99142956468722,5.54218923175727));
#24083=CARTESIAN_POINT('Ctrl Pts',(4.37357552585394,3.80197293891488,5.74070534916892));
#24084=CARTESIAN_POINT('Ctrl Pts',(7.60635940332531,2.13074181682499,5.93922146658058));
#24085=CARTESIAN_POINT('Ctrl Pts',(7.95453366396254,-1.49178213007847,6.13773758399224));
#24086=CARTESIAN_POINT('Ctrl Pts',(5.09924694286633,-3.74816037897555,6.33625370140389));
#24087=CARTESIAN_POINT('Ctrl Pts',(1.65531650589596,-2.57204465036969,6.53476981881556));
#24088=CARTESIAN_POINT('Ctrl Pts',(0.776628336729841,0.959500643563771,
6.7332859362272));
#24089=CARTESIAN_POINT('Ctrl Pts',(3.26786834626679,3.6123534997611,6.93180205363886));
#24090=CARTESIAN_POINT('Ctrl Pts',(6.84760632218384,2.95708173512582,7.1303181710505));
#24091=CARTESIAN_POINT('Ctrl Pts',(8.23758631997216,-0.406229232878139,
7.32883428846218));
#24092=CARTESIAN_POINT('Ctrl Pts',(6.16489109788061,-3.39752319671194,7.52735040587382));
#24093=CARTESIAN_POINT('Ctrl Pts',(2.52765551345678,-3.27743004474078,7.72586652328549));
#24094=CARTESIAN_POINT('Ctrl Pts',(0.656790727359,-0.155928801126063,7.92438264069713));
#24095=CARTESIAN_POINT('Ctrl Pts',(2.26559912307384,3.10836907247963,8.1228987581088));
#24096=CARTESIAN_POINT('Ctrl Pts',(5.88076457458627,3.52608167695778,8.32141487552045));
#24097=CARTESIAN_POINT('Ctrl Pts',(8.19158732913988,0.714675754863574,8.5199309929321));
#24098=CARTESIAN_POINT('Ctrl Pts',(7.08185986462416,-2.75121662896035,8.71844711034376));
#24099=CARTESIAN_POINT('Ctrl Pts',(3.56784948378791,-3.69759715767183,8.91696322775543));
#24100=CARTESIAN_POINT('Ctrl Pts',(0.867620049835816,-1.2577885451434,9.11547934516706));
#24101=CARTESIAN_POINT('Ctrl Pts',(1.45399031457103,2.33387889135228,9.31399546257875));
#24102=CARTESIAN_POINT('Ctrl Pts',(4.78997354349419,3.78822443423146,9.51251157999037));
#24103=CARTESIAN_POINT('Ctrl Pts',(7.8205397526871,1.77338609991104,9.71102769740205));
#24104=CARTESIAN_POINT('Ctrl Pts',(7.77035405525285,-1.8654854913274,9.90954381481369));
#24105=CARTESIAN_POINT('Ctrl Pts',(4.68537555826851,-3.79598095490491,10.1080599322253));
#24106=CARTESIAN_POINT('Ctrl Pts',(1.39076888675897,-2.25018926719472,10.306576049637));
#24107=CARTESIAN_POINT('Ctrl Pts',(0.903672160428571,1.35628294827392,10.5050921670486));
#24108=CARTESIAN_POINT('Ctrl Pts',(3.67015929568852,3.72069703895061,10.7036082844603));
#24109=CARTESIAN_POINT('Ctrl Pts',(7.156733998233,2.67776755651859,10.902124401872));
#24110=CARTESIAN_POINT('Ctrl Pts',(8.17045747715504,-0.817410517633158,
11.1006405192836));
#24111=CARTESIAN_POINT('Ctrl Pts',(5.78298105352307,-3.56401958853324,11.2991566366953));
#24112=CARTESIAN_POINT('Ctrl Pts',(2.18071022148213,-3.04676731509573,11.4976727541069));
#24113=CARTESIAN_POINT('Ctrl Pts',(0.662536086558379,0.260656509846819,
11.6961888715186));
#24114=CARTESIAN_POINT('Ctrl Pts',(2.61877364278075,3.32937606128419,11.8947049889302));
#24115=CARTESIAN_POINT('Ctrl Pts',(6.25793774774488,3.34911634724554,12.0932211063419));
#24116=CARTESIAN_POINT('Ctrl Pts',(8.24735113836601,0.301799589347462,12.2917372237535));
#24117=CARTESIAN_POINT('Ctrl Pts',(6.76514687416864,-3.02189949163811,12.4902533411652));
#24118=CARTESIAN_POINT('Ctrl Pts',(3.16869942579002,-3.57820050080496,12.6887694585768));
#24119=CARTESIAN_POINT('Ctrl Pts',(0.751566954770839,-0.857653555925328,
12.8872855759885));
#24120=CARTESIAN_POINT('Ctrl Pts',(1.72731339933552,2.64831620117018,13.0858016934002));
#24121=CARTESIAN_POINT('Ctrl Pts',(5.20236872621718,3.72900835754984,13.2843178108118));
#24122=CARTESIAN_POINT('Ctrl Pts',(7.99434336961907,1.39474559334568,13.4828339282235));
#24123=CARTESIAN_POINT('Ctrl Pts',(7.54640006010282,-2.21679865437008,13.6813500456351));
#24124=CARTESIAN_POINT('Ctrl Pts',(4.26875675973819,-3.79824086239538,13.8798661630468));
#24125=CARTESIAN_POINT('Ctrl Pts',(1.16301685561255,-1.9013263388412,14.0783822804584));
#24126=CARTESIAN_POINT('Ctrl Pts',(1.07335787448695,1.73678667876183,14.2768983978701));
#24127=CARTESIAN_POINT('Ctrl Pts',(4.08188780578152,3.78438349314049,14.4754145152818));
#24128=CARTESIAN_POINT('Ctrl Pts',(7.43345216672421,2.36631389110821,14.6739306326934));
#24129=CARTESIAN_POINT('Ctrl Pts',(8.05875206907788,-1.21878096033793,14.8724467501051));
#24130=CARTESIAN_POINT('Ctrl Pts',(5.38514975673243,-3.68773939197872,15.0709628675167));
#24131=CARTESIAN_POINT('Ctrl Pts',(1.86107937002522,-2.77953623668677,15.2694789849284));
#24132=CARTESIAN_POINT('Ctrl Pts',(0.713817534175901,0.674113331777405,
15.46799510234));
#24133=CARTESIAN_POINT('Ctrl Pts',(2.9940048152212,3.5104227339951,15.6665112197517));
#24134=CARTESIAN_POINT('Ctrl Pts',(6.61348907494099,3.13195377174095,15.8650273371633));
#24135=CARTESIAN_POINT('Ctrl Pts',(8.257615478175,-0.114698878595687,16.063543454575));
#24136=CARTESIAN_POINT('Ctrl Pts',(6.42072433944188,-3.25631247771842,16.2620595719866));
#24137=CARTESIAN_POINT('Ctrl Pts',(2.78500562221897,-3.41585705137789,16.4605756893983));
#24138=CARTESIAN_POINT('Ctrl Pts',(0.67998136903583,-0.447224713876356,
16.65909180681));
#24139=CARTESIAN_POINT('Ctrl Pts',(2.03339274915041,2.93096750947701,16.8576079242216));
#24140=CARTESIAN_POINT('Ctrl Pts',(5.60581136526813,3.62503544056518,17.0561240416333));
#24141=CARTESIAN_POINT('Ctrl Pts',(8.12568420335589,0.999364870669326,17.2546401590449));
#24142=CARTESIAN_POINT('Ctrl Pts',(7.28535965135699,-2.54150503784963,17.4531562764566));
#24143=CARTESIAN_POINT('Ctrl Pts',(3.85439094932391,-3.75491297725849,17.6516723938682));
#24144=CARTESIAN_POINT('Ctrl Pts',(0.974793970633971,-1.52964303811135,
17.8501885112799));
#24145=CARTESIAN_POINT('Ctrl Pts',(1.2836488526281,2.09644489844015,18.0487046286916));
#24146=CARTESIAN_POINT('Ctrl Pts',(4.49811216942012,3.80264847561477,18.2472207461032));
#24147=CARTESIAN_POINT('Ctrl Pts',(7.67443956106538,2.02645891285741,18.4457368635149));
#24148=CARTESIAN_POINT('Ctrl Pts',(7.90381082245328,-1.60552317494378,18.6442529809265));
#24149=CARTESIAN_POINT('Ctrl Pts',(4.9761721155001,-3.76719767944954,18.8427690983382));
#24150=CARTESIAN_POINT('Ctrl Pts',(1.57259927845708,-2.47894420875808,19.0412852157498));
#24151=CARTESIAN_POINT('Ctrl Pts',(0.810019572635768,1.07947921368855,19.2398013331615));
#24152=CARTESIAN_POINT('Ctrl Pts',(3.38678898688482,3.6493361063157,19.4383174505731));
#24153=CARTESIAN_POINT('Ctrl Pts',(6.94315110686829,2.87720041011993,19.6368335679848));
#24154=CARTESIAN_POINT('Ctrl Pts',(8.22225715251285,-0.529820690755693,
19.8353496853965));
#24155=CARTESIAN_POINT('Ctrl Pts',(6.05272613795891,-3.45164208273989,20.0338658028081));
#24156=CARTESIAN_POINT('Ctrl Pts',(2.42137329831411,-3.212515309774,20.2323819202198));
#24157=CARTESIAN_POINT('Ctrl Pts',(0.65372248686789,-0.0314281299545405,
20.4308980376314));
#24158=CARTESIAN_POINT('Ctrl Pts',(2.36855469553213,3.178440343651,20.6294141550431));
#24159=CARTESIAN_POINT('Ctrl Pts',(5.99545920128352,3.47755359131801,20.8279302724548));
#24160=CARTESIAN_POINT('Ctrl Pts',(8.21298586010566,0.591989447683331,21.0264463898664));
#24161=CARTESIAN_POINT('Ctrl Pts',(6.99036591797756,-2.83570744333498,21.2249625072781));
#24162=CARTESIAN_POINT('Ctrl Pts',(3.44725150283742,-3.6665172604341,21.4234786246897));
#24163=CARTESIAN_POINT('Ctrl Pts',(0.828359319011244,-1.13960058009792,
21.6219947421014));
#24164=CARTESIAN_POINT('Ctrl Pts',(1.53202116508044,2.43094114262164,21.820510859513));
#24165=CARTESIAN_POINT('Ctrl Pts',(4.91383661347899,3.77527223251319,22.0190269769247));
#24166=CARTESIAN_POINT('Ctrl Pts',(7.87680396956558,1.66228269728872,22.2175430943363));
#24167=CARTESIAN_POINT('Ctrl Pts',(7.7074930081086,-1.97299730385434,22.416059211748));
#24168=CARTESIAN_POINT('Ctrl Pts',(4.56095756308617,-3.80143701374933,22.6145753291597));
#24169=CARTESIAN_POINT('Ctrl Pts',(1.31873095853907,-2.14860623751896,22.8130914465713));
#24170=CARTESIAN_POINT('Ctrl Pts',(0.949990286798536,1.47190262315773,23.011607563983));
#24171=CARTESIAN_POINT('Ctrl Pts',(3.7924065803434,3.74442240079083,23.2101236813946));
#24172=CARTESIAN_POINT('Ctrl Pts',(7.24297719250067,2.58796472414074,23.4086397988063));
#24173=CARTESIAN_POINT('Ctrl Pts',(8.14168123233833,-0.938680920498277,
23.6071559162179));
#24174=CARTESIAN_POINT('Ctrl Pts',(5.66560616055497,-3.60535681683013,23.8056720336296));
#24175=CARTESIAN_POINT('Ctrl Pts',(2.08209581503262,-2.97097481614092,24.0041881510412));
#24176=CARTESIAN_POINT('Ctrl Pts',(0.673241827254791,0.385434817028999,
24.2027042684529));
#24177=CARTESIAN_POINT('Ctrl Pts',(2.72851506381635,3.38643791990783,24.4012203858645));
#24178=CARTESIAN_POINT('Ctrl Pts',(6.36713580394013,3.29091791303403,24.5997365032762));
#24179=CARTESIAN_POINT('Ctrl Pts',(8.25465969525897,0.17151120336101,24.7982954766299));
#24180=CARTESIAN_POINT('Ctrl Pts',(7.19525837483205,-1.99900958588141,24.9306824108463));
#24181=CARTESIAN_POINT('Ctrl Pts',(6.32311239899223,-2.62025147071356,24.9968973059255));
#24182=CARTESIAN_POINT('Ctrl Pts',(5.99341579333084,3.0962819108244,-0.27495920519366));
#24183=CARTESIAN_POINT('Ctrl Pts',(7.02329163031133,2.58506739568259,-0.208787166056442));
#24184=CARTESIAN_POINT('Ctrl Pts',(8.51497056474962,0.462964065771816,-0.0764430877820045));
#24185=CARTESIAN_POINT('Ctrl Pts',(7.04304871618797,-3.16665160770128,0.122073029629653));
#24186=CARTESIAN_POINT('Ctrl Pts',(3.19892054011338,-3.88657631350085,0.320589147041309));
#24187=CARTESIAN_POINT('Ctrl Pts',(0.508208668906595,-1.05209144762919,
0.519105264452963));
#24188=CARTESIAN_POINT('Ctrl Pts',(1.43231541168923,2.74837799923302,0.717621381864618));
#24189=CARTESIAN_POINT('Ctrl Pts',(5.12636543519397,4.03063520713254,0.916137499276276));
#24190=CARTESIAN_POINT('Ctrl Pts',(8.20668654383497,1.62239064105283,1.11465361668793));
#24191=CARTESIAN_POINT('Ctrl Pts',(7.85276047702285,-2.27196140132349,1.31316973409959));
#24192=CARTESIAN_POINT('Ctrl Pts',(4.38850729527858,-4.08551042322263,1.51168585151124));
#24193=CARTESIAN_POINT('Ctrl Pts',(0.986527733847538,-2.15772261402933,
1.7102019689229));
#24194=CARTESIAN_POINT('Ctrl Pts',(0.7622359790706,1.74611650720567,1.90871808633455));
#24195=CARTESIAN_POINT('Ctrl Pts',(3.92106229159746,4.0508692911502,2.10723420374621));
#24196=CARTESIAN_POINT('Ctrl Pts',(7.57019895508782,2.64592661456843,2.30575032115786));
#24197=CARTESIAN_POINT('Ctrl Pts',(8.36784367179503,-1.18211240346562,2.50426643856952));
#24198=CARTESIAN_POINT('Ctrl Pts',(5.58352459826198,-3.92759167890361,2.70278255598118));
#24199=CARTESIAN_POINT('Ctrl Pts',(1.7670702556363,-3.07625912870098,2.90129867339283));
#24200=CARTESIAN_POINT('Ctrl Pts',(0.413515851644582,0.592254017343965,
3.09981479080449));
#24201=CARTESIAN_POINT('Ctrl Pts',(2.76242132641212,3.7183916776686,3.29833090821614));
#24202=CARTESIAN_POINT('Ctrl Pts',(6.66270343294158,3.43929724324088,3.4968470256278));
#24203=CARTESIAN_POINT('Ctrl Pts',(8.54255816261418,0.0105596738669375,
3.69536314303945));
#24204=CARTESIAN_POINT('Ctrl Pts',(6.6804502327146,-3.42784816997514,3.89387926045112));
#24205=CARTESIAN_POINT('Ctrl Pts',(2.78166270604797,-3.72709790290783,4.09239537786277));
#24206=CARTESIAN_POINT('Ctrl Pts',(0.416631015022661,-0.613142253174304,
4.29091149527442));
#24207=CARTESIAN_POINT('Ctrl Pts',(1.75120620592284,3.06231739833558,4.48942761268608));
#24208=CARTESIAN_POINT('Ctrl Pts',(5.56320969933569,3.93336503336498,4.68794373009773));
#24209=CARTESIAN_POINT('Ctrl Pts',(8.36168121106336,1.20231178852842,4.88645984750939));
#24210=CARTESIAN_POINT('Ctrl Pts',(7.58383376163584,-2.62979572036334,5.08497596492104));
#24211=CARTESIAN_POINT('Ctrl Pts',(3.94200524984668,-4.05358633333867,5.2834920823327));
#24212=CARTESIAN_POINT('Ctrl Pts',(0.771312951433223,-1.76517968922739,
5.48200819974436));
#24213=CARTESIAN_POINT('Ctrl Pts',(0.97541656054666,2.13974493679014,5.68052431715601));
#24214=CARTESIAN_POINT('Ctrl Pts',(4.36740187430494,4.08513185206935,5.87904043456767));
#24215=CARTESIAN_POINT('Ctrl Pts',(7.84095326483218,2.28943272461384,6.07755655197932));
#24216=CARTESIAN_POINT('Ctrl Pts',(8.21505844260491,-1.60288534238506,6.27607266939098));
#24217=CARTESIAN_POINT('Ctrl Pts',(5.14711900207072,-4.02731150295548,6.47458878680263));
#24218=CARTESIAN_POINT('Ctrl Pts',(1.44669552446588,-2.76360239669899,6.6731049042143));
#24219=CARTESIAN_POINT('Ctrl Pts',(0.502565441067234,1.03096121515846,6.87162102162594));
#24220=CARTESIAN_POINT('Ctrl Pts',(3.17934512299035,3.88139015713774,7.07013713903761));
#24221=CARTESIAN_POINT('Ctrl Pts',(7.0256906552799,3.17731582507866,7.26865325644925));
#24222=CARTESIAN_POINT('Ctrl Pts',(8.51919196471455,-0.436483900631263,
7.46716937386092));
#24223=CARTESIAN_POINT('Ctrl Pts',(6.2921289615216,-3.65055997294754,7.66568549127257));
#24224=CARTESIAN_POINT('Ctrl Pts',(2.38400358079477,-3.52152266305215,7.86420160868423));
#24225=CARTESIAN_POINT('Ctrl Pts',(0.373802705776339,-0.16754188479758,
8.06271772609589));
#24226=CARTESIAN_POINT('Ctrl Pts',(2.10243005973299,3.33987056457006,8.26123384350753));
#24227=CARTESIAN_POINT('Ctrl Pts',(5.98684159389007,3.78869308197905,8.4597499609192));
#24228=CARTESIAN_POINT('Ctrl Pts',(8.4697671146088,0.767902543495819,8.65826607833084));
#24229=CARTESIAN_POINT('Ctrl Pts',(7.27739066026635,-2.95611853726567,8.85678219574251));
#24230=CARTESIAN_POINT('Ctrl Pts',(3.50166790634439,-3.97298249293629,9.05529831315416));
#24231=CARTESIAN_POINT('Ctrl Pts',(0.600333929022254,-1.35146465571633,
9.25381443056581));
#24232=CARTESIAN_POINT('Ctrl Pts',(1.23037519550738,2.50769880562501,9.45233054797748));
#24233=CARTESIAN_POINT('Ctrl Pts',(4.81481189860833,4.07035940226423,9.65084666538912));
#24234=CARTESIAN_POINT('Ctrl Pts',(8.07108508884113,1.90546228475562,9.84936278280079));
#24235=CARTESIAN_POINT('Ctrl Pts',(8.01716171947454,-2.00442094739626,10.0478789002124));
#24236=CARTESIAN_POINT('Ctrl Pts',(4.70242378644322,-4.07869360405195,10.2463950176241));
#24237=CARTESIAN_POINT('Ctrl Pts',(1.16244523581599,-2.41777624309588,10.4449111350357));
#24238=CARTESIAN_POINT('Ctrl Pts',(0.639071086725107,1.45729461030662,10.6434272524474));
#24239=CARTESIAN_POINT('Ctrl Pts',(3.61159742927608,3.99780278027315,10.841943369859));
#24240=CARTESIAN_POINT('Ctrl Pts',(7.35784118240728,2.87719921033794,11.0404594872707));
#24241=CARTESIAN_POINT('Ctrl Pts',(8.44706357811351,-0.878288666292467,
11.2389756046823));
#24242=CARTESIAN_POINT('Ctrl Pts',(5.88177546561389,-3.82945648915419,11.437491722094));
#24243=CARTESIAN_POINT('Ctrl Pts',(2.01121890138154,-3.27368090323489,11.6360078395057));
#24244=CARTESIAN_POINT('Ctrl Pts',(0.379975961147697,0.280069381853164,
11.8345239569173));
#24245=CARTESIAN_POINT('Ctrl Pts',(2.4819079000476,3.57733745452462,12.033040074329));
#24246=CARTESIAN_POINT('Ctrl Pts',(6.39210543142176,3.59854793451629,12.2315561917406));
#24247=CARTESIAN_POINT('Ctrl Pts',(8.52968403588164,0.324276667717884,12.4300723091523));
#24248=CARTESIAN_POINT('Ctrl Pts',(6.93708988851933,-3.24696100298028,12.6285884265639));
#24249=CARTESIAN_POINT('Ctrl Pts',(3.07279041513639,-3.84469355089646,12.8271045439756));
#24250=CARTESIAN_POINT('Ctrl Pts',(0.475637566686629,-0.921528878727684,
13.0256206613872));
#24251=CARTESIAN_POINT('Ctrl Pts',(1.52405451869475,2.84555441124189,13.2241367787989));
#24252=CARTESIAN_POINT('Ctrl Pts',(5.25792096951678,4.00673309958052,13.4226528962106));
#24253=CARTESIAN_POINT('Ctrl Pts',(8.257833049161,1.4986218314684,13.6211690136222));
#24254=CARTESIAN_POINT('Ctrl Pts',(7.77652833946771,-2.38189880309254,13.8196851310339));
#24255=CARTESIAN_POINT('Ctrl Pts',(4.25477653818775,-4.08112182230083,14.0182012484455));
#24256=CARTESIAN_POINT('Ctrl Pts',(0.917730954110628,-2.04293110781465,
14.2167173658572));
#24257=CARTESIAN_POINT('Ctrl Pts',(0.821394455796449,1.86613705453794,14.4152334832688));
#24258=CARTESIAN_POINT('Ctrl Pts',(4.05399017588675,4.06623240003544,14.6137496006805));
#24259=CARTESIAN_POINT('Ctrl Pts',(7.65516844441363,2.54254946152231,14.8122657180922));
#24260=CARTESIAN_POINT('Ctrl Pts',(8.32703870473431,-1.30955190943392,15.0107818355038));
#24261=CARTESIAN_POINT('Ctrl Pts',(5.45431495277465,-3.96239055204922,15.2092979529155));
#24262=CARTESIAN_POINT('Ctrl Pts',(1.66778295557931,-2.98654729975826,15.4078140703271));
#24263=CARTESIAN_POINT('Ctrl Pts',(0.435076688703739,0.724319159497842,
15.6063301877388));
#24264=CARTESIAN_POINT('Ctrl Pts',(2.88508510279309,3.77186791049719,15.8048463051504));
#24265=CARTESIAN_POINT('Ctrl Pts',(6.77413709632598,3.36521177759866,16.0033624225621));
#24266=CARTESIAN_POINT('Ctrl Pts',(8.54071283123811,-0.123241288109086,
16.2018785399737));
#24267=CARTESIAN_POINT('Ctrl Pts',(6.56701585333057,-3.49883232646441,16.4003946573854));
#24268=CARTESIAN_POINT('Ctrl Pts',(2.66052031127365,-3.67025927509159,16.598910774797));
#24269=CARTESIAN_POINT('Ctrl Pts',(0.398720513058523,-0.480532595324168,
16.7974268922087));
#24270=CARTESIAN_POINT('Ctrl Pts',(1.85292968989636,3.14925669454191,16.9959430096203));
#24271=CARTESIAN_POINT('Ctrl Pts',(5.69141073963082,3.89501660876095,17.194459127032));
#24272=CARTESIAN_POINT('Ctrl Pts',(8.39895573256671,1.07379440374864,17.3929752444437));
#24273=CARTESIAN_POINT('Ctrl Pts',(7.49604646714037,-2.73078829048094,17.5914913618553));
#24274=CARTESIAN_POINT('Ctrl Pts',(3.80955007347359,-4.03456701338995,17.790007479267));
#24275=CARTESIAN_POINT('Ctrl Pts',(0.715489824289806,-1.64356601103751,
17.9885235966786));
#24276=CARTESIAN_POINT('Ctrl Pts',(1.04734724052415,2.25258148028018,18.1870397140903));
#24277=CARTESIAN_POINT('Ctrl Pts',(4.50121361298798,4.08585770060491,18.3855558315019));
#24278=CARTESIAN_POINT('Ctrl Pts',(7.91410381728119,2.1773831599618,18.5840719489136));
#24279=CARTESIAN_POINT('Ctrl Pts',(8.16055792437237,-1.72509746033864,18.7825880663253));
#24280=CARTESIAN_POINT('Ctrl Pts',(5.0148779510323,-4.04776664132528,18.9811041837369));
#24281=CARTESIAN_POINT('Ctrl Pts',(1.35781777968586,-2.66356812881232,19.1796203011486));
#24282=CARTESIAN_POINT('Ctrl Pts',(0.538443550556935,1.1598754095142,19.3781364185603));
#24283=CARTESIAN_POINT('Ctrl Pts',(3.30712259659747,3.92112711119714,19.5766525359719));
#24284=CARTESIAN_POINT('Ctrl Pts',(7.12835131317638,3.09148519177063,19.7751686533836));
#24285=CARTESIAN_POINT('Ctrl Pts',(8.50272112937199,-0.569280059186615,
19.9736847707952));
#24286=CARTESIAN_POINT('Ctrl Pts',(6.17161031033075,-3.70870946234774,20.1722008882069));
#24287=CARTESIAN_POINT('Ctrl Pts',(2.26980580259814,-3.45177328404759,20.3707170056185));
#24288=CARTESIAN_POINT('Ctrl Pts',(0.370505952442893,-0.0337687976193256,
20.5692331230302));
#24289=CARTESIAN_POINT('Ctrl Pts',(2.21305343742525,3.41516052227788,20.7677492404418));
#24290=CARTESIAN_POINT('Ctrl Pts',(6.11007831343283,3.73655077808788,20.9662653578534));
#24291=CARTESIAN_POINT('Ctrl Pts',(8.49275934044528,0.636078948397367,21.1647814752652));
#24292=CARTESIAN_POINT('Ctrl Pts',(7.17908253400595,-3.04690196012391,21.3632975926768));
#24293=CARTESIAN_POINT('Ctrl Pts',(3.37208816940477,-3.93958786330456,21.5618137100885));
#24294=CARTESIAN_POINT('Ctrl Pts',(0.558149183206385,-1.22447442503984,
21.7603298275001));
#24295=CARTESIAN_POINT('Ctrl Pts',(1.31421753683424,2.61198994621562,21.9588459449118));
#24296=CARTESIAN_POINT('Ctrl Pts',(4.94789989808116,4.05644256154919,22.1573620623234));
#24297=CARTESIAN_POINT('Ctrl Pts',(8.13153968654471,1.78608425229248,22.3558781797351));
#24298=CARTESIAN_POINT('Ctrl Pts',(7.94961898046267,-2.11993989949929,22.5543942971467));
#24299=CARTESIAN_POINT('Ctrl Pts',(4.56873953270021,-4.0845560128934,22.7529104145584));
#24300=CARTESIAN_POINT('Ctrl Pts',(1.08504215066615,-2.30862763082918,22.95142653197));
#24301=CARTESIAN_POINT('Ctrl Pts',(0.688838840573486,1.58152527269752,23.1499426493817));
#24302=CARTESIAN_POINT('Ctrl Pts',(3.74294930484078,4.02329513198439,23.3484587667933));
#24303=CARTESIAN_POINT('Ctrl Pts',(7.45050749686758,2.78070814718547,23.546974884205));
#24304=CARTESIAN_POINT('Ctrl Pts',(8.41614416964521,-1.00859090500303,23.7454910016166));
#24305=CARTESIAN_POINT('Ctrl Pts',(5.75565886205016,-3.87387238340306,23.9440071190283));
#24306=CARTESIAN_POINT('Ctrl Pts',(1.90526000600476,-3.19224361880315,24.14252323644));
#24307=CARTESIAN_POINT('Ctrl Pts',(0.391479031532891,0.414140782493564,
24.3410393538516));
#24308=CARTESIAN_POINT('Ctrl Pts',(2.59982251484541,3.6386490998064,24.5395554712633));
#24309=CARTESIAN_POINT('Ctrl Pts',(6.50943621328541,3.53601506509354,24.7380715886749));
#24310=CARTESIAN_POINT('Ctrl Pts',(8.53753691096405,0.184284815040506,24.9366305620286));
#24311=CARTESIAN_POINT('Ctrl Pts',(7.39923473266516,-2.14788949397592,25.069017496245));
#24312=CARTESIAN_POINT('Ctrl Pts',(6.46213408444902,-2.81539950847165,25.1352323913243));
#24313=CARTESIAN_POINT('Ctrl Pts',(6.0999485000484,3.31089917470656,-0.136624119794918));
#24314=CARTESIAN_POINT('Ctrl Pts',(7.2012096761669,2.76425007587486,-0.0704520806576993));
#24315=CARTESIAN_POINT('Ctrl Pts',(8.79628360522135,0.495054193199949,0.061891997616738));
#24316=CARTESIAN_POINT('Ctrl Pts',(7.22233621477278,-3.38614651265062,0.260408115028396));
#24317=CARTESIAN_POINT('Ctrl Pts',(3.11175417728552,-4.15597244676529,0.458924232440051));
#24318=CARTESIAN_POINT('Ctrl Pts',(0.234536930817258,-1.12501665093665,
0.657440349851707));
#24319=CARTESIAN_POINT('Ctrl Pts',(1.22269767978634,2.93888047390986,0.855956467263361));
#24320=CARTESIAN_POINT('Ctrl Pts',(5.17279897107673,4.31001671203934,1.05447258467502));
#24321=CARTESIAN_POINT('Ctrl Pts',(8.46663102841521,1.73484585358162,1.25298870208667));
#24322=CARTESIAN_POINT('Ctrl Pts',(8.08817274965877,-2.42944129289705,1.45150481949833));
#24323=CARTESIAN_POINT('Ctrl Pts',(4.38379655564558,-4.36869557685114,1.65002093690999));
#24324=CARTESIAN_POINT('Ctrl Pts',(0.746010447431816,-2.30728410002347,
1.84853705432164));
#24325=CARTESIAN_POINT('Ctrl Pts',(0.506172019545635,1.86714771753756,2.04705317173329));
#24326=CARTESIAN_POINT('Ctrl Pts',(3.88395083052018,4.33165331167866,2.24556928914495));
#24327=CARTESIAN_POINT('Ctrl Pts',(7.78602561424836,2.82932772170484,2.4440854065566));
#24328=CARTESIAN_POINT('Ctrl Pts',(8.63895868375428,-1.26404994563383,2.64260152396827));
#24329=CARTESIAN_POINT('Ctrl Pts',(5.66164589758561,-4.19983077212884,2.84111764137992));
#24330=CARTESIAN_POINT('Ctrl Pts',(1.58065589175627,-3.28948852324876,3.03963375879158));
#24331=CARTESIAN_POINT('Ctrl Pts',(0.133280527313607,0.633305814430374,
3.23814987620323));
#24332=CARTESIAN_POINT('Ctrl Pts',(2.6449992344131,3.97613017528841,3.43666599361489));
#24333=CARTESIAN_POINT('Ctrl Pts',(6.81562748453676,3.67769044685756,3.63518211102655));
#24334=CARTESIAN_POINT('Ctrl Pts',(8.82578342391765,0.0112916124882134,
3.8336982284382));
#24335=CARTESIAN_POINT('Ctrl Pts',(6.83460439504253,-3.66544778668689,4.03221434584986));
#24336=CARTESIAN_POINT('Ctrl Pts',(2.66557432085276,-3.98543986826524,4.23073046326151));
#24337=CARTESIAN_POINT('Ctrl Pts',(0.13661161671523,-0.655641908094887,
4.42924658067317));
#24338=CARTESIAN_POINT('Ctrl Pts',(1.56369223320815,3.27458042867263,4.62776269808482));
#24339=CARTESIAN_POINT('Ctrl Pts',(5.63992288139177,4.20600430382654,4.82627881549648));
#24340=CARTESIAN_POINT('Ctrl Pts',(8.63236907507575,1.28564944117731,5.02479493290813));
#24341=CARTESIAN_POINT('Ctrl Pts',(7.80060551073305,-2.81207872246989,5.22331105031979));
#24342=CARTESIAN_POINT('Ctrl Pts',(3.90634543966123,-4.33455868431544,5.42182716773146));
#24343=CARTESIAN_POINT('Ctrl Pts',(0.515878157801087,-1.88753225468275,
5.62034328514309));
#24344=CARTESIAN_POINT('Ctrl Pts',(0.734129108596551,2.28806030889307,5.81885940255477));
#24345=CARTESIAN_POINT('Ctrl Pts',(4.36122822275595,4.36829076522382,6.0173755199664));
#24346=CARTESIAN_POINT('Ctrl Pts',(8.07554712633902,2.44812363240269,6.21589163737808));
#24347=CARTESIAN_POINT('Ctrl Pts',(8.47558322124728,-1.71398855469165,6.41440775478972));
#24348=CARTESIAN_POINT('Ctrl Pts',(5.19499106127511,-4.3064626269354,6.61292387220138));
#24349=CARTESIAN_POINT('Ctrl Pts',(1.2380745430358,-2.9551601430283,6.81143998961304));
#24350=CARTESIAN_POINT('Ctrl Pts',(0.228502545404632,1.10242178675316,7.00995610702469));
#24351=CARTESIAN_POINT('Ctrl Pts',(3.09082189971391,4.15042681451437,7.20847222443635));
#24352=CARTESIAN_POINT('Ctrl Pts',(7.20377498837598,3.39754991503151,7.406988341848));
#24353=CARTESIAN_POINT('Ctrl Pts',(8.80079760945692,-0.466738568384383,
7.60550445925966));
#24354=CARTESIAN_POINT('Ctrl Pts',(6.41936682516261,-3.90359674918315,7.80402057667131));
#24355=CARTESIAN_POINT('Ctrl Pts',(2.24035164813274,-3.7656152813635,8.00253669408298));
#24356=CARTESIAN_POINT('Ctrl Pts',(0.0908146841936848,-0.179154968469096,
8.20105281149462));
#24357=CARTESIAN_POINT('Ctrl Pts',(1.93926099639212,3.57137205666049,8.39956892890629));
#24358=CARTESIAN_POINT('Ctrl Pts',(6.09291861319388,4.05130448700034,8.59808504631793));
#24359=CARTESIAN_POINT('Ctrl Pts',(8.7479469000777,0.821129332128062,8.7966011637296));
#24360=CARTESIAN_POINT('Ctrl Pts',(7.47292145590854,-3.16102044557099,8.99511728114126));
#24361=CARTESIAN_POINT('Ctrl Pts',(3.43548632890085,-4.24836782820074,9.19363339855291));
#24362=CARTESIAN_POINT('Ctrl Pts',(0.333047808208697,-1.44514076628925,
9.39214951596456));
#24363=CARTESIAN_POINT('Ctrl Pts',(1.00676007644372,2.68151871989772,9.59066563337622));
#24364=CARTESIAN_POINT('Ctrl Pts',(4.83965025372247,4.352494370297,9.78918175078787));
#24365=CARTESIAN_POINT('Ctrl Pts',(8.32163042499515,2.03753846960017,9.98769786819953));
#24366=CARTESIAN_POINT('Ctrl Pts',(8.26396938369623,-2.14335640346512,10.1862139856111));
#24367=CARTESIAN_POINT('Ctrl Pts',(4.71947201461794,-4.36140625319899,10.3847301030228));
#24368=CARTESIAN_POINT('Ctrl Pts',(0.934121584873003,-2.58536321899705,
10.5832462204345));
#24369=CARTESIAN_POINT('Ctrl Pts',(0.37447001302165,1.5583062723393,10.7817623378461));
#24370=CARTESIAN_POINT('Ctrl Pts',(3.55303556286365,4.27490852159572,10.9802784552578));
#24371=CARTESIAN_POINT('Ctrl Pts',(7.55894836658157,3.07663086415728,11.1787945726694));
#24372=CARTESIAN_POINT('Ctrl Pts',(8.72366967907197,-0.939166814951776,
11.3773106900811));
#24373=CARTESIAN_POINT('Ctrl Pts',(5.98056987770475,-4.09489338977514,11.5758268074927));
#24374=CARTESIAN_POINT('Ctrl Pts',(1.84172758128094,-3.50059449137405,11.7743429249044));
#24375=CARTESIAN_POINT('Ctrl Pts',(0.0974158357370281,0.299482253859507,
11.9728590423161));
#24376=CARTESIAN_POINT('Ctrl Pts',(2.34504215731444,3.82529884776504,12.1713751597277));
#24377=CARTESIAN_POINT('Ctrl Pts',(6.52627311509865,3.84797952178704,12.3698912771394));
#24378=CARTESIAN_POINT('Ctrl Pts',(8.81201693339725,0.346753746088307,12.568407394551));
#24379=CARTESIAN_POINT('Ctrl Pts',(7.10903290287004,-3.47202251432246,12.7669235119627));
#24380=CARTESIAN_POINT('Ctrl Pts',(2.97688140448274,-4.11118660098796,12.9654396293744));
#24381=CARTESIAN_POINT('Ctrl Pts',(0.199708178602426,-0.985404201530036,
13.163955746786));
#24382=CARTESIAN_POINT('Ctrl Pts',(1.32079563805398,3.0427926213136,13.3624718641977));
#24383=CARTESIAN_POINT('Ctrl Pts',(5.3134732128164,4.28445784161121,13.5609879816093));
#24384=CARTESIAN_POINT('Ctrl Pts',(8.52132272870291,1.60249806959112,13.759504099021));
#24385=CARTESIAN_POINT('Ctrl Pts',(8.00665661883263,-2.546998951815,13.9580202164326));
#24386=CARTESIAN_POINT('Ctrl Pts',(4.24079631663729,-4.36400278220629,14.1565363338443));
#24387=CARTESIAN_POINT('Ctrl Pts',(0.672445052608722,-2.18453587678811,
14.3550524512559));
#24388=CARTESIAN_POINT('Ctrl Pts',(0.569431037105937,1.99548743031406,14.5535685686676));
#24389=CARTESIAN_POINT('Ctrl Pts',(4.02609254599198,4.3480813069304,14.7520846860792));
#24390=CARTESIAN_POINT('Ctrl Pts',(7.87688472210303,2.7187850319364,14.9506008034909));
#24391=CARTESIAN_POINT('Ctrl Pts',(8.59532534039074,-1.40032285852991,15.1491169209026));
#24392=CARTESIAN_POINT('Ctrl Pts',(5.52348014881688,-4.2370417121197,15.3476330383142));
#24393=CARTESIAN_POINT('Ctrl Pts',(1.47448654113341,-3.19355836282975,15.5461491557259));
#24394=CARTESIAN_POINT('Ctrl Pts',(0.156335843231577,0.774524987218279,
15.7446652731375));
#24395=CARTESIAN_POINT('Ctrl Pts',(2.77616539036498,4.03331308699926,15.9431813905492));
#24396=CARTESIAN_POINT('Ctrl Pts',(6.93478511771097,3.59846978345639,16.1416975079608));
#24397=CARTESIAN_POINT('Ctrl Pts',(8.82381018430121,-0.131783697622486,
16.3402136253725));
#24398=CARTESIAN_POINT('Ctrl Pts',(6.71330736721926,-3.74135217521042,16.5387297427841));
#24399=CARTESIAN_POINT('Ctrl Pts',(2.53603500032833,-3.92466149880528,16.7372458601958));
#24400=CARTESIAN_POINT('Ctrl Pts',(0.117459657081213,-0.513840476771981,
16.9357619776075));
#24401=CARTESIAN_POINT('Ctrl Pts',(1.6724666306423,3.3675458796068,17.1342780950191));
#24402=CARTESIAN_POINT('Ctrl Pts',(5.77701011399349,4.16499777695671,17.3327942124308));
#24403=CARTESIAN_POINT('Ctrl Pts',(8.67222726177754,1.14822393682795,17.5313103298424));
#24404=CARTESIAN_POINT('Ctrl Pts',(7.70673328292373,-2.92007154311226,17.7298264472541));
#24405=CARTESIAN_POINT('Ctrl Pts',(3.76470919762329,-4.31422104952143,17.9283425646657));
#24406=CARTESIAN_POINT('Ctrl Pts',(0.456185677945633,-1.75748898396369,
18.1268586820774));
#24407=CARTESIAN_POINT('Ctrl Pts',(0.811045628420214,2.40871806212022,18.3253747994891));
#24408=CARTESIAN_POINT('Ctrl Pts',(4.50431505655582,4.36906692559506,18.5238909169007));
#24409=CARTESIAN_POINT('Ctrl Pts',(8.153768073497,2.32830740706619,18.7224070343124));
#24410=CARTESIAN_POINT('Ctrl Pts',(8.41730502629147,-1.84467174573349,18.920923151724));
#24411=CARTESIAN_POINT('Ctrl Pts',(5.05358378656449,-4.328335603201,19.1194392691357));
#24412=CARTESIAN_POINT('Ctrl Pts',(1.14303628091464,-2.84819204886657,19.3179553865473));
#24413=CARTESIAN_POINT('Ctrl Pts',(0.266867528478102,1.24027160533984,19.516471503959));
#24414=CARTESIAN_POINT('Ctrl Pts',(3.22745620631011,4.19291811607857,19.7149876213706));
#24415=CARTESIAN_POINT('Ctrl Pts',(7.31355151948446,3.30576997342133,19.9135037387823));
#24416=CARTESIAN_POINT('Ctrl Pts',(8.78318510623113,-0.60873942761753,20.112019856194));
#24417=CARTESIAN_POINT('Ctrl Pts',(6.29049448270258,-3.96577684195559,20.3105359736056));
#24418=CARTESIAN_POINT('Ctrl Pts',(2.11823830688215,-3.69103125832118,20.5090520910173));
#24419=CARTESIAN_POINT('Ctrl Pts',(0.0872894180178925,-0.0361094652841183,
20.7075682084289));
#24420=CARTESIAN_POINT('Ctrl Pts',(2.05755217931839,3.65188070090475,20.9060843258406));
#24421=CARTESIAN_POINT('Ctrl Pts',(6.2246974255821,3.99554796485774,21.1046004432522));
#24422=CARTESIAN_POINT('Ctrl Pts',(8.77253282078492,0.680168449111409,21.3031165606639));
#24423=CARTESIAN_POINT('Ctrl Pts',(7.36779915003431,-3.25809647691284,21.5016326780756));
#24424=CARTESIAN_POINT('Ctrl Pts',(3.29692483597213,-4.21265846617502,21.7001487954872));
#24425=CARTESIAN_POINT('Ctrl Pts',(0.287939047401517,-1.30934826998177,
21.8986649128989));
#24426=CARTESIAN_POINT('Ctrl Pts',(1.09641390858805,2.79303874980958,22.0971810303105));
#24427=CARTESIAN_POINT('Ctrl Pts',(4.98196318268333,4.33761289058522,22.2956971477222));
#24428=CARTESIAN_POINT('Ctrl Pts',(8.38627540352384,1.90988580729624,22.4942132651338));
#24429=CARTESIAN_POINT('Ctrl Pts',(8.19174495281671,-2.26688249514424,22.6927293825455));
#24430=CARTESIAN_POINT('Ctrl Pts',(4.57652150231426,-4.36767501203749,22.8912454999571));
#24431=CARTESIAN_POINT('Ctrl Pts',(0.851353342793238,-2.46864902413938,
23.0897616173688));
#24432=CARTESIAN_POINT('Ctrl Pts',(0.42768739434844,1.69114792223732,23.2882777347804));
#24433=CARTESIAN_POINT('Ctrl Pts',(3.69349202933814,4.30216786317793,23.4867938521921));
#24434=CARTESIAN_POINT('Ctrl Pts',(7.65803780123451,2.9734515702302,23.6853099696038));
#24435=CARTESIAN_POINT('Ctrl Pts',(8.6906071069521,-1.07850088950778,23.8838260870154));
#24436=CARTESIAN_POINT('Ctrl Pts',(5.84571156354535,-4.14238794997599,24.0823422044271));
#24437=CARTESIAN_POINT('Ctrl Pts',(1.7284241969769,-3.41351242146536,24.2808583218387));
#24438=CARTESIAN_POINT('Ctrl Pts',(0.109716235810993,0.442846747958131,
24.4793744392504));
#24439=CARTESIAN_POINT('Ctrl Pts',(2.47112996587446,3.89086027970496,24.677890556662));
#24440=CARTESIAN_POINT('Ctrl Pts',(6.6517366226307,3.78111221715306,24.8764066740737));
#24441=CARTESIAN_POINT('Ctrl Pts',(8.82041412666913,0.197058426719993,25.0749656474274));
#24442=CARTESIAN_POINT('Ctrl Pts',(7.60321109049825,-2.29676940207044,25.2073525816438));
#24443=CARTESIAN_POINT('Ctrl Pts',(6.60115576990582,-3.01054754622974,25.273567476723));
#24444=CARTESIAN_POINT('Ctrl Pts',(6.20648120676596,3.5255164385887,0.00171096560382468));
#24445=CARTESIAN_POINT('Ctrl Pts',(7.37912772202248,2.94343275606714,0.0678830047410433));
#24446=CARTESIAN_POINT('Ctrl Pts',(9.07759664569311,0.527144320628084,0.200227083015481));
#24447=CARTESIAN_POINT('Ctrl Pts',(7.40162371335757,-3.60564141759996,0.398743200427137));
#24448=CARTESIAN_POINT('Ctrl Pts',(3.02458781445768,-4.42536858002973,0.597259317838794));
#24449=CARTESIAN_POINT('Ctrl Pts',(-0.0391348072720899,-1.19794185424409,
0.795775435250448));
#24450=CARTESIAN_POINT('Ctrl Pts',(1.01307994788347,3.12938294858669,0.994291552662105));
#24451=CARTESIAN_POINT('Ctrl Pts',(5.21923250695947,4.58939821694615,1.19280767007376));
#24452=CARTESIAN_POINT('Ctrl Pts',(8.72657551299543,1.84730106611042,1.39132378748542));
#24453=CARTESIAN_POINT('Ctrl Pts',(8.32358502229467,-2.58692118447061,1.58983990489707));
#24454=CARTESIAN_POINT('Ctrl Pts',(4.37908581601258,-4.65188073047965,1.78835602230873));
#24455=CARTESIAN_POINT('Ctrl Pts',(0.505493161016087,-2.45684558601761,
1.98687213972038));
#24456=CARTESIAN_POINT('Ctrl Pts',(0.250108060020668,1.98817892786946,2.18538825713204));
#24457=CARTESIAN_POINT('Ctrl Pts',(3.8468393694429,4.61243733220712,2.38390437454369));
#24458=CARTESIAN_POINT('Ctrl Pts',(8.0018522734089,3.01272882884126,2.58242049195535));
#24459=CARTESIAN_POINT('Ctrl Pts',(8.91007369571349,-1.34598748780205,2.78093660936701));
#24460=CARTESIAN_POINT('Ctrl Pts',(5.73976719690925,-4.47206986535408,2.97945272677866));
#24461=CARTESIAN_POINT('Ctrl Pts',(1.39424152787623,-3.50271791779653,3.17796884419032));
#24462=CARTESIAN_POINT('Ctrl Pts',(-0.146954797017362,0.674357611516781,
3.37648496160198));
#24463=CARTESIAN_POINT('Ctrl Pts',(2.5275771424141,4.23386867290823,3.57500107901363));
#24464=CARTESIAN_POINT('Ctrl Pts',(6.96855153613195,3.91608365047424,3.77351719642529));
#24465=CARTESIAN_POINT('Ctrl Pts',(9.10900868522111,0.0120235511094912,
3.97203331383693));
#24466=CARTESIAN_POINT('Ctrl Pts',(6.98875855737045,-3.90304740339865,4.17054943124861));
#24467=CARTESIAN_POINT('Ctrl Pts',(2.54948593565754,-4.24378183362265,4.36906554866025));
#24468=CARTESIAN_POINT('Ctrl Pts',(-0.143407781592193,-0.698141563015474,
4.56758166607191));
#24469=CARTESIAN_POINT('Ctrl Pts',(1.37617826049345,3.48684345900968,4.76609778348356));
#24470=CARTESIAN_POINT('Ctrl Pts',(5.71663606344787,4.47864357428809,4.96461390089523));
#24471=CARTESIAN_POINT('Ctrl Pts',(8.90305693908813,1.36898709382619,5.16313001830687));
#24472=CARTESIAN_POINT('Ctrl Pts',(8.01737725983028,-2.99436172457643,5.36164613571854));
#24473=CARTESIAN_POINT('Ctrl Pts',(3.87068562947579,-4.61553103529222,5.56016225313019));
#24474=CARTESIAN_POINT('Ctrl Pts',(0.260443364168955,-2.00988482013811,
5.75867837054185));
#24475=CARTESIAN_POINT('Ctrl Pts',(0.492841656646439,2.436375680996,5.95719448795349));
#24476=CARTESIAN_POINT('Ctrl Pts',(4.35505457120696,4.6514496783783,6.15571060536516));
#24477=CARTESIAN_POINT('Ctrl Pts',(8.31014098784587,2.60681454019155,6.35422672277681));
#24478=CARTESIAN_POINT('Ctrl Pts',(8.73610799988966,-1.82509176699825,6.55274284018847));
#24479=CARTESIAN_POINT('Ctrl Pts',(5.24286312047947,-4.58561375091533,6.75125895760012));
#24480=CARTESIAN_POINT('Ctrl Pts',(1.02945356160573,-3.14671788935761,6.94977507501179));
#24481=CARTESIAN_POINT('Ctrl Pts',(-0.0455603502579819,1.17388235834786,
7.14829119242343));
#24482=CARTESIAN_POINT('Ctrl Pts',(3.00229867643747,4.41946347189101,7.34680730983509));
#24483=CARTESIAN_POINT('Ctrl Pts',(7.38185932147204,3.61778400498435,7.54532342724674));
#24484=CARTESIAN_POINT('Ctrl Pts',(9.08240325419932,-0.496993236137507,
7.7438395446584));
#24485=CARTESIAN_POINT('Ctrl Pts',(6.5466046888036,-4.15663352541875,7.94235566207006));
#24486=CARTESIAN_POINT('Ctrl Pts',(2.09669971547073,-4.00970789967487,8.1408717794817));
#24487=CARTESIAN_POINT('Ctrl Pts',(-0.192173337388976,-0.19076805214061,
8.33938789689338));
#24488=CARTESIAN_POINT('Ctrl Pts',(1.77609193305126,3.80287354875093,8.53790401430502));
#24489=CARTESIAN_POINT('Ctrl Pts',(6.1989956324977,4.3139158920216,8.73642013171668));
#24490=CARTESIAN_POINT('Ctrl Pts',(9.0261266855466,0.874356120760312,8.93493624912834));
#24491=CARTESIAN_POINT('Ctrl Pts',(7.66845225155073,-3.36592235387631,9.13345236653999));
#24492=CARTESIAN_POINT('Ctrl Pts',(3.36930475145732,-4.52375316346519,9.33196848395166));
#24493=CARTESIAN_POINT('Ctrl Pts',(0.0657616873951493,-1.53881687686219,
9.53048460136329));
#24494=CARTESIAN_POINT('Ctrl Pts',(0.783144957380055,2.85533863417045,9.72900071877498));
#24495=CARTESIAN_POINT('Ctrl Pts',(4.86448860883662,4.63462933832978,9.92751683618659));
#24496=CARTESIAN_POINT('Ctrl Pts',(8.57217576114917,2.16961465444475,10.1260329535983));
#24497=CARTESIAN_POINT('Ctrl Pts',(8.51077704791793,-2.28229185953398,10.3245490710099));
#24498=CARTESIAN_POINT('Ctrl Pts',(4.73652024279266,-4.644118902346,10.5230651884216));
#24499=CARTESIAN_POINT('Ctrl Pts',(0.705797933930029,-2.75295019489822,
10.7215813058332));
#24500=CARTESIAN_POINT('Ctrl Pts',(0.109868939318185,1.65931793437198,10.9200974232449));
#24501=CARTESIAN_POINT('Ctrl Pts',(3.49447369645122,4.55201426291826,11.1186135406565));
#24502=CARTESIAN_POINT('Ctrl Pts',(7.76005555075585,3.27606251797663,11.3171296580682));
#24503=CARTESIAN_POINT('Ctrl Pts',(9.00027578003045,-1.00004496361109,11.5156457754798));
#24504=CARTESIAN_POINT('Ctrl Pts',(6.07936428979557,-4.36033029039609,11.7141618928915));
#24505=CARTESIAN_POINT('Ctrl Pts',(1.67223626118035,-3.72750807951321,11.9126780103032));
#24506=CARTESIAN_POINT('Ctrl Pts',(-0.185144289673645,0.31889512586586,
12.1111941277148));
#24507=CARTESIAN_POINT('Ctrl Pts',(2.20817641458127,4.07326024100545,12.3097102451265));
#24508=CARTESIAN_POINT('Ctrl Pts',(6.66044079877556,4.09741110905781,12.5082263625381));
#24509=CARTESIAN_POINT('Ctrl Pts',(9.09434983091284,0.369230824458725,12.7067424799498));
#24510=CARTESIAN_POINT('Ctrl Pts',(7.28097591722075,-3.69708402566464,12.9052585973614));
#24511=CARTESIAN_POINT('Ctrl Pts',(2.8809723938291,-4.37767965107946,13.1037747147731));
#24512=CARTESIAN_POINT('Ctrl Pts',(-0.0762212094817758,-1.04927952433239,
13.3022908321848));
#24513=CARTESIAN_POINT('Ctrl Pts',(1.11753675741321,3.24003083138531,13.5008069495964));
#24514=CARTESIAN_POINT('Ctrl Pts',(5.369025456116,4.5621825836419,13.6993230670081));
#24515=CARTESIAN_POINT('Ctrl Pts',(8.78481240824481,1.70637430771384,13.8978391844197));
#24516=CARTESIAN_POINT('Ctrl Pts',(8.23678489819753,-2.71209910053747,14.0963553018314));
#24517=CARTESIAN_POINT('Ctrl Pts',(4.22681609508684,-4.64688374211174,14.294871419243));
#24518=CARTESIAN_POINT('Ctrl Pts',(0.427159151106815,-2.32614064576156,
14.4933875366547));
#24519=CARTESIAN_POINT('Ctrl Pts',(0.317467618415429,2.12483780609018,14.6919036540663));
#24520=CARTESIAN_POINT('Ctrl Pts',(3.99819491609722,4.62993021382537,14.890419771478));
#24521=CARTESIAN_POINT('Ctrl Pts',(8.09860099979244,2.8950206023505,15.0889358888896));
#24522=CARTESIAN_POINT('Ctrl Pts',(8.86361197604717,-1.49109380762589,15.2874520063013));
#24523=CARTESIAN_POINT('Ctrl Pts',(5.59264534485911,-4.5116928721902,15.485968123713));
#24524=CARTESIAN_POINT('Ctrl Pts',(1.2811901266875,-3.40056942590122,15.6844842411246));
#24525=CARTESIAN_POINT('Ctrl Pts',(-0.122405002240585,0.824730814938715,
15.8830003585363));
#24526=CARTESIAN_POINT('Ctrl Pts',(2.66724567793686,4.29475826350135,16.0815164759479));
#24527=CARTESIAN_POINT('Ctrl Pts',(7.09543313909595,3.83172778931411,16.2800325933596));
#24528=CARTESIAN_POINT('Ctrl Pts',(9.10690753736432,-0.140326107135887,
16.4785487107712));
#24529=CARTESIAN_POINT('Ctrl Pts',(6.85959888110794,-3.98387202395643,16.6770648281829));
#24530=CARTESIAN_POINT('Ctrl Pts',(2.41154968938301,-4.179063722519,16.8755809455945));
#24531=CARTESIAN_POINT('Ctrl Pts',(-0.163801198896094,-0.547148358219792,
17.0740970630062));
#24532=CARTESIAN_POINT('Ctrl Pts',(1.49200357138825,3.5858350646717,17.2726131804178));
#24533=CARTESIAN_POINT('Ctrl Pts',(5.86260948835618,4.43497894515246,17.4711292978295));
#24534=CARTESIAN_POINT('Ctrl Pts',(8.94549879098837,1.22265346990726,17.6696454152412));
#24535=CARTESIAN_POINT('Ctrl Pts',(7.91742009870712,-3.10935479574357,17.8681615326528));
#24536=CARTESIAN_POINT('Ctrl Pts',(3.71986832177296,-4.59387508565289,18.0666776500645));
#24537=CARTESIAN_POINT('Ctrl Pts',(0.196881531601468,-1.87141195688986,
18.2651937674761));
#24538=CARTESIAN_POINT('Ctrl Pts',(0.574744016316265,2.56485464396025,18.4637098848878));
#24539=CARTESIAN_POINT('Ctrl Pts',(4.50741650012369,4.6522761505852,18.6622260022994));
#24540=CARTESIAN_POINT('Ctrl Pts',(8.3934323297128,2.47923165417059,18.8607421197111));
#24541=CARTESIAN_POINT('Ctrl Pts',(8.67405212821057,-1.96424603112833,19.0592582371228));
#24542=CARTESIAN_POINT('Ctrl Pts',(5.09228962209667,-4.60890456507674,19.2577743545344));
#24543=CARTESIAN_POINT('Ctrl Pts',(0.928254782143413,-3.0328159689208,19.4562904719461));
#24544=CARTESIAN_POINT('Ctrl Pts',(-0.00470849360073685,1.32066780116548,
19.6548065893577));
#24545=CARTESIAN_POINT('Ctrl Pts',(3.14778981602278,4.46470912096001,19.8533227067694));
#24546=CARTESIAN_POINT('Ctrl Pts',(7.49875172579254,3.52005475507203,20.051838824181));
#24547=CARTESIAN_POINT('Ctrl Pts',(9.06364908309027,-0.648198796048447,
20.2503549415927));
#24548=CARTESIAN_POINT('Ctrl Pts',(6.4093786550744,-4.22284422156345,20.4488710590044));
#24549=CARTESIAN_POINT('Ctrl Pts',(1.96667081116617,-3.93028923259476,20.647387176416));
#24550=CARTESIAN_POINT('Ctrl Pts',(-0.195927116407106,-0.0384501329489085,
20.8459032938277));
#24551=CARTESIAN_POINT('Ctrl Pts',(1.90205092121151,3.88860087953163,21.0444194112393));
#24552=CARTESIAN_POINT('Ctrl Pts',(6.3393165377314,4.25454515162759,21.242935528651));
#24553=CARTESIAN_POINT('Ctrl Pts',(9.05230630112455,0.724257949825445,21.4414516460626));
#24554=CARTESIAN_POINT('Ctrl Pts',(7.55651576606266,-3.46929099370176,21.6399677634743));
#24555=CARTESIAN_POINT('Ctrl Pts',(3.22176150253947,-4.48572906904549,21.838483880886));
#24556=CARTESIAN_POINT('Ctrl Pts',(0.0177289115966501,-1.39422211492368,
22.0369999982976));
#24557=CARTESIAN_POINT('Ctrl Pts',(0.878610280341868,2.97408755340353,22.2355161157093));
#24558=CARTESIAN_POINT('Ctrl Pts',(5.01602646728549,4.61878321962123,22.4340322331209));
#24559=CARTESIAN_POINT('Ctrl Pts',(8.64101112050298,2.03368736229999,22.6325483505326));
#24560=CARTESIAN_POINT('Ctrl Pts',(8.43387092517075,-2.41382509078919,22.8310644679442));
#24561=CARTESIAN_POINT('Ctrl Pts',(4.58430347192829,-4.65079401118156,23.0295805853559));
#24562=CARTESIAN_POINT('Ctrl Pts',(0.617664534920323,-2.6286704174496,23.2280967027675));
#24563=CARTESIAN_POINT('Ctrl Pts',(0.166535948123391,1.80077057177711,23.4266128201792));
#24564=CARTESIAN_POINT('Ctrl Pts',(3.64403475383551,4.58104059437149,23.6251289375908));
#24565=CARTESIAN_POINT('Ctrl Pts',(7.86556810560143,3.16619499327494,23.8236450550025));
#24566=CARTESIAN_POINT('Ctrl Pts',(8.96507004425898,-1.14841087401253,24.0221611724142));
#24567=CARTESIAN_POINT('Ctrl Pts',(5.93576426504054,-4.41090351654891,24.2206772898258));
#24568=CARTESIAN_POINT('Ctrl Pts',(1.55158838794904,-3.63478122412758,24.4191934072375));
#24569=CARTESIAN_POINT('Ctrl Pts',(-0.172046559910909,0.471552713422697,
24.6177095246491));
#24570=CARTESIAN_POINT('Ctrl Pts',(2.34243741690352,4.14307145960353,24.8162256420608));
#24571=CARTESIAN_POINT('Ctrl Pts',(6.79403703197597,4.02620936921257,25.0147417594724));
#24572=CARTESIAN_POINT('Ctrl Pts',(9.10329134237422,0.209832038399488,25.2133007328261));
#24573=CARTESIAN_POINT('Ctrl Pts',(7.80718744833136,-2.44564931016495,25.3456876670425));
#24574=CARTESIAN_POINT('Ctrl Pts',(6.7401774553626,-3.20569558398784,25.4119025621217));
#24575=CARTESIAN_POINT('Ctrl Pts',(2.17296269996979,-3.20554048108048,-0.411765747138983));
#24576=CARTESIAN_POINT('Ctrl Pts',(1.10598262521586,-2.44554835076675,-0.345549597099719));
#24577=CARTESIAN_POINT('Ctrl Pts',(-0.190085171851759,0.209786400507346,
-0.213161407923235));
#24578=CARTESIAN_POINT('Ctrl Pts',(2.11904905146237,4.02596493684606,-0.0146011796095345));
#24579=CARTESIAN_POINT('Ctrl Pts',(6.57036830017086,4.14281137096193,0.183914937802122));
#24580=CARTESIAN_POINT('Ctrl Pts',(9.08469850437939,0.471525498888313,0.382431055213778));
#24581=CARTESIAN_POINT('Ctrl Pts',(7.36116941620609,-3.63455711911314,0.580947172625436));
#24582=CARTESIAN_POINT('Ctrl Pts',(2.97726580402431,-4.41062931823268,0.77946329003709));
#24583=CARTESIAN_POINT('Ctrl Pts',(-0.0518523842630756,-1.14834011450979,
0.977979407448747));
#24584=CARTESIAN_POINT('Ctrl Pts',(1.04758148582589,3.16599895701937,1.1764955248604));
#24585=CARTESIAN_POINT('Ctrl Pts',(5.26885307852876,4.58075644304919,1.37501164227206));
#24586=CARTESIAN_POINT('Ctrl Pts',(8.74613631193873,1.80065901519612,1.57352775968371));
#24587=CARTESIAN_POINT('Ctrl Pts',(8.2950356860829,-2.62850749839492,1.77204387709537));
#24588=CARTESIAN_POINT('Ctrl Pts',(4.32864266632258,-4.6505056552148,1.97055999450703));
#24589=CARTESIAN_POINT('Ctrl Pts',(0.479313869061077,-2.41367545883394,
2.16907611191868));
#24590=CARTESIAN_POINT('Ctrl Pts',(0.272186515624751,2.03356129066451,2.36759222933034));
#24591=CARTESIAN_POINT('Ctrl Pts',(3.89694643539194,4.61849687019083,2.56610834674199));
#24592=CARTESIAN_POINT('Ctrl Pts',(8.03410612006349,2.97390317522259,2.76462446415365));
#24593=CARTESIAN_POINT('Ctrl Pts',(8.89493411795877,-1.39413568050936,2.9631405815653));
#24594=CARTESIAN_POINT('Ctrl Pts',(5.69110016326603,-4.48545097223521,3.16165669897696));
#24595=CARTESIAN_POINT('Ctrl Pts',(1.35661463604595,-3.46907591290164,3.36017281638862));
#24596=CARTESIAN_POINT('Ctrl Pts',(-0.139083166427389,0.724213049156903,
3.55868893380027));
#24597=CARTESIAN_POINT('Ctrl Pts',(2.57373840321099,4.25428138787658,3.75720505121192));
#24598=CARTESIAN_POINT('Ctrl Pts',(7.01072892820446,3.88835980295648,3.95572116862359));
#24599=CARTESIAN_POINT('Ctrl Pts',(9.10857690015422,-0.0384477492421469,
4.15423728603523));
#24600=CARTESIAN_POINT('Ctrl Pts',(6.94611304441007,-3.93004557143118,4.3527534034469));
#24601=CARTESIAN_POINT('Ctrl Pts',(2.50368062941278,-4.22258242327136,4.55126952085854));
#24602=CARTESIAN_POINT('Ctrl Pts',(-0.15042524517621,-0.648158610486061,
4.74978563827021));
#24603=CARTESIAN_POINT('Ctrl Pts',(1.41437509517098,3.51983652671062,4.94830175568186));
#24604=CARTESIAN_POINT('Ctrl Pts',(5.76506726388787,4.46443232806813,5.14681787309352));
#24605=CARTESIAN_POINT('Ctrl Pts',(8.91737013208296,1.32058592540232,5.34533399050517));
#24606=CARTESIAN_POINT('Ctrl Pts',(7.98446469607637,-3.03262794728552,5.54385010791683));
#24607=CARTESIAN_POINT('Ctrl Pts',(3.82068800849579,-4.60861883268182,5.74236622532849));
#24608=CARTESIAN_POINT('Ctrl Pts',(0.239147556357015,-1.9641242562649,5.94088234274014));
#24609=CARTESIAN_POINT('Ctrl Pts',(0.519749957626067,2.47907795239849,6.13939846015179));
#24610=CARTESIAN_POINT('Ctrl Pts',(4.40552487083362,4.65198772933701,6.33791457756345));
#24611=CARTESIAN_POINT('Ctrl Pts',(8.33795354574623,2.56469563392857,6.53643069497511));
#24612=CARTESIAN_POINT('Ctrl Pts',(8.71579260460107,-1.87129593734266,6.73494681238676));
#24613=CARTESIAN_POINT('Ctrl Pts',(5.19302422456139,-4.59359028502123,6.93346292979842));
#24614=CARTESIAN_POINT('Ctrl Pts',(0.995732677906764,-3.10916202902842,
7.13197904721008));
#24615=CARTESIAN_POINT('Ctrl Pts',(-0.0322822778871914,1.22257767061497,
7.33049516462173));
#24616=CARTESIAN_POINT('Ctrl Pts',(3.05041589877745,4.43470399540276,7.52901128203338));
#24617=CARTESIAN_POINT('Ctrl Pts',(7.42075085684839,3.58561275821527,7.72752739944505));
#24618=CARTESIAN_POINT('Ctrl Pts',(9.07645297431008,-0.547114437358846,
7.9260435168567));
#24619=CARTESIAN_POINT('Ctrl Pts',(6.5012617467849,-4.17880463841992,8.12455963426836));
#24620=CARTESIAN_POINT('Ctrl Pts',(2.05348831510913,-3.98362504090881,8.32307575168001));
#24621=CARTESIAN_POINT('Ctrl Pts',(-0.193681017610346,-0.140317407516647,
8.52159186909167));
#24622=CARTESIAN_POINT('Ctrl Pts',(1.81766867783776,3.83149023855917,8.72010798650331));
#24623=CARTESIAN_POINT('Ctrl Pts',(6.24558161029013,4.2944920068349,8.91862410391498));
#24624=CARTESIAN_POINT('Ctrl Pts',(9.03505934404192,0.824679685151172,9.11714022132663));
#24625=CARTESIAN_POINT('Ctrl Pts',(7.6315512320161,-3.40035860512303,9.31565633873829));
#24626=CARTESIAN_POINT('Ctrl Pts',(3.32036330565075,-4.51141316650472,9.51417245614994));
#24627=CARTESIAN_POINT('Ctrl Pts',(0.0495994604212725,-1.49100136617927,
9.71268857356161));
#24628=CARTESIAN_POINT('Ctrl Pts',(0.814563009263402,2.89484112343983,9.91120469097325));
#24629=CARTESIAN_POINT('Ctrl Pts',(4.91471488529713,4.62964317792977,10.1097208083849));
#24630=CARTESIAN_POINT('Ctrl Pts',(8.59521399360942,2.1247060752228,10.3082369257966));
#24631=CARTESIAN_POINT('Ctrl Pts',(8.48552926132444,-2.32599643497811,10.5067530432082));
#24632=CARTESIAN_POINT('Ctrl Pts',(4.68610787984395,-4.64659565516981,10.7052691606199));
#24633=CARTESIAN_POINT('Ctrl Pts',(0.676387677669684,-2.71193096197848,
10.9037852780315));
#24634=CARTESIAN_POINT('Ctrl Pts',(0.128394142987057,1.70626851979591,11.1023013954432));
#24635=CARTESIAN_POINT('Ctrl Pts',(3.54396933091606,4.56189974780998,11.3008175128549));
#24636=CARTESIAN_POINT('Ctrl Pts',(7.79519445548059,3.23982996331418,11.4993336302665));
#24637=CARTESIAN_POINT('Ctrl Pts',(8.98887841448097,-1.04921447348414,11.6978497476782));
#24638=CARTESIAN_POINT('Ctrl Pts',(6.03186814454124,-4.3774082536412,11.8963658650898));
#24639=CARTESIAN_POINT('Ctrl Pts',(1.63213740257258,-3.69685482224785,12.0948819825015));
#24640=CARTESIAN_POINT('Ctrl Pts',(-0.181124089683036,0.369207933724872,
12.2933980999131));
#24641=CARTESIAN_POINT('Ctrl Pts',(2.2526340504912,4.09715708707193,12.4919142173248));
#24642=CARTESIAN_POINT('Ctrl Pts',(6.70462241331237,4.07300771627025,12.6904303347364));
#24643=CARTESIAN_POINT('Ctrl Pts',(9.09779474190718,0.318875355730261,12.8889464521481));
#24644=CARTESIAN_POINT('Ctrl Pts',(7.24052934071316,-3.72727698993507,13.0874625695597));
#24645=CARTESIAN_POINT('Ctrl Pts',(2.83367453520978,-4.36005996854408,13.2859786869714));
#24646=CARTESIAN_POINT('Ctrl Pts',(-0.0870558709899348,-0.999982965095223,
13.4844948043831));
#24647=CARTESIAN_POINT('Ctrl Pts',(1.1530874699283,3.2758594160949,13.6830109217947));
#24648=CARTESIAN_POINT('Ctrl Pts',(5.41840487637927,4.55173205747878,13.8815270392064));
#24649=CARTESIAN_POINT('Ctrl Pts',(8.80279980247531,1.65921506374814,14.080043156618));
#24650=CARTESIAN_POINT('Ctrl Pts',(8.20690775291552,-2.75277952374592,14.2785592740297));
#24651=CARTESIAN_POINT('Ctrl Pts',(4.17643533161801,-4.64383098681233,14.4770753914414));
#24652=CARTESIAN_POINT('Ctrl Pts',(0.402412514292184,-2.28215036718792,
14.675591508853));
#24653=CARTESIAN_POINT('Ctrl Pts',(0.341017607518878,2.16948014760412,14.8741076262646));
#24654=CARTESIAN_POINT('Ctrl Pts',(4.04847489906614,4.63434201110855,15.0726237436763));
#24655=CARTESIAN_POINT('Ctrl Pts',(8.12956552465056,2.85516161537223,15.271139861088));
#24656=CARTESIAN_POINT('Ctrl Pts',(8.84690431993714,-1.53872147678918,15.4696559784996));
#24657=CARTESIAN_POINT('Ctrl Pts',(5.54356606143321,-4.52347271009317,15.6681720959113));
#24658=CARTESIAN_POINT('Ctrl Pts',(1.24468509012015,-3.36571368106855,15.8666882133229));
#24659=CARTESIAN_POINT('Ctrl Pts',(-0.112905173860372,0.874301914415817,
16.0652043307346));
#24660=CARTESIAN_POINT('Ctrl Pts',(2.71405060913991,4.31364844766405,16.2637204481462));
#24661=CARTESIAN_POINT('Ctrl Pts',(7.1366801074503,3.80263778683562,16.4622365655579));
#24662=CARTESIAN_POINT('Ctrl Pts',(9.10482335385156,-0.190756225336315,
16.6607526829696));
#24663=CARTESIAN_POINT('Ctrl Pts',(6.81609220134375,-4.00945931491334,16.8592688003812));
#24664=CARTESIAN_POINT('Ctrl Pts',(2.36646310311057,-4.15637583189606,17.0577849177929));
#24665=CARTESIAN_POINT('Ctrl Pts',(-0.16917825360623,-0.496962424679848,
17.2563010352045));
#24666=CARTESIAN_POINT('Ctrl Pts',(1.53126025266144,3.61755971783011,17.4548171526162));
#24667=CARTESIAN_POINT('Ctrl Pts',(5.91054938364417,4.41918948403437,17.6533332700278));
#24668=CARTESIAN_POINT('Ctrl Pts',(8.95821945609951,1.17380958265607,17.8518493874395));
#24669=CARTESIAN_POINT('Ctrl Pts',(7.88327219050615,-3.14652280629029,18.0503655048511));
#24670=CARTESIAN_POINT('Ctrl Pts',(3.67012384502666,-4.58532946245115,18.2488816222628));
#24671=CARTESIAN_POINT('Ctrl Pts',(0.177095531876928,-1.82497861910485,
18.4473977396744));
#24672=CARTESIAN_POINT('Ctrl Pts',(0.603036135785551,2.60665292882547,18.6459138570862));
#24673=CARTESIAN_POINT('Ctrl Pts',(4.55787735396168,4.65116130836808,18.8444299744978));
#24674=CARTESIAN_POINT('Ctrl Pts',(8.41985082781949,2.43622463611074,19.0429460919094));
#24675=CARTESIAN_POINT('Ctrl Pts',(8.65223471259592,-2.00976021586402,19.2414622093211));
#24676=CARTESIAN_POINT('Ctrl Pts',(5.04221626688697,-4.61524489208584,19.4399783267328));
#24677=CARTESIAN_POINT('Ctrl Pts',(0.895781713701428,-2.99417608693739,
19.6384944441444));
#24678=CARTESIAN_POINT('Ctrl Pts',(0.0101569427980723,1.36890222246852,
19.8370105615561));
#24679=CARTESIAN_POINT('Ctrl Pts',(3.1963802739596,4.47836591752857,20.0355266789677));
#24680=CARTESIAN_POINT('Ctrl Pts',(7.53656898706393,3.48662728959027,20.2340427963793));
#24681=CARTESIAN_POINT('Ctrl Pts',(9.05606082131957,-0.698098281184544,
20.432558913791));
#24682=CARTESIAN_POINT('Ctrl Pts',(6.36333405195284,-4.24351873734398,20.6310750312027));
#24683=CARTESIAN_POINT('Ctrl Pts',(1.9243366462227,-3.90280543100934,20.8295911486144));
#24684=CARTESIAN_POINT('Ctrl Pts',(-0.195782035254683,0.0120228054752082,
21.028107266026));
#24685=CARTESIAN_POINT('Ctrl Pts',(1.94454241477252,3.91584087042925,21.2266233834376));
#24686=CARTESIAN_POINT('Ctrl Pts',(6.38524148680512,4.23360619038166,21.4251395008493));
#24687=CARTESIAN_POINT('Ctrl Pts',(9.05960761710739,0.674315805600993,21.623655618261));
#24688=CARTESIAN_POINT('Ctrl Pts',(7.5185068390623,-3.50250076674849,21.8221717356726));
#24689=CARTESIAN_POINT('Ctrl Pts',(3.17325057532877,-4.47179261159471,22.0206878530843));
#24690=CARTESIAN_POINT('Ctrl Pts',(0.0031406198327811,-1.34590405051051,
22.2192039704959));
#24691=CARTESIAN_POINT('Ctrl Pts',(0.911305739869395,3.01254206724522,22.4177200879076));
#24692=CARTESIAN_POINT('Ctrl Pts',(5.06606104496655,4.6121513544261,22.6162362053192));
#24693=CARTESIAN_POINT('Ctrl Pts',(8.66256938155685,1.98805571626367,22.8147523227309));
#24694=CARTESIAN_POINT('Ctrl Pts',(8.4072000996685,-2.45669335535235,23.0132684401425));
#24695=CARTESIAN_POINT('Ctrl Pts',(4.53384760969594,-4.65159218721967,23.2117845575542));
#24696=CARTESIAN_POINT('Ctrl Pts',(0.589592923617338,-2.58676106216746,
23.4103006749659));
#24697=CARTESIAN_POINT('Ctrl Pts',(0.186627431348294,1.84718698340797,23.6088167923775));
#24698=CARTESIAN_POINT('Ctrl Pts',(3.69375302108596,4.58911293885384,23.8073329097892));
#24699=CARTESIAN_POINT('Ctrl Pts',(7.89964467060016,3.12919021086655,24.0058490272008));
#24700=CARTESIAN_POINT('Ctrl Pts',(8.95179466357075,-1.19786968887199,24.2043651446125));
#24701=CARTESIAN_POINT('Ctrl Pts',(5.88826072308503,-4.42509080397621,24.4028812620241));
#24702=CARTESIAN_POINT('Ctrl Pts',(1.51149918181804,-3.60542346049212,24.6013973794358));
#24703=CARTESIAN_POINT('Ctrl Pts',(-0.164376056275096,0.527120914407128,
24.7999134968474));
#24704=CARTESIAN_POINT('Ctrl Pts',(1.53399129555416,2.94325066577138,24.9322575751219));
#24705=CARTESIAN_POINT('Ctrl Pts',(2.70656526709436,3.52529833870864,24.9984296142591));
#24706=CARTESIAN_POINT('Ctrl Pts',(2.31196529717974,-3.01041142380583,-0.273445981108207));
#24707=CARTESIAN_POINT('Ctrl Pts',(1.30993489857133,-2.29668186568531,-0.207229831068943));
#24708=CARTESIAN_POINT('Ctrl Pts',(0.0927619053280601,0.197016191301887,
-0.0748416418924601));
#24709=CARTESIAN_POINT('Ctrl Pts',(2.26133350378215,3.78089464452436,0.123718586421241));
#24710=CARTESIAN_POINT('Ctrl Pts',(6.44169010710979,3.89062835157607,0.322234703832897));
#24711=CARTESIAN_POINT('Ctrl Pts',(8.80296690727615,0.442822593209179,0.520750821244553));
#24712=CARTESIAN_POINT('Ctrl Pts',(7.18435323294509,-3.41331277406459,0.719266938656211));
#24713=CARTESIAN_POINT('Ctrl Pts',(3.06730851213489,-4.14214356803415,0.917783056067867));
#24714=CARTESIAN_POINT('Ctrl Pts',(0.222580126422941,-1.07843785456408,
1.11629917347952));
#24715=CARTESIAN_POINT('Ctrl Pts',(1.25508877879203,2.97327688863128,1.31481529089117));
#24716=CARTESIAN_POINT('Ctrl Pts',(5.21940128729496,4.30191464036023,1.51333140830283));
#24717=CARTESIAN_POINT('Ctrl Pts',(8.48501382017349,1.69104851481962,1.71184752571448));
#24718=CARTESIAN_POINT('Ctrl Pts',(8.06137278822348,-2.46850384433775,1.91036364312614));
#24719=CARTESIAN_POINT('Ctrl Pts',(4.33642377308406,-4.36741804808325,2.1088797605378));
#24720=CARTESIAN_POINT('Ctrl Pts',(0.721412996069988,-2.26674915432179,
2.30739587794946));
#24721=CARTESIAN_POINT('Ctrl Pts',(0.526893989166935,1.90977346146706,2.50591199536111));
#24722=CARTESIAN_POINT('Ctrl Pts',(3.93100594327419,4.33735771577206,2.70442811277276));
#24723=CARTESIAN_POINT('Ctrl Pts',(7.81632664047099,2.79287444498747,2.90294423018442));
#24724=CARTESIAN_POINT('Ctrl Pts',(8.62475394129306,-1.30927124574203,3.10146034759608));
#24725=CARTESIAN_POINT('Ctrl Pts',(5.61594516345689,-4.21241064570382,3.29997646500774));
#24726=CARTESIAN_POINT('Ctrl Pts',(1.54531032840212,-3.25790481196126,3.49849258241939));
#24727=CARTESIAN_POINT('Ctrl Pts',(0.140659294449413,0.680128436785933,
3.69700869983105));
#24728=CARTESIAN_POINT('Ctrl Pts',(2.68834480713824,3.99531291703776,3.8955248172427));
#24729=CARTESIAN_POINT('Ctrl Pts',(6.85524491106594,3.65166587031902,4.09404093465435));
#24730=CARTESIAN_POINT('Ctrl Pts',(8.82539176693615,-0.0361073410931478,
4.29255705206602));
#24731=CARTESIAN_POINT('Ctrl Pts',(6.79456235351217,-3.69081412452673,4.49107316947766));
#24732=CARTESIAN_POINT('Ctrl Pts',(2.62255162068078,-3.96554354562172,4.68958928688933));
#24733=CARTESIAN_POINT('Ctrl Pts',(0.130007635661538,-0.608703617053558,
4.88810540430098));
#24734=CARTESIAN_POINT('Ctrl Pts',(1.59955476768487,3.30557550356288,5.08662152171263));
#24735=CARTESIAN_POINT('Ctrl Pts',(5.68540970649173,4.19267145760527,5.28513763912429));
#24736=CARTESIAN_POINT('Ctrl Pts',(8.64582422058695,1.24019864338394,5.48365375653594));
#24737=CARTESIAN_POINT('Ctrl Pts',(7.76970701088062,-2.84802449713069,5.68216987394761));
#24738=CARTESIAN_POINT('Ctrl Pts',(3.85938955257665,-4.32808097846753,5.88068599135924));
#24739=CARTESIAN_POINT('Ctrl Pts',(0.495866191827503,-1.844563228489,6.07920210877092));
#24740=CARTESIAN_POINT('Ctrl Pts',(0.759387641428115,2.32817043879295,6.27771822618256));
#24741=CARTESIAN_POINT('Ctrl Pts',(4.40862597053364,4.36880990474354,6.47623434359423));
#24742=CARTESIAN_POINT('Ctrl Pts',(8.10167813322798,2.40857636349708,6.67475046100588));
#24743=CARTESIAN_POINT('Ctrl Pts',(8.45651720821394,-1.75738559545474,6.87326657841754));
#24744=CARTESIAN_POINT('Ctrl Pts',(5.14818832037566,-4.31396725511023,7.0717826958292));
#24745=CARTESIAN_POINT('Ctrl Pts',(1.20639613410644,-2.9198997628929,7.27029881324085));
#24746=CARTESIAN_POINT('Ctrl Pts',(0.240958952754043,1.14815638979818,7.4688149306525));
#24747=CARTESIAN_POINT('Ctrl Pts',(3.13600578243834,4.16475276096279,7.66733104806417));
#24748=CARTESIAN_POINT('Ctrl Pts',(7.24030780616454,3.36734777563528,7.86584716547581));
#24749=CARTESIAN_POINT('Ctrl Pts',(8.79522330270695,-0.513810248872322,
8.06436328288747));
#24750=CARTESIAN_POINT('Ctrl Pts',(6.37679023796107,-3.92443062116999,8.26287940029913));
#24751=CARTESIAN_POINT('Ctrl Pts',(2.1997636091463,-3.74113208118609,8.46139551771078));
#24752=CARTESIAN_POINT('Ctrl Pts',(0.089384947459713,-0.131775945129999,
8.65991163512245));
#24753=CARTESIAN_POINT('Ctrl Pts',(1.97829888761515,3.5982580948319,8.8584277525341));
#24754=CARTESIAN_POINT('Ctrl Pts',(6.13667397417128,4.03307581767334,9.05694386994575));
#24755=CARTESIAN_POINT('Ctrl Pts',(8.75634940354159,0.774479423926291,9.2554599873574));
#24756=CARTESIAN_POINT('Ctrl Pts',(7.43827624901926,-3.19337049409171,9.45397610476906));
#24757=CARTESIAN_POINT('Ctrl Pts',(3.38952083310589,-4.23679245796831,9.65249222218073));
#24758=CARTESIAN_POINT('Ctrl Pts',(0.317856350200649,-1.40024048117564,
9.85100833959237));
#24759=CARTESIAN_POINT('Ctrl Pts',(1.03625470449417,2.71862509287945,10.049524457004));
#24760=CARTESIAN_POINT('Ctrl Pts',(4.88682034851015,4.34782552060827,10.2480405744157));
#24761=CARTESIAN_POINT('Ctrl Pts',(8.34327851098385,1.99537004097493,10.4465566918273));
#24762=CARTESIAN_POINT('Ctrl Pts',(8.24027055552775,-2.18440736622039,10.645072809239));
#24763=CARTESIAN_POINT('Ctrl Pts',(4.67212920832948,-4.36374605926514,10.8435889266506));
#24764=CARTESIAN_POINT('Ctrl Pts',(0.906490441907856,-2.54684911848653,
11.0421050440623));
#24765=CARTESIAN_POINT('Ctrl Pts',(0.391854608507251,1.60240379879482,11.2406211614739));
#24766=CARTESIAN_POINT('Ctrl Pts',(3.59951541494433,4.28420579809219,11.4391372788856));
#24767=CARTESIAN_POINT('Ctrl Pts',(7.59195811086242,3.04261362173219,11.6376533962972));
#24768=CARTESIAN_POINT('Ctrl Pts',(8.71297961965247,-0.98534623276214,11.8361695137089));
#24769=CARTESIAN_POINT('Ctrl Pts',(5.93596976765481,-4.11094475056566,12.0346856311206));
#24770=CARTESIAN_POINT('Ctrl Pts',(1.80406135300024,-3.47181826426207,12.2332017485322));
#24771=CARTESIAN_POINT('Ctrl Pts',(0.101177504597399,0.346733347466743,
12.4317178659439));
#24772=CARTESIAN_POINT('Ctrl Pts',(2.38678685852808,3.84775315515312,12.6302339833555));
#24773=CARTESIAN_POINT('Ctrl Pts',(6.56777184536255,3.82507381537617,12.8287501007672));
#24774=CARTESIAN_POINT('Ctrl Pts',(8.81526594492522,0.29946463609684,13.0272662181788));
#24775=CARTESIAN_POINT('Ctrl Pts',(7.07105681270762,-3.5003885604986,13.2257823355905));
#24776=CARTESIAN_POINT('Ctrl Pts',(2.93245799361878,-4.09465249784007,13.4242984530022));
#24777=CARTESIAN_POINT('Ctrl Pts',(0.189519561683291,-0.939111566208993,
13.6228145704138));
#24778=CARTESIAN_POINT('Ctrl Pts',(1.35417235664619,3.07644987396012,13.8213306878255));
#24779=CARTESIAN_POINT('Ctrl Pts',(5.3598495029257,4.27465703983832,14.0198468052371));
#24780=CARTESIAN_POINT('Ctrl Pts',(8.53822806601778,1.55821460123144,14.2183629226488));
#24781=CARTESIAN_POINT('Ctrl Pts',(7.97860941701375,-2.58521112879858,14.4168790400604));
#24782=CARTESIAN_POINT('Ctrl Pts',(4.19348166959603,-4.36114968300486,14.6153951574721));
#24783=CARTESIAN_POINT('Ctrl Pts',(0.649192814085452,-2.14323031537866,
14.8139112748837));
#24784=CARTESIAN_POINT('Ctrl Pts',(0.59153516483578,2.03741860650786,15.0124273922954));
#24785=CARTESIAN_POINT('Ctrl Pts',(4.07331050026509,4.35223832436584,15.2109435097071));
#24786=CARTESIAN_POINT('Ctrl Pts',(7.9059751985768,2.68136097312093,15.4094596271187));
#24787=CARTESIAN_POINT('Ctrl Pts',(8.57964783407003,-1.44505575241412,15.6079757445304));
#24788=CARTESIAN_POINT('Ctrl Pts',(5.47739182177246,-4.24811790776339,15.806491861942));
#24789=CARTESIAN_POINT('Ctrl Pts',(1.44019420657955,-3.16083449095397,16.0050079793537));
#24790=CARTESIAN_POINT('Ctrl Pts',(0.165243768843413,0.821081027223728,
16.2035240967653));
#24791=CARTESIAN_POINT('Ctrl Pts',(2.82011586731386,4.05106615928717,16.402040214177));
#24792=CARTESIAN_POINT('Ctrl Pts',(6.97352913523386,3.57116196212476,16.6005563315886));
#24793=CARTESIAN_POINT('Ctrl Pts',(8.82186670813997,-0.17914442924803,16.7990724490003));
#24794=CARTESIAN_POINT('Ctrl Pts',(6.67245619587356,-3.76539376000376,16.997588566412));
#24795=CARTESIAN_POINT('Ctrl Pts',(2.49368685944485,-3.90336711073225,17.1961046838236));
#24796=CARTESIAN_POINT('Ctrl Pts',(0.112396168534027,-0.466711111367439,
17.3946208012353));
#24797=CARTESIAN_POINT('Ctrl Pts',(1.70932484092508,3.39735004600064,17.5931369186469));
#24798=CARTESIAN_POINT('Ctrl Pts',(5.82203597524696,4.15018265569229,17.7916530360586));
#24799=CARTESIAN_POINT('Ctrl Pts',(8.68418694674809,1.10235693414467,17.9901691534703));
#24800=CARTESIAN_POINT('Ctrl Pts',(7.67467433961344,-2.9549862986379,18.1886852708819));
#24801=CARTESIAN_POINT('Ctrl Pts',(3.71799059648846,-4.30620928893205,18.3872013882936));
#24802=CARTESIAN_POINT('Ctrl Pts',(0.437591425226463,-1.7138877251997,18.5857175057052));
#24803=CARTESIAN_POINT('Ctrl Pts',(0.837603987051035,2.44797961565228,18.7842336231169));
#24804=CARTESIAN_POINT('Ctrl Pts',(4.55170438690705,4.36803379003202,18.9827497405285));
#24805=CARTESIAN_POINT('Ctrl Pts',(8.17859012825258,2.28792570825151,19.1812658579402));
#24806=CARTESIAN_POINT('Ctrl Pts',(8.39682823991214,-1.88742121606535,19.3797819753518));
#24807=CARTESIAN_POINT('Ctrl Pts',(5.0065604104293,-4.33430369349561,19.5782980927635));
#24808=CARTESIAN_POINT('Ctrl Pts',(1.11252942855707,-2.81191329518458,19.7768142101752));
#24809=CARTESIAN_POINT('Ctrl Pts',(0.280814794700937,1.28557380975688,19.9753303275868));
#24810=CARTESIAN_POINT('Ctrl Pts',(3.27308495055695,4.20575687553525,20.1738464449984));
#24811=CARTESIAN_POINT('Ctrl Pts',(7.34907580467911,3.27438779359847,20.3723625624101));
#24812=CARTESIAN_POINT('Ctrl Pts',(8.77607246974106,-0.65560333835151,20.5708786798217));
#24813=CARTESIAN_POINT('Ctrl Pts',(6.24725853788356,-3.98520541525919,20.7693947972334));
#24814=CARTESIAN_POINT('Ctrl Pts',(2.07847371693811,-3.66523215780504,20.9679109146451));
#24815=CARTESIAN_POINT('Ctrl Pts',(0.0874118238771355,0.0112909480203034,
21.1664270320568));
#24816=CARTESIAN_POINT('Ctrl Pts',(2.09744951113826,3.6774740982752,21.3649431494684));
#24817=CARTESIAN_POINT('Ctrl Pts',(6.26783241381338,3.97589626917586,21.56345926688));
#24818=CARTESIAN_POINT('Ctrl Pts',(8.77940336342984,0.633268559987037,21.7619753842917));
#24819=CARTESIAN_POINT('Ctrl Pts',(7.33211314362288,-3.28929501353682,21.9604915017033));
#24820=CARTESIAN_POINT('Ctrl Pts',(3.25136321302202,-4.1995837027451,22.159007619115));
#24821=CARTESIAN_POINT('Ctrl Pts',(0.274225572405194,-1.26397559254583,
22.3575237365266));
#24822=CARTESIAN_POINT('Ctrl Pts',(1.12710846943813,2.82916129353447,22.5560398539383));
#24823=CARTESIAN_POINT('Ctrl Pts',(5.0289536987851,4.33139846700858,22.75455597135));
#24824=CARTESIAN_POINT('Ctrl Pts',(8.40653381239982,1.86703792222437,22.9530720887616));
#24825=CARTESIAN_POINT('Ctrl Pts',(8.1667094807393,-2.30714844669435,23.1515882061733));
#24826=CARTESIAN_POINT('Ctrl Pts',(4.52913739170739,-4.36843844023836,23.3501043235849));
#24827=CARTESIAN_POINT('Ctrl Pts',(0.824979095953012,-2.42929861537115,
23.5486204409966));
#24828=CARTESIAN_POINT('Ctrl Pts',(0.44654309475883,1.73474421227166,23.7471365584082));
#24829=CARTESIAN_POINT('Ctrl Pts',(3.74018140704413,4.30976245591016,23.9456526758199));
#24830=CARTESIAN_POINT('Ctrl Pts',(7.69005018696339,2.93870878051704,24.1441687932315));
#24831=CARTESIAN_POINT('Ctrl Pts',(8.67815324699032,-1.12495244308866,24.3426849106432));
#24832=CARTESIAN_POINT('Ctrl Pts',(5.80110407974766,-4.15572474791461,24.5412010280549));
#24833=CARTESIAN_POINT('Ctrl Pts',(1.69076667459873,-3.38595255220879,24.7397171454665));
#24834=CARTESIAN_POINT('Ctrl Pts',(0.116906044416222,0.495033780363739,
24.9382332628782));
#24835=CARTESIAN_POINT('Ctrl Pts',(1.71188963858453,2.76408782845127,25.0705773411526));
#24836=CARTESIAN_POINT('Ctrl Pts',(2.81308617627174,3.31070484176046,25.1367493802898));
#24837=CARTESIAN_POINT('Ctrl Pts',(2.45096789438968,-2.81528236653118,-0.135126215077433));
#24838=CARTESIAN_POINT('Ctrl Pts',(1.5138871719268,-2.14781538060387,-0.0689100650381678));
#24839=CARTESIAN_POINT('Ctrl Pts',(0.375608982507884,0.184245982096433,
0.0634781241383155));
#24840=CARTESIAN_POINT('Ctrl Pts',(2.40361795610193,3.53582435220265,0.262038352452016));
#24841=CARTESIAN_POINT('Ctrl Pts',(6.31301191404873,3.63844533219021,0.460554469863673));
#24842=CARTESIAN_POINT('Ctrl Pts',(8.52123531017291,0.41411968753004,0.659070587275328));
#24843=CARTESIAN_POINT('Ctrl Pts',(7.00753704968407,-3.19206842901602,0.857586704686986));
#24844=CARTESIAN_POINT('Ctrl Pts',(3.15735122024546,-3.87365781783563,1.05610282209864));
#24845=CARTESIAN_POINT('Ctrl Pts',(0.497012637108953,-1.00853559461836,
1.25461893951029));
#24846=CARTESIAN_POINT('Ctrl Pts',(1.46259607175817,2.78055482024318,1.45313505692195));
#24847=CARTESIAN_POINT('Ctrl Pts',(5.16994949606116,4.02307283767128,1.6516511743336));
#24848=CARTESIAN_POINT('Ctrl Pts',(8.22389132840824,1.58143801444312,1.85016729174526));
#24849=CARTESIAN_POINT('Ctrl Pts',(7.82770989036406,-2.30850019028058,2.04868340915692));
#24850=CARTESIAN_POINT('Ctrl Pts',(4.34420487984554,-4.08433044095169,2.24719952656857));
#24851=CARTESIAN_POINT('Ctrl Pts',(0.963512123078899,-2.11982284980964,
2.44571564398023));
#24852=CARTESIAN_POINT('Ctrl Pts',(0.781601462709117,1.78598563226962,2.64423176139188));
#24853=CARTESIAN_POINT('Ctrl Pts',(3.96506545115642,4.05621856135326,2.84274787880354));
#24854=CARTESIAN_POINT('Ctrl Pts',(7.59854716087849,2.61184571475234,3.0412639962152));
#24855=CARTESIAN_POINT('Ctrl Pts',(8.35457376462735,-1.22440681097471,3.23978011362686));
#24856=CARTESIAN_POINT('Ctrl Pts',(5.54079016364776,-3.93937031917242,3.43829623103851));
#24857=CARTESIAN_POINT('Ctrl Pts',(1.7340060207583,-3.04673371102089,3.63681234845017));
#24858=CARTESIAN_POINT('Ctrl Pts',(0.420401755326215,0.636043824414959,
3.83532846586182));
#24859=CARTESIAN_POINT('Ctrl Pts',(2.8029512110655,3.73634444619894,4.03384458327349));
#24860=CARTESIAN_POINT('Ctrl Pts',(6.6997608939274,3.41497193768155,4.23236070068513));
#24861=CARTESIAN_POINT('Ctrl Pts',(8.54220663371807,-0.0337669329441494,
4.4308768180968));
#24862=CARTESIAN_POINT('Ctrl Pts',(6.64301166261426,-3.45158267762228,4.62939293550844));
#24863=CARTESIAN_POINT('Ctrl Pts',(2.74142261194879,-3.70850466797209,4.82790905292011));
#24864=CARTESIAN_POINT('Ctrl Pts',(0.410440516499291,-0.569248623621048,
5.02642517033176));
#24865=CARTESIAN_POINT('Ctrl Pts',(1.78473444019877,3.09131448041513,5.22494128774342));
#24866=CARTESIAN_POINT('Ctrl Pts',(5.60575214909559,3.92091058714242,5.42345740515506));
#24867=CARTESIAN_POINT('Ctrl Pts',(8.37427830909092,1.15981136136555,5.62197352256674));
#24868=CARTESIAN_POINT('Ctrl Pts',(7.55494932568486,-2.66342104697584,5.82048963997839));
#24869=CARTESIAN_POINT('Ctrl Pts',(3.89809109665752,-4.04754312425325,6.01900575739004));
#24870=CARTESIAN_POINT('Ctrl Pts',(0.752584827297987,-1.72500220071308,
6.21752187480171));
#24871=CARTESIAN_POINT('Ctrl Pts',(0.999025325230166,2.17726292518741,6.41603799221334));
#24872=CARTESIAN_POINT('Ctrl Pts',(4.41172707023364,4.08563208015006,6.61455410962502));
#24873=CARTESIAN_POINT('Ctrl Pts',(7.86540272070975,2.25245709306557,6.81307022703666));
#24874=CARTESIAN_POINT('Ctrl Pts',(8.1972418118268,-1.64347525356681,7.01158634444832));
#24875=CARTESIAN_POINT('Ctrl Pts',(5.10335241618994,-4.03434422519923,7.21010246185998));
#24876=CARTESIAN_POINT('Ctrl Pts',(1.4170595903061,-2.73063749675737,7.40861857927163));
#24877=CARTESIAN_POINT('Ctrl Pts',(0.514200183395272,1.07373510898141,7.60713469668328));
#24878=CARTESIAN_POINT('Ctrl Pts',(3.22159566609925,3.89480152652282,7.80565081409495));
#24879=CARTESIAN_POINT('Ctrl Pts',(7.05986475548066,3.14908279305528,8.0041669315066));
#24880=CARTESIAN_POINT('Ctrl Pts',(8.51399363110384,-0.480506060385796,
8.20268304891826));
#24881=CARTESIAN_POINT('Ctrl Pts',(6.25231872913724,-3.67005660392007,8.40119916632992));
#24882=CARTESIAN_POINT('Ctrl Pts',(2.34603890318347,-3.49863912146337,8.59971528374156));
#24883=CARTESIAN_POINT('Ctrl Pts',(0.372450912529775,-0.123234482743352,
8.79823140115322));
#24884=CARTESIAN_POINT('Ctrl Pts',(2.13892909739252,3.36502595110463,8.99674751856487));
#24885=CARTESIAN_POINT('Ctrl Pts',(6.02776633805246,3.77165962851178,9.19526363597655));
#24886=CARTESIAN_POINT('Ctrl Pts',(8.47763946304124,0.72427916270141,9.39377975338818));
#24887=CARTESIAN_POINT('Ctrl Pts',(7.24500126602242,-2.98638238306039,9.59229587079984));
#24888=CARTESIAN_POINT('Ctrl Pts',(3.45867836056103,-3.9621717494319,9.79081198821151));
#24889=CARTESIAN_POINT('Ctrl Pts',(0.586113239980029,-1.30947959617202,
9.98932810562315));
#24890=CARTESIAN_POINT('Ctrl Pts',(1.25794639972494,2.54240906231909,10.1878442230349));
#24891=CARTESIAN_POINT('Ctrl Pts',(4.85892581172318,4.06600786328675,10.3863603404465));
#24892=CARTESIAN_POINT('Ctrl Pts',(8.09134302835829,1.86603400672705,10.5848764578582));
#24893=CARTESIAN_POINT('Ctrl Pts',(7.99501184973105,-2.04281829746266,10.7833925752698));
#24894=CARTESIAN_POINT('Ctrl Pts',(4.658150536815,-4.08089646336047,10.9819086926815));
#24895=CARTESIAN_POINT('Ctrl Pts',(1.13659320614603,-2.38176727499459,11.1804248100931));
#24896=CARTESIAN_POINT('Ctrl Pts',(0.655315074027438,1.49853907779376,11.3789409275048));
#24897=CARTESIAN_POINT('Ctrl Pts',(3.6550614989726,4.00651184837438,11.5774570449165));
#24898=CARTESIAN_POINT('Ctrl Pts',(7.38872176624422,2.84539728015019,11.7759731623281));
#24899=CARTESIAN_POINT('Ctrl Pts',(8.43708082482397,-0.921477992040132,
11.9744892797398));
#24900=CARTESIAN_POINT('Ctrl Pts',(5.84007139076835,-3.84448124749012,12.1730053971514));
#24901=CARTESIAN_POINT('Ctrl Pts',(1.97598530342792,-3.24678170627628,12.3715215145631));
#24902=CARTESIAN_POINT('Ctrl Pts',(0.383479098877827,0.324258761208613,
12.5700376319747));
#24903=CARTESIAN_POINT('Ctrl Pts',(2.52093966656498,3.59834922323431,12.7685537493864));
#24904=CARTESIAN_POINT('Ctrl Pts',(6.43092127741269,3.5771399144821,12.967069866798));
#24905=CARTESIAN_POINT('Ctrl Pts',(8.53273714794332,0.280053916463419,13.1655859842097));
#24906=CARTESIAN_POINT('Ctrl Pts',(6.90158428470204,-3.27350013106212,13.3641021016213));
#24907=CARTESIAN_POINT('Ctrl Pts',(3.0312414520278,-3.82924502713605,13.562618219033));
#24908=CARTESIAN_POINT('Ctrl Pts',(0.466094994356506,-0.878240167322765,
13.7611343364446));
#24909=CARTESIAN_POINT('Ctrl Pts',(1.55525724336407,2.87704033182534,13.9596504538563));
#24910=CARTESIAN_POINT('Ctrl Pts',(5.30129412947213,3.99758202219787,14.1581665712679));
#24911=CARTESIAN_POINT('Ctrl Pts',(8.27365632956023,1.45721413871475,14.3566826886797));
#24912=CARTESIAN_POINT('Ctrl Pts',(7.75031108111198,-2.41764273385123,14.5551988060912));
#24913=CARTESIAN_POINT('Ctrl Pts',(4.21052800757405,-4.07846837919741,14.753714923503));
#24914=CARTESIAN_POINT('Ctrl Pts',(0.895973113878727,-2.00431026356939,
14.9522310409146));
#24915=CARTESIAN_POINT('Ctrl Pts',(0.842052722152676,1.9053570654116,15.1507471583263));
#24916=CARTESIAN_POINT('Ctrl Pts',(4.09814610146403,4.07013463762311,15.3492632757379));
#24917=CARTESIAN_POINT('Ctrl Pts',(7.682384872503,2.50756033086961,15.5477793931496));
#24918=CARTESIAN_POINT('Ctrl Pts',(8.31239134820293,-1.35139002803904,15.7462955105612));
#24919=CARTESIAN_POINT('Ctrl Pts',(5.41121758211169,-3.97276310543362,15.9448116279729));
#24920=CARTESIAN_POINT('Ctrl Pts',(1.63570332303896,-2.95595530083938,16.1433277453845));
#24921=CARTESIAN_POINT('Ctrl Pts',(0.443392711547191,0.767860140031627,
16.3418438627962));
#24922=CARTESIAN_POINT('Ctrl Pts',(2.92618112548781,3.7884838709103,16.5403599802078));
#24923=CARTESIAN_POINT('Ctrl Pts',(6.8103781630174,3.33968613741389,16.7388760976195));
#24924=CARTESIAN_POINT('Ctrl Pts',(8.5389100624284,-0.167532633159739,16.9373922150311));
#24925=CARTESIAN_POINT('Ctrl Pts',(6.52882019040339,-3.5213282050942,17.1359083324428));
#24926=CARTESIAN_POINT('Ctrl Pts',(2.62091061577914,-3.65035838956845,17.3344244498544));
#24927=CARTESIAN_POINT('Ctrl Pts',(0.393970590674286,-0.43645979805503,
17.5329405672661));
#24928=CARTESIAN_POINT('Ctrl Pts',(1.88738942918871,3.17714037417117,17.7314566846778));
#24929=CARTESIAN_POINT('Ctrl Pts',(5.73352256684974,3.8811758273502,17.9299728020894));
#24930=CARTESIAN_POINT('Ctrl Pts',(8.41015443739666,1.03090428563328,18.1284889195011));
#24931=CARTESIAN_POINT('Ctrl Pts',(7.46607648872073,-2.76344979098553,18.3270050369127));
#24932=CARTESIAN_POINT('Ctrl Pts',(3.76585734795025,-4.02708911541293,18.5255211543244));
#24933=CARTESIAN_POINT('Ctrl Pts',(0.698087318576006,-1.60279683129456,
18.724037271736));
#24934=CARTESIAN_POINT('Ctrl Pts',(1.07217183831651,2.28930630247911,18.9225533891477));
#24935=CARTESIAN_POINT('Ctrl Pts',(4.54553141985243,4.08490627169594,19.1210695065593));
#24936=CARTESIAN_POINT('Ctrl Pts',(7.93732942868568,2.13962678039228,19.319585623971));
#24937=CARTESIAN_POINT('Ctrl Pts',(8.14142176722837,-1.76508221626667,19.5181017413827));
#24938=CARTESIAN_POINT('Ctrl Pts',(4.97090455397163,-4.05336249490537,19.7166178587943));
#24939=CARTESIAN_POINT('Ctrl Pts',(1.3292771434127,-2.62965050343175,19.915133976206));
#24940=CARTESIAN_POINT('Ctrl Pts',(0.551472646603815,1.20224539704524,20.1136500936177));
#24941=CARTESIAN_POINT('Ctrl Pts',(3.3497896271543,3.93314783354192,20.3121662110293));
#24942=CARTESIAN_POINT('Ctrl Pts',(7.16158262229433,3.06214829760668,20.510682328441));
#24943=CARTESIAN_POINT('Ctrl Pts',(8.49608411816253,-0.613108395518473,
20.7091984458526));
#24944=CARTESIAN_POINT('Ctrl Pts',(6.13118302381429,-3.72689209317441,20.9077145632643));
#24945=CARTESIAN_POINT('Ctrl Pts',(2.23261078765349,-3.42765888460072,21.1062306806759));
#24946=CARTESIAN_POINT('Ctrl Pts',(0.370605683008962,0.0105590905653954,
21.3047467980876));
#24947=CARTESIAN_POINT('Ctrl Pts',(2.250356607504,3.43910732612115,21.5032629154992));
#24948=CARTESIAN_POINT('Ctrl Pts',(6.15042334082164,3.71818634797007,21.7017790329109));
#24949=CARTESIAN_POINT('Ctrl Pts',(8.49919910975228,0.592221314373082,21.9002951503225));
#24950=CARTESIAN_POINT('Ctrl Pts',(7.14571944818345,-3.07608926032515,22.0988112677342));
#24951=CARTESIAN_POINT('Ctrl Pts',(3.32947585071529,-3.92737479389549,22.2973273851459));
#24952=CARTESIAN_POINT('Ctrl Pts',(0.545310524977601,-1.18204713458114,
22.4958435025575));
#24953=CARTESIAN_POINT('Ctrl Pts',(1.34291119900688,2.64578051982372,22.6943596199692));
#24954=CARTESIAN_POINT('Ctrl Pts',(4.99184635260365,4.05064557959106,22.8928757373808));
#24955=CARTESIAN_POINT('Ctrl Pts',(8.15049824324278,1.74602012818506,23.0913918547925));
#24956=CARTESIAN_POINT('Ctrl Pts',(7.92621886181009,-2.15760353803636,23.2899079722041));
#24957=CARTESIAN_POINT('Ctrl Pts',(4.52442717371885,-4.08528469325705,23.4884240896158));
#24958=CARTESIAN_POINT('Ctrl Pts',(1.06036526828869,-2.27183616857484,23.6869402070274));
#24959=CARTESIAN_POINT('Ctrl Pts',(0.706458758169362,1.62230144113535,23.8854563244391));
#24960=CARTESIAN_POINT('Ctrl Pts',(3.78660979300229,4.03041197296648,24.0839724418507));
#24961=CARTESIAN_POINT('Ctrl Pts',(7.48045570332662,2.74822735016753,24.2824885592624));
#24962=CARTESIAN_POINT('Ctrl Pts',(8.40451183040988,-1.05203519730533,24.481004676674));
#24963=CARTESIAN_POINT('Ctrl Pts',(5.71394743641032,-3.88635869185298,24.6795207940858));
#24964=CARTESIAN_POINT('Ctrl Pts',(1.87003416737941,-3.16648164392546,24.8780369114974));
#24965=CARTESIAN_POINT('Ctrl Pts',(0.398188145107553,0.462946646320358,
25.076553028909));
#24966=CARTESIAN_POINT('Ctrl Pts',(1.88978798161488,2.58492499113116,25.2088971071835));
#24967=CARTESIAN_POINT('Ctrl Pts',(2.91960708544911,3.09611134481228,25.2750691463207));
#24968=CARTESIAN_POINT('Ctrl Pts',(2.58997049159961,-2.62015330925654,0.00319355095334283));
#24969=CARTESIAN_POINT('Ctrl Pts',(1.71783944528228,-1.99894889552244,0.0694097009926075));
#24970=CARTESIAN_POINT('Ctrl Pts',(0.65845605968771,0.171475772890977,0.20179789016909));
#24971=CARTESIAN_POINT('Ctrl Pts',(2.5459024084217,3.29075405988094,0.400358118482792));
#24972=CARTESIAN_POINT('Ctrl Pts',(6.18433372098768,3.38626231280436,0.598874235894448));
#24973=CARTESIAN_POINT('Ctrl Pts',(8.23950371306965,0.385416781850904,0.797390353306103));
#24974=CARTESIAN_POINT('Ctrl Pts',(6.83072086642306,-2.97082408396747,0.995906470717762));
#24975=CARTESIAN_POINT('Ctrl Pts',(3.24739392835603,-3.60517206763711,1.19442258812942));
#24976=CARTESIAN_POINT('Ctrl Pts',(0.771445147794971,-0.938633334672633,
1.39293870554108));
#24977=CARTESIAN_POINT('Ctrl Pts',(1.6701033647243,2.58783275185508,1.59145482295273));
#24978=CARTESIAN_POINT('Ctrl Pts',(5.12049770482736,3.74423103498232,1.78997094036439));
#24979=CARTESIAN_POINT('Ctrl Pts',(7.96276883664299,1.47182751406662,1.98848705777604));
#24980=CARTESIAN_POINT('Ctrl Pts',(7.59404699250464,-2.14849653622342,2.1870031751877));
#24981=CARTESIAN_POINT('Ctrl Pts',(4.35198598660702,-3.80124283382013,2.38551929259936));
#24982=CARTESIAN_POINT('Ctrl Pts',(1.20561125008781,-1.97289654529749,2.58403541001101));
#24983=CARTESIAN_POINT('Ctrl Pts',(1.0363089362513,1.66219780307218,2.78255152742267));
#24984=CARTESIAN_POINT('Ctrl Pts',(3.99912495903867,3.77507940693446,2.98106764483432));
#24985=CARTESIAN_POINT('Ctrl Pts',(7.38076768128599,2.43081698451723,3.17958376224598));
#24986=CARTESIAN_POINT('Ctrl Pts',(8.08439358796167,-1.13954237620741,3.37809987965763));
#24987=CARTESIAN_POINT('Ctrl Pts',(5.4656351638386,-3.66632999264102,3.5766159970693));
#24988=CARTESIAN_POINT('Ctrl Pts',(1.92270171311447,-2.83556261008053,3.77513211448094));
#24989=CARTESIAN_POINT('Ctrl Pts',(0.700144216203009,0.591959212043988,
3.97364823189261));
#24990=CARTESIAN_POINT('Ctrl Pts',(2.91755761499276,3.47737597536012,4.17216434930425));
#24991=CARTESIAN_POINT('Ctrl Pts',(6.54427687678886,3.1782780050441,4.37068046671592));
#24992=CARTESIAN_POINT('Ctrl Pts',(8.2590215005,-0.0314265247951463,4.56919658412757));
#24993=CARTESIAN_POINT('Ctrl Pts',(6.49146097171637,-3.21235123071783,4.76771270153922));
#24994=CARTESIAN_POINT('Ctrl Pts',(2.86029360321679,-3.45146579032245,4.96622881895089));
#24995=CARTESIAN_POINT('Ctrl Pts',(0.690873397337037,-0.529793630188544,
5.16474493636253));
#24996=CARTESIAN_POINT('Ctrl Pts',(1.96991411271267,2.8770534572674,5.36326105377419));
#24997=CARTESIAN_POINT('Ctrl Pts',(5.52609459169944,3.64914971667956,5.56177717118585));
#24998=CARTESIAN_POINT('Ctrl Pts',(8.1027323975949,1.07942407934716,5.7602932885975));
#24999=CARTESIAN_POINT('Ctrl Pts',(7.34019164048911,-2.47881759682101,5.95880940600916));
#25000=CARTESIAN_POINT('Ctrl Pts',(3.93679264073839,-3.76700527003896,6.15732552342081));
#25001=CARTESIAN_POINT('Ctrl Pts',(1.00930346276847,-1.60544117293717,6.35584164083248));
#25002=CARTESIAN_POINT('Ctrl Pts',(1.23866300903221,2.02635541158186,6.55435775824412));
#25003=CARTESIAN_POINT('Ctrl Pts',(4.41482816993367,3.80245425555658,6.75287387565579));
#25004=CARTESIAN_POINT('Ctrl Pts',(7.6291273081915,2.09633782263408,6.95138999306744));
#25005=CARTESIAN_POINT('Ctrl Pts',(7.93796641543966,-1.5295649116789,7.14990611047909));
#25006=CARTESIAN_POINT('Ctrl Pts',(5.05851651200422,-3.75472119528823,7.34842222789076));
#25007=CARTESIAN_POINT('Ctrl Pts',(1.62772304650576,-2.54137523062185,7.5469383453024));
#25008=CARTESIAN_POINT('Ctrl Pts',(0.787441414036509,0.999313828164636,
7.74545446271406));
#25009=CARTESIAN_POINT('Ctrl Pts',(3.30718554976015,3.62485029208286,7.94397058012572));
#25010=CARTESIAN_POINT('Ctrl Pts',(6.8794217047968,2.93081781047529,8.14248669753737));
#25011=CARTESIAN_POINT('Ctrl Pts',(8.23276395950072,-0.447201871899268,
8.34100281494903));
#25012=CARTESIAN_POINT('Ctrl Pts',(6.12784722031342,-3.41568258667014,8.53951893236069));
#25013=CARTESIAN_POINT('Ctrl Pts',(2.49231419722064,-3.25614616174064,8.73803504977233));
#25014=CARTESIAN_POINT('Ctrl Pts',(0.655516877599837,-0.114693020356707,
8.93655116718401));
#25015=CARTESIAN_POINT('Ctrl Pts',(2.29955930716991,3.13179380737736,9.13506728459565));
#25016=CARTESIAN_POINT('Ctrl Pts',(5.9188587019336,3.51024343935022,9.33358340200731));
#25017=CARTESIAN_POINT('Ctrl Pts',(8.19892952254092,0.674078901476532,9.53209951941897));
#25018=CARTESIAN_POINT('Ctrl Pts',(7.05172628302556,-2.77939427202906,9.73061563683061));
#25019=CARTESIAN_POINT('Ctrl Pts',(3.52783588801619,-3.68755104089551,9.92913175424228));
#25020=CARTESIAN_POINT('Ctrl Pts',(0.854370129759403,-1.21871871116838,
10.1276478716539));
#25021=CARTESIAN_POINT('Ctrl Pts',(1.47963809495571,2.36619303175871,10.3261639890656));
#25022=CARTESIAN_POINT('Ctrl Pts',(4.83103127493619,3.78419020596524,10.5246801064772));
#25023=CARTESIAN_POINT('Ctrl Pts',(7.83940754573271,1.73669797247918,10.7231962238889));
#25024=CARTESIAN_POINT('Ctrl Pts',(7.74975314393437,-1.90122922870495,10.9217123413006));
#25025=CARTESIAN_POINT('Ctrl Pts',(4.64417186530054,-3.79804686745578,11.1202284587122));
#25026=CARTESIAN_POINT('Ctrl Pts',(1.36669597038421,-2.21668543150265,11.3187445761239));
#25027=CARTESIAN_POINT('Ctrl Pts',(0.91877553954763,1.39467435679268,11.5172606935355));
#25028=CARTESIAN_POINT('Ctrl Pts',(3.71060758300086,3.72881789865659,11.7157768109472));
#25029=CARTESIAN_POINT('Ctrl Pts',(7.18548542162604,2.64818093856821,11.9142929283589));
#25030=CARTESIAN_POINT('Ctrl Pts',(8.16118202999545,-0.857609751318129,
12.1128090457705));
#25031=CARTESIAN_POINT('Ctrl Pts',(5.74417301388192,-3.57801774441457,12.3113251631822));
#25032=CARTESIAN_POINT('Ctrl Pts',(2.14790925385559,-3.02174514829049,12.5098412805938));
#25033=CARTESIAN_POINT('Ctrl Pts',(0.665780693158256,0.301784174950485,
12.7083573980055));
#25034=CARTESIAN_POINT('Ctrl Pts',(2.65509247460188,3.34894529131551,12.9068735154171));
#25035=CARTESIAN_POINT('Ctrl Pts',(6.29407070946287,3.32920601358802,13.1053896328288));
#25036=CARTESIAN_POINT('Ctrl Pts',(8.25020835096136,0.260643196829997,13.3039057502404));
#25037=CARTESIAN_POINT('Ctrl Pts',(6.7321117566965,-3.04661170162563,13.5024218676521));
#25038=CARTESIAN_POINT('Ctrl Pts',(3.1300249104368,-3.56383755643203,13.7009379850637));
#25039=CARTESIAN_POINT('Ctrl Pts',(0.742670427029733,-0.817368768436538,
13.8994541024754));
#25040=CARTESIAN_POINT('Ctrl Pts',(1.75634213008195,2.67763078969056,14.0979702198871));
#25041=CARTESIAN_POINT('Ctrl Pts',(5.24273875601857,3.7205070045574,14.2964863372987));
#25042=CARTESIAN_POINT('Ctrl Pts',(8.0090845931027,1.35621367619806,14.4950024547104));
#25043=CARTESIAN_POINT('Ctrl Pts',(7.52201274521021,-2.25007433890389,14.693518572122));
#25044=CARTESIAN_POINT('Ctrl Pts',(4.22757434555207,-3.79578707538995,14.8920346895337));
#25045=CARTESIAN_POINT('Ctrl Pts',(1.14275341367199,-1.86539021176013,15.0905508069453));
#25046=CARTESIAN_POINT('Ctrl Pts',(1.09257027946957,1.77329552431533,15.289066924357));
#25047=CARTESIAN_POINT('Ctrl Pts',(4.12298170266298,3.78803095088039,15.4875830417686));
#25048=CARTESIAN_POINT('Ctrl Pts',(7.45879454642923,2.3337596886183,15.6860991591803));
#25049=CARTESIAN_POINT('Ctrl Pts',(8.04513486233581,-1.25772430366396,15.8846152765919));
#25050=CARTESIAN_POINT('Ctrl Pts',(5.34504334245093,-3.69740830310385,16.0831313940036));
#25051=CARTESIAN_POINT('Ctrl Pts',(1.83121243949837,-2.75107611072479,16.2816475114153));
#25052=CARTESIAN_POINT('Ctrl Pts',(0.721541654250978,0.714639252839528,
16.4801636288269));
#25053=CARTESIAN_POINT('Ctrl Pts',(3.03224638366176,3.52590158253341,16.6786797462386));
#25054=CARTESIAN_POINT('Ctrl Pts',(6.64722719080097,3.10821031270302,16.8771958636502));
#25055=CARTESIAN_POINT('Ctrl Pts',(8.25595341671681,-0.155920837071448,
17.0757119810619));
#25056=CARTESIAN_POINT('Ctrl Pts',(6.38518418493321,-3.27726265018464,17.2742280984735));
#25057=CARTESIAN_POINT('Ctrl Pts',(2.74813437211341,-3.39734966840464,17.4727442158852));
#25058=CARTESIAN_POINT('Ctrl Pts',(0.675545012814546,-0.406208484742623,
17.6712603332969));
#25059=CARTESIAN_POINT('Ctrl Pts',(2.06545401745235,2.9569307023417,17.8697764507085));
#25060=CARTESIAN_POINT('Ctrl Pts',(5.64500915845253,3.61216899900811,18.0682925681202));
#25061=CARTESIAN_POINT('Ctrl Pts',(8.13612192804524,0.959451637121888,18.2668086855318));
#25062=CARTESIAN_POINT('Ctrl Pts',(7.25747863782803,-2.57191328333314,18.4653248029435));
#25063=CARTESIAN_POINT('Ctrl Pts',(3.81372409941205,-3.74796894189382,18.6638409203551));
#25064=CARTESIAN_POINT('Ctrl Pts',(0.958583211925542,-1.49170593738941,
18.8623570377668));
#25065=CARTESIAN_POINT('Ctrl Pts',(1.306739689582,2.13063298930591,19.0608731551785));
#25066=CARTESIAN_POINT('Ctrl Pts',(4.53935845279781,3.80177875335989,19.2593892725901));
#25067=CARTESIAN_POINT('Ctrl Pts',(7.69606872911877,1.99132785253305,19.4579053900018));
#25068=CARTESIAN_POINT('Ctrl Pts',(7.88601529454458,-1.64274321646801,19.6564215074134));
#25069=CARTESIAN_POINT('Ctrl Pts',(4.93524869751396,-3.77242129631514,19.8549376248251));
#25070=CARTESIAN_POINT('Ctrl Pts',(1.54602485826833,-2.44738771167893,20.0534537422367));
#25071=CARTESIAN_POINT('Ctrl Pts',(0.822130498506685,1.11891698433359,20.2519698596484));
#25072=CARTESIAN_POINT('Ctrl Pts',(3.42649430375165,3.66053879154859,20.45048597706));
#25073=CARTESIAN_POINT('Ctrl Pts',(6.97408943990954,2.84990880161489,20.6490020944717));
#25074=CARTESIAN_POINT('Ctrl Pts',(8.21609576658401,-0.570613452685432,
20.8475182118833));
#25075=CARTESIAN_POINT('Ctrl Pts',(6.015107509745,-3.46857877108964,21.046034329295));
#25076=CARTESIAN_POINT('Ctrl Pts',(2.38674785836889,-3.19008561139642,21.2445504467067));
#25077=CARTESIAN_POINT('Ctrl Pts',(0.653799542140776,0.00982723311048271,
21.4430665641183));
#25078=CARTESIAN_POINT('Ctrl Pts',(2.40326370386975,3.2007405539671,21.64158268153));
#25079=CARTESIAN_POINT('Ctrl Pts',(6.03301426782987,3.46047642676426,21.8400987989417));
#25080=CARTESIAN_POINT('Ctrl Pts',(8.21899485607472,0.551174068759129,22.0386149163533));
#25081=CARTESIAN_POINT('Ctrl Pts',(6.95932575274402,-2.86288350711349,22.2371310337649));
#25082=CARTESIAN_POINT('Ctrl Pts',(3.40758848840856,-3.65516588504588,22.4356471511766));
#25083=CARTESIAN_POINT('Ctrl Pts',(0.816395477550012,-1.10011867661645,
22.6341632685882));
#25084=CARTESIAN_POINT('Ctrl Pts',(1.55871392857562,2.46239974611297,22.8326793859999));
#25085=CARTESIAN_POINT('Ctrl Pts',(4.95473900642221,3.76989269217354,23.0311955034116));
#25086=CARTESIAN_POINT('Ctrl Pts',(7.89446267408575,1.62500233414576,23.2297116208232));
#25087=CARTESIAN_POINT('Ctrl Pts',(7.68572824288089,-2.00805862937836,23.4282277382349));
#25088=CARTESIAN_POINT('Ctrl Pts',(4.5197169557303,-3.80213094627573,23.6267438556465));
#25089=CARTESIAN_POINT('Ctrl Pts',(1.29575144062437,-2.11437372177854,23.8252599730582));
#25090=CARTESIAN_POINT('Ctrl Pts',(0.966374421579891,1.50985866999905,24.0237760904698));
#25091=CARTESIAN_POINT('Ctrl Pts',(3.83303817896047,3.7510614900228,24.2222922078815));
#25092=CARTESIAN_POINT('Ctrl Pts',(7.27086121968984,2.55774591981802,24.4208083252931));
#25093=CARTESIAN_POINT('Ctrl Pts',(8.13087041382945,-0.979117951521988,
24.6193244427048));
#25094=CARTESIAN_POINT('Ctrl Pts',(5.62679079307294,-3.61699263579137,24.8178405601165));
#25095=CARTESIAN_POINT('Ctrl Pts',(2.04930166016011,-2.94701073564213,25.0163566775281));
#25096=CARTESIAN_POINT('Ctrl Pts',(0.679470245798868,0.430859512276974,
25.2148727949398));
#25097=CARTESIAN_POINT('Ctrl Pts',(2.06768632464525,2.40576215381105,25.3472168732142));
#25098=CARTESIAN_POINT('Ctrl Pts',(3.02612799462649,2.8815178478641,25.4133889123514));
#25099=CARTESIAN_POINT('Origin',(4.45646910621825,5.55111512312578E-15,
25.));
#51536=UNCERTAINTY_MEASURE_WITH_UNIT(LENGTH_MEASURE(0.01),#51554,
'DISTANCE_ACCURACY_VALUE',
'Maximum model space distance between geometric entities at asserted c
onnectivities');
#51543=UNCERTAINTY_MEASURE_WITH_UNIT(LENGTH_MEASURE(0.01),#51554,
'DISTANCE_ACCURACY_VALUE',
'Maximum model space distance between geometric entities at asserted c
onnectivities');
#51546=(
GEOMETRIC_REPRESENTATION_CONTEXT(3)
GLOBAL_UNCERTAINTY_ASSIGNED_CONTEXT((#51536))
GLOBAL_UNIT_ASSIGNED_CONTEXT((#51554,#51556,#51557))
REPRESENTATION_CONTEXT('','3D')
);
#51553=(
GEOMETRIC_REPRESENTATION_CONTEXT(3)
GLOBAL_UNCERTAINTY_ASSIGNED_CONTEXT((#51543))
GLOBAL_UNIT_ASSIGNED_CONTEXT((#51554,#51556,#51557))
REPRESENTATION_CONTEXT('','3D')
);
#51554=(
LENGTH_UNIT()
NAMED_UNIT(*)
SI_UNIT(.MILLI.,.METRE.)
);
#51556=(
NAMED_UNIT(*)
PLANE_ANGLE_UNIT()
SI_UNIT($,.RADIAN.)
);
#51557=(
NAMED_UNIT(*)
SI_UNIT($,.STERADIAN.)
SOLID_ANGLE_UNIT()
);
#51560=SHAPE_DEFINITION_REPRESENTATION(#51569,#51586);
#51569=PRODUCT_DEFINITION_SHAPE('',$,#51596);
#51586=SHAPE_REPRESENTATION('',(#4430),#51546);
#51593=PRODUCT_DEFINITION_CONTEXT('part definition',#51622,'design');
#51596=PRODUCT_DEFINITION('Screw_01','Screw_01',#51605,#51593);
#51605=PRODUCT_DEFINITION_FORMATION('',$,#51626);
#51622=APPLICATION_CONTEXT(
'Core Data for Automotive Mechanical Design Process');
#51623=PRODUCT_CONTEXT('part definition',#51622,'mechanical');
#51626=PRODUCT('Screw_01','Screw_01',$,(#51623));
#51634=PRESENTATION_STYLE_ASSIGNMENT((#51637));
#51637=SURFACE_STYLE_USAGE(.BOTH.,#51640);
#51640=SURFACE_SIDE_STYLE('',(#51643));
#51643=SURFACE_STYLE_FILL_AREA(#51646);
#51646=FILL_AREA_STYLE('Opaque(203,203,203)',(#51649));
#51649=FILL_AREA_STYLE_COLOUR('Opaque(203,203,203)',#51652);
#51652=COLOUR_RGB('Opaque(203,203,203)', 0.09019608, 0.27058824, 0.51372549);
ENDSEC;
END-ISO-10303-21;
